ISO-10303-21;
HEADER;
/* Generated by software containing ST-Developer
 * from STEP Tools, Inc. (www.steptools.com) 
 */

FILE_DESCRIPTION(
/* description */ (''),
/* implementation_level */ '2;1');

FILE_NAME(
/* name */ 'Socket head screw M4x24.step',
/* time_stamp */ '2026-11-15T21:02:08-08:00',
/* author */ (''),
/* organization */ (''),
/* preprocessor_version */ 'ST-DEVELOPER v20.2',
/* originating_system */ 'Autodesk Translation Framework v15.17.0.0',
/* authorisation */ '');

FILE_SCHEMA (('AUTOMOTIVE_DESIGN { 1 0 10303 214 3 1 1 }'));
ENDSEC;

DATA;
#10=MECHANICAL_DESIGN_GEOMETRIC_PRESENTATION_REPRESENTATION('',(#611),#31566);
#139=B_SPLINE_SURFACE_WITH_KNOTS('',3,3,((#26552,#26553,#26554,#26555,#26556,
#26557,#26558,#26559,#26560,#26561,#26562,#26563,#26564,#26565,#26566,#26567,
#26568,#26569,#26570,#26571,#26572,#26573,#26574,#26575,#26576,#26577,#26578,
#26579,#26580,#26581,#26582,#26583,#26584,#26585,#26586,#26587,#26588,#26589,
#26590,#26591,#26592,#26593,#26594,#26595,#26596,#26597,#26598,#26599,#26600,
#26601,#26602,#26603,#26604,#26605,#26606,#26607,#26608,#26609,#26610,#26611,
#26612,#26613,#26614,#26615,#26616,#26617,#26618,#26619,#26620,#26621,#26622,
#26623,#26624,#26625,#26626,#26627,#26628,#26629,#26630,#26631,#26632,#26633,
#26634,#26635,#26636,#26637,#26638,#26639,#26640,#26641,#26642,#26643,#26644,
#26645,#26646,#26647,#26648,#26649,#26650,#26651,#26652,#26653,#26654,#26655,
#26656,#26657,#26658,#26659,#26660,#26661,#26662,#26663,#26664,#26665,#26666,
#26667,#26668,#26669,#26670,#26671,#26672,#26673,#26674,#26675,#26676,#26677,
#26678,#26679,#26680,#26681,#26682,#26683,#26684,#26685,#26686,#26687,#26688,
#26689,#26690,#26691,#26692,#26693,#26694,#26695,#26696,#26697,#26698,#26699,
#26700,#26701,#26702,#26703,#26704,#26705,#26706,#26707,#26708,#26709,#26710,
#26711,#26712,#26713,#26714,#26715,#26716,#26717,#26718,#26719,#26720,#26721,
#26722,#26723,#26724,#26725,#26726,#26727,#26728,#26729,#26730,#26731,#26732,
#26733,#26734,#26735,#26736,#26737,#26738,#26739,#26740,#26741,#26742,#26743,
#26744,#26745,#26746,#26747,#26748,#26749,#26750,#26751,#26752,#26753,#26754,
#26755,#26756,#26757,#26758,#26759,#26760,#26761,#26762,#26763,#26764,#26765,
#26766,#26767,#26768,#26769,#26770,#26771,#26772),(#26773,#26774,#26775,
#26776,#26777,#26778,#26779,#26780,#26781,#26782,#26783,#26784,#26785,#26786,
#26787,#26788,#26789,#26790,#26791,#26792,#26793,#26794,#26795,#26796,#26797,
#26798,#26799,#26800,#26801,#26802,#26803,#26804,#26805,#26806,#26807,#26808,
#26809,#26810,#26811,#26812,#26813,#26814,#26815,#26816,#26817,#26818,#26819,
#26820,#26821,#26822,#26823,#26824,#26825,#26826,#26827,#26828,#26829,#26830,
#26831,#26832,#26833,#26834,#26835,#26836,#26837,#26838,#26839,#26840,#26841,
#26842,#26843,#26844,#26845,#26846,#26847,#26848,#26849,#26850,#26851,#26852,
#26853,#26854,#26855,#26856,#26857,#26858,#26859,#26860,#26861,#26862,#26863,
#26864,#26865,#26866,#26867,#26868,#26869,#26870,#26871,#26872,#26873,#26874,
#26875,#26876,#26877,#26878,#26879,#26880,#26881,#26882,#26883,#26884,#26885,
#26886,#26887,#26888,#26889,#26890,#26891,#26892,#26893,#26894,#26895,#26896,
#26897,#26898,#26899,#26900,#26901,#26902,#26903,#26904,#26905,#26906,#26907,
#26908,#26909,#26910,#26911,#26912,#26913,#26914,#26915,#26916,#26917,#26918,
#26919,#26920,#26921,#26922,#26923,#26924,#26925,#26926,#26927,#26928,#26929,
#26930,#26931,#26932,#26933,#26934,#26935,#26936,#26937,#26938,#26939,#26940,
#26941,#26942,#26943,#26944,#26945,#26946,#26947,#26948,#26949,#26950,#26951,
#26952,#26953,#26954,#26955,#26956,#26957,#26958,#26959,#26960,#26961,#26962,
#26963,#26964,#26965,#26966,#26967,#26968,#26969,#26970,#26971,#26972,#26973,
#26974,#26975,#26976,#26977,#26978,#26979,#26980,#26981,#26982,#26983,#26984,
#26985,#26986,#26987,#26988,#26989,#26990,#26991,#26992,#26993),(#26994,
#26995,#26996,#26997,#26998,#26999,#27000,#27001,#27002,#27003,#27004,#27005,
#27006,#27007,#27008,#27009,#27010,#27011,#27012,#27013,#27014,#27015,#27016,
#27017,#27018,#27019,#27020,#27021,#27022,#27023,#27024,#27025,#27026,#27027,
#27028,#27029,#27030,#27031,#27032,#27033,#27034,#27035,#27036,#27037,#27038,
#27039,#27040,#27041,#27042,#27043,#27044,#27045,#27046,#27047,#27048,#27049,
#27050,#27051,#27052,#27053,#27054,#27055,#27056,#27057,#27058,#27059,#27060,
#27061,#27062,#27063,#27064,#27065,#27066,#27067,#27068,#27069,#27070,#27071,
#27072,#27073,#27074,#27075,#27076,#27077,#27078,#27079,#27080,#27081,#27082,
#27083,#27084,#27085,#27086,#27087,#27088,#27089,#27090,#27091,#27092,#27093,
#27094,#27095,#27096,#27097,#27098,#27099,#27100,#27101,#27102,#27103,#27104,
#27105,#27106,#27107,#27108,#27109,#27110,#27111,#27112,#27113,#27114,#27115,
#27116,#27117,#27118,#27119,#27120,#27121,#27122,#27123,#27124,#27125,#27126,
#27127,#27128,#27129,#27130,#27131,#27132,#27133,#27134,#27135,#27136,#27137,
#27138,#27139,#27140,#27141,#27142,#27143,#27144,#27145,#27146,#27147,#27148,
#27149,#27150,#27151,#27152,#27153,#27154,#27155,#27156,#27157,#27158,#27159,
#27160,#27161,#27162,#27163,#27164,#27165,#27166,#27167,#27168,#27169,#27170,
#27171,#27172,#27173,#27174,#27175,#27176,#27177,#27178,#27179,#27180,#27181,
#27182,#27183,#27184,#27185,#27186,#27187,#27188,#27189,#27190,#27191,#27192,
#27193,#27194,#27195,#27196,#27197,#27198,#27199,#27200,#27201,#27202,#27203,
#27204,#27205,#27206,#27207,#27208,#27209,#27210,#27211,#27212,#27213,#27214),
(#27215,#27216,#27217,#27218,#27219,#27220,#27221,#27222,#27223,#27224,
#27225,#27226,#27227,#27228,#27229,#27230,#27231,#27232,#27233,#27234,#27235,
#27236,#27237,#27238,#27239,#27240,#27241,#27242,#27243,#27244,#27245,#27246,
#27247,#27248,#27249,#27250,#27251,#27252,#27253,#27254,#27255,#27256,#27257,
#27258,#27259,#27260,#27261,#27262,#27263,#27264,#27265,#27266,#27267,#27268,
#27269,#27270,#27271,#27272,#27273,#27274,#27275,#27276,#27277,#27278,#27279,
#27280,#27281,#27282,#27283,#27284,#27285,#27286,#27287,#27288,#27289,#27290,
#27291,#27292,#27293,#27294,#27295,#27296,#27297,#27298,#27299,#27300,#27301,
#27302,#27303,#27304,#27305,#27306,#27307,#27308,#27309,#27310,#27311,#27312,
#27313,#27314,#27315,#27316,#27317,#27318,#27319,#27320,#27321,#27322,#27323,
#27324,#27325,#27326,#27327,#27328,#27329,#27330,#27331,#27332,#27333,#27334,
#27335,#27336,#27337,#27338,#27339,#27340,#27341,#27342,#27343,#27344,#27345,
#27346,#27347,#27348,#27349,#27350,#27351,#27352,#27353,#27354,#27355,#27356,
#27357,#27358,#27359,#27360,#27361,#27362,#27363,#27364,#27365,#27366,#27367,
#27368,#27369,#27370,#27371,#27372,#27373,#27374,#27375,#27376,#27377,#27378,
#27379,#27380,#27381,#27382,#27383,#27384,#27385,#27386,#27387,#27388,#27389,
#27390,#27391,#27392,#27393,#27394,#27395,#27396,#27397,#27398,#27399,#27400,
#27401,#27402,#27403,#27404,#27405,#27406,#27407,#27408,#27409,#27410,#27411,
#27412,#27413,#27414,#27415,#27416,#27417,#27418,#27419,#27420,#27421,#27422,
#27423,#27424,#27425,#27426,#27427,#27428,#27429,#27430,#27431,#27432,#27433,
#27434,#27435)),.UNSPECIFIED.,.F.,.F.,.F.,(4,4),(4,1,1,1,1,1,1,1,1,1,1,
1,1,1,1,1,1,1,1,1,1,1,1,1,1,1,1,1,1,1,1,1,1,1,1,1,1,1,1,1,1,1,1,1,1,1,1,
1,1,1,1,1,1,1,1,1,1,1,1,1,1,1,1,1,1,1,1,1,1,1,1,1,1,1,1,1,1,1,1,1,1,1,1,
1,1,1,1,1,1,1,1,1,1,1,1,1,1,1,1,1,1,1,1,1,1,1,1,1,1,1,1,1,1,1,1,1,1,1,1,
1,1,1,1,1,1,1,1,1,1,1,1,1,1,1,1,1,1,1,1,1,1,1,1,1,1,1,1,1,1,1,1,1,1,1,1,
1,1,1,1,1,1,1,1,1,1,1,1,1,1,1,1,1,1,1,1,1,1,1,1,1,1,1,1,1,1,1,1,1,1,1,1,
1,1,1,1,1,1,1,1,1,1,1,1,1,1,1,1,1,1,1,1,1,1,1,1,1,1,1,4),(-0.000319813591940947,
0.0463078634348368),(8.31044143726206,9.30824121805847,10.305895513377,
11.3035498086955,12.301204104014,13.2988583993325,14.296512694651,15.2941669899695,
16.291821285288,17.2894755806066,18.2871298759251,19.2847841712436,20.2824384665621,
21.2800927618806,22.2777470571991,23.2754013525176,24.2730556478361,25.2707099431546,
26.2683642384732,27.2660185337917,28.2636728291102,29.2613271244287,30.2589814197472,
31.2566357150657,32.2542900103842,33.2519443057027,34.2495986010213,35.2472528963398,
36.2449071916583,37.2425614869768,38.2402157822953,39.2378700776138,40.2355243729323,
41.2331786682508,42.2308329635693,43.2284872588879,44.2261415542064,45.2237958495249,
46.2214501448434,47.2191044401619,48.2167587354804,49.2144130307989,50.2120673261174,
51.209721621436,52.2073759167545,53.205030212073,54.2026845073915,55.20033880271,
56.1979930980285,57.195647393347,58.1933016886655,59.190955983984,60.1886102793026,
61.1862645746211,62.1839188699396,63.1815731652581,64.1792274605766,65.1768817558951,
66.1745360512136,67.1721903465321,68.1698446418506,69.1674989371692,70.1651532324877,
71.1628075278062,72.1604618231247,73.1581161184432,74.1557704137617,75.1534247090802,
76.1510790043987,77.1487332997173,78.1463875950358,79.1440418903543,80.1416961856728,
81.1393504809913,82.1370047763098,83.1346590716283,84.1323133669468,85.1299676622653,
86.1276219575839,87.1252762529024,88.1229305482209,89.1205848435394,90.1182391388579,
91.1158934341764,92.1135477294949,93.1112020248134,94.1088563201319,95.1065106154505,
96.104164910769,97.1018192060875,98.099473501406,99.0971277967245,100.094782092043,
101.092436387362,102.09009068268,103.087744977999,104.085399273317,105.083053568636,
106.080707863954,107.078362159273,108.076016454591,109.07367074991,110.071325045228,
111.068979340547,112.066633635865,113.064287931184,114.061942226502,115.059596521821,
116.057250817139,117.054905112458,118.052559407776,119.050213703095,120.047867998413,
121.045522293732,122.04317658905,123.040830884369,124.038485179687,125.036139475006,
126.033793770324,127.031448065643,128.029102360961,129.02675665628,130.024410951598,
131.022065246917,132.019719542235,133.017373837554,134.015028132872,135.012682428191,
136.010336723509,137.007991018828,138.005645314146,139.003299609465,140.000953904783,
140.998608200102,141.99626249542,142.993916790739,143.991571086058,144.989225381376,
145.986879676695,146.984533972013,147.982188267332,148.97984256265,149.977496857969,
150.975151153287,151.972805448606,152.970459743924,153.968114039243,154.965768334561,
155.96342262988,156.961076925198,157.958731220517,158.956385515835,159.954039811154,
160.951694106472,161.949348401791,162.947002697109,163.944656992428,164.942311287746,
165.939965583065,166.937619878383,167.935274173702,168.93292846902,169.930582764339,
170.928237059657,171.925891354976,172.923545650294,173.921199945613,174.918854240931,
175.91650853625,176.914162831568,177.911817126887,178.909471422205,179.907125717524,
180.904780012842,181.902434308161,182.900088603479,183.897742898798,184.895397194116,
185.893051489435,186.890705784754,187.888360080072,188.886014375391,189.883668670709,
190.881322966028,191.878977261346,192.876631556665,193.874285851983,194.871940147302,
195.86959444262,196.867248737939,197.864903033257,198.862557328576,199.860211623894,
200.857865919213,201.855520214531,202.85317450985,203.850828805168,204.848483100487,
205.846137395805,206.843791691124,207.841445986442,208.839100281761,209.836754577079,
210.834408872398,211.832063167716,212.829717463035,213.827371758353,214.825026053672,
215.82268034899,216.820334644309,217.817988939627,218.815643234946,219.813297530264,
220.810951825583,221.808606120901,222.80626041622,223.803914711538,224.801569006857,
225.799543115767),.UNSPECIFIED.);
#140=B_SPLINE_SURFACE_WITH_KNOTS('',3,3,((#27548,#27549,#27550,#27551,#27552,
#27553,#27554,#27555,#27556,#27557,#27558,#27559,#27560,#27561,#27562,#27563,
#27564,#27565,#27566,#27567,#27568,#27569,#27570,#27571,#27572,#27573,#27574,
#27575,#27576,#27577,#27578,#27579,#27580,#27581,#27582,#27583,#27584,#27585,
#27586,#27587,#27588,#27589,#27590,#27591,#27592,#27593,#27594,#27595,#27596,
#27597,#27598,#27599,#27600,#27601,#27602,#27603,#27604,#27605,#27606,#27607,
#27608,#27609,#27610,#27611,#27612,#27613,#27614,#27615,#27616,#27617,#27618,
#27619,#27620,#27621,#27622,#27623,#27624,#27625,#27626,#27627,#27628,#27629,
#27630,#27631,#27632,#27633,#27634,#27635,#27636,#27637,#27638,#27639,#27640,
#27641,#27642,#27643,#27644,#27645,#27646,#27647,#27648,#27649,#27650,#27651,
#27652,#27653,#27654,#27655,#27656,#27657,#27658,#27659,#27660,#27661,#27662,
#27663,#27664,#27665,#27666,#27667,#27668,#27669,#27670,#27671,#27672,#27673,
#27674,#27675,#27676,#27677,#27678,#27679,#27680,#27681,#27682,#27683,#27684,
#27685,#27686,#27687,#27688,#27689,#27690,#27691,#27692,#27693,#27694,#27695,
#27696,#27697,#27698,#27699,#27700,#27701,#27702,#27703,#27704,#27705,#27706,
#27707,#27708,#27709,#27710,#27711,#27712,#27713,#27714,#27715,#27716,#27717,
#27718,#27719,#27720,#27721,#27722,#27723,#27724,#27725,#27726,#27727,#27728,
#27729,#27730,#27731,#27732,#27733,#27734,#27735,#27736,#27737,#27738,#27739,
#27740,#27741,#27742,#27743,#27744,#27745,#27746,#27747,#27748,#27749,#27750,
#27751,#27752,#27753,#27754,#27755,#27756,#27757,#27758,#27759,#27760,#27761,
#27762,#27763,#27764,#27765,#27766,#27767,#27768),(#27769,#27770,#27771,
#27772,#27773,#27774,#27775,#27776,#27777,#27778,#27779,#27780,#27781,#27782,
#27783,#27784,#27785,#27786,#27787,#27788,#27789,#27790,#27791,#27792,#27793,
#27794,#27795,#27796,#27797,#27798,#27799,#27800,#27801,#27802,#27803,#27804,
#27805,#27806,#27807,#27808,#27809,#27810,#27811,#27812,#27813,#27814,#27815,
#27816,#27817,#27818,#27819,#27820,#27821,#27822,#27823,#27824,#27825,#27826,
#27827,#27828,#27829,#27830,#27831,#27832,#27833,#27834,#27835,#27836,#27837,
#27838,#27839,#27840,#27841,#27842,#27843,#27844,#27845,#27846,#27847,#27848,
#27849,#27850,#27851,#27852,#27853,#27854,#27855,#27856,#27857,#27858,#27859,
#27860,#27861,#27862,#27863,#27864,#27865,#27866,#27867,#27868,#27869,#27870,
#27871,#27872,#27873,#27874,#27875,#27876,#27877,#27878,#27879,#27880,#27881,
#27882,#27883,#27884,#27885,#27886,#27887,#27888,#27889,#27890,#27891,#27892,
#27893,#27894,#27895,#27896,#27897,#27898,#27899,#27900,#27901,#27902,#27903,
#27904,#27905,#27906,#27907,#27908,#27909,#27910,#27911,#27912,#27913,#27914,
#27915,#27916,#27917,#27918,#27919,#27920,#27921,#27922,#27923,#27924,#27925,
#27926,#27927,#27928,#27929,#27930,#27931,#27932,#27933,#27934,#27935,#27936,
#27937,#27938,#27939,#27940,#27941,#27942,#27943,#27944,#27945,#27946,#27947,
#27948,#27949,#27950,#27951,#27952,#27953,#27954,#27955,#27956,#27957,#27958,
#27959,#27960,#27961,#27962,#27963,#27964,#27965,#27966,#27967,#27968,#27969,
#27970,#27971,#27972,#27973,#27974,#27975,#27976,#27977,#27978,#27979,#27980,
#27981,#27982,#27983,#27984,#27985,#27986,#27987,#27988,#27989),(#27990,
#27991,#27992,#27993,#27994,#27995,#27996,#27997,#27998,#27999,#28000,#28001,
#28002,#28003,#28004,#28005,#28006,#28007,#28008,#28009,#28010,#28011,#28012,
#28013,#28014,#28015,#28016,#28017,#28018,#28019,#28020,#28021,#28022,#28023,
#28024,#28025,#28026,#28027,#28028,#28029,#28030,#28031,#28032,#28033,#28034,
#28035,#28036,#28037,#28038,#28039,#28040,#28041,#28042,#28043,#28044,#28045,
#28046,#28047,#28048,#28049,#28050,#28051,#28052,#28053,#28054,#28055,#28056,
#28057,#28058,#28059,#28060,#28061,#28062,#28063,#28064,#28065,#28066,#28067,
#28068,#28069,#28070,#28071,#28072,#28073,#28074,#28075,#28076,#28077,#28078,
#28079,#28080,#28081,#28082,#28083,#28084,#28085,#28086,#28087,#28088,#28089,
#28090,#28091,#28092,#28093,#28094,#28095,#28096,#28097,#28098,#28099,#28100,
#28101,#28102,#28103,#28104,#28105,#28106,#28107,#28108,#28109,#28110,#28111,
#28112,#28113,#28114,#28115,#28116,#28117,#28118,#28119,#28120,#28121,#28122,
#28123,#28124,#28125,#28126,#28127,#28128,#28129,#28130,#28131,#28132,#28133,
#28134,#28135,#28136,#28137,#28138,#28139,#28140,#28141,#28142,#28143,#28144,
#28145,#28146,#28147,#28148,#28149,#28150,#28151,#28152,#28153,#28154,#28155,
#28156,#28157,#28158,#28159,#28160,#28161,#28162,#28163,#28164,#28165,#28166,
#28167,#28168,#28169,#28170,#28171,#28172,#28173,#28174,#28175,#28176,#28177,
#28178,#28179,#28180,#28181,#28182,#28183,#28184,#28185,#28186,#28187,#28188,
#28189,#28190,#28191,#28192,#28193,#28194,#28195,#28196,#28197,#28198,#28199,
#28200,#28201,#28202,#28203,#28204,#28205,#28206,#28207,#28208,#28209,#28210),
(#28211,#28212,#28213,#28214,#28215,#28216,#28217,#28218,#28219,#28220,
#28221,#28222,#28223,#28224,#28225,#28226,#28227,#28228,#28229,#28230,#28231,
#28232,#28233,#28234,#28235,#28236,#28237,#28238,#28239,#28240,#28241,#28242,
#28243,#28244,#28245,#28246,#28247,#28248,#28249,#28250,#28251,#28252,#28253,
#28254,#28255,#28256,#28257,#28258,#28259,#28260,#28261,#28262,#28263,#28264,
#28265,#28266,#28267,#28268,#28269,#28270,#28271,#28272,#28273,#28274,#28275,
#28276,#28277,#28278,#28279,#28280,#28281,#28282,#28283,#28284,#28285,#28286,
#28287,#28288,#28289,#28290,#28291,#28292,#28293,#28294,#28295,#28296,#28297,
#28298,#28299,#28300,#28301,#28302,#28303,#28304,#28305,#28306,#28307,#28308,
#28309,#28310,#28311,#28312,#28313,#28314,#28315,#28316,#28317,#28318,#28319,
#28320,#28321,#28322,#28323,#28324,#28325,#28326,#28327,#28328,#28329,#28330,
#28331,#28332,#28333,#28334,#28335,#28336,#28337,#28338,#28339,#28340,#28341,
#28342,#28343,#28344,#28345,#28346,#28347,#28348,#28349,#28350,#28351,#28352,
#28353,#28354,#28355,#28356,#28357,#28358,#28359,#28360,#28361,#28362,#28363,
#28364,#28365,#28366,#28367,#28368,#28369,#28370,#28371,#28372,#28373,#28374,
#28375,#28376,#28377,#28378,#28379,#28380,#28381,#28382,#28383,#28384,#28385,
#28386,#28387,#28388,#28389,#28390,#28391,#28392,#28393,#28394,#28395,#28396,
#28397,#28398,#28399,#28400,#28401,#28402,#28403,#28404,#28405,#28406,#28407,
#28408,#28409,#28410,#28411,#28412,#28413,#28414,#28415,#28416,#28417,#28418,
#28419,#28420,#28421,#28422,#28423,#28424,#28425,#28426,#28427,#28428,#28429,
#28430,#28431)),.UNSPECIFIED.,.F.,.F.,.F.,(4,4),(4,1,1,1,1,1,1,1,1,1,1,
1,1,1,1,1,1,1,1,1,1,1,1,1,1,1,1,1,1,1,1,1,1,1,1,1,1,1,1,1,1,1,1,1,1,1,1,
1,1,1,1,1,1,1,1,1,1,1,1,1,1,1,1,1,1,1,1,1,1,1,1,1,1,1,1,1,1,1,1,1,1,1,1,
1,1,1,1,1,1,1,1,1,1,1,1,1,1,1,1,1,1,1,1,1,1,1,1,1,1,1,1,1,1,1,1,1,1,1,1,
1,1,1,1,1,1,1,1,1,1,1,1,1,1,1,1,1,1,1,1,1,1,1,1,1,1,1,1,1,1,1,1,1,1,1,1,
1,1,1,1,1,1,1,1,1,1,1,1,1,1,1,1,1,1,1,1,1,1,1,1,1,1,1,1,1,1,1,1,1,1,1,1,
1,1,1,1,1,1,1,1,1,1,1,1,1,1,1,1,1,1,1,1,1,1,1,1,1,1,1,4),(-0.000277866170942688,
0.0463346228827458),(11.6151017126826,12.6130758144294,13.6107301097479,
14.6083844050664,15.6060387003849,16.6036929957034,17.601347291022,18.5990015863405,
19.596655881659,20.5943101769775,21.591964472296,22.5896187676145,23.587273062933,
24.5849273582515,25.58258165357,26.5802359488886,27.5778902442071,28.5755445395256,
29.5731988348441,30.5708531301626,31.5685074254811,32.5661617207996,33.5638160161181,
34.5614703114366,35.5591246067551,36.5567789020737,37.5544331973922,38.5520874927107,
39.5497417880292,40.5473960833477,41.5450503786662,42.5427046739847,43.5403589693032,
44.5380132646217,45.5356675599403,46.5333218552588,47.5309761505773,48.5286304458958,
49.5262847412143,50.5239390365328,51.5215933318513,52.5192476271698,53.5169019224883,
54.5145562178069,55.5122105131254,56.5098648084439,57.5075191037624,58.5051733990809,
59.5028276943994,60.5004819897179,61.4981362850364,62.4957905803549,63.4934448756734,
64.491099170992,65.4887534663105,66.486407761629,67.4840620569475,68.481716352266,
69.4793706475845,70.477024942903,71.4746792382215,72.4723335335401,73.4699878288586,
74.4676421241771,75.4652964194956,76.4629507148141,77.4606050101326,78.4582593054511,
79.4559136007696,80.4535678960881,81.4512221914066,82.4488764867252,83.4465307820437,
84.4441850773622,85.4418393726807,86.4394936679992,87.4371479633177,88.4348022586362,
89.4324565539547,90.4301108492732,91.4277651445918,92.4254194399103,93.4230737352288,
94.4207280305473,95.4183823258658,96.4160366211843,97.4136909165028,98.4113452118213,
99.4089995071398,100.406653802458,101.404308097777,102.401962393095,103.399616688414,
104.397270983732,105.394925279051,106.392579574369,107.390233869688,108.387888165006,
109.385542460325,110.383196755643,111.380851050962,112.37850534628,113.376159641599,
114.373813936918,115.371468232236,116.369122527555,117.366776822873,118.364431118192,
119.36208541351,120.359739708829,121.357394004147,122.355048299466,123.352702594784,
124.350356890103,125.348011185421,126.34566548074,127.343319776058,128.340974071377,
129.338628366695,130.336282662014,131.333936957332,132.331591252651,133.329245547969,
134.326899843288,135.324554138606,136.322208433925,137.319862729243,138.317517024562,
139.31517131988,140.312825615199,141.310479910517,142.308134205836,143.305788501154,
144.303442796473,145.301097091791,146.29875138711,147.296405682428,148.294059977747,
149.291714273065,150.289368568384,151.287022863702,152.284677159021,153.282331454339,
154.279985749658,155.277640044976,156.275294340295,157.272948635613,158.270602930932,
159.268257226251,160.265911521569,161.263565816888,162.261220112206,163.258874407525,
164.256528702843,165.254182998162,166.25183729348,167.249491588799,168.247145884117,
169.244800179436,170.242454474754,171.240108770073,172.237763065391,173.23541736071,
174.233071656028,175.230725951347,176.228380246665,177.226034541984,178.223688837302,
179.221343132621,180.218997427939,181.216651723258,182.214306018576,183.211960313895,
184.209614609213,185.207268904532,186.20492319985,187.202577495169,188.200231790487,
189.197886085806,190.195540381124,191.193194676443,192.190848971761,193.18850326708,
194.186157562398,195.183811857717,196.181466153035,197.179120448354,198.176774743672,
199.174429038991,200.172083334309,201.169737629628,202.167391924946,203.165046220265,
204.162700515584,205.160354810902,206.158009106221,207.155663401539,208.153317696858,
209.150971992176,210.148626287495,211.146280582813,212.143934878132,213.14158917345,
214.139243468769,215.136897764087,216.134552059406,217.132206354724,218.129860650043,
219.127514945361,220.12516924068,221.122823535998,222.120477831317,223.118132126635,
224.115786421954,225.113440717272,226.111095012591,227.108749307909,228.106403603228,
229.104057898546),.UNSPECIFIED.);
#143=B_SPLINE_CURVE_WITH_KNOTS('',3,(#8253,#8254,#8255,#8256,#8257,#8258,
#8259,#8260,#8261,#8262,#8263,#8264,#8265,#8266,#8267,#8268,#8269,#8270,
#8271,#8272,#8273,#8274,#8275,#8276,#8277,#8278,#8279,#8280,#8281,#8282,
#8283,#8284,#8285,#8286,#8287,#8288,#8289,#8290,#8291,#8292,#8293,#8294,
#8295,#8296,#8297,#8298,#8299,#8300,#8301,#8302,#8303,#8304,#8305,#8306,
#8307,#8308,#8309,#8310,#8311,#8312,#8313,#8314,#8315,#8316,#8317,#8318,
#8319,#8320,#8321,#8322,#8323,#8324,#8325,#8326,#8327,#8328,#8329,#8330,
#8331,#8332,#8333,#8334,#8335,#8336,#8337,#8338,#8339,#8340,#8341,#8342,
#8343,#8344,#8345,#8346,#8347,#8348,#8349,#8350,#8351,#8352,#8353,#8354,
#8355,#8356,#8357,#8358,#8359,#8360,#8361,#8362,#8363,#8364,#8365,#8366,
#8367,#8368,#8369,#8370,#8371,#8372,#8373,#8374,#8375,#8376,#8377,#8378,
#8379,#8380,#8381,#8382,#8383,#8384,#8385,#8386,#8387,#8388,#8389,#8390,
#8391,#8392,#8393,#8394,#8395,#8396,#8397,#8398,#8399,#8400,#8401,#8402,
#8403,#8404,#8405,#8406,#8407,#8408,#8409,#8410,#8411,#8412,#8413,#8414,
#8415,#8416,#8417,#8418,#8419,#8420,#8421,#8422,#8423,#8424,#8425,#8426,
#8427,#8428,#8429,#8430,#8431,#8432),.UNSPECIFIED.,.F.,.F.,(4,2,2,2,2,2,
2,2,2,2,2,2,2,2,2,2,2,2,2,2,2,2,2,2,2,2,2,2,2,2,2,2,2,2,2,2,2,2,2,2,2,2,
2,2,2,2,2,2,2,2,2,2,2,2,2,2,2,2,2,2,2,2,2,2,2,2,2,2,2,2,2,2,2,2,2,2,2,2,
2,2,2,2,2,2,2,2,2,2,2,4),(-0.653335368055541,-0.630827744391981,-0.626780791882163,
-0.615626822227101,-0.613746386507816,-0.612773986726421,-0.611996972682137,
-0.611081108109938,-0.609417169194799,-0.600987942963921,-0.556733574729332,
-0.540402511494848,-0.537539421553271,-0.535750932317557,-0.534355220875731,
-0.532810773622695,-0.530272110915929,-0.521046244569413,-0.477579256047151,
-0.460385567031773,-0.458303841262293,-0.457304148793678,-0.456528658473224,
-0.455645529724309,-0.454098108893724,-0.447294147774132,-0.405054436843288,
-0.384578213990074,-0.38157676784101,-0.379775756134279,-0.378385853015247,
-0.376886876698328,-0.374508645759818,-0.366710711675292,-0.353961386986977,
-0.318721581419464,-0.304334472491172,-0.302369786948392,-0.301393524301113,
-0.300636770619692,-0.300635149391518,-0.300633934570592,-0.299773777137359,
-0.298296239677128,-0.292512595872408,-0.281693807009336,-0.260197418545613,
-0.228783310911029,-0.225338003047899,-0.223573337585265,-0.222177359960143,
-0.220612973393571,-0.21799528402457,-0.207930804816358,-0.162219818185453,
-0.148527226542504,-0.146557350854722,-0.145569231240051,-0.144791085512274,
-0.144786680978626,-0.144782342094403,-0.144778067499853,-0.144773855871636,
-0.14476970593007,-0.144765616428515,-0.144761586142939,-0.144757613893166,
-0.144753698522794,-0.144749838896611,-0.144746033926486,-0.144742282547943,
-0.144738583717294,-0.144734936410761,-0.14473133964255,-0.144727792454873,
-0.144724293904568,-0.144720843073948,-0.144717439062714,-0.143799095744793,
-0.142128551391516,-0.134081724732716,-0.0862253127166185,-0.074309960962854,
-0.0714277983940767,-0.0697756867164645,-0.0685093800882442,-0.0668722738521374,
-0.0639797476153101,-0.0504343015806197,-0.00237550598267959),
 .UNSPECIFIED.);
#144=B_SPLINE_CURVE_WITH_KNOTS('',3,(#8435,#8436,#8437,#8438,#8439,#8440,
#8441,#8442,#8443,#8444,#8445,#8446,#8447,#8448,#8449,#8450,#8451,#8452,
#8453,#8454,#8455,#8456,#8457,#8458,#8459,#8460,#8461,#8462,#8463,#8464,
#8465,#8466,#8467,#8468,#8469,#8470,#8471,#8472,#8473,#8474,#8475,#8476,
#8477,#8478,#8479,#8480),.UNSPECIFIED.,.F.,.F.,(4,3,3,3,3,3,3,3,3,3,3,3,
3,3,3,4),(11.6154215191109,11.8187185627336,12.0221213811096,12.225521337906,
12.4295729519081,12.6130758144294,12.8095574916101,13.0098506461445,13.2057833991446,
13.4082567544463,13.6107301097479,13.8095830942474,14.0081354944698,14.2064856860045,
14.405222870008,14.5586904309875),.UNSPECIFIED.);
#145=B_SPLINE_CURVE_WITH_KNOTS('',3,(#8485,#8486,#8487,#8488,#8489,#8490,
#8491,#8492,#8493,#8494,#8495,#8496,#8497,#8498,#8499,#8500,#8501,#8502,
#8503,#8504,#8505,#8506,#8507,#8508,#8509,#8510,#8511,#8512,#8513,#8514,
#8515,#8516,#8517,#8518,#8519,#8520,#8521,#8522,#8523,#8524,#8525,#8526,
#8527,#8528,#8529,#8530,#8531,#8532,#8533,#8534,#8535,#8536,#8537,#8538,
#8539,#8540,#8541,#8542,#8543,#8544,#8545,#8546,#8547,#8548,#8549,#8550,
#8551,#8552,#8553,#8554,#8555,#8556,#8557,#8558,#8559,#8560,#8561,#8562,
#8563,#8564,#8565,#8566,#8567,#8568,#8569,#8570,#8571,#8572,#8573,#8574,
#8575,#8576,#8577,#8578,#8579,#8580,#8581,#8582,#8583,#8584,#8585,#8586,
#8587,#8588,#8589,#8590,#8591,#8592,#8593,#8594,#8595,#8596,#8597,#8598,
#8599,#8600,#8601,#8602,#8603,#8604,#8605,#8606,#8607,#8608,#8609,#8610,
#8611,#8612,#8613,#8614,#8615,#8616,#8617,#8618,#8619,#8620,#8621,#8622,
#8623,#8624,#8625,#8626,#8627,#8628,#8629,#8630,#8631,#8632,#8633,#8634,
#8635,#8636,#8637,#8638,#8639,#8640,#8641,#8642,#8643,#8644,#8645,#8646,
#8647,#8648,#8649,#8650,#8651,#8652,#8653,#8654,#8655,#8656,#8657,#8658,
#8659,#8660,#8661,#8662,#8663,#8664,#8665,#8666,#8667,#8668,#8669,#8670,
#8671,#8672,#8673,#8674,#8675,#8676,#8677,#8678,#8679,#8680,#8681,#8682,
#8683,#8684,#8685,#8686,#8687,#8688,#8689,#8690,#8691,#8692,#8693,#8694,
#8695,#8696,#8697,#8698,#8699,#8700,#8701,#8702,#8703,#8704,#8705,#8706,
#8707,#8708,#8709,#8710,#8711,#8712),.UNSPECIFIED.,.F.,.F.,(4,2,2,2,2,2,
2,2,2,2,2,2,2,2,2,2,2,2,2,2,2,2,2,2,2,2,2,2,2,2,2,2,2,2,2,2,2,2,2,2,2,2,
2,2,2,2,2,2,2,2,2,2,2,2,2,2,2,2,2,2,2,2,2,2,2,2,2,2,2,2,2,2,2,2,2,2,2,2,
2,2,2,2,2,2,2,2,2,2,2,2,2,2,2,2,2,2,2,2,2,2,2,2,2,2,2,2,2,2,2,2,2,2,2,4),
(-1.6336654916901,-1.62824277434945,-1.62601171074565,-1.624708877687,-1.6233247278785,
-1.62161410474044,-1.61899596189488,-1.60680221938704,-1.6011802590482,
-1.55684017909535,-1.54916111619138,-1.54753892156619,-1.54663489729833,
-1.54585978304054,-1.54487991998877,-1.54289633121139,-1.5296339235447,
-1.48520136692885,-1.47340055857452,-1.47065690995958,-1.46907012892602,
-1.46768598011242,-1.46597775714764,-1.4633677530548,-1.45129750604337,
-1.44556096533492,-1.40129806456246,-1.39350831030722,-1.39188716495599,
-1.39098333430837,-1.39020826958534,-1.38922827148699,-1.38724344208687,
-1.37393644792458,-1.32949096921034,-1.31773095829262,-1.31499049362004,
-1.31340456923182,-1.31202058445466,-1.31031181617812,-1.30769959177109,
-1.29559297003898,-1.28989305877005,-1.24565483681943,-1.23784311635413,
-1.23622076067487,-1.23531673125631,-1.23454168558734,-1.23356200900558,
-1.23157908814874,-1.21833509092066,-1.17402336377544,-1.16207355744685,
-1.15931923840855,-1.15773004421791,-1.15634601748633,-1.15464080147506,
-1.15204069030614,-1.14011669802976,-1.13425294786415,-1.09002010954997,
-1.08216922476865,-1.08054405662702,-1.07963919938582,-1.07886366008202,
-1.07788370259289,-1.0759018980825,-1.06272293592201,-1.01822887514452,
-1.00642636019806,-1.00368159793581,-1.00209402781417,-1.00070909950449,
-0.998999792590983,-0.996387898992575,-0.984303707478293,-0.978562335419278,
-0.934265673249539,-0.926505505245042,-0.924885861743567,-0.923982208703502,
-0.923207402451168,-0.922227683627303,-0.920241865211176,-0.906873961270504,
-0.88411589228476,-0.851960939902135,-0.848540506939741,-0.846787635027711,
-0.845400566840057,-0.843845769683438,-0.841243335623051,-0.83123413446508,
-0.786213312405221,-0.783501460588735,-0.78068872680155,-0.771150793859352,
-0.769512412813916,-0.768516529635411,-0.767738571407755,-0.766856690726504,
-0.765335358356058,-0.758997735852844,-0.74658534600533,-0.715079298221367,
-0.706091953952895,-0.695113383326078,-0.692334032603312,-0.690722102582697,
-0.689338476098884,-0.687659041120033,-0.684489667747269,-0.663993301109061,
-0.653335368055541),.UNSPECIFIED.);
#146=B_SPLINE_CURVE_WITH_KNOTS('',3,(#8714,#8715,#8716,#8717,#8718,#8719,
#8720,#8721,#8722,#8723,#8724,#8725,#8726,#8727,#8728,#8729,#8730,#8731,
#8732,#8733,#8734,#8735),.UNSPECIFIED.,.F.,.F.,(4,3,3,3,3,3,3,4),(14.5586904309875,
14.6083844050664,14.8072779846533,15.0069681635862,15.205429275443,15.4057339879139,
15.6060387003849,15.7079632679491),.UNSPECIFIED.);
#147=B_SPLINE_CURVE_WITH_KNOTS('',3,(#8736,#8737,#8738,#8739,#8740,#8741,
#8742,#8743,#8744,#8745,#8746,#8747,#8748,#8749,#8750,#8751,#8752,#8753,
#8754,#8755,#8756,#8757,#8758,#8759,#8760,#8761,#8762,#8763,#8764,#8765,
#8766,#8767,#8768,#8769,#8770,#8771,#8772,#8773,#8774,#8775,#8776,#8777,
#8778,#8779,#8780,#8781,#8782,#8783,#8784,#8785,#8786,#8787,#8788,#8789,
#8790,#8791,#8792,#8793,#8794,#8795,#8796,#8797,#8798,#8799,#8800,#8801,
#8802,#8803,#8804,#8805,#8806,#8807,#8808,#8809,#8810,#8811,#8812,#8813,
#8814,#8815,#8816,#8817,#8818,#8819,#8820,#8821,#8822,#8823,#8824,#8825,
#8826,#8827,#8828,#8829,#8830,#8831,#8832,#8833,#8834,#8835,#8836,#8837,
#8838,#8839,#8840,#8841,#8842,#8843,#8844,#8845,#8846,#8847,#8848,#8849,
#8850,#8851,#8852,#8853,#8854,#8855,#8856,#8857,#8858,#8859,#8860,#8861,
#8862,#8863,#8864,#8865,#8866,#8867,#8868,#8869,#8870,#8871,#8872,#8873,
#8874,#8875,#8876,#8877,#8878,#8879,#8880,#8881,#8882,#8883,#8884,#8885,
#8886,#8887,#8888,#8889,#8890,#8891,#8892,#8893,#8894,#8895,#8896,#8897,
#8898,#8899,#8900,#8901,#8902,#8903,#8904,#8905,#8906,#8907,#8908,#8909,
#8910,#8911,#8912,#8913,#8914,#8915,#8916,#8917,#8918,#8919,#8920,#8921,
#8922,#8923,#8924,#8925),.UNSPECIFIED.,.F.,.F.,(4,2,2,2,2,2,2,2,2,2,2,2,
2,2,2,2,2,2,2,2,2,2,2,2,2,2,2,2,2,2,2,2,2,2,2,2,2,2,2,2,2,2,2,2,2,2,2,2,
2,2,2,2,2,2,2,2,2,2,2,2,2,2,2,2,2,2,2,2,2,2,2,2,2,2,2,2,2,2,2,2,2,2,2,2,
2,2,2,2,2,2,2,2,2,2,4),(-1.96156625886934,-1.92659860641184,-1.90732716118048,
-1.90286421065159,-1.90094647127445,-1.89954351095447,-1.8982517845789,
-1.8961662975017,-1.8910505695977,-1.85295586623046,-1.83677685872955,-1.82869766194432,
-1.82556091643153,-1.82328055334917,-1.82224677965939,-1.82150705897721,
-1.82076683087637,-1.81951432342556,-1.81614474862376,-1.77737520988576,
-1.75101524588943,-1.74680273494602,-1.74491784438801,-1.74350935177083,
-1.74219119292114,-1.74001398644813,-1.73441877740491,-1.72902251786991,
-1.68185009784626,-1.67344964171479,-1.67021757871639,-1.66857723309331,
-1.66755432831436,-1.66661569045782,-1.66586016418002,-1.66494256104391,
-1.66330661834126,-1.65625786254823,-1.65112631001996,-1.61401639950501,
-1.60075283621853,-1.59271817070388,-1.59030364055039,-1.58878965239272,
-1.58739112773879,-1.58558629130853,-1.58259410755891,-1.56301235661922,
-1.52015182014857,-1.51327333271664,-1.51171272841562,-1.51082253653344,
-1.51004662635945,-1.50904904701185,-1.50697192224075,-1.48075539495684,
-1.45662573109801,-1.44446585919773,-1.43692019679761,-1.43456166917119,
-1.43306137571554,-1.4316606324867,-1.42983175833002,-1.42675298709056,
-1.42001711839465,-1.41770846204196,-1.41716875646762,-1.41696492803138,
-1.40795048521513,-1.36463969373078,-1.35764500565798,-1.35607705176135,
-1.35518563671651,-1.35440955895738,-1.35341355539906,-1.35134824301463,
-1.32434638940583,-1.2954124703417,-1.28216332848089,-1.27932300317243,
-1.27771471567474,-1.27647054573972,-1.27484724908334,-1.2720161087679,
-1.26038097227321,-1.25422245589898,-1.20985943944406,-1.20211370256844,
-1.20049457541361,-1.1995908433108,-1.19881539007934,-1.19783419533342,
-1.19584416643524,-1.18238927459852,-1.16059938204844),.UNSPECIFIED.);
#148=B_SPLINE_CURVE_WITH_KNOTS('',3,(#8931,#8932,#8933,#8934,#8935,#8936,
#8937,#8938,#8939,#8940,#8941,#8942,#8943,#8944,#8945,#8946,#8947,#8948,
#8949,#8950,#8951,#8952,#8953,#8954,#8955,#8956,#8957,#8958,#8959,#8960,
#8961,#8962,#8963,#8964,#8965,#8966,#8967,#8968,#8969,#8970,#8971,#8972,
#8973,#8974,#8975,#8976,#8977,#8978,#8979,#8980,#8981,#8982,#8983,#8984,
#8985,#8986,#8987,#8988,#8989,#8990,#8991,#8992,#8993,#8994,#8995,#8996,
#8997,#8998,#8999,#9000,#9001,#9002,#9003,#9004,#9005,#9006,#9007,#9008,
#9009,#9010,#9011,#9012,#9013,#9014,#9015,#9016,#9017,#9018,#9019,#9020,
#9021,#9022,#9023,#9024,#9025,#9026,#9027,#9028,#9029,#9030,#9031,#9032,
#9033,#9034,#9035,#9036,#9037,#9038,#9039,#9040,#9041,#9042,#9043,#9044,
#9045,#9046,#9047,#9048,#9049,#9050,#9051,#9052,#9053,#9054,#9055,#9056,
#9057,#9058,#9059,#9060,#9061,#9062,#9063,#9064,#9065,#9066,#9067,#9068,
#9069,#9070,#9071,#9072,#9073,#9074,#9075,#9076,#9077,#9078,#9079,#9080,
#9081,#9082,#9083,#9084,#9085,#9086,#9087,#9088,#9089,#9090,#9091,#9092,
#9093,#9094,#9095,#9096,#9097,#9098,#9099,#9100,#9101,#9102,#9103,#9104,
#9105,#9106,#9107,#9108,#9109,#9110,#9111,#9112,#9113,#9114,#9115,#9116,
#9117,#9118,#9119,#9120,#9121,#9122,#9123,#9124,#9125,#9126,#9127,#9128,
#9129,#9130,#9131,#9132,#9133,#9134),.UNSPECIFIED.,.F.,.F.,(4,2,2,2,2,2,
2,2,2,2,2,2,2,2,2,2,2,2,2,2,2,2,2,2,2,2,2,2,2,2,2,2,2,2,2,2,2,2,2,2,2,2,
2,2,2,2,2,2,2,2,2,2,2,2,2,2,2,2,2,2,2,2,2,2,2,2,2,2,2,2,2,2,2,2,2,2,2,2,
2,2,2,2,2,2,2,2,2,2,2,2,2,2,2,2,2,2,2,2,2,2,2,4),(-0.801408127637272,-0.771904677294534,
-0.751442090154587,-0.748428518202366,-0.746617300878863,-0.745217680836779,
-0.743706329861739,-0.741304237752424,-0.733386602621748,-0.720392548290882,
-0.683066689877591,-0.680645798525123,-0.670881406783786,-0.669230887192859,
-0.668231001131795,-0.667452194474505,-0.666572096085563,-0.665059079143899,
-0.658829139984269,-0.646731802189187,-0.615311961864202,-0.595784809569082,
-0.592794302056391,-0.590989806409757,-0.589591149222151,-0.58807662181382,
-0.585660378563243,-0.577612350772039,-0.564318967812487,-0.527090627162658,
-0.515410864829396,-0.513511092530095,-0.512535428626712,-0.511760485328853,
-0.510853003212082,-0.509215519425141,-0.501155740811697,-0.457121788570278,
-0.451061783489783,-0.439352749456757,-0.436515784737386,-0.434891280240044,
-0.433647313499648,-0.432040620565844,-0.429207006864917,-0.416062417170359,
-0.387544125155396,-0.359970542496619,-0.357913715509054,-0.356919247295317,
-0.356142821151476,-0.355248846198673,-0.353672974964434,-0.346585723927676,
-0.302824429737408,-0.295737905645828,-0.283746050595315,-0.281141179661321,
-0.279434418599533,-0.278050198859604,-0.278046556306593,-0.278042933535727,
-0.278039330860513,-0.278035748120137,-0.278032185143909,-0.278028641790449,
-0.278025117901929,-0.27802161331344,-0.276454418593738,-0.27378638452301,
-0.270528827498608,-0.263883193018837,-0.218608880745754,-0.215607053633344,
-0.204047426930947,-0.202152034702858,-0.201177175042177,-0.200402106203344,
-0.199493588868725,-0.197852007844497,-0.189841277995573,-0.17179962766557,
-0.143562182184153,-0.142818928501005,-0.128370978435724,-0.125607678451565,
-0.123851801111013,-0.122462799847458,-0.121163245944523,-0.1189474899834,
-0.112262154601947,-0.101870128429215,-0.0841239827932793,-0.0506805348753447,
-0.0472186712931119,-0.0459515968833834,-0.0452081520807635,-0.0444189234570229,
-0.0433326806342394,-0.0421190019783787,-0.0400060299954982,-0.000460192131931113),
 .UNSPECIFIED.);
#149=B_SPLINE_CURVE_WITH_KNOTS('',3,(#9135,#9136,#9137,#9138,#9139,#9140,
#9141,#9142,#9143,#9144,#9145,#9146,#9147,#9148,#9149,#9150,#9151,#9152,
#9153,#9154,#9155,#9156,#9157,#9158,#9159,#9160,#9161,#9162,#9163,#9164,
#9165,#9166,#9167,#9168,#9169,#9170,#9171,#9172,#9173,#9174,#9175,#9176,
#9177,#9178,#9179,#9180,#9181,#9182),.UNSPECIFIED.,.F.,.F.,(4,2,2,2,2,2,
2,2,2,2,2,2,2,2,2,2,2,2,2,2,2,2,2,4),(-1.81289741918331,-1.79235234454203,
-1.78478324876529,-1.78272148458332,-1.7812503218432,-1.77995523560585,
-1.77855196256831,-1.77671541388916,-1.77361390266173,-1.74909585464625,
-1.73161125982571,-1.71276134110456,-1.70476946226344,-1.70312906515652,
-1.7022212026979,-1.70144668432188,-1.70047251592632,-1.69857848023461,
-1.68702630209632,-1.68239431982946,-1.67041134096808,-1.64675668637411,
-1.63539767253542,-1.6336654916901),.UNSPECIFIED.);
#150=B_SPLINE_CURVE_WITH_KNOTS('',3,(#9183,#9184,#9185,#9186,#9187,#9188,
#9189,#9190,#9191,#9192,#9193,#9194,#9195,#9196,#9197,#9198,#9199,#9200,
#9201,#9202,#9203,#9204,#9205,#9206,#9207,#9208,#9209,#9210,#9211,#9212,
#9213,#9214,#9215,#9216,#9217,#9218,#9219,#9220,#9221,#9222,#9223,#9224,
#9225,#9226,#9227,#9228,#9229,#9230,#9231,#9232,#9233,#9234,#9235,#9236,
#9237,#9238,#9239,#9240,#9241,#9242,#9243,#9244,#9245,#9246,#9247,#9248,
#9249,#9250,#9251,#9252,#9253,#9254,#9255,#9256,#9257,#9258,#9259,#9260,
#9261,#9262,#9263,#9264,#9265,#9266,#9267,#9268,#9269,#9270,#9271,#9272,
#9273,#9274,#9275,#9276,#9277,#9278,#9279,#9280,#9281,#9282,#9283,#9284,
#9285,#9286,#9287,#9288,#9289,#9290,#9291,#9292,#9293,#9294,#9295,#9296,
#9297,#9298,#9299,#9300,#9301,#9302,#9303,#9304,#9305,#9306,#9307,#9308,
#9309,#9310,#9311,#9312,#9313,#9314,#9315,#9316,#9317,#9318,#9319,#9320,
#9321,#9322,#9323,#9324,#9325,#9326,#9327,#9328,#9329,#9330,#9331,#9332,
#9333,#9334,#9335,#9336,#9337,#9338,#9339,#9340,#9341,#9342,#9343,#9344,
#9345,#9346,#9347,#9348,#9349,#9350,#9351,#9352,#9353,#9354,#9355,#9356,
#9357,#9358,#9359,#9360,#9361,#9362,#9363,#9364,#9365,#9366,#9367,#9368,
#9369,#9370,#9371,#9372,#9373,#9374,#9375,#9376,#9377,#9378,#9379,#9380,
#9381,#9382,#9383,#9384,#9385,#9386,#9387,#9388,#9389,#9390,#9391,#9392,
#9393,#9394,#9395,#9396,#9397,#9398,#9399,#9400,#9401,#9402,#9403,#9404,
#9405,#9406,#9407,#9408,#9409,#9410,#9411,#9412),.UNSPECIFIED.,.F.,.F.,
(4,2,2,2,2,2,2,2,2,2,2,2,2,2,2,2,2,2,2,2,2,2,2,2,2,2,2,2,2,2,2,2,2,2,2,
2,2,2,2,2,2,2,2,2,2,2,2,2,2,2,2,2,2,2,2,2,2,2,2,2,2,2,2,2,2,2,2,2,2,2,2,
2,2,2,2,2,2,2,2,2,2,2,2,2,2,2,2,2,2,2,2,2,2,2,2,2,2,2,2,2,2,2,2,2,2,2,2,
2,2,2,2,2,2,2,4),(-1.16059938204844,-1.1376397772446,-1.12627602602123,
-1.1235642455996,-1.12198454315578,-1.12059976257337,-1.11888194649149,
-1.11624076774638,-1.10370817248241,-1.09839856355534,-1.05405115718455,
-1.04639052196066,-1.04477748284121,-1.04387549746159,-1.0431003064223,
-1.04211799854659,-1.04012159902785,-1.02645301065094,-0.981337467812207,
-0.980728000890515,-0.97777127065291,-0.970968395755761,-0.968317500957512,
-0.96659675087213,-0.96521183928086,-0.963634416107002,-0.960932614519319,
-0.949700756310211,-0.904844704578137,-0.891299986684652,-0.889307262715579,
-0.888325648236691,-0.887550423730124,-0.88664769779691,-0.885031767615919,
-0.877327713087126,-0.83301917203181,-0.827450519045247,-0.815190331133996,
-0.81256684605222,-0.810854332565948,-0.809469725225646,-0.807885732046655,
-0.80515529101041,-0.79354231042098,-0.748945170347644,-0.735573487866166,
-0.733585926908107,-0.732605173851814,-0.731829884440097,-0.730926272233222,
-0.729306374000881,-0.721538602885769,-0.677278750639153,-0.67164297165601,
-0.659460346590478,-0.656842543132981,-0.655131817032984,-0.653747380126196,
-0.652162183977738,-0.649426138983973,-0.637734925803899,-0.593203211178834,
-0.579842744108246,-0.57785563847789,-0.57687502690842,-0.576099783551829,
-0.575196137709143,-0.57357608524576,-0.565805828057025,-0.521548910673776,
-0.515925333397171,-0.503727690052195,-0.501108819157562,-0.499397737304334,
-0.498013239680856,-0.496428223466524,-0.493693120062289,-0.482015714941103,
-0.437470293613529,-0.424107031283538,-0.422119764776551,-0.421139092677314,
-0.420363803615383,-0.419460101222214,-0.417839969156371,-0.410069726470485,
-0.365808978978721,-0.360176112749597,-0.347987368207441,-0.345368969248814,
-0.343657966719378,-0.342273380938134,-0.340688096280346,-0.337952105066744,
-0.334654785091259,-0.327895667582497,-0.282252028942882,-0.278007373554725,
-0.268121248016352,-0.26646460782486,-0.26546285836712,-0.264683753490306,
-0.263804632321155,-0.262296254837789,-0.256297409696362,-0.244803207878878,
-0.200084593430525,-0.194419701583132,-0.190137617062854,-0.188431824324415,
-0.187015054963182,-0.185713404355037,-0.18374539821509,-0.179839088431723),
 .UNSPECIFIED.);
#151=B_SPLINE_CURVE_WITH_KNOTS('',3,(#9417,#9418,#9419,#9420,#9421,#9422,
#9423,#9424,#9425,#9426,#9427,#9428,#9429,#9430,#9431,#9432,#9433,#9434,
#9435,#9436,#9437,#9438,#9439,#9440,#9441,#9442,#9443,#9444,#9445,#9446,
#9447,#9448,#9449,#9450,#9451,#9452,#9453,#9454,#9455,#9456,#9457,#9458,
#9459,#9460,#9461,#9462,#9463,#9464,#9465,#9466,#9467,#9468,#9469,#9470,
#9471,#9472,#9473,#9474,#9475,#9476,#9477,#9478,#9479,#9480,#9481,#9482,
#9483,#9484,#9485,#9486,#9487,#9488,#9489,#9490,#9491,#9492,#9493,#9494,
#9495,#9496,#9497,#9498,#9499,#9500,#9501,#9502,#9503,#9504,#9505,#9506,
#9507,#9508,#9509,#9510,#9511,#9512,#9513,#9514,#9515,#9516,#9517,#9518,
#9519,#9520,#9521,#9522,#9523,#9524,#9525,#9526,#9527,#9528,#9529,#9530,
#9531,#9532,#9533,#9534,#9535,#9536,#9537,#9538,#9539,#9540,#9541,#9542,
#9543,#9544,#9545,#9546,#9547,#9548,#9549,#9550,#9551,#9552,#9553,#9554,
#9555,#9556,#9557,#9558,#9559,#9560,#9561,#9562,#9563,#9564,#9565,#9566,
#9567,#9568,#9569,#9570,#9571,#9572,#9573,#9574,#9575,#9576,#9577,#9578,
#9579,#9580,#9581,#9582,#9583,#9584,#9585,#9586,#9587,#9588,#9589,#9590,
#9591,#9592,#9593,#9594,#9595,#9596,#9597,#9598,#9599,#9600,#9601,#9602,
#9603,#9604,#9605,#9606,#9607,#9608,#9609,#9610,#9611,#9612,#9613,#9614,
#9615,#9616,#9617,#9618,#9619,#9620,#9621,#9622,#9623,#9624,#9625,#9626,
#9627,#9628,#9629,#9630,#9631,#9632,#9633,#9634,#9635,#9636,#9637,#9638,
#9639,#9640,#9641,#9642,#9643,#9644,#9645,#9646,#9647,#9648,#9649,#9650,
#9651,#9652,#9653,#9654,#9655,#9656,#9657,#9658,#9659,#9660,#9661,#9662),
 .UNSPECIFIED.,.F.,.F.,(4,2,2,2,2,2,2,2,2,2,2,2,2,2,2,2,2,2,2,2,2,2,2,2,
2,2,2,2,2,2,2,2,2,2,2,2,2,2,2,2,2,2,2,2,2,2,2,2,2,2,2,2,2,2,2,2,2,2,2,2,
2,2,2,2,2,2,2,2,2,2,2,2,2,2,2,2,2,2,2,2,2,2,2,2,2,2,2,2,2,2,2,2,2,2,2,2,
2,2,2,2,2,2,2,2,2,2,2,2,2,2,2,2,2,2,2,2,2,2,2,2,2,2,4),(-1.78170360182271,
-1.7683034713062,-1.76015236616984,-1.75850313810802,-1.75759311919535,
-1.75681841226449,-1.75584610244542,-1.7539618167832,-1.74266556262803,
-1.73948173379604,-1.69417695521611,-1.6875210575979,-1.6842599541551,-1.68158696731005,
-1.68002014497342,-1.68001665882529,-1.68001315345354,-1.68000962869081,
-1.68000608437026,-1.68000252033479,-1.67999893643978,-1.6799953325033,
-1.67999170837276,-1.67998806410434,-1.6786040634517,-1.67689600952329,
-1.67428623934759,-1.66221675422773,-1.65648257263056,-1.61222843942018,
-1.60443125533508,-1.60280972901297,-1.60190585059751,-1.6011307634256,
-1.60015079482505,-1.59816643150886,-1.58487764914714,-1.54043328091605,
-1.52866065004123,-1.52591909480963,-1.52433282449036,-1.52294870594554,
-1.52123998724339,-1.51862823484705,-1.50653108257774,-1.50082076657738,
-1.45654737952848,-1.44877058525294,-1.44715024079711,-1.44624658910164,
-1.44547142993403,-1.44449102850313,-1.44250467060609,-1.42915784135289,
-1.38460988847945,-1.3729787048207,-1.37024720773038,-1.36866309708836,
-1.36727868011315,-1.36556677833113,-1.36294490741458,-1.35070585169779,
-1.34512190547531,-1.30075430359628,-1.29309009947167,-1.2914766452433,
-1.29057446657813,-1.28979910365859,-1.28881655769146,-1.28681965332622,
-1.27314336775102,-1.22792737328192,-1.21717892514324,-1.21451417774121,
-1.21294474717732,-1.21155851819679,-1.20982515731541,-1.20713388138239,
-1.19382234134101,-1.16103764777963,-1.13889122566265,-1.13635875792502,
-1.13527646427588,-1.13448819239254,-1.13374412780774,-1.13247266843914,
-1.1289801428155,-1.10267999448151,-1.07484765762306,-1.0618766250044,-1.05905417491396,
-1.05745002590426,-1.05620624249344,-1.05457942965848,-1.05173192746894,
-1.04453897210281,-0.994860709142551,-0.986297799958003,-0.98302502426953,
-0.980635604246661,-0.97968360741896,-0.978894906226537,-0.978064199925879,
-0.976773390819549,-0.972809368846552,-0.945708455311416,-0.909985235145147,
-0.904766067901712,-0.902653293736338,-0.901349022433496,-0.899935801846121,
-0.898009969296553,-0.893554244926042,-0.87445635710687,-0.847765591138597,
-0.826984890938684,-0.824869950215989,-0.823864122518408,-0.823086545253413,
-0.822199863358343,-0.820657124645047,-0.814037228101076,-0.801408127637272),
 .UNSPECIFIED.);
#152=B_SPLINE_CURVE_WITH_KNOTS('',3,(#9664,#9665,#9666,#9667,#9668,#9669,
#9670,#9671,#9672,#9673,#9674,#9675,#9676,#9677,#9678,#9679,#9680,#9681,
#9682,#9683,#9684,#9685,#9686,#9687,#9688,#9689,#9690,#9691,#9692,#9693,
#9694,#9695,#9696,#9697,#9698,#9699,#9700,#9701,#9702,#9703,#9704,#9705,
#9706,#9707,#9708,#9709,#9710,#9711),.UNSPECIFIED.,.F.,.F.,(4,2,2,2,2,2,
2,2,2,2,2,2,2,2,2,2,2,2,2,2,2,2,2,4),(-0.179839088431723,-0.179004660102891,
-0.172374834811605,-0.153999719879391,-0.126873490254025,-0.123674374577756,
-0.112527659510257,-0.110814604507059,-0.109796381892867,-0.109015163230315,
-0.108145490985755,-0.106679338754425,-0.101304554848563,-0.0793271074036512,
-0.0601174400930077,-0.0374409868942284,-0.0343738583758793,-0.0325469315184454,
-0.0311447844141434,-0.0298491743177718,-0.0283730448890918,-0.0262994601569834,
-0.0189618397680811,-0.000459929193491284),.UNSPECIFIED.);
#153=B_SPLINE_CURVE_WITH_KNOTS('',3,(#9712,#9713,#9714,#9715,#9716,#9717,
#9718,#9719,#9720,#9721,#9722,#9723,#9724,#9725,#9726,#9727,#9728,#9729,
#9730,#9731,#9732,#9733,#9734,#9735,#9736,#9737,#9738,#9739,#9740,#9741,
#9742,#9743,#9744,#9745,#9746,#9747,#9748,#9749,#9750,#9751,#9752,#9753,
#9754,#9755,#9756,#9757,#9758,#9759,#9760,#9761,#9762,#9763,#9764,#9765,
#9766,#9767,#9768,#9769,#9770,#9771,#9772,#9773,#9774,#9775,#9776,#9777,
#9778,#9779,#9780,#9781,#9782,#9783,#9784,#9785,#9786,#9787,#9788,#9789,
#9790,#9791,#9792,#9793,#9794,#9795,#9796,#9797,#9798,#9799,#9800,#9801,
#9802,#9803,#9804,#9805,#9806,#9807,#9808,#9809,#9810,#9811,#9812,#9813,
#9814,#9815,#9816,#9817,#9818,#9819,#9820,#9821,#9822,#9823,#9824,#9825,
#9826,#9827,#9828,#9829,#9830,#9831,#9832,#9833,#9834,#9835,#9836,#9837,
#9838,#9839,#9840,#9841,#9842,#9843,#9844,#9845,#9846,#9847,#9848,#9849,
#9850,#9851,#9852,#9853,#9854,#9855,#9856,#9857,#9858,#9859,#9860,#9861,
#9862,#9863,#9864,#9865,#9866,#9867,#9868,#9869,#9870,#9871,#9872,#9873,
#9874,#9875,#9876,#9877,#9878,#9879,#9880,#9881,#9882,#9883,#9884,#9885,
#9886,#9887,#9888,#9889,#9890,#9891,#9892,#9893,#9894,#9895,#9896,#9897,
#9898,#9899),.UNSPECIFIED.,.F.,.F.,(4,2,2,2,2,2,2,2,2,2,2,2,2,2,2,2,2,2,
2,2,2,2,2,2,2,2,2,2,2,2,2,2,2,2,2,2,2,2,2,2,2,2,2,2,2,2,2,2,2,2,2,2,2,2,
2,2,2,2,2,2,2,2,2,2,2,2,2,2,2,2,2,2,2,2,2,2,2,2,2,2,2,2,2,2,2,2,2,2,2,2,
2,2,2,4),(-1.96101216699422,-1.92376717516262,-1.91917787234555,-1.9170715814596,
-1.91586081289646,-1.91477679581723,-1.91398832062296,-1.91324491239542,
-1.91197642912747,-1.90850241090579,-1.87547801514069,-1.86158912457042,
-1.84852008682589,-1.84059656044399,-1.83824196921588,-1.83693558219688,
-1.83569195369257,-1.83406594785621,-1.83122140892527,-1.81941367803316,
-1.81692010615816,-1.78422705433009,-1.76863014499697,-1.76130508366823,
-1.75970556859133,-1.75880653793929,-1.75803098224364,-1.75704446118011,
-1.75502708662785,-1.75007437755261,-1.74882325422875,-1.71120624932441,
-1.68886568661235,-1.68556753951387,-1.68287050887521,-1.68129814241858,
-1.68005452906571,-1.67842843291343,-1.67558345517448,-1.66377002905829,
-1.65779691645305,-1.61374502958058,-1.60569256002353,-1.60405568913376,
-1.60314844501536,-1.60237364520623,-1.60139810459358,-1.5994984084991,
-1.5878133738894,-1.58430598393704,-1.53951502022394,-1.52959422421342,
-1.52699809262552,-1.525443918536,-1.52405542162033,-1.52229804978378,-1.51886029944821,
-1.48818017953218,-1.47300156061752,-1.45141937034938,-1.44888796864739,
-1.44780592253626,-1.44701775311612,-1.44627373119915,-1.44500223906049,
-1.44150906290255,-1.41531456876857,-1.38738726300822,-1.37439139561185,
-1.37156753483781,-1.36996317459946,-1.36871950786582,-1.36709325132243,
-1.36424776181924,-1.35242901342353,-1.34645996467531,-1.30240277478005,
-1.29435412790247,-1.29271742926612,-1.29181019781711,-1.29103535865443,
-1.29005970432006,-1.28815959654163,-1.2764656554289,-1.23927878053355,
-1.22598257637473,-1.21793239096081,-1.21551608655893,-1.21400165580142,
-1.21260318188758,-1.21079905653591,-1.20780943779862,-1.18832580841037,
-1.16006334462802),.UNSPECIFIED.);
#154=B_SPLINE_CURVE_WITH_KNOTS('',3,(#9905,#9906,#9907,#9908,#9909,#9910,
#9911,#9912,#9913,#9914,#9915,#9916,#9917,#9918,#9919,#9920,#9921,#9922,
#9923,#9924,#9925,#9926,#9927,#9928,#9929,#9930,#9931,#9932,#9933,#9934,
#9935,#9936,#9937,#9938,#9939,#9940,#9941,#9942,#9943,#9944,#9945,#9946,
#9947,#9948,#9949,#9950,#9951,#9952,#9953,#9954,#9955,#9956,#9957,#9958,
#9959,#9960,#9961,#9962,#9963,#9964,#9965,#9966,#9967,#9968,#9969,#9970,
#9971,#9972,#9973,#9974,#9975,#9976,#9977,#9978,#9979,#9980,#9981,#9982,
#9983,#9984,#9985,#9986,#9987,#9988,#9989,#9990,#9991,#9992,#9993,#9994,
#9995,#9996,#9997,#9998,#9999,#10000,#10001,#10002,#10003,#10004,#10005,
#10006,#10007,#10008,#10009,#10010,#10011,#10012,#10013,#10014,#10015,#10016,
#10017,#10018,#10019,#10020,#10021,#10022,#10023,#10024,#10025,#10026,#10027,
#10028,#10029,#10030,#10031,#10032,#10033,#10034,#10035,#10036,#10037,#10038,
#10039,#10040,#10041,#10042,#10043,#10044,#10045,#10046,#10047,#10048,#10049,
#10050,#10051,#10052,#10053,#10054,#10055,#10056,#10057,#10058,#10059,#10060,
#10061,#10062,#10063,#10064,#10065,#10066,#10067,#10068,#10069,#10070,#10071,
#10072,#10073,#10074,#10075,#10076,#10077,#10078,#10079,#10080,#10081,#10082,
#10083,#10084,#10085,#10086,#10087,#10088,#10089,#10090,#10091,#10092,#10093,
#10094,#10095,#10096),.UNSPECIFIED.,.F.,.F.,(4,2,2,2,2,2,2,2,2,2,2,2,2,
2,2,2,2,2,2,2,2,2,2,2,2,2,2,2,2,2,2,2,2,2,2,2,2,2,2,2,2,2,2,2,2,2,2,2,2,
2,2,2,2,2,2,2,2,2,2,2,2,2,2,2,2,2,2,2,2,2,2,2,2,2,2,2,2,2,2,2,2,2,2,2,2,
2,2,2,2,2,2,2,2,2,2,4),(-0.801823037117727,-0.784023688630058,-0.748236216965953,
-0.743586130610892,-0.734137760490493,-0.732502706660029,-0.731496521688587,
-0.730718715557687,-0.729831825304929,-0.728288847054723,-0.721669774653257,
-0.679532187120232,-0.659054313011043,-0.656039644380564,-0.654227841747118,
-0.65282781291851,-0.651316063679858,-0.648913431264255,-0.640994857138846,
-0.628000107946309,-0.59067408091829,-0.588205860252348,-0.578467710707284,
-0.576818153455657,-0.575818406173578,-0.575039430906672,-0.574158830909266,
-0.572644243380937,-0.566398001636382,-0.554254698223316,-0.522866566914076,
-0.503351584149827,-0.500360679939091,-0.498555806302408,-0.497156773936174,
-0.495641758255807,-0.493224558567718,-0.485171698523447,-0.471868650049994,
-0.434654141773758,-0.42295664892934,-0.421055775568878,-0.420079714382638,
-0.419304542715883,-0.41839689339127,-0.416759365443317,-0.408704504461344,
-0.36465233719712,-0.358600433035996,-0.346877533138093,-0.344038904018225,
-0.34241373939341,-0.341169421219202,-0.339562456542801,-0.336728893046519,
-0.333285133261875,-0.32610575247773,-0.280967774503045,-0.267332966169678,
-0.265336558013755,-0.264353846875286,-0.263578156060303,-0.262675364350169,
-0.261060248456879,-0.253495608508123,-0.209057037856655,-0.203567110206695,
-0.191219352075125,-0.188589374827605,-0.186874494202279,-0.185489208472802,
-0.184185854912427,-0.181955130936223,-0.174829591332179,-0.163534598241662,
-0.141246156991975,-0.113842073031692,-0.110345277958001,-0.109072826961984,
-0.108328342963589,-0.107539760286596,-0.106457257348446,-0.105248874065434,
-0.096530403189441,-0.0637805650890347,-0.0543807919409418,-0.047944208926656,
-0.0355754467491948,-0.032944031202,-0.0312286807453503,-0.0298433250117053,
-0.0285399838281314,-0.026987174811537,-0.0247253126703711,-0.0174352431576566,
-0.000459544977384845),.UNSPECIFIED.);
#155=B_SPLINE_CURVE_WITH_KNOTS('',3,(#10097,#10098,#10099,#10100,#10101,
#10102,#10103,#10104,#10105,#10106,#10107,#10108,#10109,#10110,#10111,#10112,
#10113,#10114,#10115,#10116,#10117,#10118,#10119,#10120,#10121,#10122,#10123,
#10124,#10125,#10126,#10127,#10128,#10129,#10130,#10131,#10132,#10133,#10134,
#10135,#10136,#10137,#10138),.UNSPECIFIED.,.F.,.F.,(4,2,2,2,2,2,2,2,2,2,
2,2,2,2,2,2,2,2,2,2,4),(-1.96082039462719,-1.92070626802204,-1.91715845252776,
-1.91461382190151,-1.91352933422924,-1.91274060793303,-1.91199702907982,
-1.91072838209475,-1.90725461064772,-1.87421821339129,-1.86065306692995,
-1.84738310607834,-1.83937084944378,-1.83700683909421,-1.83569950017748,
-1.83445544565923,-1.83283222266144,-1.83000102813636,-1.81836400302013,
-1.78688518876395,-1.78170360182271),.UNSPECIFIED.);
#156=B_SPLINE_CURVE_WITH_KNOTS('',3,(#10139,#10140,#10141,#10142,#10143,
#10144,#10145,#10146,#10147,#10148,#10149,#10150,#10151,#10152,#10153,#10154,
#10155,#10156,#10157,#10158,#10159,#10160,#10161,#10162,#10163,#10164,#10165,
#10166,#10167,#10168,#10169,#10170,#10171,#10172,#10173,#10174,#10175,#10176,
#10177,#10178,#10179,#10180,#10181,#10182,#10183,#10184,#10185,#10186,#10187,
#10188,#10189,#10190,#10191,#10192,#10193,#10194,#10195,#10196,#10197,#10198,
#10199,#10200,#10201,#10202,#10203,#10204,#10205,#10206,#10207,#10208,#10209,
#10210,#10211,#10212,#10213,#10214,#10215,#10216,#10217,#10218,#10219,#10220,
#10221,#10222,#10223,#10224,#10225,#10226,#10227,#10228,#10229,#10230,#10231,
#10232,#10233,#10234,#10235,#10236,#10237,#10238,#10239,#10240,#10241,#10242,
#10243,#10244,#10245,#10246,#10247,#10248,#10249,#10250,#10251,#10252,#10253,
#10254,#10255,#10256,#10257,#10258,#10259,#10260,#10261,#10262,#10263,#10264,
#10265,#10266,#10267,#10268,#10269,#10270,#10271,#10272,#10273,#10274,#10275,
#10276,#10277,#10278,#10279,#10280,#10281,#10282,#10283,#10284,#10285,#10286,
#10287,#10288,#10289,#10290,#10291,#10292,#10293,#10294,#10295,#10296,#10297,
#10298,#10299,#10300,#10301,#10302,#10303,#10304,#10305,#10306,#10307,#10308,
#10309,#10310,#10311,#10312,#10313,#10314,#10315,#10316,#10317,#10318,#10319,
#10320,#10321,#10322,#10323,#10324,#10325,#10326,#10327,#10328,#10329,#10330,
#10331,#10332,#10333,#10334,#10335,#10336,#10337,#10338,#10339,#10340,#10341,
#10342,#10343,#10344,#10345,#10346,#10347,#10348,#10349,#10350,#10351,#10352,
#10353,#10354,#10355,#10356,#10357,#10358,#10359,#10360,#10361,#10362,#10363,
#10364,#10365,#10366,#10367,#10368,#10369,#10370,#10371,#10372,#10373,#10374,
#10375,#10376,#10377,#10378,#10379,#10380,#10381,#10382,#10383,#10384,#10385,
#10386,#10387,#10388,#10389,#10390,#10391,#10392,#10393,#10394,#10395,#10396,
#10397,#10398,#10399,#10400),.UNSPECIFIED.,.F.,.F.,(4,2,2,2,2,2,2,2,2,2,
2,2,2,2,2,2,2,2,2,2,2,2,2,2,2,2,2,2,2,2,2,2,2,2,2,2,2,2,2,2,2,2,2,2,2,2,
2,2,2,2,2,2,2,2,2,2,2,2,2,2,2,2,2,2,2,2,2,2,2,2,2,2,2,2,2,2,2,2,2,2,2,2,
2,2,2,2,2,2,2,2,2,2,2,2,2,2,2,2,2,2,2,2,2,2,2,2,2,2,2,2,2,2,2,2,2,2,2,2,
2,2,2,2,2,2,2,2,2,2,2,2,4),(-1.16006334462802,-1.15695415773548,-1.14474945801418,
-1.1384835212994,-1.13696775675719,-1.13608710360694,-1.13530850417252,
-1.13430980687523,-1.13266316283683,-1.12297489238004,-1.12044201026335,
-1.11773919680172,-1.07264935312383,-1.0626171347475,-1.06001135200755,
-1.05845499964908,-1.05706681523399,-1.05531289005775,-1.05189147787606,
-1.01969367382795,-0.996664971587923,-0.987683575977689,-0.984301447550536,
-0.98184998017665,-0.980781908412959,-0.979996002807677,-0.979141695400166,
-0.977744027978682,-0.972812016930496,-0.964203164138319,-0.913636729286196,
-0.909632855671912,-0.905359791922181,-0.903655801450463,-0.902239835094713,
-0.900789427450258,-0.89866883324834,-0.892986555460999,-0.86254509480548,
-0.83001341333935,-0.826587213803111,-0.825326045222767,-0.824584079532824,
-0.82379474050363,-0.82270564491046,-0.820133158279236,-0.81653539403444,
-0.806706087163201,-0.790434250599599,-0.75551229896386,-0.750267129360909,
-0.748150329443177,-0.746845589379873,-0.745433442788112,-0.743511902949968,
-0.739078825493073,-0.720157113690752,-0.696429735461047,-0.69189367332266,
-0.672465848865159,-0.670360788465909,-0.669357068236445,-0.668579930658033,
-0.667692434270443,-0.666145216361041,-0.659459703818438,-0.617161185997022,
-0.596926086575843,-0.593918857449199,-0.592109796601966,-0.59071086913406,
-0.589199301478028,-0.586794796819266,-0.578850493438041,-0.565794242564795,
-0.528302874044586,-0.51652982154755,-0.5146269094935,-0.513650780184225,
-0.512876068996261,-0.511969566580366,-0.510335653515445,-0.502329443503596,
-0.45827481948449,-0.452358937542683,-0.440491888383449,-0.437896327364134,
-0.436192738284626,-0.434809137716271,-0.433219446646547,-0.430461757521969,
-0.418457603982108,-0.374156879685298,-0.360934898138545,-0.358952770209601,
-0.35797330452174,-0.357198324398725,-0.356294244948602,-0.354671563827857,
-0.346853483585681,-0.302647613358889,-0.296960961400647,-0.284838745673712,
-0.282225439913434,-0.280516312201983,-0.279132277810025,-0.279128611007164,
-0.279124964267943,-0.279121337871524,-0.279117731647333,-0.279114145433364,
-0.279110579073727,-0.279107032414747,-0.279103505295488,-0.279099997559475,
-0.277534013334995,-0.27486828581183,-0.271615246042411,-0.264981764272871,
-0.219770585861685,-0.217144613204222,-0.214781761059414,-0.20498229486787,
-0.203330010624083,-0.202329597795403,-0.201550721549415,-0.200670941485566,
-0.199159379667798,-0.193079815473416,-0.181369706556269,-0.179645560381916),
 .UNSPECIFIED.);
#157=B_SPLINE_CURVE_WITH_KNOTS('',3,(#10405,#10406,#10407,#10408,#10409,
#10410,#10411,#10412,#10413,#10414,#10415,#10416,#10417,#10418,#10419,#10420,
#10421,#10422,#10423,#10424,#10425,#10426,#10427,#10428,#10429,#10430,#10431,
#10432,#10433,#10434,#10435,#10436,#10437,#10438,#10439,#10440,#10441,#10442,
#10443,#10444,#10445,#10446,#10447,#10448,#10449,#10450,#10451,#10452,#10453,
#10454,#10455,#10456,#10457,#10458,#10459,#10460,#10461,#10462,#10463,#10464,
#10465,#10466,#10467,#10468,#10469,#10470,#10471,#10472,#10473,#10474,#10475,
#10476,#10477,#10478,#10479,#10480,#10481,#10482,#10483,#10484,#10485,#10486,
#10487,#10488,#10489,#10490,#10491,#10492,#10493,#10494,#10495,#10496,#10497,
#10498,#10499,#10500,#10501,#10502,#10503,#10504,#10505,#10506,#10507,#10508,
#10509,#10510,#10511,#10512,#10513,#10514,#10515,#10516,#10517,#10518,#10519,
#10520,#10521,#10522,#10523,#10524,#10525,#10526,#10527,#10528,#10529,#10530,
#10531,#10532,#10533,#10534,#10535,#10536,#10537,#10538,#10539,#10540,#10541,
#10542,#10543,#10544,#10545,#10546,#10547,#10548,#10549,#10550,#10551,#10552,
#10553,#10554,#10555,#10556,#10557,#10558,#10559,#10560,#10561,#10562,#10563,
#10564,#10565,#10566,#10567,#10568,#10569,#10570,#10571,#10572,#10573,#10574,
#10575,#10576,#10577,#10578,#10579,#10580,#10581,#10582,#10583,#10584,#10585,
#10586,#10587,#10588,#10589,#10590,#10591,#10592,#10593,#10594,#10595,#10596,
#10597,#10598,#10599,#10600,#10601,#10602,#10603,#10604,#10605,#10606,#10607,
#10608,#10609,#10610,#10611,#10612,#10613,#10614,#10615,#10616,#10617,#10618,
#10619,#10620,#10621,#10622,#10623,#10624,#10625,#10626,#10627,#10628,#10629,
#10630),.UNSPECIFIED.,.F.,.F.,(4,2,2,2,2,2,2,2,2,2,2,2,2,2,2,2,2,2,2,2,
2,2,2,2,2,2,2,2,2,2,2,2,2,2,2,2,2,2,2,2,2,2,2,2,2,2,2,2,2,2,2,2,2,2,2,2,
2,2,2,2,2,2,2,2,2,2,2,2,2,2,2,2,2,2,2,2,2,2,2,2,2,2,2,2,2,2,2,2,2,2,2,2,
2,2,2,2,2,2,2,2,2,2,2,2,2,2,2,2,2,2,2,2,4),(-1.78245136437627,-1.76744044651287,
-1.75496919641081,-1.74728112270941,-1.74490405263102,-1.74339802224992,
-1.74199611848338,-1.74017170218288,-1.73711360002286,-1.71486580862118,
-1.68499366565813,-1.67378534549286,-1.66985375023133,-1.66796819612799,
-1.66643876899596,-1.66556118299284,-1.66480902918777,-1.66382929018424,
-1.66184704944844,-1.64856351373072,-1.60412737186443,-1.5923178011154,
-1.58957297252364,-1.58798565011603,-1.58660111378115,-1.58489252232963,
-1.5822821607462,-1.57021433320557,-1.56447214109838,-1.52020452863946,
-1.5123993553305,-1.51077689030042,-1.50987259045687,-1.50909720466784,
-1.5081169389866,-1.50613223700723,-1.49285161387435,-1.44841284953191,
-1.43660277466148,-1.43385780268983,-1.43227039322715,-1.43088577849989,
-1.4291770871478,-1.42656656705961,-1.41449789444906,-1.40875552526734,
-1.36448531324231,-1.35667982495156,-1.35505727599923,-1.35415292678178,
-1.35337749705619,-1.35239717377589,-1.35041234846992,-1.33713063438558,
-1.2926887754824,-1.28087886780686,-1.27813380019534,-1.27654631418265,
-1.27516162006554,-1.27345281452343,-1.27084208980897,-1.25877189484171,
-1.25302995623571,-1.20875672779544,-1.20095144357245,-1.19932884235413,
-1.1984244506648,-1.19764897630252,-1.19666858605155,-1.19468359071432,
-1.18139937448144,-1.13695199547072,-1.125145703998,-1.12240078611983,-1.12081327756465,
-1.11942849894447,-1.11771950577922,-1.11510833937865,-1.10303313971384,
-1.09729475574108,-1.05301636508646,-1.04521395682267,-1.04359146636839,
-1.0426870677612,-1.04191154516288,-1.04093103968034,-1.03894563374888,
-1.02565163788004,-0.981186197547841,-0.969613041403155,-0.966786549053474,
-0.965164124911114,-0.963919684307093,-0.962309928405141,-0.959463764181939,
-0.946126913318555,-0.91683411388054,-0.890256546211244,-0.888179354489889,
-0.887180696211669,-0.886403645886897,-0.885511930484752,-0.883947141057405,
-0.8770251718542,-0.833945411873018,-0.82498038043356,-0.813851879763301,
-0.811062702029817,-0.809448885648118,-0.808079154677382,-0.806409161350799,
-0.803282707101805,-0.801823037117727),.UNSPECIFIED.);
#158=B_SPLINE_CURVE_WITH_KNOTS('',3,(#10632,#10633,#10634,#10635,#10636,
#10637,#10638,#10639,#10640,#10641,#10642,#10643,#10644,#10645,#10646,#10647,
#10648,#10649,#10650,#10651,#10652,#10653,#10654,#10655,#10656,#10657,#10658,
#10659,#10660,#10661,#10662,#10663,#10664,#10665,#10666,#10667,#10668,#10669,
#10670,#10671),.UNSPECIFIED.,.F.,.F.,(4,2,2,2,2,2,2,2,2,2,2,2,2,2,2,2,2,
2,2,4),(-0.179645560381916,-0.146159827420209,-0.129625542324312,-0.126756128831658,
-0.124968331411959,-0.123576090393712,-0.122278902789586,-0.120117575492598,
-0.113829602671236,-0.104254931678754,-0.0859058002356539,-0.0515823491832586,
-0.0482339200198023,-0.04698433590299,-0.0462444809476119,-0.0454533815944531,
-0.0443552942672115,-0.0431247166638934,-0.0409690007589198,-0.000460167162021457),
 .UNSPECIFIED.);
#159=B_SPLINE_CURVE_WITH_KNOTS('',3,(#10672,#10673,#10674,#10675,#10676,
#10677,#10678,#10679,#10680,#10681,#10682,#10683,#10684,#10685,#10686,#10687,
#10688,#10689,#10690,#10691,#10692,#10693,#10694,#10695,#10696,#10697,#10698,
#10699,#10700,#10701,#10702,#10703,#10704,#10705,#10706,#10707,#10708,#10709,
#10710,#10711,#10712,#10713,#10714,#10715,#10716,#10717,#10718,#10719,#10720,
#10721,#10722,#10723,#10724,#10725,#10726,#10727,#10728,#10729,#10730,#10731,
#10732,#10733,#10734,#10735,#10736,#10737,#10738,#10739,#10740,#10741,#10742,
#10743,#10744,#10745,#10746,#10747,#10748,#10749,#10750,#10751,#10752,#10753),
 .UNSPECIFIED.,.F.,.F.,(4,3,3,3,3,3,3,3,3,3,3,3,3,3,3,3,3,3,3,3,3,3,3,3,
3,3,3,4),(40.8407044966675,41.037551545115,41.2342884007446,41.4315010101563,
41.5450503786662,41.7435926695272,41.9433706706416,42.1414562093936,42.3420804416891,
42.5427046739847,42.7412469648515,42.9410249659644,43.1391105047221,43.3397347370126,
43.5403589693032,43.7389012601772,43.9386792612883,44.1367648000535,44.3373890323376,
44.5380132646217,44.73655555549,44.9363335566026,45.1344190953619,45.3350433276511,
45.5356675599403,45.7342191671502,45.9323412904286,45.9751165534704),
 .UNSPECIFIED.);
#160=B_SPLINE_CURVE_WITH_KNOTS('',3,(#10759,#10760,#10761,#10762,#10763,
#10764,#10765,#10766,#10767,#10768),.UNSPECIFIED.,.F.,.F.,(4,1,1,1,1,1,
1,4),(47.1238898038471,47.2191044401619,48.2167587354804,49.2144130307989,
50.2120673261174,51.209721621436,52.2073759167545,52.258435828933),
 .UNSPECIFIED.);
#161=B_SPLINE_CURVE_WITH_KNOTS('',3,(#10769,#10770,#10771,#10772,#10773,
#10774,#10775,#10776,#10777,#10778,#10779,#10780,#10781,#10782,#10783,#10784,
#10785,#10786,#10787,#10788,#10789,#10790,#10791,#10792,#10793,#10794,#10795,
#10796,#10797,#10798,#10799,#10800,#10801,#10802,#10803,#10804,#10805,#10806,
#10807,#10808,#10809,#10810,#10811,#10812,#10813,#10814,#10815,#10816,#10817,
#10818,#10819,#10820,#10821,#10822,#10823,#10824,#10825,#10826,#10827,#10828,
#10829,#10830,#10831,#10832,#10833,#10834,#10835,#10836,#10837,#10838,#10839,
#10840,#10841,#10842,#10843,#10844,#10845,#10846,#10847,#10848),
 .UNSPECIFIED.,.F.,.F.,(4,2,2,2,2,2,2,2,2,2,2,2,2,2,2,2,2,2,2,2,2,2,2,2,
2,2,2,2,2,2,2,2,2,2,2,2,2,2,2,4),(-1.96178773563397,-1.92347939810595,-1.91073511481936,
-1.90292598792833,-1.90053555319041,-1.89902662633692,-1.89762587074075,
-1.89580840232572,-1.89277393262601,-1.87151561093926,-1.84084783188495,
-1.82947385729186,-1.82550356473007,-1.8236047526262,-1.82208126938198,
-1.82119774096839,-1.82119520336292,-1.82119265557688,-1.82119009753962,
-1.82118752915564,-1.82118495033417,-1.8211823610022,-1.82117976106885,
-1.82117715043766,-1.82117429426872,-1.82117138581178,-1.82116842391008,
-1.82116540739256,-1.8211623350403,-1.82115920561571,-1.82115601783292,
-1.82115277037097,-1.82114946188555,-1.8211460909899,-1.82114265625302,
-1.82040032794713,-1.81940500783992,-1.81734421145247,-1.78996315859545,
-1.78245136437627),.UNSPECIFIED.);
#162=B_SPLINE_CURVE_WITH_KNOTS('',3,(#10850,#10851,#10852,#10853,#10854,
#10855,#10856,#10857,#10858,#10859,#10860,#10861,#10862,#10863,#10864,#10865,
#10866,#10867,#10868),.UNSPECIFIED.,.F.,.F.,(4,3,3,3,3,3,4),(45.9751165534704,
46.1731883187463,46.371748648452,46.5333218552588,46.7351974297426,46.936614823472,
47.1238898038471),.UNSPECIFIED.);
#163=B_SPLINE_CURVE_WITH_KNOTS('',3,(#10869,#10870,#10871,#10872,#10873,
#10874,#10875,#10876,#10877),.UNSPECIFIED.,.F.,.F.,(4,1,1,1,1,1,4),(47.1238961499042,
47.5309761505773,48.5286304458958,49.5262847412143,50.5239390365328,51.5215933318513,
52.2572181212454),.UNSPECIFIED.);
#164=B_SPLINE_CURVE_WITH_KNOTS('',3,(#10883,#10884,#10885,#10886,#10887,
#10888,#10889,#10890,#10891,#10892,#10893,#10894,#10895,#10896,#10897,#10898,
#10899,#10900,#10901,#10902,#10903,#10904,#10905,#10906,#10907,#10908,#10909,
#10910,#10911,#10912,#10913,#10914,#10915,#10916,#10917,#10918,#10919,#10920,
#10921,#10922,#10923,#10924,#10925,#10926,#10927,#10928,#10929,#10930,#10931,
#10932,#10933,#10934,#10935,#10936,#10937,#10938,#10939,#10940,#10941,#10942,
#10943,#10944,#10945,#10946,#10947,#10948,#10949,#10950,#10951,#10952,#10953,
#10954,#10955,#10956,#10957,#10958,#10959,#10960,#10961),.UNSPECIFIED.,
 .F.,.F.,(4,3,3,3,3,3,3,3,3,3,3,3,3,3,3,3,3,3,3,3,3,3,3,3,3,3,4),(53.4070753006206,
53.6059776023134,53.8012697164857,54.0019771119386,54.2026845073915,54.4012267982613,
54.6010047993735,54.7990903381343,54.9997145704222,55.20033880271,55.3988810935798,
55.598659094692,55.7967446334529,55.9973688657407,56.1979930980285,56.3965353888983,
56.5963133900105,56.7943989287714,56.9950231610592,57.195647393347,57.3941896842168,
57.593967685329,57.7920532240898,57.9926774563777,58.1933016886655,58.3918561713772,
58.5417292850076),.UNSPECIFIED.);
#165=B_SPLINE_CURVE_WITH_KNOTS('',3,(#10962,#10963,#10964,#10965,#10966),
 .UNSPECIFIED.,.F.,.F.,(4,1,4),(52.258435828933,53.205030212073,53.4070751110267),
 .UNSPECIFIED.);
#166=B_SPLINE_CURVE_WITH_KNOTS('',3,(#10968,#10969,#10970,#10971,#10972),
 .UNSPECIFIED.,.F.,.F.,(4,1,4),(52.2572181212454,52.5192476271698,53.4070663386681),
 .UNSPECIFIED.);
#167=B_SPLINE_CURVE_WITH_KNOTS('',3,(#10973,#10974,#10975,#10976,#10977,
#10978,#10979,#10980,#10981,#10982,#10983,#10984,#10985,#10986,#10987,#10988,
#10989,#10990,#10991,#10992,#10993,#10994,#10995,#10996,#10997,#10998,#10999,
#11000,#11001,#11002,#11003,#11004,#11005,#11006,#11007,#11008,#11009,#11010,
#11011,#11012,#11013,#11014,#11015,#11016,#11017,#11018,#11019,#11020,#11021,
#11022,#11023,#11024,#11025,#11026,#11027,#11028,#11029,#11030,#11031,#11032,
#11033,#11034,#11035,#11036,#11037,#11038,#11039,#11040,#11041,#11042,#11043,
#11044,#11045,#11046,#11047,#11048,#11049,#11050,#11051,#11052,#11053,#11054,
#11055,#11056,#11057,#11058,#11059,#11060,#11061,#11062,#11063,#11064,#11065,
#11066,#11067,#11068,#11069,#11070,#11071,#11072,#11073,#11074,#11075,#11076,
#11077,#11078,#11079,#11080,#11081,#11082,#11083,#11084,#11085,#11086,#11087,
#11088,#11089,#11090,#11091,#11092,#11093,#11094,#11095,#11096,#11097,#11098,
#11099,#11100,#11101,#11102,#11103,#11104,#11105,#11106,#11107,#11108,#11109,
#11110,#11111,#11112,#11113,#11114,#11115,#11116,#11117,#11118,#11119,#11120,
#11121,#11122,#11123,#11124,#11125,#11126,#11127,#11128,#11129,#11130,#11131,
#11132,#11133,#11134,#11135,#11136,#11137,#11138,#11139,#11140,#11141,#11142,
#11143,#11144,#11145,#11146,#11147,#11148,#11149,#11150,#11151,#11152,#11153,
#11154,#11155,#11156,#11157,#11158,#11159,#11160,#11161,#11162,#11163,#11164,
#11165,#11166,#11167,#11168,#11169,#11170,#11171,#11172,#11173,#11174,#11175,
#11176,#11177,#11178),.UNSPECIFIED.,.F.,.F.,(4,2,2,2,2,2,2,2,2,2,2,2,2,
2,2,2,2,2,2,2,2,2,2,2,2,2,2,2,2,2,2,2,2,2,2,2,2,2,2,2,2,2,2,2,2,2,2,2,2,
2,2,2,2,2,2,2,2,2,2,2,2,2,2,2,2,2,2,2,2,2,2,2,2,2,2,2,2,2,2,2,2,2,2,2,2,
2,2,2,2,2,2,2,2,2,2,2,2,2,2,2,2,2,4),(-1.96099419632204,-1.9513014516148,
-1.94705951164587,-1.94578983431876,-1.94492169502107,-1.9441940110656,
-1.94341529944014,-1.9424137279511,-1.940756701998,-1.93084818045289,-1.92480688438048,
-1.88994208877432,-1.87783407705868,-1.87031015121589,-1.86795254339656,
-1.86645140333815,-1.8650488587348,-1.86321616798416,-1.86012766341501,
-1.83632661012051,-1.80776401932063,-1.7967812745366,-1.79290358211023,
-1.79103690831438,-1.78952379918941,-1.78864836093318,-1.78787226852566,
-1.78687802310176,-1.78482095368383,-1.75738027635625,-1.73611252486617,
-1.72287171959117,-1.71484626714234,-1.71243310640668,-1.71091968139516,
-1.70952147906946,-1.70771678347637,-1.70472422476947,-1.68509287867101,
-1.65350122315967,-1.64158070348884,-1.63748503725748,-1.63554371449086,
-1.63397964407068,-1.63309383521585,-1.63231896430528,-1.63133966310854,
-1.62935794755935,-1.61613987482373,-1.57186099742114,-1.55986936415193,
-1.55711277197064,-1.55552342328942,-1.55413994866787,-1.55243629460014,
-1.54984020758755,-1.53796381210697,-1.53205178107876,-1.48797261876864,
-1.47996931392474,-1.47833559782826,-1.4774291621164,-1.4766544791083,-1.47567835335914,
-1.47377535273746,-1.46199701405454,-1.45879867385188,-1.42401399646666,
-1.40486802874797,-1.40174719177353,-1.40007901797911,-1.39871017640028,
-1.3970967062199,-1.39430638570165,-1.38315152433583,-1.37418258624708,
-1.34281894606483,-1.33047301571277,-1.3241597126109,-1.32264052491424,
-1.32175925565685,-1.32098102864057,-1.31998398700684,-1.3183424905339,
-1.30875141242944,-1.30608038552172,-1.26882902289581,-1.25585053328359,
-1.24793927144096,-1.24553836663165,-1.24402759529358,-1.24262839942346,
-1.24081757456435,-1.2378042992866,-1.21733797459818,-1.17517999007401,
-1.16855323294771,-1.16701024258132,-1.16612364974782,-1.16534630400568,
-1.16434100140869,-1.16222796112255,-1.16023075385596),.UNSPECIFIED.);
#168=B_SPLINE_CURVE_WITH_KNOTS('',3,(#11184,#11185,#11186,#11187,#11188,
#11189,#11190,#11191,#11192,#11193,#11194,#11195,#11196,#11197,#11198,#11199,
#11200,#11201,#11202,#11203,#11204,#11205,#11206,#11207,#11208,#11209,#11210,
#11211,#11212,#11213,#11214,#11215,#11216,#11217,#11218,#11219,#11220,#11221,
#11222,#11223,#11224,#11225,#11226,#11227,#11228,#11229,#11230,#11231,#11232,
#11233,#11234,#11235,#11236,#11237,#11238,#11239,#11240,#11241,#11242,#11243,
#11244,#11245,#11246,#11247,#11248,#11249,#11250,#11251,#11252,#11253,#11254,
#11255,#11256,#11257,#11258,#11259,#11260,#11261,#11262,#11263,#11264,#11265,
#11266,#11267,#11268,#11269,#11270,#11271,#11272,#11273,#11274,#11275,#11276,
#11277,#11278,#11279,#11280,#11281,#11282,#11283,#11284,#11285,#11286,#11287,
#11288,#11289,#11290,#11291,#11292,#11293,#11294,#11295,#11296,#11297,#11298,
#11299,#11300,#11301,#11302,#11303,#11304,#11305,#11306,#11307,#11308,#11309,
#11310,#11311,#11312,#11313,#11314,#11315,#11316,#11317,#11318,#11319,#11320,
#11321,#11322,#11323,#11324,#11325,#11326,#11327,#11328,#11329,#11330,#11331,
#11332,#11333,#11334,#11335,#11336,#11337,#11338,#11339,#11340,#11341,#11342,
#11343,#11344,#11345,#11346,#11347,#11348,#11349,#11350,#11351,#11352,#11353,
#11354,#11355,#11356,#11357,#11358,#11359,#11360,#11361,#11362,#11363,#11364,
#11365,#11366,#11367),.UNSPECIFIED.,.F.,.F.,(4,2,2,2,2,2,2,2,2,2,2,2,2,
2,2,2,2,2,2,2,2,2,2,2,2,2,2,2,2,2,2,2,2,2,2,2,2,2,2,2,2,2,2,2,2,2,2,2,2,
2,2,2,2,2,2,2,2,2,2,2,2,2,2,2,2,2,2,2,2,2,2,2,2,2,2,2,2,2,2,2,2,2,2,2,2,
2,2,2,2,2,2,4),(-0.801781197037416,-0.801564431273354,-0.784631761412556,
-0.781744864672891,-0.779951571262751,-0.778558361730735,-0.777023050695626,
-0.774513987802849,-0.765555515655339,-0.750078541015869,-0.712062461613006,
-0.704095050805247,-0.70254296593654,-0.701561886926095,-0.700786383110493,
-0.699882544302023,-0.698262408173563,-0.690496512902924,-0.646217299914841,
-0.640520903670275,-0.628406352664212,-0.625792588168675,-0.624082805189035,
-0.622698000843819,-0.621111138389204,-0.61836905316899,-0.606602228616763,
-0.562103221008747,-0.548796073611519,-0.546810231588376,-0.545829663022647,
-0.545054166827803,-0.544149881905276,-0.54252781110346,-0.534731130134631,
-0.490474515673364,-0.484742625951674,-0.472666880447668,-0.470055675414473,
-0.468346645942164,-0.466961839201605,-0.465374299774763,-0.462629333904826,
-0.450823271407513,-0.406349616592483,-0.393057678142898,-0.391072270933003,
-0.390091764204506,-0.389316242003469,-0.388411840638082,-0.386789345982134,
-0.378986540391174,-0.334732647199794,-0.317476722746825,-0.314317944878116,
-0.312641000883609,-0.311330850432392,-0.310032148055082,-0.307712460312073,
-0.300523745112187,-0.289148966853703,-0.265652444933814,-0.239581897585846,
-0.236086357381561,-0.234814108125912,-0.23406966760327,-0.233281068890367,
-0.232198443484937,-0.229665711286987,-0.201547070106141,-0.164858628775972,
-0.159682479308758,-0.157615771150551,-0.156189367115004,-0.154877006209078,
-0.153486256810861,-0.150084949845184,-0.116998059022532,-0.0838468120460744,
-0.080371619684191,-0.0791024991990548,-0.0783586534266667,-0.0775696526049132,
-0.0764848025660079,-0.0739393790443653,-0.0703908251530521,-0.0607605291338429,
-0.0252340113911307,-0.00623987725397335,-0.00300228405538259,-0.00133881889611477,
-0.00045986504465812),.UNSPECIFIED.);
#169=B_SPLINE_CURVE_WITH_KNOTS('',3,(#11368,#11369,#11370,#11371,#11372,
#11373,#11374,#11375,#11376,#11377,#11378,#11379,#11380,#11381,#11382,#11383,
#11384,#11385,#11386,#11387,#11388,#11389),.UNSPECIFIED.,.F.,.F.,(4,3,3,
3,3,3,3,4),(58.5417292850076,58.7398440414221,58.9379236735178,59.1364652376836,
59.190955983984,59.3995207274522,59.607179253882,59.690260417875),
 .UNSPECIFIED.);
#170=B_SPLINE_CURVE_WITH_KNOTS('',3,(#11390,#11391,#11392,#11393,#11394,
#11395,#11396,#11397,#11398,#11399,#11400,#11401,#11402,#11403,#11404,#11405,
#11406,#11407,#11408,#11409,#11410,#11411,#11412,#11413,#11414,#11415,#11416,
#11417,#11418,#11419,#11420,#11421,#11422,#11423,#11424,#11425,#11426,#11427,
#11428,#11429,#11430,#11431,#11432,#11433,#11434,#11435,#11436,#11437,#11438,
#11439,#11440,#11441,#11442,#11443,#11444,#11445,#11446,#11447,#11448,#11449,
#11450,#11451,#11452,#11453,#11454,#11455,#11456,#11457,#11458,#11459,#11460,
#11461,#11462,#11463,#11464,#11465,#11466,#11467,#11468,#11469,#11470,#11471,
#11472,#11473,#11474,#11475,#11476,#11477,#11478,#11479,#11480,#11481,#11482,
#11483,#11484,#11485,#11486,#11487,#11488,#11489,#11490,#11491,#11492,#11493,
#11494,#11495,#11496,#11497,#11498,#11499,#11500,#11501,#11502,#11503,#11504,
#11505,#11506,#11507,#11508,#11509,#11510,#11511,#11512,#11513,#11514,#11515,
#11516,#11517,#11518,#11519,#11520,#11521,#11522,#11523,#11524,#11525,#11526,
#11527,#11528,#11529,#11530,#11531,#11532,#11533,#11534,#11535,#11536,#11537,
#11538,#11539,#11540,#11541,#11542,#11543,#11544,#11545,#11546,#11547,#11548,
#11549,#11550,#11551,#11552,#11553,#11554,#11555,#11556,#11557,#11558,#11559,
#11560,#11561,#11562,#11563,#11564,#11565,#11566,#11567,#11568,#11569,#11570,
#11571,#11572,#11573,#11574,#11575,#11576,#11577,#11578,#11579,#11580,#11581,
#11582,#11583,#11584,#11585,#11586,#11587,#11588,#11589,#11590,#11591,#11592,
#11593,#11594,#11595,#11596,#11597,#11598,#11599,#11600,#11601,#11602,#11603,
#11604,#11605,#11606,#11607),.UNSPECIFIED.,.F.,.F.,(4,2,2,2,2,2,2,2,2,2,
2,2,2,2,2,2,2,2,2,2,2,2,2,2,2,2,2,2,2,2,2,2,2,2,2,2,2,2,2,2,2,2,2,2,2,2,
2,2,2,2,2,2,2,2,2,2,2,2,2,2,2,2,2,2,2,2,2,2,2,2,2,2,2,2,2,2,2,2,2,2,2,2,
2,2,2,2,2,2,2,2,2,2,2,2,2,2,2,2,2,2,2,2,2,2,2,2,2,2,4),(-1.16023075385596,
-1.14169237323851,-1.11328494959453,-1.10024368558995,-1.09230464009489,
-1.08990049019143,-1.08838885812221,-1.08698967384691,-1.08518000243611,
-1.08217112690073,-1.06189512891135,-1.019588407344,-1.01290766308251,-1.01136055927344,
-1.01047297696043,-1.00969566125427,-1.00869158297568,-1.00706287677514,
-0.997729450567957,-0.981122399408477,-0.940802439556804,-0.935874136615297,
-0.934016173491421,-0.932689704952575,-0.931290128595796,-0.929447343929366,
-0.925451336112224,-0.896067619335419,-0.859664942364794,-0.856551556868587,
-0.855338835730635,-0.85460617199995,-0.853809838362817,-0.852682847514768,
-0.849883616349157,-0.83630554657643,-0.817957217836522,-0.785617450479004,
-0.780337576845703,-0.778214564229497,-0.776908456817134,-0.775496753102549,
-0.773579239472408,-0.769170706726171,-0.750447177323274,-0.719163159974299,
-0.712729248105205,-0.702131495051325,-0.700441087596731,-0.699429497105781,
-0.698649213706853,-0.697775968861054,-0.696293687118452,-0.690440709891027,
-0.679418468458758,-0.650604289743791,-0.627110693576659,-0.624027072920194,
-0.622195395785192,-0.620792544437691,-0.619290021906622,-0.616928029913226,
-0.609371287519034,-0.597190500013532,-0.57301093143524,-0.562192712336125,
-0.558402420101115,-0.546587670848953,-0.544682805874833,-0.543706122264937,
-0.542931205032441,-0.542024731531962,-0.54039155148043,-0.532402369338922,
-0.488322463849142,-0.482429130606761,-0.470532961793422,-0.467934864853507,
-0.466230276213823,-0.464846308084849,-0.463256685772964,-0.460500369828686,
-0.448522402927491,-0.404191179446176,-0.390953875388645,-0.388970870322226,
-0.387991090652365,-0.387215920689549,-0.38631168715723,-0.384688897878654,
-0.376873510159706,-0.332653508326875,-0.326374065823214,-0.314766110908833,
-0.311960694958664,-0.310364083153132,-0.309098331123897,-0.307532106446033,
-0.304776231191199,-0.292805739122854,-0.248467104230335,-0.235225889118897,
-0.233242687560179,-0.232262843533949,-0.231487638706339,-0.230583382964214,
-0.22896059995211,-0.22114612221631,-0.179737736516157),.UNSPECIFIED.);
#171=B_SPLINE_CURVE_WITH_KNOTS('',3,(#11612,#11613,#11614,#11615,#11616,
#11617,#11618,#11619,#11620,#11621,#11622,#11623,#11624,#11625,#11626,#11627,
#11628,#11629,#11630,#11631,#11632,#11633,#11634,#11635,#11636,#11637,#11638,
#11639,#11640,#11641,#11642,#11643,#11644,#11645,#11646,#11647,#11648,#11649,
#11650,#11651,#11652,#11653,#11654,#11655,#11656,#11657,#11658,#11659,#11660,
#11661,#11662,#11663,#11664,#11665,#11666,#11667,#11668,#11669,#11670,#11671,
#11672,#11673,#11674,#11675,#11676,#11677,#11678,#11679,#11680,#11681,#11682,
#11683,#11684,#11685,#11686,#11687,#11688,#11689,#11690,#11691,#11692,#11693,
#11694,#11695,#11696,#11697,#11698,#11699,#11700,#11701,#11702,#11703,#11704,
#11705,#11706,#11707,#11708,#11709,#11710,#11711,#11712,#11713,#11714,#11715,
#11716,#11717,#11718,#11719,#11720,#11721,#11722,#11723,#11724,#11725,#11726,
#11727,#11728,#11729,#11730,#11731,#11732,#11733,#11734,#11735,#11736,#11737,
#11738,#11739,#11740,#11741,#11742,#11743,#11744,#11745,#11746,#11747,#11748,
#11749,#11750,#11751,#11752,#11753,#11754,#11755,#11756,#11757,#11758,#11759,
#11760,#11761,#11762,#11763,#11764,#11765,#11766,#11767,#11768,#11769,#11770,
#11771,#11772,#11773,#11774,#11775,#11776,#11777,#11778,#11779,#11780,#11781,
#11782,#11783,#11784,#11785,#11786,#11787,#11788,#11789,#11790,#11791,#11792,
#11793,#11794,#11795,#11796,#11797,#11798,#11799,#11800,#11801,#11802,#11803,
#11804,#11805,#11806,#11807,#11808,#11809,#11810,#11811,#11812,#11813,#11814,
#11815,#11816,#11817,#11818,#11819,#11820,#11821,#11822,#11823,#11824,#11825,
#11826,#11827,#11828,#11829,#11830,#11831,#11832,#11833,#11834,#11835,#11836,
#11837),.UNSPECIFIED.,.F.,.F.,(4,2,2,2,2,2,2,2,2,2,2,2,2,2,2,2,2,2,2,2,
2,2,2,2,2,2,2,2,2,2,2,2,2,2,2,2,2,2,2,2,2,2,2,2,2,2,2,2,2,2,2,2,2,2,2,2,
2,2,2,2,2,2,2,2,2,2,2,2,2,2,2,2,2,2,2,2,2,2,2,2,2,2,2,2,2,2,2,2,2,2,2,2,
2,2,2,2,2,2,2,2,2,2,2,2,2,2,2,2,2,2,2,2,4),(-1.78239840749006,-1.77284562178477,
-1.72778854987453,-1.71777087403357,-1.71516594519601,-1.71360955145615,
-1.7122209815346,-1.71046609554332,-1.70704130712832,-1.675825302405,-1.65445396972294,
-1.64365927870122,-1.63982580401912,-1.63797415348664,-1.63646822466227,
-1.63559538730729,-1.63559347561779,-1.63559241310626,-1.6355913502754,
-1.63559028715512,-1.63558922364734,-1.63485485296981,-1.63387469702792,
-1.63189021683031,-1.61861070353855,-1.57417630052034,-1.56236843104286,
-1.5596238294537,-1.55803661172293,-1.5566521508909,-1.55494363230592,-1.55233334427224,
-1.54026513508306,-1.53452420752606,-1.49025841048117,-1.48245447871828,
-1.48083215321063,-1.47992791442734,-1.47915257070224,-1.47817234500265,
-1.47618768085193,-1.46290560254032,-1.41846554068109,-1.40666148533971,
-1.4039170475879,-1.4023298104286,-1.40094526481334,-1.39923655440781,-1.39662581110934,
-1.38455239745824,-1.37881520388222,-1.33454412174122,-1.32674321952217,
-1.32512101416403,-1.32421677051514,-1.32344137835469,-1.32246103465894,
-1.32047594610352,-1.30718366948274,-1.26272480296003,-1.25094322009141,
-1.2482002758304,-1.24661331194263,-1.24522865369113,-1.24351935291935,
-1.24090686758408,-1.22880932318379,-1.22309282888017,-1.17880471165658,
-1.17102144590226,-1.16940025375004,-1.16849620003081,-1.1677207396055,
-1.16674001309906,-1.1647531796914,-1.15141050868083,-1.10686186725147,
-1.09520250361167,-1.09246822313687,-1.09088311162763,-1.08949818584946,
-1.08778612693812,-1.08516489680534,-1.07294617143502,-1.0673376690503,
-1.02296925849174,-1.01528157186809,-1.01366620817817,-1.01276339549851,
-1.01198775635481,-1.0110052058272,-1.00900942961206,-0.995389611623066,
-0.98124423528614,-0.943311722561338,-0.938198116727199,-0.936102683071357,
-0.93480134148511,-0.933385139599993,-0.93144414372252,-0.926902678137378,
-0.90711886907993,-0.876897772530609,-0.8709700969086,-0.866845968151487,
-0.859696072948218,-0.858197964127305,-0.857233426416594,-0.856458953790592,
-0.855542225640735,-0.853862716329921,-0.845051468345399,-0.801781197037416),
 .UNSPECIFIED.);
#172=B_SPLINE_CURVE_WITH_KNOTS('',3,(#11839,#11840,#11841,#11842,#11843,
#11844,#11845,#11846,#11847,#11848,#11849,#11850,#11851,#11852,#11853,#11854,
#11855,#11856,#11857,#11858,#11859,#11860,#11861,#11862,#11863,#11864,#11865,
#11866,#11867,#11868,#11869,#11870,#11871,#11872,#11873,#11874,#11875,#11876,
#11877,#11878,#11879,#11880,#11881,#11882,#11883,#11884,#11885,#11886,#11887,
#11888,#11889,#11890,#11891,#11892,#11893,#11894,#11895,#11896,#11897,#11898,
#11899,#11900,#11901,#11902,#11903,#11904,#11905,#11906,#11907,#11908,#11909,
#11910,#11911,#11912,#11913,#11914,#11915,#11916),.UNSPECIFIED.,.F.,.F.,
(4,2,2,2,2,2,2,2,2,2,2,2,2,2,2,2,2,2,2,2,2,2,2,2,2,2,2,2,2,2,2,2,2,2,2,
2,2,2,4),(-0.179737736516157,-0.1769232270991,-0.159644222022814,-0.156490498628278,
-0.154815044125389,-0.153505865105826,-0.153475766098181,-0.153451524629101,
-0.153431689909591,-0.153400337945444,-0.153370155173738,-0.153340997035231,
-0.15331273942471,-0.153285274796565,-0.153258509146771,-0.153232359639407,
-0.153206752727951,-0.153181622639818,-0.153156910148042,-0.153132561572531,
-0.15310852793948,-0.153084764295521,-0.153061229129292,-0.153037883877162,
-0.151356144806248,-0.147985758223778,-0.117994593050442,-0.0811636312334916,
-0.0780867407108284,-0.0768799022254691,-0.0761483265207869,-0.075350958552095,
-0.0742187631733703,-0.0713875196662592,-0.0575134608539688,-0.0253441239235573,
-0.00564734167008595,-0.00218675447415778,-0.000459928765327191),
 .UNSPECIFIED.);
#173=B_SPLINE_CURVE_WITH_KNOTS('',3,(#11917,#11918,#11919,#11920,#11921,
#11922,#11923,#11924,#11925,#11926,#11927,#11928,#11929,#11930,#11931,#11932,
#11933,#11934,#11935,#11936,#11937,#11938,#11939,#11940,#11941,#11942,#11943,
#11944,#11945,#11946,#11947,#11948,#11949,#11950,#11951,#11952,#11953,#11954,
#11955,#11956,#11957,#11958,#11959,#11960,#11961,#11962,#11963,#11964,#11965,
#11966,#11967,#11968,#11969,#11970,#11971,#11972,#11973,#11974,#11975,#11976,
#11977,#11978,#11979,#11980,#11981,#11982,#11983,#11984,#11985,#11986,#11987,
#11988,#11989,#11990,#11991,#11992,#11993,#11994,#11995,#11996,#11997,#11998,
#11999,#12000,#12001,#12002,#12003,#12004,#12005,#12006,#12007,#12008,#12009,
#12010,#12011,#12012,#12013,#12014,#12015,#12016,#12017,#12018,#12019,#12020,
#12021,#12022,#12023,#12024,#12025,#12026,#12027,#12028,#12029,#12030,#12031,
#12032,#12033,#12034,#12035,#12036,#12037,#12038,#12039,#12040,#12041,#12042,
#12043,#12044,#12045,#12046,#12047,#12048,#12049,#12050,#12051,#12052,#12053,
#12054,#12055,#12056,#12057,#12058,#12059,#12060,#12061,#12062,#12063,#12064,
#12065,#12066,#12067,#12068,#12069,#12070,#12071,#12072,#12073,#12074,#12075,
#12076,#12077,#12078,#12079,#12080,#12081,#12082,#12083,#12084,#12085,#12086,
#12087,#12088,#12089,#12090,#12091,#12092,#12093,#12094,#12095,#12096,#12097,
#12098,#12099,#12100,#12101,#12102,#12103,#12104,#12105,#12106,#12107,#12108,
#12109,#12110),.UNSPECIFIED.,.F.,.F.,(4,2,2,2,2,2,2,2,2,2,2,2,2,2,2,2,2,
2,2,2,2,2,2,2,2,2,2,2,2,2,2,2,2,2,2,2,2,2,2,2,2,2,2,2,2,2,2,2,2,2,2,2,2,
2,2,2,2,2,2,2,2,2,2,2,2,2,2,2,2,2,2,2,2,2,2,2,2,2,2,2,2,2,2,2,2,2,2,2,2,
2,2,2,2,2,2,2,4),(-1.9600875839387,-1.95934093715801,-1.95805933249976,
-1.95667819987209,-1.95482891097818,-1.95083423577423,-1.94672671667632,
-1.93497892918676,-1.89092130768535,-1.88293385487988,-1.881301859421,-1.88039616971909,
-1.87962199684674,-1.87864635117661,-1.8767438048867,-1.86495193330382,
-1.86115690531924,-1.83018701563879,-1.8154088803222,-1.80673597886826,
-1.80491064335427,-1.80353000125775,-1.8021497171777,-1.8008422165049,-1.79878192320611,
-1.7936348353588,-1.75646869809257,-1.74201405554711,-1.73239541927384,
-1.72885146347219,-1.72630953307478,-1.72522616150818,-1.72443823541844,
-1.72369541003229,-1.72242805827455,-1.7189579099933,-1.68604203700969,
-1.65607040410987,-1.65043352013277,-1.64882792003788,-1.64730045160312,
-1.64594980102297,-1.64422289553059,-1.64098771693729,-1.62167690995825,
-1.57865420762684,-1.57174479024544,-1.57018216749663,-1.56929159549042,
-1.56851548308769,-1.56751797563354,-1.56544298688517,-1.53906457028005,
-1.51500354297263,-1.50292256936688,-1.49541167328284,-1.49305614467637,
-1.49155584981712,-1.49015375987227,-1.48832118171311,-1.48523179305424,
-1.45166371568129,-1.43943946475487,-1.41775204615246,-1.41522200674474,
-1.41414060284988,-1.41335292417017,-1.41260938406906,-1.41133875518179,
-1.40784816982517,-1.38163238947312,-1.35375176496569,-1.34077152517159,
-1.33794991784222,-1.33634667376802,-1.33510379494901,-1.33347845813631,
-1.33063429577889,-1.31881715816348,-1.31285721994045,-1.26882475504054,
-1.2607851991246,-1.25914976991026,-1.25824316281056,-1.2574688084132,-1.25649370273112,
-1.25459448150224,-1.24289989439707,-1.2392540446794,-1.19459751745936,
-1.18472581909819,-1.18213496219784,-1.18058253093539,-1.17919469940038,
-1.17743696075175,-1.17399467190637,-1.15958133138081),.UNSPECIFIED.);
#174=B_SPLINE_CURVE_WITH_KNOTS('',3,(#12116,#12117,#12118,#12119,#12120,
#12121,#12122,#12123,#12124,#12125,#12126,#12127,#12128,#12129,#12130,#12131,
#12132,#12133,#12134,#12135,#12136,#12137,#12138,#12139,#12140,#12141,#12142,
#12143,#12144,#12145,#12146,#12147,#12148,#12149,#12150,#12151,#12152,#12153,
#12154,#12155,#12156,#12157,#12158,#12159,#12160,#12161,#12162,#12163,#12164,
#12165,#12166,#12167,#12168,#12169,#12170,#12171,#12172,#12173,#12174,#12175,
#12176,#12177,#12178,#12179,#12180,#12181,#12182,#12183,#12184,#12185,#12186,
#12187,#12188,#12189,#12190,#12191,#12192,#12193,#12194,#12195,#12196,#12197,
#12198,#12199,#12200,#12201,#12202,#12203,#12204,#12205,#12206,#12207,#12208,
#12209,#12210,#12211,#12212,#12213,#12214,#12215,#12216,#12217,#12218,#12219,
#12220,#12221,#12222,#12223,#12224,#12225,#12226,#12227,#12228,#12229,#12230,
#12231,#12232,#12233,#12234,#12235,#12236,#12237,#12238,#12239,#12240,#12241,
#12242,#12243,#12244,#12245,#12246,#12247,#12248,#12249,#12250,#12251,#12252,
#12253,#12254,#12255,#12256,#12257,#12258,#12259,#12260,#12261,#12262,#12263,
#12264,#12265,#12266,#12267,#12268,#12269,#12270,#12271,#12272,#12273,#12274,
#12275,#12276,#12277,#12278,#12279,#12280,#12281,#12282,#12283,#12284,#12285,
#12286,#12287,#12288,#12289,#12290,#12291,#12292,#12293,#12294,#12295,#12296,
#12297,#12298,#12299,#12300,#12301,#12302,#12303,#12304,#12305,#12306,#12307,
#12308,#12309,#12310,#12311,#12312,#12313,#12314,#12315,#12316,#12317,#12318,
#12319,#12320,#12321,#12322,#12323,#12324,#12325,#12326,#12327,#12328,#12329,
#12330,#12331,#12332,#12333,#12334,#12335),.UNSPECIFIED.,.F.,.F.,(4,2,2,
2,2,2,2,2,2,2,2,2,2,2,2,2,2,2,2,2,2,2,2,2,2,2,2,2,2,2,2,2,2,2,2,2,2,2,2,
2,2,2,2,2,2,2,2,2,2,2,2,2,2,2,2,2,2,2,2,2,2,2,2,2,2,2,2,2,2,2,2,2,2,2,2,
2,2,2,2,2,2,2,2,2,2,2,2,2,2,2,2,2,2,2,2,2,2,2,2,2,2,2,2,2,2,2,2,2,2,4),
(-0.801722752441873,-0.78065717023981,-0.767362084515214,-0.765377067388483,
-0.764396824969129,-0.763621546938173,-0.762717470689388,-0.76109566007094,
-0.753298060507483,-0.709056128687175,-0.703322235667132,-0.691253819841489,
-0.688643607569661,-0.686935134061989,-0.685550715385673,-0.683963552116032,
-0.681219062189337,-0.669412299506496,-0.624953702235781,-0.611667051281045,
-0.609682245572363,-0.608702020197228,-0.607926712834498,-0.607022553163146,
-0.60540047001783,-0.5975992232714,-0.553358021684475,-0.54762001048994,
-0.535555380534457,-0.532945348157145,-0.531236891174371,-0.529852418512279,
-0.528265119177102,-0.525520205636661,-0.513708653362249,-0.469251123666496,
-0.455965643469658,-0.45398080917297,-0.453000552705642,-0.452225212431715,
-0.451321004815732,-0.449698811778175,-0.441896582234841,-0.397653969918475,
-0.391914956011652,-0.379850639401331,-0.377240550463772,-0.375532036757892,
-0.374147505015917,-0.37256012350856,-0.369815031209097,-0.358002131985904,
-0.313543250445868,-0.30025377472458,-0.29827123072108,-0.297291408397522,
-0.296539287975931,-0.295661722340187,-0.294139317927457,-0.292259897439224,
-0.28834640497997,-0.277216274844477,-0.247761380106628,-0.225040245846044,
-0.221971851959613,-0.220144378650866,-0.218741929044931,-0.21723707896719,
-0.214865607327831,-0.207228221955087,-0.194868620467261,-0.172283141841685,
-0.144743779054548,-0.14268541881812,-0.141690526590898,-0.140948427976586,
-0.140945004504463,-0.140941644597975,-0.140938346837832,-0.140935109846264,
-0.14093193228487,-0.140928812829985,-0.140925750210286,-0.140922743198353,
-0.14091979059585,-0.140916891222301,-0.140914043927115,-0.140911435093213,
-0.1409088369345,-0.140906249362769,-0.140903672286988,-0.140901105617953,
-0.140898549279099,-0.140896003179264,-0.140893467241901,-0.140009651033863,
-0.138485285185047,-0.136585161562114,-0.132611404217846,-0.12122411065082,
-0.0904944251324556,-0.069343359262306,-0.0663115254870869,-0.0644947211505962,
-0.0630939494698289,-0.0615844847895973,-0.0591920876558504,-0.0513667070427022,
-0.0385839865583593,-0.000460346267092497),.UNSPECIFIED.);
#175=B_SPLINE_CURVE_WITH_KNOTS('',3,(#12336,#12337,#12338,#12339,#12340,
#12341,#12342,#12343,#12344,#12345,#12346,#12347,#12348,#12349,#12350,#12351,
#12352,#12353,#12354,#12355,#12356,#12357,#12358,#12359,#12360,#12361,#12362,
#12363,#12364,#12365,#12366,#12367,#12368,#12369,#12370,#12371,#12372,#12373,
#12374,#12375,#12376,#12377,#12378,#12379,#12380,#12381,#12382,#12383,#12384,
#12385,#12386,#12387,#12388,#12389,#12390,#12391,#12392,#12393),
 .UNSPECIFIED.,.F.,.F.,(4,2,2,2,2,2,2,2,2,2,2,2,2,2,2,2,2,2,2,2,2,2,2,2,
2,2,2,2,4),(-1.96155185877725,-1.94987305567131,-1.94854983047148,-1.94765950245194,
-1.9469272038431,-1.94615159644688,-1.94516776474917,-1.94360639721424,
-1.93548419247702,-1.92964326762137,-1.89364864512461,-1.88085803289035,
-1.87302840038722,-1.87063566330137,-1.8691261996907,-1.86772557693905,
-1.86590917406853,-1.86287844117196,-1.84177023273213,-1.81098481128685,
-1.79958134117371,-1.79560413647834,-1.79370293947677,-1.79216611434465,
-1.79128548516075,-1.79050954111915,-1.78952162698962,-1.78749838779007,
-1.78239840749006),.UNSPECIFIED.);
#176=B_SPLINE_CURVE_WITH_KNOTS('',3,(#12394,#12395,#12396,#12397,#12398,
#12399,#12400,#12401,#12402,#12403,#12404,#12405,#12406,#12407,#12408,#12409,
#12410,#12411,#12412,#12413,#12414,#12415,#12416,#12417,#12418,#12419,#12420,
#12421,#12422,#12423,#12424,#12425,#12426,#12427,#12428,#12429,#12430,#12431,
#12432,#12433,#12434,#12435,#12436,#12437,#12438,#12439,#12440,#12441,#12442,
#12443,#12444,#12445,#12446,#12447,#12448,#12449,#12450,#12451,#12452,#12453,
#12454,#12455,#12456,#12457,#12458,#12459,#12460,#12461,#12462,#12463,#12464,
#12465,#12466,#12467,#12468,#12469,#12470,#12471,#12472,#12473,#12474,#12475,
#12476,#12477,#12478,#12479,#12480,#12481,#12482,#12483,#12484,#12485,#12486,
#12487,#12488,#12489,#12490,#12491,#12492,#12493,#12494,#12495,#12496,#12497,
#12498,#12499,#12500,#12501,#12502,#12503,#12504,#12505,#12506,#12507,#12508,
#12509,#12510,#12511,#12512,#12513,#12514,#12515,#12516,#12517,#12518,#12519,
#12520,#12521,#12522,#12523,#12524,#12525,#12526,#12527,#12528,#12529,#12530,
#12531,#12532,#12533,#12534,#12535,#12536,#12537,#12538,#12539,#12540,#12541,
#12542,#12543,#12544,#12545,#12546,#12547,#12548,#12549,#12550,#12551,#12552,
#12553,#12554,#12555,#12556,#12557,#12558,#12559,#12560,#12561,#12562,#12563,
#12564,#12565,#12566,#12567,#12568,#12569,#12570,#12571,#12572,#12573,#12574,
#12575,#12576,#12577,#12578,#12579,#12580,#12581,#12582,#12583,#12584,#12585,
#12586,#12587,#12588,#12589,#12590,#12591,#12592,#12593,#12594,#12595,#12596,
#12597,#12598,#12599,#12600,#12601,#12602,#12603,#12604,#12605,#12606,#12607,
#12608,#12609),.UNSPECIFIED.,.F.,.F.,(4,2,2,2,2,2,2,2,2,2,2,2,2,2,2,2,2,
2,2,2,2,2,2,2,2,2,2,2,2,2,2,2,2,2,2,2,2,2,2,2,2,2,2,2,2,2,2,2,2,2,2,2,2,
2,2,2,2,2,2,2,2,2,2,2,2,2,2,2,2,2,2,2,2,2,2,2,2,2,2,2,2,2,2,2,2,2,2,2,2,
2,2,2,2,2,2,2,2,2,2,2,2,2,2,2,2,2,2,4),(-1.15958133138081,-1.14530457866119,
-1.12483368809695,-1.11163403576874,-1.10503853507038,-1.10349845086023,
-1.1026128107544,-1.10183583021972,-1.10083037770834,-1.09871481324313,
-1.07734590571552,-1.05121430682451,-1.03220486816744,-1.02776143864966,
-1.02583867904839,-1.02442686941848,-1.02312330519995,-1.02101035942866,
-1.01578427188395,-0.980307983620089,-0.963674202751702,-0.950258281455218,
-0.948270573228327,-0.947290286350016,-0.946515603785185,-0.945612959448085,
-0.94399556664806,-0.936254359713296,-0.892012388924327,-0.88641167918616,
-0.874203380763913,-0.871584734488881,-0.869874413800588,-0.868490939442315,
-0.866907541422678,-0.864176358749767,-0.852533123478051,-0.808003830245064,
-0.794642339862062,-0.792656328679721,-0.791676356213017,-0.790901666489291,
-0.789998720170527,-0.788380054632066,-0.780618948074043,-0.73639083984906,
-0.730767925334323,-0.718582979154276,-0.715966268198572,-0.714256506900754,
-0.712873017385328,-0.711289088816377,-0.70855569364178,-0.696882942514304,
-0.652372416140613,-0.63902194840188,-0.637036228625098,-0.636056288953383,
-0.63528157083429,-0.634378529011887,-0.632759536698366,-0.624993921257931,
-0.580767230004565,-0.575139358219915,-0.562959158778991,-0.56034268924591,
-0.558632963075584,-0.557249420587868,-0.555665342022872,-0.552931462031809,
-0.541253135629998,-0.496744260384614,-0.483395236440537,-0.481409495622696,
-0.480429526121469,-0.479654774902392,-0.478751683562759,-0.477132575212989,
-0.469365887438029,-0.425137839085798,-0.419508892827036,-0.407329084537554,
-0.404712562444806,-0.403002780401332,-0.401619178408638,-0.400035016025266,
-0.397300951696883,-0.385621222195671,-0.341111021912406,-0.327761697339501,
-0.325775924943254,-0.324795923498939,-0.324036174860809,-0.323159646904321,
-0.32222035495408,-0.320778137973031,-0.318075969119637,-0.289943309751929,
-0.255409972254572,-0.250156961702153,-0.24803925756151,-0.246734667349714,
-0.245323236279037,-0.243403656949208,-0.238979513629093,-0.220123039434933,
-0.192053274695651,-0.179622088260795),.UNSPECIFIED.);
#177=B_SPLINE_CURVE_WITH_KNOTS('',3,(#12614,#12615,#12616,#12617,#12618,
#12619,#12620,#12621,#12622,#12623,#12624,#12625,#12626,#12627,#12628,#12629,
#12630,#12631,#12632,#12633,#12634,#12635,#12636,#12637,#12638,#12639,#12640,
#12641,#12642,#12643,#12644,#12645,#12646,#12647,#12648,#12649,#12650,#12651,
#12652,#12653,#12654,#12655,#12656,#12657,#12658,#12659,#12660,#12661,#12662,
#12663,#12664,#12665,#12666,#12667,#12668,#12669,#12670,#12671,#12672,#12673,
#12674,#12675,#12676,#12677,#12678,#12679,#12680,#12681,#12682,#12683,#12684,
#12685,#12686,#12687,#12688,#12689,#12690,#12691,#12692,#12693,#12694,#12695,
#12696,#12697,#12698,#12699,#12700,#12701,#12702,#12703,#12704,#12705,#12706,
#12707,#12708,#12709,#12710,#12711,#12712,#12713,#12714,#12715,#12716,#12717,
#12718,#12719,#12720,#12721,#12722,#12723,#12724,#12725,#12726,#12727,#12728,
#12729,#12730,#12731,#12732,#12733,#12734,#12735,#12736,#12737,#12738,#12739,
#12740,#12741,#12742,#12743,#12744,#12745,#12746,#12747,#12748,#12749,#12750,
#12751,#12752,#12753,#12754,#12755,#12756,#12757,#12758,#12759,#12760,#12761,
#12762,#12763,#12764,#12765,#12766,#12767,#12768,#12769,#12770,#12771,#12772,
#12773,#12774,#12775,#12776,#12777,#12778,#12779,#12780,#12781,#12782,#12783,
#12784,#12785,#12786,#12787,#12788,#12789,#12790,#12791,#12792,#12793,#12794,
#12795,#12796,#12797,#12798,#12799,#12800,#12801,#12802,#12803,#12804,#12805,
#12806,#12807,#12808,#12809,#12810,#12811,#12812,#12813,#12814,#12815,#12816,
#12817,#12818,#12819,#12820,#12821,#12822,#12823,#12824,#12825,#12826,#12827,
#12828,#12829,#12830,#12831,#12832,#12833,#12834,#12835,#12836,#12837,#12838,
#12839,#12840,#12841,#12842,#12843,#12844,#12845,#12846,#12847,#12848,#12849,
#12850,#12851,#12852,#12853),.UNSPECIFIED.,.F.,.F.,(4,2,2,2,2,2,2,2,2,2,
2,2,2,2,2,2,2,2,2,2,2,2,2,2,2,2,2,2,2,2,2,2,2,2,2,2,2,2,2,2,2,2,2,2,2,2,
2,2,2,2,2,2,2,2,2,2,2,2,2,2,2,2,2,2,2,2,2,2,2,2,2,2,2,2,2,2,2,2,2,2,2,2,
2,2,2,2,2,2,2,2,2,2,2,2,2,2,2,2,2,2,2,2,2,2,2,2,2,2,2,2,2,2,2,2,2,2,2,2,
2,4),(-1.78180985311435,-1.77825266409,-1.77649562722809,-1.77510332126124,
-1.7735695193173,-1.7710640873189,-1.76305956789903,-1.71703756079089,-1.7010450209152,
-1.69908708188978,-1.69811253487568,-1.69733795777592,-1.6964303012081,
-1.69483495978262,-1.68827533000465,-1.6461197212578,-1.63238871561382,
-1.62693790394529,-1.62411304409934,-1.62169750505939,-1.62018353819947,
-1.618785479316,-1.61698186749213,-1.61399304244887,-1.59450378578539,-1.56311469317457,
-1.55095924308641,-1.54471095845163,-1.54319689293844,-1.54231678012067,
-1.54153835441266,-1.54053947441449,-1.53889168835474,-1.52917270690637,
-1.52669317337052,-1.48942391024915,-1.47644110520431,-1.46852824512162,
-1.4661272400671,-1.46461648460115,-1.46321735495467,-1.46140668516399,
-1.45839380912516,-1.43793233570973,-1.39578945689481,-1.38916923725802,
-1.38762677788022,-1.38674032365478,-1.38596298602337,-1.384957529054,-1.38284356986091,
-1.36209628446893,-1.33541790232099,-1.32139939936812,-1.31587012253483,
-1.31173342415358,-1.30986479483821,-1.30846139265048,-1.30714287478308,
-1.3053145953017,-1.30057691663108,-1.29756869105931,-1.29525216762823,
-1.2935076318331,-1.29304438562751,-1.29286411014328,-1.24981118055704,
-1.23916166995177,-1.23344492648263,-1.23197435165953,-1.23110377104137,
-1.23032292026565,-1.22930672681737,-1.22760039788386,-1.21661706353546,
-1.21090926922551,-1.16707132855638,-1.15760298571133,-1.15504700621201,
-1.15350174146035,-1.1521115526828,-1.15033881644478,-1.14670743017367,
-1.14149006082097,-1.09818808706836,-1.08464385753197,-1.07793573764695,
-1.07638668388754,-1.07549868877602,-1.0747214674267,-1.07371809773257,
-1.07161536692718,-1.0528927141948,-1.04541857876941,-1.02129766906186,
-1.0029621897881,-0.999871271680354,-0.998209172260584,-0.996840192106802,
-0.995220529317871,-0.992404377093466,-0.980947526066571,-0.936394277279604,
-0.923052470168436,-0.921065984029007,-0.920085472414105,-0.919310204889693,
-0.91840639763235,-0.916785710074557,-0.909005665452878,-0.864751810349182,
-0.859038195805657,-0.846947967826858,-0.844336349654703,-0.842627479878105,
-0.84124308868024,-0.839656340490345,-0.836913541691698,-0.825129361556584,
-0.801722752441873),.UNSPECIFIED.);
#178=B_SPLINE_CURVE_WITH_KNOTS('',3,(#12855,#12856,#12857,#12858,#12859,
#12860,#12861,#12862,#12863,#12864,#12865,#12866,#12867,#12868,#12869,#12870,
#12871,#12872,#12873,#12874,#12875,#12876,#12877,#12878,#12879,#12880,#12881,
#12882,#12883,#12884,#12885,#12886,#12887,#12888,#12889,#12890,#12891,#12892,
#12893,#12894,#12895,#12896,#12897,#12898,#12899,#12900,#12901,#12902,#12903,
#12904,#12905,#12906,#12907,#12908,#12909,#12910,#12911,#12912,#12913,#12914,
#12915,#12916,#12917,#12918,#12919,#12920,#12921,#12922,#12923,#12924,#12925,
#12926,#12927,#12928,#12929,#12930,#12931,#12932,#12933,#12934,#12935,#12936,
#12937,#12938,#12939,#12940,#12941,#12942,#12943,#12944,#12945,#12946,#12947,
#12948,#12949,#12950,#12951,#12952,#12953,#12954),.UNSPECIFIED.,.F.,.F.,
(4,2,2,2,2,2,2,2,2,2,2,2,2,2,2,2,2,2,2,2,2,2,2,2,2,2,2,2,2,2,2,2,2,2,2,
2,2,2,2,2,2,2,2,2,2,2,2,2,2,4),(-0.179622088260795,-0.172374607901156,-0.170268173383137,
-0.169264380712101,-0.168517786869452,-0.168515300919091,-0.168512838350807,
-0.168510391795445,-0.168507961153133,-0.168505546309182,-0.168503147138293,
-0.168500763541524,-0.168498390557965,-0.168496023095012,-0.16849367057981,
-0.168491332887838,-0.16848900989474,-0.168486701502562,-0.16848440760483,
-0.168482128105852,-0.168479862891079,-0.168477611855461,-0.168475374894854,
-0.168473151915777,-0.168470942801158,-0.167595299574883,-0.166078007122841,
-0.16420799867126,-0.160321337522865,-0.149303453012972,-0.120512283999247,
-0.0969967272189737,-0.0939129301970814,-0.092081289530703,-0.0906785479401655,
-0.0891762227318545,-0.0868147085420767,-0.0792609286287479,-0.0670862848672435,
-0.027603499308661,-0.0219317403002707,-0.0201903824192217,-0.0155585596301801,
-0.01413575877173,-0.0132757739927139,-0.0125272992372366,-0.0117595462868871,
-0.0107489723956134,-0.00913518205521087,-0.000459424761613156),
 .UNSPECIFIED.);
#179=B_SPLINE_CURVE_WITH_KNOTS('',3,(#12955,#12956,#12957,#12958,#12959,
#12960,#12961,#12962,#12963,#12964,#12965,#12966,#12967,#12968,#12969,#12970,
#12971,#12972,#12973,#12974,#12975,#12976,#12977,#12978,#12979,#12980,#12981,
#12982,#12983,#12984,#12985,#12986,#12987,#12988,#12989,#12990,#12991,#12992,
#12993,#12994,#12995,#12996,#12997,#12998,#12999,#13000,#13001,#13002,#13003,
#13004,#13005,#13006,#13007,#13008,#13009,#13010,#13011,#13012,#13013,#13014,
#13015,#13016,#13017,#13018,#13019,#13020,#13021,#13022,#13023,#13024,#13025,
#13026,#13027,#13028,#13029,#13030,#13031,#13032,#13033,#13034,#13035,#13036,
#13037,#13038,#13039,#13040,#13041,#13042,#13043,#13044,#13045,#13046,#13047,
#13048,#13049,#13050,#13051,#13052,#13053,#13054,#13055,#13056,#13057,#13058,
#13059,#13060,#13061,#13062,#13063,#13064,#13065,#13066,#13067,#13068,#13069,
#13070,#13071,#13072,#13073,#13074,#13075,#13076,#13077,#13078,#13079,#13080,
#13081,#13082,#13083,#13084,#13085,#13086,#13087,#13088,#13089,#13090,#13091,
#13092,#13093,#13094,#13095,#13096,#13097,#13098,#13099,#13100,#13101,#13102,
#13103,#13104,#13105,#13106,#13107,#13108,#13109,#13110,#13111,#13112,#13113,
#13114,#13115,#13116,#13117,#13118,#13119,#13120,#13121,#13122,#13123,#13124,
#13125,#13126,#13127,#13128,#13129,#13130,#13131,#13132,#13133,#13134,#13135,
#13136,#13137,#13138,#13139,#13140,#13141,#13142,#13143,#13144,#13145,#13146,
#13147,#13148),.UNSPECIFIED.,.F.,.F.,(4,2,2,2,2,2,2,2,2,2,2,2,2,2,2,2,2,
2,2,2,2,2,2,2,2,2,2,2,2,2,2,2,2,2,2,2,2,2,2,2,2,2,2,2,2,2,2,2,2,2,2,2,2,
2,2,2,2,2,2,2,2,2,2,2,2,2,2,2,2,2,2,2,2,2,2,2,2,2,2,2,2,2,2,2,2,2,2,2,2,
2,2,2,2,2,2,2,4),(-1.96146538068136,-1.9225304253061,-1.90383070095087,
-1.89942562847256,-1.89750917597009,-1.89609808255127,-1.89479241568132,
-1.89266985006171,-1.88738973706424,-1.85528202876609,-1.83649722903484,
-1.82647857779344,-1.82283423001772,-1.82104874699235,-1.81959973659847,
-1.81873361870667,-1.81799537723252,-1.8170076092791,-1.81498337010756,
-1.80034046124051,-1.76891939329666,-1.74853947446037,-1.74392639143348,
-1.74197402508409,-1.74055658200039,-1.73925897767339,-1.73718027004422,
-1.73216192636669,-1.69289498133107,-1.66875524932273,-1.66623411913357,
-1.66486091963958,-1.663950140907,-1.66309578857874,-1.66234179059955,-1.66133569521654,
-1.6592181873244,-1.63767628734376,-1.61167560092799,-1.59267664780642,
-1.58823361519605,-1.58631041073267,-1.58489804135184,-1.58359379629092,
-1.58147937975776,-1.57624784314212,-1.5408468668102,-1.52496766467099,
-1.51182417719274,-1.50907306176176,-1.50795408195252,-1.50715941646251,
-1.50642517799848,-1.5052035419586,-1.50203400902748,-1.5010768211437,-1.49979667073604,
-1.4971082564235,-1.49309684180038,-1.47779986719723,-1.45355051130261,
-1.43499031598387,-1.43189117131455,-1.43022754115955,-1.42885879593576,
-1.4272411739766,-1.42443300338077,-1.41306767427709,-1.40984903105896,
-1.37452851755286,-1.36104362060793,-1.35435460297857,-1.35280708310944,
-1.35191950531526,-1.35114235225081,-1.35013869353996,-1.34851108121659,
-1.33919493806612,-1.33644715284248,-1.2995318673895,-1.28618441373468,
-1.27811248441603,-1.27569414257748,-1.27417944215607,-1.27278140428006,
-1.27097879966951,-1.26799377395149,-1.24866739678322,-1.20562925313045,
-1.19871914053297,-1.19715568099967,-1.19626452508796,-1.19548783489501,
-1.19448949442455,-1.19241245943815,-1.16588454451059,-1.16050672125936),
 .UNSPECIFIED.);
#180=B_SPLINE_CURVE_WITH_KNOTS('',3,(#13154,#13155,#13156,#13157,#13158,
#13159,#13160,#13161,#13162,#13163,#13164,#13165,#13166,#13167,#13168,#13169,
#13170,#13171,#13172,#13173,#13174,#13175,#13176,#13177,#13178,#13179,#13180,
#13181,#13182,#13183,#13184,#13185,#13186,#13187,#13188,#13189,#13190,#13191,
#13192,#13193,#13194,#13195,#13196,#13197,#13198,#13199,#13200,#13201,#13202,
#13203,#13204,#13205,#13206,#13207,#13208,#13209,#13210,#13211,#13212,#13213,
#13214,#13215,#13216,#13217,#13218,#13219,#13220,#13221,#13222,#13223,#13224,
#13225,#13226,#13227,#13228,#13229,#13230,#13231,#13232,#13233,#13234,#13235,
#13236,#13237,#13238,#13239,#13240,#13241,#13242,#13243,#13244,#13245,#13246,
#13247,#13248,#13249,#13250,#13251,#13252,#13253,#13254,#13255,#13256,#13257,
#13258,#13259,#13260,#13261,#13262,#13263,#13264,#13265,#13266,#13267,#13268,
#13269,#13270,#13271,#13272,#13273,#13274,#13275,#13276,#13277,#13278,#13279,
#13280,#13281,#13282,#13283,#13284,#13285,#13286,#13287,#13288,#13289,#13290,
#13291,#13292,#13293,#13294,#13295,#13296,#13297,#13298,#13299,#13300,#13301,
#13302,#13303,#13304,#13305,#13306,#13307,#13308,#13309,#13310,#13311,#13312,
#13313,#13314,#13315,#13316,#13317,#13318,#13319,#13320,#13321,#13322,#13323,
#13324,#13325,#13326,#13327,#13328,#13329,#13330,#13331,#13332,#13333,#13334,
#13335,#13336,#13337,#13338,#13339,#13340,#13341,#13342,#13343,#13344,#13345,
#13346,#13347,#13348,#13349,#13350,#13351,#13352,#13353,#13354,#13355,#13356,
#13357),.UNSPECIFIED.,.F.,.F.,(4,2,2,2,2,2,2,2,2,2,2,2,2,2,2,2,2,2,2,2,
2,2,2,2,2,2,2,2,2,2,2,2,2,2,2,2,2,2,2,2,2,2,2,2,2,2,2,2,2,2,2,2,2,2,2,2,
2,2,2,2,2,2,2,2,2,2,2,2,2,2,2,2,2,2,2,2,2,2,2,2,2,2,2,2,2,2,2,2,2,2,2,2,
2,2,2,2,2,2,2,2,2,4),(-0.801433111655479,-0.775159245849183,-0.754653621656624,
-0.751639129200467,-0.749827706159005,-0.748428132005271,-0.746917033744593,
-0.744515779544564,-0.736604867850778,-0.723625824496955,-0.68635394912236,
-0.683669172705429,-0.674080726758402,-0.672439025902231,-0.671441781763254,
-0.670663342698426,-0.669781751618357,-0.668261822573895,-0.661942496006328,
-0.649581857774969,-0.618223829352296,-0.60925925728251,-0.598150562812303,
-0.595363667354653,-0.593750687981787,-0.592381382022701,-0.59071155589933,
-0.587584360946739,-0.568282944182112,-0.532146905883789,-0.518744541593491,
-0.516756145412135,-0.51577527442042,-0.515000008141656,-0.514096530145747,
-0.512477249976737,-0.504719407655079,-0.460449677449668,-0.454761500524851,
-0.442643609743187,-0.440030185246532,-0.43832079227486,-0.43693641524014,
-0.435350164972444,-0.432609448213555,-0.42085335974348,-0.376363467348406,
-0.363057677502036,-0.361072369490632,-0.360092092164516,-0.359316839800562,
-0.358412854720092,-0.356791360491892,-0.348998186687032,-0.304754729938819,
-0.299025867806436,-0.286952586347072,-0.284342114852897,-0.282633597265193,
-0.281249226451485,-0.281245579387401,-0.281241952243014,-0.281238345312432,
-0.281234758432733,-0.281231191439533,-0.281227644172117,-0.281224116479174,
-0.281220608194223,-0.281217119159661,-0.279649882043694,-0.276976487620036,
-0.273714566257554,-0.267056618791725,-0.221725854512607,-0.218552941149592,
-0.207225331694529,-0.20533928083146,-0.204366423002644,-0.203591471213309,
-0.202681383243968,-0.201032595909647,-0.192895113711643,-0.174371873182415,
-0.143101921734939,-0.131233224080841,-0.128636337198476,-0.126931692005924,
-0.125547106322859,-0.124242488570711,-0.121927955135659,-0.11437317444251,
-0.102135049643601,-0.0876110376321648,-0.0538191250905355,-0.0503915729741181,
-0.0491297206439079,-0.0483872992140738,-0.0475974243730106,-0.0465074923170961,
-0.043932577175537,-0.0403310696103786,-0.000460210966472357),
 .UNSPECIFIED.);
#181=B_SPLINE_CURVE_WITH_KNOTS('',3,(#13358,#13359,#13360,#13361,#13362,
#13363,#13364,#13365,#13366,#13367,#13368,#13369,#13370,#13371,#13372,#13373,
#13374,#13375,#13376,#13377,#13378,#13379,#13380,#13381,#13382,#13383,#13384,
#13385,#13386,#13387,#13388,#13389,#13390,#13391,#13392,#13393,#13394,#13395,
#13396,#13397,#13398,#13399,#13400,#13401,#13402,#13403,#13404,#13405,#13406,
#13407),.UNSPECIFIED.,.F.,.F.,(4,2,2,2,2,2,2,2,2,2,2,2,2,2,2,2,2,2,2,2,
2,2,2,2,4),(-1.96102705992237,-1.94412017883534,-1.93679141301454,-1.93448028336829,
-1.93290767593673,-1.93160159451574,-1.9303582798539,-1.92873284212444,
-1.9258896905923,-1.91409267225893,-1.90663976279395,-1.89712543469352,
-1.86488877597605,-1.85616304049253,-1.85495512329353,-1.85387317308645,
-1.85308518461179,-1.85234141434389,-1.85107051574839,-1.84757984900415,
-1.82011283268145,-1.79749119233811,-1.78650204388423,-1.78183577529276,
-1.78180985311435),.UNSPECIFIED.);
#182=B_SPLINE_CURVE_WITH_KNOTS('',3,(#13408,#13409,#13410,#13411,#13412,
#13413,#13414,#13415,#13416,#13417,#13418,#13419,#13420,#13421,#13422,#13423,
#13424,#13425,#13426,#13427,#13428,#13429,#13430,#13431,#13432,#13433,#13434,
#13435,#13436,#13437,#13438,#13439,#13440,#13441,#13442,#13443,#13444,#13445,
#13446,#13447,#13448,#13449,#13450,#13451,#13452,#13453,#13454,#13455,#13456,
#13457,#13458,#13459,#13460,#13461,#13462,#13463,#13464,#13465,#13466,#13467,
#13468,#13469,#13470,#13471,#13472,#13473,#13474,#13475,#13476,#13477,#13478,
#13479,#13480,#13481,#13482,#13483,#13484,#13485,#13486,#13487,#13488,#13489,
#13490,#13491,#13492,#13493,#13494,#13495,#13496,#13497,#13498,#13499,#13500,
#13501,#13502,#13503,#13504,#13505,#13506,#13507,#13508,#13509,#13510,#13511,
#13512,#13513,#13514,#13515,#13516,#13517,#13518,#13519,#13520,#13521,#13522,
#13523,#13524,#13525,#13526,#13527,#13528,#13529,#13530,#13531,#13532,#13533,
#13534,#13535,#13536,#13537,#13538,#13539,#13540,#13541,#13542,#13543,#13544,
#13545,#13546,#13547,#13548,#13549,#13550,#13551,#13552,#13553,#13554,#13555,
#13556,#13557,#13558,#13559,#13560,#13561,#13562,#13563,#13564,#13565,#13566,
#13567,#13568,#13569,#13570,#13571,#13572,#13573,#13574,#13575,#13576,#13577,
#13578,#13579,#13580,#13581,#13582,#13583,#13584,#13585,#13586,#13587,#13588,
#13589,#13590,#13591,#13592,#13593,#13594,#13595,#13596,#13597,#13598,#13599,
#13600,#13601,#13602,#13603,#13604,#13605,#13606,#13607,#13608,#13609,#13610,
#13611,#13612,#13613,#13614,#13615,#13616,#13617,#13618,#13619,#13620,#13621,
#13622,#13623,#13624,#13625,#13626,#13627,#13628,#13629,#13630,#13631,#13632,
#13633,#13634,#13635,#13636,#13637,#13638,#13639,#13640,#13641,#13642,#13643,
#13644,#13645,#13646,#13647,#13648,#13649,#13650,#13651,#13652,#13653,#13654,
#13655,#13656,#13657,#13658,#13659,#13660,#13661,#13662,#13663,#13664,#13665,
#13666,#13667,#13668,#13669,#13670,#13671,#13672,#13673,#13674,#13675,#13676,
#13677,#13678,#13679,#13680,#13681,#13682,#13683,#13684,#13685,#13686,#13687,
#13688,#13689,#13690,#13691,#13692,#13693,#13694,#13695,#13696,#13697,#13698,
#13699,#13700,#13701,#13702,#13703,#13704,#13705,#13706,#13707,#13708,#13709,
#13710,#13711,#13712,#13713,#13714,#13715,#13716,#13717,#13718,#13719,#13720,
#13721,#13722,#13723,#13724,#13725,#13726,#13727,#13728,#13729,#13730,#13731,
#13732,#13733,#13734,#13735,#13736,#13737,#13738,#13739,#13740,#13741,#13742,
#13743,#13744,#13745,#13746,#13747,#13748,#13749,#13750,#13751,#13752,#13753,
#13754,#13755,#13756,#13757,#13758,#13759,#13760,#13761,#13762,#13763,#13764,
#13765,#13766,#13767,#13768,#13769,#13770,#13771,#13772,#13773,#13774,#13775,
#13776,#13777,#13778,#13779,#13780,#13781,#13782,#13783,#13784,#13785,#13786,
#13787,#13788,#13789,#13790,#13791,#13792,#13793,#13794,#13795,#13796,#13797,
#13798,#13799),.UNSPECIFIED.,.F.,.F.,(4,2,2,2,2,2,2,2,2,2,2,2,2,2,2,2,2,
2,2,2,2,2,2,2,2,2,2,2,2,2,2,2,2,2,2,2,2,2,2,2,2,2,2,2,2,2,2,2,2,2,2,2,2,
2,2,2,2,2,2,2,2,2,2,2,2,2,2,2,2,2,2,2,2,2,2,2,2,2,2,2,2,2,2,2,2,2,2,2,2,
2,2,2,2,2,2,2,2,2,2,2,2,2,2,2,2,2,2,2,2,2,2,2,2,2,2,2,2,2,2,2,2,2,2,2,2,
2,2,2,2,2,2,2,2,2,2,2,2,2,2,2,2,2,2,2,2,2,2,2,2,2,2,2,2,2,2,2,2,2,2,2,2,
2,2,2,2,2,2,2,2,2,2,2,2,2,2,2,2,2,2,2,2,2,2,2,2,2,2,2,2,2,2,2,2,2,2,4),
(-1.16050672125936,-1.13658797771447,-1.12325146763907,-1.12040624604766,
-1.11879714613831,-1.11755326941281,-1.11593166924341,-1.11310683508528,
-1.1015440333472,-1.09533917016703,-1.05141500268395,-1.04318894357646,
-1.04154187277803,-1.04063234732588,-1.03985764275991,-1.03888481974403,
-1.03699803944337,-1.02564064794427,-1.01216043658711,-0.981311096955009,
-0.967844709397715,-0.9651434330647,-0.963406854909695,-0.962020152090692,
-0.960452432223601,-0.957796086446112,-0.947157022676203,-0.901820982983431,
-0.89681332168628,-0.887740070346934,-0.886124703940506,-0.885124530860051,
-0.884347469966316,-0.88345706668008,-0.881897726581934,-0.875050001580883,
-0.832241811488523,-0.812639565198644,-0.809646851508131,-0.807841660840296,
-0.806442845716016,-0.804928529580441,-0.802513456431045,-0.794477182880794,
-0.781211689771461,-0.743840597244101,-0.732227967153351,-0.730330709843061,
-0.72935555838399,-0.728580614859418,-0.727672674197026,-0.726033217740437,
-0.71794100239879,-0.673932163862546,-0.667907050424341,-0.656151911367998,
-0.653311071940292,-0.651685627219854,-0.650441615056989,-0.648835662942649,
-0.646005686365083,-0.632921510287751,-0.604650023138001,-0.587407689850453,
-0.576482898555614,-0.574778643868645,-0.573762972623271,-0.572982091572767,
-0.572111002620281,-0.57063855928568,-0.564901965089997,-0.554201216951262,
-0.510334353318773,-0.50726942733268,-0.500753020889885,-0.498015224500325,
-0.496267505748658,-0.494879818212073,-0.49331936623797,-0.490695566177447,
-0.480452682402657,-0.434796051841406,-0.430598756339604,-0.42066195834132,
-0.419002917052987,-0.418000489194207,-0.417221333861661,-0.416342687777439,
-0.414836343440348,-0.408691245774602,-0.396841466417074,-0.365235547677384,
-0.345528611545284,-0.342533293469695,-0.340727335627656,-0.339328402285089,
-0.339323857935652,-0.339319352370189,-0.339314885236623,-0.33931045619602,
-0.339306064898714,-0.339301711008387,-0.339297394170184,-0.339293114045987,
-0.339288870311452,-0.339284662631023,-0.339280490664529,-0.339276354092131,
-0.33927225258856,-0.339268185852101,-0.339264153544142,-0.339260155354349,
-0.339256190976604,-0.339252260114969,-0.339248362443475,-0.339244497673467,
-0.339240665514632,-0.339236865653649,-0.339233097789755,-0.339229361650208,
-0.339225656940361,-0.339221983369571,-0.339218340651027,-0.339214728527488,
-0.339211146714534,-0.339207594938659,-0.339204072920932,-0.33920058038965,
-0.339197117075535,-0.33919368272291,-0.339190277075752,-0.339186899854147,
-0.339183550804388,-0.339180229696334,-0.33917693626758,-0.339173670264504,
-0.339171163995327,-0.339168662973366,-0.33916616678394,-0.339163675419185,
-0.339161188874753,-0.339158707143298,-0.339156230204622,-0.339153758026079,
-0.339151290602902,-0.339148827921157,-0.339146369982959,-0.339143916767275,
-0.339141468250363,-0.339139024431141,-0.339136585286716,-0.339134150817317,
-0.339131721004108,-0.339129295813795,-0.339126875245179,-0.339124459281576,
-0.339122047936093,-0.33911964119357,-0.3391172390237,-0.339114841390878,
-0.339112448302961,-0.339110059760955,-0.33910767572495,-0.339105296186166,
-0.339102921133349,-0.339100550561894,-0.337545801628347,-0.3349011609442,
-0.331699631582162,-0.325211962534818,-0.280588976144251,-0.276869237098302,
-0.265098134172531,-0.263194700597936,-0.262218225312468,-0.261443198504544,
-0.260536279385063,-0.258901495635772,-0.251003341027479,-0.20685139100601,
-0.201057954306407,-0.189047947845654,-0.186441624012335,-0.184734327430287,
-0.183349953970372,-0.183338368875809,-0.183327191713962,-0.183316408267552,
-0.183306003692731,-0.183295963745638,-0.183286276051788,-0.183276928768914,
-0.183267906941564,-0.183259198518953,-0.181669373545164,-0.179852073555682),
 .UNSPECIFIED.);
#183=B_SPLINE_CURVE_WITH_KNOTS('',3,(#13804,#13805,#13806,#13807,#13808,
#13809,#13810,#13811,#13812,#13813,#13814,#13815,#13816,#13817,#13818,#13819,
#13820,#13821,#13822,#13823,#13824,#13825,#13826,#13827,#13828,#13829,#13830,
#13831,#13832,#13833,#13834,#13835,#13836,#13837,#13838,#13839,#13840,#13841,
#13842,#13843,#13844,#13845,#13846,#13847,#13848,#13849,#13850,#13851,#13852,
#13853,#13854,#13855,#13856,#13857,#13858,#13859,#13860,#13861,#13862,#13863,
#13864,#13865,#13866,#13867,#13868,#13869,#13870,#13871,#13872,#13873,#13874,
#13875,#13876,#13877,#13878,#13879,#13880,#13881,#13882,#13883,#13884,#13885,
#13886,#13887,#13888,#13889,#13890,#13891,#13892,#13893,#13894,#13895,#13896,
#13897,#13898,#13899,#13900,#13901,#13902,#13903,#13904,#13905,#13906,#13907,
#13908,#13909,#13910,#13911,#13912,#13913,#13914,#13915,#13916,#13917,#13918,
#13919,#13920,#13921,#13922,#13923,#13924,#13925,#13926,#13927,#13928,#13929,
#13930,#13931,#13932,#13933,#13934,#13935,#13936,#13937,#13938,#13939,#13940,
#13941,#13942,#13943,#13944,#13945,#13946,#13947,#13948,#13949,#13950,#13951,
#13952,#13953,#13954,#13955,#13956,#13957,#13958,#13959,#13960,#13961,#13962,
#13963,#13964,#13965,#13966,#13967,#13968,#13969,#13970,#13971,#13972,#13973,
#13974,#13975,#13976,#13977,#13978,#13979,#13980,#13981,#13982,#13983,#13984,
#13985,#13986,#13987,#13988,#13989,#13990,#13991,#13992,#13993,#13994,#13995,
#13996,#13997,#13998,#13999,#14000,#14001,#14002,#14003,#14004,#14005,#14006,
#14007,#14008,#14009,#14010,#14011,#14012,#14013,#14014,#14015,#14016,#14017,
#14018,#14019,#14020,#14021,#14022,#14023,#14024,#14025,#14026,#14027,#14028,
#14029,#14030,#14031,#14032,#14033,#14034,#14035,#14036,#14037,#14038,#14039,
#14040,#14041,#14042,#14043,#14044,#14045,#14046,#14047,#14048,#14049),
 .UNSPECIFIED.,.F.,.F.,(4,2,2,2,2,2,2,2,2,2,2,2,2,2,2,2,2,2,2,2,2,2,2,2,
2,2,2,2,2,2,2,2,2,2,2,2,2,2,2,2,2,2,2,2,2,2,2,2,2,2,2,2,2,2,2,2,2,2,2,2,
2,2,2,2,2,2,2,2,2,2,2,2,2,2,2,2,2,2,2,2,2,2,2,2,2,2,2,2,2,2,2,2,2,2,2,2,
2,2,2,2,2,2,2,2,2,2,2,2,2,2,2,2,2,2,2,2,2,2,2,2,2,2,4),(-1.78170741026359,
-1.77139420245484,-1.76332743792697,-1.76168306777715,-1.7607741496317,
-1.75999942313482,-1.75902587233313,-1.75713561890463,-1.74569030602177,
-1.74260851916196,-1.69734956609914,-1.69070338081476,-1.68744577678322,
-1.68477757017397,-1.68321072749998,-1.68320722821,-1.68320370964983,-1.6832001716673,
-1.68319661410376,-1.68319303680128,-1.68318943959573,-1.6831858223304,
-1.68318218484626,-1.68317852720448,-1.68179464445203,-1.68008686597183,
-1.67747775836826,-1.66541595601263,-1.65967617399006,-1.61542964749078,
-1.60762790099442,-1.60600618574291,-1.60510230907244,-1.60432728938023,
-1.60334749069679,-1.60136374784442,-1.58809008197448,-1.5436734689132,
-1.53186727292633,-1.52912347545126,-1.52753678829489,-1.52615282920023,
-1.52444497983836,-1.52183580733392,-1.5097745337863,-1.50403334230908,
-1.45978506202724,-1.45198194850415,-1.45036008520169,-1.44945614518642,
-1.4486810829916,-1.44770124572058,-1.44571747422532,-1.43244557578626,
-1.38803077178286,-1.37621776566786,-1.37347337658652,-1.37188650374007,
-1.37050247559103,-1.36879466040507,-1.36618576215494,-1.3541299962284,
-1.34838292660021,-1.30413594753992,-1.29632765893282,-1.29470541546936,
-1.29380136148975,-1.29302626189234,-1.29204645466502,-1.29006299659631,
-1.27680317922937,-1.2324077662769,-1.22056285708051,-1.21781609678637,
-1.21622864658763,-1.21484458601124,-1.21313733586261,-1.21053042536963,
-1.19850527800456,-1.19272976835506,-1.14849934940822,-1.14066682387664,
-1.13904304144341,-1.13813862083536,-1.13736350909541,-1.13638407377269,
-1.13440263230767,-1.1212058383141,-1.07691420359242,-1.06491541041669,
-1.06215772345684,-1.06056781406325,-1.05918389020121,-1.05747972968807,
-1.0548829504671,-1.04300428626409,-1.03568456526173,-0.991982193092347,
-0.984910625319681,-0.983335839248477,-0.982442119419145,-0.981665681534951,
-0.98067089988623,-0.978612390404106,-0.975904803983002,-0.947661542595715,
-0.913237037660929,-0.907979562174086,-0.905860392343265,-0.904554998790264,
-0.903142774435695,-0.901222247930651,-0.896796482759925,-0.877935781650044,
-0.851356180149381,-0.830191596028536,-0.828075088674039,-0.827068998675036,
-0.826291439579715,-0.825405024502319,-0.823863323342374,-0.817256504014559,
-0.801433111655479),.UNSPECIFIED.);
#184=B_SPLINE_CURVE_WITH_KNOTS('',3,(#14051,#14052,#14053,#14054,#14055,
#14056,#14057,#14058,#14059,#14060,#14061,#14062,#14063,#14064,#14065,#14066,
#14067,#14068,#14069,#14070,#14071,#14072,#14073,#14074,#14075,#14076,#14077,
#14078,#14079,#14080,#14081,#14082,#14083,#14084,#14085,#14086,#14087,#14088,
#14089,#14090,#14091,#14092,#14093,#14094,#14095,#14096,#14097,#14098,#14099,
#14100),.UNSPECIFIED.,.F.,.F.,(4,2,2,2,2,2,2,2,2,2,2,2,2,2,2,2,2,2,2,2,
2,2,2,2,4),(-0.179852073555682,-0.178878435810792,-0.175450539953574,-0.168316256847422,
-0.14771672789062,-0.111178057748267,-0.108072550368483,-0.106861072900725,
-0.106128620433403,-0.105332032945858,-0.104203869302599,-0.101397602678173,
-0.0892071044472608,-0.0586364436391121,-0.0496241211686591,-0.0456935464141843,
-0.0334250198293235,-0.030800780394571,-0.0290879388733611,-0.0277031758227639,
-0.0264000299616105,-0.0248463918548199,-0.0225820312570058,-0.0156371952265505,
-0.000459509676940365),.UNSPECIFIED.);
#185=B_SPLINE_CURVE_WITH_KNOTS('',3,(#14101,#14102,#14103,#14104,#14105,
#14106,#14107,#14108,#14109,#14110,#14111,#14112,#14113,#14114,#14115,#14116,
#14117,#14118,#14119,#14120,#14121,#14122,#14123,#14124,#14125,#14126,#14127,
#14128,#14129,#14130,#14131,#14132,#14133,#14134,#14135,#14136,#14137,#14138,
#14139,#14140,#14141,#14142,#14143,#14144,#14145,#14146,#14147,#14148,#14149,
#14150,#14151,#14152,#14153,#14154,#14155,#14156,#14157,#14158,#14159,#14160,
#14161,#14162,#14163,#14164,#14165,#14166,#14167,#14168,#14169,#14170,#14171,
#14172,#14173,#14174,#14175,#14176,#14177,#14178,#14179,#14180,#14181,#14182,
#14183,#14184,#14185,#14186,#14187,#14188,#14189,#14190,#14191,#14192,#14193,
#14194,#14195,#14196,#14197,#14198,#14199,#14200,#14201,#14202,#14203,#14204,
#14205,#14206,#14207,#14208,#14209,#14210,#14211,#14212,#14213,#14214,#14215,
#14216,#14217,#14218,#14219,#14220,#14221,#14222,#14223,#14224,#14225,#14226,
#14227,#14228,#14229,#14230,#14231,#14232,#14233,#14234,#14235,#14236,#14237,
#14238,#14239,#14240,#14241,#14242,#14243,#14244,#14245,#14246,#14247,#14248,
#14249,#14250,#14251,#14252,#14253,#14254,#14255,#14256,#14257,#14258,#14259,
#14260,#14261,#14262,#14263,#14264,#14265,#14266,#14267,#14268,#14269,#14270,
#14271,#14272,#14273,#14274,#14275,#14276,#14277,#14278,#14279,#14280,#14281,
#14282,#14283,#14284,#14285,#14286,#14287,#14288,#14289,#14290,#14291,#14292,
#14293,#14294,#14295,#14296,#14297,#14298,#14299,#14300),.UNSPECIFIED.,
 .F.,.F.,(4,2,2,2,2,2,2,2,2,2,2,2,2,2,2,2,2,2,2,2,2,2,2,2,2,2,2,2,2,2,2,
2,2,2,2,2,2,2,2,2,2,2,2,2,2,2,2,2,2,2,2,2,2,2,2,2,2,2,2,2,2,2,2,2,2,2,2,
2,2,2,2,2,2,2,2,2,2,2,2,2,2,2,2,2,2,2,2,2,2,2,2,2,2,2,2,2,2,2,2,4),(-1.96069987759182,
-1.91845884062044,-1.91490970624029,-1.91236466372798,-1.91128050011752,
-1.91049220108497,-1.90974918646458,-1.90848186321831,-1.90501377579469,
-1.87177032517842,-1.8582009874233,-1.84507642640989,-1.83712775120393,
-1.83477211187913,-1.8334660218736,-1.83222279387898,-1.8305981325039,-1.82775803702758,
-1.81599755965749,-1.80998148156486,-1.76597016925142,-1.75789691373428,
-1.75625265022867,-1.75534397892635,-1.75456958037236,-1.75359660568952,
-1.75170796113064,-1.74028926353391,-1.73718781016408,-1.6919285709932,
-1.68528011084203,-1.68202205084216,-1.67935006559657,-1.67778456422658,
-1.67778108423104,-1.6777775849879,-1.67777406632914,-1.67777052811106,
-1.67776697017973,-1.67776339236119,-1.67775979449114,-1.67775617640286,
-1.6777525379283,-1.67774887911552,-1.67636536954792,-1.67465562350651,
-1.67203899064432,-1.6598561591188,-1.6542247615872,-1.60997465978654,-1.60220583877028,
-1.60058658823094,-1.59968347174851,-1.59890872933706,-1.59792881529424,
-1.59594332484397,-1.5825994599447,-1.53811128811494,-1.52643687298707,
-1.5237032454324,-1.52211919470659,-1.52073560529017,-1.5190257293684,-1.51640883951757,
-1.50422368749246,-1.49859343623657,-1.45433981757096,-1.44657185353636,
-1.44495259156031,-1.44404944182408,-1.44327465430576,-1.44229466193643,
-1.44030894315071,-1.42696074276319,-1.38246369429336,-1.3707975735219,
-1.36806443776634,-1.36648044043244,-1.36509675958176,-1.36338659265735,
-1.3607689252673,-1.34857373642418,-1.34295150844639,-1.29868945320575,
-1.290928442227,-1.2893095426576,-1.2884064412267,-1.28763160022206,-1.28665141838019,
-1.28466491682819,-1.27129536869087,-1.22675887188467,-1.21514368919964,
-1.2124141293189,-1.21083086477891,-1.20944702446029,-1.20773562856479,
-1.20511415254834,-1.19287010978845,-1.15986353876316),.UNSPECIFIED.);
#186=B_SPLINE_CURVE_WITH_KNOTS('',3,(#14306,#14307,#14308,#14309,#14310,
#14311,#14312,#14313,#14314,#14315,#14316,#14317,#14318,#14319,#14320,#14321,
#14322,#14323,#14324,#14325,#14326,#14327,#14328,#14329,#14330,#14331,#14332,
#14333,#14334,#14335,#14336,#14337,#14338,#14339,#14340,#14341,#14342,#14343,
#14344,#14345,#14346,#14347,#14348,#14349,#14350,#14351,#14352,#14353,#14354,
#14355,#14356,#14357,#14358,#14359,#14360,#14361,#14362,#14363,#14364,#14365,
#14366,#14367,#14368,#14369,#14370,#14371,#14372,#14373,#14374,#14375,#14376,
#14377,#14378,#14379,#14380,#14381,#14382,#14383,#14384,#14385,#14386,#14387,
#14388,#14389,#14390,#14391,#14392,#14393,#14394,#14395,#14396,#14397,#14398,
#14399,#14400,#14401,#14402,#14403,#14404,#14405,#14406,#14407,#14408,#14409,
#14410,#14411,#14412,#14413,#14414,#14415,#14416,#14417,#14418,#14419,#14420,
#14421,#14422,#14423,#14424,#14425,#14426,#14427,#14428,#14429,#14430,#14431,
#14432,#14433,#14434,#14435,#14436,#14437,#14438,#14439,#14440,#14441,#14442,
#14443,#14444,#14445,#14446,#14447,#14448,#14449,#14450,#14451,#14452,#14453,
#14454,#14455,#14456,#14457,#14458,#14459,#14460,#14461,#14462,#14463,#14464,
#14465,#14466,#14467,#14468,#14469,#14470,#14471,#14472,#14473,#14474,#14475,
#14476,#14477,#14478,#14479,#14480,#14481,#14482,#14483,#14484,#14485,#14486,
#14487,#14488,#14489,#14490,#14491,#14492,#14493,#14494,#14495,#14496,#14497,
#14498,#14499,#14500,#14501,#14502,#14503),.UNSPECIFIED.,.F.,.F.,(4,2,2,
2,2,2,2,2,2,2,2,2,2,2,2,2,2,2,2,2,2,2,2,2,2,2,2,2,2,2,2,2,2,2,2,2,2,2,2,
2,2,2,2,2,2,2,2,2,2,2,2,2,2,2,2,2,2,2,2,2,2,2,2,2,2,2,2,2,2,2,2,2,2,2,2,
2,2,2,2,2,2,2,2,2,2,2,2,2,2,2,2,2,2,2,2,2,2,2,4),(-0.801736014421406,-0.799581811946282,
-0.786209666041104,-0.74936065287489,-0.746990920996527,-0.737255478959455,
-0.735606057239272,-0.734606350787257,-0.733827381547235,-0.732946759298924,
-0.731432067556231,-0.725184478761221,-0.713037220202634,-0.681652814287474,
-0.662139640151576,-0.65914878586409,-0.657343928333994,-0.655944900135632,
-0.654429880668577,-0.652012656973972,-0.643959550155184,-0.630655923318393,
-0.593444004693946,-0.581745016771518,-0.579844087335122,-0.578868014973784,
-0.578092843662842,-0.577185205425138,-0.575547724460788,-0.567493632303464,
-0.523440945880881,-0.5173900401822,-0.505666078908615,-0.502827366741388,
-0.501202184643843,-0.499957868908011,-0.498350926083002,-0.495517455474805,
-0.482384326914722,-0.453918733901765,-0.444577110488416,-0.436139833649767,
-0.425951636746667,-0.424280237635206,-0.423274079479185,-0.422494329466205,
-0.421617580490128,-0.420120225711973,-0.414088640926143,-0.402564846887454,
-0.371379915070074,-0.350845008934168,-0.347828888464038,-0.346016659672986,
-0.344616564658634,-0.343105004868396,-0.340703233739555,-0.332792583503428,
-0.319815939748242,-0.276376738732361,-0.275623251472852,-0.273817368571057,
-0.269447399524127,-0.268055445688625,-0.267202113744547,-0.266415215595033,
-0.265343097293166,-0.263029103693493,-0.245890571718042,-0.203821008599721,
-0.198910163307287,-0.196251849981033,-0.192581081170869,-0.190763692728898,
-0.18944754718031,-0.188041564262708,-0.186198210194599,-0.182175397196218,
-0.176782914666108,-0.163267578331553,-0.141761351985546,-0.11492981288647,
-0.11285975016619,-0.11186249878683,-0.111085596799273,-0.110192985811116,
-0.108624087553022,-0.101756566331568,-0.0819348749466729,-0.0640483815359052,
-0.0396378439030753,-0.0365365080531776,-0.0346993352740578,-0.0332951743186159,
-0.0319991340209431,-0.0305265880276274,-0.0284625165163476,-0.0209035907064299,
-0.000459615136305543),.UNSPECIFIED.);
#187=B_SPLINE_CURVE_WITH_KNOTS('',3,(#14504,#14505,#14506,#14507,#14508,
#14509,#14510,#14511,#14512,#14513,#14514,#14515,#14516,#14517,#14518,#14519,
#14520,#14521,#14522,#14523,#14524,#14525,#14526,#14527,#14528,#14529,#14530,
#14531,#14532,#14533,#14534,#14535,#14536,#14537,#14538,#14539,#14540,#14541,
#14542,#14543,#14544,#14545),.UNSPECIFIED.,.F.,.F.,(4,2,2,2,2,2,2,2,2,2,
2,2,2,2,2,2,2,2,2,2,4),(-1.96080348278997,-1.92112421592769,-1.91900621949408,
-1.91779070717829,-1.91670329693965,-1.91591411202519,-1.91517143078537,
-1.91390718425261,-1.91046181988859,-1.87688943572253,-1.85901222475556,
-1.8488083647261,-1.84221430945411,-1.84001055546783,-1.83871197973006,
-1.83732281946126,-1.83556117019383,-1.83277779482363,-1.81793256979077,
-1.78965448236495,-1.78170741026359),.UNSPECIFIED.);
#188=B_SPLINE_CURVE_WITH_KNOTS('',3,(#14546,#14547,#14548,#14549,#14550,
#14551,#14552,#14553,#14554,#14555,#14556,#14557,#14558,#14559,#14560,#14561,
#14562,#14563,#14564,#14565,#14566,#14567,#14568,#14569,#14570,#14571,#14572,
#14573,#14574,#14575,#14576,#14577,#14578,#14579,#14580,#14581,#14582,#14583,
#14584,#14585,#14586,#14587,#14588,#14589,#14590,#14591,#14592,#14593,#14594,
#14595,#14596,#14597,#14598,#14599,#14600,#14601,#14602,#14603,#14604,#14605,
#14606,#14607,#14608,#14609,#14610,#14611,#14612,#14613,#14614,#14615,#14616,
#14617,#14618,#14619,#14620,#14621,#14622,#14623,#14624,#14625,#14626,#14627,
#14628,#14629,#14630,#14631,#14632,#14633,#14634,#14635,#14636,#14637,#14638,
#14639,#14640,#14641,#14642,#14643,#14644,#14645,#14646,#14647,#14648,#14649,
#14650,#14651,#14652,#14653,#14654,#14655,#14656,#14657,#14658,#14659,#14660,
#14661,#14662,#14663,#14664,#14665,#14666,#14667,#14668,#14669,#14670,#14671,
#14672,#14673,#14674,#14675,#14676,#14677,#14678,#14679,#14680,#14681,#14682,
#14683,#14684,#14685,#14686,#14687,#14688,#14689,#14690,#14691,#14692,#14693,
#14694,#14695,#14696,#14697,#14698,#14699,#14700,#14701,#14702,#14703,#14704,
#14705,#14706,#14707,#14708,#14709,#14710,#14711,#14712,#14713,#14714,#14715,
#14716,#14717,#14718,#14719,#14720,#14721,#14722,#14723,#14724,#14725,#14726,
#14727,#14728,#14729,#14730,#14731,#14732,#14733,#14734,#14735,#14736,#14737,
#14738,#14739,#14740,#14741,#14742,#14743,#14744,#14745,#14746,#14747,#14748,
#14749,#14750,#14751,#14752,#14753,#14754,#14755,#14756,#14757,#14758,#14759,
#14760,#14761,#14762,#14763,#14764,#14765,#14766,#14767,#14768,#14769,#14770,
#14771,#14772,#14773,#14774,#14775,#14776,#14777,#14778,#14779,#14780,#14781,
#14782,#14783,#14784,#14785,#14786,#14787,#14788,#14789,#14790,#14791,#14792,
#14793,#14794,#14795,#14796,#14797,#14798,#14799,#14800,#14801),
 .UNSPECIFIED.,.F.,.F.,(4,2,2,2,2,2,2,2,2,2,2,2,2,2,2,2,2,2,2,2,2,2,2,2,
2,2,2,2,2,2,2,2,2,2,2,2,2,2,2,2,2,2,2,2,2,2,2,2,2,2,2,2,2,2,2,2,2,2,2,2,
2,2,2,2,2,2,2,2,2,2,2,2,2,2,2,2,2,2,2,2,2,2,2,2,2,2,2,2,2,2,2,2,2,2,2,2,
2,2,2,2,2,2,2,2,2,2,2,2,2,2,2,2,2,2,2,2,2,2,2,2,2,2,2,2,2,2,2,4),(-1.15986353876316,
-1.15495867850168,-1.14175904705784,-1.1351629966844,-1.13362261718722,
-1.13273677987422,-1.13195960835742,-1.13095388491762,-1.12883766586569,
-1.10740677657844,-1.08131814215635,-1.06231067802686,-1.05786699876735,
-1.05594391764032,-1.05453179125116,-1.05322787780649,-1.0511142389345,
-1.04588581019901,-1.0104321745147,-0.980666401933017,-0.978460612453208,
-0.977448638450662,-0.976668587876089,-0.975796190960301,-0.97431663989005,
-0.968490849648887,-0.957541774780541,-0.936340089929828,-0.905229067644997,
-0.901803915865218,-0.900049503700995,-0.898661637452001,-0.89710637963854,
-0.894504186833417,-0.884507856564803,-0.839507550004001,-0.836515338582123,
-0.834012864181881,-0.824432458371408,-0.822791485487271,-0.821794611158168,
-0.821016417682501,-0.820135068691051,-0.818615486547449,-0.812296704528674,
-0.799936473572604,-0.76856760039765,-0.759601643664272,-0.748500022717946,
-0.745714253073186,-0.7441018269715,-0.742732935527723,-0.74106354982356,
-0.737936995467345,-0.718634870499409,-0.68250151589321,-0.669094006890376,
-0.667105849646672,-0.666125202821074,-0.665350168083612,-0.664447035633299,
-0.662828574539928,-0.65507860489707,-0.610820297515902,-0.605211207037558,
-0.593002979424579,-0.59038394479401,-0.588673086537345,-0.587288988968702,
-0.585704671020448,-0.582971379341359,-0.571311078773968,-0.52676947647019,
-0.513406452537092,-0.511419672278857,-0.510439275763811,-0.509664229016491,
-0.508760841517006,-0.507141322659481,-0.499374944175718,-0.455127672194173,
-0.449500261110734,-0.437311781993052,-0.434694000353402,-0.432983490301602,
-0.431599362279075,-0.430014666872687,-0.427279857768263,-0.4155996636971,
-0.371069940060048,-0.357714094278084,-0.355727480084304,-0.354747091231235,
-0.35397201418579,-0.353068549603149,-0.351448788432619,-0.34367927845436,
-0.299432310379321,-0.293801497053899,-0.281616019753565,-0.278998361741958,
-0.27728785033777,-0.275903666698296,-0.275899970384863,-0.275896294307179,
-0.275892638723789,-0.275889003472613,-0.275885388368658,-0.275881793268624,
-0.275878218012326,-0.275874662428703,-0.275871126379079,-0.275867609688949,
-0.27430115952195,-0.27163961612077,-0.268388698231828,-0.261761342997514,
-0.216576682819282,-0.214178274703862,-0.210534877081703,-0.201660088246841,
-0.200055481560891,-0.199058586684916,-0.198281891664026,-0.197389451716405,
-0.195852238546242,-0.189244216540455,-0.179585755313572),.UNSPECIFIED.);
#189=B_SPLINE_CURVE_WITH_KNOTS('',3,(#14806,#14807,#14808,#14809,#14810,
#14811,#14812,#14813,#14814,#14815,#14816,#14817,#14818,#14819,#14820,#14821,
#14822,#14823,#14824,#14825,#14826,#14827,#14828,#14829,#14830,#14831,#14832,
#14833,#14834,#14835,#14836,#14837,#14838,#14839,#14840,#14841,#14842,#14843,
#14844,#14845,#14846,#14847,#14848,#14849,#14850,#14851,#14852,#14853,#14854,
#14855,#14856,#14857,#14858,#14859,#14860,#14861,#14862,#14863,#14864,#14865,
#14866,#14867,#14868,#14869,#14870,#14871,#14872,#14873,#14874,#14875,#14876,
#14877,#14878,#14879,#14880,#14881,#14882,#14883,#14884,#14885,#14886,#14887,
#14888,#14889,#14890,#14891,#14892,#14893,#14894,#14895,#14896,#14897,#14898,
#14899,#14900,#14901,#14902,#14903,#14904,#14905,#14906,#14907,#14908,#14909,
#14910,#14911,#14912,#14913,#14914,#14915,#14916,#14917,#14918,#14919,#14920,
#14921,#14922,#14923,#14924,#14925,#14926,#14927,#14928,#14929,#14930,#14931,
#14932,#14933,#14934,#14935,#14936,#14937,#14938,#14939,#14940,#14941,#14942,
#14943,#14944,#14945,#14946,#14947,#14948,#14949,#14950,#14951,#14952,#14953,
#14954,#14955,#14956,#14957,#14958,#14959,#14960,#14961,#14962,#14963,#14964,
#14965,#14966,#14967,#14968,#14969,#14970,#14971,#14972,#14973,#14974,#14975,
#14976,#14977,#14978,#14979,#14980,#14981,#14982,#14983,#14984,#14985,#14986,
#14987,#14988,#14989,#14990,#14991,#14992,#14993,#14994,#14995,#14996,#14997,
#14998,#14999,#15000,#15001,#15002,#15003,#15004,#15005,#15006,#15007,#15008,
#15009,#15010,#15011,#15012,#15013,#15014,#15015,#15016,#15017,#15018,#15019,
#15020,#15021,#15022,#15023,#15024,#15025,#15026,#15027,#15028,#15029,#15030,
#15031,#15032,#15033,#15034,#15035,#15036,#15037,#15038,#15039,#15040,#15041,
#15042,#15043,#15044,#15045,#15046,#15047),.UNSPECIFIED.,.F.,.F.,(4,2,2,
2,2,2,2,2,2,2,2,2,2,2,2,2,2,2,2,2,2,2,2,2,2,2,2,2,2,2,2,2,2,2,2,2,2,2,2,
2,2,2,2,2,2,2,2,2,2,2,2,2,2,2,2,2,2,2,2,2,2,2,2,2,2,2,2,2,2,2,2,2,2,2,2,
2,2,2,2,2,2,2,2,2,2,2,2,2,2,2,2,2,2,2,2,2,2,2,2,2,2,2,2,2,2,2,2,2,2,2,2,
2,2,2,2,2,2,2,2,2,4),(-1.78190244653125,-1.77200868256019,-1.75328004368102,
-1.74887061521904,-1.74695295631717,-1.74554123240277,-1.74423516243715,
-1.74211234313619,-1.73683348299684,-1.70421673361218,-1.68584745493587,
-1.67588936352327,-1.67225964458583,-1.67047911262385,-1.66904226233087,
-1.66822238692452,-1.66744721360907,-1.66646723515569,-1.66448317552644,
-1.6512092584759,-1.60678788985221,-1.59497347602076,-1.59222871393679,
-1.59064161815708,-1.5892573912631,-1.58754932530048,-1.58494003366211,
-1.57288225332685,-1.56713461767231,-1.52288112234591,-1.51507193410924,
-1.51344947154688,-1.51254529093412,-1.51177007997497,-1.51079012839565,
-1.50880636641984,-1.49554405586124,-1.45931070509532,-1.44649224817082,
-1.43865066013505,-1.43625682861186,-1.43474726379943,-1.43334695256219,
-1.43153152701537,-1.42850368046637,-1.407494623618,-1.37664021955004,-1.36521899408719,
-1.35922464044709,-1.35773055345891,-1.35685465848211,-1.35607494105831,
-1.35506789137943,-1.35339306487235,-1.34312904726704,-1.32725767432596,
-1.30297643698827,-1.29064042446784,-1.28301303048465,-1.28064293414308,
-1.27913854391298,-1.27773623516422,-1.27590853323477,-1.27283881580251,
-1.25004440996076,-1.22063140048047,-1.20950557322381,-1.20361609010587,
-1.20213064080079,-1.2012566380236,-1.20047642961679,-1.19946591263889,
-1.19777935925272,-1.18727064336203,-1.17162391919845,-1.1473553115595,
-1.12876414179781,-1.12566291869733,-1.12399844276655,-1.12262913782025,
-1.1210110117645,-1.11820235209479,-1.10683968477102,-1.1004529000864,-1.05657106709834,
-1.04826964419452,-1.04661801281888,-1.04570736457408,-1.04493254226705,
-1.04396062104761,-1.04243836183204,-1.03493599535656,-0.996672112128502,
-0.981036614342849,-0.978619059928186,-0.976094644725976,-0.97108996763833,
-0.969012718378032,-0.96771478796018,-0.966295990134023,-0.964339934999445,
-0.959709549548212,-0.939193525411031,-0.904988690061857,-0.902508925466035,
-0.892898127035476,-0.891254952756727,-0.890257116585476,-0.889478405216726,
-0.888596720156414,-0.887077117940799,-0.880766052288347,-0.868431766917954,
-0.837101558379535,-0.817787889837261,-0.814802370709961,-0.81299912476786,
-0.811600390825296,-0.810084736028705,-0.807664431424583,-0.801736014421406),
 .UNSPECIFIED.);
#190=B_SPLINE_CURVE_WITH_KNOTS('',3,(#15049,#15050,#15051,#15052,#15053,
#15054,#15055,#15056,#15057,#15058,#15059,#15060,#15061,#15062,#15063,#15064,
#15065,#15066,#15067,#15068,#15069,#15070,#15071,#15072,#15073,#15074,#15075,
#15076,#15077,#15078,#15079,#15080,#15081,#15082,#15083,#15084,#15085,#15086,
#15087,#15088,#15089,#15090,#15091,#15092,#15093,#15094,#15095,#15096),
 .UNSPECIFIED.,.F.,.F.,(4,2,2,2,2,2,2,2,2,2,2,2,2,2,2,2,2,2,2,2,2,2,2,4),
(-0.179585755313572,-0.175967937818465,-0.145634237770135,-0.136632875108729,
-0.12573674578162,-0.122965633031804,-0.121356158290008,-0.119973254234572,
-0.118650029470105,-0.116080412267979,-0.10589524409011,-0.0871223915043526,
-0.0765752847012227,-0.0608164388935438,-0.0578246341694164,-0.0462515126542455,
-0.0443559436050484,-0.0433812055735334,-0.0426063519953875,-0.0416982405767139,
-0.0407356219690761,-0.0392376733234128,-0.0363880930835168,-0.000460083170512367),
 .UNSPECIFIED.);
#191=B_SPLINE_CURVE_WITH_KNOTS('',3,(#15097,#15098,#15099,#15100,#15101,
#15102,#15103,#15104,#15105,#15106,#15107,#15108,#15109,#15110,#15111,#15112,
#15113,#15114,#15115,#15116,#15117,#15118,#15119,#15120,#15121,#15122,#15123,
#15124,#15125,#15126,#15127,#15128,#15129,#15130,#15131,#15132,#15133,#15134,
#15135,#15136,#15137,#15138,#15139,#15140,#15141,#15142,#15143,#15144,#15145,
#15146,#15147,#15148,#15149,#15150,#15151,#15152,#15153,#15154,#15155,#15156,
#15157,#15158,#15159,#15160,#15161,#15162,#15163,#15164,#15165,#15166,#15167,
#15168,#15169,#15170,#15171,#15172,#15173,#15174,#15175,#15176,#15177,#15178,
#15179,#15180,#15181,#15182,#15183,#15184,#15185,#15186,#15187,#15188,#15189,
#15190,#15191,#15192,#15193,#15194,#15195,#15196,#15197,#15198,#15199,#15200,
#15201,#15202,#15203,#15204,#15205,#15206,#15207,#15208,#15209,#15210,#15211,
#15212,#15213,#15214,#15215,#15216,#15217,#15218,#15219,#15220,#15221,#15222,
#15223,#15224,#15225,#15226,#15227,#15228,#15229,#15230,#15231,#15232,#15233,
#15234,#15235,#15236,#15237,#15238,#15239,#15240,#15241,#15242,#15243,#15244,
#15245,#15246,#15247,#15248,#15249,#15250,#15251,#15252,#15253,#15254,#15255,
#15256,#15257,#15258,#15259,#15260,#15261,#15262,#15263,#15264,#15265,#15266,
#15267,#15268,#15269,#15270,#15271,#15272,#15273,#15274,#15275,#15276,#15277,
#15278,#15279,#15280,#15281,#15282,#15283,#15284),.UNSPECIFIED.,.F.,.F.,
(4,2,2,2,2,2,2,2,2,2,2,2,2,2,2,2,2,2,2,2,2,2,2,2,2,2,2,2,2,2,2,2,2,2,2,
2,2,2,2,2,2,2,2,2,2,2,2,2,2,2,2,2,2,2,2,2,2,2,2,2,2,2,2,2,2,2,2,2,2,2,2,
2,2,2,2,2,2,2,2,2,2,2,2,2,2,2,2,2,2,2,2,2,2,4),(-1.96101303986741,-1.93902401091282,
-1.93113846510848,-1.92894324877324,-1.92741834039913,-1.92612012274045,
-1.92473222852842,-1.92297639792385,-1.91954411705765,-1.8931174819877,
-1.87529707263454,-1.85327739359925,-1.84994765342302,-1.84901615134286,
-1.84813011971587,-1.84735299763854,-1.84634762918817,-1.84471378202726,
-1.83526883130606,-1.81924644662274,-1.79774973243118,-1.78310945761126,
-1.77451653327791,-1.77203519316913,-1.77072863867773,-1.76948529762749,
-1.76786277831882,-1.76503224350567,-1.75339069778963,-1.71324624518786,
-1.69671232685801,-1.69411819909489,-1.69299722255528,-1.69220226652829,
-1.69146863637253,-1.69024979469663,-1.68709694070262,-1.68610250863524,
-1.68275133659059,-1.63800954869283,-1.62605200703821,-1.61859643106826,
-1.6162467927143,-1.61474749542882,-1.61334440509118,-1.61150773513733,
-1.60840522264195,-1.58381306331285,-1.56195946248712,-1.54093884855941,
-1.53840942963677,-1.53732794952146,-1.53654008479381,-1.53579626450685,
-1.53452492947323,-1.53103115499119,-1.50462156490907,-1.47688013913641,
-1.46393391637975,-1.46111389564662,-1.45951071638265,-1.45826749337579,
-1.45664114202461,-1.45379376307038,-1.44194328316521,-1.4360089645457,
-1.39194727688528,-1.38392672259596,-1.38229207967544,-1.38138548593529,
-1.38061088522677,-1.37963514054276,-1.3777337030146,-1.36599276707245,
-1.36229560630959,-1.31769132294265,-1.30784362638777,-1.30525436153139,
-1.30370200241855,-1.30231367907121,-1.30055456246614,-1.29710718493171,
-1.26781524875205,-1.25121268257237,-1.24289363998706,-1.22998683065394,
-1.22726223270271,-1.22614774752391,-1.22535403886612,-1.22461893855669,
-1.22339229425033,-1.22019029989984,-1.18507537092657,-1.16012005622424),
 .UNSPECIFIED.);
#192=B_SPLINE_CURVE_WITH_KNOTS('',3,(#15290,#15291,#15292,#15293,#15294,
#15295,#15296,#15297,#15298,#15299,#15300,#15301,#15302,#15303,#15304,#15305,
#15306,#15307,#15308,#15309,#15310,#15311,#15312,#15313,#15314,#15315,#15316,
#15317,#15318,#15319,#15320,#15321,#15322,#15323,#15324,#15325,#15326,#15327,
#15328,#15329,#15330,#15331,#15332,#15333,#15334,#15335,#15336,#15337,#15338,
#15339,#15340,#15341,#15342,#15343,#15344,#15345,#15346,#15347,#15348,#15349,
#15350,#15351,#15352,#15353,#15354,#15355,#15356,#15357,#15358,#15359,#15360,
#15361,#15362,#15363,#15364,#15365,#15366,#15367,#15368,#15369,#15370,#15371,
#15372,#15373,#15374,#15375,#15376,#15377,#15378,#15379,#15380,#15381,#15382,
#15383,#15384,#15385,#15386,#15387,#15388,#15389,#15390,#15391,#15392,#15393,
#15394,#15395,#15396,#15397,#15398,#15399,#15400,#15401,#15402,#15403,#15404,
#15405,#15406,#15407,#15408,#15409,#15410,#15411,#15412,#15413,#15414,#15415,
#15416,#15417,#15418,#15419,#15420,#15421,#15422,#15423,#15424,#15425,#15426,
#15427,#15428,#15429,#15430,#15431,#15432,#15433,#15434,#15435,#15436,#15437,
#15438,#15439,#15440,#15441,#15442,#15443,#15444,#15445,#15446,#15447,#15448,
#15449,#15450,#15451,#15452,#15453,#15454,#15455,#15456,#15457,#15458,#15459,
#15460,#15461,#15462,#15463,#15464,#15465,#15466,#15467,#15468,#15469,#15470,
#15471,#15472,#15473,#15474,#15475,#15476,#15477,#15478,#15479,#15480,#15481,
#15482,#15483,#15484,#15485,#15486,#15487,#15488,#15489,#15490,#15491,#15492,
#15493,#15494,#15495,#15496,#15497),.UNSPECIFIED.,.F.,.F.,(4,2,2,2,2,2,
2,2,2,2,2,2,2,2,2,2,2,2,2,2,2,2,2,2,2,2,2,2,2,2,2,2,2,2,2,2,2,2,2,2,2,2,
2,2,2,2,2,2,2,2,2,2,2,2,2,2,2,2,2,2,2,2,2,2,2,2,2,2,2,2,2,2,2,2,2,2,2,2,
2,2,2,2,2,2,2,2,2,2,2,2,2,2,2,2,2,2,2,2,2,2,2,2,2,4),(-0.801445826041384,
-0.800349872747114,-0.798233649121384,-0.797227462568897,-0.796449722874802,
-0.795562983792323,-0.794020444136553,-0.787405896305061,-0.745282452454743,
-0.724792932592394,-0.72177821601145,-0.719966491510252,-0.718566586111227,
-0.717055032691816,-0.714652845801367,-0.706736959950589,-0.693747847084072,
-0.656441125823533,-0.653896555831325,-0.644209249979237,-0.642562325177746,
-0.641563406516178,-0.640784597730487,-0.639903645509488,-0.638387224591242,
-0.632116295283881,-0.619899951401964,-0.588574070016861,-0.569103302469967,
-0.566113776876449,-0.564309400269157,-0.562910554451685,-0.561395542430526,
-0.558977919157017,-0.550919658642684,-0.537603603411906,-0.500456054967528,
-0.496273369488784,-0.488377184934789,-0.486829596030842,-0.485849921398991,
-0.485074566802187,-0.484169796547961,-0.482545229310055,-0.474705514007188,
-0.430488826995907,-0.424705793814949,-0.41268897356705,-0.410081980099038,
-0.40837435215295,-0.406989778392695,-0.405401511506826,-0.402652760045989,
-0.390790460628714,-0.346361891053286,-0.333094991300973,-0.331110579736527,
-0.330130335301258,-0.329354908091178,-0.328468659343816,-0.326904649506807,
-0.324963596360095,-0.320870029795502,-0.30896338727734,-0.277384920028211,
-0.257736322028934,-0.254742071525236,-0.252936218517003,-0.251537043489257,
-0.250022488151055,-0.247607352678036,-0.239573692920807,-0.22631494733403,
-0.205031505395017,-0.177570105319812,-0.175511292045496,-0.174516267460523,
-0.173739597030473,-0.172863521179655,-0.171350359937348,-0.169483324409091,
-0.165605886374729,-0.154628715563976,-0.12609596652198,-0.102270638965284,
-0.0991800710208497,-0.0973460714663988,-0.0959424819366718,-0.0944401796405462,
-0.0920806497362481,-0.0845497257440485,-0.0689544035445026,-0.0385355031996928,
-0.032373166813516,-0.0321516368702968,-0.02163216896645,-0.0199448253821705,
-0.0189339640671128,-0.0181535664101605,-0.0174261139967939,-0.016562105395811,
-0.015303185199615,-0.0109280128442772,-0.000459407788868288),
 .UNSPECIFIED.);
#193=B_SPLINE_CURVE_WITH_KNOTS('',3,(#15498,#15499,#15500,#15501,#15502,
#15503,#15504,#15505,#15506,#15507,#15508,#15509,#15510,#15511,#15512,#15513,
#15514,#15515,#15516,#15517,#15518,#15519,#15520,#15521,#15522,#15523,#15524,
#15525,#15526,#15527,#15528,#15529,#15530,#15531,#15532,#15533,#15534,#15535,
#15536,#15537,#15538,#15539),.UNSPECIFIED.,.F.,.F.,(4,2,2,2,2,2,2,2,2,2,
2,2,2,2,2,2,2,2,2,2,4),(-1.96128995591211,-1.92896923717076,-1.90915238863806,
-1.90460711608528,-1.90266581915441,-1.9012498872605,-1.89994913118757,
-1.89785539507136,-1.8927497295996,-1.85469262340958,-1.83834374865397,
-1.83052648440257,-1.82745437191466,-1.82520885095882,-1.82417525899136,
-1.82343299341078,-1.82268947117772,-1.82142116943337,-1.81794974541144,
-1.81752473904244,-1.78190244653125),.UNSPECIFIED.);
#194=B_SPLINE_CURVE_WITH_KNOTS('',3,(#15540,#15541,#15542,#15543,#15544,
#15545,#15546,#15547,#15548,#15549,#15550,#15551,#15552,#15553,#15554,#15555,
#15556,#15557,#15558,#15559,#15560,#15561,#15562,#15563,#15564,#15565,#15566,
#15567,#15568,#15569,#15570,#15571,#15572,#15573,#15574,#15575,#15576,#15577,
#15578,#15579,#15580,#15581,#15582,#15583,#15584,#15585,#15586,#15587,#15588,
#15589,#15590,#15591,#15592,#15593,#15594,#15595,#15596,#15597,#15598,#15599,
#15600,#15601,#15602,#15603,#15604,#15605,#15606,#15607,#15608,#15609,#15610,
#15611,#15612,#15613,#15614,#15615,#15616,#15617,#15618,#15619,#15620,#15621,
#15622,#15623,#15624,#15625,#15626,#15627,#15628,#15629,#15630,#15631,#15632,
#15633,#15634,#15635,#15636,#15637,#15638,#15639,#15640,#15641,#15642,#15643,
#15644,#15645,#15646,#15647,#15648,#15649,#15650,#15651,#15652,#15653,#15654,
#15655,#15656,#15657,#15658,#15659,#15660,#15661,#15662,#15663,#15664,#15665,
#15666,#15667,#15668,#15669,#15670,#15671,#15672,#15673,#15674,#15675,#15676,
#15677,#15678,#15679,#15680,#15681,#15682,#15683,#15684,#15685,#15686,#15687,
#15688,#15689,#15690,#15691,#15692,#15693,#15694,#15695,#15696,#15697,#15698,
#15699,#15700,#15701,#15702,#15703,#15704,#15705,#15706,#15707,#15708,#15709,
#15710,#15711,#15712,#15713,#15714,#15715,#15716,#15717,#15718,#15719,#15720,
#15721,#15722,#15723,#15724,#15725,#15726,#15727,#15728,#15729,#15730,#15731,
#15732,#15733,#15734,#15735,#15736,#15737,#15738,#15739,#15740,#15741,#15742,
#15743,#15744,#15745,#15746,#15747,#15748,#15749,#15750,#15751,#15752,#15753,
#15754,#15755,#15756,#15757,#15758,#15759,#15760,#15761,#15762,#15763,#15764,
#15765,#15766,#15767,#15768,#15769,#15770,#15771,#15772,#15773,#15774,#15775,
#15776,#15777,#15778,#15779),.UNSPECIFIED.,.F.,.F.,(4,2,2,2,2,2,2,2,2,2,
2,2,2,2,2,2,2,2,2,2,2,2,2,2,2,2,2,2,2,2,2,2,2,2,2,2,2,2,2,2,2,2,2,2,2,2,
2,2,2,2,2,2,2,2,2,2,2,2,2,2,2,2,2,2,2,2,2,2,2,2,2,2,2,2,2,2,2,2,2,2,2,2,
2,2,2,2,2,2,2,2,2,2,2,2,2,2,2,2,2,2,2,2,2,2,2,2,2,2,2,2,2,2,2,2,2,2,2,2,
2,4),(-1.16012005622424,-1.15415813050765,-1.15044685505235,-1.14865884109744,
-1.14726724866216,-1.14573120252076,-1.14321521305641,-1.13512049870346,
-1.13396102106544,-1.13373336672688,-1.08729962664451,-1.07764256493671,
-1.07408832682855,-1.07154034941925,-1.07045557817196,-1.06966708134879,
-1.06892407530831,-1.06765718839674,-1.06419268431622,-1.03535532330225,
-0.999284713641795,-0.995056232045912,-0.993171210352436,-0.991765435043037,
-0.990451878352686,-0.98864184224745,-0.984013991047981,-0.980812189523047,
-0.969509609496407,-0.946083219768486,-0.919857268268363,-0.916364437150595,
-0.915093186215055,-0.914349335666649,-0.913561372470622,-0.912479650843354,
-0.909949182919926,-0.888344440827802,-0.874037908551752,-0.84254476738048,
-0.839117849737984,-0.837363039771678,-0.835975107626667,-0.834420036767001,
-0.831818776909092,-0.821833726842604,-0.776863594799361,-0.773774600973159,
-0.770932056135287,-0.761710213942626,-0.760087552197246,-0.7590854243908,
-0.758308482307567,-0.757420048400854,-0.755868472902261,-0.74912221708597,
-0.73546018596828,-0.702648300221043,-0.686412338616625,-0.683558993829449,
-0.68177637404806,-0.680385174442506,-0.678845683479245,-0.67631516491035,
-0.667120697648695,-0.623690262423908,-0.606514485084176,-0.604434535733032,
-0.603435680968508,-0.602659006567975,-0.601768329715578,-0.600206814099761,
-0.593322625486607,-0.550394814609992,-0.530971301534117,-0.527984084170803,
-0.526180858437776,-0.5247827645668,-0.523268429371774,-0.520851594346215,
-0.512793382934143,-0.499475218952549,-0.462344527025023,-0.458244348019622,
-0.450272237834714,-0.448720454523785,-0.447739759462335,-0.446964690764981,
-0.446061523521919,-0.444443011983169,-0.436693025213383,-0.392432546389212,
-0.386823569434167,-0.374614413881065,-0.371995239021018,-0.370284298426949,
-0.368900140394718,-0.36731575998158,-0.364582377584561,-0.35292195375019,
-0.308378152637977,-0.295014398285981,-0.293027527126415,-0.292047087212644,
-0.291272006869944,-0.29045247645357,-0.289013942049652,-0.287233415920234,
-0.28360367381898,-0.273645944872561,-0.239275826685809,-0.219656087035516,
-0.21666367922967,-0.214858853159472,-0.213460427308733,-0.211946639042526,
-0.209532637939071,-0.2015020629797,-0.188248151775626,-0.17987795927969),
 .UNSPECIFIED.);
#195=B_SPLINE_CURVE_WITH_KNOTS('',3,(#15784,#15785,#15786,#15787,#15788,
#15789,#15790,#15791,#15792,#15793,#15794,#15795,#15796,#15797,#15798,#15799,
#15800,#15801,#15802,#15803,#15804,#15805,#15806,#15807,#15808,#15809,#15810,
#15811,#15812,#15813,#15814,#15815,#15816,#15817,#15818,#15819,#15820,#15821,
#15822,#15823,#15824,#15825,#15826,#15827,#15828,#15829,#15830,#15831,#15832,
#15833,#15834,#15835,#15836,#15837,#15838,#15839,#15840,#15841,#15842,#15843,
#15844,#15845,#15846,#15847,#15848,#15849,#15850,#15851,#15852,#15853,#15854,
#15855,#15856,#15857,#15858,#15859,#15860,#15861,#15862,#15863,#15864,#15865,
#15866,#15867,#15868,#15869,#15870,#15871,#15872,#15873,#15874,#15875,#15876,
#15877,#15878,#15879,#15880,#15881,#15882,#15883,#15884,#15885,#15886,#15887,
#15888,#15889,#15890,#15891,#15892,#15893,#15894,#15895,#15896,#15897,#15898,
#15899,#15900,#15901,#15902,#15903,#15904,#15905,#15906,#15907,#15908,#15909,
#15910,#15911,#15912,#15913,#15914,#15915,#15916,#15917,#15918,#15919,#15920,
#15921,#15922,#15923,#15924,#15925,#15926,#15927,#15928,#15929,#15930,#15931,
#15932,#15933,#15934,#15935,#15936,#15937,#15938,#15939,#15940,#15941,#15942,
#15943,#15944,#15945,#15946,#15947,#15948,#15949,#15950,#15951,#15952,#15953,
#15954,#15955,#15956,#15957,#15958,#15959,#15960,#15961,#15962,#15963,#15964,
#15965,#15966,#15967,#15968,#15969,#15970,#15971,#15972,#15973,#15974,#15975,
#15976,#15977,#15978,#15979,#15980,#15981,#15982,#15983,#15984,#15985,#15986,
#15987,#15988,#15989,#15990,#15991,#15992,#15993,#15994,#15995,#15996,#15997,
#15998,#15999,#16000,#16001,#16002,#16003,#16004,#16005,#16006,#16007,#16008,
#16009,#16010,#16011),.UNSPECIFIED.,.F.,.F.,(4,2,2,2,2,2,2,2,2,2,2,2,2,
2,2,2,2,2,2,2,2,2,2,2,2,2,2,2,2,2,2,2,2,2,2,2,2,2,2,2,2,2,2,2,2,2,2,2,2,
2,2,2,2,2,2,2,2,2,2,2,2,2,2,2,2,2,2,2,2,2,2,2,2,2,2,2,2,2,2,2,2,2,2,2,2,
2,2,2,2,2,2,2,2,2,2,2,2,2,2,2,2,2,2,2,2,2,2,2,2,2,2,2,2,4),(-1.7820183274493,
-1.77638176080533,-1.74715212882205,-1.73833521233597,-1.73499552512745,
-1.73256791526149,-1.73150382689449,-1.73071830156585,-1.72996829096072,
-1.72866767460946,-1.72499426195066,-1.72344811708588,-1.67485095227704,
-1.66397287879935,-1.65701637496962,-1.65530428363814,-1.65369986399018,
-1.6523477953927,-1.65071053970372,-1.64787124038574,-1.63583794333267,
-1.63004712718618,-1.58575486349801,-1.57797877267479,-1.57635805682508,
-1.57545412478334,-1.57467867994129,-1.57369785922229,-1.57171046213532,
-1.55834901701542,-1.5137672909055,-1.50215645110387,-1.4994257439447,-1.49784145138354,
-1.49645649319771,-1.49474342866019,-1.49211885453612,-1.47984899192827,
-1.44194754241661,-1.42873981219348,-1.42213958354263,-1.42059807233498,
-1.41971155431095,-1.41893376159289,-1.4179271876616,-1.41580900364501,
-1.39400946423344,-1.38829795325573,-1.35982960417762,-1.34669547024539,
-1.34386202417565,-1.3422551137299,-1.34101082874239,-1.33938570056183,
-1.33654710679659,-1.32482413520142,-1.31876638779678,-1.27469201592413,
-1.26663225904502,-1.26499438278356,-1.26408664086502,-1.26331144853767,
-1.26233544059798,-1.2604349040229,-1.24874581441117,-1.24525586328687,
-1.20044383639529,-1.19051993139808,-1.18792267273261,-1.18636775368084,
-1.18497854429074,-1.18322020403655,-1.17978033483721,-1.1527222218404,
-1.14614919292542,-1.12553946981631,-1.11590822462521,-1.11235976839988,
-1.10981464006502,-1.10872990641278,-1.10794098833984,-1.10719721838534,
-1.10592822305707,-1.10245337221938,-1.07400989047575,-1.03729458758953,
-1.03322445961232,-1.03136752899994,-1.02996541863394,-1.02864260311311,
-1.02679952077802,-1.02197163841473,-0.980595005383374,-0.96683214214974,
-0.955683882751211,-0.953970449650863,-0.952951972635141,-0.952170538977476,
-0.951300593586297,-0.949833893519707,-0.944166428436368,-0.933654875851704,
-0.926145783705573,-0.925335701235225,-0.882593183474118,-0.877926393932956,
-0.876109201278924,-0.874793204445442,-0.87338738685576,-0.871506757785655,
-0.867306855534465,-0.850196437521089,-0.821319314117838,-0.801445826041384),
 .UNSPECIFIED.);
#196=B_SPLINE_CURVE_WITH_KNOTS('',3,(#16013,#16014,#16015,#16016,#16017,
#16018,#16019,#16020,#16021,#16022,#16023,#16024,#16025,#16026,#16027,#16028,
#16029,#16030,#16031,#16032,#16033,#16034,#16035,#16036,#16037,#16038,#16039,
#16040,#16041,#16042,#16043,#16044,#16045,#16046,#16047,#16048,#16049,#16050,
#16051,#16052,#16053,#16054),.UNSPECIFIED.,.F.,.F.,(4,2,2,2,2,2,2,2,2,2,
2,2,2,2,2,2,2,2,2,2,4),(-0.17987795927969,-0.145959516617287,-0.138816103552565,
-0.137318875760568,-0.136354831707817,-0.135580707523949,-0.134682747526293,
-0.133106271723474,-0.131118248051813,-0.126885155200885,-0.114356570881015,
-0.0822039428817398,-0.0755338261407026,-0.0632995564264635,-0.0606778611037748,
-0.0589659393235315,-0.0575814286910333,-0.0559971284805531,-0.053265106453469,
-0.0416293542253508,-0.000460323532593378),.UNSPECIFIED.);
#197=B_SPLINE_CURVE_WITH_KNOTS('',3,(#16055,#16056,#16057,#16058,#16059,
#16060,#16061,#16062,#16063,#16064,#16065,#16066,#16067,#16068,#16069,#16070,
#16071,#16072,#16073,#16074,#16075,#16076,#16077,#16078,#16079,#16080,#16081,
#16082,#16083,#16084,#16085,#16086,#16087,#16088,#16089,#16090,#16091,#16092,
#16093,#16094,#16095,#16096,#16097,#16098,#16099,#16100,#16101,#16102,#16103,
#16104,#16105,#16106,#16107,#16108,#16109,#16110,#16111,#16112,#16113,#16114,
#16115,#16116,#16117,#16118,#16119,#16120,#16121,#16122,#16123,#16124,#16125,
#16126,#16127,#16128,#16129,#16130,#16131,#16132,#16133,#16134,#16135,#16136),
 .UNSPECIFIED.,.F.,.F.,(4,3,3,3,3,3,3,3,3,3,3,3,3,3,3,3,3,3,3,3,3,3,3,3,
3,3,3,4),(116.238928182823,116.369122527555,116.567664818425,116.767442819537,
116.965528358298,117.166152590585,117.366776822873,117.565319113743,117.765097114855,
117.963182653616,118.163806885904,118.364431118192,118.562973409062,118.762751410174,
118.960836948935,119.161461181222,119.36208541351,119.56062770438,119.760405705492,
119.958491244253,120.159115476541,120.359739708829,120.558281999699,120.758060000811,
120.956145539572,121.156769771859,121.357394004147,121.373252558517),
 .UNSPECIFIED.);
#198=B_SPLINE_CURVE_WITH_KNOTS('',3,(#16142,#16143,#16144,#16145,#16146,
#16147,#16148,#16149,#16150),.UNSPECIFIED.,.F.,.F.,(4,1,1,1,1,1,4),(122.522113490002,
123.040830884369,124.038485179687,125.036139475006,126.033793770324,127.031448065643,
127.655725185573),.UNSPECIFIED.);
#199=B_SPLINE_CURVE_WITH_KNOTS('',3,(#16151,#16152,#16153,#16154,#16155,
#16156,#16157,#16158,#16159,#16160,#16161,#16162,#16163,#16164,#16165,#16166,
#16167,#16168,#16169,#16170,#16171,#16172,#16173,#16174,#16175,#16176,#16177,
#16178,#16179,#16180,#16181,#16182,#16183,#16184,#16185,#16186,#16187,#16188,
#16189,#16190,#16191,#16192,#16193,#16194,#16195,#16196,#16197,#16198,#16199,
#16200,#16201,#16202,#16203,#16204,#16205,#16206,#16207,#16208,#16209,#16210,
#16211,#16212,#16213,#16214,#16215,#16216,#16217,#16218,#16219,#16220,#16221,
#16222,#16223,#16224,#16225,#16226,#16227,#16228,#16229,#16230,#16231,#16232,
#16233,#16234),.UNSPECIFIED.,.F.,.F.,(4,2,2,2,2,2,2,2,2,2,2,2,2,2,2,2,2,
2,2,2,2,2,2,2,2,2,2,2,2,2,2,2,2,2,2,2,2,2,2,2,2,4),(-1.96128222253846,-1.95958363623628,
-1.95630370014159,-1.94144445515337,-1.89718230505077,-1.88936987786217,
-1.88774696253415,-1.88684256059216,-1.88606717896178,-1.88508703610749,
-1.88310296685397,-1.8698417562419,-1.8346986810638,-1.8211583699688,-1.81300241363437,
-1.81120770552465,-1.80954407165404,-1.80952953053889,-1.80951457375782,
-1.80949916961573,-1.80948328329705,-1.80946687643486,-1.80944990661459,
-1.80943232678431,-1.80941408455338,-1.80939512135814,-1.8093753714631,
-1.80935476074941,-1.80933320523811,-1.80931060928038,-1.80928686332031,
-1.80926184108749,-1.80923539605991,-1.80920735663572,-1.8091775206023,
-1.80914564843925,-1.80911883506897,-1.80908079907286,-1.80774045339956,
-1.80600936930746,-1.80260197344681,-1.7820183274493),.UNSPECIFIED.);
#200=B_SPLINE_CURVE_WITH_KNOTS('',3,(#16236,#16237,#16238,#16239,#16240,
#16241,#16242,#16243,#16244,#16245,#16246,#16247,#16248,#16249,#16250,#16251,
#16252,#16253,#16254),.UNSPECIFIED.,.F.,.F.,(4,3,3,3,3,3,4),(121.373252558517,
121.571751272604,121.7700124529,121.968092146591,122.166669391268,122.355048299466,
122.522113490002),.UNSPECIFIED.);
#201=B_SPLINE_CURVE_WITH_KNOTS('',3,(#16255,#16256,#16257,#16258,#16259,
#16260,#16261,#16262,#16263),.UNSPECIFIED.,.F.,.F.,(4,1,1,1,1,1,4),(122.522119580395,
123.352702594784,124.350356890103,125.348011185421,126.34566548074,127.343319776058,
127.657159480932),.UNSPECIFIED.);
#202=B_SPLINE_CURVE_WITH_KNOTS('',3,(#16269,#16270,#16271,#16272,#16273,
#16274,#16275,#16276,#16277,#16278,#16279,#16280,#16281,#16282,#16283,#16284,
#16285,#16286,#16287,#16288,#16289,#16290,#16291,#16292,#16293,#16294,#16295,
#16296,#16297,#16298,#16299,#16300,#16301,#16302,#16303,#16304,#16305,#16306,
#16307,#16308,#16309,#16310,#16311,#16312,#16313,#16314,#16315,#16316,#16317,
#16318,#16319,#16320,#16321,#16322,#16323,#16324,#16325,#16326,#16327,#16328,
#16329,#16330,#16331,#16332,#16333,#16334,#16335,#16336,#16337,#16338,#16339,
#16340,#16341,#16342,#16343,#16344,#16345,#16346,#16347),.UNSPECIFIED.,
 .F.,.F.,(4,3,3,3,3,3,3,3,3,3,3,3,3,3,3,3,3,3,3,3,3,3,3,3,3,3,4),(128.805298797182,
129.02675665628,129.22529894715,129.425076948262,129.623162487023,129.82378671931,
130.024410951598,130.222953242468,130.42273124358,130.620816782341,130.821441014629,
131.022065246917,131.220607537787,131.420385538899,131.61847107766,131.819095309947,
132.019719542235,132.218261833105,132.418039834217,132.616125372978,132.816749605266,
133.017373837554,133.215921390413,133.414151854748,133.612180481121,133.810554859578,
133.939161505613),.UNSPECIFIED.);
#203=B_SPLINE_CURVE_WITH_KNOTS('',3,(#16348,#16349,#16350,#16351,#16352),
 .UNSPECIFIED.,.F.,.F.,(4,1,4),(127.655725185573,128.029102360961,128.805297760461),
 .UNSPECIFIED.);
#204=B_SPLINE_CURVE_WITH_KNOTS('',3,(#16354,#16355,#16356,#16357,#16358),
 .UNSPECIFIED.,.F.,.F.,(4,1,4),(127.657159480932,128.340974071377,128.805296175662),
 .UNSPECIFIED.);
#205=B_SPLINE_CURVE_WITH_KNOTS('',3,(#16359,#16360,#16361,#16362,#16363,
#16364,#16365,#16366,#16367,#16368,#16369,#16370,#16371,#16372,#16373,#16374,
#16375,#16376,#16377,#16378,#16379,#16380,#16381,#16382,#16383,#16384,#16385,
#16386,#16387,#16388,#16389,#16390,#16391,#16392,#16393,#16394,#16395,#16396,
#16397,#16398,#16399,#16400,#16401,#16402,#16403,#16404,#16405,#16406,#16407,
#16408,#16409,#16410,#16411,#16412,#16413,#16414,#16415,#16416,#16417,#16418,
#16419,#16420,#16421,#16422,#16423,#16424,#16425,#16426,#16427,#16428,#16429,
#16430,#16431,#16432,#16433,#16434,#16435,#16436,#16437,#16438,#16439,#16440,
#16441,#16442,#16443,#16444,#16445,#16446,#16447,#16448,#16449,#16450,#16451,
#16452,#16453,#16454,#16455,#16456,#16457,#16458,#16459,#16460,#16461,#16462,
#16463,#16464,#16465,#16466,#16467,#16468,#16469,#16470,#16471,#16472,#16473,
#16474,#16475,#16476,#16477,#16478,#16479,#16480,#16481,#16482,#16483,#16484,
#16485,#16486,#16487,#16488,#16489,#16490,#16491,#16492,#16493,#16494,#16495,
#16496,#16497,#16498,#16499,#16500,#16501,#16502,#16503,#16504,#16505,#16506,
#16507,#16508,#16509,#16510,#16511,#16512,#16513,#16514,#16515,#16516,#16517,
#16518,#16519,#16520,#16521,#16522,#16523,#16524,#16525,#16526,#16527,#16528,
#16529,#16530,#16531,#16532,#16533,#16534,#16535,#16536,#16537,#16538,#16539,
#16540,#16541,#16542,#16543,#16544,#16545,#16546,#16547,#16548,#16549,#16550,
#16551,#16552,#16553,#16554,#16555,#16556,#16557,#16558),.UNSPECIFIED.,
 .F.,.F.,(4,2,2,2,2,2,2,2,2,2,2,2,2,2,2,2,2,2,2,2,2,2,2,2,2,2,2,2,2,2,2,
2,2,2,2,2,2,2,2,2,2,2,2,2,2,2,2,2,2,2,2,2,2,2,2,2,2,2,2,2,2,2,2,2,2,2,2,
2,2,2,2,2,2,2,2,2,2,2,2,2,2,2,2,2,2,2,2,2,2,2,2,2,2,2,2,2,2,2,2,4),(-1.96108238987861,
-1.95962527398827,-1.95805600276329,-1.95670126082934,-1.95536452789458,
-1.95403545240248,-1.95179028303077,-1.94573147315617,-1.89863151775104,
-1.88663302728454,-1.8804379472618,-1.87892792299045,-1.87804862810209,
-1.8772699012373,-1.87626932856835,-1.87461606059931,-1.86478964781739,
-1.86249101981947,-1.83467772864677,-1.80872771981097,-1.80518064403458,
-1.80309568869222,-1.80122435588287,-1.79983924839755,-1.7985360549032,
-1.79642785598399,-1.79125080324649,-1.75458124763867,-1.72651427561873,
-1.72391824403796,-1.72282505883563,-1.72203495360458,-1.72129401263089,
-1.72003831269686,-1.71664860811503,-1.68426485737966,-1.65367330149517,
-1.64983793789101,-1.64763652277233,-1.64610884268141,-1.64463554055501,
-1.64327458345385,-1.64147264707135,-1.63849017037257,-1.61893317628298,
-1.58744910862982,-1.57537346873885,-1.56915179643041,-1.56763960712186,
-1.56675979845136,-1.5659811184105,-1.56498125237321,-1.56333048592694,
-1.55355650504723,-1.53725460120878,-1.51293280581748,-1.50054908094957,
-1.49290054874344,-1.49052835258819,-1.48902368985411,-1.48762186672719,
-1.48579585723203,-1.48273133872076,-1.46016500993314,-1.45185120721396,
-1.43676378281074,-1.41517637294027,-1.41264483764011,-1.41156273648884,
-1.41077452782028,-1.41003046971386,-1.40875891710535,-1.40526558237236,
-1.37906847406862,-1.35114080388952,-1.33814455470387,-1.33532057144844,
-1.33371613596061,-1.33247240823027,-1.33084606811697,-1.32800042268292,
-1.31618089301717,-1.31021173080889,-1.26615238992651,-1.25810335186605,
-1.25646657315324,-1.25555929725335,-1.25478441994791,-1.25380871743035,
-1.25190851572126,-1.24021399338478,-1.23658494020635,-1.19187905017021,
-1.18199292865903,-1.17939963839018,-1.17784600162827,-1.17645725159261,
-1.17469856550342,-1.17125510381233,-1.16001003225657),.UNSPECIFIED.);
#206=B_SPLINE_CURVE_WITH_KNOTS('',3,(#16564,#16565,#16566,#16567,#16568,
#16569,#16570,#16571,#16572,#16573,#16574,#16575,#16576,#16577,#16578,#16579,
#16580,#16581,#16582,#16583,#16584,#16585,#16586,#16587,#16588,#16589,#16590,
#16591,#16592,#16593,#16594,#16595,#16596,#16597,#16598,#16599,#16600,#16601,
#16602,#16603,#16604,#16605,#16606,#16607,#16608,#16609,#16610,#16611,#16612,
#16613,#16614,#16615,#16616,#16617,#16618,#16619,#16620,#16621,#16622,#16623,
#16624,#16625,#16626,#16627,#16628,#16629,#16630,#16631,#16632,#16633,#16634,
#16635,#16636,#16637,#16638,#16639,#16640,#16641,#16642,#16643,#16644,#16645,
#16646,#16647,#16648,#16649,#16650,#16651,#16652,#16653,#16654,#16655,#16656,
#16657,#16658,#16659,#16660,#16661,#16662,#16663,#16664,#16665,#16666,#16667,
#16668,#16669,#16670,#16671,#16672,#16673,#16674,#16675,#16676,#16677,#16678,
#16679,#16680,#16681,#16682,#16683,#16684,#16685,#16686,#16687,#16688,#16689,
#16690,#16691,#16692,#16693,#16694,#16695,#16696,#16697,#16698,#16699,#16700,
#16701,#16702,#16703,#16704,#16705,#16706,#16707,#16708,#16709,#16710,#16711,
#16712,#16713,#16714,#16715,#16716,#16717,#16718,#16719,#16720,#16721,#16722,
#16723,#16724,#16725,#16726,#16727,#16728,#16729,#16730,#16731,#16732,#16733,
#16734,#16735,#16736,#16737,#16738,#16739,#16740,#16741,#16742,#16743,#16744,
#16745,#16746,#16747,#16748,#16749,#16750,#16751),.UNSPECIFIED.,.F.,.F.,
(4,2,2,2,2,2,2,2,2,2,2,2,2,2,2,2,2,2,2,2,2,2,2,2,2,2,2,2,2,2,2,2,2,2,2,
2,2,2,2,2,2,2,2,2,2,2,2,2,2,2,2,2,2,2,2,2,2,2,2,2,2,2,2,2,2,2,2,2,2,2,2,
2,2,2,2,2,2,2,2,2,2,2,2,2,2,2,2,2,2,2,2,2,2,4),(-0.801648158832126,-0.78213823686765,
-0.781014765677329,-0.770306567636845,-0.768611249732307,-0.767598142695125,
-0.766817552819496,-0.765944911392444,-0.76446572093286,-0.758651079336189,
-0.747735441952474,-0.726495051199371,-0.695357700750936,-0.691931669929365,
-0.690176460432175,-0.68878778941575,-0.687231444709382,-0.684626985824291,
-0.674616138217384,-0.629561927187327,-0.626701306196766,-0.624390725327106,
-0.614561649852437,-0.612907690563772,-0.611906674151297,-0.611127581383509,
-0.610247829361824,-0.608736920519546,-0.602536551650829,-0.590526830318372,
-0.559015781156644,-0.539444088903777,-0.536451899042796,-0.534646702930499,
-0.53324768945808,-0.531732962470556,-0.529316803763471,-0.521272795872992,
-0.507989875744357,-0.470701058912443,-0.459048226596414,-0.45714918610198,
-0.456173552892839,-0.455398452048785,-0.454490574492869,-0.452851847420105,
-0.44477535977028,-0.400742970753238,-0.394662428765651,-0.38297186749627,
-0.380135974334613,-0.378511493532836,-0.377267234426126,-0.375659796446321,
-0.372823799876876,-0.359648317775045,-0.331011393757186,-0.303577241885318,
-0.301518493494147,-0.300523512882973,-0.299769524916084,-0.29889802404045,
-0.297972817000706,-0.29656526584481,-0.293955182604191,-0.267935405277803,
-0.230946648362081,-0.225781533148655,-0.223677629722732,-0.222374841617613,
-0.220960079590524,-0.219026489731675,-0.214527177807558,-0.195082563635142,
-0.167455048587957,-0.147993955374993,-0.145887426004711,-0.144883128266496,
-0.144136091225494,-0.143276738016289,-0.141859162851745,-0.140120958147904,
-0.136611646115393,-0.127135950678105,-0.0934422327538317,-0.0725036106061738,
-0.0694773029840937,-0.0676621500206694,-0.0662616758716257,-0.0647515672106966,
-0.0623560866390103,-0.0545021128486099,-0.0416542836801877,-0.000460315519253413),
 .UNSPECIFIED.);
#207=B_SPLINE_CURVE_WITH_KNOTS('',3,(#16752,#16753,#16754,#16755,#16756,
#16757,#16758,#16759,#16760,#16761,#16762,#16763,#16764,#16765,#16766,#16767,
#16768,#16769,#16770,#16771,#16772,#16773),.UNSPECIFIED.,.F.,.F.,(4,3,3,
3,3,3,3,4),(133.939161505613,134.015028132872,134.213570423742,134.413348424854,
134.611433963615,134.812058195903,135.012682428191,135.088484104361),
 .UNSPECIFIED.);
#208=B_SPLINE_CURVE_WITH_KNOTS('',3,(#16774,#16775,#16776,#16777,#16778,
#16779,#16780,#16781,#16782,#16783,#16784,#16785,#16786,#16787,#16788,#16789,
#16790,#16791,#16792,#16793,#16794,#16795,#16796,#16797,#16798,#16799,#16800,
#16801,#16802,#16803,#16804,#16805,#16806,#16807,#16808,#16809,#16810,#16811,
#16812,#16813,#16814,#16815,#16816,#16817,#16818,#16819,#16820,#16821,#16822,
#16823,#16824,#16825,#16826,#16827,#16828,#16829,#16830,#16831,#16832,#16833,
#16834,#16835,#16836,#16837,#16838,#16839,#16840,#16841,#16842,#16843,#16844,
#16845,#16846,#16847,#16848,#16849,#16850,#16851,#16852,#16853,#16854,#16855,
#16856,#16857,#16858,#16859,#16860,#16861,#16862,#16863,#16864,#16865,#16866,
#16867,#16868,#16869,#16870,#16871,#16872,#16873,#16874,#16875,#16876,#16877,
#16878,#16879,#16880,#16881,#16882,#16883,#16884,#16885,#16886,#16887,#16888,
#16889,#16890,#16891,#16892,#16893,#16894,#16895,#16896,#16897,#16898,#16899,
#16900,#16901,#16902,#16903,#16904,#16905,#16906,#16907,#16908,#16909,#16910,
#16911,#16912,#16913,#16914,#16915,#16916,#16917,#16918,#16919,#16920,#16921,
#16922,#16923,#16924,#16925,#16926,#16927,#16928,#16929,#16930,#16931,#16932,
#16933,#16934,#16935,#16936,#16937,#16938,#16939,#16940,#16941,#16942,#16943,
#16944,#16945,#16946,#16947,#16948,#16949,#16950,#16951,#16952,#16953,#16954,
#16955,#16956,#16957,#16958,#16959,#16960,#16961,#16962,#16963,#16964,#16965,
#16966,#16967,#16968,#16969,#16970,#16971,#16972,#16973,#16974,#16975,#16976,
#16977,#16978,#16979,#16980,#16981,#16982,#16983,#16984,#16985,#16986,#16987,
#16988,#16989,#16990,#16991,#16992,#16993,#16994,#16995,#16996,#16997,#16998,
#16999,#17000,#17001,#17002,#17003),.UNSPECIFIED.,.F.,.F.,(4,2,2,2,2,2,
2,2,2,2,2,2,2,2,2,2,2,2,2,2,2,2,2,2,2,2,2,2,2,2,2,2,2,2,2,2,2,2,2,2,2,2,
2,2,2,2,2,2,2,2,2,2,2,2,2,2,2,2,2,2,2,2,2,2,2,2,2,2,2,2,2,2,2,2,2,2,2,2,
2,2,2,2,2,2,2,2,2,2,2,2,2,2,2,2,2,2,2,2,2,2,2,2,2,2,2,2,2,2,2,2,2,2,2,2,
4),(-1.16001003225657,-1.1429307201912,-1.11889769922653,-1.10795658489296,
-1.10213363116416,-1.100653952482,-1.09978133247617,-1.09900097538504,-1.0979884743361,
-1.09629482640386,-1.08561871277599,-1.07936970935277,-1.04801404557703,
-1.02930305097426,-1.02489588234255,-1.02297868676905,-1.02156711054281,
-1.02026104238578,-1.01813792674338,-1.01285694873877,-0.980611544930864,
-0.973858585284931,-0.972027388600992,-0.959198144127172,-0.956755689781633,
-0.94710621148281,-0.945461516435653,-0.944463421923748,-0.943684927527861,
-0.942803973204306,-0.941286746692366,-0.935001344956756,-0.922741110165887,
-0.891421398550156,-0.872000821566398,-0.869013212815021,-0.867209697584171,
-0.86581134765867,-0.864296703570325,-0.861879307230727,-0.853818588799811,
-0.840495630159603,-0.803368759929907,-0.791622190722028,-0.789719971468083,
-0.788743860607362,-0.787968987763851,-0.787062092534455,-0.785426957310112,
-0.777404578436029,-0.733351016303359,-0.72741551957575,-0.715565766575734,
-0.712717676802668,-0.711090760529626,-0.709847025642558,-0.708243086832567,
-0.705421453421397,-0.6924633077725,-0.664682568163185,-0.638259582356622,
-0.634763846556083,-0.633491891371915,-0.632747731985936,-0.631959527595578,
-0.630877613907926,-0.62834731644099,-0.607257023549327,-0.584930046436624,
-0.560871674365034,-0.557777652939642,-0.55594301500481,-0.554539756196093,
-0.553038607257348,-0.550682569759479,-0.543177185660699,-0.531109851804377,
-0.507025749923546,-0.480562605538079,-0.47848221045133,-0.477483180014358,
-0.476706386907004,-0.475815594023372,-0.474253922615354,-0.467369805234921,
-0.424439493958543,-0.405008167397624,-0.40202037573363,-0.400216842870063,
-0.398818534341326,-0.397303990073394,-0.394886872118563,-0.386828189232162,
-0.373509729466546,-0.336365544703593,-0.33220204331563,-0.32428963198472,
-0.322741395169118,-0.321761706255257,-0.321005178755623,-0.320128252130178,
-0.319189324392779,-0.317748381396495,-0.31505010845968,-0.287025516163436,
-0.252339164762221,-0.247086932824349,-0.244968773037614,-0.243663660612136,
-0.242251475578793,-0.240330533807881,-0.235901744386162,-0.217016213327319,
-0.186955256986825,-0.179694752014396),.UNSPECIFIED.);
#209=B_SPLINE_CURVE_WITH_KNOTS('',3,(#17008,#17009,#17010,#17011,#17012,
#17013,#17014,#17015,#17016,#17017,#17018,#17019,#17020,#17021,#17022,#17023,
#17024,#17025,#17026,#17027,#17028,#17029,#17030,#17031,#17032,#17033,#17034,
#17035,#17036,#17037,#17038,#17039,#17040,#17041,#17042,#17043,#17044,#17045,
#17046,#17047,#17048,#17049,#17050,#17051,#17052,#17053,#17054,#17055,#17056,
#17057,#17058,#17059,#17060,#17061,#17062,#17063,#17064,#17065,#17066,#17067,
#17068,#17069,#17070,#17071,#17072,#17073,#17074,#17075,#17076,#17077,#17078,
#17079,#17080,#17081,#17082,#17083,#17084,#17085,#17086,#17087,#17088,#17089,
#17090,#17091,#17092,#17093,#17094,#17095,#17096,#17097,#17098,#17099,#17100,
#17101,#17102,#17103,#17104,#17105,#17106,#17107,#17108,#17109,#17110,#17111,
#17112,#17113,#17114,#17115,#17116,#17117,#17118,#17119,#17120,#17121,#17122,
#17123,#17124,#17125,#17126,#17127,#17128,#17129,#17130,#17131,#17132,#17133,
#17134,#17135,#17136,#17137,#17138,#17139,#17140,#17141,#17142,#17143,#17144,
#17145,#17146,#17147,#17148,#17149,#17150,#17151,#17152,#17153,#17154,#17155,
#17156,#17157,#17158,#17159,#17160,#17161,#17162,#17163,#17164,#17165,#17166,
#17167,#17168,#17169,#17170,#17171,#17172,#17173,#17174,#17175,#17176,#17177,
#17178,#17179,#17180,#17181,#17182,#17183,#17184,#17185,#17186,#17187,#17188,
#17189,#17190,#17191,#17192,#17193,#17194,#17195,#17196,#17197,#17198,#17199,
#17200,#17201,#17202,#17203,#17204,#17205,#17206,#17207,#17208,#17209,#17210,
#17211,#17212,#17213,#17214,#17215,#17216,#17217,#17218,#17219,#17220,#17221,
#17222,#17223,#17224,#17225,#17226,#17227,#17228,#17229,#17230,#17231,#17232,
#17233,#17234,#17235,#17236,#17237,#17238,#17239,#17240,#17241,#17242,#17243,
#17244,#17245,#17246,#17247,#17248,#17249,#17250,#17251,#17252,#17253,#17254,
#17255,#17256,#17257,#17258,#17259,#17260,#17261,#17262,#17263),
 .UNSPECIFIED.,.F.,.F.,(4,2,2,2,2,2,2,2,2,2,2,2,2,2,2,2,2,2,2,2,2,2,2,2,
2,2,2,2,2,2,2,2,2,2,2,2,2,2,2,2,2,2,2,2,2,2,2,2,2,2,2,2,2,2,2,2,2,2,2,2,
2,2,2,2,2,2,2,2,2,2,2,2,2,2,2,2,2,2,2,2,2,2,2,2,2,2,2,2,2,2,2,2,2,2,2,2,
2,2,2,2,2,2,2,2,2,2,2,2,2,2,2,2,2,2,2,2,2,2,2,2,2,2,2,2,2,2,2,4),(-1.78189016740401,
-1.78097762397856,-1.7793868830838,-1.77937825793148,-1.77936932347904,
-1.77936006788285,-1.77935047755204,-1.7793405383494,-1.7793302395449,-1.77931956715433,
-1.779308506606,-1.7792970427107,-1.77928515963152,-1.77927284135281,-1.7778882946397,
-1.77617212134381,-1.77353599926515,-1.76107718639576,-1.75568937526266,
-1.71117029652588,-1.70374008738545,-1.70211528874888,-1.70121071634051,
-1.7004357291812,-1.69945677749505,-1.69791082421215,-1.69003288258165,
-1.68584165643759,-1.68215848393462,-1.63753630787342,-1.63104399407679,
-1.62784095298482,-1.62519509499241,-1.62364044872693,-1.62225638809367,
-1.62054783360161,-1.61793650478277,-1.60584462045305,-1.59889974118267,
-1.55509820923944,-1.54800473144218,-1.54642858847634,-1.54553464041386,
-1.54475834997213,-1.54376420841648,-1.54170856799923,-1.5142139133888,
-1.48566929350021,-1.47251844714414,-1.46968473067084,-1.46807814025253,
-1.46683432537117,-1.46521012818052,-1.46237396633077,-1.45067204613949,
-1.44460146148795,-1.4005529965357,-1.39248476217533,-1.39084683611567,
-1.38993929508306,-1.38916441346297,-1.38818897412444,-1.38629006814448,
-1.37462850018787,-1.33739622727743,-1.32411976353444,-1.31607816499716,
-1.31366267372027,-1.31214834641487,-1.31074968885041,-1.30894493243135,
-1.30595340432594,-1.28639492673917,-1.25490722278886,-1.24285582497432,
-1.23664232804476,-1.23513061408447,-1.23425081626536,-1.23347196268052,
-1.23247162349808,-1.23081955340855,-1.22102261221577,-1.1848116113587,
-1.16952034496615,-1.16063618711611,-1.15813474793616,-1.15660138114605,
-1.15520815376355,-1.15341233308467,-1.15051622761162,-1.13335023638649,
-1.08933178059441,-1.08121658028887,-1.07957576491946,-1.07866752615317,
-1.07789259797486,-1.07691779955488,-1.07502220146438,-1.063449218963,-1.02596396727725,
-1.0079534196037,-1.00363555404761,-1.00173389192165,-1.0003247311448,-0.999014467137427,
-0.996869909828757,-0.991465201524918,-0.990221588073983,-0.985796184932943,
-0.980827381378573,-0.945955797577871,-0.926334582089454,-0.924227244646424,
-0.923222828785436,-0.922445329923792,-0.921557606157399,-0.920010413397297,
-0.913331328182177,-0.871037532483332,-0.850785719417413,-0.847777190640499,
-0.845967354780583,-0.844567828470549,-0.843055611742428,-0.840650064235996,
-0.832702091163431,-0.819639154923715,-0.801648158832126),.UNSPECIFIED.);
#210=B_SPLINE_CURVE_WITH_KNOTS('',3,(#17265,#17266,#17267,#17268,#17269,
#17270,#17271,#17272,#17273,#17274,#17275,#17276,#17277,#17278,#17279,#17280,
#17281,#17282,#17283,#17284,#17285,#17286,#17287,#17288,#17289,#17290,#17291,
#17292,#17293,#17294,#17295,#17296,#17297,#17298,#17299,#17300,#17301,#17302,
#17303,#17304,#17305,#17306,#17307,#17308,#17309,#17310,#17311,#17312,#17313,
#17314,#17315,#17316,#17317,#17318,#17319,#17320,#17321,#17322,#17323,#17324,
#17325,#17326,#17327,#17328,#17329,#17330,#17331,#17332,#17333,#17334,#17335,
#17336,#17337,#17338,#17339,#17340,#17341,#17342,#17343,#17344),
 .UNSPECIFIED.,.F.,.F.,(4,2,2,2,2,2,2,2,2,2,2,2,2,2,2,2,2,2,2,2,2,2,2,2,
2,2,2,2,2,2,2,2,2,2,2,2,2,2,2,4),(-0.179694752014396,-0.169232971543531,
-0.167146791452086,-0.16614665326122,-0.16539187472898,-0.165389478319393,
-0.165387101742208,-0.165384730808494,-0.16538237492749,-0.1653800340132,
-0.165377707927058,-0.165375396557726,-0.165373099830874,-0.165370817625747,
-0.165368549846061,-0.164499024789559,-0.162997007392346,-0.161151599734927,
-0.157336229071969,-0.146618052698146,-0.102467342342709,-0.0977535951278928,
-0.0963818512050153,-0.0913313288327745,-0.0892469330705607,-0.0879480189146197,
-0.0865309304732562,-0.0845823123318504,-0.0799933255352574,-0.0598141466092381,
-0.0212971210955963,-0.0157234450070977,-0.0121263351176517,-0.010839559275635,
-0.0100924296425617,-0.00934771185438471,-0.0085762850858009,-0.00755523319220333,
-0.00487600720888848,-0.000459481853183011),.UNSPECIFIED.);
#211=B_SPLINE_CURVE_WITH_KNOTS('',3,(#17345,#17346,#17347,#17348,#17349,
#17350,#17351,#17352,#17353,#17354,#17355,#17356,#17357,#17358,#17359,#17360,
#17361,#17362,#17363,#17364,#17365,#17366,#17367,#17368,#17369,#17370,#17371,
#17372,#17373,#17374,#17375,#17376,#17377,#17378,#17379,#17380,#17381,#17382,
#17383,#17384,#17385,#17386,#17387,#17388,#17389,#17390,#17391,#17392,#17393,
#17394,#17395,#17396,#17397,#17398,#17399,#17400,#17401,#17402,#17403,#17404,
#17405,#17406,#17407,#17408,#17409,#17410,#17411,#17412,#17413,#17414,#17415,
#17416,#17417,#17418,#17419,#17420,#17421,#17422,#17423,#17424,#17425,#17426,
#17427,#17428,#17429,#17430,#17431,#17432,#17433,#17434,#17435,#17436,#17437,
#17438,#17439,#17440,#17441,#17442,#17443,#17444,#17445,#17446,#17447,#17448,
#17449,#17450,#17451,#17452,#17453,#17454,#17455,#17456,#17457,#17458,#17459,
#17460,#17461,#17462,#17463,#17464,#17465,#17466,#17467,#17468,#17469,#17470,
#17471,#17472,#17473,#17474,#17475,#17476,#17477,#17478,#17479,#17480,#17481,
#17482,#17483,#17484,#17485,#17486,#17487,#17488,#17489,#17490,#17491,#17492,
#17493,#17494,#17495,#17496,#17497,#17498,#17499,#17500,#17501,#17502,#17503,
#17504,#17505,#17506,#17507,#17508,#17509,#17510,#17511,#17512,#17513,#17514,
#17515,#17516,#17517,#17518,#17519,#17520,#17521,#17522,#17523,#17524,#17525,
#17526,#17527,#17528,#17529,#17530),.UNSPECIFIED.,.F.,.F.,(4,2,2,2,2,2,
2,2,2,2,2,2,2,2,2,2,2,2,2,2,2,2,2,2,2,2,2,2,2,2,2,2,2,2,2,2,2,2,2,2,2,2,
2,2,2,2,2,2,2,2,2,2,2,2,2,2,2,2,2,2,2,2,2,2,2,2,2,2,2,2,2,2,2,2,2,2,2,2,
2,2,2,2,2,2,2,2,2,2,2,2,2,2,4),(-1.96178823063968,-1.92015699406122,-1.90104139823297,
-1.89658339907792,-1.89465740191917,-1.89324437179041,-1.89194049343592,
-1.88982885555551,-1.88461498903075,-1.84869964983826,-1.83327427643038,
-1.82348284810212,-1.81989464023885,-1.81812876418854,-1.81669536810835,
-1.81583137222111,-1.81507790016888,-1.81407815074661,-1.81199389798747,
-1.79436181259743,-1.76411834203387,-1.74534114677007,-1.74092567319364,
-1.73900706389289,-1.73759528314338,-1.73628961625884,-1.73416848131252,
-1.72889877204048,-1.69502507656166,-1.66623881527138,-1.66350831021409,
-1.66205520395792,-1.66111123142317,-1.66021681130518,-1.65946299734386,
-1.65848227298375,-1.65649435351309,-1.6431401767911,-1.59861881564175,
-1.58694975974644,-1.58421546658385,-1.58263072343693,-1.58124634635177,
-1.5795352612272,-1.57691608073556,-1.56471176216921,-1.55908942658897,
-1.51480330668824,-1.5070408173816,-1.50542125590241,-1.50451773517547,
-1.50374250353335,-1.50276178788567,-1.50077407465394,-1.48739112055412,
-1.44282019076947,-1.43121612435183,-1.42848642732634,-1.42690264174766,
-1.42551808233169,-1.4238054566201,-1.4211814603269,-1.40891309222829,-1.40334741525865,
-1.35901717229993,-1.35130564644038,-1.34968916141231,-1.34878628134226,
-1.34801093431948,-1.34702921827301,-1.34510110748023,-1.33270418476113,
-1.31888114158313,-1.29467058921394,-1.28242488009734,-1.27483782931146,
-1.27247227047646,-1.27096887426272,-1.26956618003006,-1.26773610090895,
-1.2646582394983,-1.24147854779099,-1.21236935210413,-1.20129373442427,
-1.19542203295883,-1.19393806266891,-1.19306438676141,-1.19228410124699,
-1.19127301784116,-1.18958454059045,-1.17903123747843,-1.16454368588016,
-1.16053736820673),.UNSPECIFIED.);
#212=B_SPLINE_CURVE_WITH_KNOTS('',3,(#17536,#17537,#17538,#17539,#17540,
#17541,#17542,#17543,#17544,#17545,#17546,#17547,#17548,#17549,#17550,#17551,
#17552,#17553,#17554,#17555,#17556,#17557,#17558,#17559,#17560,#17561,#17562,
#17563,#17564,#17565,#17566,#17567,#17568,#17569,#17570,#17571,#17572,#17573,
#17574,#17575,#17576,#17577,#17578,#17579,#17580,#17581,#17582,#17583,#17584,
#17585,#17586,#17587,#17588,#17589,#17590,#17591,#17592,#17593,#17594,#17595,
#17596,#17597,#17598,#17599,#17600,#17601,#17602,#17603,#17604,#17605,#17606,
#17607,#17608,#17609,#17610,#17611,#17612,#17613,#17614,#17615,#17616,#17617,
#17618,#17619,#17620,#17621,#17622,#17623,#17624,#17625,#17626,#17627,#17628,
#17629,#17630,#17631,#17632,#17633,#17634,#17635,#17636,#17637,#17638,#17639,
#17640,#17641,#17642,#17643,#17644,#17645,#17646,#17647,#17648,#17649,#17650,
#17651,#17652,#17653,#17654,#17655,#17656,#17657,#17658,#17659,#17660,#17661,
#17662,#17663,#17664,#17665,#17666,#17667,#17668,#17669,#17670,#17671,#17672,
#17673,#17674,#17675,#17676,#17677,#17678,#17679,#17680,#17681,#17682,#17683,
#17684,#17685,#17686,#17687,#17688,#17689,#17690,#17691,#17692,#17693,#17694,
#17695,#17696,#17697,#17698,#17699,#17700,#17701,#17702,#17703,#17704,#17705,
#17706,#17707,#17708,#17709,#17710,#17711,#17712,#17713,#17714,#17715,#17716,
#17717,#17718,#17719,#17720,#17721,#17722,#17723,#17724,#17725,#17726,#17727,
#17728,#17729,#17730,#17731,#17732,#17733),.UNSPECIFIED.,.F.,.F.,(4,2,2,
2,2,2,2,2,2,2,2,2,2,2,2,2,2,2,2,2,2,2,2,2,2,2,2,2,2,2,2,2,2,2,2,2,2,2,2,
2,2,2,2,2,2,2,2,2,2,2,2,2,2,2,2,2,2,2,2,2,2,2,2,2,2,2,2,2,2,2,2,2,2,2,2,
2,2,2,2,2,2,2,2,2,2,2,2,2,2,2,2,2,2,2,2,2,2,2,4),(-0.801672621689487,-0.775144182679054,
-0.769558497734334,-0.75732586504302,-0.754704200883258,-0.752992228277144,
-0.751607626219412,-0.750023163594684,-0.747290707428512,-0.735650342531249,
-0.691076411964111,-0.677723443498291,-0.675736537216563,-0.674755920727979,
-0.673980620461586,-0.67307683269042,-0.67145632385569,-0.663679860789934,
-0.619421328508415,-0.613711974726309,-0.601616336646214,-0.599004287325825,
-0.597295252096799,-0.595910804465792,-0.594324076968803,-0.591581530517489,
-0.579801835198178,-0.535324611137639,-0.522027055396067,-0.52004190189089,
-0.519061611475709,-0.518286304966448,-0.517382206407886,-0.515760382976406,
-0.507963239039879,-0.463719149825019,-0.457985908889692,-0.445916111521329,
-0.443305741762336,-0.441597187556258,-0.440212718384911,-0.438625513623674,
-0.435880993582319,-0.424074757022352,-0.37961391895947,-0.366326410313487,
-0.364341521434044,-0.363361258732845,-0.36258592368456,-0.361681733838776,
-0.36005960183359,-0.352258220424035,-0.308015335822943,-0.302277287353168,
-0.290212044304654,-0.287601906750548,-0.285893385271818,-0.284508863239945,
-0.284505233120815,-0.284501622843,-0.284498032687251,-0.284494462499623,
-0.284490912124095,-0.284487381397944,-0.284483870163517,-0.284480378246844,
-0.28291413008154,-0.280241645731619,-0.27698387756458,-0.270338009310462,
-0.225060705621588,-0.222075040441391,-0.210493825268747,-0.208597380244882,
-0.207622216437789,-0.206847034817886,-0.2059385375939,-0.204297361303713,
-0.196295979583224,-0.152205410590055,-0.146209464900609,-0.134423586151869,
-0.131579679617832,-0.129953211020496,-0.128708796484505,-0.127401460849067,
-0.125044302867417,-0.117092862636708,-0.103964735537841,-0.0903323947878016,
-0.0570799980975347,-0.0536073648076114,-0.0523386097532334,-0.0515948163220773,
-0.050805735689954,-0.0497205564985315,-0.0471733757100796,-0.0436217126386154,
-0.00046026236518319),.UNSPECIFIED.);
#213=B_SPLINE_CURVE_WITH_KNOTS('',3,(#17734,#17735,#17736,#17737,#17738,
#17739,#17740,#17741,#17742,#17743,#17744,#17745,#17746,#17747,#17748,#17749,
#17750,#17751,#17752,#17753,#17754,#17755,#17756,#17757,#17758,#17759,#17760,
#17761,#17762,#17763,#17764,#17765,#17766,#17767,#17768,#17769,#17770,#17771,
#17772,#17773,#17774,#17775,#17776,#17777,#17778,#17779,#17780,#17781),
 .UNSPECIFIED.,.F.,.F.,(4,2,2,2,2,2,2,2,2,2,2,2,2,2,2,2,2,2,2,2,2,2,2,4),
(-1.96112458302763,-1.94650977042956,-1.93972955151073,-1.93754441074125,
-1.9360235449391,-1.93472568696693,-1.93333684428161,-1.93157344354963,
-1.92878304301402,-1.91379416887626,-1.90485058299271,-1.87332820087799,
-1.86113603460614,-1.85833953920825,-1.85721326624138,-1.85641730739077,
-1.85568487705038,-1.85447230686389,-1.85135806380523,-1.81512123989301,
-1.79437839984539,-1.78721392420322,-1.78377585719125,-1.78189016740401),
 .UNSPECIFIED.);
#214=B_SPLINE_CURVE_WITH_KNOTS('',3,(#17782,#17783,#17784,#17785,#17786,
#17787,#17788,#17789,#17790,#17791,#17792,#17793,#17794,#17795,#17796,#17797,
#17798,#17799,#17800,#17801,#17802,#17803,#17804,#17805,#17806,#17807,#17808,
#17809,#17810,#17811,#17812,#17813,#17814,#17815,#17816,#17817,#17818,#17819,
#17820,#17821,#17822,#17823,#17824,#17825,#17826,#17827,#17828,#17829,#17830,
#17831,#17832,#17833,#17834,#17835,#17836,#17837,#17838,#17839,#17840,#17841,
#17842,#17843,#17844,#17845,#17846,#17847,#17848,#17849,#17850,#17851,#17852,
#17853,#17854,#17855,#17856,#17857,#17858,#17859,#17860,#17861,#17862,#17863,
#17864,#17865,#17866,#17867,#17868,#17869,#17870,#17871,#17872,#17873,#17874,
#17875,#17876,#17877,#17878,#17879,#17880,#17881,#17882,#17883,#17884,#17885,
#17886,#17887,#17888,#17889,#17890,#17891,#17892,#17893,#17894,#17895,#17896,
#17897,#17898,#17899,#17900,#17901,#17902,#17903,#17904,#17905,#17906,#17907,
#17908,#17909,#17910,#17911,#17912,#17913,#17914,#17915,#17916,#17917,#17918,
#17919,#17920,#17921,#17922,#17923,#17924,#17925,#17926,#17927,#17928,#17929,
#17930,#17931,#17932,#17933,#17934,#17935,#17936,#17937,#17938,#17939,#17940,
#17941,#17942,#17943,#17944,#17945,#17946,#17947,#17948,#17949,#17950,#17951,
#17952,#17953,#17954,#17955,#17956,#17957,#17958,#17959,#17960,#17961,#17962,
#17963,#17964,#17965,#17966,#17967,#17968,#17969,#17970,#17971,#17972,#17973,
#17974,#17975,#17976,#17977,#17978,#17979,#17980,#17981,#17982,#17983,#17984,
#17985,#17986,#17987,#17988,#17989,#17990,#17991,#17992,#17993,#17994,#17995,
#17996,#17997,#17998,#17999,#18000,#18001,#18002,#18003,#18004,#18005,#18006,
#18007,#18008,#18009,#18010,#18011,#18012,#18013,#18014,#18015,#18016,#18017,
#18018,#18019,#18020,#18021,#18022,#18023,#18024,#18025,#18026,#18027,#18028,
#18029,#18030,#18031,#18032,#18033,#18034,#18035,#18036,#18037,#18038,#18039,
#18040,#18041,#18042,#18043,#18044,#18045,#18046,#18047,#18048,#18049,#18050,
#18051,#18052,#18053,#18054,#18055,#18056,#18057,#18058,#18059,#18060,#18061,
#18062,#18063,#18064,#18065,#18066,#18067,#18068,#18069,#18070,#18071,#18072,
#18073,#18074,#18075,#18076,#18077,#18078,#18079,#18080,#18081,#18082,#18083,
#18084,#18085,#18086,#18087,#18088,#18089,#18090,#18091,#18092,#18093,#18094,
#18095),.UNSPECIFIED.,.F.,.F.,(4,2,2,2,2,2,2,2,2,2,2,2,2,2,2,2,2,2,2,2,
2,2,2,2,2,2,2,2,2,2,2,2,2,2,2,2,2,2,2,2,2,2,2,2,2,2,2,2,2,2,2,2,2,2,2,2,
2,2,2,2,2,2,2,2,2,2,2,2,2,2,2,2,2,2,2,2,2,2,2,2,2,2,2,2,2,2,2,2,2,2,2,2,
2,2,2,2,2,2,2,2,2,2,2,2,2,2,2,2,2,2,2,2,2,2,2,2,2,2,2,2,2,2,2,2,2,2,2,2,
2,2,2,2,2,2,2,2,2,2,2,2,2,2,2,2,2,2,2,2,2,2,2,2,2,2,2,2,4),(-1.16053736820673,
-1.14155815964385,-1.12262370826275,-1.11818787834328,-1.11626542160771,
-1.1148527039373,-1.11354750528723,-1.11143012648783,-1.10618429468265,
-1.07115027688277,-1.04338728244901,-1.03937817628469,-1.03808178962915,
-1.03724980244178,-1.03646175234525,-1.03551255964686,-1.03314070731746,
-1.03074109444545,-0.981266927380947,-0.964910049662874,-0.962050028113323,
-0.960265031946295,-0.958873087586267,-0.957333903794165,-0.954806484486732,
-0.945651907420497,-0.902262580384309,-0.900879376749887,-0.896366698843762,
-0.884722707525326,-0.882824190943104,-0.881848758487983,-0.881073783782946,
-0.880166028795487,-0.878527470302939,-0.870450963910527,-0.826429064686011,
-0.820424586876839,-0.808646563137754,-0.805803843465067,-0.804177951625829,
-0.802933927440493,-0.801328349738844,-0.798500164359894,-0.785445033080755,
-0.757288914631586,-0.756182832547103,-0.729242380066489,-0.727174744855765,
-0.726178112915842,-0.725401437698846,-0.724508811973903,-0.722939242715166,
-0.715944819510251,-0.672590954487486,-0.663571659366365,-0.663214084012877,
-0.661994174597095,-0.6525600816973,-0.649893889702218,-0.648323991814367,
-0.647076235546957,-0.645407525343655,-0.642285890848176,-0.623144525344255,
-0.58850660682205,-0.585022630618363,-0.573311684574237,-0.571410687320906,
-0.570434775373894,-0.569659836240935,-0.568752604340327,-0.567116207485564,
-0.559074637616738,-0.515030380572884,-0.509070757387959,-0.497245384464062,
-0.494399036238392,-0.492772408113018,-0.491528522966139,-0.48992395340734,
-0.487099945201931,-0.47410791847647,-0.446197570720464,-0.419931568170017,
-0.416437416087385,-0.415165626904609,-0.414421444616375,-0.413633116021297,
-0.412550870143094,-0.41001907495101,-0.388318914107292,-0.372381273155706,
-0.342596675566372,-0.339162386234467,-0.337405528570271,-0.336016823750962,
-0.336013415619075,-0.336010035654314,-0.336006683876058,-0.336003360004943,
-0.336000063797418,-0.33599679501583,-0.335993553405864,-0.335991052557717,
-0.335988556945046,-0.335986066159208,-0.335983580167727,-0.335981098972663,
-0.335978622572367,-0.3359761509534,-0.335973684074507,-0.335971221928687,
-0.335968764492674,-0.335966311772249,-0.335963863778011,-0.335961420468532,
-0.335958981821319,-0.335956547844142,-0.335954118517713,-0.335951693815784,
-0.335949273735142,-0.33594685825989,-0.335944447374503,-0.335942041076944,
-0.335939639347168,-0.335937242169554,-0.335934849532215,-0.335932461432634,
-0.335930077845004,-0.335927698773454,-0.335925324174456,-0.334370672665213,
-0.331724708510753,-0.328522327768988,-0.322032194702877,-0.277400704373564,
-0.273687125657739,-0.261924110268713,-0.260021026873319,-0.259044641389193,
-0.258269638856414,-0.257362693855451,-0.255727726428632,-0.247711272327178,
-0.203645198076067,-0.197717935825418,-0.185856273980575,-0.183006933107235,
-0.181379578020498,-0.180135652199593,-0.180125392469073,-0.180115487169854,
-0.180105926541083,-0.180096699279647,-0.180087790648967,-0.179857088658834),
 .UNSPECIFIED.);
#215=B_SPLINE_CURVE_WITH_KNOTS('',3,(#18100,#18101,#18102,#18103,#18104,
#18105,#18106,#18107,#18108,#18109,#18110,#18111,#18112,#18113,#18114,#18115,
#18116,#18117,#18118,#18119,#18120,#18121,#18122,#18123,#18124,#18125,#18126,
#18127,#18128,#18129,#18130,#18131,#18132,#18133,#18134,#18135,#18136,#18137,
#18138,#18139,#18140,#18141,#18142,#18143,#18144,#18145,#18146,#18147,#18148,
#18149,#18150,#18151,#18152,#18153,#18154,#18155,#18156,#18157,#18158,#18159,
#18160,#18161,#18162,#18163,#18164,#18165,#18166,#18167,#18168,#18169,#18170,
#18171,#18172,#18173,#18174,#18175,#18176,#18177,#18178,#18179,#18180,#18181,
#18182,#18183,#18184,#18185,#18186,#18187,#18188,#18189,#18190,#18191,#18192,
#18193,#18194,#18195,#18196,#18197,#18198,#18199,#18200,#18201,#18202,#18203,
#18204,#18205,#18206,#18207,#18208,#18209,#18210,#18211,#18212,#18213,#18214,
#18215,#18216,#18217,#18218,#18219,#18220,#18221,#18222,#18223,#18224,#18225,
#18226,#18227,#18228,#18229,#18230,#18231,#18232,#18233,#18234,#18235,#18236,
#18237,#18238,#18239,#18240,#18241,#18242,#18243,#18244,#18245,#18246,#18247,
#18248,#18249,#18250,#18251,#18252,#18253,#18254,#18255,#18256,#18257,#18258,
#18259,#18260,#18261,#18262,#18263,#18264,#18265,#18266,#18267,#18268,#18269,
#18270,#18271,#18272,#18273,#18274,#18275,#18276,#18277,#18278,#18279,#18280,
#18281,#18282,#18283,#18284,#18285,#18286,#18287,#18288,#18289,#18290,#18291,
#18292,#18293,#18294,#18295,#18296,#18297,#18298,#18299,#18300,#18301,#18302,
#18303,#18304,#18305,#18306,#18307,#18308,#18309,#18310,#18311,#18312,#18313,
#18314,#18315,#18316,#18317,#18318,#18319,#18320,#18321,#18322,#18323,#18324,
#18325,#18326,#18327,#18328,#18329,#18330,#18331,#18332,#18333,#18334,#18335,
#18336,#18337,#18338,#18339,#18340,#18341),.UNSPECIFIED.,.F.,.F.,(4,2,2,
2,2,2,2,2,2,2,2,2,2,2,2,2,2,2,2,2,2,2,2,2,2,2,2,2,2,2,2,2,2,2,2,2,2,2,2,
2,2,2,2,2,2,2,2,2,2,2,2,2,2,2,2,2,2,2,2,2,2,2,2,2,2,2,2,2,2,2,2,2,2,2,2,
2,2,2,2,2,2,2,2,2,2,2,2,2,2,2,2,2,2,2,2,2,2,2,2,2,2,2,2,2,2,2,2,2,2,2,2,
2,2,2,2,2,2,2,2,2,4),(-1.78172815281824,-1.77253372019698,-1.76631370808231,
-1.76480570691446,-1.7639201043268,-1.76314274020048,-1.76213622478509,
-1.76049885300652,-1.75098779831253,-1.74641201713466,-1.74269643920981,
-1.69942310822093,-1.69342224665427,-1.68904750588581,-1.68713860201849,
-1.6857220330961,-1.68442354327318,-1.68267268132171,-1.67839240588933,
-1.67456158001473,-1.670979313909,-1.67029906550083,-1.66125482516073,-1.61780714154226,
-1.61079304046626,-1.6092225582893,-1.60832996284903,-1.60755365809344,
-1.6065579439109,-1.60449371496109,-1.577463354171,-1.54857547056023,-1.53534094091444,
-1.53250242558939,-1.53089498173639,-1.52965138168029,-1.52802871193439,
-1.52519838164536,-1.51356354338677,-1.50743475020068,-1.46342973770787,
-1.45531820383914,-1.45367798002095,-1.45277004835105,-1.45199536982876,
-1.45102086970807,-1.44912580534688,-1.43755455489337,-1.40007365989095,
-1.38690550936001,-1.37891137868578,-1.37650129676547,-1.37498836004355,
-1.37358962189756,-1.37178284693218,-1.36878381809816,-1.34890082833157,
-1.30631432665826,-1.29953938942786,-1.29798547850884,-1.29709639563306,
-1.29631932470044,-1.29531760128442,-1.29369671814283,-1.28451322332276,
-1.2816370041638,-1.24423088930667,-1.2312006579526,-1.22326641013149,-1.22086263665544,
-1.21935098716401,-1.21795161020848,-1.21614143787634,-1.21313117111143,
-1.19280221892162,-1.1505455793434,-1.14388510284953,-1.14233938100341,
-1.14145204825295,-1.14067459181924,-1.13966984225465,-1.13756041877337,
-1.11792532820679,-1.08985518461517,-1.07097999978118,-1.06655189688075,
-1.06463088112568,-1.06321849438777,-1.06191308656034,-1.05979420877457,
-1.05453894974272,-1.01993907672026,-1.00403900251007,-0.993713453888721,
-0.989993277386549,-0.987353145567405,-0.986252355937933,-0.985460789879611,
-0.984721658564797,-0.983683318547428,-0.980930955099377,-0.967258431406432,
-0.949810773628827,-0.916692347775683,-0.911416131731427,-0.909293675577322,
-0.90798761113116,-0.906575718096371,-0.904657524327172,-0.900245519868065,
-0.88149482297644,-0.851082879833142,-0.845864837668614,-0.833362401812989,
-0.831430138514274,-0.830447532049146,-0.829672110324767,-0.828769845520952,
-0.827156202273705,-0.819490080623062,-0.801672621689487),.UNSPECIFIED.);
#216=B_SPLINE_CURVE_WITH_KNOTS('',3,(#18343,#18344,#18345,#18346,#18347,
#18348,#18349,#18350,#18351,#18352,#18353,#18354,#18355,#18356,#18357,#18358,
#18359,#18360,#18361,#18362,#18363,#18364,#18365,#18366,#18367,#18368,#18369,
#18370,#18371,#18372,#18373,#18374,#18375,#18376,#18377,#18378,#18379,#18380,
#18381,#18382,#18383,#18384,#18385,#18386,#18387,#18388,#18389,#18390),
 .UNSPECIFIED.,.F.,.F.,(4,2,2,2,2,2,2,2,2,2,2,2,2,2,2,2,2,2,2,2,2,2,2,4),
(-0.179857088658834,-0.178497778536323,-0.17570120334603,-0.172268087202898,
-0.165118744853604,-0.144450508006672,-0.108014815567082,-0.104902711334605,
-0.103690147151367,-0.10295747702479,-0.102161045916296,-0.101033764902274,
-0.0982330428526651,-0.0859987301545725,-0.0519637944323866,-0.0431570796128006,
-0.03031520294166,-0.0276534749732519,-0.0259290526584936,-0.0245433855940571,
-0.0232415172836668,-0.0216956360921947,-0.0194501360584109,-0.000459478261909778),
 .UNSPECIFIED.);
#217=B_SPLINE_CURVE_WITH_KNOTS('',3,(#18391,#18392,#18393,#18394,#18395,
#18396,#18397,#18398,#18399,#18400,#18401,#18402,#18403,#18404,#18405,#18406,
#18407,#18408,#18409,#18410,#18411,#18412,#18413,#18414,#18415,#18416,#18417,
#18418,#18419,#18420,#18421,#18422,#18423,#18424,#18425,#18426,#18427,#18428,
#18429,#18430,#18431,#18432,#18433,#18434,#18435,#18436,#18437,#18438,#18439,
#18440,#18441,#18442,#18443,#18444,#18445,#18446,#18447,#18448,#18449,#18450,
#18451,#18452,#18453,#18454,#18455,#18456,#18457,#18458,#18459,#18460,#18461,
#18462,#18463,#18464,#18465,#18466,#18467,#18468,#18469,#18470,#18471,#18472,
#18473,#18474,#18475,#18476,#18477,#18478,#18479,#18480,#18481,#18482,#18483,
#18484,#18485,#18486,#18487,#18488,#18489,#18490,#18491,#18492,#18493,#18494,
#18495,#18496,#18497,#18498,#18499,#18500,#18501,#18502,#18503,#18504,#18505,
#18506,#18507,#18508,#18509,#18510,#18511,#18512,#18513,#18514,#18515,#18516,
#18517,#18518,#18519,#18520,#18521,#18522,#18523,#18524,#18525,#18526,#18527,
#18528,#18529,#18530,#18531,#18532,#18533,#18534,#18535,#18536,#18537,#18538,
#18539,#18540,#18541,#18542,#18543,#18544,#18545,#18546,#18547,#18548,#18549,
#18550,#18551,#18552,#18553,#18554,#18555,#18556,#18557,#18558,#18559,#18560,
#18561,#18562,#18563,#18564,#18565,#18566,#18567,#18568,#18569,#18570,#18571,
#18572,#18573,#18574,#18575,#18576,#18577,#18578,#18579,#18580,#18581,#18582,
#18583,#18584,#18585,#18586,#18587,#18588,#18589,#18590,#18591,#18592,#18593,
#18594,#18595,#18596,#18597,#18598,#18599,#18600),.UNSPECIFIED.,.F.,.F.,
(4,2,2,2,2,2,2,2,2,2,2,2,2,2,2,2,2,2,2,2,2,2,2,2,2,2,2,2,2,2,2,2,2,2,2,
2,2,2,2,2,2,2,2,2,2,2,2,2,2,2,2,2,2,2,2,2,2,2,2,2,2,2,2,2,2,2,2,2,2,2,2,
2,2,2,2,2,2,2,2,2,2,2,2,2,2,2,2,2,2,2,2,2,2,2,2,2,2,2,2,2,2,2,2,2,4),(-1.96079121561173,
-1.91694482162004,-1.91024146039047,-1.90869345153882,-1.90780605107279,
-1.90702935167909,-1.90602667259015,-1.90392545789794,-1.88480510825376,
-1.86489414423652,-1.84667203000836,-1.83880113263009,-1.83512296427284,
-1.83217578327906,-1.83054790398943,-1.83053360022794,-1.83051903681914,
-1.83050420539703,-1.83048909725358,-1.83047370331781,-1.83045801352482,
-1.83044201745044,-1.830425706684,-1.83041455064203,-1.83040235418818,-1.83038901082079,
-1.83037440138794,-1.83035839225484,-1.82897501105994,-1.82726802395791,
-1.82466045321368,-1.81261263536704,-1.80685955812779,-1.76269065445403,
-1.7548171464742,-1.75319147251431,-1.75228692665544,-1.75151228166359,
-1.75053418571882,-1.74899038080902,-1.7411403549141,-1.70476034992802,
-1.68236974208065,-1.67906858564697,-1.6763664185471,-1.67479487218404,
-1.67355170692737,-1.67192590954822,-1.66908072181032,-1.65725628704226,
-1.65129912473464,-1.60725393172834,-1.5992157412494,-1.59758012270399,
-1.59667334666993,-1.59589880898111,-1.59492342274383,-1.59302350816615,
-1.58131972043172,-1.57766139359075,-1.53300710403504,-1.52313826341641,
-1.52054725289542,-1.51899456060461,-1.51760638917655,-1.51584807551323,
-1.51240420339761,-1.48353506331741,-1.46648374147773,-1.44500197000472,
-1.44247165961581,-1.44139003310733,-1.44060215146508,-1.43985838708379,
-1.43858730386408,-1.43509507960738,-1.40894868923879,-1.38100156106593,
-1.36800274037116,-1.365179410787,-1.36357552072257,-1.36233229776347,-1.36070673491446,
-1.35786274847095,-1.34605424190649,-1.34008185195058,-1.29604389366619,
-1.28799375367975,-1.28635738497572,-1.28545042308891,-1.2846758668287,
-1.28370063596442,-1.28180155177318,-1.27012057123348,-1.25369578333642,
-1.22547135538671,-1.21240125801682,-1.2095731164756,-1.20796801724572,
-1.2067245741268,-1.20509974776509,-1.20225965961727,-1.19050327604798,
-1.1844805867176,-1.1601095629489),.UNSPECIFIED.);
#218=B_SPLINE_CURVE_WITH_KNOTS('',3,(#18606,#18607,#18608,#18609,#18610,
#18611,#18612,#18613,#18614,#18615,#18616,#18617,#18618,#18619,#18620,#18621,
#18622,#18623,#18624,#18625,#18626,#18627,#18628,#18629,#18630,#18631,#18632,
#18633,#18634,#18635,#18636,#18637,#18638,#18639,#18640,#18641,#18642,#18643,
#18644,#18645,#18646,#18647,#18648,#18649,#18650,#18651,#18652,#18653,#18654,
#18655,#18656,#18657,#18658,#18659,#18660,#18661,#18662,#18663,#18664,#18665,
#18666,#18667,#18668,#18669,#18670,#18671,#18672,#18673,#18674,#18675,#18676,
#18677,#18678,#18679,#18680,#18681,#18682,#18683,#18684,#18685,#18686,#18687,
#18688,#18689,#18690,#18691,#18692,#18693,#18694,#18695,#18696,#18697,#18698,
#18699,#18700,#18701,#18702,#18703,#18704,#18705,#18706,#18707,#18708,#18709,
#18710,#18711,#18712,#18713,#18714,#18715,#18716,#18717,#18718,#18719,#18720,
#18721,#18722,#18723,#18724,#18725,#18726,#18727,#18728,#18729,#18730,#18731,
#18732,#18733,#18734,#18735,#18736,#18737,#18738,#18739,#18740,#18741,#18742,
#18743,#18744,#18745,#18746,#18747,#18748,#18749,#18750,#18751,#18752,#18753,
#18754,#18755,#18756,#18757,#18758,#18759,#18760,#18761,#18762,#18763,#18764,
#18765,#18766,#18767,#18768,#18769,#18770,#18771,#18772,#18773,#18774,#18775,
#18776,#18777,#18778,#18779,#18780,#18781,#18782,#18783,#18784,#18785,#18786,
#18787,#18788,#18789,#18790,#18791),.UNSPECIFIED.,.F.,.F.,(4,2,2,2,2,2,
2,2,2,2,2,2,2,2,2,2,2,2,2,2,2,2,2,2,2,2,2,2,2,2,2,2,2,2,2,2,2,2,2,2,2,2,
2,2,2,2,2,2,2,2,2,2,2,2,2,2,2,2,2,2,2,2,2,2,2,2,2,2,2,2,2,2,2,2,2,2,2,2,
2,2,2,2,2,2,2,2,2,2,2,2,2,2,4),(-0.801883478262616,-0.796942743005185,-0.767998750680466,
-0.740967488840241,-0.738901381511447,-0.737904955494984,-0.737128189429027,
-0.73623516297459,-0.734664170188142,-0.727651551007394,-0.684215617767987,
-0.675179910689682,-0.674564397621058,-0.671555310128778,-0.664859244302258,
-0.662179926777577,-0.660449958259594,-0.659063645598381,-0.657491113644681,
-0.654813712089845,-0.643911738186813,-0.598774695165539,-0.585139571457424,
-0.583143321661039,-0.582160704583504,-0.581385095862041,-0.580482408693454,
-0.578867502150835,-0.571185944167539,-0.526839180605354,-0.521237384782666,
-0.509017953759545,-0.506396687844682,-0.504684598640432,-0.503299652438316,
-0.501714521962304,-0.498980221802812,-0.487321310764517,-0.442746563208531,
-0.429396212262029,-0.427408978772931,-0.42642814162249,-0.425652637927385,
-0.424748579728398,-0.423127503005166,-0.415346742533404,-0.371078218393625,
-0.365364769018602,-0.353268784117248,-0.350656234532991,-0.348946804686762,
-0.347561992616929,-0.345974798180025,-0.343231319709185,-0.331445659475355,
-0.286958584810694,-0.273658640608339,-0.271672996516007,-0.270692452684378,
-0.269916940281395,-0.26901259534087,-0.267499299905258,-0.264587039832033,
-0.243056010195007,-0.205262123477829,-0.198898661972958,-0.195178796563468,
-0.19338813349005,-0.191995136447937,-0.190458203953769,-0.187973943304827,
-0.179263845213553,-0.164341118946122,-0.142633057238069,-0.130097698415107,
-0.126991715461381,-0.117705944672987,-0.116079246282222,-0.115075574035733,
-0.114298036772574,-0.113409582779292,-0.112474952353912,-0.109114061319104,
-0.0875220680580351,-0.0700306888754584,-0.0428956979680085,-0.0394556561690335,
-0.0376972505485617,-0.0363080017449152,-0.0347530512650087,-0.0331437931308085,
-0.0307454907072447,-0.000459705691028188),.UNSPECIFIED.);
#219=B_SPLINE_CURVE_WITH_KNOTS('',3,(#18792,#18793,#18794,#18795,#18796,
#18797,#18798,#18799,#18800,#18801,#18802,#18803,#18804,#18805,#18806,#18807,
#18808,#18809,#18810,#18811,#18812,#18813,#18814,#18815,#18816,#18817,#18818,
#18819,#18820,#18821,#18822,#18823,#18824,#18825,#18826,#18827,#18828,#18829,
#18830,#18831,#18832,#18833,#18834,#18835),.UNSPECIFIED.,.F.,.F.,(4,2,2,
2,2,2,2,2,2,2,2,2,2,2,2,2,2,2,2,2,2,4),(-1.96072017599113,-1.92534306313198,
-1.92268432270731,-1.92125856958759,-1.92032606841099,-1.91943931152633,
-1.91866220733764,-1.91765771170252,-1.91554810917444,-1.89601694840939,
-1.88267789013014,-1.86761833902883,-1.84962034927292,-1.84481937820509,
-1.84327215882423,-1.84176054561153,-1.84036174603569,-1.83855308551815,
-1.83554699819581,-1.81535510840621,-1.78465470035516,-1.78172815281824),
 .UNSPECIFIED.);
#220=B_SPLINE_CURVE_WITH_KNOTS('',3,(#18836,#18837,#18838,#18839,#18840,
#18841,#18842,#18843,#18844,#18845,#18846,#18847,#18848,#18849,#18850,#18851,
#18852,#18853,#18854,#18855,#18856,#18857,#18858,#18859,#18860,#18861,#18862,
#18863,#18864,#18865,#18866,#18867,#18868,#18869,#18870,#18871,#18872,#18873,
#18874,#18875,#18876,#18877,#18878,#18879,#18880,#18881,#18882,#18883,#18884,
#18885,#18886,#18887,#18888,#18889,#18890,#18891,#18892,#18893,#18894,#18895,
#18896,#18897,#18898,#18899,#18900,#18901,#18902,#18903,#18904,#18905,#18906,
#18907,#18908,#18909,#18910,#18911,#18912,#18913,#18914,#18915,#18916,#18917,
#18918,#18919,#18920,#18921,#18922,#18923,#18924,#18925,#18926,#18927,#18928,
#18929,#18930,#18931,#18932,#18933,#18934,#18935,#18936,#18937,#18938,#18939,
#18940,#18941,#18942,#18943,#18944,#18945,#18946,#18947,#18948,#18949,#18950,
#18951,#18952,#18953,#18954,#18955,#18956,#18957,#18958,#18959,#18960,#18961,
#18962,#18963,#18964,#18965,#18966,#18967,#18968,#18969,#18970,#18971,#18972,
#18973,#18974,#18975,#18976,#18977,#18978,#18979,#18980,#18981,#18982,#18983,
#18984,#18985,#18986,#18987,#18988,#18989,#18990,#18991,#18992,#18993,#18994,
#18995,#18996,#18997,#18998,#18999,#19000,#19001,#19002,#19003,#19004,#19005,
#19006,#19007,#19008,#19009,#19010,#19011,#19012,#19013,#19014,#19015,#19016,
#19017,#19018,#19019,#19020,#19021,#19022,#19023,#19024,#19025,#19026,#19027,
#19028,#19029,#19030,#19031,#19032,#19033,#19034,#19035,#19036,#19037,#19038,
#19039,#19040,#19041,#19042,#19043,#19044,#19045,#19046,#19047,#19048,#19049,
#19050,#19051,#19052,#19053,#19054,#19055,#19056,#19057,#19058,#19059,#19060,
#19061,#19062,#19063,#19064,#19065,#19066,#19067,#19068,#19069),
 .UNSPECIFIED.,.F.,.F.,(4,2,2,2,2,2,2,2,2,2,2,2,2,2,2,2,2,2,2,2,2,2,2,2,
2,2,2,2,2,2,2,2,2,2,2,2,2,2,2,2,2,2,2,2,2,2,2,2,2,2,2,2,2,2,2,2,2,2,2,2,
2,2,2,2,2,2,2,2,2,2,2,2,2,2,2,2,2,2,2,2,2,2,2,2,2,2,2,2,2,2,2,2,2,2,2,2,
2,2,2,2,2,2,2,2,2,2,2,2,2,2,2,2,2,2,2,2,4),(-1.1601095629489,-1.1404650525258,
-1.13237572786878,-1.13073687955802,-1.12982929081243,-1.12905465409522,
-1.12807990159606,-1.12618345773339,-1.11457559580012,-1.07724042304681,
-1.06399017827743,-1.0559603656158,-1.05354655589803,-1.0520328730841,-1.05063453424885,
-1.04882980490709,-1.04583749899097,-1.02622801104323,-0.988594891105816,
-0.980809613121384,-0.976307668925648,-0.974900345686425,-0.974043914980851,
-0.973258842803546,-0.972195847416052,-0.96977273851594,-0.966440876724249,
-0.957653145476374,-0.93386959672387,-0.902178664417379,-0.8987606748163,
-0.897007533974661,-0.895619493901943,-0.894062802945646,-0.891455262193384,
-0.881401582164383,-0.83623703230447,-0.833815652136543,-0.830211896673024,
-0.821308612170261,-0.819702646049156,-0.818705428116093,-0.81792881779091,
-0.817036853937235,-0.815469847794772,-0.808509526507781,-0.765294850933047,
-0.756303361201351,-0.745360590599289,-0.742585852902515,-0.740975784205431,
-0.739593272782693,-0.737914597473864,-0.734744894894185,-0.714184409329306,
-0.681456569453589,-0.677682987468375,-0.665875346229079,-0.66397087699806,
-0.662994326133177,-0.662219477553941,-0.66131304202802,-0.65967982366322,
-0.65168835055567,-0.607614474778559,-0.60171790077584,-0.589826837129825,
-0.58722925799045,-0.585524905486244,-0.5841410598657,-0.582551501768166,
-0.579795101873942,-0.567813626543313,-0.523489243444557,-0.510254944092308,
-0.50827216886184,-0.507292484226493,-0.506517380365583,-0.505613213491227,
-0.503990517728597,-0.496175082211189,-0.451959363234099,-0.446276300213773,
-0.434147243186193,-0.431533199351003,-0.429823705313632,-0.42843945163138,
-0.426853570902119,-0.424114079079006,-0.412372813868788,-0.367878219018491,
-0.354544155891085,-0.352558011656175,-0.351577625690443,-0.350802438795201,
-0.349898717316991,-0.348278174251431,-0.340498829097557,-0.296251868475326,
-0.290610397590587,-0.278433967463194,-0.275816638929641,-0.274106088301622,
-0.272721703927525,-0.271136469616492,-0.268542479953017,-0.258023075418503,
-0.212615783939347,-0.207825182258011,-0.198525129652494,-0.196898032232426,
-0.195894403735116,-0.195117087540541,-0.194229108190455,-0.19271151804396,
-0.186361782024664,-0.17958692698941),.UNSPECIFIED.);
#221=B_SPLINE_CURVE_WITH_KNOTS('',3,(#19074,#19075,#19076,#19077,#19078,
#19079,#19080,#19081,#19082,#19083,#19084,#19085,#19086,#19087,#19088,#19089,
#19090,#19091,#19092,#19093,#19094,#19095,#19096,#19097,#19098,#19099,#19100,
#19101,#19102,#19103,#19104,#19105,#19106,#19107,#19108,#19109,#19110,#19111,
#19112,#19113,#19114,#19115,#19116,#19117,#19118,#19119,#19120,#19121,#19122,
#19123,#19124,#19125,#19126,#19127,#19128,#19129,#19130,#19131,#19132,#19133,
#19134,#19135,#19136,#19137,#19138,#19139,#19140,#19141,#19142,#19143,#19144,
#19145,#19146,#19147,#19148,#19149,#19150,#19151,#19152,#19153,#19154,#19155,
#19156,#19157,#19158,#19159,#19160,#19161,#19162,#19163,#19164,#19165,#19166,
#19167,#19168,#19169,#19170,#19171,#19172,#19173,#19174,#19175,#19176,#19177,
#19178,#19179,#19180,#19181,#19182,#19183,#19184,#19185,#19186,#19187,#19188,
#19189,#19190,#19191,#19192,#19193,#19194,#19195,#19196,#19197,#19198,#19199,
#19200,#19201,#19202,#19203,#19204,#19205,#19206,#19207,#19208,#19209,#19210,
#19211,#19212,#19213,#19214,#19215,#19216,#19217,#19218,#19219,#19220,#19221,
#19222,#19223,#19224,#19225,#19226,#19227,#19228,#19229,#19230,#19231,#19232,
#19233,#19234,#19235,#19236,#19237,#19238,#19239,#19240,#19241,#19242,#19243,
#19244,#19245,#19246,#19247,#19248,#19249,#19250,#19251,#19252,#19253,#19254,
#19255,#19256,#19257,#19258,#19259,#19260,#19261,#19262,#19263,#19264,#19265,
#19266,#19267,#19268,#19269,#19270,#19271,#19272,#19273,#19274,#19275,#19276,
#19277,#19278,#19279,#19280,#19281,#19282,#19283,#19284,#19285,#19286,#19287,
#19288,#19289,#19290,#19291,#19292,#19293,#19294,#19295,#19296,#19297,#19298,
#19299,#19300,#19301,#19302,#19303,#19304,#19305,#19306,#19307),
 .UNSPECIFIED.,.F.,.F.,(4,2,2,2,2,2,2,2,2,2,2,2,2,2,2,2,2,2,2,2,2,2,2,2,
2,2,2,2,2,2,2,2,2,2,2,2,2,2,2,2,2,2,2,2,2,2,2,2,2,2,2,2,2,2,2,2,2,2,2,2,
2,2,2,2,2,2,2,2,2,2,2,2,2,2,2,2,2,2,2,2,2,2,2,2,2,2,2,2,2,2,2,2,2,2,2,2,
2,2,2,2,2,2,2,2,2,2,2,2,2,2,2,2,2,2,2,2,4),(-1.78228100909597,-1.77482955259016,
-1.76157546457646,-1.75354358706471,-1.75112915374112,-1.74961507015703,
-1.7482163518803,-1.74641111671003,-1.74341792728819,-1.72379216544428,
-1.68947185549358,-1.6794652988586,-1.67582352152111,-1.6740387294826,-1.67259712934658,
-1.67177662526936,-1.67100141119668,-1.67002134291365,-1.66803697625781,
-1.65475604767349,-1.61032158914733,-1.59852215776555,-1.59577836884746,
-1.59419143958521,-1.59280712252757,-1.59109864274847,-1.58848815611925,
-1.57641409994712,-1.57068026443617,-1.52641496850095,-1.5186174267709,
-1.51699561896725,-1.51609155444831,-1.51531628971783,-1.51433607356715,
-1.51235113356259,-1.49905549291884,-1.45459439368868,-1.4428285298906,
-1.44008702689787,-1.43850054537812,-1.43711609897054,-1.43540679081641,
-1.43279379356419,-1.42068428332079,-1.41498128613184,-1.37069185440041,
-1.36292075724331,-1.36130050259736,-1.36039674581166,-1.35962140073622,
-1.35864064130474,-1.35665315594087,-1.34328254864858,-1.29868694333994,
-1.28710534855124,-1.28437702223952,-1.2827933875441,-1.28140857209393,
-1.27969512548769,-1.27706892124057,-1.26477079262898,-1.22692422924379,
-1.21370679142639,-1.20710371764126,-1.20556213949451,-1.20467568102094,
-1.20389800485231,-1.20289166686687,-1.20077428181155,-1.17844643690694,
-1.17286361932347,-1.1447137165688,-1.13166047816908,-1.12883237806385,
-1.12722676967467,-1.12598267923159,-1.1243566432211,-1.12151350519676,
-1.10973115048512,-1.10373000261349,-1.05962806983969,-1.05161239979747,
-1.04997727646066,-1.04907020788959,-1.04829507054251,-1.04731846816782,
-1.04541481254306,-1.03364046047982,-1.02758303927016,-0.991002810217955,
-0.981222835820473,-0.980013101003812,-0.974617734268927,-0.972474588927608,
-0.971164473639897,-0.969754916993157,-0.967851749691,-0.963526260266344,
-0.945456019528111,-0.907997699949179,-0.896421646754376,-0.894525635184769,
-0.893550654997816,-0.892775598715743,-0.891867224511571,-0.890226209906355,
-0.88211049886817,-0.838108542293483,-0.831975987186352,-0.820342143876954,
-0.817510873882053,-0.815887452833581,-0.814643168161072,-0.813034705308378,
-0.810194011031848,-0.801883478262616),.UNSPECIFIED.);
#222=B_SPLINE_CURVE_WITH_KNOTS('',3,(#19309,#19310,#19311,#19312,#19313,
#19314,#19315,#19316,#19317,#19318,#19319,#19320,#19321,#19322,#19323,#19324,
#19325,#19326,#19327,#19328,#19329,#19330,#19331,#19332,#19333,#19334,#19335,
#19336,#19337,#19338,#19339,#19340,#19341,#19342,#19343,#19344,#19345,#19346,
#19347,#19348,#19349,#19350),.UNSPECIFIED.,.F.,.F.,(4,2,2,2,2,2,2,2,2,2,
2,2,2,2,2,2,2,2,2,2,4),(-0.17958692698941,-0.17386743549034,-0.145639157150684,
-0.123567275624923,-0.120513468693085,-0.118690452328767,-0.117288958496497,
-0.115782718022685,-0.114243576408732,-0.109533175038598,-0.0901174104874177,
-0.0748291750643691,-0.045346741968868,-0.0418850008757082,-0.0406182111285593,
-0.0398750029645828,-0.0390860743667612,-0.0380003577072798,-0.0367873172160553,
-0.0346756350602518,-0.000459986905719233),.UNSPECIFIED.);
#223=B_SPLINE_CURVE_WITH_KNOTS('',3,(#19351,#19352,#19353,#19354,#19355,
#19356,#19357,#19358,#19359,#19360,#19361,#19362,#19363,#19364,#19365,#19366,
#19367,#19368,#19369,#19370,#19371,#19372,#19373,#19374,#19375,#19376,#19377,
#19378,#19379,#19380,#19381,#19382,#19383,#19384,#19385,#19386,#19387,#19388,
#19389,#19390,#19391,#19392,#19393,#19394,#19395,#19396,#19397,#19398,#19399,
#19400,#19401,#19402,#19403,#19404,#19405,#19406,#19407,#19408,#19409,#19410,
#19411,#19412,#19413,#19414,#19415,#19416,#19417,#19418,#19419,#19420,#19421,
#19422,#19423,#19424,#19425,#19426,#19427,#19428,#19429,#19430,#19431,#19432,
#19433,#19434,#19435,#19436,#19437,#19438,#19439,#19440,#19441,#19442,#19443,
#19444,#19445,#19446,#19447,#19448,#19449,#19450,#19451,#19452,#19453,#19454,
#19455,#19456,#19457,#19458,#19459,#19460,#19461,#19462,#19463,#19464,#19465,
#19466,#19467,#19468,#19469,#19470,#19471,#19472,#19473,#19474,#19475,#19476,
#19477,#19478,#19479,#19480,#19481,#19482,#19483,#19484,#19485,#19486,#19487,
#19488,#19489,#19490,#19491,#19492,#19493,#19494,#19495,#19496,#19497,#19498,
#19499,#19500,#19501,#19502,#19503,#19504,#19505,#19506,#19507,#19508,#19509,
#19510,#19511,#19512,#19513,#19514,#19515,#19516,#19517,#19518,#19519,#19520,
#19521,#19522,#19523,#19524,#19525,#19526,#19527,#19528,#19529,#19530,#19531,
#19532,#19533,#19534),.UNSPECIFIED.,.F.,.F.,(4,2,2,2,2,2,2,2,2,2,2,2,2,
2,2,2,2,2,2,2,2,2,2,2,2,2,2,2,2,2,2,2,2,2,2,2,2,2,2,2,2,2,2,2,2,2,2,2,2,
2,2,2,2,2,2,2,2,2,2,2,2,2,2,2,2,2,2,2,2,2,2,2,2,2,2,2,2,2,2,2,2,2,2,2,2,
2,2,2,2,2,2,4),(-1.96151746922958,-1.93727845031055,-1.92898480844812,-1.92659162702624,
-1.92498491993979,-1.92343202148895,-1.92204358143207,-1.92028481312109,
-1.9168396885906,-1.88785898840766,-1.87113312630283,-1.85057292507077,
-1.84724551398873,-1.84631416469784,-1.84542819473164,-1.84465087947126,
-1.84364493379295,-1.84152811838242,-1.81932918197427,-1.79790337945429,
-1.78131157110743,-1.7719381670023,-1.76945230339913,-1.76788739961022,
-1.76650086025616,-1.76476139471517,-1.76204965271811,-1.74840992452315,
-1.7105047322141,-1.69842384303046,-1.69228729026909,-1.69077507009605,
-1.68987164801956,-1.68909662644185,-1.68811633747501,-1.68613001591616,
-1.67277769161369,-1.62826703898947,-1.61659762481968,-1.61386368015248,
-1.61227920804905,-1.61089510891462,-1.60918442042709,-1.60656594615312,
-1.5943668329289,-1.58874312157041,-1.54446754366595,-1.53670437923497,
-1.53508500239637,-1.5341816307481,-1.53340655545089,-1.53242607407969,
-1.53043895517707,-1.51706483565853,-1.47251392379055,-1.46089657373112,
-1.45816628659279,-1.45658256525736,-1.45519830481026,-1.45348636239918,
-1.45086399889714,-1.43861481869602,-1.43303537697942,-1.38872491425792,
-1.38100135470469,-1.37938435144635,-1.37848146701998,-1.37770629255487,
-1.37672502146537,-1.37473412349328,-1.3612453916283,-1.31647811126868,
-1.30515290239546,-1.30244399942862,-1.30086493780993,-1.29948009596275,
-1.2977613937601,-1.29511732468393,-1.28254011330064,-1.27724753366755,
-1.23269855765341,-1.22525982519969,-1.22366073654916,-1.22276173770474,
-1.22198607821221,-1.22099925600954,-1.21942760138736,-1.21113209034205,
-1.2067489935596,-1.20136265316979,-1.17191730528522,-1.16031565334655),
 .UNSPECIFIED.);
#224=B_SPLINE_CURVE_WITH_KNOTS('',3,(#19540,#19541,#19542,#19543,#19544,
#19545,#19546,#19547,#19548,#19549,#19550,#19551,#19552,#19553,#19554,#19555,
#19556,#19557,#19558,#19559,#19560,#19561,#19562,#19563,#19564,#19565,#19566,
#19567,#19568,#19569,#19570,#19571,#19572,#19573,#19574,#19575,#19576,#19577,
#19578,#19579,#19580,#19581,#19582,#19583,#19584,#19585,#19586,#19587,#19588,
#19589,#19590,#19591,#19592,#19593,#19594,#19595,#19596,#19597,#19598,#19599,
#19600,#19601,#19602,#19603,#19604,#19605,#19606,#19607,#19608,#19609,#19610,
#19611,#19612,#19613,#19614,#19615,#19616,#19617,#19618,#19619,#19620,#19621,
#19622,#19623,#19624,#19625,#19626,#19627,#19628,#19629,#19630,#19631,#19632,
#19633,#19634,#19635,#19636,#19637,#19638,#19639,#19640,#19641,#19642,#19643,
#19644,#19645,#19646,#19647,#19648,#19649,#19650,#19651,#19652,#19653,#19654,
#19655,#19656,#19657,#19658,#19659,#19660,#19661,#19662,#19663,#19664,#19665,
#19666,#19667,#19668,#19669,#19670,#19671,#19672,#19673,#19674,#19675,#19676,
#19677,#19678,#19679,#19680,#19681,#19682,#19683,#19684,#19685,#19686,#19687,
#19688,#19689,#19690,#19691,#19692,#19693,#19694,#19695,#19696,#19697,#19698,
#19699,#19700,#19701,#19702,#19703,#19704,#19705,#19706,#19707,#19708,#19709,
#19710,#19711,#19712,#19713,#19714,#19715,#19716,#19717,#19718,#19719,#19720,
#19721,#19722,#19723,#19724,#19725,#19726,#19727,#19728,#19729,#19730,#19731,
#19732,#19733,#19734,#19735,#19736,#19737),.UNSPECIFIED.,.F.,.F.,(4,2,2,
2,2,2,2,2,2,2,2,2,2,2,2,2,2,2,2,2,2,2,2,2,2,2,2,2,2,2,2,2,2,2,2,2,2,2,2,
2,2,2,2,2,2,2,2,2,2,2,2,2,2,2,2,2,2,2,2,2,2,2,2,2,2,2,2,2,2,2,2,2,2,2,2,
2,2,2,2,2,2,2,2,2,2,2,2,2,2,2,2,2,2,2,2,2,2,2,4),(-0.801569876662303,-0.801463858289568,
-0.800482425275218,-0.799707068486446,-0.798803891038373,-0.797186160095882,
-0.789454757931817,-0.745160175146095,-0.739502265562737,-0.727349256919827,
-0.724733330520345,-0.723023101294776,-0.721638578695533,-0.720052745901819,
-0.717314230398579,-0.705590694732003,-0.661074136886435,-0.647753922838687,
-0.645768034199026,-0.644787600629747,-0.644012288598972,-0.643108307384019,
-0.641487003347999,-0.633698223197594,-0.589447778114414,-0.583724261980592,
-0.571643756383663,-0.569032671005808,-0.567323901723564,-0.565939426837225,
-0.564352401042487,-0.561608661341011,-0.549813191712586,-0.505345166819569,
-0.492053390125155,-0.490068371466816,-0.489088086999237,-0.488312755477423,
-0.487408593589715,-0.485786571273855,-0.477986849676421,-0.433743001442838,
-0.428006870141869,-0.415939625547551,-0.413329364783807,-0.411620811727912,
-0.410236296770244,-0.408648988088626,-0.405904157778154,-0.394094529716444,
-0.349634163397666,-0.336347385742434,-0.334362465036885,-0.333382174855872,
-0.332606812307873,-0.33172075121546,-0.330158873001522,-0.328220012042088,
-0.324132738076345,-0.31225309554124,-0.270088997756828,-0.26714277861644,
-0.260278105308956,-0.25764832486264,-0.255933680916197,-0.25454865805872,
-0.252965617884811,-0.250240411818147,-0.239304301113367,-0.194252412631134,
-0.180656367313936,-0.178661400890362,-0.177679064473676,-0.176903506177318,
-0.176018823753888,-0.17447154027809,-0.17254943680273,-0.16851145891962,
-0.156847167086858,-0.137828617482657,-0.105499170228988,-0.102082215881069,
-0.100328809719274,-0.0989401639124942,-0.0973823753025414,-0.094771990863102,
-0.0846944940112641,-0.0462381770388969,-0.0391970233454014,-0.036003345961913,
-0.0248449281017594,-0.023131075511108,-0.022112466437153,-0.0213310021061866,
-0.0206041548507821,-0.0197442688011261,-0.0184954649651884,-0.013736546252949,
-0.000459443335965334),.UNSPECIFIED.);
#225=B_SPLINE_CURVE_WITH_KNOTS('',3,(#19738,#19739,#19740,#19741,#19742,
#19743,#19744,#19745,#19746,#19747,#19748,#19749,#19750,#19751,#19752,#19753,
#19754,#19755,#19756,#19757,#19758,#19759,#19760,#19761,#19762,#19763,#19764,
#19765,#19766,#19767,#19768,#19769,#19770,#19771,#19772,#19773,#19774,#19775,
#19776,#19777),.UNSPECIFIED.,.F.,.F.,(4,2,2,2,2,2,2,2,2,2,2,2,2,2,2,2,2,
2,2,4),(-1.9616930950669,-1.91882405866371,-1.91264227358543,-1.90812554288186,
-1.90618919366793,-1.90477417343448,-1.9034723736324,-1.90137279507223,
-1.89623193052963,-1.85877429407012,-1.84271434581574,-1.8343410922473,
-1.82952531234533,-1.82814087505396,-1.82740855395721,-1.82663312178802,
-1.82565027240673,-1.82409189630884,-1.81601648426919,-1.78228100909597),
 .UNSPECIFIED.);
#226=B_SPLINE_CURVE_WITH_KNOTS('',3,(#19778,#19779,#19780,#19781,#19782,
#19783,#19784,#19785,#19786,#19787,#19788,#19789,#19790,#19791,#19792,#19793,
#19794,#19795,#19796,#19797,#19798,#19799,#19800,#19801,#19802,#19803,#19804,
#19805,#19806,#19807,#19808,#19809,#19810,#19811,#19812,#19813,#19814,#19815,
#19816,#19817,#19818,#19819,#19820,#19821,#19822,#19823,#19824,#19825,#19826,
#19827,#19828,#19829,#19830,#19831,#19832,#19833,#19834,#19835,#19836,#19837,
#19838,#19839,#19840,#19841,#19842,#19843,#19844,#19845,#19846,#19847,#19848,
#19849,#19850,#19851,#19852,#19853,#19854,#19855,#19856,#19857,#19858,#19859,
#19860,#19861,#19862,#19863,#19864,#19865,#19866,#19867,#19868,#19869,#19870,
#19871,#19872,#19873,#19874,#19875,#19876,#19877,#19878,#19879,#19880,#19881,
#19882,#19883,#19884,#19885,#19886,#19887,#19888,#19889,#19890,#19891,#19892,
#19893,#19894,#19895,#19896,#19897,#19898,#19899,#19900,#19901,#19902,#19903,
#19904,#19905,#19906,#19907,#19908,#19909,#19910,#19911,#19912,#19913,#19914,
#19915,#19916,#19917,#19918,#19919,#19920,#19921,#19922,#19923,#19924,#19925,
#19926,#19927,#19928,#19929,#19930,#19931,#19932,#19933,#19934,#19935,#19936,
#19937,#19938,#19939,#19940,#19941,#19942,#19943,#19944,#19945,#19946,#19947,
#19948,#19949,#19950,#19951,#19952,#19953,#19954,#19955,#19956,#19957,#19958,
#19959,#19960,#19961,#19962,#19963,#19964,#19965,#19966,#19967,#19968,#19969,
#19970,#19971,#19972,#19973,#19974,#19975,#19976,#19977,#19978,#19979,#19980,
#19981,#19982,#19983,#19984,#19985,#19986,#19987,#19988,#19989,#19990,#19991,
#19992,#19993,#19994,#19995,#19996,#19997,#19998,#19999,#20000,#20001,#20002,
#20003,#20004,#20005,#20006,#20007,#20008,#20009,#20010,#20011,#20012,#20013,
#20014,#20015,#20016,#20017,#20018,#20019,#20020,#20021,#20022,#20023,#20024,
#20025),.UNSPECIFIED.,.F.,.F.,(4,2,2,2,2,2,2,2,2,2,2,2,2,2,2,2,2,2,2,2,
2,2,2,2,2,2,2,2,2,2,2,2,2,2,2,2,2,2,2,2,2,2,2,2,2,2,2,2,2,2,2,2,2,2,2,2,
2,2,2,2,2,2,2,2,2,2,2,2,2,2,2,2,2,2,2,2,2,2,2,2,2,2,2,2,2,2,2,2,2,2,2,2,
2,2,2,2,2,2,2,2,2,2,2,2,2,2,2,2,2,2,2,2,2,2,2,2,2,2,2,2,2,2,2,4),(-1.16031565334655,
-1.1523673019911,-1.14785507366041,-1.14591960065616,-1.14450483217052,
-1.14320299451157,-1.14110276182394,-1.13595736912939,-1.13460617764447,
-1.12997769923691,-1.12915159021155,-1.1288777943079,-1.08582161433698,
-1.07510385683424,-1.06936172998066,-1.06788882347475,-1.06701764560893,
-1.06623680838649,-1.06522136664119,-1.06351787069468,-1.05260983184458,
-1.04675761591003,-1.01355437678732,-0.996263279450873,-0.992039456976342,
-0.990154732372975,-0.988748474761843,-0.987433959098141,-0.985621800596761,
-0.980984198074936,-0.959588741131954,-0.92576208051337,-0.914449902568713,
-0.912564864604286,-0.911592393020659,-0.910817679489454,-0.909907804202454,
-0.908259241851401,-0.90000757724465,-0.856125099040339,-0.849884600885847,
-0.838365541213197,-0.835544122640188,-0.833923202066467,-0.832679172460978,
-0.831069068772479,-0.828219726257148,-0.814819825257841,-0.785260983898237,
-0.775814978572803,-0.759029000198427,-0.756952758562451,-0.755954511199894,
-0.75517776137945,-0.754286382142591,-0.752722173486889,-0.7458027557844,
-0.702743196561065,-0.693781739159207,-0.682632497009242,-0.679842214769354,
-0.678228514269354,-0.676859329700738,-0.67519055587507,-0.672068055233415,
-0.652894887063777,-0.617891491203387,-0.615207746475259,-0.61253423219707,
-0.602937515005818,-0.601295399164744,-0.600298043200082,-0.599519607036988,
-0.598638133757354,-0.597118680723868,-0.590805287070827,-0.578462765474866,
-0.547112847724725,-0.538152799437653,-0.526991399645208,-0.524200014558887,
-0.522586024766068,-0.52121680016192,-0.519548229843057,-0.516426866112247,
-0.497287482406008,-0.462657118186587,-0.459167059164731,-0.447458225940103,
-0.445557429421433,-0.444581607127788,-0.443806732168894,-0.442899567288428,
-0.441263270823624,-0.433221786600635,-0.389181586661826,-0.383221713536389,
-0.371398118994128,-0.368552069041258,-0.366925589097279,-0.36568180558335,
-0.364077353349327,-0.361253511728051,-0.348261525455421,-0.320349458563087,
-0.294096609446201,-0.290598350985114,-0.289325978397033,-0.288581721547749,
-0.287839004420659,-0.286880814434218,-0.284802913401485,-0.282006636755118,
-0.251607225783504,-0.219524941223758,-0.214244036214387,-0.21212093211589,
-0.210814870378466,-0.209403295591622,-0.207486098587411,-0.203078922671946,
-0.197086732289873,-0.181309345770682,-0.179896456144152),.UNSPECIFIED.);
#227=B_SPLINE_CURVE_WITH_KNOTS('',3,(#20030,#20031,#20032,#20033,#20034,
#20035,#20036,#20037,#20038,#20039,#20040,#20041,#20042,#20043,#20044,#20045,
#20046,#20047,#20048,#20049,#20050,#20051,#20052,#20053,#20054,#20055,#20056,
#20057,#20058,#20059,#20060,#20061,#20062,#20063,#20064,#20065,#20066,#20067,
#20068,#20069,#20070,#20071,#20072,#20073,#20074,#20075,#20076,#20077,#20078,
#20079,#20080,#20081,#20082,#20083,#20084,#20085,#20086,#20087,#20088,#20089,
#20090,#20091,#20092,#20093,#20094,#20095,#20096,#20097,#20098,#20099,#20100,
#20101,#20102,#20103,#20104,#20105,#20106,#20107,#20108,#20109,#20110,#20111,
#20112,#20113,#20114,#20115,#20116,#20117,#20118,#20119,#20120,#20121,#20122,
#20123,#20124,#20125,#20126,#20127,#20128,#20129,#20130,#20131,#20132,#20133,
#20134,#20135,#20136,#20137,#20138,#20139,#20140,#20141,#20142,#20143,#20144,
#20145,#20146,#20147,#20148,#20149,#20150,#20151,#20152,#20153,#20154,#20155,
#20156,#20157,#20158,#20159,#20160,#20161,#20162,#20163,#20164,#20165,#20166,
#20167,#20168,#20169,#20170,#20171,#20172,#20173,#20174,#20175,#20176,#20177,
#20178,#20179,#20180,#20181,#20182,#20183,#20184,#20185,#20186,#20187,#20188,
#20189,#20190,#20191,#20192,#20193,#20194,#20195,#20196,#20197,#20198,#20199,
#20200,#20201,#20202,#20203,#20204,#20205,#20206,#20207,#20208,#20209,#20210,
#20211,#20212,#20213,#20214,#20215,#20216,#20217,#20218,#20219,#20220,#20221,
#20222,#20223,#20224,#20225,#20226,#20227,#20228,#20229,#20230,#20231,#20232,
#20233,#20234,#20235,#20236,#20237,#20238,#20239,#20240,#20241,#20242,#20243,
#20244,#20245,#20246,#20247,#20248,#20249,#20250,#20251,#20252,#20253,#20254,
#20255,#20256,#20257,#20258,#20259,#20260,#20261,#20262,#20263,#20264,#20265,
#20266,#20267,#20268,#20269,#20270,#20271,#20272,#20273,#20274,#20275,#20276,
#20277,#20278,#20279,#20280,#20281,#20282,#20283,#20284,#20285,#20286,#20287,
#20288,#20289,#20290,#20291,#20292,#20293,#20294,#20295,#20296,#20297),
 .UNSPECIFIED.,.F.,.F.,(4,2,2,2,2,2,2,2,2,2,2,2,2,2,2,2,2,2,2,2,2,2,2,2,
2,2,2,2,2,2,2,2,2,2,2,2,2,2,2,2,2,2,2,2,2,2,2,2,2,2,2,2,2,2,2,2,2,2,2,2,
2,2,2,2,2,2,2,2,2,2,2,2,2,2,2,2,2,2,2,2,2,2,2,2,2,2,2,2,2,2,2,2,2,2,2,2,
2,2,2,2,2,2,2,2,2,2,2,2,2,2,2,2,2,2,2,2,2,2,2,2,2,2,2,2,2,2,2,2,2,2,2,2,
2,4),(-1.78157392576435,-1.77703986719531,-1.75183319619201,-1.73827487711637,
-1.73547815848269,-1.73435161834043,-1.73355540911073,-1.73282270068874,
-1.73160957411766,-1.72849339879885,-1.69230500609923,-1.66219518654377,
-1.65966339436276,-1.65799877502422,-1.65642827813615,-1.65642456312669,
-1.65642083260329,-1.65641708641202,-1.65641332439903,-1.6564095464009,
-1.65640575226783,-1.65640194184385,-1.65639811496712,-1.65639427145904,
-1.65639041116129,-1.65638653391513,-1.65638263954875,-1.65637872789209,
-1.65637479876522,-1.65637085199926,-1.65636688740295,-1.65636290480605,
-1.65635890402627,-1.65635488486844,-1.65635084714899,-1.65634679068422,
-1.65634271542142,-1.6549889433836,-1.65327486426759,-1.6500997041622,-1.63238876722318,
-1.59967144067176,-1.58709227218365,-1.58070072137787,-1.57917549504868,
-1.57829288112802,-1.5775148975866,-1.57651998720862,-1.57440499194861,
-1.55123771017638,-1.54690886626453,-1.51845272167325,-1.50532498054874,
-1.50249305163127,-1.50088702121455,-1.49964342687909,-1.49801921388676,
-1.4951822520972,-1.48346647742908,-1.47741146468242,-1.43336194169185,
-1.42530617929179,-1.42366918431813,-1.42276194033454,-1.42198717902635,
-1.42101172114954,-1.41911227748877,-1.40743063973138,-1.37024355756011,
-1.35695941054654,-1.34891487615597,-1.34649933647858,-1.34498516636977,
-1.3435867816907,-1.34178255619808,-1.33879229544754,-1.31926699010906,
-1.28785312968101,-1.27573233182799,-1.26949544208271,-1.26798205969689,
-1.26710198542805,-1.26632335330376,-1.26532389880708,-1.26367452719552,
-1.2539283386789,-1.2515770057581,-1.21423149008515,-1.20122448856538,-1.19330057924157,
-1.19089805402565,-1.18938675998721,-1.1879874178821,-1.18617687638681,
-1.18316509291153,-1.16276749776549,-1.12056606932057,-1.11392545846318,
-1.11238128001053,-1.11149433284049,-1.11071688691739,-1.10971171822844,
-1.10759988313139,-1.08728518949668,-1.05781589971924,-1.04532672323364,
-1.03763111015008,-1.03525351936236,-1.03374758284089,-1.03234606024005,
-1.03052255846313,-1.02746691316668,-1.00530609355621,-0.980688863891826,
-0.959290533031398,-0.957173317188728,-0.956177821375156,-0.955399592326297,
-0.954516932260381,-0.952992170219633,-0.946610153339468,-0.934063253638346,
-0.901712058815225,-0.895695800147351,-0.883098238582525,-0.880452551544035,
-0.878733159612078,-0.877348005872783,-0.875768851224845,-0.873060438659509,
-0.861746850641419,-0.816934939181304,-0.803454861381081,-0.801569876662303),
 .UNSPECIFIED.);
#228=B_SPLINE_CURVE_WITH_KNOTS('',3,(#20299,#20300,#20301,#20302,#20303,
#20304,#20305,#20306,#20307,#20308,#20309,#20310,#20311,#20312,#20313,#20314,
#20315,#20316,#20317,#20318,#20319,#20320,#20321,#20322,#20323,#20324,#20325,
#20326,#20327,#20328,#20329,#20330,#20331,#20332,#20333,#20334,#20335,#20336,
#20337,#20338),.UNSPECIFIED.,.F.,.F.,(4,2,2,2,2,2,2,2,2,2,2,2,2,2,2,2,2,
2,2,4),(-0.179896456144152,-0.145985047401615,-0.135982032119122,-0.13431993856968,
-0.133316680841151,-0.132537509157973,-0.131809685279224,-0.130494634624559,
-0.126340778320527,-0.119504086046154,-0.101385875338663,-0.0636422736938331,
-0.0585183563700689,-0.056421716430441,-0.05512054055286,-0.0537052463391859,
-0.0517668127261477,-0.0472374260604156,-0.0410328162612283,-0.000460268800049601),
 .UNSPECIFIED.);
#229=B_SPLINE_CURVE_WITH_KNOTS('',3,(#20339,#20340,#20341,#20342,#20343,
#20344,#20345,#20346,#20347),.UNSPECIFIED.,.F.,.F.,(4,1,1,1,1,1,4),(179.070781254618,
179.221343132621,180.218997427939,181.216651723258,182.214306018576,183.211960313895,
184.204982640327),.UNSPECIFIED.);
#230=B_SPLINE_CURVE_WITH_KNOTS('',3,(#20353,#20354,#20355,#20356,#20357,
#20358,#20359,#20360,#20361,#20362,#20363,#20364,#20365,#20366,#20367,#20368,
#20369,#20370,#20371,#20372,#20373,#20374,#20375,#20376,#20377,#20378,#20379,
#20380,#20381,#20382,#20383,#20384,#20385,#20386,#20387,#20388,#20389,#20390,
#20391,#20392,#20393,#20394,#20395,#20396,#20397,#20398,#20399,#20400,#20401,
#20402,#20403,#20404,#20405,#20406,#20407,#20408,#20409,#20410,#20411,#20412,
#20413,#20414,#20415,#20416,#20417,#20418,#20419,#20420,#20421,#20422,#20423,
#20424,#20425,#20426,#20427,#20428,#20429,#20430,#20431,#20432,#20433,#20434,
#20435,#20436,#20437,#20438,#20439,#20440,#20441,#20442,#20443,#20444,#20445,
#20446,#20447,#20448,#20449,#20450,#20451,#20452,#20453,#20454,#20455,#20456,
#20457,#20458,#20459,#20460,#20461,#20462,#20463,#20464,#20465,#20466,#20467,
#20468,#20469,#20470,#20471,#20472,#20473,#20474,#20475,#20476,#20477,#20478,
#20479,#20480,#20481,#20482,#20483,#20484,#20485,#20486,#20487,#20488,#20489,
#20490,#20491,#20492,#20493,#20494,#20495,#20496,#20497,#20498,#20499,#20500,
#20501,#20502,#20503,#20504,#20505,#20506,#20507,#20508,#20509,#20510,#20511,
#20512,#20513,#20514,#20515,#20516,#20517,#20518,#20519,#20520,#20521,#20522,
#20523,#20524,#20525,#20526,#20527,#20528,#20529,#20530,#20531,#20532,#20533,
#20534,#20535,#20536,#20537,#20538,#20539,#20540,#20541,#20542,#20543,#20544,
#20545,#20546,#20547,#20548),.UNSPECIFIED.,.F.,.F.,(4,2,2,2,2,2,2,2,2,2,
2,2,2,2,2,2,2,2,2,2,2,2,2,2,2,2,2,2,2,2,2,2,2,2,2,2,2,2,2,2,2,2,2,2,2,2,
2,2,2,2,2,2,2,2,2,2,2,2,2,2,2,2,2,2,2,2,2,2,2,2,2,2,2,2,2,2,2,2,2,2,2,2,
2,2,2,2,2,2,2,2,2,2,2,2,2,2,2,4),(-0.801804981179806,-0.791195181952112,
-0.78820379362701,-0.78639864088365,-0.784999399902408,-0.783484166028639,
-0.781066634915162,-0.773012825789302,-0.759708368143552,-0.722486014975232,
-0.710788191922156,-0.708887092198146,-0.707910898492826,-0.707135613048346,
-0.706227820637099,-0.704590009597872,-0.696533258951253,-0.652475124541805,
-0.646421413217755,-0.63469777726604,-0.631858809355539,-0.630233423006621,
-0.628988920467047,-0.627381700427813,-0.624547636466169,-0.611409824376443,
-0.582929094133007,-0.57659321994821,-0.555382330138853,-0.553264718573913,
-0.552258140865215,-0.551480221862471,-0.550593415458993,-0.549051077822034,
-0.542442194165679,-0.500328073024698,-0.479809619561363,-0.476793655627731,
-0.474981375070188,-0.473581154106954,-0.472069373104979,-0.469667067488223,
-0.461752996108073,-0.448769074051514,-0.411484258891166,-0.408773200682247,
-0.39919795411811,-0.397556381805616,-0.396558940683188,-0.395780175377634,
-0.394898019913743,-0.393376673005521,-0.387045155925027,-0.374651345922992,
-0.343224652481315,-0.324051009245048,-0.321080607647489,-0.319281669821315,
-0.31792080664303,-0.316445009591454,-0.314913905802875,-0.312705023756506,
-0.3088518933673,-0.277970702210061,-0.245813850415554,-0.242456681833825,
-0.241205466117216,-0.240465088819104,-0.239673803790103,-0.238576055805226,
-0.235955587474011,-0.208002316387905,-0.171261442735374,-0.166086824696459,
-0.163978234720007,-0.162674368778266,-0.161288209928795,-0.159415023700057,
-0.157327606071686,-0.153775409699347,-0.127761519786595,-0.100451926709456,
-0.0880266345113613,-0.0860968103046999,-0.0851144928007718,-0.0843388085831969,
-0.0834356757270043,-0.0818190833842118,-0.0741129438788946,-0.0297790823181762,
-0.017138014229754,-0.0107741459344145,-0.00848312639086696,-0.0071444586676528,
-0.00580070256809082,-0.0044503611599955,-0.00251092333097463,-0.000459684857462615),
 .UNSPECIFIED.);
#231=B_SPLINE_CURVE_WITH_KNOTS('',3,(#20549,#20550,#20551,#20552,#20553,
#20554,#20555,#20556,#20557,#20558,#20559,#20560,#20561,#20562,#20563,#20564,
#20565,#20566,#20567,#20568,#20569,#20570,#20571,#20572,#20573,#20574,#20575,
#20576,#20577,#20578,#20579,#20580,#20581,#20582,#20583,#20584,#20585,#20586,
#20587,#20588,#20589,#20590,#20591,#20592,#20593,#20594,#20595,#20596,#20597,
#20598,#20599,#20600,#20601,#20602,#20603,#20604,#20605,#20606,#20607,#20608,
#20609,#20610,#20611,#20612,#20613,#20614,#20615,#20616,#20617,#20618,#20619,
#20620,#20621,#20622,#20623,#20624,#20625,#20626,#20627,#20628,#20629,#20630),
 .UNSPECIFIED.,.F.,.F.,(4,2,2,2,2,2,2,2,2,2,2,2,2,2,2,2,2,2,2,2,2,2,2,2,
2,2,2,2,2,2,2,2,2,2,2,2,2,2,2,2,4),(-1.96076531947618,-1.94084069828309,
-1.89859390740446,-1.89193598296996,-1.89039057645452,-1.88950337962962,
-1.8887260128179,-1.8877213401337,-1.88609061961138,-1.87671706757189,-1.87374154668446,
-1.83654431366111,-1.82357963776505,-1.81834047535616,-1.81559441560497,
-1.81384023680584,-1.81220579194079,-1.81219072987945,-1.81217546787841,
-1.81215999766016,-1.81214431057571,-1.81212839757627,-1.81211224918606,
-1.81209585547706,-1.81208474088437,-1.81207280521556,-1.81205997335984,
-1.81204616119084,-1.8120312741524,-1.81201520556063,-1.81199783454238,
-1.81197902354186,-1.81195861526728,-1.81193642849298,-1.81191225379885,
-1.8118858491898,-1.81185693010414,-1.81049833731243,-1.80873027082396,
-1.8053131326592,-1.78157392576435),.UNSPECIFIED.);
#232=B_SPLINE_CURVE_WITH_KNOTS('',3,(#20632,#20633,#20634,#20635,#20636,
#20637),.UNSPECIFIED.,.F.,.F.,(4,1,1,4),(184.204982640327,184.209614609213,
185.207268904532,185.353966561798),.UNSPECIFIED.);
#233=B_SPLINE_CURVE_WITH_KNOTS('',3,(#20638,#20639,#20640,#20641,#20642,
#20643,#20644,#20645,#20646,#20647,#20648,#20649,#20650,#20651,#20652,#20653,
#20654,#20655,#20656,#20657,#20658,#20659,#20660,#20661,#20662,#20663,#20664,
#20665,#20666,#20667,#20668,#20669,#20670,#20671,#20672,#20673,#20674,#20675,
#20676,#20677,#20678,#20679,#20680,#20681,#20682,#20683,#20684,#20685,#20686,
#20687,#20688,#20689,#20690,#20691,#20692,#20693,#20694,#20695,#20696,#20697,
#20698,#20699,#20700,#20701,#20702,#20703,#20704,#20705,#20706,#20707,#20708,
#20709,#20710,#20711,#20712,#20713,#20714,#20715,#20716,#20717,#20718,#20719,
#20720,#20721,#20722,#20723,#20724,#20725,#20726,#20727,#20728,#20729,#20730,
#20731,#20732,#20733,#20734,#20735,#20736,#20737,#20738,#20739,#20740,#20741,
#20742,#20743,#20744,#20745,#20746,#20747,#20748,#20749,#20750,#20751,#20752,
#20753,#20754,#20755,#20756,#20757,#20758,#20759,#20760,#20761,#20762,#20763,
#20764,#20765,#20766,#20767,#20768,#20769,#20770,#20771,#20772,#20773,#20774,
#20775,#20776,#20777,#20778,#20779,#20780,#20781,#20782,#20783,#20784,#20785,
#20786,#20787,#20788,#20789,#20790,#20791,#20792,#20793,#20794,#20795,#20796,
#20797,#20798,#20799,#20800,#20801,#20802,#20803,#20804,#20805,#20806,#20807,
#20808,#20809,#20810,#20811,#20812,#20813,#20814,#20815,#20816,#20817,#20818,
#20819,#20820,#20821,#20822,#20823),.UNSPECIFIED.,.F.,.F.,(4,2,2,2,2,2,
2,2,2,2,2,2,2,2,2,2,2,2,2,2,2,2,2,2,2,2,2,2,2,2,2,2,2,2,2,2,2,2,2,2,2,2,
2,2,2,2,2,2,2,2,2,2,2,2,2,2,2,2,2,2,2,2,2,2,2,2,2,2,2,2,2,2,2,2,2,2,2,2,
2,2,2,2,2,2,2,2,2,2,2,2,2,2,4),(-1.96154615893119,-1.9204301144835,-1.91421112519999,
-1.90967349501717,-1.90773406611444,-1.90631898335972,-1.90501865184091,
-1.90292481837855,-1.89781502448428,-1.85984841609893,-1.84188976150091,
-1.83507397559582,-1.83092965281337,-1.82961639162936,-1.8288888845317,
-1.82810988983151,-1.82710620718605,-1.82544205879453,-1.81538722150474,
-1.77627551365403,-1.76309687074975,-1.75509850389648,-1.75268831831728,
-1.7511755908826,-1.74977723604173,-1.74797122575642,-1.74497406136101,
-1.72515117763501,-1.69090606373307,-1.68099351808462,-1.67737544669124,
-1.67559918847939,-1.67416313343874,-1.67334463311578,-1.67256962720246,
-1.67158833532593,-1.66959662616788,-1.65607040342538,-1.61123318159724,
-1.60001893629797,-1.59731881511132,-1.59574192996661,-1.59435722115097,
-1.59263637003297,-1.58998462886248,-1.57728267596355,-1.571417884776,-1.52729146054624,
-1.52013006658682,-1.51854954888397,-1.51765475940199,-1.51687878551326,
-1.51588642844732,-1.51383919085038,-1.48594169652985,-1.4576946664555,
-1.44461852412824,-1.44178988638511,-1.44018462139884,-1.43894110435512,
-1.43731625918759,-1.43447633623332,-1.4227233563749,-1.41669657975516,
-1.37268069735914,-1.36458805425462,-1.36294894452887,-1.36204126695385,
-1.36126658844729,-1.36029182671763,-1.35839549260358,-1.34679253028865,
-1.34225651823929,-1.30852822021364,-1.29120857661103,-1.28698143329094,
-1.28509636693623,-1.2836903049292,-1.28237629743356,-1.28056535202266,
-1.27593362407305,-1.23290256833061,-1.22479443634851,-1.21428031910573,
-1.20861311665486,-1.20714683633494,-1.20627721677358,-1.20549612938089,
-1.20447819929962,-1.20276590325398,-1.19163256212389,-1.18843259486761,
-1.1604089144409),.UNSPECIFIED.);
#234=B_SPLINE_CURVE_WITH_KNOTS('',3,(#20828,#20829,#20830,#20831,#20832,
#20833,#20834,#20835,#20836,#20837,#20838,#20839,#20840,#20841,#20842,#20843,
#20844,#20845,#20846,#20847,#20848,#20849,#20850,#20851,#20852,#20853,#20854,
#20855,#20856,#20857,#20858,#20859,#20860,#20861,#20862,#20863,#20864,#20865,
#20866,#20867,#20868,#20869,#20870,#20871,#20872,#20873,#20874,#20875,#20876,
#20877,#20878,#20879,#20880,#20881,#20882,#20883,#20884,#20885,#20886,#20887,
#20888,#20889,#20890,#20891,#20892,#20893,#20894,#20895,#20896,#20897,#20898,
#20899,#20900,#20901,#20902,#20903,#20904,#20905,#20906,#20907,#20908,#20909,
#20910,#20911,#20912,#20913,#20914,#20915,#20916,#20917,#20918,#20919,#20920,
#20921,#20922,#20923,#20924,#20925,#20926,#20927,#20928,#20929,#20930,#20931,
#20932,#20933,#20934,#20935,#20936,#20937,#20938,#20939,#20940,#20941,#20942,
#20943,#20944,#20945,#20946,#20947,#20948,#20949,#20950,#20951,#20952,#20953,
#20954,#20955,#20956,#20957,#20958,#20959,#20960,#20961,#20962,#20963,#20964,
#20965,#20966,#20967,#20968,#20969,#20970,#20971,#20972,#20973,#20974,#20975,
#20976,#20977,#20978,#20979,#20980,#20981,#20982,#20983,#20984,#20985,#20986,
#20987,#20988,#20989,#20990,#20991,#20992,#20993,#20994,#20995,#20996,#20997,
#20998,#20999,#21000,#21001,#21002,#21003,#21004,#21005,#21006,#21007,#21008,
#21009,#21010,#21011,#21012,#21013,#21014,#21015,#21016,#21017,#21018,#21019,
#21020,#21021,#21022,#21023,#21024,#21025,#21026,#21027,#21028,#21029,#21030,
#21031,#21032,#21033,#21034,#21035,#21036,#21037,#21038,#21039,#21040,#21041,
#21042,#21043,#21044,#21045,#21046,#21047,#21048,#21049),.UNSPECIFIED.,
 .F.,.F.,(4,2,2,2,2,2,2,2,2,2,2,2,2,2,2,2,2,2,2,2,2,2,2,2,2,2,2,2,2,2,2,
2,2,2,2,2,2,2,2,2,2,2,2,2,2,2,2,2,2,2,2,2,2,2,2,2,2,2,2,2,2,2,2,2,2,2,2,
2,2,2,2,2,2,2,2,2,2,2,2,2,2,2,2,2,2,2,2,2,2,2,2,2,2,2,2,2,2,2,2,2,2,2,2,
2,2,2,2,2,2,2,4),(-1.78229182699827,-1.77770006527103,-1.74728035674964,
-1.72722535303527,-1.72265056195955,-1.72070401254425,-1.71928696319564,
-1.71798706378127,-1.71589885047568,-1.71082762541292,-1.67223444044944,
-1.64752983476097,-1.64498095721691,-1.64359685769358,-1.64268136183101,
-1.64182077443158,-1.64106521535437,-1.64006101330455,-1.63843247151083,
-1.62910925449238,-1.6243756754617,-1.5789882557114,-1.56843404951485,-1.56578431027004,
-1.56421790544764,-1.56283077099427,-1.56109153229788,-1.55838201035786,
-1.54479651559656,-1.51216480444941,-1.49015262721293,-1.48761968100296,
-1.48653711254194,-1.48574861367651,-1.48500431351154,-1.48373240483364,
-1.48023838775766,-1.45413407404517,-1.42613534393613,-1.41312006270762,
-1.4102942149044,-1.40868902900732,-1.40744486278802,-1.40581815150025,
-1.40297236355887,-1.3911587623582,-1.38518496978347,-1.34106294051767,
-1.33306838337939,-1.33143442686769,-1.33052757310081,-1.32975235514613,
-1.32877531391351,-1.32686980440679,-1.31505008398384,-1.27760856441345,
-1.26456380318881,-1.25662228690092,-1.25421709163038,-1.25270472569067,
-1.2513048071232,-1.24949410535442,-1.24648333099836,-1.22617519094581,
-1.18387963955269,-1.17720850620729,-1.17566157010041,-1.17477374504427,
-1.1739959910329,-1.17299103360034,-1.17136027695541,-1.16199793714452,
-1.14540186853179,-1.12375086261623,-1.10437341472612,-1.09988152441872,
-1.09794891733958,-1.0965340458668,-1.09523057379023,-1.09312427935216,
-1.08794685017318,-1.05113546407829,-1.0232122483063,-1.02059167294599,
-1.0194938696369,-1.01870254272551,-1.01796212380633,-1.01671083342138,
-1.01335343759903,-0.981228689407384,-0.947011206645786,-0.943932276143987,
-0.942101488150138,-0.940698213617958,-0.939194157648731,-0.936827476357734,
-0.929236059216975,-0.916980174939113,-0.892734951719288,-0.878430304643932,
-0.876064713121345,-0.866322573478264,-0.864672646487258,-0.863672714249389,
-0.86289361929424,-0.862012911520759,-0.860498201068073,-0.854252320692013,
-0.84211098432762,-0.810714702698044,-0.801804981179806),.UNSPECIFIED.);
#235=B_SPLINE_CURVE_WITH_KNOTS('',3,(#21050,#21051,#21052,#21053,#21054,
#21055,#21056,#21057,#21058,#21059,#21060,#21061,#21062,#21063,#21064,#21065,
#21066,#21067,#21068,#21069,#21070,#21071,#21072,#21073,#21074,#21075,#21076,
#21077,#21078,#21079,#21080,#21081,#21082,#21083,#21084,#21085,#21086,#21087,
#21088,#21089,#21090,#21091,#21092,#21093,#21094,#21095,#21096,#21097,#21098,
#21099,#21100,#21101,#21102,#21103,#21104,#21105,#21106,#21107,#21108,#21109,
#21110,#21111,#21112,#21113,#21114,#21115,#21116,#21117,#21118,#21119,#21120,
#21121,#21122,#21123,#21124,#21125,#21126,#21127,#21128,#21129,#21130,#21131,
#21132,#21133,#21134,#21135,#21136,#21137,#21138,#21139,#21140,#21141,#21142,
#21143,#21144,#21145,#21146,#21147,#21148,#21149,#21150,#21151,#21152,#21153,
#21154,#21155,#21156,#21157,#21158,#21159,#21160,#21161,#21162,#21163,#21164,
#21165,#21166,#21167,#21168,#21169,#21170,#21171,#21172,#21173,#21174,#21175,
#21176,#21177,#21178,#21179,#21180,#21181,#21182,#21183,#21184,#21185,#21186,
#21187,#21188,#21189,#21190,#21191,#21192,#21193,#21194,#21195,#21196,#21197,
#21198,#21199,#21200,#21201,#21202,#21203,#21204,#21205,#21206,#21207,#21208,
#21209,#21210,#21211,#21212,#21213,#21214,#21215,#21216,#21217,#21218,#21219,
#21220,#21221,#21222,#21223,#21224,#21225,#21226,#21227,#21228,#21229,#21230,
#21231,#21232,#21233,#21234,#21235,#21236,#21237,#21238,#21239,#21240,#21241,
#21242,#21243,#21244,#21245,#21246,#21247,#21248,#21249,#21250,#21251,#21252,
#21253,#21254,#21255,#21256,#21257,#21258,#21259,#21260,#21261,#21262,#21263,
#21264,#21265,#21266,#21267,#21268,#21269,#21270,#21271,#21272,#21273,#21274,
#21275,#21276,#21277,#21278,#21279,#21280,#21281),.UNSPECIFIED.,.F.,.F.,
(4,2,2,2,2,2,2,2,2,2,2,2,2,2,2,2,2,2,2,2,2,2,2,2,2,2,2,2,2,2,2,2,2,2,2,
2,2,2,2,2,2,2,2,2,2,2,2,2,2,2,2,2,2,2,2,2,2,2,2,2,2,2,2,2,2,2,2,2,2,2,2,
2,2,2,2,2,2,2,2,2,2,2,2,2,2,2,2,2,2,2,2,2,2,2,2,2,2,2,2,2,2,2,2,2,2,2,2,
2,2,2,2,2,2,2,2,4),(-1.1604089144409,-1.15301712491792,-1.1338042420669,
-1.13068051289322,-1.12901153209055,-1.12764240662223,-1.12602904408292,
-1.12324001000303,-1.11210442569331,-1.10313057710444,-1.07175088106854,
-1.05939417886841,-1.05307681964018,-1.05155711810077,-1.05067562963774,
-1.04989726168839,-1.04890010709256,-1.04725856324169,-1.03767102385391,
-1.00635729547857,-0.981218835397845,-0.976166204963473,-0.974081488014664,
-0.972782535873951,-0.971365535445268,-0.969417273943396,-0.964830224656248,
-0.944666579985529,-0.913243095579635,-0.909871213480826,-0.905759400379418,
-0.897797095538855,-0.896245785835583,-0.895265171617205,-0.894490021105889,
-0.893586591162298,-0.89196719186132,-0.884205084181735,-0.839948068302154,
-0.834325866530686,-0.822129237122471,-0.819510681777071,-0.817799820056214,
-0.816415509602126,-0.81483071742641,-0.812096024767854,-0.800420722036785,
-0.755880920441822,-0.742520864445167,-0.740533919546976,-0.739553391857166,
-0.73877821697435,-0.737874652047628,-0.736254745129661,-0.728485182119267,
-0.684231961683498,-0.678601482084515,-0.666413324999779,-0.663795262389957,
-0.66208451356173,-0.660700155690935,-0.659115156918223,-0.656379722577751,
-0.644695280675613,-0.600159672584616,-0.586802488947652,-0.584815569613071,
-0.583835021420027,-0.583059814118981,-0.582156192782227,-0.580536138305966,
-0.572764989251016,-0.528510824957319,-0.522878689857053,-0.510691575115682,
-0.508073503859469,-0.506362712727791,-0.504978296292453,-0.503393203756708,
-0.500657540041379,-0.488971070219121,-0.444434581289266,-0.431077417471671,
-0.429090430541218,-0.42810984317089,-0.427334602049022,-0.426430938017126,
-0.424810798837877,-0.417039089136524,-0.372783153470298,-0.367150523091922,
-0.354963149405569,-0.352344981651356,-0.350634121020652,-0.349249644068411,
-0.347664477549055,-0.344928674273935,-0.333241424026262,-0.288703164602155,
-0.275345519732835,-0.273358448839536,-0.27237781901006,-0.271602543819682,
-0.270698839500287,-0.269186179378965,-0.263391821277015,-0.252166053312491,
-0.213302891610325,-0.199460213040507,-0.1967331721054,-0.19498869811307,
-0.193601263172659,-0.192038634393199,-0.189552228995395,-0.180241678035301,
-0.179869993025475),.UNSPECIFIED.);
#236=B_SPLINE_CURVE_WITH_KNOTS('',3,(#21287,#21288,#21289,#21290,#21291,
#21292,#21293,#21294,#21295),.UNSPECIFIED.,.F.,.F.,(4,1,1,1,1,1,4),(197.920343780393,
198.862557328576,199.860211623894,200.857865919213,201.855520214531,202.85317450985,
203.05545769227),.UNSPECIFIED.);
#237=B_SPLINE_CURVE_WITH_KNOTS('',3,(#21296,#21297,#21298,#21299,#21300,
#21301,#21302,#21303,#21304,#21305,#21306,#21307,#21308,#21309,#21310,#21311,
#21312,#21313,#21314,#21315,#21316,#21317,#21318,#21319,#21320,#21321,#21322,
#21323,#21324,#21325,#21326,#21327,#21328,#21329,#21330,#21331,#21332,#21333,
#21334,#21335,#21336,#21337,#21338,#21339,#21340,#21341,#21342,#21343,#21344,
#21345,#21346,#21347,#21348,#21349,#21350,#21351,#21352,#21353),
 .UNSPECIFIED.,.F.,.F.,(4,2,2,2,2,2,2,2,2,2,2,2,2,2,2,2,2,2,2,2,2,2,2,2,
2,2,2,2,4),(-1.9615148801207,-1.95785930310038,-1.95543652480846,-1.95436909446081,
-1.95358068958562,-1.95284838445205,-1.95211996770514,-1.95093027299669,
-1.94795677294164,-1.94237790205886,-1.90140356101455,-1.88263440278567,
-1.87821944696884,-1.87630059519408,-1.87488845379201,-1.87358232287792,
-1.87146013636454,-1.86618634365039,-1.83259983769925,-1.80945080302022,
-1.8032887874351,-1.80068993723764,-1.79928673563025,-1.79836335709454,
-1.79749796900988,-1.79674322859053,-1.79574856420446,-1.79369123295163,
-1.78229182699827),.UNSPECIFIED.);
#238=B_SPLINE_CURVE_WITH_KNOTS('',3,(#21355,#21356,#21357,#21358,#21359,
#21360,#21361,#21362,#21363,#21364,#21365,#21366,#21367,#21368,#21369,#21370,
#21371,#21372,#21373,#21374,#21375,#21376,#21377,#21378,#21379,#21380,#21381,
#21382,#21383,#21384,#21385,#21386,#21387,#21388,#21389,#21390,#21391,#21392,
#21393,#21394),.UNSPECIFIED.,.F.,.F.,(4,2,2,2,2,2,2,2,2,2,2,2,2,2,2,2,2,
2,2,4),(-0.179869993025475,-0.163811595497955,-0.142530502780673,-0.119886253534804,
-0.117769196411936,-0.116762987487965,-0.115985403780305,-0.115099048419803,
-0.114167300882653,-0.1108377978002,-0.0899917403801816,-0.0730740043608321,
-0.0445831457109489,-0.0411392387991886,-0.0393803473849921,-0.0379914470417024,
-0.0364376543779964,-0.0348298470050013,-0.0324345490511391,-0.000459757364235491),
 .UNSPECIFIED.);
#239=B_SPLINE_CURVE_WITH_KNOTS('',3,(#21395,#21396,#21397,#21398,#21399,
#21400,#21401,#21402,#21403,#21404,#21405,#21406,#21407,#21408,#21409,#21410,
#21411,#21412,#21413,#21414,#21415,#21416,#21417,#21418,#21419,#21420,#21421,
#21422,#21423,#21424,#21425,#21426,#21427,#21428,#21429,#21430,#21431,#21432,
#21433,#21434,#21435,#21436,#21437,#21438,#21439,#21440,#21441,#21442,#21443,
#21444,#21445,#21446,#21447,#21448,#21449,#21450,#21451,#21452,#21453,#21454,
#21455,#21456,#21457,#21458,#21459,#21460,#21461,#21462,#21463,#21464,#21465,
#21466,#21467,#21468,#21469,#21470,#21471,#21472,#21473,#21474,#21475,#21476,
#21477,#21478,#21479,#21480,#21481,#21482,#21483,#21484,#21485,#21486,#21487,
#21488,#21489,#21490,#21491,#21492,#21493,#21494,#21495,#21496,#21497,#21498,
#21499,#21500,#21501,#21502,#21503,#21504,#21505,#21506,#21507,#21508,#21509,
#21510,#21511,#21512,#21513,#21514,#21515,#21516,#21517,#21518,#21519,#21520,
#21521,#21522,#21523,#21524,#21525,#21526,#21527,#21528,#21529,#21530,#21531,
#21532,#21533,#21534,#21535,#21536,#21537,#21538,#21539,#21540,#21541,#21542,
#21543,#21544,#21545,#21546,#21547,#21548,#21549,#21550,#21551,#21552,#21553,
#21554,#21555,#21556,#21557,#21558,#21559,#21560,#21561,#21562,#21563,#21564,
#21565,#21566,#21567,#21568,#21569,#21570,#21571,#21572,#21573,#21574,#21575,
#21576,#21577,#21578,#21579,#21580,#21581,#21582),.UNSPECIFIED.,.F.,.F.,
(4,2,2,2,2,2,2,2,2,2,2,2,2,2,2,2,2,2,2,2,2,2,2,2,2,2,2,2,2,2,2,2,2,2,2,
2,2,2,2,2,2,2,2,2,2,2,2,2,2,2,2,2,2,2,2,2,2,2,2,2,2,2,2,2,2,2,2,2,2,2,2,
2,2,2,2,2,2,2,2,2,2,2,2,2,2,2,2,2,2,2,2,2,2,4),(-1.96082658239079,-1.92602912275097,
-1.92391265918641,-1.9226980023526,-1.9216113461444,-1.92082269324694,-1.92008050876462,
-1.91881711121155,-1.91537410270121,-1.88549619304636,-1.87029251594664,
-1.85123746030756,-1.84653828417131,-1.84500099645138,-1.84349630338714,
-1.84209558600681,-1.84027263360582,-1.83721681887257,-1.81498141790064,
-1.78387566150072,-1.7735473936807,-1.76796809773533,-1.76651269513947,
-1.76563914191328,-1.76485956308448,-1.76385017322892,-1.7621661638449,
-1.75169513583186,-1.75143077427964,-1.74526404675889,-1.71116843487286,
-1.69922104241752,-1.69179772305969,-1.68950304768023,-1.6882005043922,
-1.68681692635051,-1.68510822134661,-1.68249527967644,-1.67037002298248,
-1.66468534211715,-1.62046716655693,-1.61265153424839,-1.61102929622464,
-1.61012546600139,-1.60935069797371,-1.60837150360438,-1.60638992851264,
-1.59316982774372,-1.54889067676612,-1.53690975383071,-1.53415416904679,
-1.5325651748407,-1.53118187495095,-1.52947826479315,-1.5268819275384,-1.51499890060777,
-1.50909516957812,-1.46501732898557,-1.45702103002851,-1.45538788533665,
-1.45448164846656,-1.45370706322193,-1.45273096851452,-1.45082775571268,
-1.43903885429282,-1.43503553418016,-1.42284034116326,-1.39453250422579,
-1.38144163821978,-1.37861227308363,-1.37700694565556,-1.37576354494997,
-1.37413908691075,-1.37130043900867,-1.3595609458052,-1.35352347109607,
-1.30951854092663,-1.3014181039286,-1.29977865386854,-1.29887095626339,
-1.29809636308121,-1.29712183918595,-1.29522635196791,-1.28364126863433,
-1.24625480834406,-1.23302398021995,-1.22500268161307,-1.22258984808002,
-1.22107642036994,-1.21967807384737,-1.21787299353315,-1.21487936627816,
-1.19521268181508,-1.16013501283535),.UNSPECIFIED.);
#240=B_SPLINE_CURVE_WITH_KNOTS('',3,(#21588,#21589,#21590,#21591,#21592,
#21593,#21594,#21595,#21596,#21597,#21598,#21599,#21600,#21601,#21602,#21603,
#21604,#21605,#21606,#21607,#21608,#21609,#21610,#21611,#21612,#21613,#21614,
#21615,#21616,#21617,#21618,#21619,#21620,#21621,#21622,#21623,#21624,#21625,
#21626,#21627,#21628,#21629,#21630,#21631,#21632,#21633,#21634,#21635,#21636,
#21637,#21638,#21639,#21640,#21641,#21642,#21643,#21644,#21645,#21646,#21647,
#21648,#21649,#21650,#21651,#21652,#21653,#21654,#21655,#21656,#21657,#21658,
#21659,#21660,#21661,#21662,#21663,#21664,#21665,#21666,#21667,#21668,#21669),
 .UNSPECIFIED.,.F.,.F.,(4,3,3,3,3,3,3,3,3,3,3,3,3,3,3,3,3,3,3,3,3,3,3,3,
3,3,3,4),(204.203522483337,204.4022267974,204.600944713539,204.800173276778,
204.848483100487,205.047025400352,205.246803399215,205.444888946928,205.645513171366,
205.846137395805,206.044679670632,206.244457675755,206.442543198879,206.643167445002,
206.843791691124,207.042333982541,207.242111983516,207.440197522141,207.640821754292,
207.841445986442,208.039988334246,208.239766321125,208.437851916756,208.638476099258,
208.839100281761,209.037642471706,209.235805250642,209.337753800715),
 .UNSPECIFIED.);
#241=B_SPLINE_CURVE_WITH_KNOTS('',3,(#21670,#21671,#21672,#21673,#21674),
 .UNSPECIFIED.,.F.,.F.,(4,1,4),(203.05545769227,203.850828805168,204.203515180604),
 .UNSPECIFIED.);
#242=B_SPLINE_CURVE_WITH_KNOTS('',3,(#21675,#21676,#21677,#21678,#21679,
#21680,#21681,#21682,#21683,#21684,#21685,#21686,#21687,#21688,#21689,#21690,
#21691,#21692,#21693,#21694,#21695,#21696,#21697,#21698,#21699,#21700,#21701,
#21702,#21703,#21704,#21705,#21706,#21707,#21708,#21709,#21710,#21711,#21712,
#21713,#21714,#21715,#21716,#21717,#21718,#21719,#21720,#21721,#21722,#21723,
#21724,#21725,#21726,#21727,#21728,#21729,#21730,#21731,#21732,#21733,#21734,
#21735,#21736,#21737,#21738,#21739,#21740,#21741,#21742,#21743,#21744,#21745,
#21746,#21747,#21748,#21749,#21750,#21751,#21752,#21753,#21754,#21755,#21756,
#21757,#21758,#21759,#21760,#21761,#21762,#21763,#21764,#21765,#21766,#21767,
#21768,#21769,#21770,#21771,#21772,#21773,#21774,#21775,#21776,#21777,#21778,
#21779,#21780,#21781,#21782,#21783,#21784,#21785,#21786,#21787,#21788,#21789,
#21790,#21791,#21792,#21793,#21794,#21795,#21796,#21797,#21798,#21799,#21800,
#21801,#21802,#21803,#21804,#21805,#21806,#21807,#21808,#21809,#21810,#21811,
#21812,#21813,#21814,#21815,#21816,#21817,#21818,#21819,#21820,#21821,#21822,
#21823,#21824,#21825,#21826,#21827,#21828,#21829,#21830,#21831,#21832,#21833,
#21834,#21835,#21836,#21837,#21838,#21839,#21840,#21841,#21842,#21843,#21844,
#21845,#21846,#21847,#21848,#21849,#21850,#21851,#21852,#21853,#21854,#21855,
#21856,#21857,#21858,#21859,#21860,#21861,#21862,#21863,#21864,#21865,#21866,
#21867,#21868,#21869,#21870,#21871,#21872,#21873,#21874,#21875,#21876,#21877,
#21878,#21879,#21880,#21881,#21882,#21883,#21884,#21885,#21886,#21887,#21888,
#21889,#21890,#21891,#21892,#21893,#21894,#21895,#21896,#21897,#21898,#21899,
#21900,#21901,#21902,#21903,#21904,#21905,#21906,#21907,#21908,#21909,#21910,
#21911,#21912,#21913,#21914,#21915,#21916,#21917,#21918,#21919,#21920,#21921,
#21922,#21923,#21924,#21925,#21926,#21927,#21928,#21929,#21930),
 .UNSPECIFIED.,.F.,.F.,(4,2,2,2,2,2,2,2,2,2,2,2,2,2,2,2,2,2,2,2,2,2,2,2,
2,2,2,2,2,2,2,2,2,2,2,2,2,2,2,2,2,2,2,2,2,2,2,2,2,2,2,2,2,2,2,2,2,2,2,2,
2,2,2,2,2,2,2,2,2,2,2,2,2,2,2,2,2,2,2,2,2,2,2,2,2,2,2,2,2,2,2,2,2,2,2,2,
2,2,2,2,2,2,2,2,2,2,2,2,2,2,2,2,2,2,2,2,2,2,2,2,2,2,2,2,2,2,2,4),(-1.16013501283535,
-1.15244795152998,-1.14561574671098,-1.14405785862302,-1.14316796281657,
-1.14239113281632,-1.14139098574942,-1.13930453000753,-1.12155879054906,
-1.09167128973203,-1.07269589882701,-1.06825554410622,-1.06633264804388,
-1.06492018332803,-1.06361562372442,-1.06150018992778,-1.0562636372972,
-1.02098865865973,-1.00498955056935,-0.99517620192596,-0.991582552993478,
-0.989012495185446,-0.987923765088775,-0.987134443174618,-0.986392295414844,
-0.985342381568503,-0.982508762486278,-0.980953553527101,-0.952012391238002,
-0.918350586309311,-0.913079577190366,-0.910958308611932,-0.909652689997913,
-0.908241058428202,-0.906322830921879,-0.90190904444032,-0.883141086531339,
-0.853124549737448,-0.845103438767711,-0.834863311384136,-0.833189896800554,
-0.832183388219915,-0.831403900133244,-0.830528054587987,-0.829033612197652,
-0.823031946695105,-0.811591119013575,-0.780653141438465,-0.759778577490916,
-0.756754755791123,-0.754940706370542,-0.753540859388188,-0.7520312076194,
-0.74963598827415,-0.741778826998395,-0.728922166577821,-0.692375048878608,
-0.679419274860688,-0.677470427286,-0.676484403497884,-0.675708852049611,
-0.674809380282094,-0.673207993034462,-0.665732235130786,-0.62124138524943,
-0.615914951783187,-0.60338383301454,-0.600742799493143,-0.599025021989373,
-0.59764024315472,-0.596060510556278,-0.593348600081016,-0.581983521160895,
-0.537220440924614,-0.523739574703585,-0.521748787742838,-0.520767512871396,
-0.519992308623926,-0.519089353841843,-0.517472144703771,-0.509745723692276,
-0.465459555989856,-0.459877296554102,-0.447636426779179,-0.445014459664544,
-0.44330253723789,-0.441918143321858,-0.440334105199491,-0.437602859622623,
-0.425975414710597,-0.381401070394554,-0.368021802137539,-0.366034222576292,
-0.365053564513879,-0.364278375918171,-0.363374897577985,-0.361755401947534,
-0.353992651323872,-0.309733627887707,-0.304110693997192,-0.291913970427097,
-0.289295319536869,-0.287584383497084,-0.286200005011609,-0.286196352880906,
-0.286192720827022,-0.286189109127128,-0.286185517613882,-0.286181946115099,
-0.286178394471249,-0.286174862517547,-0.286171350091802,-0.286167857030312,
-0.286164383175913,-0.284598023349195,-0.281922495827144,-0.27866106761613,
-0.272004267093479,-0.226684740495946,-0.223551865373127,-0.212159378920945,
-0.210270804662788,-0.209297472368981,-0.208522581740232,-0.207613088393781,
-0.205966721704878,-0.197756983940576,-0.179683013393011),.UNSPECIFIED.);
#243=B_SPLINE_CURVE_WITH_KNOTS('',3,(#21936,#21937,#21938,#21939,#21940,
#21941,#21942,#21943,#21944,#21945,#21946,#21947,#21948,#21949,#21950,#21951,
#21952,#21953,#21954,#21955,#21956,#21957,#21958,#21959,#21960,#21961,#21962,
#21963,#21964,#21965,#21966,#21967,#21968,#21969,#21970,#21971,#21972,#21973,
#21974,#21975,#21976,#21977,#21978,#21979,#21980,#21981,#21982,#21983,#21984,
#21985,#21986,#21987,#21988,#21989,#21990,#21991,#21992,#21993,#21994,#21995,
#21996,#21997,#21998,#21999,#22000,#22001,#22002,#22003,#22004,#22005,#22006,
#22007,#22008,#22009,#22010,#22011,#22012,#22013,#22014,#22015,#22016,#22017,
#22018,#22019,#22020,#22021,#22022,#22023,#22024,#22025,#22026,#22027,#22028,
#22029,#22030,#22031,#22032,#22033,#22034,#22035,#22036,#22037,#22038,#22039,
#22040,#22041,#22042,#22043,#22044,#22045,#22046,#22047,#22048,#22049,#22050,
#22051,#22052,#22053,#22054,#22055,#22056,#22057,#22058,#22059,#22060,#22061,
#22062,#22063,#22064,#22065,#22066,#22067,#22068,#22069,#22070,#22071,#22072,
#22073,#22074,#22075,#22076,#22077,#22078,#22079,#22080,#22081,#22082,#22083,
#22084,#22085,#22086,#22087,#22088,#22089,#22090,#22091,#22092,#22093,#22094,
#22095,#22096,#22097,#22098,#22099,#22100,#22101,#22102,#22103,#22104,#22105,
#22106,#22107,#22108,#22109,#22110,#22111,#22112,#22113,#22114,#22115,#22116,
#22117),.UNSPECIFIED.,.F.,.F.,(4,2,2,2,2,2,2,2,2,2,2,2,2,2,2,2,2,2,2,2,
2,2,2,2,2,2,2,2,2,2,2,2,2,2,2,2,2,2,2,2,2,2,2,2,2,2,2,2,2,2,2,2,2,2,2,2,
2,2,2,2,2,2,2,2,2,2,2,2,2,2,2,2,2,2,2,2,2,2,2,2,2,2,2,2,2,2,2,2,2,2,4),
(-0.801755247281622,-0.78086201411725,-0.761282731388872,-0.758289959061391,
-0.756484478492026,-0.755085286016964,-0.75357040783494,-0.751154103284936,
-0.743110564267746,-0.729829646726836,-0.69250539174903,-0.680862109261831,
-0.678963244350437,-0.677987581088989,-0.677212339088328,-0.676304133469897,
-0.674664643021354,-0.666580951608885,-0.622539809537711,-0.616439439894876,
-0.604762977396565,-0.601927603904639,-0.600302913425538,-0.599058225915042,
-0.597449916624031,-0.594611455031511,-0.581407033654533,-0.552659239739768,
-0.525359636983343,-0.523297617902993,-0.522301774821857,-0.521524832642854,
-0.520630910515257,-0.519056561998955,-0.511999749847502,-0.46836910385605,
-0.459292426077767,-0.457929708764234,-0.448646406687241,-0.445996975423015,
-0.444430373126496,-0.443181592086351,-0.441506830318308,-0.438358562770144,
-0.418488401102963,-0.380968651225515,-0.369399812699514,-0.367503822308947,
-0.366528744988159,-0.365753554817715,-0.364844959510768,-0.363203384903601,
-0.355081681308867,-0.311075568993249,-0.304943900381447,-0.293305699768569,
-0.290473727609101,-0.288849967611286,-0.287605456890989,-0.286028835564392,
-0.283307911589251,-0.27997955813019,-0.25723037982761,-0.243289374138446,
-0.216010296347387,-0.212519401424734,-0.211247820435019,-0.210503472899165,
-0.20971470939341,-0.208631451720734,-0.206095448663128,-0.178171937163344,
-0.140901328534064,-0.135997095718667,-0.13414214919743,-0.132816039415444,
-0.131480976478667,-0.129707507675679,-0.126058957312403,-0.12127959948803,
-0.10991348618691,-0.0949394951243235,-0.0599704736272973,-0.0567348544962777,
-0.0555022377686479,-0.0547654854864833,-0.053971680163666,-0.0528598336409613,
-0.0501551366038624,-0.0463178883774756,-0.000462826290749375),
 .UNSPECIFIED.);
#244=B_SPLINE_CURVE_WITH_KNOTS('',3,(#22118,#22119,#22120,#22121,#22122,
#22123,#22124,#22125,#22126,#22127,#22128,#22129,#22130,#22131,#22132,#22133,
#22134,#22135,#22136,#22137,#22138,#22139),.UNSPECIFIED.,.F.,.F.,(4,3,3,
3,3,3,3,4),(209.337753800715,209.535821987683,209.734362197183,209.836754577079,
210.035772951847,210.23433093735,210.432737935524,210.486707790516),
 .UNSPECIFIED.);
#245=B_SPLINE_CURVE_WITH_KNOTS('',3,(#22141,#22142,#22143,#22144,#22145,
#22146,#22147,#22148,#22149,#22150,#22151,#22152,#22153,#22154,#22155,#22156,
#22157,#22158,#22159,#22160,#22161,#22162,#22163,#22164,#22165,#22166,#22167,
#22168,#22169,#22170,#22171,#22172,#22173,#22174,#22175,#22176,#22177,#22178,
#22179,#22180,#22181,#22182,#22183,#22184,#22185,#22186,#22187,#22188,#22189,
#22190,#22191,#22192,#22193,#22194,#22195,#22196,#22197,#22198,#22199,#22200),
 .UNSPECIFIED.,.F.,.F.,(4,2,2,2,2,2,2,2,2,2,2,2,2,2,2,2,2,2,2,2,2,2,2,2,
2,2,2,2,2,4),(-0.179683013393011,-0.153833929778708,-0.147651743902397,
-0.136066129701737,-0.133238916153645,-0.131616500613473,-0.130372292347068,
-0.130361163143912,-0.130344843018896,-0.13032883620451,-0.130313134155593,
-0.130297727819773,-0.130282606547122,-0.130267761318402,-0.130253183474055,
-0.130238864690741,-0.128608632247454,-0.125657092723767,-0.121971128085402,
-0.114079103967532,-0.0957409663085824,-0.0797737773767086,-0.056779181564577,
-0.0546625224908131,-0.0536563157597635,-0.052878648238301,-0.0519921021928767,
-0.0504501672964389,-0.0438423698564559,-0.000460287074351403),
 .UNSPECIFIED.);
#246=B_SPLINE_CURVE_WITH_KNOTS('',3,(#22201,#22202,#22203,#22204,#22205,
#22206,#22207,#22208,#22209,#22210,#22211,#22212,#22213,#22214,#22215,#22216,
#22217,#22218,#22219,#22220,#22221,#22222,#22223,#22224,#22225,#22226,#22227,
#22228,#22229,#22230,#22231,#22232,#22233,#22234,#22235,#22236,#22237,#22238,
#22239,#22240,#22241,#22242,#22243,#22244,#22245,#22246,#22247,#22248,#22249,
#22250,#22251,#22252,#22253,#22254,#22255,#22256,#22257,#22258,#22259,#22260,
#22261,#22262,#22263,#22264,#22265,#22266,#22267,#22268,#22269,#22270,#22271,
#22272,#22273,#22274,#22275,#22276,#22277,#22278,#22279,#22280,#22281,#22282),
 .UNSPECIFIED.,.F.,.F.,(4,3,3,3,3,3,3,3,3,3,3,3,3,3,3,3,3,3,3,3,3,3,3,3,
3,3,3,4),(210.486707790516,210.684874749739,210.88302187909,211.081668186406,
211.146280582813,211.344822930682,211.544600917545,211.74268651324,211.943310695686,
212.143934878132,212.34247704944,212.542255080443,212.740340502248,212.940964837849,
213.14158917345,213.340131504725,213.539909495736,213.737995069762,213.938619269265,
214.139243468769,214.337786108943,214.537564022729,214.735649911972,214.93627383803,
215.136897764087,215.335440942814,215.533590738744,215.620984071508),
 .UNSPECIFIED.);
#247=B_SPLINE_CURVE_WITH_KNOTS('',3,(#22287,#22288,#22289,#22290,#22291,
#22292,#22293,#22294,#22295,#22296,#22297,#22298,#22299,#22300,#22301,#22302,
#22303,#22304,#22305,#22306,#22307,#22308,#22309,#22310,#22311,#22312,#22313,
#22314,#22315,#22316,#22317,#22318,#22319,#22320,#22321,#22322,#22323,#22324,
#22325,#22326,#22327,#22328,#22329,#22330,#22331,#22332,#22333,#22334,#22335,
#22336,#22337,#22338,#22339,#22340,#22341,#22342,#22343,#22344,#22345,#22346,
#22347,#22348,#22349,#22350,#22351,#22352,#22353,#22354,#22355,#22356,#22357,
#22358,#22359,#22360,#22361,#22362,#22363,#22364,#22365,#22366,#22367,#22368,
#22369,#22370,#22371,#22372,#22373,#22374,#22375,#22376,#22377,#22378,#22379,
#22380,#22381,#22382,#22383,#22384,#22385,#22386,#22387,#22388,#22389,#22390,
#22391,#22392,#22393,#22394,#22395,#22396,#22397,#22398,#22399,#22400,#22401,
#22402,#22403,#22404,#22405,#22406,#22407,#22408,#22409,#22410,#22411,#22412,
#22413,#22414,#22415,#22416,#22417,#22418,#22419,#22420,#22421,#22422,#22423,
#22424,#22425,#22426,#22427,#22428,#22429,#22430,#22431,#22432,#22433,#22434,
#22435,#22436,#22437,#22438,#22439,#22440,#22441,#22442,#22443,#22444,#22445,
#22446,#22447,#22448,#22449,#22450,#22451,#22452,#22453,#22454,#22455,#22456,
#22457,#22458,#22459,#22460,#22461,#22462,#22463,#22464,#22465,#22466,#22467,
#22468,#22469,#22470,#22471,#22472,#22473,#22474,#22475,#22476,#22477,#22478,
#22479,#22480,#22481,#22482,#22483,#22484,#22485,#22486,#22487,#22488,#22489,
#22490,#22491,#22492,#22493,#22494,#22495,#22496,#22497,#22498,#22499,#22500,
#22501,#22502,#22503,#22504,#22505,#22506,#22507,#22508,#22509,#22510,#22511,
#22512,#22513,#22514,#22515,#22516,#22517,#22518,#22519,#22520),
 .UNSPECIFIED.,.F.,.F.,(4,2,2,2,2,2,2,2,2,2,2,2,2,2,2,2,2,2,2,2,2,2,2,2,
2,2,2,2,2,2,2,2,2,2,2,2,2,2,2,2,2,2,2,2,2,2,2,2,2,2,2,2,2,2,2,2,2,2,2,2,
2,2,2,2,2,2,2,2,2,2,2,2,2,2,2,2,2,2,2,2,2,2,2,2,2,2,2,2,2,2,2,2,2,2,2,2,
2,2,2,2,2,2,2,2,2,2,2,2,2,2,2,2,2,2,2,2,4),(-1.78243981456369,-1.77781910849269,
-1.77045667882715,-1.76886762186785,-1.76796289004524,-1.76718965527803,
-1.76621499263851,-1.764240560818,-1.751023706825,-1.7496780453941,-1.70453298226282,
-1.6944549873362,-1.69190889410289,-1.69034169332121,-1.6889664160694,-1.68725857376783,
-1.68462953443928,-1.67211062151324,-1.66595586433131,-1.62259226068631,
-1.61451420740382,-1.61288487756901,-1.61198374080067,-1.61121066848732,
-1.61023637536237,-1.60834470707781,-1.59689176458797,-1.59404751390318,
-1.59069275844223,-1.54734791285111,-1.53820385320524,-1.53567261217881,
-1.53412964097899,-1.53273329188368,-1.53094123994273,-1.52806686633859,
-1.51152490377523,-1.4667479288529,-1.45895712885065,-1.45733025785726,
-1.45642232404805,-1.45564445933202,-1.45466112995711,-1.45266603575424,
-1.43913436595251,-1.39384131902477,-1.38304352560909,-1.38037318429321,
-1.37880157066246,-1.37741408958584,-1.37568005264275,-1.37298943766206,
-1.35971748488825,-1.35515658228287,-1.31091107188864,-1.30315587089286,
-1.30153643728556,-1.30063280390261,-1.29985770089437,-1.29887732508598,
-1.29689000238447,-1.28350173658133,-1.23902096997954,-1.22732632743332,
-1.2245910241943,-1.22300652779084,-1.22162286985777,-1.21991333101168,
-1.21729776680558,-1.20513637915205,-1.16702814691573,-1.15384258508155,
-1.14725040957389,-1.14571042103203,-1.144824739813,-1.14404699333597,-1.1430400854616,
-1.14092126462828,-1.11907332751573,-1.09149667020153,-1.07875250813313,
-1.07094167312938,-1.0685498218238,-1.06703978132904,-1.06563783603358,
-1.06381859648723,-1.06078064219458,-1.03944602358168,-1.013296717493,-0.992392256212847,
-0.990390079119862,-0.989405759764212,-0.988703228678187,-0.987827985072771,
-0.986338397977094,-0.981110592730136,-0.971501591535719,-0.937451337526512,
-0.917028200318629,-0.914014410714383,-0.912202653056938,-0.910802372715922,
-0.909290067798029,-0.906885942408039,-0.898956932868385,-0.885939901310233,
-0.848547469404808,-0.846257713720262,-0.836421630151211,-0.834767107765206,
-0.833765838297843,-0.832986616635607,-0.832106820659761,-0.830596005665425,
-0.824398396726793,-0.812397727156659,-0.801755247281622),.UNSPECIFIED.);
#248=B_SPLINE_CURVE_WITH_KNOTS('',3,(#22522,#22523,#22524,#22525,#22526,
#22527,#22528,#22529,#22530,#22531,#22532,#22533,#22534,#22535,#22536,#22537,
#22538,#22539,#22540,#22541,#22542,#22543),.UNSPECIFIED.,.F.,.F.,(4,3,3,
3,3,3,3,4),(215.620984071508,215.819050588149,216.017592804227,216.134552059406,
216.334181857737,216.533339860188,216.732307834584,216.769893097696),
 .UNSPECIFIED.);
#249=B_SPLINE_CURVE_WITH_KNOTS('',3,(#22544,#22545,#22546,#22547,#22548,
#22549,#22550,#22551,#22552,#22553,#22554,#22555,#22556,#22557,#22558,#22559,
#22560,#22561,#22562,#22563,#22564,#22565,#22566,#22567,#22568,#22569,#22570,
#22571,#22572,#22573,#22574,#22575,#22576,#22577,#22578,#22579,#22580,#22581,
#22582,#22583,#22584,#22585,#22586,#22587,#22588,#22589,#22590,#22591,#22592,
#22593,#22594,#22595,#22596,#22597,#22598,#22599,#22600,#22601,#22602,#22603,
#22604,#22605,#22606,#22607,#22608,#22609,#22610,#22611,#22612,#22613,#22614,
#22615,#22616,#22617,#22618,#22619,#22620,#22621,#22622,#22623,#22624,#22625,
#22626,#22627,#22628,#22629,#22630,#22631,#22632,#22633,#22634,#22635,#22636,
#22637,#22638,#22639,#22640,#22641,#22642,#22643,#22644,#22645,#22646,#22647,
#22648,#22649,#22650,#22651,#22652,#22653,#22654,#22655,#22656,#22657,#22658,
#22659,#22660,#22661,#22662,#22663,#22664,#22665,#22666,#22667,#22668,#22669,
#22670,#22671,#22672,#22673,#22674,#22675,#22676,#22677,#22678,#22679,#22680,
#22681,#22682,#22683,#22684,#22685,#22686,#22687,#22688,#22689,#22690,#22691,
#22692,#22693,#22694,#22695,#22696,#22697,#22698,#22699,#22700,#22701,#22702,
#22703,#22704,#22705,#22706,#22707,#22708,#22709,#22710,#22711,#22712,#22713,
#22714,#22715,#22716,#22717,#22718,#22719,#22720,#22721,#22722,#22723,#22724,
#22725,#22726,#22727,#22728,#22729,#22730,#22731,#22732,#22733,#22734,#22735,
#22736,#22737,#22738,#22739,#22740,#22741,#22742,#22743,#22744,#22745,#22746,
#22747,#22748,#22749,#22750,#22751,#22752,#22753,#22754,#22755,#22756,#22757,
#22758,#22759,#22760,#22761,#22762,#22763,#22764,#22765,#22766,#22767,#22768,
#22769,#22770,#22771,#22772,#22773,#22774,#22775,#22776,#22777),
 .UNSPECIFIED.,.F.,.F.,(4,2,2,2,2,2,2,2,2,2,2,2,2,2,2,2,2,2,2,2,2,2,2,2,
2,2,2,2,2,2,2,2,2,2,2,2,2,2,2,2,2,2,2,2,2,2,2,2,2,2,2,2,2,2,2,2,2,2,2,2,
2,2,2,2,2,2,2,2,2,2,2,2,2,2,2,2,2,2,2,2,2,2,2,2,2,2,2,2,2,2,2,2,2,2,2,2,
2,2,2,2,2,2,2,2,2,2,2,2,2,2,2,2,2,2,2,2,4),(0.801779048931175,0.837019428551869,
0.842251000008229,0.844364256943249,0.8456674029493,0.847078273207283,0.848998871291302,
0.85343323992529,0.872375231227022,0.89536395452256,0.909893793462966,0.920405701387156,
0.922090746550154,0.923100051204982,0.923879420356136,0.924753001182252,
0.926237117106791,0.932113343220088,0.943202918540473,0.965286187621122,
0.972061840758756,0.995440331953748,0.998522268183578,1.00035364490514,
1.00175668521912,1.00325982405532,1.00562366804595,1.01319424345447,1.02540428513485,
1.04958762899285,1.06292102961666,1.07579436658856,1.07774089166114,1.07872675105735,
1.07950254252534,1.08040261592641,1.08200663665984,1.08952253460432,1.13401090295301,
1.13943419408526,1.15185317753889,1.1544865534054,1.15620179683352,1.15758615787785,
1.1591671869967,1.16188577149141,1.17334577260415,1.21798985728666,1.23144976926967,
1.23343934169617,1.23442017684465,1.2351950966167,1.2360977685617,1.237714661135,
1.24544267181117,1.28973072566158,1.30704293533181,1.3099400120814,1.31173552938767,
1.31312796223201,1.31460743893859,1.31697911193565,1.31979298365672,1.32521473453014,
1.33884041088381,1.37251068040171,1.37494023736084,1.37837826462356,1.38740059305954,
1.38901232829137,1.39001100327299,1.39078742466878,1.39167772253962,1.3932381313028,
1.40011014733151,1.4430052825361,1.46248832628739,1.46547466519161,1.46727738229634,
1.46867510415258,1.46871509302788,1.46873895559707,1.46876950891625,1.46879713079223,
1.46882214224099,1.46884482211883,1.46886541544488,1.4688841372923,1.46890117672574,
1.46891670076855,1.46893085740554,1.46894377812929,1.46895558008434,1.46897201594382,
1.46898812916944,1.46900392876709,1.46901942553776,1.46903462989518,1.4690495512811,
1.46906419875769,1.46907858102038,1.47070128375678,1.47363365309485,1.47728287114657,
1.48506720671879,1.50317813768614,1.52863612831214,1.53221362698308,1.54282936168681,
1.54451980939672,1.54553112896458,1.54631100333078,1.54718353029088,1.5486641556082,
1.55450486038028,1.56549818412402,1.60250354857828),.UNSPECIFIED.);
#250=B_SPLINE_CURVE_WITH_KNOTS('',3,(#22781,#22782,#22783,#22784,#22785,
#22786,#22787,#22788,#22789,#22790,#22791,#22792,#22793,#22794,#22795,#22796,
#22797,#22798,#22799,#22800,#22801,#22802,#22803,#22804,#22805,#22806,#22807,
#22808,#22809,#22810,#22811,#22812,#22813,#22814,#22815,#22816,#22817),
 .UNSPECIFIED.,.F.,.F.,(4,3,3,3,3,3,3,3,3,3,3,3,4),(-4.0925417488383,-3.99061718127404,
-3.80271607511609,-3.61521129929871,-3.42774226886674,-3.24028946643165,
-3.0524192190311,-2.99296288595553,-2.80713361459988,-2.62153830198906,
-2.43611803811621,-2.25027574028768,-2.0654894469632),.UNSPECIFIED.);
#251=B_SPLINE_CURVE_WITH_KNOTS('',3,(#22821,#22822,#22823,#22824,#22825,
#22826,#22827,#22828,#22829,#22830,#22831,#22832,#22833,#22834,#22835,#22836,
#22837,#22838,#22839,#22840,#22841,#22842),.UNSPECIFIED.,.F.,.F.,(4,3,3,
3,3,3,3,4),(0.,0.192029026907948,0.393435344010587,0.58555661568393,0.777819410374763,
0.970607640201115,0.997654295318505,1.11419103802989),.UNSPECIFIED.);
#252=B_SPLINE_CURVE_WITH_KNOTS('',3,(#22844,#22845,#22846,#22847,#22848,
#22849,#22850,#22851,#22852,#22853,#22854,#22855,#22856,#22857,#22858,#22859,
#22860,#22861,#22862,#22863,#22864,#22865,#22866,#22867,#22868,#22869,#22870,
#22871,#22872,#22873,#22874,#22875,#22876,#22877,#22878,#22879,#22880,#22881,
#22882,#22883,#22884,#22885,#22886,#22887,#22888,#22889,#22890,#22891,#22892,
#22893,#22894,#22895,#22896,#22897,#22898,#22899,#22900,#22901,#22902,#22903,
#22904,#22905,#22906,#22907,#22908,#22909,#22910,#22911,#22912,#22913,#22914,
#22915,#22916,#22917,#22918,#22919,#22920,#22921,#22922,#22923,#22924,#22925,
#22926,#22927,#22928,#22929,#22930,#22931,#22932,#22933,#22934,#22935,#22936,
#22937,#22938,#22939,#22940,#22941,#22942,#22943,#22944,#22945,#22946,#22947,
#22948,#22949,#22950,#22951,#22952,#22953,#22954,#22955),.UNSPECIFIED.,
 .F.,.F.,(4,3,3,3,3,3,3,3,3,3,3,3,3,3,3,3,3,3,3,3,3,3,3,3,3,3,3,3,3,3,3,
3,3,3,3,3,3,4),(1.11419103844207,1.29729781656767,1.48020848463403,1.6629748443953,
1.84617221538369,1.99530859063702,2.18313685847596,2.37057148514672,2.55797502099778,
2.74536494778383,2.93317706372225,2.99296288595553,3.18083272060202,3.3683199864994,
3.55579169057548,3.74325886950682,3.93116039865387,3.99061718127404,4.17789585759714,
4.36477521905835,4.55162388290638,4.73845861120085,4.92572539060956,4.98827147659255,
5.17586619279521,5.36306763434357,5.55024230049996,5.73740566481817,5.92499894751711,
5.98592577191106,6.17350335525126,6.36068874716866,6.54784921468969,6.73499944084289,
6.92258141640707,6.98358006722958,7.19047800572963,7.39737594422968),
 .UNSPECIFIED.);
#253=B_SPLINE_CURVE_WITH_KNOTS('',3,(#22957,#22958,#22959,#22960,#22961,
#22962,#22963,#22964,#22965,#22966),.UNSPECIFIED.,.F.,.F.,(4,1,1,1,1,1,
1,4),(7.39737634520948,7.98123436254809,8.97888865786661,9.97654295318512,
10.9741972485036,11.9718515438221,12.9695058391407,13.6805616523891),
 .UNSPECIFIED.);
#254=B_SPLINE_CURVE_WITH_KNOTS('',3,(#22968,#22969,#22970,#22971,#22972,
#22973,#22974,#22975,#22976,#22977,#22978),.UNSPECIFIED.,.F.,.F.,(4,1,1,
1,1,1,1,1,4),(13.6805616523891,13.9671601344592,14.9648144297777,15.9624687250962,
16.9601230204147,17.9577773157332,18.9554316110517,19.9530859063702,19.9637469595687),
 .UNSPECIFIED.);
#255=B_SPLINE_CURVE_WITH_KNOTS('',3,(#22980,#22981,#22982,#22983,#22984,
#22985,#22986,#22987,#22988,#22989,#22990,#22991,#22992,#22993,#22994,#22995,
#22996,#22997,#22998,#22999,#23000,#23001,#23002,#23003,#23004,#23005,#23006,
#23007,#23008,#23009,#23010,#23011,#23012,#23013,#23014,#23015,#23016,#23017,
#23018,#23019,#23020,#23021,#23022,#23023,#23024,#23025,#23026,#23027,#23028,
#23029,#23030,#23031,#23032,#23033,#23034,#23035,#23036,#23037,#23038,#23039,
#23040,#23041,#23042,#23043,#23044,#23045,#23046,#23047,#23048,#23049,#23050,
#23051,#23052,#23053,#23054,#23055,#23056,#23057,#23058,#23059,#23060,#23061,
#23062,#23063,#23064,#23065,#23066,#23067,#23068,#23069,#23070,#23071,#23072,
#23073,#23074,#23075,#23076,#23077,#23078,#23079,#23080,#23081,#23082,#23083,
#23084,#23085,#23086,#23087,#23088,#23089,#23090,#23091,#23092,#23093,#23094),
 .UNSPECIFIED.,.F.,.F.,(4,3,3,3,3,3,3,3,3,3,3,3,3,3,3,3,3,3,3,3,3,3,3,3,
3,3,3,3,3,3,3,3,3,3,3,3,3,3,4),(19.9637469595687,20.1509331180402,20.3377271974283,
20.5244962077931,20.7112586063894,20.8984478398483,20.9507402016887,21.1382782494911,
21.3254226909156,21.5125407629289,21.6996477118573,21.8871858954244,21.9483944970072,
22.1359325437719,22.3230769840842,22.5101950548933,22.6973020025625,22.8848401848119,
22.9460487923258,23.1335868421645,23.3207312856336,23.5078493596721,23.6949563106163,
23.882494496148,23.9437030876443,24.1312411360172,24.318385577994,24.5055036505241,
24.692610599949,24.8801487839735,24.9413573829628,25.128895431322,25.3160398732771,
25.5031579457749,25.6902648951611,25.8778030791379,25.9390116782813,26.1636929039991,
26.2469320713865),.UNSPECIFIED.);
#256=B_SPLINE_CURVE_WITH_KNOTS('',3,(#23096,#23097,#23098,#23099,#23100,
#23101,#23102,#23103,#23104,#23105),.UNSPECIFIED.,.F.,.F.,(4,1,1,1,1,1,
1,4),(26.2469322667482,26.9366659735998,27.9343202689183,28.9319745642368,
29.9296288595553,30.9272831548739,31.9249374501924,32.5301175739278),
 .UNSPECIFIED.);
#257=B_SPLINE_CURVE_WITH_KNOTS('',3,(#23107,#23108,#23109,#23110,#23111,
#23112,#23113,#23114,#23115,#23116),.UNSPECIFIED.,.F.,.F.,(4,1,1,1,1,1,
1,4),(32.5301175739278,32.9225917455109,33.9202460408294,34.9179003361479,
35.9155546314664,36.9132089267849,37.9108632221034,38.8132941166151),
 .UNSPECIFIED.);
#258=B_SPLINE_CURVE_WITH_KNOTS('',3,(#23118,#23119,#23120,#23121,#23122,
#23123,#23124,#23125,#23126,#23127,#23128,#23129,#23130,#23131,#23132,#23133,
#23134,#23135,#23136,#23137,#23138,#23139,#23140,#23141,#23142,#23143,#23144,
#23145,#23146,#23147,#23148,#23149,#23150,#23151,#23152,#23153,#23154,#23155,
#23156,#23157,#23158,#23159,#23160,#23161,#23162,#23163,#23164,#23165,#23166,
#23167,#23168,#23169,#23170,#23171,#23172,#23173,#23174,#23175,#23176,#23177,
#23178,#23179,#23180,#23181,#23182,#23183,#23184,#23185,#23186,#23187,#23188,
#23189,#23190,#23191,#23192,#23193,#23194,#23195,#23196,#23197,#23198,#23199,
#23200,#23201,#23202,#23203,#23204,#23205,#23206,#23207,#23208,#23209,#23210,
#23211,#23212,#23213,#23214,#23215,#23216,#23217,#23218,#23219,#23220,#23221,
#23222,#23223,#23224,#23225,#23226,#23227,#23228,#23229,#23230,#23231,#23232),
 .UNSPECIFIED.,.F.,.F.,(4,3,3,3,3,3,3,3,3,3,3,3,3,3,3,3,3,3,3,3,3,3,3,3,
3,3,3,3,3,3,3,3,3,3,3,3,3,3,4),(38.8133028811074,38.908517517422,39.0960555660062,
39.2832000081941,39.4703180809318,39.6574250305625,39.8449632147861,39.9061718127405,
40.0937098613254,40.2808543035139,40.4679723762523,40.6550793258838,40.8426175101081,
40.903826108059,41.0913641566439,41.2785085988324,41.4656266715708,41.6527336212022,
41.8402718054265,41.9014804033775,42.0890184519623,42.2761628941507,42.4632809668889,
42.6503879165202,42.8379261007444,42.899134698696,43.0866727472808,43.2738171894693,
43.4609352622076,43.648042211839,43.8355803960632,43.8967889940145,44.0843270425993,
44.2714714847877,44.4585895575261,44.6456965071574,44.8332346913816,44.894443289333,
45.096488188287),.UNSPECIFIED.);
#259=B_SPLINE_CURVE_WITH_KNOTS('',3,(#23234,#23235,#23236,#23237,#23238,
#23239,#23240,#23241,#23242,#23243),.UNSPECIFIED.,.F.,.F.,(4,1,1,1,1,1,
1,4),(45.0964910901625,45.8920975846515,46.8897518799701,47.8874061752886,
48.8850604706071,49.8827147659256,50.8803690612441,51.3796734954666),
 .UNSPECIFIED.);
#260=B_SPLINE_CURVE_WITH_KNOTS('',3,(#23245,#23246,#23247,#23248,#23249,
#23250,#23251,#23252,#23253,#23254),.UNSPECIFIED.,.F.,.F.,(4,1,1,1,1,1,
1,4),(51.3796734954666,51.8780233565626,52.8756776518811,53.8733319471996,
54.8709862425181,55.8686405378366,56.8662948331552,57.6628558111006),
 .UNSPECIFIED.);
#261=B_SPLINE_CURVE_WITH_KNOTS('',3,(#23256,#23257,#23258,#23259,#23260,
#23261,#23262,#23263,#23264,#23265,#23266,#23267,#23268,#23269,#23270,#23271,
#23272,#23273,#23274,#23275,#23276,#23277,#23278,#23279,#23280,#23281,#23282,
#23283,#23284,#23285,#23286,#23287,#23288,#23289,#23290,#23291,#23292,#23293,
#23294,#23295,#23296,#23297,#23298,#23299,#23300,#23301,#23302,#23303,#23304,
#23305,#23306,#23307,#23308,#23309,#23310,#23311,#23312,#23313,#23314,#23315,
#23316,#23317,#23318,#23319,#23320,#23321,#23322,#23323,#23324,#23325,#23326,
#23327,#23328,#23329,#23330,#23331,#23332,#23333,#23334,#23335,#23336,#23337,
#23338,#23339,#23340,#23341,#23342,#23343,#23344,#23345,#23346,#23347,#23348,
#23349,#23350,#23351,#23352,#23353,#23354,#23355,#23356,#23357,#23358,#23359,
#23360,#23361,#23362,#23363,#23364,#23365,#23366,#23367,#23368,#23369,#23370),
 .UNSPECIFIED.,.F.,.F.,(4,3,3,3,3,3,3,3,3,3,3,3,3,3,3,3,3,3,3,3,3,3,3,3,
3,3,3,3,3,3,3,3,3,3,3,3,3,3,4),(57.6628588026462,57.8639491284737,58.0514871770584,
58.2386316192467,58.4257496919849,58.6128566416161,58.8003948258402,58.8616034237922,
59.049141472377,59.2362859145655,59.4234039873038,59.6105109369352,59.7980491211594,
59.8592577191107,60.0467957676955,60.233940209884,60.4210582826223,60.6081652322537,
60.7957034164779,60.8569120144292,61.044450063014,61.2315945052024,61.4187125779407,
61.6058195275721,61.7933577117963,61.8545663097477,62.0421043583325,62.229248800521,
62.4163668732593,62.6034738228906,62.7910120071149,62.8522206050662,63.039758653651,
63.2269030958394,63.4140211685777,63.601128118209,63.7886663024333,63.8498749003847,
63.9460441098258),.UNSPECIFIED.);
#262=B_SPLINE_CURVE_WITH_KNOTS('',3,(#23372,#23373,#23374,#23375,#23376,
#23377,#23378,#23379,#23380,#23381),.UNSPECIFIED.,.F.,.F.,(4,1,1,1,1,1,
1,4),(63.9460528873255,64.8475291957032,65.8451834910218,66.8428377863403,
67.8404920816588,68.8381463769773,69.8358006722958,70.2292294170054),
 .UNSPECIFIED.);
#263=B_SPLINE_CURVE_WITH_KNOTS('',3,(#23383,#23384,#23385,#23386,#23387,
#23388,#23389,#23390,#23391,#23392),.UNSPECIFIED.,.F.,.F.,(4,1,1,1,1,1,
1,4),(70.2292294170054,70.8334549676143,71.8311092629328,72.8287635582514,
73.8264178535699,74.8240721488884,75.8217264442069,76.512414724185),
 .UNSPECIFIED.);
#264=B_SPLINE_CURVE_WITH_KNOTS('',3,(#23394,#23395,#23396,#23397,#23398,
#23399,#23400,#23401,#23402,#23403,#23404,#23405,#23406,#23407,#23408,#23409,
#23410,#23411,#23412,#23413,#23414,#23415,#23416,#23417,#23418,#23419,#23420,
#23421,#23422,#23423,#23424,#23425,#23426,#23427,#23428,#23429,#23430,#23431,
#23432,#23433,#23434,#23435,#23436,#23437,#23438,#23439,#23440,#23441,#23442,
#23443,#23444,#23445,#23446,#23447,#23448,#23449,#23450,#23451,#23452,#23453,
#23454,#23455,#23456,#23457,#23458,#23459,#23460,#23461,#23462,#23463,#23464,
#23465,#23466,#23467,#23468,#23469,#23470,#23471,#23472,#23473,#23474,#23475,
#23476,#23477,#23478,#23479,#23480,#23481,#23482,#23483,#23484,#23485,#23486,
#23487,#23488,#23489,#23490,#23491,#23492,#23493,#23494,#23495,#23496,#23497,
#23498,#23499,#23500,#23501,#23502,#23503,#23504,#23505,#23506,#23507,#23508),
 .UNSPECIFIED.,.F.,.F.,(4,3,3,3,3,3,3,3,3,3,3,3,3,3,3,3,3,3,3,3,3,3,3,3,
3,3,3,3,3,3,3,3,3,3,3,3,3,3,4),(76.5124149178937,76.737332646363,76.8193807395254,
77.0069187881103,77.1940632302988,77.3811813030371,77.5682882526685,77.7558264368928,
77.8170350348439,78.0045730834287,78.1917175256171,78.3788355983554,78.5659425479868,
78.753480732211,78.8146893301624,79.0022273787472,79.1893718209356,79.3764898936739,
79.5635968433053,79.7511350275295,79.8123436254809,79.9998816740657,80.1870261162542,
80.3741441889925,80.5612511386239,80.7487893228481,80.8099979207994,80.9975359693842,
81.1846804115726,81.3717984843109,81.5589054339422,81.7464436181664,81.8076522161179,
81.994870137769,82.1816952728114,82.368494414651,82.5552860710844,82.7425043086765,
82.7956000313646),.UNSPECIFIED.);
#265=B_SPLINE_CURVE_WITH_KNOTS('',3,(#23510,#23511,#23512,#23513,#23514,
#23515,#23516,#23517,#23518,#23519,#23520,#23521),.UNSPECIFIED.,.F.,.F.,
(4,2,1,1,1,1,1,1,4),(82.7956000313646,82.8053065114364,83.802960806755,
84.8006151020735,85.798269397392,86.7959236927105,87.793577988029,88.7912322833475,
89.0787853385442),.UNSPECIFIED.);
#266=B_SPLINE_CURVE_WITH_KNOTS('',3,(#23523,#23524,#23525,#23526,#23527,
#23528,#23529,#23530,#23531,#23532),.UNSPECIFIED.,.F.,.F.,(4,1,1,1,1,1,
1,4),(89.0787853385442,89.7888865786661,90.7865408739846,91.7841951693031,
92.7818494646216,93.7795037599401,94.7771580552586,95.3619706457238),
 .UNSPECIFIED.);
#267=B_SPLINE_CURVE_WITH_KNOTS('',3,(#23534,#23535,#23536,#23537,#23538,
#23539,#23540,#23541,#23542,#23543,#23544,#23545,#23546,#23547,#23548,#23549,
#23550,#23551,#23552,#23553,#23554,#23555,#23556,#23557,#23558,#23559,#23560,
#23561,#23562,#23563,#23564,#23565,#23566,#23567,#23568,#23569,#23570,#23571,
#23572,#23573,#23574,#23575,#23576,#23577,#23578,#23579,#23580,#23581,#23582,
#23583,#23584,#23585,#23586,#23587,#23588,#23589,#23590,#23591,#23592,#23593,
#23594,#23595,#23596,#23597,#23598,#23599,#23600,#23601,#23602,#23603,#23604,
#23605,#23606,#23607,#23608,#23609,#23610,#23611,#23612,#23613,#23614,#23615,
#23616,#23617,#23618,#23619,#23620,#23621,#23622,#23623,#23624,#23625,#23626,
#23627,#23628,#23629,#23630,#23631,#23632,#23633,#23634,#23635,#23636,#23637,
#23638,#23639,#23640,#23641,#23642,#23643,#23644,#23645),.UNSPECIFIED.,
 .F.,.F.,(4,3,3,3,3,3,3,3,3,3,3,3,3,3,3,3,3,3,3,3,3,3,3,3,3,3,3,3,3,3,3,
3,3,3,3,3,3,4),(95.3619710488281,95.5683916997026,95.7748123505771,95.9623503991619,
96.1494948413504,96.3366129140888,96.5237198637202,96.7112580479445,96.7724666458956,
96.9600046944804,97.1471491366689,97.3342672094072,97.5213741590385,97.7089123432627,
97.7701209412141,97.9576589897989,98.1448034319873,98.3319215047256,98.5190284543569,
98.7065666385811,98.7677752365326,98.9553132851174,99.1424577273058,99.3295758000441,
99.5166827496755,99.7042209338997,99.7654295318512,99.9529675804363,100.140112022625,
100.327230095364,100.514337044995,100.70187522922,100.76308382717,100.94809698056,
101.13284606384,101.317418303564,101.502339127779,101.645155952903),
 .UNSPECIFIED.);
#268=B_SPLINE_CURVE_WITH_KNOTS('',3,(#23647,#23648,#23649,#23650,#23651,
#23652,#23653,#23654,#23655,#23656,#23657),.UNSPECIFIED.,.F.,.F.,(4,1,1,
1,1,1,1,1,4),(101.645155952903,101.760738122488,102.758392417807,103.756046713125,
104.753701008444,105.751355303762,106.749009599081,107.746663894399,107.928341260083),
 .UNSPECIFIED.);
#269=B_SPLINE_CURVE_WITH_KNOTS('',3,(#23659,#23660,#23661,#23662,#23663,
#23664,#23665,#23666,#23667,#23668),.UNSPECIFIED.,.F.,.F.,(4,1,1,1,1,1,
1,4),(107.928341260083,108.744318189718,109.741972485036,110.739626780355,
111.737281075673,112.734935370992,113.73258966631,114.211525038399),
 .UNSPECIFIED.);
#270=B_SPLINE_CURVE_WITH_KNOTS('',3,(#23670,#23671,#23672,#23673,#23674,
#23675,#23676,#23677,#23678,#23679,#23680,#23681,#23682,#23683,#23684,#23685,
#23686,#23687,#23688,#23689,#23690,#23691,#23692,#23693,#23694,#23695,#23696,
#23697,#23698,#23699,#23700,#23701,#23702,#23703,#23704,#23705,#23706,#23707,
#23708,#23709,#23710,#23711,#23712,#23713,#23714,#23715,#23716,#23717,#23718,
#23719,#23720,#23721,#23722,#23723,#23724,#23725,#23726,#23727,#23728,#23729,
#23730,#23731,#23732,#23733,#23734,#23735,#23736,#23737,#23738,#23739,#23740,
#23741,#23742,#23743,#23744,#23745,#23746,#23747,#23748,#23749,#23750,#23751,
#23752,#23753,#23754,#23755,#23756,#23757,#23758,#23759,#23760,#23761,#23762,
#23763,#23764,#23765,#23766,#23767,#23768,#23769,#23770,#23771,#23772,#23773,
#23774,#23775,#23776,#23777,#23778,#23779,#23780,#23781,#23782,#23783,#23784),
 .UNSPECIFIED.,.F.,.F.,(4,3,3,3,3,3,3,3,3,3,3,3,3,3,3,3,3,3,3,3,3,3,3,3,
3,3,3,3,3,3,3,3,3,3,3,3,3,3,4),(114.211526567263,114.406050577366,114.601390959919,
114.730243961629,114.917782010213,115.104926452402,115.29204452514,115.479151474771,
115.666689658995,115.727898256947,115.915436305532,116.102580747721,116.28969882046,
116.476805770092,116.664343954316,116.725552552266,116.913090600851,117.100235043039,
117.287353115777,117.474460065408,117.661998249632,117.723206847584,117.910744896169,
118.097889338357,118.285007411096,118.472114360727,118.659652544952,118.720861142903,
118.908399191488,119.095543633676,119.282661706415,119.469768656046,119.65730684027,
119.718515438221,119.912564547276,120.097240508108,120.2817442013,120.466424250738,
120.494711874442),.UNSPECIFIED.);
#271=B_SPLINE_CURVE_WITH_KNOTS('',3,(#23786,#23787,#23788,#23789,#23790,
#23791,#23792,#23793,#23794,#23795,#23796),.UNSPECIFIED.,.F.,.F.,(4,1,1,
1,1,1,1,1,4),(120.494711874442,120.71616973354,121.713824028858,122.711478324177,
123.709132619495,124.706786914814,125.704441210132,126.702095505451,126.777897181622),
 .UNSPECIFIED.);
#272=B_SPLINE_CURVE_WITH_KNOTS('',3,(#23798,#23799,#23800,#23801,#23802,
#23803,#23804,#23805,#23806,#23807),.UNSPECIFIED.,.F.,.F.,(4,1,1,1,1,1,
1,4),(126.777897181622,127.699749800769,128.697404096088,129.695058391406,
130.692712686725,131.690366982044,132.688021277362,133.061074978669),
 .UNSPECIFIED.);
#273=B_SPLINE_CURVE_WITH_KNOTS('',3,(#23809,#23810,#23811,#23812,#23813,
#23814,#23815,#23816,#23817,#23818,#23819,#23820,#23821,#23822,#23823,#23824,
#23825,#23826,#23827,#23828,#23829,#23830,#23831,#23832,#23833,#23834,#23835,
#23836,#23837,#23838,#23839,#23840,#23841,#23842,#23843,#23844,#23845,#23846,
#23847,#23848,#23849,#23850,#23851,#23852,#23853,#23854,#23855,#23856,#23857,
#23858,#23859,#23860,#23861,#23862,#23863,#23864,#23865,#23866,#23867,#23868,
#23869,#23870,#23871,#23872,#23873,#23874,#23875,#23876,#23877,#23878,#23879,
#23880,#23881,#23882,#23883,#23884,#23885,#23886,#23887,#23888,#23889,#23890,
#23891,#23892,#23893,#23894,#23895,#23896,#23897,#23898,#23899,#23900,#23901,
#23902,#23903,#23904,#23905,#23906,#23907,#23908,#23909,#23910,#23911,#23912,
#23913,#23914,#23915,#23916,#23917,#23918,#23919,#23920,#23921,#23922,#23923),
 .UNSPECIFIED.,.F.,.F.,(4,3,3,3,3,3,3,3,3,3,3,3,3,3,3,3,3,3,3,3,3,3,3,3,
3,3,3,3,3,3,3,3,3,3,3,3,3,3,4),(133.061082488801,133.249569004459,133.4381076651,
133.627144886932,133.685675572681,133.873213621265,134.060358063453,134.24747613619,
134.434583085821,134.622121270044,134.683329867999,134.870867916584,135.058012358773,
135.245130431511,135.432237381143,135.619775565367,135.680984163318,135.868522211903,
136.055666654091,136.242784726829,136.429891676461,136.617429860685,136.678638458636,
136.866176507221,137.053320949409,137.240439022148,137.427545971779,137.615084156004,
137.676292753955,137.86383080254,138.050975244728,138.238093317467,138.425200267098,
138.612738451322,138.673947049273,138.861220080197,139.048088728297,139.234874348461,
139.344267795981),.UNSPECIFIED.);
#274=B_SPLINE_CURVE_WITH_KNOTS('',3,(#23925,#23926,#23927,#23928,#23929,
#23930,#23931,#23932,#23933,#23934),.UNSPECIFIED.,.F.,.F.,(4,1,1,1,1,1,
1,4),(139.344274773769,139.671601344592,140.66925563991,141.666909935229,
142.664564230547,143.662218525866,144.659872821184,145.62745310316),
 .UNSPECIFIED.);
#275=B_SPLINE_CURVE_WITH_KNOTS('',3,(#23936,#23937,#23938,#23939,#23940,
#23941,#23942,#23943,#23944,#23945,#23946,#23947),.UNSPECIFIED.,.F.,.F.,
(4,2,1,1,1,1,1,1,4),(145.62745310316,145.657527116503,146.655181411821,
147.65283570714,148.650490002458,149.648144297777,150.645798593095,151.643452888414,
151.910635273349),.UNSPECIFIED.);
#276=B_SPLINE_CURVE_WITH_KNOTS('',3,(#23949,#23950,#23951,#23952,#23953,
#23954,#23955,#23956,#23957,#23958,#23959,#23960,#23961,#23962,#23963,#23964,
#23965,#23966,#23967,#23968,#23969,#23970,#23971,#23972,#23973,#23974,#23975,
#23976,#23977,#23978,#23979,#23980,#23981,#23982,#23983,#23984,#23985,#23986,
#23987,#23988,#23989,#23990,#23991,#23992,#23993,#23994,#23995,#23996,#23997,
#23998,#23999,#24000,#24001,#24002,#24003,#24004,#24005,#24006,#24007,#24008,
#24009,#24010,#24011,#24012,#24013,#24014,#24015,#24016,#24017,#24018,#24019,
#24020,#24021,#24022,#24023,#24024,#24025,#24026,#24027,#24028,#24029,#24030,
#24031,#24032,#24033,#24034,#24035,#24036,#24037,#24038,#24039,#24040,#24041,
#24042,#24043,#24044,#24045,#24046,#24047,#24048,#24049,#24050,#24051,#24052,
#24053,#24054,#24055,#24056,#24057,#24058,#24059,#24060),.UNSPECIFIED.,
 .F.,.F.,(4,3,3,3,3,3,3,3,3,3,3,3,3,3,3,3,3,3,3,3,3,3,3,3,3,3,3,3,3,3,3,
3,3,3,3,3,3,4),(151.91063841034,152.096050504932,152.281317851542,152.467037581743,
152.641107183732,152.828645232317,153.015789674506,153.202907747245,153.390014696877,
153.577552881102,153.638761479051,153.826299527635,154.013443969824,154.200562042562,
154.387668992193,154.575207176417,154.636415774369,154.823953822954,155.011098265143,
155.198216337881,155.385323287513,155.572861471737,155.634070069688,155.821608118273,
156.008752560461,156.195870633199,156.382977582831,156.570515767055,156.631724365006,
156.819262413591,157.006406855779,157.193524928517,157.380631878149,157.568170062373,
157.629378660325,157.821576221357,158.01326351236,158.19382371752),
 .UNSPECIFIED.);
#277=B_SPLINE_CURVE_WITH_KNOTS('',3,(#24062,#24063,#24064,#24065,#24066,
#24067,#24068,#24069,#24070,#24071),.UNSPECIFIED.,.F.,.F.,(4,1,1,1,1,1,
1,4),(158.193828690622,158.627032955643,159.624687250962,160.62234154628,
161.619995841599,162.617650136917,163.615304432236,164.477009024699),
 .UNSPECIFIED.);
#278=B_SPLINE_CURVE_WITH_KNOTS('',3,(#24073,#24074,#24075,#24076,#24077,
#24078,#24079,#24080,#24081,#24082,#24083),.UNSPECIFIED.,.F.,.F.,(4,1,1,
1,1,1,1,1,4),(164.477009024699,164.612958727554,165.610613022873,166.608267318191,
167.60592161351,168.603575908828,169.601230204147,170.598884499465,170.760194331879),
 .UNSPECIFIED.);
#279=B_SPLINE_CURVE_WITH_KNOTS('',3,(#24085,#24086,#24087,#24088,#24089,
#24090,#24091,#24092,#24093,#24094,#24095,#24096,#24097,#24098,#24099,#24100,
#24101,#24102,#24103,#24104,#24105,#24106,#24107,#24108,#24109,#24110,#24111,
#24112,#24113,#24114,#24115,#24116,#24117,#24118,#24119,#24120,#24121,#24122,
#24123,#24124,#24125,#24126,#24127,#24128,#24129,#24130,#24131,#24132,#24133,
#24134,#24135,#24136,#24137,#24138,#24139,#24140,#24141,#24142,#24143,#24144,
#24145,#24146,#24147,#24148,#24149,#24150,#24151,#24152,#24153,#24154,#24155,
#24156,#24157,#24158,#24159,#24160,#24161,#24162,#24163,#24164,#24165,#24166,
#24167,#24168,#24169,#24170,#24171,#24172,#24173,#24174,#24175,#24176,#24177,
#24178,#24179,#24180,#24181,#24182,#24183,#24184,#24185,#24186,#24187,#24188,
#24189,#24190,#24191,#24192,#24193,#24194,#24195,#24196,#24197,#24198,#24199),
 .UNSPECIFIED.,.F.,.F.,(4,3,3,3,3,3,3,3,3,3,3,3,3,3,3,3,3,3,3,3,3,3,3,3,
3,3,3,3,3,3,3,3,3,3,3,3,3,3,4),(170.760194331879,170.944734727437,171.129147203637,
171.313475752256,171.498218708515,171.596538794784,171.784076843369,171.971221285557,
172.158339358295,172.345446307926,172.53298449215,172.594193090102,172.781731138687,
172.968875580876,173.155993653614,173.343100603245,173.53063878747,173.591847385421,
173.779385434006,173.966529876195,174.153647948934,174.340754898566,174.528293082791,
174.58950168074,174.777039729324,174.964184171512,175.15130224425,175.338409193881,
175.525947378105,175.587155976058,175.774694024643,175.961838466832,176.14895653957,
176.336063489202,176.523601673426,176.584810271377,176.785743470653,176.985583319409,
177.04337942508),.UNSPECIFIED.);
#280=B_SPLINE_CURVE_WITH_KNOTS('',3,(#24201,#24202,#24203,#24204,#24205,
#24206,#24207,#24208,#24209,#24210),.UNSPECIFIED.,.F.,.F.,(4,1,1,1,1,1,
1,4),(177.043379639058,177.582464566695,178.580118862014,179.577773157332,
180.575427452651,181.573081747969,182.570736043288,183.326564946238),
 .UNSPECIFIED.);
#281=B_SPLINE_CURVE_WITH_KNOTS('',3,(#24212,#24213,#24214,#24215,#24216,
#24217,#24218,#24219,#24220,#24221,#24222),.UNSPECIFIED.,.F.,.F.,(4,1,1,
1,1,1,1,1,4),(183.326564946238,183.568390338606,184.566044633925,185.563698929243,
186.561353224562,187.55900751988,188.556661815199,189.554316110517,189.609750253417),
 .UNSPECIFIED.);
#282=B_SPLINE_CURVE_WITH_KNOTS('',3,(#24224,#24225,#24226,#24227,#24228,
#24229,#24230,#24231,#24232,#24233,#24234,#24235,#24236,#24237,#24238,#24239,
#24240,#24241,#24242,#24243,#24244,#24245,#24246,#24247,#24248,#24249,#24250,
#24251,#24252,#24253,#24254,#24255,#24256,#24257,#24258,#24259,#24260,#24261,
#24262,#24263,#24264,#24265,#24266,#24267,#24268,#24269,#24270,#24271,#24272,
#24273,#24274,#24275,#24276,#24277,#24278,#24279,#24280,#24281,#24282,#24283,
#24284,#24285,#24286,#24287,#24288,#24289,#24290,#24291,#24292,#24293,#24294,
#24295,#24296,#24297,#24298,#24299,#24300,#24301,#24302,#24303,#24304,#24305,
#24306,#24307,#24308,#24309,#24310,#24311,#24312,#24313,#24314,#24315,#24316,
#24317,#24318,#24319,#24320,#24321,#24322,#24323,#24324,#24325,#24326,#24327,
#24328,#24329,#24330,#24331,#24332,#24333,#24334,#24335),.UNSPECIFIED.,
 .F.,.F.,(4,3,3,3,3,3,3,3,3,3,3,3,3,3,3,3,3,3,3,3,3,3,3,3,3,3,3,3,3,3,3,
3,3,3,3,3,3,4),(189.609750253417,189.795701084287,189.984768414674,190.1703338432,
190.361152124518,190.551970405836,190.739508454616,190.926652897001,191.113770969932,
191.300877919756,191.488416104167,191.549624701154,191.737162749492,191.924307191435,
192.111425263935,192.298532213331,192.48607039733,192.547278996473,192.734817044858,
192.921961486842,193.109079559371,193.29618650879,193.483724692802,193.544933291791,
193.732471341682,193.919615785181,194.106733859215,194.293840810136,194.481378995615,
194.54258758711,194.730125633722,194.917270073948,195.10438814477,195.291495092509,
195.479033274912,195.540241882428,195.755377132594,195.892935318778),
 .UNSPECIFIED.);
#283=B_SPLINE_CURVE_WITH_KNOTS('',3,(#24337,#24338,#24339,#24340,#24341,
#24342,#24343,#24344,#24345,#24346),.UNSPECIFIED.,.F.,.F.,(4,1,1,1,1,1,
1,4),(195.892935560597,196.537896177747,197.535550473065,198.533204768384,
199.530859063702,200.528513359021,201.526167654339,202.176120867777),
 .UNSPECIFIED.);
#284=B_SPLINE_CURVE_WITH_KNOTS('',3,(#24348,#24349,#24350,#24351,#24352,
#24353,#24354,#24355,#24356,#24357,#24358,#24359,#24360,#24361,#24362,#24363,
#24364,#24365,#24366,#24367,#24368,#24369,#24370,#24371,#24372,#24373,#24374,
#24375,#24376,#24377,#24378,#24379,#24380,#24381,#24382,#24383,#24384,#24385,
#24386,#24387,#24388,#24389,#24390,#24391,#24392,#24393,#24394,#24395,#24396,
#24397,#24398,#24399,#24400,#24401,#24402,#24403,#24404,#24405,#24406,#24407,
#24408,#24409,#24410,#24411,#24412,#24413,#24414,#24415,#24416,#24417,#24418,
#24419,#24420,#24421,#24422,#24423,#24424,#24425,#24426,#24427,#24428,#24429,
#24430,#24431,#24432,#24433,#24434,#24435,#24436,#24437,#24438,#24439,#24440,
#24441,#24442,#24443,#24444,#24445,#24446,#24447,#24448,#24449,#24450,#24451,
#24452,#24453,#24454,#24455,#24456,#24457,#24458,#24459),.UNSPECIFIED.,
 .F.,.F.,(4,3,3,3,3,3,3,3,3,3,3,3,3,3,3,3,3,3,3,3,3,3,3,3,3,3,3,3,3,3,3,
3,3,3,3,3,3,4),(202.176121107729,202.392189019061,202.523821949658,202.711360327859,
202.898505102102,203.085623505374,203.272730785002,203.460269292354,203.521476244976,
203.709013475378,203.896157100508,204.083274370061,204.270380523695,204.457917936997,
204.519130540295,204.70666908409,204.893814010344,205.080932544026,205.268039941717,
205.455578547114,205.516784835613,205.704324823687,205.891471224293,206.078591252941,
206.26570015905,206.45324026446,206.514439130932,206.701971386111,206.889110036183,
207.07622240564,207.263323697418,207.450856393847,207.51209342625,207.698196269153,
207.888473745604,208.074153943652,208.266730059304,208.459306174956),
 .UNSPECIFIED.);
#285=B_SPLINE_CURVE_WITH_KNOTS('',3,(#24461,#24462,#24463,#24464,#24465,
#24466,#24467,#24468,#24469,#24470,#24471),.UNSPECIFIED.,.F.,.F.,(4,1,1,
1,1,1,1,1,4),(208.459306174956,208.509747721569,209.507402016887,210.505056312206,
211.502710607524,212.500364902843,213.498019198161,214.49567349348,214.742490275424),
 .UNSPECIFIED.);
#286=B_SPLINE_CURVE_WITH_KNOTS('',3,(#24473,#24474,#24475,#24476,#24477,
#24478,#24479,#24480,#24481,#24482,#24483,#24484,#24485),.UNSPECIFIED.,
 .F.,.F.,(4,3,3,3,4),(214.742491482136,214.924334961889,215.106007171726,
215.288050992593,215.423492510042),.UNSPECIFIED.);
#287=B_SPLINE_CURVE_WITH_KNOTS('',3,(#24489,#24490,#24491,#24492,#24493,
#24494,#24495,#24496,#24497,#24498),.UNSPECIFIED.,.F.,.F.,(4,1,1,1,1,1,
1,4),(-217.488636379435,-216.490982084117,-215.493327788798,-214.49567349348,
-213.498019198161,-212.500364902843,-211.502710607524,-211.437656885764),
 .UNSPECIFIED.);
#288=B_SPLINE_CURVE_WITH_KNOTS('',3,(#24500,#24501,#24502,#24503,#24504,
#24505,#24506,#24507,#24508,#24509,#24510,#24511,#24512,#24513,#24514,#24515,
#24516,#24517,#24518,#24519,#24520,#24521,#24522,#24523,#24524,#24525,#24526,
#24527,#24528,#24529,#24530,#24531,#24532,#24533,#24534,#24535,#24536,#24537,
#24538,#24539,#24540,#24541,#24542,#24543,#24544,#24545,#24546,#24547,#24548,
#24549,#24550,#24551,#24552,#24553,#24554,#24555,#24556,#24557,#24558,#24559,
#24560,#24561,#24562,#24563,#24564,#24565,#24566,#24567,#24568,#24569,#24570,
#24571,#24572,#24573,#24574,#24575,#24576,#24577,#24578,#24579,#24580,#24581,
#24582,#24583,#24584,#24585,#24586,#24587,#24588,#24589,#24590,#24591,#24592,
#24593,#24594,#24595,#24596,#24597,#24598,#24599,#24600,#24601,#24602,#24603,
#24604,#24605,#24606,#24607,#24608,#24609,#24610,#24611),.UNSPECIFIED.,
 .F.,.F.,(4,3,3,3,3,3,3,3,3,3,3,3,3,3,3,3,3,3,3,3,3,3,3,3,3,3,3,3,3,3,3,
3,3,3,3,3,3,4),(-211.437656885764,-211.251875774012,-211.065170908561,-210.879760937552,
-210.692408624879,-210.505056312206,-210.317556428218,-210.130451044026,
-209.9433727371,-209.756306005462,-209.568807969712,-209.507402016887,-209.319853122717,
-209.13269771433,-208.945568669285,-208.758450732574,-208.570901743242,
-208.509747721569,-208.322205304621,-208.135056315231,-207.947933502637,
-207.760821696469,-207.573278571308,-207.51209342625,-207.324560864371,
-207.137422044073,-206.950309704675,-206.763208558969,-206.575676176528,
-206.514439130932,-206.326899161105,-206.139752769977,-205.952632737958,
-205.765523821033,-205.577983694059,-205.516784835613,-205.303371487571,
-205.154471579052),.UNSPECIFIED.);
#289=B_SPLINE_CURVE_WITH_KNOTS('',3,(#24613,#24614,#24615,#24616,#24617,
#24618,#24619,#24620,#24621,#24622,#24623,#24624,#24625,#24626,#24627,#24628,
#24629,#24630,#24631,#24632,#24633,#24634,#24635,#24636,#24637,#24638,#24639,
#24640,#24641,#24642,#24643,#24644,#24645,#24646,#24647,#24648,#24649,#24650,
#24651,#24652,#24653,#24654,#24655,#24656,#24657,#24658,#24659,#24660,#24661,
#24662,#24663,#24664,#24665,#24666,#24667,#24668,#24669,#24670,#24671,#24672,
#24673,#24674,#24675,#24676,#24677,#24678,#24679,#24680,#24681,#24682,#24683,
#24684,#24685,#24686,#24687,#24688,#24689,#24690,#24691,#24692,#24693,#24694,
#24695,#24696,#24697,#24698,#24699,#24700,#24701,#24702,#24703,#24704,#24705,
#24706,#24707,#24708,#24709,#24710,#24711,#24712,#24713,#24714,#24715,#24716,
#24717,#24718,#24719,#24720,#24721,#24722,#24723,#24724,#24725,#24726,#24727),
 .UNSPECIFIED.,.F.,.F.,(4,3,3,3,3,3,3,3,3,3,3,3,3,3,3,3,3,3,3,3,3,3,3,3,
3,3,3,3,3,3,3,3,3,3,3,3,3,3,4),(-205.154471578585,-204.966416462605,-204.778333592112,
-204.589761204189,-204.519130540295,-204.331593262598,-204.144449611253,
-203.957332346419,-203.770226215423,-203.582688850692,-203.521476244976,
-203.33393787321,-203.146793102426,-202.95967469825,-202.77256741519,-202.585028900752,
-202.523821949658,-202.336283872299,-202.149139398908,-201.962021291873,
-201.774914306113,-201.587376083692,-201.526167654339,-201.338629711466,
-201.15148537787,-200.964367416273,-200.777260579377,-200.58972250818,-200.528513359021,
-200.340975258119,-200.153830762642,-199.966712636016,-199.779605632095,
-199.592067393986,-199.530859063702,-199.343221598296,-199.155994350822,
-198.968876899421,-198.871286271405),.UNSPECIFIED.);
#290=B_SPLINE_CURVE_WITH_KNOTS('',3,(#24729,#24730,#24731,#24732,#24733,
#24734,#24735,#24736,#24737,#24738),.UNSPECIFIED.,.F.,.F.,(4,1,1,1,1,1,
1,4),(-198.871278975199,-198.533204768384,-197.535550473065,-196.537896177747,
-195.540241882428,-194.54258758711,-193.544933291791,-192.588106266864),
 .UNSPECIFIED.);
#291=B_SPLINE_CURVE_WITH_KNOTS('',3,(#24740,#24741,#24742,#24743,#24744,
#24745,#24746,#24747,#24748,#24749,#24750,#24751,#24752,#24753,#24754,#24755,
#24756,#24757,#24758,#24759,#24760,#24761,#24762,#24763,#24764,#24765,#24766,
#24767,#24768,#24769,#24770,#24771,#24772,#24773,#24774,#24775,#24776,#24777,
#24778,#24779,#24780,#24781,#24782,#24783,#24784,#24785,#24786,#24787,#24788,
#24789,#24790,#24791,#24792,#24793,#24794,#24795,#24796,#24797,#24798,#24799,
#24800,#24801,#24802,#24803,#24804,#24805,#24806,#24807,#24808,#24809,#24810,
#24811,#24812,#24813,#24814,#24815,#24816,#24817,#24818,#24819,#24820,#24821,
#24822,#24823,#24824,#24825,#24826,#24827,#24828,#24829,#24830,#24831,#24832,
#24833,#24834,#24835,#24836,#24837,#24838,#24839,#24840,#24841,#24842,#24843,
#24844,#24845,#24846,#24847,#24848,#24849,#24850,#24851,#24852,#24853,#24854,
#24855,#24856,#24857),.UNSPECIFIED.,.F.,.F.,(4,3,3,3,3,3,3,3,3,3,3,3,3,
3,3,3,3,3,3,3,3,3,3,3,3,3,3,3,3,3,3,3,3,3,3,3,3,3,3,4),(-192.588100964226,
-192.547278996473,-192.359740948114,-192.172596506158,-191.985478433661,
-191.798371484274,-191.610833300298,-191.549624701154,-191.362086652382,
-191.174942210002,-190.987824137069,-190.800717187241,-190.613179002821,
-190.551970405836,-190.364432357295,-190.177287915152,-189.990169842458,
-189.803062892871,-189.61552470869,-189.554316110517,-189.366778061959,
-189.179633619798,-188.992515547088,-188.805408597486,-188.617870413291,
-188.556661815199,-188.369123766587,-188.18197932437,-187.994861251603,
-187.807754301943,-187.62021611769,-187.55900751988,-187.371469471304,-187.184325029124,
-186.997206956394,-186.810100006771,-186.622561822555,-186.561353224562,
-186.321110839942,-186.304915803035),.UNSPECIFIED.);
#292=B_SPLINE_CURVE_WITH_KNOTS('',3,(#24859,#24860,#24861,#24862,#24863,
#24864,#24865,#24866,#24867,#24868),.UNSPECIFIED.,.F.,.F.,(4,1,1,1,1,1,
1,4),(-186.304915657046,-185.563698929243,-184.566044633925,-183.568390338606,
-182.570736043288,-181.573081747969,-180.575427452651,-180.021730349867),
 .UNSPECIFIED.);
#293=B_SPLINE_CURVE_WITH_KNOTS('',3,(#24870,#24871,#24872,#24873,#24874,
#24875,#24876,#24877,#24878,#24879),.UNSPECIFIED.,.F.,.F.,(4,1,1,1,1,1,
1,4),(-180.021730349867,-179.577773157332,-178.580118862013,-177.582464566695,
-176.584810271376,-175.587155976058,-174.589501680739,-173.738552553459),
 .UNSPECIFIED.);
#294=B_SPLINE_CURVE_WITH_KNOTS('',3,(#24881,#24882,#24883,#24884,#24885,
#24886,#24887,#24888,#24889,#24890,#24891,#24892,#24893,#24894,#24895,#24896,
#24897,#24898,#24899,#24900,#24901,#24902,#24903,#24904,#24905,#24906,#24907,
#24908,#24909,#24910,#24911,#24912,#24913,#24914,#24915,#24916,#24917,#24918,
#24919,#24920,#24921,#24922,#24923,#24924,#24925,#24926,#24927,#24928,#24929,
#24930,#24931,#24932,#24933,#24934,#24935,#24936,#24937,#24938,#24939,#24940,
#24941,#24942,#24943,#24944,#24945,#24946,#24947,#24948,#24949,#24950,#24951,
#24952,#24953,#24954,#24955,#24956,#24957,#24958,#24959,#24960,#24961,#24962,
#24963,#24964,#24965,#24966,#24967,#24968,#24969,#24970,#24971,#24972,#24973,
#24974,#24975,#24976,#24977,#24978,#24979,#24980,#24981,#24982,#24983,#24984,
#24985,#24986,#24987,#24988,#24989,#24990,#24991,#24992,#24993,#24994,#24995),
 .UNSPECIFIED.,.F.,.F.,(4,3,3,3,3,3,3,3,3,3,3,3,3,3,3,3,3,3,3,3,3,3,3,3,
3,3,3,3,3,3,3,3,3,3,3,3,3,3,4),(-173.738545042687,-173.591847385421,-173.404309336835,
-173.217164894645,-173.030046821905,-172.842939872272,-172.655401688047,
-172.594193090102,-172.406655041518,-172.21951059933,-172.032392526592,
-171.845285576961,-171.657747392738,-171.596538794784,-171.409000746199,
-171.221856304011,-171.034738231272,-170.847631281641,-170.660093097417,
-170.598884499465,-170.41134645088,-170.224202008692,-170.037083935953,
-169.849976986322,-169.662438802098,-169.601230204147,-169.413692155562,
-169.226547713374,-169.039429640635,-168.852322691004,-168.66478450678,
-168.603575908828,-168.416037860243,-168.228893418054,-168.041775345316,
-167.854668395684,-167.66713021146,-167.60592161351,-167.455359735508),
 .UNSPECIFIED.);
#295=B_SPLINE_CURVE_WITH_KNOTS('',3,(#24997,#24998,#24999,#25000,#25001,
#25002,#25003,#25004,#25005,#25006),.UNSPECIFIED.,.F.,.F.,(4,1,1,1,1,1,
1,4),(-167.455352458497,-166.608267318191,-165.610613022873,-164.612958727554,
-163.615304432236,-162.617650136917,-161.619995841599,-161.172174428328),
 .UNSPECIFIED.);
#296=B_SPLINE_CURVE_WITH_KNOTS('',3,(#25008,#25009,#25010,#25011,#25012,
#25013,#25014,#25015,#25016,#25017),.UNSPECIFIED.,.F.,.F.,(4,1,1,1,1,1,
1,4),(-161.172174428328,-160.62234154628,-159.624687250962,-158.627032955643,
-157.629378660325,-156.631724365006,-155.634070069688,-154.888989121148),
 .UNSPECIFIED.);
#297=B_SPLINE_CURVE_WITH_KNOTS('',3,(#25019,#25020,#25021,#25022,#25023,
#25024,#25025,#25026,#25027,#25028,#25029,#25030,#25031,#25032,#25033,#25034,
#25035,#25036,#25037,#25038,#25039,#25040,#25041,#25042,#25043,#25044,#25045,
#25046,#25047,#25048,#25049,#25050,#25051,#25052,#25053,#25054,#25055,#25056,
#25057,#25058,#25059,#25060,#25061,#25062,#25063,#25064,#25065,#25066,#25067,
#25068,#25069,#25070,#25071,#25072,#25073,#25074,#25075,#25076,#25077,#25078,
#25079,#25080,#25081,#25082,#25083,#25084,#25085,#25086,#25087,#25088,#25089,
#25090,#25091,#25092,#25093,#25094,#25095,#25096,#25097,#25098,#25099,#25100,
#25101,#25102,#25103,#25104,#25105,#25106,#25107,#25108,#25109,#25110,#25111,
#25112,#25113,#25114,#25115,#25116,#25117,#25118,#25119,#25120,#25121,#25122,
#25123,#25124,#25125,#25126,#25127,#25128,#25129,#25130,#25131,#25132,#25133),
 .UNSPECIFIED.,.F.,.F.,(4,3,3,3,3,3,3,3,3,3,3,3,3,3,3,3,3,3,3,3,3,3,3,3,
3,3,3,3,3,3,3,3,3,3,3,3,3,3,4),(-154.88898899765,-154.636415774369,-154.448877725784,
-154.261733283596,-154.074615210858,-153.887508261227,-153.699970077003,
-153.638761479051,-153.451223430466,-153.264078988277,-153.076960915538,
-152.889853965907,-152.702315781682,-152.641107183732,-152.453569135147,
-152.266424692959,-152.079306620221,-151.89219967059,-151.704661486366,
-151.643452888414,-151.455914839829,-151.268770397641,-151.081652324902,
-150.894545375271,-150.707007191046,-150.645798593095,-150.45826054451,
-150.271116102322,-150.083998029584,-149.896891079952,-149.709352895728,
-149.648144297777,-149.460606249192,-149.273461807004,-149.086343734265,
-148.899236784634,-148.71169860041,-148.650490002458,-148.605803813969),
 .UNSPECIFIED.);
#298=B_SPLINE_CURVE_WITH_KNOTS('',3,(#25135,#25136,#25137,#25138,#25139,
#25140,#25141,#25142,#25143,#25144),.UNSPECIFIED.,.F.,.F.,(4,1,1,1,1,1,
1,4),(-148.605798125697,-147.65283570714,-146.655181411821,-145.657527116503,
-144.659872821184,-143.662218525866,-142.664564230547,-142.322618506789),
 .UNSPECIFIED.);
#299=B_SPLINE_CURVE_WITH_KNOTS('',3,(#25146,#25147,#25148,#25149,#25150,
#25151,#25152,#25153,#25154,#25155),.UNSPECIFIED.,.F.,.F.,(4,1,1,1,1,1,
1,4),(-142.322618506789,-141.666909935229,-140.66925563991,-139.671601344592,
-138.673947049273,-137.676292753955,-136.678638458636,-136.03943319961),
 .UNSPECIFIED.);
#300=B_SPLINE_CURVE_WITH_KNOTS('',3,(#25157,#25158,#25159,#25160,#25161,
#25162,#25163,#25164,#25165,#25166,#25167,#25168,#25169,#25170,#25171,#25172,
#25173,#25174,#25175,#25176,#25177,#25178,#25179,#25180,#25181,#25182,#25183,
#25184,#25185,#25186,#25187,#25188,#25189,#25190,#25191,#25192,#25193,#25194,
#25195,#25196,#25197,#25198,#25199,#25200,#25201,#25202,#25203,#25204,#25205,
#25206,#25207,#25208,#25209,#25210,#25211,#25212,#25213,#25214,#25215,#25216,
#25217,#25218,#25219,#25220,#25221,#25222,#25223,#25224,#25225,#25226,#25227,
#25228,#25229,#25230,#25231,#25232,#25233,#25234,#25235,#25236,#25237,#25238,
#25239,#25240,#25241,#25242,#25243,#25244,#25245,#25246,#25247,#25248,#25249,
#25250,#25251,#25252,#25253,#25254,#25255,#25256,#25257,#25258,#25259,#25260,
#25261,#25262,#25263,#25264,#25265,#25266,#25267,#25268),.UNSPECIFIED.,
 .F.,.F.,(4,3,3,3,3,3,3,3,3,3,3,3,3,3,3,3,3,3,3,3,3,3,3,3,3,3,3,3,3,3,3,
3,3,3,3,3,3,4),(-136.039432956653,-135.825338523247,-135.680984163318,-135.493446114733,
-135.306301672544,-135.119183599805,-134.932076650173,-134.744538465948,
-134.683329867999,-134.495791819414,-134.308647377225,-134.121529304486,
-133.934422354855,-133.74688417063,-133.68567557268,-133.498137524096,-133.310993081908,
-133.12387500917,-132.936768059539,-132.749229875315,-132.688021277362,
-132.500483228777,-132.313338786588,-132.12622071385,-131.939113764218,
-131.751575579994,-131.690366982043,-131.502828933458,-131.31568449127,
-131.128566418532,-130.9414594689,-130.753921284676,-130.692712686725,-130.506853125115,
-130.319201816944,-130.133765499097,-129.945006695764,-129.75624789243),
 .UNSPECIFIED.);
#301=B_SPLINE_CURVE_WITH_KNOTS('',3,(#25270,#25271,#25272,#25273,#25274,
#25275,#25276,#25277,#25278,#25279,#25280),.UNSPECIFIED.,.F.,.F.,(4,1,1,
1,1,1,1,1,4),(-129.75624789243,-129.695058391406,-128.697404096088,-127.699749800769,
-126.702095505451,-125.704441210132,-124.706786914814,-123.709132619495,
-123.473062585251),.UNSPECIFIED.);
#302=B_SPLINE_CURVE_WITH_KNOTS('',3,(#25282,#25283,#25284,#25285,#25286,
#25287,#25288,#25289,#25290,#25291),.UNSPECIFIED.,.F.,.F.,(4,1,1,1,1,1,
1,4),(-123.473062585251,-122.711478324177,-121.713824028858,-120.71616973354,
-119.718515438221,-118.720861142903,-117.723206847584,-117.189877278071),
 .UNSPECIFIED.);
#303=B_SPLINE_CURVE_WITH_KNOTS('',3,(#25293,#25294,#25295,#25296,#25297,
#25298,#25299,#25300,#25301,#25302,#25303,#25304,#25305,#25306,#25307,#25308,
#25309,#25310,#25311,#25312,#25313,#25314,#25315,#25316,#25317,#25318,#25319,
#25320,#25321,#25322,#25323,#25324,#25325,#25326,#25327,#25328,#25329,#25330,
#25331,#25332,#25333,#25334,#25335,#25336,#25337,#25338,#25339,#25340,#25341,
#25342,#25343,#25344,#25345,#25346,#25347,#25348,#25349,#25350,#25351,#25352,
#25353,#25354,#25355,#25356,#25357,#25358,#25359,#25360,#25361,#25362,#25363,
#25364,#25365,#25366,#25367,#25368,#25369,#25370,#25371,#25372,#25373,#25374,
#25375,#25376,#25377,#25378,#25379,#25380,#25381,#25382,#25383,#25384,#25385,
#25386,#25387,#25388,#25389,#25390,#25391,#25392,#25393,#25394,#25395,#25396,
#25397,#25398,#25399,#25400,#25401,#25402,#25403,#25404,#25405,#25406,#25407),
 .UNSPECIFIED.,.F.,.F.,(4,3,3,3,3,3,3,3,3,3,3,3,3,3,3,3,3,3,3,3,3,3,3,3,
3,3,3,3,3,3,3,3,3,3,3,3,3,3,4),(-117.189877092994,-116.990698231071,-116.790432269088,
-116.725552552266,-116.538014503681,-116.350870061492,-116.163751988753,
-115.976645039121,-115.789106854896,-115.727898256947,-115.540360208363,
-115.353215766174,-115.166097693436,-114.978990743805,-114.791452559582,
-114.730243961629,-114.542705913044,-114.355561470855,-114.168443398117,
-113.981336448486,-113.793798264261,-113.73258966631,-113.545051617725,
-113.357907175537,-113.170789102799,-112.983682153167,-112.796143968943,
-112.734935370992,-112.547397322407,-112.360252880219,-112.173134807481,
-111.986027857849,-111.798489673625,-111.737281075673,-111.552535196557,
-111.368083942092,-111.183809075707,-110.999269022242,-110.906691970891),
 .UNSPECIFIED.);
#304=B_SPLINE_CURVE_WITH_KNOTS('',3,(#25409,#25410,#25411,#25412,#25413,
#25414,#25415,#25416,#25417,#25418,#25419),.UNSPECIFIED.,.F.,.F.,(4,1,1,
1,1,1,1,1,4),(-110.906691970891,-110.739626780355,-109.741972485036,-108.744318189718,
-107.746663894399,-106.749009599081,-105.751355303762,-104.753701008444,
-104.623506663712),.UNSPECIFIED.);
#305=B_SPLINE_CURVE_WITH_KNOTS('',3,(#25421,#25422,#25423,#25424,#25425,
#25426,#25427,#25428,#25429,#25430),.UNSPECIFIED.,.F.,.F.,(4,1,1,1,1,1,
1,4),(-104.623506663712,-103.756046713125,-102.758392417807,-101.760738122488,
-100.76308382717,-99.7654295318511,-98.7677752365326,-98.3403266725638),
 .UNSPECIFIED.);
#306=B_SPLINE_CURVE_WITH_KNOTS('',3,(#25432,#25433,#25434,#25435,#25436,
#25437,#25438,#25439,#25440,#25441,#25442,#25443,#25444,#25445,#25446,#25447,
#25448,#25449,#25450,#25451,#25452,#25453,#25454,#25455,#25456,#25457,#25458,
#25459,#25460,#25461,#25462,#25463,#25464,#25465,#25466,#25467,#25468,#25469,
#25470,#25471,#25472,#25473,#25474,#25475,#25476,#25477,#25478,#25479,#25480,
#25481,#25482,#25483,#25484,#25485,#25486,#25487,#25488,#25489,#25490,#25491,
#25492,#25493,#25494,#25495,#25496,#25497,#25498,#25499,#25500,#25501,#25502,
#25503,#25504,#25505,#25506,#25507,#25508,#25509,#25510,#25511,#25512,#25513,
#25514,#25515,#25516,#25517,#25518,#25519,#25520,#25521,#25522,#25523,#25524,
#25525,#25526,#25527,#25528,#25529,#25530,#25531,#25532,#25533,#25534,#25535,
#25536,#25537,#25538,#25539,#25540,#25541,#25542,#25543),.UNSPECIFIED.,
 .F.,.F.,(4,3,3,3,3,3,3,3,3,3,3,3,3,3,3,3,3,3,3,3,3,3,3,3,3,3,3,3,3,3,3,
3,3,3,3,3,3,4),(-98.3403213565322,-98.1491648751557,-97.9573414616566,-97.7701209412141,
-97.5825828926293,-97.3954384504409,-97.2083203777026,-97.0212134280712,
-96.833675243847,-96.7724666458956,-96.5849285973108,-96.3977841551224,
-96.2106660823841,-96.0235591327527,-95.8360209485285,-95.7748123505771,
-95.5872743019923,-95.4001298598038,-95.2130117870654,-95.025904837434,
-94.8383666532097,-94.7771580552585,-94.5896200066737,-94.4024755644853,
-94.215357491747,-94.0282505421157,-93.8407123578914,-93.77950375994,-93.5919657113552,
-93.4048212691667,-93.2177031964284,-93.030596246797,-92.8430580625728,
-92.7818494646215,-92.5960124093366,-92.4105589018408,-92.2250567751402,
-92.0571360493526),.UNSPECIFIED.);
#307=B_SPLINE_CURVE_WITH_KNOTS('',3,(#25545,#25546,#25547,#25548,#25549,
#25550,#25551,#25552,#25553,#25554,#25555),.UNSPECIFIED.,.F.,.F.,(4,1,1,
1,1,1,1,1,4),(-92.0571324486301,-91.784195169303,-90.7865408739845,-89.788886578666,
-88.7912322833475,-87.793577988029,-86.7959236927104,-85.7982693973919,
-85.773950742173),.UNSPECIFIED.);
#308=B_SPLINE_CURVE_WITH_KNOTS('',3,(#25557,#25558,#25559,#25560,#25561,
#25562,#25563,#25564,#25565,#25566),.UNSPECIFIED.,.F.,.F.,(4,1,1,1,1,1,
1,4),(-85.773950742173,-84.8006151020734,-83.8029608067549,-82.8053065114364,
-81.8076522161179,-80.8099979207994,-79.8123436254809,-79.4907721948393),
 .UNSPECIFIED.);
#309=B_SPLINE_CURVE_WITH_KNOTS('',3,(#25568,#25569,#25570,#25571,#25572,
#25573,#25574,#25575,#25576,#25577,#25578,#25579,#25580,#25581,#25582,#25583,
#25584,#25585,#25586,#25587,#25588,#25589,#25590,#25591,#25592,#25593,#25594,
#25595,#25596,#25597,#25598,#25599,#25600,#25601,#25602,#25603,#25604,#25605,
#25606,#25607,#25608,#25609,#25610,#25611,#25612,#25613,#25614,#25615,#25616,
#25617,#25618,#25619,#25620,#25621,#25622,#25623,#25624,#25625,#25626,#25627,
#25628,#25629,#25630,#25631,#25632,#25633,#25634,#25635,#25636,#25637,#25638,
#25639,#25640,#25641,#25642,#25643,#25644,#25645,#25646,#25647,#25648,#25649,
#25650,#25651,#25652,#25653,#25654,#25655,#25656,#25657,#25658,#25659,#25660,
#25661,#25662,#25663,#25664,#25665,#25666,#25667,#25668,#25669,#25670,#25671,
#25672,#25673,#25674,#25675,#25676,#25677,#25678,#25679,#25680,#25681,#25682),
 .UNSPECIFIED.,.F.,.F.,(4,3,3,3,3,3,3,3,3,3,3,3,3,3,3,3,3,3,3,3,3,3,3,3,
3,3,3,3,3,3,3,3,3,3,3,3,3,3,4),(-79.4907654349934,-79.304094347987,-79.1174778110582,
-78.9303964543316,-78.8146893301624,-78.6271512815776,-78.4400068393891,
-78.2528887666508,-78.0657818170195,-77.8782436327954,-77.8170350348439,
-77.629496986259,-77.4423525440705,-77.2552344713322,-77.0681275217008,
-76.8805893374765,-76.8193807395253,-76.6318426909405,-76.4446982487521,
-76.2575801760138,-76.0704732263825,-75.8829350421583,-75.8217264442068,
-75.634188395622,-75.4470439534335,-75.2599258806952,-75.0728189310639,
-74.8852807468398,-74.8240721488883,-74.6365341003035,-74.4493896581151,
-74.2622715853767,-74.0751646357452,-73.887626451521,-73.8264178535698,
-73.6371361639319,-73.448293995353,-73.2596672789205,-73.2075801278138),
 .UNSPECIFIED.);
#310=B_SPLINE_CURVE_WITH_KNOTS('',3,(#25684,#25685,#25686,#25687,#25688,
#25689,#25690,#25691,#25692,#25693),.UNSPECIFIED.,.F.,.F.,(4,1,1,1,1,1,
1,4),(-73.2075727019911,-72.8287635582513,-71.8311092629328,-70.8334549676143,
-69.8358006722958,-68.8381463769772,-67.8404920816587,-66.9243948206342),
 .UNSPECIFIED.);
#311=B_SPLINE_CURVE_WITH_KNOTS('',3,(#25695,#25696,#25697,#25698,#25699,
#25700,#25701,#25702,#25703,#25704,#25705),.UNSPECIFIED.,.F.,.F.,(4,1,1,
1,1,1,1,1,4),(-66.9243948206342,-66.8428377863402,-65.8451834910217,-64.8475291957032,
-63.8498749003847,-62.8522206050662,-61.8545663097477,-60.8569120144292,
-60.6412095134546),.UNSPECIFIED.);
#312=B_SPLINE_CURVE_WITH_KNOTS('',3,(#25707,#25708,#25709,#25710,#25711,
#25712,#25713,#25714,#25715,#25716,#25717,#25718,#25719,#25720,#25721,#25722,
#25723,#25724,#25725,#25726,#25727,#25728,#25729,#25730,#25731,#25732,#25733,
#25734,#25735,#25736,#25737,#25738,#25739,#25740,#25741,#25742,#25743,#25744,
#25745,#25746,#25747,#25748,#25749,#25750,#25751,#25752,#25753,#25754,#25755,
#25756,#25757,#25758,#25759,#25760,#25761,#25762,#25763,#25764,#25765,#25766,
#25767,#25768,#25769,#25770,#25771,#25772,#25773,#25774,#25775,#25776,#25777,
#25778,#25779,#25780,#25781,#25782,#25783,#25784,#25785,#25786,#25787,#25788,
#25789,#25790,#25791,#25792,#25793,#25794,#25795,#25796,#25797,#25798,#25799,
#25800,#25801,#25802,#25803,#25804,#25805,#25806,#25807,#25808,#25809,#25810,
#25811,#25812,#25813,#25814,#25815,#25816,#25817,#25818,#25819,#25820,#25821),
 .UNSPECIFIED.,.F.,.F.,(4,3,3,3,3,3,3,3,3,3,3,3,3,3,3,3,3,3,3,3,3,3,3,3,
3,3,3,3,3,3,3,3,3,3,3,3,3,3,4),(-60.6412095134546,-60.4565760673968,-60.2720035492817,
-60.0874545223872,-59.9024986035968,-59.8592577191107,-59.6717196705258,
-59.4845752283373,-59.2974571555989,-59.1103502059676,-58.9228120217433,
-58.8616034237921,-58.6740653752073,-58.4869209330187,-58.2998028602804,
-58.112695910649,-57.9251577264247,-57.8639491284736,-57.6764110798888,
-57.4892666377004,-57.3021485649622,-57.1150416153308,-56.9275034311067,
-56.8662948331551,-56.6787567845703,-56.4916123423818,-56.3044942696435,
-56.1173873200121,-55.9298491357879,-55.8686405378366,-55.6811024892518,
-55.4939580470634,-55.3068399743251,-55.1197330246937,-54.9321948404695,
-54.8709862425181,-54.6751263136016,-54.4800162445405,-54.358024206275),
 .UNSPECIFIED.);
#313=B_SPLINE_CURVE_WITH_KNOTS('',3,(#25823,#25824,#25825,#25826,#25827,
#25828,#25829,#25830,#25831,#25832),.UNSPECIFIED.,.F.,.F.,(4,1,1,1,1,1,
1,4),(-54.358023115501,-53.8733319471996,-52.8756776518811,-51.8780233565626,
-50.8803690612441,-49.8827147659256,-48.885060470607,-48.0748388990954),
 .UNSPECIFIED.);
#314=B_SPLINE_CURVE_WITH_KNOTS('',3,(#25834,#25835,#25836,#25837,#25838,
#25839,#25840,#25841,#25842,#25843,#25844),.UNSPECIFIED.,.F.,.F.,(4,1,1,
1,1,1,1,1,4),(-48.0748388990954,-47.8874061752885,-46.88975187997,-45.8920975846515,
-44.894443289333,-43.8967889940145,-42.899134698696,-41.9014804033775,-41.7916535919158),
 .UNSPECIFIED.);
#315=B_SPLINE_CURVE_WITH_KNOTS('',3,(#25846,#25847,#25848,#25849,#25850,
#25851,#25852,#25853,#25854,#25855,#25856,#25857,#25858,#25859,#25860,#25861,
#25862,#25863,#25864,#25865,#25866,#25867,#25868,#25869,#25870,#25871,#25872,
#25873,#25874,#25875,#25876,#25877,#25878,#25879,#25880,#25881,#25882,#25883,
#25884,#25885,#25886,#25887,#25888,#25889,#25890,#25891,#25892,#25893,#25894,
#25895,#25896,#25897,#25898,#25899,#25900,#25901,#25902,#25903,#25904,#25905,
#25906,#25907,#25908,#25909,#25910,#25911,#25912,#25913,#25914,#25915,#25916,
#25917,#25918,#25919,#25920,#25921,#25922,#25923,#25924,#25925,#25926,#25927,
#25928,#25929,#25930,#25931,#25932,#25933,#25934,#25935,#25936,#25937,#25938,
#25939,#25940,#25941,#25942,#25943,#25944,#25945,#25946,#25947,#25948,#25949,
#25950,#25951,#25952,#25953,#25954,#25955,#25956,#25957),.UNSPECIFIED.,
 .F.,.F.,(4,3,3,3,3,3,3,3,3,3,3,3,3,3,3,3,3,3,3,3,3,3,3,3,3,3,3,3,3,3,3,
3,3,3,3,3,3,4),(-41.7916535919158,-41.606689253253,-41.4219028141221,-41.2372475937333,
-41.0521611009319,-40.903826108059,-40.7162880594741,-40.5291436172856,
-40.3420255445473,-40.1549185949159,-39.9673804106916,-39.9061718127404,
-39.7186337641556,-39.5314893219672,-39.3443712492289,-39.1572642995975,
-38.9697261153734,-38.9085175174219,-38.7209794688371,-38.5338350266486,
-38.3467169539102,-38.1596100042788,-37.9720718200545,-37.9108632221034,
-37.7233251735186,-37.5361807313301,-37.3490626585918,-37.1619557089604,
-36.9744175247362,-36.9132089267849,-36.7256708782003,-36.5385264360123,
-36.3514083632743,-36.1643014136432,-35.9767632294192,-35.9155546314664,
-35.7089829159113,-35.5084687048588),.UNSPECIFIED.);
#316=B_SPLINE_CURVE_WITH_KNOTS('',3,(#25959,#25960,#25961,#25962,#25963,
#25964,#25965,#25966,#25967,#25968),.UNSPECIFIED.,.F.,.F.,(4,1,1,1,1,1,
1,4),(-35.5084682847362,-34.9179003361479,-33.9202460408294,-32.9225917455109,
-31.9249374501923,-30.9272831548738,-29.9296288595553,-29.2252829775566),
 .UNSPECIFIED.);
#317=B_SPLINE_CURVE_WITH_KNOTS('',3,(#25970,#25971,#25972,#25973,#25974,
#25975,#25976,#25977,#25978,#25979,#25980,#25981,#25982,#25983,#25984,#25985,
#25986,#25987,#25988,#25989,#25990,#25991,#25992,#25993,#25994,#25995,#25996,
#25997,#25998,#25999,#26000,#26001,#26002,#26003,#26004,#26005,#26006,#26007,
#26008,#26009,#26010,#26011,#26012,#26013,#26014,#26015,#26016,#26017,#26018,
#26019,#26020,#26021,#26022,#26023,#26024,#26025,#26026,#26027,#26028,#26029,
#26030,#26031,#26032,#26033,#26034,#26035,#26036,#26037,#26038,#26039,#26040,
#26041,#26042,#26043,#26044,#26045,#26046,#26047,#26048,#26049,#26050,#26051,
#26052,#26053,#26054,#26055,#26056,#26057,#26058,#26059,#26060,#26061,#26062,
#26063,#26064,#26065,#26066,#26067,#26068,#26069,#26070,#26071,#26072,#26073,
#26074,#26075,#26076,#26077,#26078,#26079,#26080,#26081,#26082,#26083,#26084),
 .UNSPECIFIED.,.F.,.F.,(4,3,3,3,3,3,3,3,3,3,3,3,3,3,3,3,3,3,3,3,3,3,3,3,
3,3,3,3,3,3,3,3,3,3,3,3,3,3,4),(-29.2252828103121,-28.9967968814183,-28.9319745642368,
-28.7444365156814,-28.557292073522,-28.3701740008118,-28.1830670512081,
-27.9955288670104,-27.9343202689183,-27.746782220377,-27.5596377782329,
-27.3725197055393,-27.1854127559528,-26.9978745717731,-26.9366659735998,
-26.7491279248186,-26.5619834824335,-26.374865409501,-26.1877584596766,
-26.0002202752648,-25.9390116782813,-25.751473629944,-25.5643291880011,
-25.3772111155019,-25.1901041661061,-25.002565982108,-24.9413573829628,
-24.7538193345779,-24.5666748925946,-24.3795568200659,-24.1924498706469,
-24.0049116866351,-23.9437030876443,-23.7560287176089,-23.5687482990062,
-23.3814945807613,-23.1942535727822,-23.0065797464408,-22.9420976703771),
 .UNSPECIFIED.);
#318=B_SPLINE_CURVE_WITH_KNOTS('',3,(#26086,#26087,#26088,#26089,#26090,
#26091,#26092,#26093,#26094,#26095,#26096,#26097,#26098,#26099,#26100,#26101,
#26102,#26103,#26104,#26105,#26106,#26107,#26108,#26109,#26110,#26111,#26112,
#26113,#26114,#26115,#26116,#26117,#26118,#26119,#26120,#26121,#26122,#26123,
#26124,#26125,#26126,#26127,#26128,#26129,#26130,#26131,#26132,#26133,#26134,
#26135,#26136,#26137,#26138,#26139,#26140,#26141,#26142,#26143,#26144,#26145,
#26146,#26147,#26148,#26149,#26150,#26151,#26152,#26153,#26154,#26155,#26156,
#26157,#26158,#26159,#26160,#26161,#26162,#26163,#26164,#26165,#26166,#26167,
#26168,#26169,#26170,#26171,#26172,#26173,#26174,#26175,#26176,#26177,#26178,
#26179,#26180,#26181,#26182,#26183,#26184,#26185,#26186,#26187,#26188,#26189,
#26190,#26191,#26192,#26193,#26194,#26195,#26196,#26197,#26198,#26199,#26200),
 .UNSPECIFIED.,.F.,.F.,(4,3,3,3,3,3,3,3,3,3,3,3,3,3,3,3,3,3,3,3,3,3,3,3,
3,3,3,3,3,3,3,3,3,3,3,3,3,3,4),(-22.9420976699444,-22.7546926683555,-22.5676808462314,
-22.3806950377695,-22.1937187529239,-22.0063128931654,-21.9483944970072,
-21.7608564490805,-21.5737120075872,-21.3865939355861,-21.1994869867172,
-21.0119488032776,-20.9507402016887,-20.7632021445966,-20.5760576938657,
-20.3889396126633,-20.2018326546044,-20.014294462161,-19.9530859063702,
-19.7655478729557,-19.5784034458762,-19.3912853879325,-19.2041784529296,
-19.0166402828235,-18.9554316110517,-18.7678935619543,-18.5807491195069,
-18.3936310468746,-18.2065240975601,-18.0189859139515,-17.9577773157332,
-17.7702392133082,-17.583094716978,-17.3959765904825,-17.2088695872607,
-17.0213313506759,-16.9601230204147,-16.7337449968225,-16.6589125463892),
 .UNSPECIFIED.);
#319=B_SPLINE_CURVE_WITH_KNOTS('',3,(#26202,#26203,#26204,#26205,#26206,
#26207,#26208,#26209,#26210,#26211),.UNSPECIFIED.,.F.,.F.,(4,1,1,1,1,1,
1,4),(-16.6589123631975,-15.9624687250962,-14.9648144297777,-13.9671601344592,
-12.9695058391406,-11.9718515438221,-10.9741972485036,-10.3757270560179),
 .UNSPECIFIED.);
#320=B_SPLINE_CURVE_WITH_KNOTS('',3,(#26212,#26213,#26214,#26215,#26216,
#26217,#26218,#26219,#26220,#26221),.UNSPECIFIED.,.F.,.F.,(4,1,1,1,1,1,
1,4),(-10.3757270560179,-9.97654295318511,-8.9788886578666,-7.98123436254809,
-6.98358006722958,-5.98592577191107,-4.98827147659255,-4.09255058081676),
 .UNSPECIFIED.);
#321=B_SPLINE_CURVE_WITH_KNOTS('',3,(#26224,#26225,#26226,#26227,#26228,
#26229,#26230,#26231,#26232,#26233,#26234,#26235,#26236,#26237,#26238,#26239,
#26240,#26241,#26242,#26243,#26244,#26245,#26246,#26247,#26248,#26249,#26250,
#26251,#26252,#26253,#26254,#26255,#26256,#26257,#26258,#26259,#26260,#26261,
#26262,#26263,#26264,#26265,#26266,#26267,#26268,#26269,#26270,#26271,#26272,
#26273,#26274,#26275,#26276,#26277,#26278,#26279,#26280,#26281,#26282,#26283,
#26284,#26285,#26286,#26287,#26288,#26289,#26290,#26291,#26292,#26293,#26294,
#26295,#26296,#26297,#26298,#26299,#26300,#26301,#26302,#26303,#26304,#26305,
#26306,#26307,#26308,#26309,#26310,#26311,#26312,#26313,#26314,#26315,#26316,
#26317,#26318,#26319,#26320,#26321,#26322,#26323,#26324,#26325,#26326,#26327,
#26328,#26329,#26330,#26331,#26332,#26333,#26334,#26335,#26336,#26337,#26338,
#26339,#26340,#26341,#26342,#26343,#26344,#26345,#26346,#26347,#26348,#26349,
#26350,#26351,#26352,#26353,#26354,#26355,#26356,#26357,#26358,#26359,#26360,
#26361,#26362,#26363,#26364,#26365,#26366,#26367,#26368,#26369,#26370,#26371,
#26372,#26373,#26374,#26375,#26376,#26377,#26378,#26379,#26380,#26381,#26382,
#26383,#26384,#26385,#26386,#26387,#26388,#26389,#26390,#26391,#26392,#26393,
#26394,#26395,#26396,#26397,#26398,#26399,#26400,#26401,#26402,#26403,#26404,
#26405,#26406,#26407,#26408,#26409,#26410,#26411,#26412,#26413,#26414,#26415,
#26416,#26417,#26418,#26419,#26420,#26421,#26422,#26423,#26424,#26425,#26426,
#26427,#26428,#26429,#26430,#26431,#26432,#26433,#26434,#26435,#26436,#26437,
#26438,#26439,#26440,#26441,#26442,#26443,#26444,#26445,#26446,#26447,#26448,
#26449,#26450,#26451,#26452,#26453,#26454,#26455,#26456,#26457,#26458,#26459,
#26460,#26461),.UNSPECIFIED.,.F.,.F.,(4,2,2,2,2,2,2,2,2,2,2,2,2,2,2,2,2,
2,2,2,2,2,2,2,2,2,2,2,2,2,2,2,2,2,2,2,2,2,2,2,2,2,2,2,2,2,2,2,2,2,2,2,2,
2,2,2,2,2,2,2,2,2,2,2,2,2,2,2,2,2,2,2,2,2,2,2,2,2,2,2,2,2,2,2,2,2,2,2,2,
2,2,2,2,2,2,2,2,2,2,2,2,2,2,2,2,2,2,2,2,2,2,2,2,2,2,2,2,2,4),(0.00242918935322954,
0.0505226468104856,0.0640385215741708,0.0669286141768185,0.0685648686987503,
0.0698307604367571,0.0714826753751052,0.0743653603778451,0.0862943637434652,
0.134113484602536,0.142180620281222,0.143852029721217,0.144770387023611,
0.144773779031473,0.14477721763177,0.144780703710955,0.144784238174555,
0.144787821959457,0.144791456033152,0.144795141369183,0.144798878976188,
0.144802669887737,0.144806515164096,0.144810415902515,0.144814373219479,
0.144818388256983,0.14482246218383,0.144826596235181,0.144830791648857,
0.144835049687563,0.144839371667068,0.144843758943846,0.144848212891647,
0.144852734924487,0.144857326511917,0.144861989155769,0.144866724407045,
0.144871533853314,0.144876419120238,0.144881381891246,0.144886423900231,
0.14566638153748,0.146677815262381,0.148757527729657,0.171783571528887,
0.196782559947427,0.210240787798856,0.218362841192007,0.220794721189844,
0.222317759204107,0.223723438679273,0.225535860417369,0.228537058752678,
0.247993293423039,0.279604858173132,0.291922205180772,0.298232088044613,
0.2997523291405,0.300629094591326,0.301384669018166,0.302348035457082,0.304253869745646,
0.316704528616778,0.35369951060433,0.366633777158306,0.374512391147684,
0.376898922896855,0.378399402173584,0.379788141857469,0.381584041810109,
0.384569105905836,0.404403899847237,0.436386959026362,0.448092667714902,
0.454177972001239,0.455670829512531,0.456541673307705,0.457319337950041,
0.458321442969748,0.459979184762913,0.469885443273327,0.474044967198328,
0.477793798562439,0.521127178688317,0.530261230573272,0.532790624444463,
0.534332636991339,0.535728223937639,0.537519441663396,0.540392734731223,
0.556933725177588,0.601629007291696,0.609449109466361,0.611077051839486,
0.611984877523952,0.612762212040367,0.613744288517051,0.615734937152515,
0.629153701833238,0.674154376990143,0.685318692935192,0.688016240151554,
0.689593218484605,0.690978977752344,0.692702401801144,0.695360473672499,
0.708141141000251,0.713107609325545,0.756919625772014,0.765145527407682,
0.766792023320811,0.767701150500468,0.768475133820461,0.769446637304088,
0.771330455415657,0.782652593667203,0.785658621100046,0.801643789430652,
0.801779048931175),.UNSPECIFIED.);
#322=B_SPLINE_CURVE_WITH_KNOTS('',3,(#26465,#26466,#26467,#26468,#26469,
#26470,#26471,#26472,#26473,#26474,#26475,#26476,#26477,#26478,#26479,#26480,
#26481,#26482,#26483,#26484,#26485,#26486,#26487,#26488,#26489,#26490,#26491,
#26492,#26493,#26494,#26495,#26496,#26497,#26498,#26499,#26500,#26501,#26502,
#26503,#26504,#26505,#26506,#26507),.UNSPECIFIED.,.F.,.F.,(4,3,3,3,3,3,
3,3,3,3,3,3,3,3,4),(223.053078404875,223.249759833269,223.446265667279,
223.643245097141,223.803914711538,224.000284327898,224.200605497638,224.396553130159,
224.599061068508,224.801569006857,225.005649510053,225.209253391211,225.412535507524,
225.615947120473,225.799223302175),.UNSPECIFIED.);
#323=B_SPLINE_CURVE_WITH_KNOTS('',3,(#26508,#26509,#26510,#26511,#26512,
#26513,#26514,#26515,#26516,#26517,#26518,#26519,#26520,#26521,#26522,#26523,
#26524,#26525,#26526,#26527,#26528,#26529,#26530,#26531,#26532,#26533,#26534,
#26535,#26536,#26537,#26538,#26539,#26540,#26541,#26542,#26543,#26544,#26545,
#26546,#26547,#26548,#26549,#26550,#26551),.UNSPECIFIED.,.F.,.F.,(4,2,2,
2,2,2,2,2,2,2,2,2,2,2,2,2,2,2,2,2,2,4),(-1.96155998999565,-1.93145588063156,
-1.92783250967384,-1.92604050708938,-1.92494602585897,-1.9241353570081,
-1.92332132892803,-1.92256838047723,-1.92128904881891,-1.91780013673092,
-1.89003524213539,-1.87442280300735,-1.85403488840081,-1.84929335704467,
-1.84774484628021,-1.8462297091599,-1.84482039163455,-1.84298779932934,
-1.83991922159517,-1.81784809663805,-1.79351172412742,-1.78243981456369),
 .UNSPECIFIED.);
#324=B_SPLINE_CURVE_WITH_KNOTS('',3,(#27436,#27437,#27438,#27439,#27440,
#27441,#27442,#27443,#27444,#27445,#27446,#27447,#27448,#27449,#27450,#27451,
#27452,#27453,#27454,#27455,#27456,#27457,#27458,#27459,#27460,#27461,#27462,
#27463,#27464,#27465,#27466,#27467,#27468,#27469,#27470,#27471,#27472,#27473,
#27474,#27475,#27476,#27477,#27478,#27479,#27480,#27481,#27482,#27483,#27484,
#27485,#27486,#27487,#27488,#27489,#27490),.UNSPECIFIED.,.F.,.F.,(4,3,3,
3,3,3,3,3,3,3,3,3,3,3,3,3,3,3,4),(3.98819129420962E-5,0.0136872263540572,
0.0522766260806668,0.0709950800646878,0.0819953190919729,0.119305547150835,
0.143879290941371,0.156749831780157,0.182262464866333,0.192145397802465,
0.199552864933563,0.215672767979732,0.228806216382242,0.263204057038138,
0.279098426169674,0.293672482722726,0.320133366208391,0.333322815206606,
0.366397579005826),.UNSPECIFIED.);
#325=B_SPLINE_CURVE_WITH_KNOTS('',3,(#27492,#27493,#27494,#27495,#27496,
#27497,#27498,#27499,#27500,#27501,#27502,#27503,#27504,#27505,#27506,#27507,
#27508,#27509,#27510,#27511,#27512,#27513,#27514,#27515,#27516,#27517,#27518,
#27519,#27520,#27521,#27522,#27523,#27524,#27525,#27526,#27527,#27528,#27529,
#27530,#27531,#27532,#27533,#27534,#27535,#27536,#27537,#27538,#27539,#27540,
#27541,#27542,#27543),.UNSPECIFIED.,.F.,.F.,(4,3,3,3,3,3,3,3,3,3,3,3,3,
3,3,3,3,4),(-0.366397579005832,-0.355349081053819,-0.328627709487585,-0.313113754886802,
-0.287021709507735,-0.271827012252881,-0.236673702273149,-0.219261174131459,
-0.205739586164244,-0.187146499846321,-0.163753187365531,-0.146916306560471,
-0.134322373995578,-0.100741780496684,-0.0810578579737637,-0.0639676522746132,
-0.0255059552299406,0.),.UNSPECIFIED.);
#326=B_SPLINE_CURVE_WITH_KNOTS('',3,(#27544,#27545,#27546,#27547),
 .UNSPECIFIED.,.F.,.F.,(4,4),(-0.0124837338197822,0.),.UNSPECIFIED.);
#327=B_SPLINE_CURVE_WITH_KNOTS('',3,(#28433,#28434,#28435,#28436,#28437,
#28438,#28439,#28440,#28441,#28442,#28443,#28444,#28445,#28446,#28447,#28448,
#28449,#28450,#28451,#28452,#28453,#28454,#28455,#28456,#28457,#28458,#28459,
#28460,#28461,#28462,#28463,#28464,#28465,#28466,#28467,#28468,#28469,#28470,
#28471,#28472,#28473,#28474,#28475,#28476,#28477,#28478,#28479,#28480,#28481,
#28482,#28483,#28484,#28485,#28486,#28487),.UNSPECIFIED.,.F.,.F.,(4,3,3,
3,3,3,3,3,3,3,3,3,3,3,3,3,3,3,4),(0.,0.0110072508574968,0.0431732332201684,
0.0597682846665091,0.0725876156054097,0.101643661993379,0.12367084288124,
0.136673094424233,0.169449851669546,0.178576016460901,0.191988153704559,
0.204131677343237,0.240029786311497,0.259562619766513,0.274889031344431,
0.300880821280637,0.315410186444722,0.35044636731004,0.364629307890676),
 .UNSPECIFIED.);
#328=B_SPLINE_CURVE_WITH_KNOTS('',3,(#28488,#28489,#28490,#28491),
 .UNSPECIFIED.,.F.,.F.,(4,4),(0.,0.0126590312177446),.UNSPECIFIED.);
#329=B_SPLINE_CURVE_WITH_KNOTS('',3,(#28492,#28493,#28494,#28495,#28496,
#28497,#28498,#28499,#28500,#28501,#28502,#28503,#28504,#28505,#28506,#28507,
#28508,#28509,#28510,#28511,#28512,#28513,#28514,#28515,#28516,#28517,#28518,
#28519,#28520,#28521,#28522,#28523,#28524,#28525,#28526,#28527,#28528,#28529,
#28530,#28531,#28532,#28533,#28534,#28535,#28536,#28537,#28538,#28539,#28540,
#28541,#28542,#28543,#28544,#28545,#28546),.UNSPECIFIED.,.F.,.F.,(4,3,3,
3,3,3,3,3,3,3,3,3,3,3,3,3,3,3,4),(-0.364629307890679,-0.351009649103909,
-0.326038221408134,-0.303066964546125,-0.28084190913311,-0.266670788375262,
-0.255213797252058,-0.218743200019854,-0.200542226689968,-0.18462877353026,
-0.166229720628164,-0.142000108891583,-0.126480131478723,-0.113571829528596,
-0.085178872146449,-0.0628315401147363,-0.0519092898672653,-0.0282641710864551,
-9.4448362746773E-15),.UNSPECIFIED.);
#409=FACE_BOUND('',#1106,.T.);
#410=FACE_BOUND('',#1109,.T.);
#469=CIRCLE('',#6091,0.15555);
#470=CIRCLE('',#6126,0.1954);
#471=CIRCLE('',#6127,0.1954);
#472=CIRCLE('',#6129,0.15555);
#473=CIRCLE('',#6138,0.4);
#474=CIRCLE('',#6140,0.4);
#516=CYLINDRICAL_SURFACE('',#6090,0.15555);
#517=CYLINDRICAL_SURFACE('',#6092,0.15555);
#518=CYLINDRICAL_SURFACE('',#6093,0.15555);
#519=CYLINDRICAL_SURFACE('',#6094,0.15555);
#520=CYLINDRICAL_SURFACE('',#6095,0.15555);
#521=CYLINDRICAL_SURFACE('',#6096,0.15555);
#522=CYLINDRICAL_SURFACE('',#6097,0.15555);
#523=CYLINDRICAL_SURFACE('',#6098,0.15555);
#524=CYLINDRICAL_SURFACE('',#6099,0.15555);
#525=CYLINDRICAL_SURFACE('',#6100,0.15555);
#526=CYLINDRICAL_SURFACE('',#6101,0.15555);
#527=CYLINDRICAL_SURFACE('',#6102,0.15555);
#528=CYLINDRICAL_SURFACE('',#6103,0.15555);
#529=CYLINDRICAL_SURFACE('',#6104,0.15555);
#530=CYLINDRICAL_SURFACE('',#6105,0.15555);
#531=CYLINDRICAL_SURFACE('',#6106,0.15555);
#532=CYLINDRICAL_SURFACE('',#6107,0.15555);
#533=CYLINDRICAL_SURFACE('',#6108,0.15555);
#534=CYLINDRICAL_SURFACE('',#6109,0.15555);
#535=CYLINDRICAL_SURFACE('',#6110,0.15555);
#536=CYLINDRICAL_SURFACE('',#6111,0.15555);
#537=CYLINDRICAL_SURFACE('',#6112,0.15555);
#538=CYLINDRICAL_SURFACE('',#6113,0.15555);
#539=CYLINDRICAL_SURFACE('',#6114,0.15555);
#540=CYLINDRICAL_SURFACE('',#6115,0.15555);
#541=CYLINDRICAL_SURFACE('',#6116,0.15555);
#542=CYLINDRICAL_SURFACE('',#6117,0.15555);
#543=CYLINDRICAL_SURFACE('',#6118,0.15555);
#544=CYLINDRICAL_SURFACE('',#6119,0.15555);
#545=CYLINDRICAL_SURFACE('',#6120,0.15555);
#546=CYLINDRICAL_SURFACE('',#6121,0.15555);
#547=CYLINDRICAL_SURFACE('',#6122,0.15555);
#548=CYLINDRICAL_SURFACE('',#6123,0.15555);
#549=CYLINDRICAL_SURFACE('',#6124,0.15555);
#550=CYLINDRICAL_SURFACE('',#6125,0.1954);
#551=CYLINDRICAL_SURFACE('',#6128,0.15555);
#552=CYLINDRICAL_SURFACE('',#6139,0.4);
#581=SHAPE_REPRESENTATION_RELATIONSHIP('SRR','None',#31645,#596);
#596=ADVANCED_BREP_SHAPE_REPRESENTATION('',(#626),#31560);
#611=STYLED_ITEM('',(#31720),#626);
#626=MANIFOLD_SOLID_BREP('Body1',#5724);
#763=FACE_OUTER_BOUND('',#1060,.T.);
#764=FACE_OUTER_BOUND('',#1061,.T.);
#765=FACE_OUTER_BOUND('',#1062,.T.);
#766=FACE_OUTER_BOUND('',#1063,.T.);
#767=FACE_OUTER_BOUND('',#1064,.T.);
#768=FACE_OUTER_BOUND('',#1065,.T.);
#769=FACE_OUTER_BOUND('',#1066,.T.);
#770=FACE_OUTER_BOUND('',#1067,.T.);
#771=FACE_OUTER_BOUND('',#1068,.T.);
#772=FACE_OUTER_BOUND('',#1069,.T.);
#773=FACE_OUTER_BOUND('',#1070,.T.);
#774=FACE_OUTER_BOUND('',#1071,.T.);
#775=FACE_OUTER_BOUND('',#1072,.T.);
#776=FACE_OUTER_BOUND('',#1073,.T.);
#777=FACE_OUTER_BOUND('',#1074,.T.);
#778=FACE_OUTER_BOUND('',#1075,.T.);
#779=FACE_OUTER_BOUND('',#1076,.T.);
#780=FACE_OUTER_BOUND('',#1077,.T.);
#781=FACE_OUTER_BOUND('',#1078,.T.);
#782=FACE_OUTER_BOUND('',#1079,.T.);
#783=FACE_OUTER_BOUND('',#1080,.T.);
#784=FACE_OUTER_BOUND('',#1081,.T.);
#785=FACE_OUTER_BOUND('',#1082,.T.);
#786=FACE_OUTER_BOUND('',#1083,.T.);
#787=FACE_OUTER_BOUND('',#1084,.T.);
#788=FACE_OUTER_BOUND('',#1085,.T.);
#789=FACE_OUTER_BOUND('',#1086,.T.);
#790=FACE_OUTER_BOUND('',#1087,.T.);
#791=FACE_OUTER_BOUND('',#1088,.T.);
#792=FACE_OUTER_BOUND('',#1089,.T.);
#793=FACE_OUTER_BOUND('',#1090,.T.);
#794=FACE_OUTER_BOUND('',#1091,.T.);
#795=FACE_OUTER_BOUND('',#1092,.T.);
#796=FACE_OUTER_BOUND('',#1093,.T.);
#797=FACE_OUTER_BOUND('',#1094,.T.);
#798=FACE_OUTER_BOUND('',#1095,.T.);
#799=FACE_OUTER_BOUND('',#1096,.T.);
#800=FACE_OUTER_BOUND('',#1097,.T.);
#801=FACE_OUTER_BOUND('',#1098,.T.);
#802=FACE_OUTER_BOUND('',#1099,.T.);
#803=FACE_OUTER_BOUND('',#1100,.T.);
#804=FACE_OUTER_BOUND('',#1101,.T.);
#805=FACE_OUTER_BOUND('',#1102,.T.);
#806=FACE_OUTER_BOUND('',#1103,.T.);
#807=FACE_OUTER_BOUND('',#1104,.T.);
#808=FACE_OUTER_BOUND('',#1105,.T.);
#809=FACE_OUTER_BOUND('',#1107,.T.);
#810=FACE_OUTER_BOUND('',#1108,.T.);
#811=FACE_OUTER_BOUND('',#1110,.T.);
#1060=EDGE_LOOP('',(#4281,#4282,#4283,#4284));
#1061=EDGE_LOOP('',(#4285,#4286,#4287,#4288,#4289));
#1062=EDGE_LOOP('',(#4290,#4291,#4292,#4293,#4294));
#1063=EDGE_LOOP('',(#4295,#4296,#4297,#4298,#4299));
#1064=EDGE_LOOP('',(#4300,#4301,#4302,#4303,#4304));
#1065=EDGE_LOOP('',(#4305,#4306,#4307,#4308,#4309));
#1066=EDGE_LOOP('',(#4310,#4311,#4312,#4313,#4314,#4315));
#1067=EDGE_LOOP('',(#4316,#4317,#4318,#4319,#4320,#4321));
#1068=EDGE_LOOP('',(#4322,#4323,#4324,#4325,#4326));
#1069=EDGE_LOOP('',(#4327,#4328,#4329,#4330,#4331));
#1070=EDGE_LOOP('',(#4332,#4333,#4334,#4335,#4336));
#1071=EDGE_LOOP('',(#4337,#4338,#4339,#4340,#4341));
#1072=EDGE_LOOP('',(#4342,#4343,#4344,#4345,#4346));
#1073=EDGE_LOOP('',(#4347,#4348,#4349,#4350,#4351));
#1074=EDGE_LOOP('',(#4352,#4353,#4354,#4355,#4356));
#1075=EDGE_LOOP('',(#4357,#4358,#4359,#4360,#4361));
#1076=EDGE_LOOP('',(#4362,#4363,#4364,#4365,#4366));
#1077=EDGE_LOOP('',(#4367,#4368,#4369,#4370,#4371));
#1078=EDGE_LOOP('',(#4372,#4373,#4374,#4375,#4376,#4377));
#1079=EDGE_LOOP('',(#4378,#4379,#4380,#4381,#4382,#4383));
#1080=EDGE_LOOP('',(#4384,#4385,#4386,#4387,#4388));
#1081=EDGE_LOOP('',(#4389,#4390,#4391,#4392,#4393));
#1082=EDGE_LOOP('',(#4394,#4395,#4396,#4397,#4398));
#1083=EDGE_LOOP('',(#4399,#4400,#4401,#4402,#4403));
#1084=EDGE_LOOP('',(#4404,#4405,#4406,#4407,#4408));
#1085=EDGE_LOOP('',(#4409,#4410,#4411,#4412,#4413));
#1086=EDGE_LOOP('',(#4414,#4415,#4416,#4417,#4418));
#1087=EDGE_LOOP('',(#4419,#4420,#4421,#4422,#4423));
#1088=EDGE_LOOP('',(#4424,#4425,#4426,#4427,#4428,#4429));
#1089=EDGE_LOOP('',(#4430,#4431,#4432,#4433));
#1090=EDGE_LOOP('',(#4434,#4435,#4436,#4437,#4438,#4439));
#1091=EDGE_LOOP('',(#4440,#4441,#4442,#4443,#4444));
#1092=EDGE_LOOP('',(#4445,#4446,#4447,#4448,#4449,#4450));
#1093=EDGE_LOOP('',(#4451,#4452,#4453,#4454,#4455));
#1094=EDGE_LOOP('',(#4456,#4457,#4458,#4459,#4460,#4461,#4462,#4463,#4464,
#4465,#4466,#4467,#4468,#4469,#4470,#4471,#4472,#4473,#4474,#4475,#4476,
#4477,#4478,#4479,#4480,#4481,#4482,#4483,#4484,#4485,#4486,#4487,#4488,
#4489,#4490,#4491,#4492,#4493,#4494,#4495,#4496,#4497,#4498,#4499,#4500,
#4501,#4502,#4503,#4504,#4505,#4506,#4507,#4508,#4509,#4510,#4511,#4512,
#4513,#4514,#4515,#4516,#4517,#4518,#4519,#4520,#4521,#4522,#4523,#4524,
#4525,#4526,#4527,#4528));
#1095=EDGE_LOOP('',(#4529,#4530,#4531,#4532,#4533));
#1096=EDGE_LOOP('',(#4534,#4535,#4536,#4537,#4538,#4539,#4540,#4541,#4542,
#4543,#4544,#4545,#4546,#4547,#4548,#4549,#4550,#4551,#4552,#4553,#4554,
#4555,#4556,#4557,#4558,#4559,#4560,#4561,#4562,#4563,#4564,#4565,#4566,
#4567,#4568,#4569,#4570,#4571,#4572,#4573,#4574,#4575,#4576,#4577,#4578,
#4579,#4580,#4581,#4582,#4583,#4584,#4585,#4586,#4587,#4588,#4589,#4590,
#4591,#4592,#4593,#4594,#4595,#4596,#4597,#4598,#4599,#4600,#4601,#4602,
#4603,#4604,#4605,#4606,#4607,#4608,#4609,#4610,#4611,#4612,#4613,#4614,
#4615,#4616,#4617,#4618,#4619,#4620,#4621,#4622,#4623,#4624,#4625,#4626,
#4627));
#1097=EDGE_LOOP('',(#4628,#4629,#4630,#4631,#4632,#4633,#4634,#4635,#4636,
#4637,#4638,#4639,#4640,#4641,#4642,#4643,#4644,#4645,#4646,#4647,#4648,
#4649,#4650,#4651,#4652,#4653,#4654,#4655,#4656,#4657,#4658,#4659,#4660,
#4661,#4662,#4663,#4664,#4665,#4666,#4667,#4668,#4669,#4670,#4671,#4672,
#4673,#4674,#4675,#4676,#4677,#4678,#4679,#4680,#4681,#4682,#4683,#4684,
#4685,#4686,#4687,#4688,#4689,#4690,#4691,#4692,#4693,#4694,#4695,#4696,
#4697,#4698,#4699,#4700,#4701,#4702,#4703,#4704,#4705,#4706,#4707,#4708,
#4709,#4710,#4711,#4712,#4713,#4714,#4715,#4716,#4717,#4718,#4719,#4720));
#1098=EDGE_LOOP('',(#4721,#4722,#4723,#4724));
#1099=EDGE_LOOP('',(#4725,#4726,#4727,#4728));
#1100=EDGE_LOOP('',(#4729,#4730,#4731,#4732));
#1101=EDGE_LOOP('',(#4733,#4734,#4735,#4736));
#1102=EDGE_LOOP('',(#4737,#4738,#4739,#4740));
#1103=EDGE_LOOP('',(#4741,#4742,#4743,#4744));
#1104=EDGE_LOOP('',(#4745,#4746,#4747,#4748,#4749,#4750));
#1105=EDGE_LOOP('',(#4751));
#1106=EDGE_LOOP('',(#4752,#4753,#4754,#4755,#4756));
#1107=EDGE_LOOP('',(#4757,#4758,#4759,#4760));
#1108=EDGE_LOOP('',(#4761));
#1109=EDGE_LOOP('',(#4762,#4763,#4764,#4765,#4766,#4767));
#1110=EDGE_LOOP('',(#4768,#4769,#4770,#4771,#4772));
#1481=LINE('',#8251,#1988);
#1482=LINE('',#8484,#1989);
#1483=LINE('',#8929,#1990);
#1484=LINE('',#9416,#1991);
#1485=LINE('',#9903,#1992);
#1486=LINE('',#10404,#1993);
#1487=LINE('',#10757,#1994);
#1488=LINE('',#10881,#1995);
#1489=LINE('',#11182,#1996);
#1490=LINE('',#11611,#1997);
#1491=LINE('',#12114,#1998);
#1492=LINE('',#12613,#1999);
#1493=LINE('',#13152,#2000);
#1494=LINE('',#13803,#2001);
#1495=LINE('',#14304,#2002);
#1496=LINE('',#14805,#2003);
#1497=LINE('',#15288,#2004);
#1498=LINE('',#15783,#2005);
#1499=LINE('',#16140,#2006);
#1500=LINE('',#16267,#2007);
#1501=LINE('',#16562,#2008);
#1502=LINE('',#17007,#2009);
#1503=LINE('',#17534,#2010);
#1504=LINE('',#18099,#2011);
#1505=LINE('',#18604,#2012);
#1506=LINE('',#19073,#2013);
#1507=LINE('',#19538,#2014);
#1508=LINE('',#20029,#2015);
#1509=LINE('',#20351,#2016);
#1510=LINE('',#20827,#2017);
#1511=LINE('',#21285,#2018);
#1512=LINE('',#21586,#2019);
#1513=LINE('',#21934,#2020);
#1514=LINE('',#22286,#2021);
#1515=LINE('',#28550,#2022);
#1516=LINE('',#28552,#2023);
#1517=LINE('',#28554,#2024);
#1518=LINE('',#28555,#2025);
#1519=LINE('',#28558,#2026);
#1520=LINE('',#28560,#2027);
#1521=LINE('',#28561,#2028);
#1522=LINE('',#28564,#2029);
#1523=LINE('',#28566,#2030);
#1524=LINE('',#28567,#2031);
#1525=LINE('',#28570,#2032);
#1526=LINE('',#28572,#2033);
#1527=LINE('',#28573,#2034);
#1528=LINE('',#28576,#2035);
#1529=LINE('',#28578,#2036);
#1530=LINE('',#28579,#2037);
#1531=LINE('',#28581,#2038);
#1532=LINE('',#28582,#2039);
#1533=LINE('',#28589,#2040);
#1988=VECTOR('',#6947,0.15555);
#1989=VECTOR('',#6952,0.15555);
#1990=VECTOR('',#6955,0.15555);
#1991=VECTOR('',#6958,0.15555);
#1992=VECTOR('',#6961,0.15555);
#1993=VECTOR('',#6964,0.15555);
#1994=VECTOR('',#6967,0.15555);
#1995=VECTOR('',#6970,0.15555);
#1996=VECTOR('',#6973,0.15555);
#1997=VECTOR('',#6976,0.15555);
#1998=VECTOR('',#6979,0.15555);
#1999=VECTOR('',#6982,0.15555);
#2000=VECTOR('',#6985,0.15555);
#2001=VECTOR('',#6988,0.15555);
#2002=VECTOR('',#6991,0.15555);
#2003=VECTOR('',#6994,0.15555);
#2004=VECTOR('',#6997,0.15555);
#2005=VECTOR('',#7000,0.15555);
#2006=VECTOR('',#7003,0.15555);
#2007=VECTOR('',#7006,0.15555);
#2008=VECTOR('',#7009,0.15555);
#2009=VECTOR('',#7012,0.15555);
#2010=VECTOR('',#7015,0.15555);
#2011=VECTOR('',#7018,0.15555);
#2012=VECTOR('',#7021,0.15555);
#2013=VECTOR('',#7024,0.15555);
#2014=VECTOR('',#7027,0.15555);
#2015=VECTOR('',#7030,0.15555);
#2016=VECTOR('',#7033,0.15555);
#2017=VECTOR('',#7036,0.15555);
#2018=VECTOR('',#7039,0.15555);
#2019=VECTOR('',#7042,0.15555);
#2020=VECTOR('',#7045,0.15555);
#2021=VECTOR('',#7048,0.15555);
#2022=VECTOR('',#7061,1.);
#2023=VECTOR('',#7062,1.);
#2024=VECTOR('',#7063,1.);
#2025=VECTOR('',#7064,1.);
#2026=VECTOR('',#7067,1.);
#2027=VECTOR('',#7068,1.);
#2028=VECTOR('',#7069,1.);
#2029=VECTOR('',#7072,1.);
#2030=VECTOR('',#7073,1.);
#2031=VECTOR('',#7074,1.);
#2032=VECTOR('',#7077,1.);
#2033=VECTOR('',#7078,1.);
#2034=VECTOR('',#7079,1.);
#2035=VECTOR('',#7082,1.);
#2036=VECTOR('',#7083,1.);
#2037=VECTOR('',#7084,1.);
#2038=VECTOR('',#7087,1.);
#2039=VECTOR('',#7088,1.);
#2040=VECTOR('',#7097,0.4);
#2438=VERTEX_POINT('',#8249);
#2439=VERTEX_POINT('',#8250);
#2440=VERTEX_POINT('',#8252);
#2441=VERTEX_POINT('',#8433);
#2442=VERTEX_POINT('',#8482);
#2443=VERTEX_POINT('',#8483);
#2444=VERTEX_POINT('',#8713);
#2445=VERTEX_POINT('',#8927);
#2446=VERTEX_POINT('',#8928);
#2447=VERTEX_POINT('',#8930);
#2448=VERTEX_POINT('',#9414);
#2449=VERTEX_POINT('',#9415);
#2450=VERTEX_POINT('',#9663);
#2451=VERTEX_POINT('',#9901);
#2452=VERTEX_POINT('',#9902);
#2453=VERTEX_POINT('',#9904);
#2454=VERTEX_POINT('',#10402);
#2455=VERTEX_POINT('',#10403);
#2456=VERTEX_POINT('',#10631);
#2457=VERTEX_POINT('',#10755);
#2458=VERTEX_POINT('',#10756);
#2459=VERTEX_POINT('',#10758);
#2460=VERTEX_POINT('',#10849);
#2461=VERTEX_POINT('',#10879);
#2462=VERTEX_POINT('',#10880);
#2463=VERTEX_POINT('',#10882);
#2464=VERTEX_POINT('',#10967);
#2465=VERTEX_POINT('',#11180);
#2466=VERTEX_POINT('',#11181);
#2467=VERTEX_POINT('',#11183);
#2468=VERTEX_POINT('',#11609);
#2469=VERTEX_POINT('',#11610);
#2470=VERTEX_POINT('',#11838);
#2471=VERTEX_POINT('',#12112);
#2472=VERTEX_POINT('',#12113);
#2473=VERTEX_POINT('',#12115);
#2474=VERTEX_POINT('',#12611);
#2475=VERTEX_POINT('',#12612);
#2476=VERTEX_POINT('',#12854);
#2477=VERTEX_POINT('',#13150);
#2478=VERTEX_POINT('',#13151);
#2479=VERTEX_POINT('',#13153);
#2480=VERTEX_POINT('',#13801);
#2481=VERTEX_POINT('',#13802);
#2482=VERTEX_POINT('',#14050);
#2483=VERTEX_POINT('',#14302);
#2484=VERTEX_POINT('',#14303);
#2485=VERTEX_POINT('',#14305);
#2486=VERTEX_POINT('',#14803);
#2487=VERTEX_POINT('',#14804);
#2488=VERTEX_POINT('',#15048);
#2489=VERTEX_POINT('',#15286);
#2490=VERTEX_POINT('',#15287);
#2491=VERTEX_POINT('',#15289);
#2492=VERTEX_POINT('',#15781);
#2493=VERTEX_POINT('',#15782);
#2494=VERTEX_POINT('',#16012);
#2495=VERTEX_POINT('',#16138);
#2496=VERTEX_POINT('',#16139);
#2497=VERTEX_POINT('',#16141);
#2498=VERTEX_POINT('',#16235);
#2499=VERTEX_POINT('',#16265);
#2500=VERTEX_POINT('',#16266);
#2501=VERTEX_POINT('',#16268);
#2502=VERTEX_POINT('',#16353);
#2503=VERTEX_POINT('',#16560);
#2504=VERTEX_POINT('',#16561);
#2505=VERTEX_POINT('',#16563);
#2506=VERTEX_POINT('',#17005);
#2507=VERTEX_POINT('',#17006);
#2508=VERTEX_POINT('',#17264);
#2509=VERTEX_POINT('',#17532);
#2510=VERTEX_POINT('',#17533);
#2511=VERTEX_POINT('',#17535);
#2512=VERTEX_POINT('',#18097);
#2513=VERTEX_POINT('',#18098);
#2514=VERTEX_POINT('',#18342);
#2515=VERTEX_POINT('',#18602);
#2516=VERTEX_POINT('',#18603);
#2517=VERTEX_POINT('',#18605);
#2518=VERTEX_POINT('',#19071);
#2519=VERTEX_POINT('',#19072);
#2520=VERTEX_POINT('',#19308);
#2521=VERTEX_POINT('',#19536);
#2522=VERTEX_POINT('',#19537);
#2523=VERTEX_POINT('',#19539);
#2524=VERTEX_POINT('',#20027);
#2525=VERTEX_POINT('',#20028);
#2526=VERTEX_POINT('',#20298);
#2527=VERTEX_POINT('',#20349);
#2528=VERTEX_POINT('',#20350);
#2529=VERTEX_POINT('',#20352);
#2530=VERTEX_POINT('',#20631);
#2531=VERTEX_POINT('',#20825);
#2532=VERTEX_POINT('',#20826);
#2533=VERTEX_POINT('',#21283);
#2534=VERTEX_POINT('',#21284);
#2535=VERTEX_POINT('',#21286);
#2536=VERTEX_POINT('',#21354);
#2537=VERTEX_POINT('',#21584);
#2538=VERTEX_POINT('',#21585);
#2539=VERTEX_POINT('',#21587);
#2540=VERTEX_POINT('',#21932);
#2541=VERTEX_POINT('',#21933);
#2542=VERTEX_POINT('',#21935);
#2543=VERTEX_POINT('',#22140);
#2544=VERTEX_POINT('',#22284);
#2545=VERTEX_POINT('',#22285);
#2546=VERTEX_POINT('',#22521);
#2547=VERTEX_POINT('',#22779);
#2548=VERTEX_POINT('',#22780);
#2549=VERTEX_POINT('',#22818);
#2550=VERTEX_POINT('',#22820);
#2551=VERTEX_POINT('',#22843);
#2552=VERTEX_POINT('',#22956);
#2553=VERTEX_POINT('',#22967);
#2554=VERTEX_POINT('',#22979);
#2555=VERTEX_POINT('',#23095);
#2556=VERTEX_POINT('',#23106);
#2557=VERTEX_POINT('',#23117);
#2558=VERTEX_POINT('',#23233);
#2559=VERTEX_POINT('',#23244);
#2560=VERTEX_POINT('',#23255);
#2561=VERTEX_POINT('',#23371);
#2562=VERTEX_POINT('',#23382);
#2563=VERTEX_POINT('',#23393);
#2564=VERTEX_POINT('',#23509);
#2565=VERTEX_POINT('',#23522);
#2566=VERTEX_POINT('',#23533);
#2567=VERTEX_POINT('',#23646);
#2568=VERTEX_POINT('',#23658);
#2569=VERTEX_POINT('',#23669);
#2570=VERTEX_POINT('',#23785);
#2571=VERTEX_POINT('',#23797);
#2572=VERTEX_POINT('',#23808);
#2573=VERTEX_POINT('',#23924);
#2574=VERTEX_POINT('',#23935);
#2575=VERTEX_POINT('',#23948);
#2576=VERTEX_POINT('',#24061);
#2577=VERTEX_POINT('',#24072);
#2578=VERTEX_POINT('',#24084);
#2579=VERTEX_POINT('',#24200);
#2580=VERTEX_POINT('',#24211);
#2581=VERTEX_POINT('',#24223);
#2582=VERTEX_POINT('',#24336);
#2583=VERTEX_POINT('',#24347);
#2584=VERTEX_POINT('',#24460);
#2585=VERTEX_POINT('',#24472);
#2586=VERTEX_POINT('',#24486);
#2587=VERTEX_POINT('',#24488);
#2588=VERTEX_POINT('',#24499);
#2589=VERTEX_POINT('',#24612);
#2590=VERTEX_POINT('',#24728);
#2591=VERTEX_POINT('',#24739);
#2592=VERTEX_POINT('',#24858);
#2593=VERTEX_POINT('',#24869);
#2594=VERTEX_POINT('',#24880);
#2595=VERTEX_POINT('',#24996);
#2596=VERTEX_POINT('',#25007);
#2597=VERTEX_POINT('',#25018);
#2598=VERTEX_POINT('',#25134);
#2599=VERTEX_POINT('',#25145);
#2600=VERTEX_POINT('',#25156);
#2601=VERTEX_POINT('',#25269);
#2602=VERTEX_POINT('',#25281);
#2603=VERTEX_POINT('',#25292);
#2604=VERTEX_POINT('',#25408);
#2605=VERTEX_POINT('',#25420);
#2606=VERTEX_POINT('',#25431);
#2607=VERTEX_POINT('',#25544);
#2608=VERTEX_POINT('',#25556);
#2609=VERTEX_POINT('',#25567);
#2610=VERTEX_POINT('',#25683);
#2611=VERTEX_POINT('',#25694);
#2612=VERTEX_POINT('',#25706);
#2613=VERTEX_POINT('',#25822);
#2614=VERTEX_POINT('',#25833);
#2615=VERTEX_POINT('',#25845);
#2616=VERTEX_POINT('',#25958);
#2617=VERTEX_POINT('',#25969);
#2618=VERTEX_POINT('',#26085);
#2619=VERTEX_POINT('',#26201);
#2620=VERTEX_POINT('',#26223);
#2621=VERTEX_POINT('',#26462);
#2622=VERTEX_POINT('',#26464);
#2623=VERTEX_POINT('',#27491);
#2624=VERTEX_POINT('',#28432);
#2625=VERTEX_POINT('',#28548);
#2626=VERTEX_POINT('',#28549);
#2627=VERTEX_POINT('',#28551);
#2628=VERTEX_POINT('',#28553);
#2629=VERTEX_POINT('',#28557);
#2630=VERTEX_POINT('',#28559);
#2631=VERTEX_POINT('',#28563);
#2632=VERTEX_POINT('',#28565);
#2633=VERTEX_POINT('',#28569);
#2634=VERTEX_POINT('',#28571);
#2635=VERTEX_POINT('',#28575);
#2636=VERTEX_POINT('',#28577);
#2637=VERTEX_POINT('',#28585);
#2638=VERTEX_POINT('',#28588);
#3136=EDGE_CURVE('',#2438,#2439,#1481,.T.);
#3137=EDGE_CURVE('',#2440,#2438,#143,.F.);
#3138=EDGE_CURVE('',#2441,#2440,#469,.T.);
#3139=EDGE_CURVE('',#2441,#2439,#144,.T.);
#3140=EDGE_CURVE('',#2442,#2443,#1482,.T.);
#3141=EDGE_CURVE('',#2438,#2442,#145,.F.);
#3142=EDGE_CURVE('',#2439,#2444,#146,.T.);
#3143=EDGE_CURVE('',#2444,#2443,#147,.T.);
#3144=EDGE_CURVE('',#2445,#2446,#1483,.T.);
#3145=EDGE_CURVE('',#2447,#2445,#148,.F.);
#3146=EDGE_CURVE('',#2442,#2447,#149,.F.);
#3147=EDGE_CURVE('',#2443,#2446,#150,.T.);
#3148=EDGE_CURVE('',#2448,#2449,#1484,.T.);
#3149=EDGE_CURVE('',#2445,#2448,#151,.F.);
#3150=EDGE_CURVE('',#2446,#2450,#152,.T.);
#3151=EDGE_CURVE('',#2450,#2449,#153,.T.);
#3152=EDGE_CURVE('',#2451,#2452,#1485,.T.);
#3153=EDGE_CURVE('',#2453,#2451,#154,.F.);
#3154=EDGE_CURVE('',#2448,#2453,#155,.F.);
#3155=EDGE_CURVE('',#2449,#2452,#156,.T.);
#3156=EDGE_CURVE('',#2454,#2455,#1486,.T.);
#3157=EDGE_CURVE('',#2451,#2454,#157,.F.);
#3158=EDGE_CURVE('',#2452,#2456,#158,.T.);
#3159=EDGE_CURVE('',#2456,#2455,#159,.T.);
#3160=EDGE_CURVE('',#2457,#2458,#1487,.T.);
#3161=EDGE_CURVE('',#2459,#2457,#160,.T.);
#3162=EDGE_CURVE('',#2454,#2459,#161,.F.);
#3163=EDGE_CURVE('',#2455,#2460,#162,.T.);
#3164=EDGE_CURVE('',#2460,#2458,#163,.T.);
#3165=EDGE_CURVE('',#2461,#2462,#1488,.T.);
#3166=EDGE_CURVE('',#2463,#2461,#164,.T.);
#3167=EDGE_CURVE('',#2457,#2463,#165,.T.);
#3168=EDGE_CURVE('',#2458,#2464,#166,.T.);
#3169=EDGE_CURVE('',#2464,#2462,#167,.T.);
#3170=EDGE_CURVE('',#2465,#2466,#1489,.T.);
#3171=EDGE_CURVE('',#2467,#2465,#168,.F.);
#3172=EDGE_CURVE('',#2461,#2467,#169,.T.);
#3173=EDGE_CURVE('',#2462,#2466,#170,.T.);
#3174=EDGE_CURVE('',#2468,#2469,#1490,.T.);
#3175=EDGE_CURVE('',#2465,#2468,#171,.F.);
#3176=EDGE_CURVE('',#2466,#2470,#172,.T.);
#3177=EDGE_CURVE('',#2470,#2469,#173,.T.);
#3178=EDGE_CURVE('',#2471,#2472,#1491,.T.);
#3179=EDGE_CURVE('',#2473,#2471,#174,.F.);
#3180=EDGE_CURVE('',#2468,#2473,#175,.F.);
#3181=EDGE_CURVE('',#2469,#2472,#176,.T.);
#3182=EDGE_CURVE('',#2474,#2475,#1492,.T.);
#3183=EDGE_CURVE('',#2471,#2474,#177,.F.);
#3184=EDGE_CURVE('',#2472,#2476,#178,.T.);
#3185=EDGE_CURVE('',#2476,#2475,#179,.T.);
#3186=EDGE_CURVE('',#2477,#2478,#1493,.T.);
#3187=EDGE_CURVE('',#2479,#2477,#180,.F.);
#3188=EDGE_CURVE('',#2474,#2479,#181,.F.);
#3189=EDGE_CURVE('',#2475,#2478,#182,.T.);
#3190=EDGE_CURVE('',#2480,#2481,#1494,.T.);
#3191=EDGE_CURVE('',#2477,#2480,#183,.F.);
#3192=EDGE_CURVE('',#2478,#2482,#184,.T.);
#3193=EDGE_CURVE('',#2482,#2481,#185,.T.);
#3194=EDGE_CURVE('',#2483,#2484,#1495,.T.);
#3195=EDGE_CURVE('',#2485,#2483,#186,.F.);
#3196=EDGE_CURVE('',#2480,#2485,#187,.F.);
#3197=EDGE_CURVE('',#2481,#2484,#188,.T.);
#3198=EDGE_CURVE('',#2486,#2487,#1496,.T.);
#3199=EDGE_CURVE('',#2483,#2486,#189,.F.);
#3200=EDGE_CURVE('',#2484,#2488,#190,.T.);
#3201=EDGE_CURVE('',#2488,#2487,#191,.T.);
#3202=EDGE_CURVE('',#2489,#2490,#1497,.T.);
#3203=EDGE_CURVE('',#2491,#2489,#192,.F.);
#3204=EDGE_CURVE('',#2486,#2491,#193,.F.);
#3205=EDGE_CURVE('',#2487,#2490,#194,.T.);
#3206=EDGE_CURVE('',#2492,#2493,#1498,.T.);
#3207=EDGE_CURVE('',#2489,#2492,#195,.F.);
#3208=EDGE_CURVE('',#2490,#2494,#196,.T.);
#3209=EDGE_CURVE('',#2494,#2493,#197,.T.);
#3210=EDGE_CURVE('',#2495,#2496,#1499,.T.);
#3211=EDGE_CURVE('',#2497,#2495,#198,.T.);
#3212=EDGE_CURVE('',#2492,#2497,#199,.F.);
#3213=EDGE_CURVE('',#2493,#2498,#200,.T.);
#3214=EDGE_CURVE('',#2498,#2496,#201,.T.);
#3215=EDGE_CURVE('',#2499,#2500,#1500,.T.);
#3216=EDGE_CURVE('',#2501,#2499,#202,.T.);
#3217=EDGE_CURVE('',#2495,#2501,#203,.T.);
#3218=EDGE_CURVE('',#2496,#2502,#204,.T.);
#3219=EDGE_CURVE('',#2502,#2500,#205,.T.);
#3220=EDGE_CURVE('',#2503,#2504,#1501,.T.);
#3221=EDGE_CURVE('',#2505,#2503,#206,.F.);
#3222=EDGE_CURVE('',#2499,#2505,#207,.T.);
#3223=EDGE_CURVE('',#2500,#2504,#208,.T.);
#3224=EDGE_CURVE('',#2506,#2507,#1502,.T.);
#3225=EDGE_CURVE('',#2503,#2506,#209,.F.);
#3226=EDGE_CURVE('',#2504,#2508,#210,.T.);
#3227=EDGE_CURVE('',#2508,#2507,#211,.T.);
#3228=EDGE_CURVE('',#2509,#2510,#1503,.T.);
#3229=EDGE_CURVE('',#2511,#2509,#212,.F.);
#3230=EDGE_CURVE('',#2506,#2511,#213,.F.);
#3231=EDGE_CURVE('',#2507,#2510,#214,.T.);
#3232=EDGE_CURVE('',#2512,#2513,#1504,.T.);
#3233=EDGE_CURVE('',#2509,#2512,#215,.F.);
#3234=EDGE_CURVE('',#2510,#2514,#216,.T.);
#3235=EDGE_CURVE('',#2514,#2513,#217,.T.);
#3236=EDGE_CURVE('',#2515,#2516,#1505,.T.);
#3237=EDGE_CURVE('',#2517,#2515,#218,.F.);
#3238=EDGE_CURVE('',#2512,#2517,#219,.F.);
#3239=EDGE_CURVE('',#2513,#2516,#220,.T.);
#3240=EDGE_CURVE('',#2518,#2519,#1506,.T.);
#3241=EDGE_CURVE('',#2515,#2518,#221,.F.);
#3242=EDGE_CURVE('',#2516,#2520,#222,.T.);
#3243=EDGE_CURVE('',#2520,#2519,#223,.T.);
#3244=EDGE_CURVE('',#2521,#2522,#1507,.T.);
#3245=EDGE_CURVE('',#2523,#2521,#224,.F.);
#3246=EDGE_CURVE('',#2518,#2523,#225,.F.);
#3247=EDGE_CURVE('',#2519,#2522,#226,.T.);
#3248=EDGE_CURVE('',#2524,#2525,#1508,.T.);
#3249=EDGE_CURVE('',#2521,#2524,#227,.F.);
#3250=EDGE_CURVE('',#2522,#2526,#228,.T.);
#3251=EDGE_CURVE('',#2526,#2525,#229,.T.);
#3252=EDGE_CURVE('',#2527,#2528,#1509,.T.);
#3253=EDGE_CURVE('',#2529,#2527,#230,.F.);
#3254=EDGE_CURVE('',#2524,#2529,#231,.F.);
#3255=EDGE_CURVE('',#2525,#2530,#232,.T.);
#3256=EDGE_CURVE('',#2530,#2528,#233,.T.);
#3257=EDGE_CURVE('',#2531,#2532,#1510,.T.);
#3258=EDGE_CURVE('',#2527,#2531,#234,.F.);
#3259=EDGE_CURVE('',#2528,#2532,#235,.T.);
#3260=EDGE_CURVE('',#2533,#2534,#1511,.T.);
#3261=EDGE_CURVE('',#2535,#2533,#236,.T.);
#3262=EDGE_CURVE('',#2531,#2535,#237,.F.);
#3263=EDGE_CURVE('',#2532,#2536,#238,.T.);
#3264=EDGE_CURVE('',#2536,#2534,#239,.T.);
#3265=EDGE_CURVE('',#2537,#2538,#1512,.T.);
#3266=EDGE_CURVE('',#2539,#2537,#240,.T.);
#3267=EDGE_CURVE('',#2533,#2539,#241,.T.);
#3268=EDGE_CURVE('',#2534,#2538,#242,.T.);
#3269=EDGE_CURVE('',#2540,#2541,#1513,.T.);
#3270=EDGE_CURVE('',#2542,#2540,#243,.F.);
#3271=EDGE_CURVE('',#2537,#2542,#244,.T.);
#3272=EDGE_CURVE('',#2538,#2543,#245,.T.);
#3273=EDGE_CURVE('',#2543,#2541,#246,.T.);
#3274=EDGE_CURVE('',#2544,#2545,#1514,.T.);
#3275=EDGE_CURVE('',#2540,#2544,#247,.F.);
#3276=EDGE_CURVE('',#2541,#2546,#248,.T.);
#3277=EDGE_CURVE('',#2546,#2545,#249,.F.);
#3278=EDGE_CURVE('',#2547,#2548,#250,.T.);
#3279=EDGE_CURVE('',#2548,#2549,#470,.F.);
#3280=EDGE_CURVE('',#2549,#2550,#251,.T.);
#3281=EDGE_CURVE('',#2550,#2551,#252,.T.);
#3282=EDGE_CURVE('',#2551,#2552,#253,.T.);
#3283=EDGE_CURVE('',#2552,#2553,#254,.T.);
#3284=EDGE_CURVE('',#2553,#2554,#255,.T.);
#3285=EDGE_CURVE('',#2554,#2555,#256,.T.);
#3286=EDGE_CURVE('',#2555,#2556,#257,.T.);
#3287=EDGE_CURVE('',#2556,#2557,#258,.T.);
#3288=EDGE_CURVE('',#2557,#2558,#259,.T.);
#3289=EDGE_CURVE('',#2558,#2559,#260,.T.);
#3290=EDGE_CURVE('',#2559,#2560,#261,.T.);
#3291=EDGE_CURVE('',#2560,#2561,#262,.T.);
#3292=EDGE_CURVE('',#2561,#2562,#263,.T.);
#3293=EDGE_CURVE('',#2562,#2563,#264,.T.);
#3294=EDGE_CURVE('',#2563,#2564,#265,.T.);
#3295=EDGE_CURVE('',#2564,#2565,#266,.T.);
#3296=EDGE_CURVE('',#2565,#2566,#267,.T.);
#3297=EDGE_CURVE('',#2566,#2567,#268,.T.);
#3298=EDGE_CURVE('',#2567,#2568,#269,.T.);
#3299=EDGE_CURVE('',#2568,#2569,#270,.T.);
#3300=EDGE_CURVE('',#2569,#2570,#271,.T.);
#3301=EDGE_CURVE('',#2570,#2571,#272,.T.);
#3302=EDGE_CURVE('',#2571,#2572,#273,.T.);
#3303=EDGE_CURVE('',#2572,#2573,#274,.T.);
#3304=EDGE_CURVE('',#2573,#2574,#275,.T.);
#3305=EDGE_CURVE('',#2574,#2575,#276,.T.);
#3306=EDGE_CURVE('',#2575,#2576,#277,.T.);
#3307=EDGE_CURVE('',#2576,#2577,#278,.T.);
#3308=EDGE_CURVE('',#2577,#2578,#279,.T.);
#3309=EDGE_CURVE('',#2578,#2579,#280,.T.);
#3310=EDGE_CURVE('',#2579,#2580,#281,.T.);
#3311=EDGE_CURVE('',#2580,#2581,#282,.T.);
#3312=EDGE_CURVE('',#2581,#2582,#283,.T.);
#3313=EDGE_CURVE('',#2582,#2583,#284,.T.);
#3314=EDGE_CURVE('',#2583,#2584,#285,.T.);
#3315=EDGE_CURVE('',#2584,#2585,#286,.T.);
#3316=EDGE_CURVE('',#2586,#2585,#471,.F.);
#3317=EDGE_CURVE('',#2586,#2587,#287,.T.);
#3318=EDGE_CURVE('',#2587,#2588,#288,.T.);
#3319=EDGE_CURVE('',#2588,#2589,#289,.T.);
#3320=EDGE_CURVE('',#2589,#2590,#290,.T.);
#3321=EDGE_CURVE('',#2590,#2591,#291,.T.);
#3322=EDGE_CURVE('',#2591,#2592,#292,.T.);
#3323=EDGE_CURVE('',#2592,#2593,#293,.T.);
#3324=EDGE_CURVE('',#2593,#2594,#294,.T.);
#3325=EDGE_CURVE('',#2594,#2595,#295,.T.);
#3326=EDGE_CURVE('',#2595,#2596,#296,.T.);
#3327=EDGE_CURVE('',#2596,#2597,#297,.T.);
#3328=EDGE_CURVE('',#2597,#2598,#298,.T.);
#3329=EDGE_CURVE('',#2598,#2599,#299,.T.);
#3330=EDGE_CURVE('',#2599,#2600,#300,.T.);
#3331=EDGE_CURVE('',#2600,#2601,#301,.T.);
#3332=EDGE_CURVE('',#2601,#2602,#302,.T.);
#3333=EDGE_CURVE('',#2602,#2603,#303,.T.);
#3334=EDGE_CURVE('',#2603,#2604,#304,.T.);
#3335=EDGE_CURVE('',#2604,#2605,#305,.T.);
#3336=EDGE_CURVE('',#2605,#2606,#306,.T.);
#3337=EDGE_CURVE('',#2606,#2607,#307,.T.);
#3338=EDGE_CURVE('',#2607,#2608,#308,.T.);
#3339=EDGE_CURVE('',#2608,#2609,#309,.T.);
#3340=EDGE_CURVE('',#2609,#2610,#310,.T.);
#3341=EDGE_CURVE('',#2610,#2611,#311,.T.);
#3342=EDGE_CURVE('',#2611,#2612,#312,.T.);
#3343=EDGE_CURVE('',#2612,#2613,#313,.T.);
#3344=EDGE_CURVE('',#2613,#2614,#314,.T.);
#3345=EDGE_CURVE('',#2614,#2615,#315,.T.);
#3346=EDGE_CURVE('',#2615,#2616,#316,.T.);
#3347=EDGE_CURVE('',#2616,#2617,#317,.T.);
#3348=EDGE_CURVE('',#2617,#2618,#318,.T.);
#3349=EDGE_CURVE('',#2618,#2619,#319,.T.);
#3350=EDGE_CURVE('',#2619,#2547,#320,.T.);
#3351=EDGE_CURVE('',#2545,#2620,#321,.F.);
#3352=EDGE_CURVE('',#2621,#2620,#472,.T.);
#3353=EDGE_CURVE('',#2622,#2621,#322,.T.);
#3354=EDGE_CURVE('',#2544,#2622,#323,.F.);
#3355=EDGE_CURVE('',#2585,#2621,#324,.T.);
#3356=EDGE_CURVE('',#2623,#2549,#325,.T.);
#3357=EDGE_CURVE('',#2623,#2440,#326,.T.);
#3358=EDGE_CURVE('',#2624,#2586,#327,.T.);
#3359=EDGE_CURVE('',#2620,#2624,#328,.T.);
#3360=EDGE_CURVE('',#2548,#2441,#329,.T.);
#3361=EDGE_CURVE('',#2625,#2626,#1515,.T.);
#3362=EDGE_CURVE('',#2625,#2627,#1516,.T.);
#3363=EDGE_CURVE('',#2627,#2628,#1517,.T.);
#3364=EDGE_CURVE('',#2626,#2628,#1518,.T.);
#3365=EDGE_CURVE('',#2629,#2625,#1519,.T.);
#3366=EDGE_CURVE('',#2629,#2630,#1520,.T.);
#3367=EDGE_CURVE('',#2630,#2627,#1521,.T.);
#3368=EDGE_CURVE('',#2631,#2629,#1522,.T.);
#3369=EDGE_CURVE('',#2631,#2632,#1523,.T.);
#3370=EDGE_CURVE('',#2632,#2630,#1524,.T.);
#3371=EDGE_CURVE('',#2633,#2631,#1525,.T.);
#3372=EDGE_CURVE('',#2633,#2634,#1526,.T.);
#3373=EDGE_CURVE('',#2634,#2632,#1527,.T.);
#3374=EDGE_CURVE('',#2635,#2633,#1528,.T.);
#3375=EDGE_CURVE('',#2635,#2636,#1529,.T.);
#3376=EDGE_CURVE('',#2636,#2634,#1530,.T.);
#3377=EDGE_CURVE('',#2626,#2635,#1531,.T.);
#3378=EDGE_CURVE('',#2628,#2636,#1532,.T.);
#3379=EDGE_CURVE('',#2637,#2637,#473,.T.);
#3380=EDGE_CURVE('',#2637,#2638,#1533,.T.);
#3381=EDGE_CURVE('',#2638,#2638,#474,.T.);
#4281=ORIENTED_EDGE('',*,*,#3136,.F.);
#4282=ORIENTED_EDGE('',*,*,#3137,.F.);
#4283=ORIENTED_EDGE('',*,*,#3138,.F.);
#4284=ORIENTED_EDGE('',*,*,#3139,.T.);
#4285=ORIENTED_EDGE('',*,*,#3140,.F.);
#4286=ORIENTED_EDGE('',*,*,#3141,.F.);
#4287=ORIENTED_EDGE('',*,*,#3136,.T.);
#4288=ORIENTED_EDGE('',*,*,#3142,.T.);
#4289=ORIENTED_EDGE('',*,*,#3143,.T.);
#4290=ORIENTED_EDGE('',*,*,#3144,.F.);
#4291=ORIENTED_EDGE('',*,*,#3145,.F.);
#4292=ORIENTED_EDGE('',*,*,#3146,.F.);
#4293=ORIENTED_EDGE('',*,*,#3140,.T.);
#4294=ORIENTED_EDGE('',*,*,#3147,.T.);
#4295=ORIENTED_EDGE('',*,*,#3148,.F.);
#4296=ORIENTED_EDGE('',*,*,#3149,.F.);
#4297=ORIENTED_EDGE('',*,*,#3144,.T.);
#4298=ORIENTED_EDGE('',*,*,#3150,.T.);
#4299=ORIENTED_EDGE('',*,*,#3151,.T.);
#4300=ORIENTED_EDGE('',*,*,#3152,.F.);
#4301=ORIENTED_EDGE('',*,*,#3153,.F.);
#4302=ORIENTED_EDGE('',*,*,#3154,.F.);
#4303=ORIENTED_EDGE('',*,*,#3148,.T.);
#4304=ORIENTED_EDGE('',*,*,#3155,.T.);
#4305=ORIENTED_EDGE('',*,*,#3156,.F.);
#4306=ORIENTED_EDGE('',*,*,#3157,.F.);
#4307=ORIENTED_EDGE('',*,*,#3152,.T.);
#4308=ORIENTED_EDGE('',*,*,#3158,.T.);
#4309=ORIENTED_EDGE('',*,*,#3159,.T.);
#4310=ORIENTED_EDGE('',*,*,#3160,.F.);
#4311=ORIENTED_EDGE('',*,*,#3161,.F.);
#4312=ORIENTED_EDGE('',*,*,#3162,.F.);
#4313=ORIENTED_EDGE('',*,*,#3156,.T.);
#4314=ORIENTED_EDGE('',*,*,#3163,.T.);
#4315=ORIENTED_EDGE('',*,*,#3164,.T.);
#4316=ORIENTED_EDGE('',*,*,#3165,.F.);
#4317=ORIENTED_EDGE('',*,*,#3166,.F.);
#4318=ORIENTED_EDGE('',*,*,#3167,.F.);
#4319=ORIENTED_EDGE('',*,*,#3160,.T.);
#4320=ORIENTED_EDGE('',*,*,#3168,.T.);
#4321=ORIENTED_EDGE('',*,*,#3169,.T.);
#4322=ORIENTED_EDGE('',*,*,#3170,.F.);
#4323=ORIENTED_EDGE('',*,*,#3171,.F.);
#4324=ORIENTED_EDGE('',*,*,#3172,.F.);
#4325=ORIENTED_EDGE('',*,*,#3165,.T.);
#4326=ORIENTED_EDGE('',*,*,#3173,.T.);
#4327=ORIENTED_EDGE('',*,*,#3174,.F.);
#4328=ORIENTED_EDGE('',*,*,#3175,.F.);
#4329=ORIENTED_EDGE('',*,*,#3170,.T.);
#4330=ORIENTED_EDGE('',*,*,#3176,.T.);
#4331=ORIENTED_EDGE('',*,*,#3177,.T.);
#4332=ORIENTED_EDGE('',*,*,#3178,.F.);
#4333=ORIENTED_EDGE('',*,*,#3179,.F.);
#4334=ORIENTED_EDGE('',*,*,#3180,.F.);
#4335=ORIENTED_EDGE('',*,*,#3174,.T.);
#4336=ORIENTED_EDGE('',*,*,#3181,.T.);
#4337=ORIENTED_EDGE('',*,*,#3182,.F.);
#4338=ORIENTED_EDGE('',*,*,#3183,.F.);
#4339=ORIENTED_EDGE('',*,*,#3178,.T.);
#4340=ORIENTED_EDGE('',*,*,#3184,.T.);
#4341=ORIENTED_EDGE('',*,*,#3185,.T.);
#4342=ORIENTED_EDGE('',*,*,#3186,.F.);
#4343=ORIENTED_EDGE('',*,*,#3187,.F.);
#4344=ORIENTED_EDGE('',*,*,#3188,.F.);
#4345=ORIENTED_EDGE('',*,*,#3182,.T.);
#4346=ORIENTED_EDGE('',*,*,#3189,.T.);
#4347=ORIENTED_EDGE('',*,*,#3190,.F.);
#4348=ORIENTED_EDGE('',*,*,#3191,.F.);
#4349=ORIENTED_EDGE('',*,*,#3186,.T.);
#4350=ORIENTED_EDGE('',*,*,#3192,.T.);
#4351=ORIENTED_EDGE('',*,*,#3193,.T.);
#4352=ORIENTED_EDGE('',*,*,#3194,.F.);
#4353=ORIENTED_EDGE('',*,*,#3195,.F.);
#4354=ORIENTED_EDGE('',*,*,#3196,.F.);
#4355=ORIENTED_EDGE('',*,*,#3190,.T.);
#4356=ORIENTED_EDGE('',*,*,#3197,.T.);
#4357=ORIENTED_EDGE('',*,*,#3198,.F.);
#4358=ORIENTED_EDGE('',*,*,#3199,.F.);
#4359=ORIENTED_EDGE('',*,*,#3194,.T.);
#4360=ORIENTED_EDGE('',*,*,#3200,.T.);
#4361=ORIENTED_EDGE('',*,*,#3201,.T.);
#4362=ORIENTED_EDGE('',*,*,#3202,.F.);
#4363=ORIENTED_EDGE('',*,*,#3203,.F.);
#4364=ORIENTED_EDGE('',*,*,#3204,.F.);
#4365=ORIENTED_EDGE('',*,*,#3198,.T.);
#4366=ORIENTED_EDGE('',*,*,#3205,.T.);
#4367=ORIENTED_EDGE('',*,*,#3206,.F.);
#4368=ORIENTED_EDGE('',*,*,#3207,.F.);
#4369=ORIENTED_EDGE('',*,*,#3202,.T.);
#4370=ORIENTED_EDGE('',*,*,#3208,.T.);
#4371=ORIENTED_EDGE('',*,*,#3209,.T.);
#4372=ORIENTED_EDGE('',*,*,#3210,.F.);
#4373=ORIENTED_EDGE('',*,*,#3211,.F.);
#4374=ORIENTED_EDGE('',*,*,#3212,.F.);
#4375=ORIENTED_EDGE('',*,*,#3206,.T.);
#4376=ORIENTED_EDGE('',*,*,#3213,.T.);
#4377=ORIENTED_EDGE('',*,*,#3214,.T.);
#4378=ORIENTED_EDGE('',*,*,#3215,.F.);
#4379=ORIENTED_EDGE('',*,*,#3216,.F.);
#4380=ORIENTED_EDGE('',*,*,#3217,.F.);
#4381=ORIENTED_EDGE('',*,*,#3210,.T.);
#4382=ORIENTED_EDGE('',*,*,#3218,.T.);
#4383=ORIENTED_EDGE('',*,*,#3219,.T.);
#4384=ORIENTED_EDGE('',*,*,#3220,.F.);
#4385=ORIENTED_EDGE('',*,*,#3221,.F.);
#4386=ORIENTED_EDGE('',*,*,#3222,.F.);
#4387=ORIENTED_EDGE('',*,*,#3215,.T.);
#4388=ORIENTED_EDGE('',*,*,#3223,.T.);
#4389=ORIENTED_EDGE('',*,*,#3224,.F.);
#4390=ORIENTED_EDGE('',*,*,#3225,.F.);
#4391=ORIENTED_EDGE('',*,*,#3220,.T.);
#4392=ORIENTED_EDGE('',*,*,#3226,.T.);
#4393=ORIENTED_EDGE('',*,*,#3227,.T.);
#4394=ORIENTED_EDGE('',*,*,#3228,.F.);
#4395=ORIENTED_EDGE('',*,*,#3229,.F.);
#4396=ORIENTED_EDGE('',*,*,#3230,.F.);
#4397=ORIENTED_EDGE('',*,*,#3224,.T.);
#4398=ORIENTED_EDGE('',*,*,#3231,.T.);
#4399=ORIENTED_EDGE('',*,*,#3232,.F.);
#4400=ORIENTED_EDGE('',*,*,#3233,.F.);
#4401=ORIENTED_EDGE('',*,*,#3228,.T.);
#4402=ORIENTED_EDGE('',*,*,#3234,.T.);
#4403=ORIENTED_EDGE('',*,*,#3235,.T.);
#4404=ORIENTED_EDGE('',*,*,#3236,.F.);
#4405=ORIENTED_EDGE('',*,*,#3237,.F.);
#4406=ORIENTED_EDGE('',*,*,#3238,.F.);
#4407=ORIENTED_EDGE('',*,*,#3232,.T.);
#4408=ORIENTED_EDGE('',*,*,#3239,.T.);
#4409=ORIENTED_EDGE('',*,*,#3240,.F.);
#4410=ORIENTED_EDGE('',*,*,#3241,.F.);
#4411=ORIENTED_EDGE('',*,*,#3236,.T.);
#4412=ORIENTED_EDGE('',*,*,#3242,.T.);
#4413=ORIENTED_EDGE('',*,*,#3243,.T.);
#4414=ORIENTED_EDGE('',*,*,#3244,.F.);
#4415=ORIENTED_EDGE('',*,*,#3245,.F.);
#4416=ORIENTED_EDGE('',*,*,#3246,.F.);
#4417=ORIENTED_EDGE('',*,*,#3240,.T.);
#4418=ORIENTED_EDGE('',*,*,#3247,.T.);
#4419=ORIENTED_EDGE('',*,*,#3248,.F.);
#4420=ORIENTED_EDGE('',*,*,#3249,.F.);
#4421=ORIENTED_EDGE('',*,*,#3244,.T.);
#4422=ORIENTED_EDGE('',*,*,#3250,.T.);
#4423=ORIENTED_EDGE('',*,*,#3251,.T.);
#4424=ORIENTED_EDGE('',*,*,#3252,.F.);
#4425=ORIENTED_EDGE('',*,*,#3253,.F.);
#4426=ORIENTED_EDGE('',*,*,#3254,.F.);
#4427=ORIENTED_EDGE('',*,*,#3248,.T.);
#4428=ORIENTED_EDGE('',*,*,#3255,.T.);
#4429=ORIENTED_EDGE('',*,*,#3256,.T.);
#4430=ORIENTED_EDGE('',*,*,#3257,.F.);
#4431=ORIENTED_EDGE('',*,*,#3258,.F.);
#4432=ORIENTED_EDGE('',*,*,#3252,.T.);
#4433=ORIENTED_EDGE('',*,*,#3259,.T.);
#4434=ORIENTED_EDGE('',*,*,#3260,.F.);
#4435=ORIENTED_EDGE('',*,*,#3261,.F.);
#4436=ORIENTED_EDGE('',*,*,#3262,.F.);
#4437=ORIENTED_EDGE('',*,*,#3257,.T.);
#4438=ORIENTED_EDGE('',*,*,#3263,.T.);
#4439=ORIENTED_EDGE('',*,*,#3264,.T.);
#4440=ORIENTED_EDGE('',*,*,#3265,.F.);
#4441=ORIENTED_EDGE('',*,*,#3266,.F.);
#4442=ORIENTED_EDGE('',*,*,#3267,.F.);
#4443=ORIENTED_EDGE('',*,*,#3260,.T.);
#4444=ORIENTED_EDGE('',*,*,#3268,.T.);
#4445=ORIENTED_EDGE('',*,*,#3269,.F.);
#4446=ORIENTED_EDGE('',*,*,#3270,.F.);
#4447=ORIENTED_EDGE('',*,*,#3271,.F.);
#4448=ORIENTED_EDGE('',*,*,#3265,.T.);
#4449=ORIENTED_EDGE('',*,*,#3272,.T.);
#4450=ORIENTED_EDGE('',*,*,#3273,.T.);
#4451=ORIENTED_EDGE('',*,*,#3274,.F.);
#4452=ORIENTED_EDGE('',*,*,#3275,.F.);
#4453=ORIENTED_EDGE('',*,*,#3269,.T.);
#4454=ORIENTED_EDGE('',*,*,#3276,.T.);
#4455=ORIENTED_EDGE('',*,*,#3277,.T.);
#4456=ORIENTED_EDGE('',*,*,#3278,.T.);
#4457=ORIENTED_EDGE('',*,*,#3279,.T.);
#4458=ORIENTED_EDGE('',*,*,#3280,.T.);
#4459=ORIENTED_EDGE('',*,*,#3281,.T.);
#4460=ORIENTED_EDGE('',*,*,#3282,.T.);
#4461=ORIENTED_EDGE('',*,*,#3283,.T.);
#4462=ORIENTED_EDGE('',*,*,#3284,.T.);
#4463=ORIENTED_EDGE('',*,*,#3285,.T.);
#4464=ORIENTED_EDGE('',*,*,#3286,.T.);
#4465=ORIENTED_EDGE('',*,*,#3287,.T.);
#4466=ORIENTED_EDGE('',*,*,#3288,.T.);
#4467=ORIENTED_EDGE('',*,*,#3289,.T.);
#4468=ORIENTED_EDGE('',*,*,#3290,.T.);
#4469=ORIENTED_EDGE('',*,*,#3291,.T.);
#4470=ORIENTED_EDGE('',*,*,#3292,.T.);
#4471=ORIENTED_EDGE('',*,*,#3293,.T.);
#4472=ORIENTED_EDGE('',*,*,#3294,.T.);
#4473=ORIENTED_EDGE('',*,*,#3295,.T.);
#4474=ORIENTED_EDGE('',*,*,#3296,.T.);
#4475=ORIENTED_EDGE('',*,*,#3297,.T.);
#4476=ORIENTED_EDGE('',*,*,#3298,.T.);
#4477=ORIENTED_EDGE('',*,*,#3299,.T.);
#4478=ORIENTED_EDGE('',*,*,#3300,.T.);
#4479=ORIENTED_EDGE('',*,*,#3301,.T.);
#4480=ORIENTED_EDGE('',*,*,#3302,.T.);
#4481=ORIENTED_EDGE('',*,*,#3303,.T.);
#4482=ORIENTED_EDGE('',*,*,#3304,.T.);
#4483=ORIENTED_EDGE('',*,*,#3305,.T.);
#4484=ORIENTED_EDGE('',*,*,#3306,.T.);
#4485=ORIENTED_EDGE('',*,*,#3307,.T.);
#4486=ORIENTED_EDGE('',*,*,#3308,.T.);
#4487=ORIENTED_EDGE('',*,*,#3309,.T.);
#4488=ORIENTED_EDGE('',*,*,#3310,.T.);
#4489=ORIENTED_EDGE('',*,*,#3311,.T.);
#4490=ORIENTED_EDGE('',*,*,#3312,.T.);
#4491=ORIENTED_EDGE('',*,*,#3313,.T.);
#4492=ORIENTED_EDGE('',*,*,#3314,.T.);
#4493=ORIENTED_EDGE('',*,*,#3315,.T.);
#4494=ORIENTED_EDGE('',*,*,#3316,.F.);
#4495=ORIENTED_EDGE('',*,*,#3317,.T.);
#4496=ORIENTED_EDGE('',*,*,#3318,.T.);
#4497=ORIENTED_EDGE('',*,*,#3319,.T.);
#4498=ORIENTED_EDGE('',*,*,#3320,.T.);
#4499=ORIENTED_EDGE('',*,*,#3321,.T.);
#4500=ORIENTED_EDGE('',*,*,#3322,.T.);
#4501=ORIENTED_EDGE('',*,*,#3323,.T.);
#4502=ORIENTED_EDGE('',*,*,#3324,.T.);
#4503=ORIENTED_EDGE('',*,*,#3325,.T.);
#4504=ORIENTED_EDGE('',*,*,#3326,.T.);
#4505=ORIENTED_EDGE('',*,*,#3327,.T.);
#4506=ORIENTED_EDGE('',*,*,#3328,.T.);
#4507=ORIENTED_EDGE('',*,*,#3329,.T.);
#4508=ORIENTED_EDGE('',*,*,#3330,.T.);
#4509=ORIENTED_EDGE('',*,*,#3331,.T.);
#4510=ORIENTED_EDGE('',*,*,#3332,.T.);
#4511=ORIENTED_EDGE('',*,*,#3333,.T.);
#4512=ORIENTED_EDGE('',*,*,#3334,.T.);
#4513=ORIENTED_EDGE('',*,*,#3335,.T.);
#4514=ORIENTED_EDGE('',*,*,#3336,.T.);
#4515=ORIENTED_EDGE('',*,*,#3337,.T.);
#4516=ORIENTED_EDGE('',*,*,#3338,.T.);
#4517=ORIENTED_EDGE('',*,*,#3339,.T.);
#4518=ORIENTED_EDGE('',*,*,#3340,.T.);
#4519=ORIENTED_EDGE('',*,*,#3341,.T.);
#4520=ORIENTED_EDGE('',*,*,#3342,.T.);
#4521=ORIENTED_EDGE('',*,*,#3343,.T.);
#4522=ORIENTED_EDGE('',*,*,#3344,.T.);
#4523=ORIENTED_EDGE('',*,*,#3345,.T.);
#4524=ORIENTED_EDGE('',*,*,#3346,.T.);
#4525=ORIENTED_EDGE('',*,*,#3347,.T.);
#4526=ORIENTED_EDGE('',*,*,#3348,.T.);
#4527=ORIENTED_EDGE('',*,*,#3349,.T.);
#4528=ORIENTED_EDGE('',*,*,#3350,.T.);
#4529=ORIENTED_EDGE('',*,*,#3274,.T.);
#4530=ORIENTED_EDGE('',*,*,#3351,.T.);
#4531=ORIENTED_EDGE('',*,*,#3352,.F.);
#4532=ORIENTED_EDGE('',*,*,#3353,.F.);
#4533=ORIENTED_EDGE('',*,*,#3354,.F.);
#4534=ORIENTED_EDGE('',*,*,#3355,.F.);
#4535=ORIENTED_EDGE('',*,*,#3315,.F.);
#4536=ORIENTED_EDGE('',*,*,#3314,.F.);
#4537=ORIENTED_EDGE('',*,*,#3313,.F.);
#4538=ORIENTED_EDGE('',*,*,#3312,.F.);
#4539=ORIENTED_EDGE('',*,*,#3311,.F.);
#4540=ORIENTED_EDGE('',*,*,#3310,.F.);
#4541=ORIENTED_EDGE('',*,*,#3309,.F.);
#4542=ORIENTED_EDGE('',*,*,#3308,.F.);
#4543=ORIENTED_EDGE('',*,*,#3307,.F.);
#4544=ORIENTED_EDGE('',*,*,#3306,.F.);
#4545=ORIENTED_EDGE('',*,*,#3305,.F.);
#4546=ORIENTED_EDGE('',*,*,#3304,.F.);
#4547=ORIENTED_EDGE('',*,*,#3303,.F.);
#4548=ORIENTED_EDGE('',*,*,#3302,.F.);
#4549=ORIENTED_EDGE('',*,*,#3301,.F.);
#4550=ORIENTED_EDGE('',*,*,#3300,.F.);
#4551=ORIENTED_EDGE('',*,*,#3299,.F.);
#4552=ORIENTED_EDGE('',*,*,#3298,.F.);
#4553=ORIENTED_EDGE('',*,*,#3297,.F.);
#4554=ORIENTED_EDGE('',*,*,#3296,.F.);
#4555=ORIENTED_EDGE('',*,*,#3295,.F.);
#4556=ORIENTED_EDGE('',*,*,#3294,.F.);
#4557=ORIENTED_EDGE('',*,*,#3293,.F.);
#4558=ORIENTED_EDGE('',*,*,#3292,.F.);
#4559=ORIENTED_EDGE('',*,*,#3291,.F.);
#4560=ORIENTED_EDGE('',*,*,#3290,.F.);
#4561=ORIENTED_EDGE('',*,*,#3289,.F.);
#4562=ORIENTED_EDGE('',*,*,#3288,.F.);
#4563=ORIENTED_EDGE('',*,*,#3287,.F.);
#4564=ORIENTED_EDGE('',*,*,#3286,.F.);
#4565=ORIENTED_EDGE('',*,*,#3285,.F.);
#4566=ORIENTED_EDGE('',*,*,#3284,.F.);
#4567=ORIENTED_EDGE('',*,*,#3283,.F.);
#4568=ORIENTED_EDGE('',*,*,#3282,.F.);
#4569=ORIENTED_EDGE('',*,*,#3281,.F.);
#4570=ORIENTED_EDGE('',*,*,#3280,.F.);
#4571=ORIENTED_EDGE('',*,*,#3356,.F.);
#4572=ORIENTED_EDGE('',*,*,#3357,.T.);
#4573=ORIENTED_EDGE('',*,*,#3137,.T.);
#4574=ORIENTED_EDGE('',*,*,#3141,.T.);
#4575=ORIENTED_EDGE('',*,*,#3146,.T.);
#4576=ORIENTED_EDGE('',*,*,#3145,.T.);
#4577=ORIENTED_EDGE('',*,*,#3149,.T.);
#4578=ORIENTED_EDGE('',*,*,#3154,.T.);
#4579=ORIENTED_EDGE('',*,*,#3153,.T.);
#4580=ORIENTED_EDGE('',*,*,#3157,.T.);
#4581=ORIENTED_EDGE('',*,*,#3162,.T.);
#4582=ORIENTED_EDGE('',*,*,#3161,.T.);
#4583=ORIENTED_EDGE('',*,*,#3167,.T.);
#4584=ORIENTED_EDGE('',*,*,#3166,.T.);
#4585=ORIENTED_EDGE('',*,*,#3172,.T.);
#4586=ORIENTED_EDGE('',*,*,#3171,.T.);
#4587=ORIENTED_EDGE('',*,*,#3175,.T.);
#4588=ORIENTED_EDGE('',*,*,#3180,.T.);
#4589=ORIENTED_EDGE('',*,*,#3179,.T.);
#4590=ORIENTED_EDGE('',*,*,#3183,.T.);
#4591=ORIENTED_EDGE('',*,*,#3188,.T.);
#4592=ORIENTED_EDGE('',*,*,#3187,.T.);
#4593=ORIENTED_EDGE('',*,*,#3191,.T.);
#4594=ORIENTED_EDGE('',*,*,#3196,.T.);
#4595=ORIENTED_EDGE('',*,*,#3195,.T.);
#4596=ORIENTED_EDGE('',*,*,#3199,.T.);
#4597=ORIENTED_EDGE('',*,*,#3204,.T.);
#4598=ORIENTED_EDGE('',*,*,#3203,.T.);
#4599=ORIENTED_EDGE('',*,*,#3207,.T.);
#4600=ORIENTED_EDGE('',*,*,#3212,.T.);
#4601=ORIENTED_EDGE('',*,*,#3211,.T.);
#4602=ORIENTED_EDGE('',*,*,#3217,.T.);
#4603=ORIENTED_EDGE('',*,*,#3216,.T.);
#4604=ORIENTED_EDGE('',*,*,#3222,.T.);
#4605=ORIENTED_EDGE('',*,*,#3221,.T.);
#4606=ORIENTED_EDGE('',*,*,#3225,.T.);
#4607=ORIENTED_EDGE('',*,*,#3230,.T.);
#4608=ORIENTED_EDGE('',*,*,#3229,.T.);
#4609=ORIENTED_EDGE('',*,*,#3233,.T.);
#4610=ORIENTED_EDGE('',*,*,#3238,.T.);
#4611=ORIENTED_EDGE('',*,*,#3237,.T.);
#4612=ORIENTED_EDGE('',*,*,#3241,.T.);
#4613=ORIENTED_EDGE('',*,*,#3246,.T.);
#4614=ORIENTED_EDGE('',*,*,#3245,.T.);
#4615=ORIENTED_EDGE('',*,*,#3249,.T.);
#4616=ORIENTED_EDGE('',*,*,#3254,.T.);
#4617=ORIENTED_EDGE('',*,*,#3253,.T.);
#4618=ORIENTED_EDGE('',*,*,#3258,.T.);
#4619=ORIENTED_EDGE('',*,*,#3262,.T.);
#4620=ORIENTED_EDGE('',*,*,#3261,.T.);
#4621=ORIENTED_EDGE('',*,*,#3267,.T.);
#4622=ORIENTED_EDGE('',*,*,#3266,.T.);
#4623=ORIENTED_EDGE('',*,*,#3271,.T.);
#4624=ORIENTED_EDGE('',*,*,#3270,.T.);
#4625=ORIENTED_EDGE('',*,*,#3275,.T.);
#4626=ORIENTED_EDGE('',*,*,#3354,.T.);
#4627=ORIENTED_EDGE('',*,*,#3353,.T.);
#4628=ORIENTED_EDGE('',*,*,#3358,.F.);
#4629=ORIENTED_EDGE('',*,*,#3359,.F.);
#4630=ORIENTED_EDGE('',*,*,#3351,.F.);
#4631=ORIENTED_EDGE('',*,*,#3277,.F.);
#4632=ORIENTED_EDGE('',*,*,#3276,.F.);
#4633=ORIENTED_EDGE('',*,*,#3273,.F.);
#4634=ORIENTED_EDGE('',*,*,#3272,.F.);
#4635=ORIENTED_EDGE('',*,*,#3268,.F.);
#4636=ORIENTED_EDGE('',*,*,#3264,.F.);
#4637=ORIENTED_EDGE('',*,*,#3263,.F.);
#4638=ORIENTED_EDGE('',*,*,#3259,.F.);
#4639=ORIENTED_EDGE('',*,*,#3256,.F.);
#4640=ORIENTED_EDGE('',*,*,#3255,.F.);
#4641=ORIENTED_EDGE('',*,*,#3251,.F.);
#4642=ORIENTED_EDGE('',*,*,#3250,.F.);
#4643=ORIENTED_EDGE('',*,*,#3247,.F.);
#4644=ORIENTED_EDGE('',*,*,#3243,.F.);
#4645=ORIENTED_EDGE('',*,*,#3242,.F.);
#4646=ORIENTED_EDGE('',*,*,#3239,.F.);
#4647=ORIENTED_EDGE('',*,*,#3235,.F.);
#4648=ORIENTED_EDGE('',*,*,#3234,.F.);
#4649=ORIENTED_EDGE('',*,*,#3231,.F.);
#4650=ORIENTED_EDGE('',*,*,#3227,.F.);
#4651=ORIENTED_EDGE('',*,*,#3226,.F.);
#4652=ORIENTED_EDGE('',*,*,#3223,.F.);
#4653=ORIENTED_EDGE('',*,*,#3219,.F.);
#4654=ORIENTED_EDGE('',*,*,#3218,.F.);
#4655=ORIENTED_EDGE('',*,*,#3214,.F.);
#4656=ORIENTED_EDGE('',*,*,#3213,.F.);
#4657=ORIENTED_EDGE('',*,*,#3209,.F.);
#4658=ORIENTED_EDGE('',*,*,#3208,.F.);
#4659=ORIENTED_EDGE('',*,*,#3205,.F.);
#4660=ORIENTED_EDGE('',*,*,#3201,.F.);
#4661=ORIENTED_EDGE('',*,*,#3200,.F.);
#4662=ORIENTED_EDGE('',*,*,#3197,.F.);
#4663=ORIENTED_EDGE('',*,*,#3193,.F.);
#4664=ORIENTED_EDGE('',*,*,#3192,.F.);
#4665=ORIENTED_EDGE('',*,*,#3189,.F.);
#4666=ORIENTED_EDGE('',*,*,#3185,.F.);
#4667=ORIENTED_EDGE('',*,*,#3184,.F.);
#4668=ORIENTED_EDGE('',*,*,#3181,.F.);
#4669=ORIENTED_EDGE('',*,*,#3177,.F.);
#4670=ORIENTED_EDGE('',*,*,#3176,.F.);
#4671=ORIENTED_EDGE('',*,*,#3173,.F.);
#4672=ORIENTED_EDGE('',*,*,#3169,.F.);
#4673=ORIENTED_EDGE('',*,*,#3168,.F.);
#4674=ORIENTED_EDGE('',*,*,#3164,.F.);
#4675=ORIENTED_EDGE('',*,*,#3163,.F.);
#4676=ORIENTED_EDGE('',*,*,#3159,.F.);
#4677=ORIENTED_EDGE('',*,*,#3158,.F.);
#4678=ORIENTED_EDGE('',*,*,#3155,.F.);
#4679=ORIENTED_EDGE('',*,*,#3151,.F.);
#4680=ORIENTED_EDGE('',*,*,#3150,.F.);
#4681=ORIENTED_EDGE('',*,*,#3147,.F.);
#4682=ORIENTED_EDGE('',*,*,#3143,.F.);
#4683=ORIENTED_EDGE('',*,*,#3142,.F.);
#4684=ORIENTED_EDGE('',*,*,#3139,.F.);
#4685=ORIENTED_EDGE('',*,*,#3360,.F.);
#4686=ORIENTED_EDGE('',*,*,#3278,.F.);
#4687=ORIENTED_EDGE('',*,*,#3350,.F.);
#4688=ORIENTED_EDGE('',*,*,#3349,.F.);
#4689=ORIENTED_EDGE('',*,*,#3348,.F.);
#4690=ORIENTED_EDGE('',*,*,#3347,.F.);
#4691=ORIENTED_EDGE('',*,*,#3346,.F.);
#4692=ORIENTED_EDGE('',*,*,#3345,.F.);
#4693=ORIENTED_EDGE('',*,*,#3344,.F.);
#4694=ORIENTED_EDGE('',*,*,#3343,.F.);
#4695=ORIENTED_EDGE('',*,*,#3342,.F.);
#4696=ORIENTED_EDGE('',*,*,#3341,.F.);
#4697=ORIENTED_EDGE('',*,*,#3340,.F.);
#4698=ORIENTED_EDGE('',*,*,#3339,.F.);
#4699=ORIENTED_EDGE('',*,*,#3338,.F.);
#4700=ORIENTED_EDGE('',*,*,#3337,.F.);
#4701=ORIENTED_EDGE('',*,*,#3336,.F.);
#4702=ORIENTED_EDGE('',*,*,#3335,.F.);
#4703=ORIENTED_EDGE('',*,*,#3334,.F.);
#4704=ORIENTED_EDGE('',*,*,#3333,.F.);
#4705=ORIENTED_EDGE('',*,*,#3332,.F.);
#4706=ORIENTED_EDGE('',*,*,#3331,.F.);
#4707=ORIENTED_EDGE('',*,*,#3330,.F.);
#4708=ORIENTED_EDGE('',*,*,#3329,.F.);
#4709=ORIENTED_EDGE('',*,*,#3328,.F.);
#4710=ORIENTED_EDGE('',*,*,#3327,.F.);
#4711=ORIENTED_EDGE('',*,*,#3326,.F.);
#4712=ORIENTED_EDGE('',*,*,#3325,.F.);
#4713=ORIENTED_EDGE('',*,*,#3324,.F.);
#4714=ORIENTED_EDGE('',*,*,#3323,.F.);
#4715=ORIENTED_EDGE('',*,*,#3322,.F.);
#4716=ORIENTED_EDGE('',*,*,#3321,.F.);
#4717=ORIENTED_EDGE('',*,*,#3320,.F.);
#4718=ORIENTED_EDGE('',*,*,#3319,.F.);
#4719=ORIENTED_EDGE('',*,*,#3318,.F.);
#4720=ORIENTED_EDGE('',*,*,#3317,.F.);
#4721=ORIENTED_EDGE('',*,*,#3361,.F.);
#4722=ORIENTED_EDGE('',*,*,#3362,.T.);
#4723=ORIENTED_EDGE('',*,*,#3363,.T.);
#4724=ORIENTED_EDGE('',*,*,#3364,.F.);
#4725=ORIENTED_EDGE('',*,*,#3365,.F.);
#4726=ORIENTED_EDGE('',*,*,#3366,.T.);
#4727=ORIENTED_EDGE('',*,*,#3367,.T.);
#4728=ORIENTED_EDGE('',*,*,#3362,.F.);
#4729=ORIENTED_EDGE('',*,*,#3368,.F.);
#4730=ORIENTED_EDGE('',*,*,#3369,.T.);
#4731=ORIENTED_EDGE('',*,*,#3370,.T.);
#4732=ORIENTED_EDGE('',*,*,#3366,.F.);
#4733=ORIENTED_EDGE('',*,*,#3371,.F.);
#4734=ORIENTED_EDGE('',*,*,#3372,.T.);
#4735=ORIENTED_EDGE('',*,*,#3373,.T.);
#4736=ORIENTED_EDGE('',*,*,#3369,.F.);
#4737=ORIENTED_EDGE('',*,*,#3374,.F.);
#4738=ORIENTED_EDGE('',*,*,#3375,.T.);
#4739=ORIENTED_EDGE('',*,*,#3376,.T.);
#4740=ORIENTED_EDGE('',*,*,#3372,.F.);
#4741=ORIENTED_EDGE('',*,*,#3377,.F.);
#4742=ORIENTED_EDGE('',*,*,#3364,.T.);
#4743=ORIENTED_EDGE('',*,*,#3378,.T.);
#4744=ORIENTED_EDGE('',*,*,#3375,.F.);
#4745=ORIENTED_EDGE('',*,*,#3378,.F.);
#4746=ORIENTED_EDGE('',*,*,#3363,.F.);
#4747=ORIENTED_EDGE('',*,*,#3367,.F.);
#4748=ORIENTED_EDGE('',*,*,#3370,.F.);
#4749=ORIENTED_EDGE('',*,*,#3373,.F.);
#4750=ORIENTED_EDGE('',*,*,#3376,.F.);
#4751=ORIENTED_EDGE('',*,*,#3379,.T.);
#4752=ORIENTED_EDGE('',*,*,#3360,.T.);
#4753=ORIENTED_EDGE('',*,*,#3138,.T.);
#4754=ORIENTED_EDGE('',*,*,#3357,.F.);
#4755=ORIENTED_EDGE('',*,*,#3356,.T.);
#4756=ORIENTED_EDGE('',*,*,#3279,.F.);
#4757=ORIENTED_EDGE('',*,*,#3379,.F.);
#4758=ORIENTED_EDGE('',*,*,#3380,.T.);
#4759=ORIENTED_EDGE('',*,*,#3381,.T.);
#4760=ORIENTED_EDGE('',*,*,#3380,.F.);
#4761=ORIENTED_EDGE('',*,*,#3381,.F.);
#4762=ORIENTED_EDGE('',*,*,#3361,.T.);
#4763=ORIENTED_EDGE('',*,*,#3377,.T.);
#4764=ORIENTED_EDGE('',*,*,#3374,.T.);
#4765=ORIENTED_EDGE('',*,*,#3371,.T.);
#4766=ORIENTED_EDGE('',*,*,#3368,.T.);
#4767=ORIENTED_EDGE('',*,*,#3365,.T.);
#4768=ORIENTED_EDGE('',*,*,#3358,.T.);
#4769=ORIENTED_EDGE('',*,*,#3316,.T.);
#4770=ORIENTED_EDGE('',*,*,#3355,.T.);
#4771=ORIENTED_EDGE('',*,*,#3352,.T.);
#4772=ORIENTED_EDGE('',*,*,#3359,.T.);
#5368=PLANE('',#6130);
#5369=PLANE('',#6131);
#5370=PLANE('',#6132);
#5371=PLANE('',#6133);
#5372=PLANE('',#6134);
#5373=PLANE('',#6135);
#5374=PLANE('',#6136);
#5375=PLANE('',#6137);
#5376=PLANE('',#6141);
#5377=PLANE('',#6142);
#5577=ADVANCED_FACE('',(#763),#516,.T.);
#5578=ADVANCED_FACE('',(#764),#517,.T.);
#5579=ADVANCED_FACE('',(#765),#518,.T.);
#5580=ADVANCED_FACE('',(#766),#519,.T.);
#5581=ADVANCED_FACE('',(#767),#520,.T.);
#5582=ADVANCED_FACE('',(#768),#521,.T.);
#5583=ADVANCED_FACE('',(#769),#522,.T.);
#5584=ADVANCED_FACE('',(#770),#523,.T.);
#5585=ADVANCED_FACE('',(#771),#524,.T.);
#5586=ADVANCED_FACE('',(#772),#525,.T.);
#5587=ADVANCED_FACE('',(#773),#526,.T.);
#5588=ADVANCED_FACE('',(#774),#527,.T.);
#5589=ADVANCED_FACE('',(#775),#528,.T.);
#5590=ADVANCED_FACE('',(#776),#529,.T.);
#5591=ADVANCED_FACE('',(#777),#530,.T.);
#5592=ADVANCED_FACE('',(#778),#531,.T.);
#5593=ADVANCED_FACE('',(#779),#532,.T.);
#5594=ADVANCED_FACE('',(#780),#533,.T.);
#5595=ADVANCED_FACE('',(#781),#534,.T.);
#5596=ADVANCED_FACE('',(#782),#535,.T.);
#5597=ADVANCED_FACE('',(#783),#536,.T.);
#5598=ADVANCED_FACE('',(#784),#537,.T.);
#5599=ADVANCED_FACE('',(#785),#538,.T.);
#5600=ADVANCED_FACE('',(#786),#539,.T.);
#5601=ADVANCED_FACE('',(#787),#540,.T.);
#5602=ADVANCED_FACE('',(#788),#541,.T.);
#5603=ADVANCED_FACE('',(#789),#542,.T.);
#5604=ADVANCED_FACE('',(#790),#543,.T.);
#5605=ADVANCED_FACE('',(#791),#544,.T.);
#5606=ADVANCED_FACE('',(#792),#545,.T.);
#5607=ADVANCED_FACE('',(#793),#546,.T.);
#5608=ADVANCED_FACE('',(#794),#547,.T.);
#5609=ADVANCED_FACE('',(#795),#548,.T.);
#5610=ADVANCED_FACE('',(#796),#549,.T.);
#5611=ADVANCED_FACE('',(#797),#550,.T.);
#5612=ADVANCED_FACE('',(#798),#551,.T.);
#5613=ADVANCED_FACE('',(#799),#139,.F.);
#5614=ADVANCED_FACE('',(#800),#140,.F.);
#5615=ADVANCED_FACE('',(#801),#5368,.F.);
#5616=ADVANCED_FACE('',(#802),#5369,.F.);
#5617=ADVANCED_FACE('',(#803),#5370,.F.);
#5618=ADVANCED_FACE('',(#804),#5371,.F.);
#5619=ADVANCED_FACE('',(#805),#5372,.F.);
#5620=ADVANCED_FACE('',(#806),#5373,.F.);
#5621=ADVANCED_FACE('',(#807),#5374,.F.);
#5622=ADVANCED_FACE('',(#808,#409),#5375,.T.);
#5623=ADVANCED_FACE('',(#809),#552,.T.);
#5624=ADVANCED_FACE('',(#810,#410),#5376,.F.);
#5625=ADVANCED_FACE('',(#811),#5377,.T.);
#5724=CLOSED_SHELL('',(#5577,#5578,#5579,#5580,#5581,#5582,#5583,#5584,
#5585,#5586,#5587,#5588,#5589,#5590,#5591,#5592,#5593,#5594,#5595,#5596,
#5597,#5598,#5599,#5600,#5601,#5602,#5603,#5604,#5605,#5606,#5607,#5608,
#5609,#5610,#5611,#5612,#5613,#5614,#5615,#5616,#5617,#5618,#5619,#5620,
#5621,#5622,#5623,#5624,#5625));
#6089=AXIS2_PLACEMENT_3D('',#8247,#6943,#6944);
#6090=AXIS2_PLACEMENT_3D('',#8248,#6945,#6946);
#6091=AXIS2_PLACEMENT_3D('',#8434,#6948,#6949);
#6092=AXIS2_PLACEMENT_3D('',#8481,#6950,#6951);
#6093=AXIS2_PLACEMENT_3D('',#8926,#6953,#6954);
#6094=AXIS2_PLACEMENT_3D('',#9413,#6956,#6957);
#6095=AXIS2_PLACEMENT_3D('',#9900,#6959,#6960);
#6096=AXIS2_PLACEMENT_3D('',#10401,#6962,#6963);
#6097=AXIS2_PLACEMENT_3D('',#10754,#6965,#6966);
#6098=AXIS2_PLACEMENT_3D('',#10878,#6968,#6969);
#6099=AXIS2_PLACEMENT_3D('',#11179,#6971,#6972);
#6100=AXIS2_PLACEMENT_3D('',#11608,#6974,#6975);
#6101=AXIS2_PLACEMENT_3D('',#12111,#6977,#6978);
#6102=AXIS2_PLACEMENT_3D('',#12610,#6980,#6981);
#6103=AXIS2_PLACEMENT_3D('',#13149,#6983,#6984);
#6104=AXIS2_PLACEMENT_3D('',#13800,#6986,#6987);
#6105=AXIS2_PLACEMENT_3D('',#14301,#6989,#6990);
#6106=AXIS2_PLACEMENT_3D('',#14802,#6992,#6993);
#6107=AXIS2_PLACEMENT_3D('',#15285,#6995,#6996);
#6108=AXIS2_PLACEMENT_3D('',#15780,#6998,#6999);
#6109=AXIS2_PLACEMENT_3D('',#16137,#7001,#7002);
#6110=AXIS2_PLACEMENT_3D('',#16264,#7004,#7005);
#6111=AXIS2_PLACEMENT_3D('',#16559,#7007,#7008);
#6112=AXIS2_PLACEMENT_3D('',#17004,#7010,#7011);
#6113=AXIS2_PLACEMENT_3D('',#17531,#7013,#7014);
#6114=AXIS2_PLACEMENT_3D('',#18096,#7016,#7017);
#6115=AXIS2_PLACEMENT_3D('',#18601,#7019,#7020);
#6116=AXIS2_PLACEMENT_3D('',#19070,#7022,#7023);
#6117=AXIS2_PLACEMENT_3D('',#19535,#7025,#7026);
#6118=AXIS2_PLACEMENT_3D('',#20026,#7028,#7029);
#6119=AXIS2_PLACEMENT_3D('',#20348,#7031,#7032);
#6120=AXIS2_PLACEMENT_3D('',#20824,#7034,#7035);
#6121=AXIS2_PLACEMENT_3D('',#21282,#7037,#7038);
#6122=AXIS2_PLACEMENT_3D('',#21583,#7040,#7041);
#6123=AXIS2_PLACEMENT_3D('',#21931,#7043,#7044);
#6124=AXIS2_PLACEMENT_3D('',#22283,#7046,#7047);
#6125=AXIS2_PLACEMENT_3D('',#22778,#7049,#7050);
#6126=AXIS2_PLACEMENT_3D('',#22819,#7051,#7052);
#6127=AXIS2_PLACEMENT_3D('',#24487,#7053,#7054);
#6128=AXIS2_PLACEMENT_3D('',#26222,#7055,#7056);
#6129=AXIS2_PLACEMENT_3D('',#26463,#7057,#7058);
#6130=AXIS2_PLACEMENT_3D('',#28547,#7059,#7060);
#6131=AXIS2_PLACEMENT_3D('',#28556,#7065,#7066);
#6132=AXIS2_PLACEMENT_3D('',#28562,#7070,#7071);
#6133=AXIS2_PLACEMENT_3D('',#28568,#7075,#7076);
#6134=AXIS2_PLACEMENT_3D('',#28574,#7080,#7081);
#6135=AXIS2_PLACEMENT_3D('',#28580,#7085,#7086);
#6136=AXIS2_PLACEMENT_3D('',#28583,#7089,#7090);
#6137=AXIS2_PLACEMENT_3D('',#28584,#7091,#7092);
#6138=AXIS2_PLACEMENT_3D('',#28586,#7093,#7094);
#6139=AXIS2_PLACEMENT_3D('',#28587,#7095,#7096);
#6140=AXIS2_PLACEMENT_3D('',#28590,#7098,#7099);
#6141=AXIS2_PLACEMENT_3D('',#28591,#7100,#7101);
#6142=AXIS2_PLACEMENT_3D('',#28592,#7102,#7103);
#6943=DIRECTION('axis',(0.,0.,1.));
#6944=DIRECTION('refdir',(1.,0.,0.));
#6945=DIRECTION('center_axis',(0.,0.,1.));
#6946=DIRECTION('ref_axis',(0.409441503265782,-0.912336371851663,0.));
#6947=DIRECTION('',(0.,0.,-1.));
#6948=DIRECTION('center_axis',(0.,0.,-1.));
#6949=DIRECTION('ref_axis',(1.,-2.80853466614331E-13,0.));
#6950=DIRECTION('center_axis',(0.,0.,1.));
#6951=DIRECTION('ref_axis',(0.409441503265782,-0.912336371851663,0.));
#6952=DIRECTION('',(0.,0.,-1.));
#6953=DIRECTION('center_axis',(0.,0.,1.));
#6954=DIRECTION('ref_axis',(0.409441503265782,-0.912336371851663,0.));
#6955=DIRECTION('',(0.,0.,-1.));
#6956=DIRECTION('center_axis',(0.,0.,1.));
#6957=DIRECTION('ref_axis',(0.409441503265782,-0.912336371851663,0.));
#6958=DIRECTION('',(0.,0.,-1.));
#6959=DIRECTION('center_axis',(0.,0.,1.));
#6960=DIRECTION('ref_axis',(0.409441503265782,-0.912336371851663,0.));
#6961=DIRECTION('',(0.,0.,-1.));
#6962=DIRECTION('center_axis',(0.,0.,1.));
#6963=DIRECTION('ref_axis',(0.409441503265782,-0.912336371851663,0.));
#6964=DIRECTION('',(0.,0.,-1.));
#6965=DIRECTION('center_axis',(0.,0.,1.));
#6966=DIRECTION('ref_axis',(0.409441503265782,-0.912336371851663,0.));
#6967=DIRECTION('',(0.,0.,-1.));
#6968=DIRECTION('center_axis',(0.,0.,1.));
#6969=DIRECTION('ref_axis',(0.409441503265782,-0.912336371851663,0.));
#6970=DIRECTION('',(0.,0.,-1.));
#6971=DIRECTION('center_axis',(0.,0.,1.));
#6972=DIRECTION('ref_axis',(0.409441503265782,-0.912336371851663,0.));
#6973=DIRECTION('',(0.,0.,-1.));
#6974=DIRECTION('center_axis',(0.,0.,1.));
#6975=DIRECTION('ref_axis',(0.409441503265782,-0.912336371851663,0.));
#6976=DIRECTION('',(0.,0.,-1.));
#6977=DIRECTION('center_axis',(0.,0.,1.));
#6978=DIRECTION('ref_axis',(0.409441503265782,-0.912336371851663,0.));
#6979=DIRECTION('',(0.,0.,-1.));
#6980=DIRECTION('center_axis',(0.,0.,1.));
#6981=DIRECTION('ref_axis',(0.409441503265782,-0.912336371851663,0.));
#6982=DIRECTION('',(0.,0.,-1.));
#6983=DIRECTION('center_axis',(0.,0.,1.));
#6984=DIRECTION('ref_axis',(0.409441503265782,-0.912336371851663,0.));
#6985=DIRECTION('',(0.,0.,-1.));
#6986=DIRECTION('center_axis',(0.,0.,1.));
#6987=DIRECTION('ref_axis',(0.409441503265782,-0.912336371851663,0.));
#6988=DIRECTION('',(0.,0.,-1.));
#6989=DIRECTION('center_axis',(0.,0.,1.));
#6990=DIRECTION('ref_axis',(0.409441503265782,-0.912336371851663,0.));
#6991=DIRECTION('',(0.,0.,-1.));
#6992=DIRECTION('center_axis',(0.,0.,1.));
#6993=DIRECTION('ref_axis',(0.409441503265782,-0.912336371851663,0.));
#6994=DIRECTION('',(0.,0.,-1.));
#6995=DIRECTION('center_axis',(0.,0.,1.));
#6996=DIRECTION('ref_axis',(0.409441503265782,-0.912336371851663,0.));
#6997=DIRECTION('',(0.,0.,-1.));
#6998=DIRECTION('center_axis',(0.,0.,1.));
#6999=DIRECTION('ref_axis',(0.409441503265782,-0.912336371851663,0.));
#7000=DIRECTION('',(0.,0.,-1.));
#7001=DIRECTION('center_axis',(0.,0.,1.));
#7002=DIRECTION('ref_axis',(0.409441503265782,-0.912336371851663,0.));
#7003=DIRECTION('',(0.,0.,-1.));
#7004=DIRECTION('center_axis',(0.,0.,1.));
#7005=DIRECTION('ref_axis',(0.409441503265782,-0.912336371851663,0.));
#7006=DIRECTION('',(0.,0.,-1.));
#7007=DIRECTION('center_axis',(0.,0.,1.));
#7008=DIRECTION('ref_axis',(0.409441503265782,-0.912336371851663,0.));
#7009=DIRECTION('',(0.,0.,-1.));
#7010=DIRECTION('center_axis',(0.,0.,1.));
#7011=DIRECTION('ref_axis',(0.409441503265782,-0.912336371851663,0.));
#7012=DIRECTION('',(0.,0.,-1.));
#7013=DIRECTION('center_axis',(0.,0.,1.));
#7014=DIRECTION('ref_axis',(0.409441503265782,-0.912336371851663,0.));
#7015=DIRECTION('',(0.,0.,-1.));
#7016=DIRECTION('center_axis',(0.,0.,1.));
#7017=DIRECTION('ref_axis',(0.409441503265782,-0.912336371851663,0.));
#7018=DIRECTION('',(0.,0.,-1.));
#7019=DIRECTION('center_axis',(0.,0.,1.));
#7020=DIRECTION('ref_axis',(0.409441503265782,-0.912336371851663,0.));
#7021=DIRECTION('',(0.,0.,-1.));
#7022=DIRECTION('center_axis',(0.,0.,1.));
#7023=DIRECTION('ref_axis',(0.409441503265782,-0.912336371851663,0.));
#7024=DIRECTION('',(0.,0.,-1.));
#7025=DIRECTION('center_axis',(0.,0.,1.));
#7026=DIRECTION('ref_axis',(0.409441503265782,-0.912336371851663,0.));
#7027=DIRECTION('',(0.,0.,-1.));
#7028=DIRECTION('center_axis',(0.,0.,1.));
#7029=DIRECTION('ref_axis',(0.409441503265782,-0.912336371851663,0.));
#7030=DIRECTION('',(0.,0.,-1.));
#7031=DIRECTION('center_axis',(0.,0.,1.));
#7032=DIRECTION('ref_axis',(0.409441503265782,-0.912336371851663,0.));
#7033=DIRECTION('',(0.,0.,-1.));
#7034=DIRECTION('center_axis',(0.,0.,1.));
#7035=DIRECTION('ref_axis',(0.409441503265782,-0.912336371851663,0.));
#7036=DIRECTION('',(0.,0.,-1.));
#7037=DIRECTION('center_axis',(0.,0.,1.));
#7038=DIRECTION('ref_axis',(0.409441503265782,-0.912336371851663,0.));
#7039=DIRECTION('',(0.,0.,-1.));
#7040=DIRECTION('center_axis',(0.,0.,1.));
#7041=DIRECTION('ref_axis',(0.409441503265782,-0.912336371851663,0.));
#7042=DIRECTION('',(0.,0.,-1.));
#7043=DIRECTION('center_axis',(0.,0.,1.));
#7044=DIRECTION('ref_axis',(0.409441503265782,-0.912336371851663,0.));
#7045=DIRECTION('',(0.,0.,-1.));
#7046=DIRECTION('center_axis',(0.,0.,1.));
#7047=DIRECTION('ref_axis',(0.409441503265782,-0.912336371851663,0.));
#7048=DIRECTION('',(0.,0.,-1.));
#7049=DIRECTION('center_axis',(0.,0.,1.));
#7050=DIRECTION('ref_axis',(1.,0.,0.));
#7051=DIRECTION('center_axis',(0.,0.,-1.));
#7052=DIRECTION('ref_axis',(1.,0.,0.));
#7053=DIRECTION('center_axis',(0.,0.,-1.));
#7054=DIRECTION('ref_axis',(1.,0.,0.));
#7055=DIRECTION('center_axis',(0.,0.,1.));
#7056=DIRECTION('ref_axis',(0.409441503265782,-0.912336371851663,0.));
#7057=DIRECTION('center_axis',(0.,0.,1.));
#7058=DIRECTION('ref_axis',(1.,-2.80853466614331E-13,0.));
#7059=DIRECTION('center_axis',(-1.60246890531964E-16,-1.,0.));
#7060=DIRECTION('ref_axis',(1.,-1.60246890531964E-16,0.));
#7061=DIRECTION('',(1.,-1.60246890531964E-16,0.));
#7062=DIRECTION('',(0.,0.,1.));
#7063=DIRECTION('',(1.,-1.60246890531964E-16,0.));
#7064=DIRECTION('',(0.,0.,1.));
#7065=DIRECTION('center_axis',(-0.866025403784439,-0.5,0.));
#7066=DIRECTION('ref_axis',(0.5,-0.866025403784439,0.));
#7067=DIRECTION('',(0.5,-0.866025403784439,0.));
#7068=DIRECTION('',(0.,0.,1.));
#7069=DIRECTION('',(0.5,-0.866025403784439,0.));
#7070=DIRECTION('center_axis',(-0.866025403784439,0.5,0.));
#7071=DIRECTION('ref_axis',(-0.5,-0.866025403784439,0.));
#7072=DIRECTION('',(-0.5,-0.866025403784439,0.));
#7073=DIRECTION('',(0.,0.,1.));
#7074=DIRECTION('',(-0.5,-0.866025403784439,0.));
#7075=DIRECTION('center_axis',(1.60246890531964E-16,1.,0.));
#7076=DIRECTION('ref_axis',(-1.,1.60246890531964E-16,0.));
#7077=DIRECTION('',(-1.,1.60246890531964E-16,0.));
#7078=DIRECTION('',(0.,0.,1.));
#7079=DIRECTION('',(-1.,1.60246890531964E-16,0.));
#7080=DIRECTION('center_axis',(0.866025403784439,0.5,0.));
#7081=DIRECTION('ref_axis',(-0.5,0.866025403784439,0.));
#7082=DIRECTION('',(-0.5,0.866025403784439,0.));
#7083=DIRECTION('',(0.,0.,1.));
#7084=DIRECTION('',(-0.5,0.866025403784439,0.));
#7085=DIRECTION('center_axis',(0.866025403784439,-0.5,0.));
#7086=DIRECTION('ref_axis',(0.5,0.866025403784439,0.));
#7087=DIRECTION('',(0.5,0.866025403784439,0.));
#7088=DIRECTION('',(0.5,0.866025403784439,0.));
#7089=DIRECTION('center_axis',(0.,0.,1.));
#7090=DIRECTION('ref_axis',(1.,0.,0.));
#7091=DIRECTION('center_axis',(0.,0.,1.));
#7092=DIRECTION('ref_axis',(1.,0.,0.));
#7093=DIRECTION('center_axis',(0.,0.,1.));
#7094=DIRECTION('ref_axis',(1.,0.,0.));
#7095=DIRECTION('center_axis',(0.,0.,1.));
#7096=DIRECTION('ref_axis',(1.,0.,0.));
#7097=DIRECTION('',(0.,0.,-1.));
#7098=DIRECTION('center_axis',(0.,0.,1.));
#7099=DIRECTION('ref_axis',(1.,0.,0.));
#7100=DIRECTION('center_axis',(0.,0.,1.));
#7101=DIRECTION('ref_axis',(1.,0.,0.));
#7102=DIRECTION('center_axis',(0.,0.,1.));
#7103=DIRECTION('ref_axis',(1.,0.,0.));
#8247=CARTESIAN_POINT('',(0.,0.,0.));
#8248=CARTESIAN_POINT('Origin',(0.,0.,-0.129405622560373));
#8249=CARTESIAN_POINT('',(-0.0636885943104742,0.141913936788308,0.0466443258702189));
#8250=CARTESIAN_POINT('',(-0.0636886258329924,0.141913922641526,0.0327905057321709));
#8251=CARTESIAN_POINT('',(-0.0636886258329924,0.141913922641526,-0.129405622560373));
#8252=CARTESIAN_POINT('',(-0.0887899522119582,-0.127719015366539,5.89805981832114E-17));
#8253=CARTESIAN_POINT('Ctrl Pts',(-0.0636885943104762,0.141913936788307,
0.046644325870219));
#8254=CARTESIAN_POINT('Ctrl Pts',(-0.0568706875042543,0.144973698996693,
0.0460674767969737));
#8255=CARTESIAN_POINT('Ctrl Pts',(-0.0498372314917207,0.147539905386712,
0.0454841194495339));
#8256=CARTESIAN_POINT('Ctrl Pts',(-0.0413488363880294,0.149959613661576,
0.0448074822562266));
#8257=CARTESIAN_POINT('Ctrl Pts',(-0.0400504322490268,0.150311593213423,
0.0447047356879959));
#8258=CARTESIAN_POINT('Ctrl Pts',(-0.0351567921767657,0.151570278540172,
0.0443206555495273));
#8259=CARTESIAN_POINT('Ctrl Pts',(-0.0315337316229291,0.152365280825276,
0.0440426625291857));
#8260=CARTESIAN_POINT('Ctrl Pts',(-0.0272702941063451,0.153142170667987,
0.0437254306071763));
#8261=CARTESIAN_POINT('Ctrl Pts',(-0.0266545361742012,0.153250543602531,
0.0436798532206328));
#8262=CARTESIAN_POINT('Ctrl Pts',(-0.0257193741345411,0.153409324446148,
0.0436110140072139));
#8263=CARTESIAN_POINT('Ctrl Pts',(-0.025400448699141,0.153462452228372,
0.0435876041457351));
#8264=CARTESIAN_POINT('Ctrl Pts',(-0.0248263790894383,0.153556244255832,
0.0435455891848324));
#8265=CARTESIAN_POINT('Ctrl Pts',(-0.0245712997285078,0.153597267167013,
0.0435269643365862));
#8266=CARTESIAN_POINT('Ctrl Pts',(-0.0240153248161858,0.153685260886435,
0.0434864647056545));
#8267=CARTESIAN_POINT('Ctrl Pts',(-0.0237143940782576,0.153731983521882,
0.0434646040589109));
#8268=CARTESIAN_POINT('Ctrl Pts',(-0.0228663427562202,0.153861102926211,
0.0434031639073866));
#8269=CARTESIAN_POINT('Ctrl Pts',(-0.0223189094731189,0.153941465919114,
0.0433636966382276));
#8270=CARTESIAN_POINT('Ctrl Pts',(-0.0189956769671261,0.154411215091918,
0.0431252161329079));
#8271=CARTESIAN_POINT('Ctrl Pts',(-0.0162099741319758,0.154728466865676,
0.0429299935086839));
#8272=CARTESIAN_POINT('Ctrl Pts',(0.00124647087156192,0.156239808213013,
0.0417272042602695));
#8273=CARTESIAN_POINT('Ctrl Pts',(0.0160171008148657,0.155421956466042,
0.0407933739561897));
#8274=CARTESIAN_POINT('Ctrl Pts',(0.0357815183452902,0.151476070394245,
0.0394361505080405));
#8275=CARTESIAN_POINT('Ctrl Pts',(0.0410491476710349,0.150134185089699,
0.0390643164092514));
#8276=CARTESIAN_POINT('Ctrl Pts',(0.0471445959753226,0.148236622932751,
0.0386166913475808));
#8277=CARTESIAN_POINT('Ctrl Pts',(0.048051184941417,0.147945236025617,0.0385496598891293));
#8278=CARTESIAN_POINT('Ctrl Pts',(0.0495196256884408,0.147458343246464,
0.0384403167580589));
#8279=CARTESIAN_POINT('Ctrl Pts',(0.0500831419342288,0.147267902808322,
0.0383981708569045));
#8280=CARTESIAN_POINT('Ctrl Pts',(0.0510844363447539,0.146923103460167,
0.0383229459682699));
#8281=CARTESIAN_POINT('Ctrl Pts',(0.0515226445693025,0.146770007341707,
0.038289908868643));
#8282=CARTESIAN_POINT('Ctrl Pts',(0.0524442928143612,0.146443376353324,
0.0382201774063333));
#8283=CARTESIAN_POINT('Ctrl Pts',(0.0529275707304974,0.146269404085352,
0.0381834689226026));
#8284=CARTESIAN_POINT('Ctrl Pts',(0.054202914277151,0.145803152834494,0.0380862108751925));
#8285=CARTESIAN_POINT('Ctrl Pts',(0.0549934676451898,0.145506816874414,
0.0380255273703788));
#8286=CARTESIAN_POINT('Ctrl Pts',(0.0586455792660056,0.144103822642237,
0.0377433135274135));
#8287=CARTESIAN_POINT('Ctrl Pts',(0.061476221414232,0.142919163836473,0.0375191986505781));
#8288=CARTESIAN_POINT('Ctrl Pts',(0.0774315956669701,0.135679934608843,
0.036223664566306));
#8289=CARTESIAN_POINT('Ctrl Pts',(0.0896951437222894,0.127903540121908,
0.0350913654422326));
#8290=CARTESIAN_POINT('Ctrl Pts',(0.105061585360943,0.114850011548946,0.0335398665531906));
#8291=CARTESIAN_POINT('Ctrl Pts',(0.109210447074238,0.110912385410338,0.0331057258356621));
#8292=CARTESIAN_POINT('Ctrl Pts',(0.113608594865368,0.106251440848463,0.0326360161345161));
#8293=CARTESIAN_POINT('Ctrl Pts',(0.114080237597373,0.105744886152826,0.032585516938738));
#8294=CARTESIAN_POINT('Ctrl Pts',(0.11477336334011,0.104990418825038,0.0325111330022006));
#8295=CARTESIAN_POINT('Ctrl Pts',(0.11499744915996,0.104744926701814,0.0324870581311852));
#8296=CARTESIAN_POINT('Ctrl Pts',(0.115393969483804,0.104307721624725,0.0324444129315734));
#8297=CARTESIAN_POINT('Ctrl Pts',(0.115566716870844,0.104116295264915,0.0324258190496426));
#8298=CARTESIAN_POINT('Ctrl Pts',(0.115935176202657,0.103705947972701,0.0323861283601505));
#8299=CARTESIAN_POINT('Ctrl Pts',(0.116130744868572,0.103486901713488,0.0323650423753064));
#8300=CARTESIAN_POINT('Ctrl Pts',(0.116667285269238,0.102882514513061,0.0323071358146115));
#8301=CARTESIAN_POINT('Ctrl Pts',(0.117006971450516,0.102496028688104,0.0322704106681944));
#8302=CARTESIAN_POINT('Ctrl Pts',(0.118829898217057,0.100401078566248,0.0320729299171071));
#8303=CARTESIAN_POINT('Ctrl Pts',(0.120277748849068,0.0986619778996509,
0.0319146577500692));
#8304=CARTESIAN_POINT('Ctrl Pts',(0.130437515508156,0.0859022380018732,
0.0307882427301412));
#8305=CARTESIAN_POINT('Ctrl Pts',(0.13765988439999,0.0737767332478561,0.0298957087520044));
#8306=CARTESIAN_POINT('Ctrl Pts',(0.145820741216985,0.0545757551836579,
0.0285039182135418));
#8307=CARTESIAN_POINT('Ctrl Pts',(0.148070190666843,0.0481393836691937,
0.0280415146952546));
#8308=CARTESIAN_POINT('Ctrl Pts',(0.150157317995708,0.0406150079109869,
0.0274945939492325));
#8309=CARTESIAN_POINT('Ctrl Pts',(0.150414869932778,0.0396505464712973,
0.0274243838614422));
#8310=CARTESIAN_POINT('Ctrl Pts',(0.150812075043454,0.0381035338796276,
0.0273115638515942));
#8311=CARTESIAN_POINT('Ctrl Pts',(0.150957680204654,0.0375225271263452,
0.0272691471353898));
#8312=CARTESIAN_POINT('Ctrl Pts',(0.151209698811495,0.0364916860455356,
0.0271938032756404));
#8313=CARTESIAN_POINT('Ctrl Pts',(0.151317470305596,0.0360421882925573,
0.0271609205117994));
#8314=CARTESIAN_POINT('Ctrl Pts',(0.151537300894291,0.035106942954735,0.0270924394105436));
#8315=CARTESIAN_POINT('Ctrl Pts',(0.151649031450763,0.0346211244076252,
0.0270568308784482));
#8316=CARTESIAN_POINT('Ctrl Pts',(0.151931981890424,0.0333631666977353,
0.0269645309005217));
#8317=CARTESIAN_POINT('Ctrl Pts',(0.152099649686521,0.0325902521513084,
0.0269077258040014));
#8318=CARTESIAN_POINT('Ctrl Pts',(0.152791815876093,0.0292777725240725,
0.0266638468777155));
#8319=CARTESIAN_POINT('Ctrl Pts',(0.153258629729472,0.0267267255748599,
0.0264749410446673));
#8320=CARTESIAN_POINT('Ctrl Pts',(0.15432002483048,0.0199775760837909,0.0259719459324084));
#8321=CARTESIAN_POINT('Ctrl Pts',(0.154807078932913,0.0157650218380878,
0.0256546958910069));
#8322=CARTESIAN_POINT('Ctrl Pts',(0.155990495241355,-0.000145061447557968,
0.0244446576807383));
#8323=CARTESIAN_POINT('Ctrl Pts',(0.155536710792408,-0.0118887813816597,
0.023524005431808));
#8324=CARTESIAN_POINT('Ctrl Pts',(0.153047927123364,-0.0281958210189353,
0.022260263756572));
#8325=CARTESIAN_POINT('Ctrl Pts',(0.152108692168808,-0.0328881310512085,
0.0218989631250029));
#8326=CARTESIAN_POINT('Ctrl Pts',(0.150796977338198,-0.038164129955926,
0.0215005883543145));
#8327=CARTESIAN_POINT('Ctrl Pts',(0.150635378084855,-0.0387970630280932,
0.0214529292213288));
#8328=CARTESIAN_POINT('Ctrl Pts',(0.150387512308824,-0.0397429743179642,
0.021381919701207));
#8329=CARTESIAN_POINT('Ctrl Pts',(0.15030424830047,-0.0400567199625435,
0.021358402603714));
#8330=CARTESIAN_POINT('Ctrl Pts',(0.150154697699623,-0.0406132068729712,
0.0213167569614059));
#8331=CARTESIAN_POINT('Ctrl Pts',(0.150088804241103,-0.0408560479998004,
0.0212986062025822));
#8332=CARTESIAN_POINT('Ctrl Pts',(0.15002217775146,-0.0410992540443237,
0.0212804509122708));
#8333=CARTESIAN_POINT('Ctrl Pts',(0.150022035316903,-0.0410997739612348,
0.0212804121006641));
#8334=CARTESIAN_POINT('Ctrl Pts',(0.1500217861134,-0.0411006835893117,0.0212803441974421));
#8335=CARTESIAN_POINT('Ctrl Pts',(0.150021679365621,-0.0411010732278623,
0.0212803151112024));
#8336=CARTESIAN_POINT('Ctrl Pts',(0.149945988073925,-0.041377348713481,
0.0212596913844328));
#8337=CARTESIAN_POINT('Ctrl Pts',(0.149869641824313,-0.0416530285702638,
0.021239141158709));
#8338=CARTESIAN_POINT('Ctrl Pts',(0.149660083720702,-0.0424016897444627,
0.0211834081084647));
#8339=CARTESIAN_POINT('Ctrl Pts',(0.149525388905231,-0.0428742585092002,
0.0211483098705703));
#8340=CARTESIAN_POINT('Ctrl Pts',(0.148852441292606,-0.0451935074389334,
0.0209764210814314));
#8341=CARTESIAN_POINT('Ctrl Pts',(0.148282175366296,-0.0470308385630788,
0.0208413871428836));
#8342=CARTESIAN_POINT('Ctrl Pts',(0.146547663600301,-0.0522736475130693,
0.0204580775309201));
#8343=CARTESIAN_POINT('Ctrl Pts',(0.145299081924695,-0.0556500929327148,
0.020213674159934));
#8344=CARTESIAN_POINT('Ctrl Pts',(0.141222836798195,-0.0655976606615059,
0.0194925501555046));
#8345=CARTESIAN_POINT('Ctrl Pts',(0.138058054156169,-0.0720203169219205,
0.0190252143776118));
#8346=CARTESIAN_POINT('Ctrl Pts',(0.129207914896176,-0.0872373344194798,
0.0178651299980061));
#8347=CARTESIAN_POINT('Ctrl Pts',(0.123057151797318,-0.095717941047913,
0.017169351109896));
#8348=CARTESIAN_POINT('Ctrl Pts',(0.115340690505904,-0.104372606189801,
0.0163572971506247));
#8349=CARTESIAN_POINT('Ctrl Pts',(0.114568628014315,-0.105219509408824,
0.0162766613466596));
#8350=CARTESIAN_POINT('Ctrl Pts',(0.113387102756084,-0.10648714444917,0.0161541320151808));
#8351=CARTESIAN_POINT('Ctrl Pts',(0.112984487424815,-0.106914230056936,
0.0161125285405117));
#8352=CARTESIAN_POINT('Ctrl Pts',(0.112259071133417,-0.107675062232297,
0.0160378289602106));
#8353=CARTESIAN_POINT('Ctrl Pts',(0.111937172987326,-0.10800966333412,0.0160047718486466));
#8354=CARTESIAN_POINT('Ctrl Pts',(0.111251383395406,-0.108716157548238,
0.0159345323623914));
#8355=CARTESIAN_POINT('Ctrl Pts',(0.1108871151897,-0.109087675253784,0.0158973338766515));
#8356=CARTESIAN_POINT('Ctrl Pts',(0.109908362866084,-0.110075938493984,
0.0157976733317111));
#8357=CARTESIAN_POINT('Ctrl Pts',(0.109290561071052,-0.110689356611725,
0.0157350663452626));
#8358=CARTESIAN_POINT('Ctrl Pts',(0.106272703409519,-0.113635904194289,
0.0154306438519125));
#8359=CARTESIAN_POINT('Ctrl Pts',(0.103803085387429,-0.115896171158918,
0.0151857395511717));
#8360=CARTESIAN_POINT('Ctrl Pts',(0.0897245142846927,-0.127970149818489,
0.0138109281765094));
#8361=CARTESIAN_POINT('Ctrl Pts',(0.0767990645433999,-0.136119732114037,
0.0126146394232799));
#8362=CARTESIAN_POINT('Ctrl Pts',(0.0587395372212553,-0.144104772115435,
0.0111057763044583));
#8363=CARTESIAN_POINT('Ctrl Pts',(0.0544975130973068,-0.145761960890926,
0.0107627464206152));
#8364=CARTESIAN_POINT('Ctrl Pts',(0.0495685260728842,-0.147442167242722,
0.0103813898888732));
#8365=CARTESIAN_POINT('Ctrl Pts',(0.0489472619512179,-0.147649575164198,
0.0103336304574409));
#8366=CARTESIAN_POINT('Ctrl Pts',(0.0480124011775435,-0.147955127578881,
0.0102622435689829));
#8367=CARTESIAN_POINT('Ctrl Pts',(0.0476997840424651,-0.148056209094316,
0.0102384521091382));
#8368=CARTESIAN_POINT('Ctrl Pts',(0.0471404052402745,-0.148235122826344,
0.0101960272985566));
#8369=CARTESIAN_POINT('Ctrl Pts',(0.0468937721907758,-0.148313329059141,
0.0101773729345747));
#8370=CARTESIAN_POINT('Ctrl Pts',(0.0466455424533205,-0.148391360501144,
0.0101586483329417));
#8371=CARTESIAN_POINT('Ctrl Pts',(0.0466441453019813,-0.148391799676372,
0.0101585429438606));
#8372=CARTESIAN_POINT('Ctrl Pts',(0.0466413718085115,-0.148392671442702,
0.0101583337385513));
#8373=CARTESIAN_POINT('Ctrl Pts',(0.0466399954679868,-0.14839310403394,
0.0101582299223967));
#8374=CARTESIAN_POINT('Ctrl Pts',(0.0466372631672831,-0.148393962768995,
0.0101580238304495));
#8375=CARTESIAN_POINT('Ctrl Pts',(0.0466359072077521,-0.148394388913227,
0.0101579215546601));
#8376=CARTESIAN_POINT('Ctrl Pts',(0.0466332152539379,-0.148395234886573,
0.0101577185119968));
#8377=CARTESIAN_POINT('Ctrl Pts',(0.0466318792582104,-0.148395654716736,
0.0101576177449698));
#8378=CARTESIAN_POINT('Ctrl Pts',(0.0466292268259325,-0.148396488191331,
0.0101574176890716));
#8379=CARTESIAN_POINT('Ctrl Pts',(0.046627910388248,-0.148396901836695,
0.0101573184000722));
#8380=CARTESIAN_POINT('Ctrl Pts',(0.046625296669606,-0.148397723069865,
0.0101571212697479));
#8381=CARTESIAN_POINT('Ctrl Pts',(0.0466239993912728,-0.148398130657403,
0.0101570234285797));
#8382=CARTESIAN_POINT('Ctrl Pts',(0.0466214236110177,-0.148398939896072,
0.0101568291651111));
#8383=CARTESIAN_POINT('Ctrl Pts',(0.0466201451079589,-0.148399341548097,
0.0101567327426853));
#8384=CARTESIAN_POINT('Ctrl Pts',(0.0466176065015387,-0.14840013903569,
0.0101565412881715));
#8385=CARTESIAN_POINT('Ctrl Pts',(0.0466163463984353,-0.148400534871697,
0.0101564462560646));
#8386=CARTESIAN_POINT('Ctrl Pts',(0.0466138442202533,-0.148401320845554,
0.0101562575540438));
#8387=CARTESIAN_POINT('Ctrl Pts',(0.0466126021480873,-0.148401710982991,
0.0101561638843125));
#8388=CARTESIAN_POINT('Ctrl Pts',(0.0466101356848381,-0.14840248567018,
0.0101559778807678));
#8389=CARTESIAN_POINT('Ctrl Pts',(0.0466089112902633,-0.148402870221514,
0.0101558855466552));
#8390=CARTESIAN_POINT('Ctrl Pts',(0.0466064798309384,-0.148403633848262,
0.0101557021877516));
#8391=CARTESIAN_POINT('Ctrl Pts',(0.046605272765933,-0.148404012924226,
0.0101556111629068));
#8392=CARTESIAN_POINT('Ctrl Pts',(0.0466028756256244,-0.148404765708445,
0.0101554303967867));
#8393=CARTESIAN_POINT('Ctrl Pts',(0.0466016855514885,-0.148405139416787,
0.010155340655566));
#8394=CARTESIAN_POINT('Ctrl Pts',(0.0465993220602246,-0.148405881571588,
0.0101551624315061));
#8395=CARTESIAN_POINT('Ctrl Pts',(0.0465981486452686,-0.148406250017801,
0.0101550739487984));
#8396=CARTESIAN_POINT('Ctrl Pts',(0.0465958181561974,-0.148406981748924,
0.0101548982178271));
#8397=CARTESIAN_POINT('Ctrl Pts',(0.046594661080117,-0.148407345034873,
0.010154810969384));
#8398=CARTESIAN_POINT('Ctrl Pts',(0.0465923629565717,-0.148408066544758,
0.0101546376833051));
#8399=CARTESIAN_POINT('Ctrl Pts',(0.0465912219070507,-0.148408424769749,
0.010154551645484));
#8400=CARTESIAN_POINT('Ctrl Pts',(0.0465889555256895,-0.148409136256554,
0.0101543807571137));
#8401=CARTESIAN_POINT('Ctrl Pts',(0.0465878301955188,-0.14840948951824,
0.0101542959066611));
#8402=CARTESIAN_POINT('Ctrl Pts',(0.0465855949552014,-0.148410191173057,
0.0101541273704966));
#8403=CARTESIAN_POINT('Ctrl Pts',(0.0465844850461195,-0.148410539566235,
0.0101540436848368));
#8404=CARTESIAN_POINT('Ctrl Pts',(0.0465822803588516,-0.148411231575936,
0.0101538774563735));
#8405=CARTESIAN_POINT('Ctrl Pts',(0.0465811855808898,-0.148411575192757,
0.0101537949135595));
#8406=CARTESIAN_POINT('Ctrl Pts',(0.0465790108671126,-0.148412257741477,
0.0101536309489353));
#8407=CARTESIAN_POINT('Ctrl Pts',(0.0465779309332553,-0.148412596673119,
0.0101535495272461));
#8408=CARTESIAN_POINT('Ctrl Pts',(0.0462855042456526,-0.148504369766908,
0.0101315022555262));
#8409=CARTESIAN_POINT('Ctrl Pts',(0.045993885571223,-0.148594946877211,
0.0101095855078975));
#8410=CARTESIAN_POINT('Ctrl Pts',(0.0451710318809876,-0.148847871804948,
0.0100479345324943));
#8411=CARTESIAN_POINT('Ctrl Pts',(0.0446391841159549,-0.14900823577186,
0.0100083107017172));
#8412=CARTESIAN_POINT('Ctrl Pts',(0.0415404932451031,-0.149924480561179,
0.00977868969122265));
#8413=CARTESIAN_POINT('Ctrl Pts',(0.0389551547198484,-0.150616933343872,
0.00959203927228974));
#8414=CARTESIAN_POINT('Ctrl Pts',(0.0208776402604556,-0.154962094998815,
0.00831261627153842));
#8415=CARTESIAN_POINT('Ctrl Pts',(0.00492201038245046,-0.156285049961146,
0.00730396116553906));
#8416=CARTESIAN_POINT('Ctrl Pts',(-0.0149121393797758,-0.154884285211148,
0.00594895935770095));
#8417=CARTESIAN_POINT('Ctrl Pts',(-0.0188535971841461,-0.154454042139276,
0.0056752698206136));
#8418=CARTESIAN_POINT('Ctrl Pts',(-0.0237223738176185,-0.153733439655815,
0.00532961666321505));
#8419=CARTESIAN_POINT('Ctrl Pts',(-0.0246693454163375,-0.153584324763353,
0.00526203192250643));
#8420=CARTESIAN_POINT('Ctrl Pts',(-0.0261568474217181,-0.153335983288259,
0.00515528200138179));
#8421=CARTESIAN_POINT('Ctrl Pts',(-0.0266983452501157,-0.153242627180339,
0.0051162987199291));
#8422=CARTESIAN_POINT('Ctrl Pts',(-0.0276539843532365,-0.153072652770617,
0.00504727817049372));
#8423=CARTESIAN_POINT('Ctrl Pts',(-0.028068332820119,-0.152997217501706,
0.0050172779711637));
#8424=CARTESIAN_POINT('Ctrl Pts',(-0.0290176366931578,-0.152820403463939,
0.00494837240085321));
#8425=CARTESIAN_POINT('Ctrl Pts',(-0.0295523737923494,-0.152717897260602,
0.004909432220776));
#8426=CARTESIAN_POINT('Ctrl Pts',(-0.0310303763384798,-0.15242651889748,
0.00480144636119746));
#8427=CARTESIAN_POINT('Ctrl Pts',(-0.0319724308261527,-0.152231703366812,
0.00473221574503593));
#8428=CARTESIAN_POINT('Ctrl Pts',(-0.0373153219638589,-0.151075020128567,
0.00433721632589114));
#8429=CARTESIAN_POINT('Ctrl Pts',(-0.0416741038301823,-0.149931172198991,
0.00400576933909942));
#8430=CARTESIAN_POINT('Ctrl Pts',(-0.0612423353659838,-0.14387677254724,
0.00247333227659507));
#8431=CARTESIAN_POINT('Ctrl Pts',(-0.0756810659941349,-0.136832281527354,
0.00120507771614184));
#8432=CARTESIAN_POINT('Ctrl Pts',(-0.0887899522119582,-0.127719015366539,
5.89805981832114E-17));
#8433=CARTESIAN_POINT('',(0.090360677865021,-0.126612599672283,0.));
#8434=CARTESIAN_POINT('Origin',(0.,0.,0.));
#8435=CARTESIAN_POINT('Ctrl Pts',(0.0903606778650134,-0.126612599672289,
0.));
#8436=CARTESIAN_POINT('Ctrl Pts',(0.0989406669312652,-0.12048924678239,
0.000754967019532015));
#8437=CARTESIAN_POINT('Ctrl Pts',(0.106907661992801,-0.113481681412107,
0.00150993403906405));
#8438=CARTESIAN_POINT('Ctrl Pts',(0.114086638781495,-0.105735714645245,
0.00226490105859606));
#8439=CARTESIAN_POINT('Ctrl Pts',(0.12126935076715,-0.0979857176784843,
0.00302026088487475));
#8440=CARTESIAN_POINT('Ctrl Pts',(0.127662609751503,-0.0894971609184212,
0.00377562071115349));
#8441=CARTESIAN_POINT('Ctrl Pts',(0.13312848579982,-0.0804525249364313,
0.00453098053743217));
#8442=CARTESIAN_POINT('Ctrl Pts',(0.138594284951268,-0.0714080161992201,
0.00528632973690464));
#8443=CARTESIAN_POINT('Ctrl Pts',(0.143132299633338,-0.061808197917734,
0.00604167893637711));
#8444=CARTESIAN_POINT('Ctrl Pts',(0.146649814579393,-0.0518616851233123,
0.00679702813584959));
#8445=CARTESIAN_POINT('Ctrl Pts',(0.150178599016343,-0.0418833054748524,
0.007554797339517));
#8446=CARTESIAN_POINT('Ctrl Pts',(0.152680093031621,-0.0315568445592943,
0.0083125665431844));
#8447=CARTESIAN_POINT('Ctrl Pts',(0.154111282327439,-0.0211072300265195,
0.00907033574685182));
#8448=CARTESIAN_POINT('Ctrl Pts',(0.155398345573063,-0.0117099302875016,
0.00975179479182663));
#8449=CARTESIAN_POINT('Ctrl Pts',(0.155820496503437,-0.00221365697179131,
0.0104332538368014));
#8450=CARTESIAN_POINT('Ctrl Pts',(0.155382497872137,0.0072167759432721,
0.0111147128817762));
#8451=CARTESIAN_POINT('Ctrl Pts',(0.154913520415882,0.0173142057611671,
0.0118443702519497));
#8452=CARTESIAN_POINT('Ctrl Pts',(0.153453826316537,0.0274118070963533,
0.0125740276221232));
#8453=CARTESIAN_POINT('Ctrl Pts',(0.151012327303487,0.0372971782094091,
0.0133036849922967));
#8454=CARTESIAN_POINT('Ctrl Pts',(0.148523466529631,0.0473743120795403,
0.0140474967232347));
#8455=CARTESIAN_POINT('Ctrl Pts',(0.145014246588351,0.0572298640738792,
0.0147913084541726));
#8456=CARTESIAN_POINT('Ctrl Pts',(0.14054958495577,0.0666454549745192,0.0155351201851106));
#8457=CARTESIAN_POINT('Ctrl Pts',(0.13618211944294,0.0758560675417475,0.0162627390620271));
#8458=CARTESIAN_POINT('Ctrl Pts',(0.130900902593814,0.0846448311825029,
0.0169903579389437));
#8459=CARTESIAN_POINT('Ctrl Pts',(0.124815278386068,0.092827521680848,0.0177179768158602));
#8460=CARTESIAN_POINT('Ctrl Pts',(0.118526504643136,0.101283365715225,0.0184698849738089));
#8461=CARTESIAN_POINT('Ctrl Pts',(0.111379145922307,0.109090974738866,0.0192217931317575));
#8462=CARTESIAN_POINT('Ctrl Pts',(0.103539598349753,0.116083392755259,0.0199737012897062));
#8463=CARTESIAN_POINT('Ctrl Pts',(0.0957000507771991,0.123075810771653,
0.0207256094476549));
#8464=CARTESIAN_POINT('Ctrl Pts',(0.0871692388652433,0.129252422489904,
0.0214775176056037));
#8465=CARTESIAN_POINT('Ctrl Pts',(0.0781478618527984,0.134494290539918,
0.0222294257635524));
#8466=CARTESIAN_POINT('Ctrl Pts',(0.0692877936203789,0.139642430178069,
0.0229678892569579));
#8467=CARTESIAN_POINT('Ctrl Pts',(0.0598842350155881,0.143930256984207,
0.0237063527503634));
#8468=CARTESIAN_POINT('Ctrl Pts',(0.0501269156700459,0.14725180754547,0.0244448162437689));
#8469=CARTESIAN_POINT('Ctrl Pts',(0.040384345395474,0.150568337282547,0.0251821634827927));
#8470=CARTESIAN_POINT('Ctrl Pts',(0.0302899137296858,0.152921108078114,
0.0259195107218165));
#8471=CARTESIAN_POINT('Ctrl Pts',(0.0200541531958801,0.154251850684509,
0.0266568579608404));
#8472=CARTESIAN_POINT('Ctrl Pts',(0.00982881691130718,0.155581238043042,
0.0273934542745797));
#8473=CARTESIAN_POINT('Ctrl Pts',(-0.00053664974832034,0.155890524510869,
0.028130050588319));
#8474=CARTESIAN_POINT('Ctrl Pts',(-0.0108238371310163,0.155172958500382,
0.0288666469020583));
#8475=CARTESIAN_POINT('Ctrl Pts',(-0.0211310953995098,0.154453992477928,
0.0296046803569658));
#8476=CARTESIAN_POINT('Ctrl Pts',(-0.0313588440257055,0.152704250068778,
0.0303427138118732));
#8477=CARTESIAN_POINT('Ctrl Pts',(-0.041292688961979,0.149969051268218,
0.0310807472667807));
#8478=CARTESIAN_POINT('Ctrl Pts',(-0.0489637393553047,0.147856893491499,
0.0316506667552441));
#8479=CARTESIAN_POINT('Ctrl Pts',(-0.0564595315799098,0.14515822080781,
0.0322205862437075));
#8480=CARTESIAN_POINT('Ctrl Pts',(-0.0636886258329924,0.141913922641526,
0.0327905057321709));
#8481=CARTESIAN_POINT('Origin',(0.,0.,-0.129405622560373));
#8482=CARTESIAN_POINT('',(-0.0636886257863082,0.141913922662477,0.116740348554263));
#8483=CARTESIAN_POINT('',(-0.0636886551490397,0.141913909484965,0.102789135277549));
#8484=CARTESIAN_POINT('',(-0.0636886258329924,0.141913922641526,-0.129405622560373));
#8485=CARTESIAN_POINT('Ctrl Pts',(-0.0636886257863082,0.141913922662477,
0.116740348554263));
#8486=CARTESIAN_POINT('Ctrl Pts',(-0.0620424217405237,0.14265271186281,
0.116615168449032));
#8487=CARTESIAN_POINT('Ctrl Pts',(-0.060383508450654,0.143362791762632,
0.116489085809456));
#8488=CARTESIAN_POINT('Ctrl Pts',(-0.0580251874220437,0.144324049354148,
0.116309752685824));
#8489=CARTESIAN_POINT('Ctrl Pts',(-0.0573357548266734,0.144599324969004,
0.116257315595819));
#8490=CARTESIAN_POINT('Ctrl Pts',(-0.0562406645258442,0.145027507962682,
0.116173995856029));
#8491=CARTESIAN_POINT('Ctrl Pts',(-0.0558362859078551,0.145183675326336,
0.116143222574248));
#8492=CARTESIAN_POINT('Ctrl Pts',(-0.0550009614651376,0.14550226400819,
0.116079638619344));
#8493=CARTESIAN_POINT('Ctrl Pts',(-0.0545699370206578,0.145664465669511,
0.116046820987017));
#8494=CARTESIAN_POINT('Ctrl Pts',(-0.0536046374289098,0.146022838204867,
0.115973301883517));
#8495=CARTESIAN_POINT('Ctrl Pts',(-0.0530699954896766,0.146217994768411,
0.115932567177777));
#8496=CARTESIAN_POINT('Ctrl Pts',(-0.0517144100575374,0.146704400279421,
0.115829238947803));
#8497=CARTESIAN_POINT('Ctrl Pts',(-0.0508920781983923,0.146991692242151,
0.115766515520857));
#8498=CARTESIAN_POINT('Ctrl Pts',(-0.0462264976389446,0.148577827833571,
0.115410366051632));
#8499=CARTESIAN_POINT('Ctrl Pts',(-0.0423363550000382,0.149732719843836,
0.11511227047896));
#8500=CARTESIAN_POINT('Ctrl Pts',(-0.0365936699490618,0.15119590928656,
0.114670077836691));
#8501=CARTESIAN_POINT('Ctrl Pts',(-0.0347733839474204,0.151624902111698,
0.114529616664305));
#8502=CARTESIAN_POINT('Ctrl Pts',(-0.018532365430285,0.15514464355927,0.113273956077463));
#8503=CARTESIAN_POINT('Ctrl Pts',(-0.00375017290465386,0.156202328724143,
0.112104252392861));
#8504=CARTESIAN_POINT('Ctrl Pts',(0.0135060121633154,0.154983584715789,
0.110803350586831));
#8505=CARTESIAN_POINT('Ctrl Pts',(0.0160487586668345,0.154740955461415,
0.110613591171677));
#8506=CARTESIAN_POINT('Ctrl Pts',(0.0191202559914391,0.154371336158605,
0.110387594302892));
#8507=CARTESIAN_POINT('Ctrl Pts',(0.0196556150860335,0.154304084312003,
0.110348322492503));
#8508=CARTESIAN_POINT('Ctrl Pts',(0.0204887762746792,0.154195016018532,
0.110287401994921));
#8509=CARTESIAN_POINT('Ctrl Pts',(0.0207868182158148,0.154155120287452,
0.110265648549342));
#8510=CARTESIAN_POINT('Ctrl Pts',(0.0213401906058271,0.154079412116607,
0.110225334398859));
#8511=CARTESIAN_POINT('Ctrl Pts',(0.0215955451519675,0.154043829492524,
0.110206761463916));
#8512=CARTESIAN_POINT('Ctrl Pts',(0.0221735181575856,0.153961825870212,
0.110164790378353));
#8513=CARTESIAN_POINT('Ctrl Pts',(0.022496079293076,0.153915025759317,0.110141413858272));
#8514=CARTESIAN_POINT('Ctrl Pts',(0.023471178059506,0.153770418691644,0.110070882932183));
#8515=CARTESIAN_POINT('Ctrl Pts',(0.0241232542399938,0.153669471628086,
0.110023901317037));
#8516=CARTESIAN_POINT('Ctrl Pts',(0.0291301855315081,0.152861698739198,
0.109664435415316));
#8517=CARTESIAN_POINT('Ctrl Pts',(0.0334543419803127,0.151973954159337,
0.109361424648245));
#8518=CARTESIAN_POINT('Ctrl Pts',(0.0520779461492593,0.147316878891845,
0.108065797467015));
#8519=CARTESIAN_POINT('Ctrl Pts',(0.0658360290695337,0.141704062681687,
0.107125770940083));
#8520=CARTESIAN_POINT('Ctrl Pts',(0.0819844109561111,0.132248931608589,
0.105851090010686));
#8521=CARTESIAN_POINT('Ctrl Pts',(0.085296588201257,0.130137277885921,0.105579892784939));
#8522=CARTESIAN_POINT('Ctrl Pts',(0.0892757280571787,0.127383202256364,
0.105239884234909));
#8523=CARTESIAN_POINT('Ctrl Pts',(0.0900217455712659,0.126857089270066,
0.10517550248814));
#8524=CARTESIAN_POINT('Ctrl Pts',(0.091191820718928,0.126016399931856,0.105073491205992));
#8525=CARTESIAN_POINT('Ctrl Pts',(0.0916189904716938,0.12570617244299,0.10503602875127));
#8526=CARTESIAN_POINT('Ctrl Pts',(0.0924157990538203,0.125121279781125,
0.104965730633107));
#8527=CARTESIAN_POINT('Ctrl Pts',(0.0927858145336516,0.124847135256586,
0.104932915401712));
#8528=CARTESIAN_POINT('Ctrl Pts',(0.0936097381018163,0.124231004254791,
0.104859458681007));
#8529=CARTESIAN_POINT('Ctrl Pts',(0.094062998284304,0.123888166600215,0.104818784236378));
#8530=CARTESIAN_POINT('Ctrl Pts',(0.0952040084068251,0.123015256188798,
0.104715715820081));
#8531=CARTESIAN_POINT('Ctrl Pts',(0.0958892096394038,0.122481900253955,
0.104653193107215));
#8532=CARTESIAN_POINT('Ctrl Pts',(0.0997178081236886,0.119449927700367,
0.104300245200098));
#8533=CARTESIAN_POINT('Ctrl Pts',(0.102767714767939,0.116836286286229,0.104005248543059));
#8534=CARTESIAN_POINT('Ctrl Pts',(0.107112586733107,0.112811067830142,0.103563450863328));
#8535=CARTESIAN_POINT('Ctrl Pts',(0.108488276448277,0.11148872862088,0.103420161536768));
#8536=CARTESIAN_POINT('Ctrl Pts',(0.120263270408494,0.0997460443329424,
0.102163703646519));
#8537=CARTESIAN_POINT('Ctrl Pts',(0.129157277509931,0.0879252375315936,
0.100996246852023));
#8538=CARTESIAN_POINT('Ctrl Pts',(0.137506680229921,0.0727628020848725,
0.0996941507690236));
#8539=CARTESIAN_POINT('Ctrl Pts',(0.138699407337796,0.0704626782054384,
0.0995016226795695));
#8540=CARTESIAN_POINT('Ctrl Pts',(0.140070380004365,0.0676489604699325,
0.0992729768596523));
#8541=CARTESIAN_POINT('Ctrl Pts',(0.140304030234754,0.067163028001066,0.0992337329494705));
#8542=CARTESIAN_POINT('Ctrl Pts',(0.140664010968958,0.0664042836522418,
0.0991728461428898));
#8543=CARTESIAN_POINT('Ctrl Pts',(0.140792082175231,0.0661323103345795,
0.0991510986731898));
#8544=CARTESIAN_POINT('Ctrl Pts',(0.141028515351933,0.0656264185744549,
0.0991107927785622));
#8545=CARTESIAN_POINT('Ctrl Pts',(0.141137083211397,0.0653926043351209,
0.0990922221368308));
#8546=CARTESIAN_POINT('Ctrl Pts',(0.141381613834733,0.0648625317080488,
0.0990502515201702));
#8547=CARTESIAN_POINT('Ctrl Pts',(0.14151722668911,0.0645661157697593,0.0990268731973769));
#8548=CARTESIAN_POINT('Ctrl Pts',(0.141924684838699,0.0636680625841192,
0.0989563138682866));
#8549=CARTESIAN_POINT('Ctrl Pts',(0.14219363741077,0.0630651082709919,0.0989093059459589));
#8550=CARTESIAN_POINT('Ctrl Pts',(0.144236152422842,0.0584065738729217,
0.0985487844421466));
#8551=CARTESIAN_POINT('Ctrl Pts',(0.145839920019718,0.0542781948779205,
0.098244810634397));
#8552=CARTESIAN_POINT('Ctrl Pts',(0.152027122322435,0.0360864539923843,
0.0969481510169046));
#8553=CARTESIAN_POINT('Ctrl Pts',(0.154768156470612,0.0214789260872862,
0.0960079134648093));
#8554=CARTESIAN_POINT('Ctrl Pts',(0.155574130201168,0.00279381243316039,
0.0947338128348807));
#8555=CARTESIAN_POINT('Ctrl Pts',(0.155595166007918,-0.00112037355489537,
0.0944635500631644));
#8556=CARTESIAN_POINT('Ctrl Pts',(0.155439132628317,-0.00594220989985941,
0.0941245856004825));
#8557=CARTESIAN_POINT('Ctrl Pts',(0.155401632513466,-0.0068532006863372,
0.0940602818139225));
#8558=CARTESIAN_POINT('Ctrl Pts',(0.155329791835799,-0.0082907571383169,
0.093958371248773));
#8559=CARTESIAN_POINT('Ctrl Pts',(0.15530077648645,-0.00881757880059143,
0.0939209310804517));
#8560=CARTESIAN_POINT('Ctrl Pts',(0.155241422728809,-0.00980383414171339,
0.0938506610407032));
#8561=CARTESIAN_POINT('Ctrl Pts',(0.155211723532694,-0.0102633018265468,
0.093817851527963));
#8562=CARTESIAN_POINT('Ctrl Pts',(0.155140798579042,-0.0112897418853935,
0.0937443898396944));
#8563=CARTESIAN_POINT('Ctrl Pts',(0.155098503974531,-0.0118566312491732,
0.0937037046278102));
#8564=CARTESIAN_POINT('Ctrl Pts',(0.154983698814881,-0.0132894985631701,
0.0936005757014586));
#8565=CARTESIAN_POINT('Ctrl Pts',(0.154907037762978,-0.0141551144439102,
0.0935380029090524));
#8566=CARTESIAN_POINT('Ctrl Pts',(0.154434245828433,-0.0190285497217535,
0.0931841433825164));
#8567=CARTESIAN_POINT('Ctrl Pts',(0.153889870631527,-0.0230200817577691,
0.0928882561223398));
#8568=CARTESIAN_POINT('Ctrl Pts',(0.152862412609119,-0.0288527177048803,
0.0924464454901346));
#8569=CARTESIAN_POINT('Ctrl Pts',(0.152499428661536,-0.0307135190158705,
0.0923040716077476));
#8570=CARTESIAN_POINT('Ctrl Pts',(0.149022206790747,-0.0469536313242474,
0.0910492079518989));
#8571=CARTESIAN_POINT('Ctrl Pts',(0.143917074941132,-0.0608281133680812,
0.0898824871410277));
#8572=CARTESIAN_POINT('Ctrl Pts',(0.135708076983116,-0.0760648897494929,
0.0885804253885668));
#8573=CARTESIAN_POINT('Ctrl Pts',(0.134418872659339,-0.0783206131333061,
0.0883873531254169));
#8574=CARTESIAN_POINT('Ctrl Pts',(0.132794297997063,-0.0810047407770551,
0.0881581535448154));
#8575=CARTESIAN_POINT('Ctrl Pts',(0.132512518454237,-0.0814648763886238,
0.0881188820412622));
#8576=CARTESIAN_POINT('Ctrl Pts',(0.132069994028353,-0.082179131026283,
0.0880579640894007));
#8577=CARTESIAN_POINT('Ctrl Pts',(0.131910900688816,-0.0824342597621625,
0.088036212861481));
#8578=CARTESIAN_POINT('Ctrl Pts',(0.131614037400122,-0.0829072620813196,
0.0879959045761039));
#8579=CARTESIAN_POINT('Ctrl Pts',(0.131476466998102,-0.0831252523251769,
0.0879773352816231));
#8580=CARTESIAN_POINT('Ctrl Pts',(0.131163771188332,-0.0836180231536749,
0.0879353748081064));
#8581=CARTESIAN_POINT('Ctrl Pts',(0.130988324235096,-0.0838925955482885,
0.0879120052431236));
#8582=CARTESIAN_POINT('Ctrl Pts',(0.130455150987439,-0.0847212550308258,
0.0878415021975801));
#8583=CARTESIAN_POINT('Ctrl Pts',(0.130094756001872,-0.0852736300118598,
0.0877945413727638));
#8584=CARTESIAN_POINT('Ctrl Pts',(0.127300309468236,-0.0894977066437365,
0.0874355629769011));
#8585=CARTESIAN_POINT('Ctrl Pts',(0.124714502402889,-0.0930672350041507,
0.087132992378933));
#8586=CARTESIAN_POINT('Ctrl Pts',(0.112832350526481,-0.108083300538572,
0.0858405801862741));
#8587=CARTESIAN_POINT('Ctrl Pts',(0.102087439196792,-0.11828500668543,0.0849031470599794));
#8588=CARTESIAN_POINT('Ctrl Pts',(0.0868246806062007,-0.129124307259356,
0.0836284823518068));
#8589=CARTESIAN_POINT('Ctrl Pts',(0.0834960959158585,-0.131301215515034,
0.0833539682714985));
#8590=CARTESIAN_POINT('Ctrl Pts',(0.0793024801449853,-0.133819874399062,
0.0830102838809307));
#8591=CARTESIAN_POINT('Ctrl Pts',(0.0785128104048151,-0.134284700094577,
0.08294566149629));
#8592=CARTESIAN_POINT('Ctrl Pts',(0.0772611346561105,-0.135006663074031,
0.0828433559093042));
#8593=CARTESIAN_POINT('Ctrl Pts',(0.0768018360474147,-0.135268473673388,
0.0828058414584501));
#8594=CARTESIAN_POINT('Ctrl Pts',(0.0759400642149028,-0.135753899134797,
0.0827354982276535));
#8595=CARTESIAN_POINT('Ctrl Pts',(0.0755379143604969,-0.135978079001588,
0.0827026901430807));
#8596=CARTESIAN_POINT('Ctrl Pts',(0.0746380887361048,-0.136474466426095,
0.082629317281405));
#8597=CARTESIAN_POINT('Ctrl Pts',(0.074139909465216,-0.136745742475572,
0.0825887198845213));
#8598=CARTESIAN_POINT('Ctrl Pts',(0.0728784041261681,-0.137423756349601,
0.0824859736068982));
#8599=CARTESIAN_POINT('Ctrl Pts',(0.0721131573090637,-0.137826859080366,
0.0824236973756138));
#8600=CARTESIAN_POINT('Ctrl Pts',(0.0678200458718348,-0.140042764594081,
0.0820745617190062));
#8601=CARTESIAN_POINT('Ctrl Pts',(0.0642275231545033,-0.141726336682912,
0.0817832455929904));
#8602=CARTESIAN_POINT('Ctrl Pts',(0.0587786614215767,-0.144030117114458,
0.081342146320132));
#8603=CARTESIAN_POINT('Ctrl Pts',(0.0569683840613695,-0.144755684965672,
0.0811957296120877));
#8604=CARTESIAN_POINT('Ctrl Pts',(0.0413904993789112,-0.150661909183268,
0.0799370815355001));
#8605=CARTESIAN_POINT('Ctrl Pts',(0.0269680403509924,-0.153898768608725,
0.0787706492050606));
#8606=CARTESIAN_POINT('Ctrl Pts',(0.00970466905530235,-0.155268915258471,
0.077467670514589));
#8607=CARTESIAN_POINT('Ctrl Pts',(0.00709745880679463,-0.15540992539813,
0.0772736249341517));
#8608=CARTESIAN_POINT('Ctrl Pts',(0.00394751013914065,-0.155500841635551,
0.0770434164607347));
#8609=CARTESIAN_POINT('Ctrl Pts',(0.00340719718354766,-0.155513618748746,
0.077004078915776));
#8610=CARTESIAN_POINT('Ctrl Pts',(0.00256594683112066,-0.155529125796509,
0.0769430766562806));
#8611=CARTESIAN_POINT('Ctrl Pts',(0.00226505679554624,-0.155533798822233,
0.0769213067721626));
#8612=CARTESIAN_POINT('Ctrl Pts',(0.00170625040128141,-0.15554085551139,
0.0768809691482868));
#8613=CARTESIAN_POINT('Ctrl Pts',(0.00144834432381692,-0.155543470850301,
0.0768623891417416));
#8614=CARTESIAN_POINT('Ctrl Pts',(0.000864526454679085,-0.155547938948567,
0.0768204126446921));
#8615=CARTESIAN_POINT('Ctrl Pts',(0.000538615213439235,-0.155549408922255,
0.0767970377394832));
#8616=CARTESIAN_POINT('Ctrl Pts',(-0.000446417359977353,-0.155550755848506,
0.0767265585835222));
#8617=CARTESIAN_POINT('Ctrl Pts',(-0.00110554718381486,-0.155547467804036,
0.0766796265436433));
#8618=CARTESIAN_POINT('Ctrl Pts',(-0.00614768498146172,-0.155490263109722,
0.0763222232301394));
#8619=CARTESIAN_POINT('Ctrl Pts',(-0.0105271793515263,-0.155255284526461,
0.0760210954838136));
#8620=CARTESIAN_POINT('Ctrl Pts',(-0.0296255250221091,-0.153418493025023,
0.0747258095397929));
#8621=CARTESIAN_POINT('Ctrl Pts',(-0.0440820349770182,-0.149905735658397,
0.0737846722921825));
#8622=CARTESIAN_POINT('Ctrl Pts',(-0.0614703784982253,-0.142942699521187,
0.0725087381242133));
#8623=CARTESIAN_POINT('Ctrl Pts',(-0.0650589438490988,-0.14134550615587,
0.0722375431063856));
#8624=CARTESIAN_POINT('Ctrl Pts',(-0.0694025467099712,-0.139211790956327,
0.0718975236628699));
#8625=CARTESIAN_POINT('Ctrl Pts',(-0.0702185156422144,-0.138802003690988,
0.0718331262762424));
#8626=CARTESIAN_POINT('Ctrl Pts',(-0.0715006475479744,-0.138143906129541,
0.0717310868852342));
#8627=CARTESIAN_POINT('Ctrl Pts',(-0.0719692443877624,-0.137900359862675,
0.0716936119503776));
#8628=CARTESIAN_POINT('Ctrl Pts',(-0.0728442761628356,-0.137439900196713,
0.0716232882724585));
#8629=CARTESIAN_POINT('Ctrl Pts',(-0.0732510064601142,-0.137223557671308,
0.0715904599580668));
#8630=CARTESIAN_POINT('Ctrl Pts',(-0.0741575620964936,-0.136736175790977,
0.0715169710569374));
#8631=CARTESIAN_POINT('Ctrl Pts',(-0.0746568722625348,-0.13646419748105,
0.0714762774888386));
#8632=CARTESIAN_POINT('Ctrl Pts',(-0.0759153361796357,-0.135769727998318,
0.071373155025313));
#8633=CARTESIAN_POINT('Ctrl Pts',(-0.0766724535884431,-0.135343607576513,
0.0713105972786505));
#8634=CARTESIAN_POINT('Ctrl Pts',(-0.0809120641337486,-0.132910481753134,
0.0709573261910329));
#8635=CARTESIAN_POINT('Ctrl Pts',(-0.0843189980026695,-0.130775606864694,
0.0706620337934866));
#8636=CARTESIAN_POINT('Ctrl Pts',(-0.0892166422127744,-0.127435626540591,
0.0702198337913709));
#8637=CARTESIAN_POINT('Ctrl Pts',(-0.0907741064144418,-0.126330951227118,
0.0700764441889221));
#8638=CARTESIAN_POINT('Ctrl Pts',(-0.104166813738272,-0.116456256076863,
0.0688191948786559));
#8639=CARTESIAN_POINT('Ctrl Pts',(-0.114719286602177,-0.106076350818248,
0.0676510071300562));
#8640=CARTESIAN_POINT('Ctrl Pts',(-0.125219507963493,-0.0923175723981026,
0.0663491698909107));
#8641=CARTESIAN_POINT('Ctrl Pts',(-0.126733642344316,-0.0902277416492988,
0.0661574216084644));
#8642=CARTESIAN_POINT('Ctrl Pts',(-0.128500239017742,-0.0876571796417167,
0.0659295738996789));
#8643=CARTESIAN_POINT('Ctrl Pts',(-0.128802981934727,-0.0872117219080123,
0.0658903735618032));
#8644=CARTESIAN_POINT('Ctrl Pts',(-0.12927103040024,-0.0865152790108211,
0.0658295381904516));
#8645=CARTESIAN_POINT('Ctrl Pts',(-0.129437928623524,-0.0862653779965664,
0.065807798884406));
#8646=CARTESIAN_POINT('Ctrl Pts',(-0.129746584477844,-0.0858003071483235,
0.0657675106319524));
#8647=CARTESIAN_POINT('Ctrl Pts',(-0.129888530418938,-0.0855852706839214,
0.0657489494466757));
#8648=CARTESIAN_POINT('Ctrl Pts',(-0.130208759221599,-0.0850975186224531,
0.0657069991243744));
#8649=CARTESIAN_POINT('Ctrl Pts',(-0.130386719592729,-0.0848245955655089,
0.0656836316371968));
#8650=CARTESIAN_POINT('Ctrl Pts',(-0.130922799657613,-0.083996780753346,
0.0656130681186414));
#8651=CARTESIAN_POINT('Ctrl Pts',(-0.131278250648963,-0.0834401557722822,
0.0655660455506756));
#8652=CARTESIAN_POINT('Ctrl Pts',(-0.13399905783635,-0.079119031505382,
0.0652041345617505));
#8653=CARTESIAN_POINT('Ctrl Pts',(-0.136205859503016,-0.0752565065471865,
0.0648988822822525));
#8654=CARTESIAN_POINT('Ctrl Pts',(-0.141714760659104,-0.0645758808156944,
0.0640881135628669));
#8655=CARTESIAN_POINT('Ctrl Pts',(-0.144689543731709,-0.0576026739184621,
0.063593327653544));
#8656=CARTESIAN_POINT('Ctrl Pts',(-0.150613829678048,-0.0403202637994308,
0.0623900042066171));
#8657=CARTESIAN_POINT('Ctrl Pts',(-0.153029106901279,-0.0298712104368924,
0.0616792021526925));
#8658=CARTESIAN_POINT('Ctrl Pts',(-0.154494129726095,-0.018129004019262,
0.0608506590700042));
#8659=CARTESIAN_POINT('Ctrl Pts',(-0.154622592056141,-0.0169985531895867,
0.0607706245342408));
#8660=CARTESIAN_POINT('Ctrl Pts',(-0.154798110114348,-0.0152868413419617,
0.0606489874582022));
#8661=CARTESIAN_POINT('Ctrl Pts',(-0.154854318963561,-0.0147065391824214,
0.0606076722568643));
#8662=CARTESIAN_POINT('Ctrl Pts',(-0.154949159031645,-0.0136665083244172,
0.0605334804305667));
#8663=CARTESIAN_POINT('Ctrl Pts',(-0.154989010070782,-0.0132068952923857,
0.0605006424688547));
#8664=CARTESIAN_POINT('Ctrl Pts',(-0.155069192505128,-0.012231739251074,
0.0604308592307879));
#8665=CARTESIAN_POINT('Ctrl Pts',(-0.155108998752173,-0.0117161599282944,
0.0603938978999998));
#8666=CARTESIAN_POINT('Ctrl Pts',(-0.1552085558945,-0.010337109253723,0.0602948536877656));
#8667=CARTESIAN_POINT('Ctrl Pts',(-0.15526367110381,-0.00947333255247916,
0.060232626508677));
#8668=CARTESIAN_POINT('Ctrl Pts',(-0.155495811388464,-0.00528545753706559,
0.0599299675461191));
#8669=CARTESIAN_POINT('Ctrl Pts',(-0.155573296462417,-0.0019569579792852,
0.0596864564976343));
#8670=CARTESIAN_POINT('Ctrl Pts',(-0.155411983463436,0.0163412818140053,
0.0583301774315003));
#8671=CARTESIAN_POINT('Ctrl Pts',(-0.15311936023218,0.0312124088466213,
0.0571524755466076));
#8672=CARTESIAN_POINT('Ctrl Pts',(-0.148476009409317,0.0463841534662506,
0.0559365572065336));
#8673=CARTESIAN_POINT('Ctrl Pts',(-0.148204713258434,0.0472438152887168,
0.0558676484324315));
#8674=CARTESIAN_POINT('Ctrl Pts',(-0.147636827434995,0.0489902427401683,
0.0557276896387132));
#8675=CARTESIAN_POINT('Ctrl Pts',(-0.147339682704012,0.0498767948979903,
0.0556566578947094));
#8676=CARTESIAN_POINT('Ctrl Pts',(-0.145999878873975,0.0537577053059277,
0.0553459295842282));
#8677=CARTESIAN_POINT('Ctrl Pts',(-0.144873707694657,0.056722729542674,
0.0551090871481001));
#8678=CARTESIAN_POINT('Ctrl Pts',(-0.143448677357211,0.0601546025319333,
0.0548372133532378));
#8679=CARTESIAN_POINT('Ctrl Pts',(-0.143237130899882,0.0606566038985881,
0.054797502630525));
#8680=CARTESIAN_POINT('Ctrl Pts',(-0.142892756882392,0.0614619571625992,
0.0547339004482372));
#8681=CARTESIAN_POINT('Ctrl Pts',(-0.142761592817414,0.0617660082042662,
0.0547099124555957));
#8682=CARTESIAN_POINT('Ctrl Pts',(-0.142526236218627,0.0623068327183942,
0.0546672904537251));
#8683=CARTESIAN_POINT('Ctrl Pts',(-0.142422423149672,0.0625437670930051,
0.0546486337898382));
#8684=CARTESIAN_POINT('Ctrl Pts',(-0.142199663998522,0.0630487434381924,
0.0546089057718721));
#8685=CARTESIAN_POINT('Ctrl Pts',(-0.142080551168763,0.0633167076993923,
0.0545878448247476));
#8686=CARTESIAN_POINT('Ctrl Pts',(-0.141753890060667,0.0640460230549665,
0.0545305754020657));
#8687=CARTESIAN_POINT('Ctrl Pts',(-0.141544845310254,0.0645067066410245,
0.0544944570395705));
#8688=CARTESIAN_POINT('Ctrl Pts',(-0.140453343128435,0.0668812564207846,
0.0543085402394668));
#8689=CARTESIAN_POINT('Ctrl Pts',(-0.139534248819734,0.0687781843952986,
0.0541608668139271));
#8690=CARTESIAN_POINT('Ctrl Pts',(-0.136701685617625,0.0743336613117928,
0.0537291738344154));
#8691=CARTESIAN_POINT('Ctrl Pts',(-0.134680722045666,0.0779355691557279,
0.0534503055345552));
#8692=CARTESIAN_POINT('Ctrl Pts',(-0.12703079751817,0.0903814811031068,
0.0524752682921748));
#8693=CARTESIAN_POINT('Ctrl Pts',(-0.120654684808217,0.098732428056966,
0.051797935341465));
#8694=CARTESIAN_POINT('Ctrl Pts',(-0.111442521379164,0.108560144880349,
0.0508963679610258));
#8695=CARTESIAN_POINT('Ctrl Pts',(-0.109335556218786,0.110681864931461,
0.0506946575231969));
#8696=CARTESIAN_POINT('Ctrl Pts',(-0.104522098578831,0.115257401612486,
0.05024149871917));
#8697=CARTESIAN_POINT('Ctrl Pts',(-0.101787768178444,0.117679158397521,
0.0499890649108242));
#8698=CARTESIAN_POINT('Ctrl Pts',(-0.0982578283029227,0.120590447827129,
0.0496676822709614));
#8699=CARTESIAN_POINT('Ctrl Pts',(-0.0975395019251896,0.121172201549451,
0.0496025083143314));
#8700=CARTESIAN_POINT('Ctrl Pts',(-0.0963964672043183,0.122081165563429,
0.0494991309605083));
#8701=CARTESIAN_POINT('Ctrl Pts',(-0.0959751703780766,0.122412648581027,
0.0494610983007411));
#8702=CARTESIAN_POINT('Ctrl Pts',(-0.0951890867126423,0.123024599153411,
0.0493902589202329));
#8703=CARTESIAN_POINT('Ctrl Pts',(-0.094824751407512,0.123305639523101,
0.0493574753332094));
#8704=CARTESIAN_POINT('Ctrl Pts',(-0.0940154479961255,0.12392421054803,
0.0492847577468119));
#8705=CARTESIAN_POINT('Ctrl Pts',(-0.0935698999852716,0.124260968222449,
0.0492447940238498));
#8706=CARTESIAN_POINT('Ctrl Pts',(-0.0922783358781314,0.125226283390147,
0.0491291395502704));
#8707=CARTESIAN_POINT('Ctrl Pts',(-0.0914277471660367,0.125848640321269,
0.0490532098600685));
#8708=CARTESIAN_POINT('Ctrl Pts',(-0.0850298019981282,0.130430779120129,
0.0484837363602214));
#8709=CARTESIAN_POINT('Ctrl Pts',(-0.0792347281175303,0.134030174044826,
0.0479766144168766));
#8710=CARTESIAN_POINT('Ctrl Pts',(-0.0700971602533137,0.138905522278269,
0.0471892813764483));
#8711=CARTESIAN_POINT('Ctrl Pts',(-0.066917046829144,0.140465061453259,
0.046917478598225));
#8712=CARTESIAN_POINT('Ctrl Pts',(-0.0636885943104762,0.141913936788307,
0.046644325870219));
#8713=CARTESIAN_POINT('',(-0.155549967545476,0.000100481845383891,0.045594377439629));
#8714=CARTESIAN_POINT('Ctrl Pts',(-0.0636886258329924,0.141913922641526,
0.0327905057321709));
#8715=CARTESIAN_POINT('Ctrl Pts',(-0.0660294620340356,0.140863393995925,
0.0329750500365568));
#8716=CARTESIAN_POINT('Ctrl Pts',(-0.0683424013010257,0.139755784576519,
0.0331595943409427));
#8717=CARTESIAN_POINT('Ctrl Pts',(-0.0706245494042477,0.138592840801562,
0.0333441386453286));
#8718=CARTESIAN_POINT('Ctrl Pts',(-0.079758546308512,0.133938311665045,
0.0340827528932735));
#8719=CARTESIAN_POINT('Ctrl Pts',(-0.0884632964101746,0.128360212860196,
0.0348213671412184));
#8720=CARTESIAN_POINT('Ctrl Pts',(-0.0965470015752083,0.121960973212076,
0.0355599813891633));
#8721=CARTESIAN_POINT('Ctrl Pts',(-0.104663083221479,0.11553610362593,0.0363015539006584));
#8722=CARTESIAN_POINT('Ctrl Pts',(-0.112152308750486,0.108283954652407,
0.0370431264121535));
#8723=CARTESIAN_POINT('Ctrl Pts',(-0.118849199871259,0.100352728861558,
0.0377846989236486));
#8724=CARTESIAN_POINT('Ctrl Pts',(-0.1255048724983,0.0924703187337775,0.0385217071527975));
#8725=CARTESIAN_POINT('Ctrl Pts',(-0.131377343306342,0.083917886634347,
0.0392587153819463));
#8726=CARTESIAN_POINT('Ctrl Pts',(-0.136342973587973,0.0748758709678172,
0.0399957236110952));
#8727=CARTESIAN_POINT('Ctrl Pts',(-0.141354731994914,0.0657498596737304,
0.0407395782637634));
#8728=CARTESIAN_POINT('Ctrl Pts',(-0.145442231278217,0.0561259457345724,
0.0414834329164317));
#8729=CARTESIAN_POINT('Ctrl Pts',(-0.14852637524592,0.046213832954086,0.0422272875690999));
#8730=CARTESIAN_POINT('Ctrl Pts',(-0.151610519213623,0.0363017201735995,
0.0429711422217682));
#8731=CARTESIAN_POINT('Ctrl Pts',(-0.153691150142048,0.0261023555329522,
0.0437149968744365));
#8732=CARTESIAN_POINT('Ctrl Pts',(-0.154741787599696,0.0158360875992346,
0.0444588515271047));
#8733=CARTESIAN_POINT('Ctrl Pts',(-0.155276401924124,0.0106121220382939,
0.0448373601646128));
#8734=CARTESIAN_POINT('Ctrl Pts',(-0.155546569792262,0.00536034147729075,
0.0452158688021209));
#8735=CARTESIAN_POINT('Ctrl Pts',(-0.155549967545476,0.000100481845383891,
0.045594377439629));
#8736=CARTESIAN_POINT('Ctrl Pts',(-0.155549962667911,0.000107768322894147,
0.0457021375939884));
#8737=CARTESIAN_POINT('Ctrl Pts',(-0.155558024611102,-0.0115286284275358,
0.0464889715817548));
#8738=CARTESIAN_POINT('Ctrl Pts',(-0.154260364033593,-0.0231303105295702,
0.0472366725437763));
#8739=CARTESIAN_POINT('Ctrl Pts',(-0.150258512393375,-0.0407348573768369,
0.0484402774613486));
#8740=CARTESIAN_POINT('Ctrl Pts',(-0.148451260673314,-0.0468951615387702,
0.0488747267934762));
#8741=CARTESIAN_POINT('Ctrl Pts',(-0.145763792723458,-0.0543224180017188,
0.0494253367338388));
#8742=CARTESIAN_POINT('Ctrl Pts',(-0.145238488188932,-0.0557116652596488,
0.0495295004996491));
#8743=CARTESIAN_POINT('Ctrl Pts',(-0.144459156074046,-0.0576867573758456,
0.0496793745242537));
#8744=CARTESIAN_POINT('Ctrl Pts',(-0.144221277345524,-0.0582789231962408,
0.0497245408636152));
#8745=CARTESIAN_POINT('Ctrl Pts',(-0.143803081270126,-0.0593017222636224,
0.0498029629727483));
#8746=CARTESIAN_POINT('Ctrl Pts',(-0.143624455195613,-0.0597330420054922,
0.0498361610287936));
#8747=CARTESIAN_POINT('Ctrl Pts',(-0.143277644681902,-0.060559918951737,
0.0499000521954672));
#8748=CARTESIAN_POINT('Ctrl Pts',(-0.143109756781965,-0.0609555965926227,
0.0499307349388027));
#8749=CARTESIAN_POINT('Ctrl Pts',(-0.142666536556045,-0.0619882520766492,
0.050011101922015));
#8750=CARTESIAN_POINT('Ctrl Pts',(-0.142388580540545,-0.0626240860287197,
0.0500608756447366));
#8751=CARTESIAN_POINT('Ctrl Pts',(-0.14141415028925,-0.0648131007742427,
0.0502332522957411));
#8752=CARTESIAN_POINT('Ctrl Pts',(-0.140696464959421,-0.0663566443604307,
0.0503565821150925));
#8753=CARTESIAN_POINT('Ctrl Pts',(-0.134421968092164,-0.0792917431082303,
0.0514056797504091));
#8754=CARTESIAN_POINT('Ctrl Pts',(-0.127518436468818,-0.0899741896379027,
0.0523810920631677));
#8755=CARTESIAN_POINT('Ctrl Pts',(-0.115949656265776,-0.103828851920947,
0.0537820188206415));
#8756=CARTESIAN_POINT('Ctrl Pts',(-0.112288856128531,-0.10777741771989,
0.0541992656013646));
#8757=CARTESIAN_POINT('Ctrl Pts',(-0.106503961533513,-0.113401628571723,
0.054813925867454));
#8758=CARTESIAN_POINT('Ctrl Pts',(-0.104528951963616,-0.115224664689301,
0.0550166942025176));
#8759=CARTESIAN_POINT('Ctrl Pts',(-0.101722769557173,-0.11768334368236,
0.0552940821521655));
#8760=CARTESIAN_POINT('Ctrl Pts',(-0.10093104274525,-0.118363068506035,
0.0553712058482486));
#8761=CARTESIAN_POINT('Ctrl Pts',(-0.0995519884880571,-0.119523134015233,
0.0555035075653008));
#8762=CARTESIAN_POINT('Ctrl Pts',(-0.0989678869695426,-0.120007230569266,
0.0555589268443804));
#8763=CARTESIAN_POINT('Ctrl Pts',(-0.098113854120641,-0.120704566655798,
0.0556390363765802));
#8764=CARTESIAN_POINT('Ctrl Pts',(-0.0978467327447785,-0.120921204424147,
0.0556639633352689));
#8765=CARTESIAN_POINT('Ctrl Pts',(-0.0973872367572115,-0.121291340096473,
0.055706617471833));
#8766=CARTESIAN_POINT('Ctrl Pts',(-0.0971952150907193,-0.12144526846428,
0.0557243754795696));
#8767=CARTESIAN_POINT('Ctrl Pts',(-0.096810301883321,-0.121752324829042,
0.055759837718814));
#8768=CARTESIAN_POINT('Ctrl Pts',(-0.0966174129919684,-0.121905449677483,
0.055777541853343));
#8769=CARTESIAN_POINT('Ctrl Pts',(-0.0960971635096071,-0.122316439295845,
0.0558251154853686));
#8770=CARTESIAN_POINT('Ctrl Pts',(-0.0957691257672256,-0.122573450294928,
0.0558549246400376));
#8771=CARTESIAN_POINT('Ctrl Pts',(-0.0945547644075812,-0.123517026958475,
0.0559646005871443));
#8772=CARTESIAN_POINT('Ctrl Pts',(-0.0936620297372567,-0.124195345321396,
0.0560439100399647));
#8773=CARTESIAN_POINT('Ctrl Pts',(-0.0824065301544903,-0.132557106066507,
0.0570285880487809));
#8774=CARTESIAN_POINT('Ctrl Pts',(-0.0711324056003403,-0.138933518089678,
0.0578577485246019));
#8775=CARTESIAN_POINT('Ctrl Pts',(-0.051084477838859,-0.147184125789049,
0.0592908711371011));
#8776=CARTESIAN_POINT('Ctrl Pts',(-0.0427036775644092,-0.149830411958971,
0.0598787750660659));
#8777=CARTESIAN_POINT('Ctrl Pts',(-0.0327776107720131,-0.152063789268373,
0.0605889673347968));
#8778=CARTESIAN_POINT('Ctrl Pts',(-0.0314058639598889,-0.152353008694267,
0.0606873811812471));
#8779=CARTESIAN_POINT('Ctrl Pts',(-0.0294149968837752,-0.152744734393208,
0.060830680738746));
#8780=CARTESIAN_POINT('Ctrl Pts',(-0.0287988413252484,-0.152862103361327,
0.060875095072924));
#8781=CARTESIAN_POINT('Ctrl Pts',(-0.0277210640757414,-0.153060657191675,
0.060952904455174));
#8782=CARTESIAN_POINT('Ctrl Pts',(-0.0272597505570381,-0.153143488807817,
0.0609862469561173));
#8783=CARTESIAN_POINT('Ctrl Pts',(-0.0263660076807935,-0.153299799513147,
0.061050921551755));
#8784=CARTESIAN_POINT('Ctrl Pts',(-0.0259336274836434,-0.153373536994129,
0.0610822451364215));
#8785=CARTESIAN_POINT('Ctrl Pts',(-0.0247862828144139,-0.153564213059886,
0.0611654598481627));
#8786=CARTESIAN_POINT('Ctrl Pts',(-0.0240708107705878,-0.153677986011225,
0.0612174502547086));
#8787=CARTESIAN_POINT('Ctrl Pts',(-0.0215139405372053,-0.154066281045172,
0.0614036168498079));
#8788=CARTESIAN_POINT('Ctrl Pts',(-0.0196685075761934,-0.15431272742267,
0.0615386684898708));
#8789=CARTESIAN_POINT('Ctrl Pts',(-0.0160355858013158,-0.154731657896973,
0.0618059932502063));
#8790=CARTESIAN_POINT('Ctrl Pts',(-0.0142486467287317,-0.154906428358918,
0.0619381738702446));
#8791=CARTESIAN_POINT('Ctrl Pts',(0.00318408565992699,-0.156307245454273,
0.063234632820172));
#8792=CARTESIAN_POINT('Ctrl Pts',(0.0189263985821658,-0.155189236581051,
0.0644731630295722));
#8793=CARTESIAN_POINT('Ctrl Pts',(0.0369547823508225,-0.151122305282958,
0.0658815128390439));
#8794=CARTESIAN_POINT('Ctrl Pts',(0.0396631080709215,-0.150434195178028,
0.0660924094410291));
#8795=CARTESIAN_POINT('Ctrl Pts',(0.0433859963875568,-0.149380766691674,
0.0663801336570163));
#8796=CARTESIAN_POINT('Ctrl Pts',(0.0444173646932103,-0.149077349095493,
0.0664596077686002));
#8797=CARTESIAN_POINT('Ctrl Pts',(0.0459673615309527,-0.148603842090421,
0.0665786077371196));
#8798=CARTESIAN_POINT('Ctrl Pts',(0.0464883513607945,-0.148441683569055,
0.0666185312696393));
#8799=CARTESIAN_POINT('Ctrl Pts',(0.0473328390247322,-0.148173953946187,
0.0666831105193796));
#8800=CARTESIAN_POINT('Ctrl Pts',(0.0476568567849441,-0.148070058706635,
0.0667078565054399));
#8801=CARTESIAN_POINT('Ctrl Pts',(0.0482775487280908,-0.147868787382596,
0.0667551950621032));
#8802=CARTESIAN_POINT('Ctrl Pts',(0.0485742752651706,-0.147771579744889,
0.0667777969958995));
#8803=CARTESIAN_POINT('Ctrl Pts',(0.0491093166747904,-0.147594514409789,
0.066818497369476));
#8804=CARTESIAN_POINT('Ctrl Pts',(0.0493477316498017,-0.14751497229936,
0.0668366138577791));
#8805=CARTESIAN_POINT('Ctrl Pts',(0.0498752900744485,-0.147337541454609,
0.0668766576513732));
#8806=CARTESIAN_POINT('Ctrl Pts',(0.0501643380131203,-0.147239379508195,
0.066898568653258));
#8807=CARTESIAN_POINT('Ctrl Pts',(0.0509679131858796,-0.146963840861739,
0.0669594073880247));
#8808=CARTESIAN_POINT('Ctrl Pts',(0.0514818081365596,-0.146784611420634,
0.0669982280784462));
#8809=CARTESIAN_POINT('Ctrl Pts',(0.054204916723793,-0.145818821585571,
0.0672035319946431));
#8810=CARTESIAN_POINT('Ctrl Pts',(0.0563972238880154,-0.144985021483711,
0.0673673975335468));
#8811=CARTESIAN_POINT('Ctrl Pts',(0.0601517844275243,-0.143458986269328,
0.0676469578857969));
#8812=CARTESIAN_POINT('Ctrl Pts',(0.0617229480510002,-0.142790041880342,
0.067763611754893));
#8813=CARTESIAN_POINT('Ctrl Pts',(0.0745635247938152,-0.137071429470947,
0.0687167466592353));
#8814=CARTESIAN_POINT('Ctrl Pts',(0.0852064307917572,-0.130721865472826,
0.0695085577317131));
#8815=CARTESIAN_POINT('Ctrl Pts',(0.0984826038764124,-0.120484294574988,
0.0706295555624915));
#8816=CARTESIAN_POINT('Ctrl Pts',(0.101861688190277,-0.117641318565557,
0.0709281200845115));
#8817=CARTESIAN_POINT('Ctrl Pts',(0.107085941658198,-0.112851903994566,
0.0714162424586966));
#8818=CARTESIAN_POINT('Ctrl Pts',(0.109009746513577,-0.11099470621197,0.071602268243785));
#8819=CARTESIAN_POINT('Ctrl Pts',(0.111448073854493,-0.108516242025504,
0.0718469891751459));
#8820=CARTESIAN_POINT('Ctrl Pts',(0.112007051120769,-0.107939188458225,
0.0719037267329255));
#8821=CARTESIAN_POINT('Ctrl Pts',(0.112909196081731,-0.106993316118218,
0.0719963556560799));
#8822=CARTESIAN_POINT('Ctrl Pts',(0.113255091767286,-0.106627109272011,
0.0720321289145246));
#8823=CARTESIAN_POINT('Ctrl Pts',(0.113917062813364,-0.105919411892233,
0.0721010942523742));
#8824=CARTESIAN_POINT('Ctrl Pts',(0.114233397141567,-0.105578170018578,
0.0721342747567758));
#8825=CARTESIAN_POINT('Ctrl Pts',(0.114954444913339,-0.104793314096841,
0.072210425512628));
#8826=CARTESIAN_POINT('Ctrl Pts',(0.115358127973879,-0.104348767967743,
0.0722534386550659));
#8827=CARTESIAN_POINT('Ctrl Pts',(0.116424182888106,-0.103161054502894,
0.0723680521683697));
#8828=CARTESIAN_POINT('Ctrl Pts',(0.1170820019893,-0.102413857713801,0.0724398408761141));
#8829=CARTESIAN_POINT('Ctrl Pts',(0.121990231966919,-0.0967296527928284,
0.0729836934464149));
#8830=CARTESIAN_POINT('Ctrl Pts',(0.125933277609011,-0.0915370390176759,
0.0734681461051096));
#8831=CARTESIAN_POINT('Ctrl Pts',(0.137430671811926,-0.0742416881248383,
0.0750451771246575));
#8832=CARTESIAN_POINT('Ctrl Pts',(0.14365234563892,-0.0613430800222112,
0.0761752967707421));
#8833=CARTESIAN_POINT('Ctrl Pts',(0.148733105106667,-0.0456015200528958,
0.0774156868990523));
#8834=CARTESIAN_POINT('Ctrl Pts',(0.149387677125026,-0.043409199728889,
0.0775853047829655));
#8835=CARTESIAN_POINT('Ctrl Pts',(0.150131188385693,-0.0407025577367529,
0.077790258551602));
#8836=CARTESIAN_POINT('Ctrl Pts',(0.150266179081798,-0.0402013355163685,
0.0778280264041635));
#8837=CARTESIAN_POINT('Ctrl Pts',(0.150474230345912,-0.0394131472304948,
0.0778871159788191));
#8838=CARTESIAN_POINT('Ctrl Pts',(0.150548983151571,-0.0391266386090154,
0.0779085327960744));
#8839=CARTESIAN_POINT('Ctrl Pts',(0.150687361646393,-0.038590000650366,
0.0779485281033003));
#8840=CARTESIAN_POINT('Ctrl Pts',(0.150751182210413,-0.038339929237776,
0.0779671172590649));
#8841=CARTESIAN_POINT('Ctrl Pts',(0.150895636425184,-0.0377679694572135,
0.0780095244812217));
#8842=CARTESIAN_POINT('Ctrl Pts',(0.15097586256843,-0.0374459815783716,
0.0780333188822446));
#8843=CARTESIAN_POINT('Ctrl Pts',(0.151219958242503,-0.0364527656206297,
0.078106479848725));
#8844=CARTESIAN_POINT('Ctrl Pts',(0.151380389455408,-0.0357806879209509,
0.0781556536594493));
#8845=CARTESIAN_POINT('Ctrl Pts',(0.153504691109276,-0.0266114656720041,
0.0788223059836024));
#8846=CARTESIAN_POINT('Ctrl Pts',(0.154755391654972,-0.017963342508237,
0.0794020841493169));
#8847=CARTESIAN_POINT('Ctrl Pts',(0.155752183254429,-0.00123921421103569,
0.080507138202634));
#8848=CARTESIAN_POINT('Ctrl Pts',(0.155608548296183,0.00680087273579766,
0.0810315888583669));
#8849=CARTESIAN_POINT('Ctrl Pts',(0.154460085448954,0.0188217121798087,
0.0818414361465043));
#8850=CARTESIAN_POINT('Ctrl Pts',(0.153918268762738,0.0228328106236434,
0.0821158983468834));
#8851=CARTESIAN_POINT('Ctrl Pts',(0.152787911037918,0.0292909474186763,
0.0825681029008388));
#8852=CARTESIAN_POINT('Ctrl Pts',(0.152295290364591,0.0317529312997165,
0.0827429436213154));
#8853=CARTESIAN_POINT('Ctrl Pts',(0.151570810338119,0.0349672362451497,
0.0829749201731549));
#8854=CARTESIAN_POINT('Ctrl Pts',(0.151392500530438,0.0357313433805167,
0.0830303425629312));
#8855=CARTESIAN_POINT('Ctrl Pts',(0.151091324107297,0.0369792290831497,
0.0831213226498433));
#8856=CARTESIAN_POINT('Ctrl Pts',(0.150971894803402,0.0374638301960137,
0.0831567696267183));
#8857=CARTESIAN_POINT('Ctrl Pts',(0.150736457502403,0.0383997397544758,
0.0832254568595244));
#8858=CARTESIAN_POINT('Ctrl Pts',(0.150620749542859,0.0388511188003107,
0.0832586871131321));
#8859=CARTESIAN_POINT('Ctrl Pts',(0.150349298437739,0.0398906141129895,
0.0833354557927926));
#8860=CARTESIAN_POINT('Ctrl Pts',(0.150192130468377,0.0404783468154918,
0.0833790398548015));
#8861=CARTESIAN_POINT('Ctrl Pts',(0.149761146365117,0.0420529477719267,
0.0834962955242785));
#8862=CARTESIAN_POINT('Ctrl Pts',(0.149481029097176,0.0430380439094717,
0.0835701701675548));
#8863=CARTESIAN_POINT('Ctrl Pts',(0.148557133993372,0.0461692604169829,
0.0838066811538148));
#8864=CARTESIAN_POINT('Ctrl Pts',(0.147876732132729,0.0483041798830264,
0.0839704940352888));
#8865=CARTESIAN_POINT('Ctrl Pts',(0.146901578784998,0.051149958571924,0.0841924081563293));
#8866=CARTESIAN_POINT('Ctrl Pts',(0.146647295184703,0.0518744916966867,
0.084249220159159));
#8867=CARTESIAN_POINT('Ctrl Pts',(0.146326965820198,0.0527660287916067,
0.0843195156183678));
#8868=CARTESIAN_POINT('Ctrl Pts',(0.146265977903483,0.0529348507889367,
0.0843328440527218));
#8869=CARTESIAN_POINT('Ctrl Pts',(0.146181554839517,0.0531672843044193,
0.0843512183737236));
#8870=CARTESIAN_POINT('Ctrl Pts',(0.146158369932953,0.0532309871608371,
0.0843562566718793));
#8871=CARTESIAN_POINT('Ctrl Pts',(0.145107936421894,0.0561112984219894,
0.0845841737184084));
#8872=CARTESIAN_POINT('Ctrl Pts',(0.143999574791482,0.0588974655605329,
0.0848094817287628));
#8873=CARTESIAN_POINT('Ctrl Pts',(0.137103080170915,0.0748731838230996,
0.0861292289374501));
#8874=CARTESIAN_POINT('Ctrl Pts',(0.129586648033349,0.0872381444160453,
0.0872713781692285));
#8875=CARTESIAN_POINT('Ctrl Pts',(0.11900619799879,0.100193495529096,0.088526201729839));
#8876=CARTESIAN_POINT('Ctrl Pts',(0.117494720853587,0.101961776490896,0.0886987074177071));
#8877=CARTESIAN_POINT('Ctrl Pts',(0.115596440733447,0.104084279688444,0.0889066365208618));
#8878=CARTESIAN_POINT('Ctrl Pts',(0.115246877053464,0.104471200524094,0.0889445770185912));
#8879=CARTESIAN_POINT('Ctrl Pts',(0.1146955270513,0.105075337068371,0.089003864028735));
#8880=CARTESIAN_POINT('Ctrl Pts',(0.114495058603682,0.105293741243097,0.0890253068505789));
#8881=CARTESIAN_POINT('Ctrl Pts',(0.114118889685862,0.105701221063637,0.0890653290028614));
#8882=CARTESIAN_POINT('Ctrl Pts',(0.113943345146594,0.105890430236815,0.0890839190988131));
#8883=CARTESIAN_POINT('Ctrl Pts',(0.113541427113537,0.106321477392285,0.0891262857528071));
#8884=CARTESIAN_POINT('Ctrl Pts',(0.113314751734507,0.106563029568117,0.089150038874487));
#8885=CARTESIAN_POINT('Ctrl Pts',(0.112615667305244,0.10730324227165,0.0892228704552363));
#8886=CARTESIAN_POINT('Ctrl Pts',(0.112140716672478,0.107799508512047,0.0892717590913689));
#8887=CARTESIAN_POINT('Ctrl Pts',(0.105410058011079,0.11473961231674,0.0899565808054583));
#8888=CARTESIAN_POINT('Ctrl Pts',(0.0986098782160602,0.120634188275095,
0.0905525431422003));
#8889=CARTESIAN_POINT('Ctrl Pts',(0.0835453215612041,0.131562374809492,
0.0917795091300265));
#8890=CARTESIAN_POINT('Ctrl Pts',(0.0752455179674333,0.136479212827507,
0.0924080151029762));
#8891=CARTESIAN_POINT('Ctrl Pts',(0.0625606422289995,0.142482974006043,
0.0933603769199756));
#8892=CARTESIAN_POINT('Ctrl Pts',(0.0584984990174048,0.144198305232682,
0.0936639678667445));
#8893=CARTESIAN_POINT('Ctrl Pts',(0.0534841057086612,0.146068975430538,
0.0940398198854358));
#8894=CARTESIAN_POINT('Ctrl Pts',(0.0525959262452387,0.146391132309801,
0.09410643001814));
#8895=CARTESIAN_POINT('Ctrl Pts',(0.0512003464698362,0.146882991526082,
0.094211176230548));
#8896=CARTESIAN_POINT('Ctrl Pts',(0.0506949004772042,0.147058205248446,
0.0942491297188462));
#8897=CARTESIAN_POINT('Ctrl Pts',(0.0497968667716964,0.147364330205717,
0.0943165967950538));
#8898=CARTESIAN_POINT('Ctrl Pts',(0.0494046393550158,0.147496289313962,
0.0943460755069624));
#8899=CARTESIAN_POINT('Ctrl Pts',(0.048499469048707,0.147796804847332,0.0944141348913068));
#8900=CARTESIAN_POINT('Ctrl Pts',(0.0479861683694208,0.147964258024481,
0.0944527513980877));
#8901=CARTESIAN_POINT('Ctrl Pts',(0.0465752887030418,0.14841641311634,0.0945589598256062));
#8902=CARTESIAN_POINT('Ctrl Pts',(0.0456759929124442,0.148695638130801,
0.0946267297538776));
#8903=CARTESIAN_POINT('Ctrl Pts',(0.0410682830418304,0.150080556510872,
0.0949743838729365));
#8904=CARTESIAN_POINT('Ctrl Pts',(0.0373223893648925,0.15105565743645,0.0952584556716677));
#8905=CARTESIAN_POINT('Ctrl Pts',(0.0315445934031727,0.152331661586899,
0.0956992788964798));
#8906=CARTESIAN_POINT('Ctrl Pts',(0.0295364100201812,0.152733743243059,
0.0958529679858877));
#8907=CARTESIAN_POINT('Ctrl Pts',(0.013002539994223,0.155705915445292,0.0971219733518095));
#8908=CARTESIAN_POINT('Ctrl Pts',(-0.00181097028508723,0.156237127116136,
0.0982917574966761));
#8909=CARTESIAN_POINT('Ctrl Pts',(-0.0190370354801933,0.15440215264804,
0.0995946714836518));
#8910=CARTESIAN_POINT('Ctrl Pts',(-0.0215906548923594,0.154065827447587,
0.0997860352101843));
#8911=CARTESIAN_POINT('Ctrl Pts',(-0.0246667820386182,0.153582688473664,
0.100013496516563));
#8912=CARTESIAN_POINT('Ctrl Pts',(-0.0251981988019866,0.153496394534569,
0.100052680492912));
#8913=CARTESIAN_POINT('Ctrl Pts',(-0.0260255327087407,0.153357635774511,
0.100113499571183));
#8914=CARTESIAN_POINT('Ctrl Pts',(-0.0263217568898874,0.153307070683407,
0.10013523875439));
#8915=CARTESIAN_POINT('Ctrl Pts',(-0.0268718887738776,0.153211522358686,
0.100175540737239));
#8916=CARTESIAN_POINT('Ctrl Pts',(-0.0271258287181839,0.153166766656477,
0.100194115696471));
#8917=CARTESIAN_POINT('Ctrl Pts',(-0.0277008428175408,0.153063948277369,
0.100236112945029));
#8918=CARTESIAN_POINT('Ctrl Pts',(-0.0280218456686519,0.153005506847545,
0.100259513500185));
#8919=CARTESIAN_POINT('Ctrl Pts',(-0.0289933446315104,0.152825476896183,
0.100330205888139));
#8920=CARTESIAN_POINT('Ctrl Pts',(-0.0296432624678985,0.152700744770797,
0.100377323741381));
#8921=CARTESIAN_POINT('Ctrl Pts',(-0.0346811631386657,0.151700494819882,
0.100741349702883));
#8922=CARTESIAN_POINT('Ctrl Pts',(-0.0390308352015495,0.150640056251004,
0.101048511024141));
#8923=CARTESIAN_POINT('Ctrl Pts',(-0.0502903072525949,0.147374423467926,
0.101839319898168));
#8924=CARTESIAN_POINT('Ctrl Pts',(-0.0570928375707449,0.144874005170402,
0.102313059788725));
#8925=CARTESIAN_POINT('Ctrl Pts',(-0.0636886551490397,0.141913909484965,
0.102789135277549));
#8926=CARTESIAN_POINT('Origin',(0.,0.,-0.129405622560373));
#8927=CARTESIAN_POINT('',(-0.0636885950184591,0.141913936470576,0.186516973639706));
#8928=CARTESIAN_POINT('',(-0.0636886258390813,0.141913922638794,0.172648810545196));
#8929=CARTESIAN_POINT('',(-0.0636886258329924,0.141913922641526,-0.129405622560373));
#8930=CARTESIAN_POINT('',(-0.155549942714367,-0.000133497404892293,0.12945317097425));
#8931=CARTESIAN_POINT('Ctrl Pts',(-0.063688595018437,0.141913936470586,
0.186516973639705));
#8932=CARTESIAN_POINT('Ctrl Pts',(-0.0547516337114912,0.145924694846607,
0.1858638558966));
#8933=CARTESIAN_POINT('Ctrl Pts',(-0.0454464797629655,0.149086491021556,
0.185228745135963));
#8934=CARTESIAN_POINT('Ctrl Pts',(-0.0292704465762964,0.152922845709905,
0.184118833909094));
#8935=CARTESIAN_POINT('Ctrl Pts',(-0.0225507434434849,0.154057132232873,
0.183656424950485));
#8936=CARTESIAN_POINT('Ctrl Pts',(-0.0147816897437891,0.154849310886087,
0.183109322551273));
#8937=CARTESIAN_POINT('Ctrl Pts',(-0.0137834585228433,0.154941355426672,
0.183038802246957));
#8938=CARTESIAN_POINT('Ctrl Pts',(-0.012183990092204,0.155073259663454,
0.182925416882625));
#8939=CARTESIAN_POINT('Ctrl Pts',(-0.0115832776387197,0.155119286801718,
0.182882744753399));
#8940=CARTESIAN_POINT('Ctrl Pts',(-0.0105179303025587,0.155194691857778,
0.182806904164193));
#8941=CARTESIAN_POINT('Ctrl Pts',(-0.0100533995318077,0.1552254759629,0.182773780085784));
#8942=CARTESIAN_POINT('Ctrl Pts',(-0.0090869914159759,0.155285162849253,
0.182704751594438));
#8943=CARTESIAN_POINT('Ctrl Pts',(-0.00858509890767695,0.155313718904405,
0.182668836736412));
#8944=CARTESIAN_POINT('Ctrl Pts',(-0.00728519311551275,0.15538135928089,
0.182575641941608));
#8945=CARTESIAN_POINT('Ctrl Pts',(-0.00648701011967386,0.155416728527545,
0.182518246658301));
#8946=CARTESIAN_POINT('Ctrl Pts',(-0.00305694329666138,0.155542253131225,
0.182270837842607));
#8947=CARTESIAN_POINT('Ctrl Pts',(-0.000423421283886921,0.155571708707789,
0.182078947633174));
#8948=CARTESIAN_POINT('Ctrl Pts',(0.0065303586225725,0.155472927086741,
0.181566769287899));
#8949=CARTESIAN_POINT('Ctrl Pts',(0.0108464483791228,0.155231520348021,
0.181243212047379));
#8950=CARTESIAN_POINT('Ctrl Pts',(0.027498725224259,0.153602276842521,0.179973542688244));
#8951=CARTESIAN_POINT('Ctrl Pts',(0.0396603851378657,0.150920006644976,
0.178996237327103));
#8952=CARTESIAN_POINT('Ctrl Pts',(0.0521330956168747,0.146555759436606,
0.177989540617218));
#8953=CARTESIAN_POINT('Ctrl Pts',(0.0528907209374828,0.146284045492707,
0.17792839330452));
#8954=CARTESIAN_POINT('Ctrl Pts',(0.0566934194818898,0.144886844377341,
0.177621595108224));
#8955=CARTESIAN_POINT('Ctrl Pts',(0.0597051221718255,0.143672000866532,
0.177378971935045));
#8956=CARTESIAN_POINT('Ctrl Pts',(0.0631791836847363,0.142142514713832,
0.177101236362889));
#8957=CARTESIAN_POINT('Ctrl Pts',(0.0636803457653474,0.141918699710725,
0.177061223958485));
#8958=CARTESIAN_POINT('Ctrl Pts',(0.0644832090229408,0.141555038117688,
0.176997221662148));
#8959=CARTESIAN_POINT('Ctrl Pts',(0.0647856585736385,0.141416871380987,
0.176973133507578));
#8960=CARTESIAN_POINT('Ctrl Pts',(0.0653228992149329,0.141169360759828,
0.176930388619169));
#8961=CARTESIAN_POINT('Ctrl Pts',(0.0655578625192123,0.141060399280504,
0.176911708817605));
#8962=CARTESIAN_POINT('Ctrl Pts',(0.0660577780660054,0.14082705040128,0.176871997332508));
#8963=CARTESIAN_POINT('Ctrl Pts',(0.0663226511489675,0.140702502167427,
0.176850975782961));
#8964=CARTESIAN_POINT('Ctrl Pts',(0.067041927429953,0.140361802729578,0.176793938174323));
#8965=CARTESIAN_POINT('Ctrl Pts',(0.0674956413189466,0.140144190463788,
0.176758010962983));
#8966=CARTESIAN_POINT('Ctrl Pts',(0.0698121476504684,0.13901927806143,0.176574803024153));
#8967=CARTESIAN_POINT('Ctrl Pts',(0.0716578485735978,0.138076969476781,
0.176429573657961));
#8968=CARTESIAN_POINT('Ctrl Pts',(0.0770308816922076,0.135197033132444,
0.176007360634448));
#8969=CARTESIAN_POINT('Ctrl Pts',(0.0805026809625757,0.133158996252508,
0.175735262078017));
#8970=CARTESIAN_POINT('Ctrl Pts',(0.0926941724550466,0.125350932158238,
0.17476811721607));
#8971=CARTESIAN_POINT('Ctrl Pts',(0.100905933775115,0.118840521275051,0.174092564810614));
#8972=CARTESIAN_POINT('Ctrl Pts',(0.11306205334004,0.107027949585954,0.172958987921739));
#8973=CARTESIAN_POINT('Ctrl Pts',(0.117432493036791,0.102213511529725,0.17251699971998));
#8974=CARTESIAN_POINT('Ctrl Pts',(0.122110043324089,0.0963635269647403,
0.171992199939395));
#8975=CARTESIAN_POINT('Ctrl Pts',(0.12272377571439,0.0955806821628197,0.171922216851082));
#8976=CARTESIAN_POINT('Ctrl Pts',(0.123695712300763,0.0943161360014855,
0.171809531129689));
#8977=CARTESIAN_POINT('Ctrl Pts',(0.124058717425556,0.0938381445057863,
0.171767017626774));
#8978=CARTESIAN_POINT('Ctrl Pts',(0.12469815147557,0.0929859663466096,0.171691359746565));
#8979=CARTESIAN_POINT('Ctrl Pts',(0.124975686944939,0.0926126156788095,
0.171658259027021));
#8980=CARTESIAN_POINT('Ctrl Pts',(0.125550247248289,0.0918324107704236,
0.171589179339217));
#8981=CARTESIAN_POINT('Ctrl Pts',(0.125846978403247,0.091425348059369,0.171553189517737));
#8982=CARTESIAN_POINT('Ctrl Pts',(0.126611954222842,0.0903651557686301,
0.171459583030827));
#8983=CARTESIAN_POINT('Ctrl Pts',(0.127077118727621,0.089709833240905,0.171401849089149));
#8984=CARTESIAN_POINT('Ctrl Pts',(0.129069537241057,0.0868563270160509,
0.171150967762642));
#8985=CARTESIAN_POINT('Ctrl Pts',(0.130544902077878,0.0846226557958453,
0.170955877687407));
#8986=CARTESIAN_POINT('Ctrl Pts',(0.134302246723993,0.0786018535376741,
0.170432986527685));
#8987=CARTESIAN_POINT('Ctrl Pts',(0.136481509337154,0.074753834456864,0.170101743536016));
#8988=CARTESIAN_POINT('Ctrl Pts',(0.144129260829888,0.0597977821701023,
0.168825938444051));
#8989=CARTESIAN_POINT('Ctrl Pts',(0.148428542713818,0.0481450395304601,
0.167851067287483));
#8990=CARTESIAN_POINT('Ctrl Pts',(0.152202686408833,0.0323298854149088,
0.166613409286367));
#8991=CARTESIAN_POINT('Ctrl Pts',(0.152962356934765,0.0285202210843172,
0.166321906167617));
#8992=CARTESIAN_POINT('Ctrl Pts',(0.153678950619842,0.0240620382810823,
0.165991304140812));
#8993=CARTESIAN_POINT('Ctrl Pts',(0.153775403873182,0.0234377206704377,
0.165945245724463));
#8994=CARTESIAN_POINT('Ctrl Pts',(0.153915635083043,0.0224918882546469,
0.165875845963868));
#8995=CARTESIAN_POINT('Ctrl Pts',(0.153962213322886,0.0221708058992135,
0.165852352608535));
#8996=CARTESIAN_POINT('Ctrl Pts',(0.154043985301968,0.0215944321772633,
0.16581030063509));
#8997=CARTESIAN_POINT('Ctrl Pts',(0.154079549351653,0.0213391982935048,
0.165791721538635));
#8998=CARTESIAN_POINT('Ctrl Pts',(0.154155384443697,0.020784874762471,0.165751463818454));
#8999=CARTESIAN_POINT('Ctrl Pts',(0.154195419341405,0.0204857567646991,
0.165729798643258));
#9000=CARTESIAN_POINT('Ctrl Pts',(0.154305253530392,0.01964657151326,0.165669174756813));
#9001=CARTESIAN_POINT('Ctrl Pts',(0.154373088639696,0.0191062441838966,
0.165630324681178));
#9002=CARTESIAN_POINT('Ctrl Pts',(0.154758007033303,0.0159042908461808,
0.165401129271739));
#9003=CARTESIAN_POINT('Ctrl Pts',(0.155009112345932,0.0132349776210906,
0.165214262687112));
#9004=CARTESIAN_POINT('Ctrl Pts',(0.156185481362583,-0.00405260664255331,
0.16402332579295));
#9005=CARTESIAN_POINT('Ctrl Pts',(0.155111150311053,-0.0187340395242954,
0.163094510693396));
#9006=CARTESIAN_POINT('Ctrl Pts',(0.151570014298421,-0.0350199697808364,
0.161974577435958));
#9007=CARTESIAN_POINT('Ctrl Pts',(0.1511033827012,-0.0369815462714318,0.161838293118428));
#9008=CARTESIAN_POINT('Ctrl Pts',(0.149623767401304,-0.0427048585837868,
0.161435745818667));
#9009=CARTESIAN_POINT('Ctrl Pts',(0.148507518051081,-0.046438017014586,
0.161166855466282));
#9010=CARTESIAN_POINT('Ctrl Pts',(0.14694833090306,-0.0510184385412151,
0.160827116432248));
#9011=CARTESIAN_POINT('Ctrl Pts',(0.146636119344421,-0.0519089728275574,
0.160760596641834));
#9012=CARTESIAN_POINT('Ctrl Pts',(0.14613242602927,-0.053304864116192,0.160655566323352));
#9013=CARTESIAN_POINT('Ctrl Pts',(0.145946376804749,-0.0538121692539915,
0.160617236041259));
#9014=CARTESIAN_POINT('Ctrl Pts',(0.145613203190448,-0.0547062039999561,
0.160549399037869));
#9015=CARTESIAN_POINT('Ctrl Pts',(0.145467171046953,-0.0550933375372713,
0.160519928967588));
#9016=CARTESIAN_POINT('Ctrl Pts',(0.145128992844146,-0.0559791346927276,
0.160452277246934));
#9017=CARTESIAN_POINT('Ctrl Pts',(0.144935819022094,-0.0564773975687085,
0.160414061513008));
#9018=CARTESIAN_POINT('Ctrl Pts',(0.144394878721728,-0.0578516182988463,
0.160308208370373));
#9019=CARTESIAN_POINT('Ctrl Pts',(0.144041717908249,-0.0587254133255446,
0.160240390613471));
#9020=CARTESIAN_POINT('Ctrl Pts',(0.142005700518275,-0.0636340757980171,
0.159856463657057));
#9021=CARTESIAN_POINT('Ctrl Pts',(0.140161435160248,-0.0675994054020957,
0.159534930030714));
#9022=CARTESIAN_POINT('Ctrl Pts',(0.133794953660373,-0.079903954863038,
0.15849919757464));
#9023=CARTESIAN_POINT('Ctrl Pts',(0.128676549976145,-0.0879092219880076,
0.157766253588319));
#9024=CARTESIAN_POINT('Ctrl Pts',(0.117240305671925,-0.102637907989317,
0.156320146337081));
#9025=CARTESIAN_POINT('Ctrl Pts',(0.110988697852455,-0.109368111070109,
0.155610275487766));
#9026=CARTESIAN_POINT('Ctrl Pts',(0.103671966195352,-0.115967209706039,
0.154888199958129));
#9027=CARTESIAN_POINT('Ctrl Pts',(0.103161038849738,-0.11642194987081,0.154838300314794));
#9028=CARTESIAN_POINT('Ctrl Pts',(0.102398636310875,-0.11709155029266,0.154764633015736));
#9029=CARTESIAN_POINT('Ctrl Pts',(0.102149458068934,-0.117308994071282,
0.154740680295833));
#9030=CARTESIAN_POINT('Ctrl Pts',(0.101704498029839,-0.117694792793475,
0.154698131151275));
#9031=CARTESIAN_POINT('Ctrl Pts',(0.101508989280126,-0.117863456038336,
0.15467951213126));
#9032=CARTESIAN_POINT('Ctrl Pts',(0.101087460535421,-0.118225277387001,
0.154639533007339));
#9033=CARTESIAN_POINT('Ctrl Pts',(0.100861307056234,-0.118418274069846,
0.15461818474709));
#9034=CARTESIAN_POINT('Ctrl Pts',(0.100234965217823,-0.118949690716906,
0.154559333214837));
#9035=CARTESIAN_POINT('Ctrl Pts',(0.099833612621343,-0.11928674270848,0.154521928579502));
#9036=CARTESIAN_POINT('Ctrl Pts',(0.0976178700080409,-0.121128485461158,
0.15431705865648));
#9037=CARTESIAN_POINT('Ctrl Pts',(0.0957710359323388,-0.122593918440155,
0.154152267516732));
#9038=CARTESIAN_POINT('Ctrl Pts',(0.0822858271866923,-0.132803381906686,
0.15298514996007));
#9039=CARTESIAN_POINT('Ctrl Pts',(0.0695030731198153,-0.139918307065511,
0.152061634398111));
#9040=CARTESIAN_POINT('Ctrl Pts',(0.053715630839533,-0.145999976098753,
0.150927747879091));
#9041=CARTESIAN_POINT('Ctrl Pts',(0.0514964701124916,-0.146797393795023,
0.1507686848099));
#9042=CARTESIAN_POINT('Ctrl Pts',(0.0454757451872059,-0.148807516398727,
0.150336782986503));
#9043=CARTESIAN_POINT('Ctrl Pts',(0.041644476239146,-0.149924825345288,
0.150061532498368));
#9044=CARTESIAN_POINT('Ctrl Pts',(0.0369341827546044,-0.151104002260415,
0.149720629425166));
#9045=CARTESIAN_POINT('Ctrl Pts',(0.0360918751996719,-0.151307401819402,
0.149659574805439));
#9046=CARTESIAN_POINT('Ctrl Pts',(0.0346949562912331,-0.151632400349437,
0.149558144119532));
#9047=CARTESIAN_POINT('Ctrl Pts',(0.0341412919989688,-0.151758021181475,
0.149517897102319));
#9048=CARTESIAN_POINT('Ctrl Pts',(0.0331373830802062,-0.151980026139405,
0.149444833196336));
#9049=CARTESIAN_POINT('Ctrl Pts',(0.0326873724276947,-0.152077447960423,
0.149412049888066));
#9050=CARTESIAN_POINT('Ctrl Pts',(0.0322357549628178,-0.152173120502424,
0.149379116121447));
#9051=CARTESIAN_POINT('Ctrl Pts',(0.0322345696545825,-0.152173371588628,
0.149379029683759));
#9052=CARTESIAN_POINT('Ctrl Pts',(0.0322322059491332,-0.152173872268217,
0.149378857311907));
#9053=CARTESIAN_POINT('Ctrl Pts',(0.0322310273115069,-0.152174121912682,
0.149378771360213));
#9054=CARTESIAN_POINT('Ctrl Pts',(0.0322286765883317,-0.152174619785296,
0.149378599934177));
#9055=CARTESIAN_POINT('Ctrl Pts',(0.032227504492861,-0.152174868015706,
0.149378514459115));
#9056=CARTESIAN_POINT('Ctrl Pts',(0.0322251667920374,-0.152175363073805,
0.149378343981833));
#9057=CARTESIAN_POINT('Ctrl Pts',(0.0322240011816163,-0.152175609902724,
0.149378258979246));
#9058=CARTESIAN_POINT('Ctrl Pts',(0.0322216764117314,-0.152176102166605,
0.149378089444066));
#9059=CARTESIAN_POINT('Ctrl Pts',(0.0322205172390236,-0.152176347604524,
0.14937800491051));
#9060=CARTESIAN_POINT('Ctrl Pts',(0.0322182052855862,-0.152176837099355,
0.149377836309097));
#9061=CARTESIAN_POINT('Ctrl Pts',(0.0322170524981316,-0.152177081157842,
0.149377752240753));
#9062=CARTESIAN_POINT('Ctrl Pts',(0.0322147532554497,-0.152177567906913,
0.149377584565415));
#9063=CARTESIAN_POINT('Ctrl Pts',(0.0322136067977378,-0.152177810598173,
0.149377500958242));
#9064=CARTESIAN_POINT('Ctrl Pts',(0.0322113201784562,-0.152178294620877,
0.149377334202621));
#9065=CARTESIAN_POINT('Ctrl Pts',(0.0322101800056327,-0.152178535954852,
0.149377251053355));
#9066=CARTESIAN_POINT('Ctrl Pts',(0.0316991731472682,-0.152286691905048,
0.149339984813314));
#9067=CARTESIAN_POINT('Ctrl Pts',(0.0311887731469123,-0.152392042203614,
0.149302720145424));
#9068=CARTESIAN_POINT('Ctrl Pts',(0.0298080652547318,-0.152669803513008,
0.14920179291402));
#9069=CARTESIAN_POINT('Ctrl Pts',(0.0289368074588397,-0.15283733435398,
0.149137976075716));
#9070=CARTESIAN_POINT('Ctrl Pts',(0.0269987402217567,-0.153192832351303,
0.14899571243784));
#9071=CARTESIAN_POINT('Ctrl Pts',(0.0259313131540722,-0.153377125886362,
0.14891715259092));
#9072=CARTESIAN_POINT('Ctrl Pts',(0.0226807515252329,-0.15390344023369,
0.148677258912362));
#9073=CARTESIAN_POINT('Ctrl Pts',(0.0204922597599656,-0.154210089745347,
0.148514839253952));
#9074=CARTESIAN_POINT('Ctrl Pts',(0.00334991008706172,-0.156240723797499,
0.147235129313097));
#9075=CARTESIAN_POINT('Ctrl Pts',(-0.0117747635777276,-0.155831865596905,
0.146050435500232));
#9076=CARTESIAN_POINT('Ctrl Pts',(-0.0275831092416756,-0.153088111616821,
0.144821713065297));
#9077=CARTESIAN_POINT('Ctrl Pts',(-0.0285644318820091,-0.152908047983781,
0.144745526597874));
#9078=CARTESIAN_POINT('Ctrl Pts',(-0.033316046149697,-0.151988830537548,
0.144377239524371));
#9079=CARTESIAN_POINT('Ctrl Pts',(-0.0370602039367026,-0.151119525722049,
0.144088885480912));
#9080=CARTESIAN_POINT('Ctrl Pts',(-0.0413767562929535,-0.149947202565584,
0.143761406030212));
#9081=CARTESIAN_POINT('Ctrl Pts',(-0.0419838287918148,-0.149778361838437,
0.143715466170576));
#9082=CARTESIAN_POINT('Ctrl Pts',(-0.0429015796008725,-0.149517096023816,
0.143646209426549));
#9083=CARTESIAN_POINT('Ctrl Pts',(-0.0432130126092813,-0.149427383976584,
0.143622741448045));
#9084=CARTESIAN_POINT('Ctrl Pts',(-0.0437715520658734,-0.149264597703823,
0.143580716442843));
#9085=CARTESIAN_POINT('Ctrl Pts',(-0.0440187580466708,-0.149191882625673,
0.143562139056385));
#9086=CARTESIAN_POINT('Ctrl Pts',(-0.0445553513344724,-0.149032595101734,
0.143521863778969));
#9087=CARTESIAN_POINT('Ctrl Pts',(-0.044844666728571,-0.14894579418543,
0.143500179431414));
#9088=CARTESIAN_POINT('Ctrl Pts',(-0.0456560346319368,-0.148699787765839,
0.143439448914677));
#9089=CARTESIAN_POINT('Ctrl Pts',(-0.0461775118148835,-0.148538674446524,
0.143400511992213));
#9090=CARTESIAN_POINT('Ctrl Pts',(-0.0492387501123485,-0.147575208140343,
0.143172441492734));
#9091=CARTESIAN_POINT('Ctrl Pts',(-0.0517586103782475,-0.146710412426594,
0.142986739257247));
#9092=CARTESIAN_POINT('Ctrl Pts',(-0.0598780282123614,-0.143688619595042,
0.142391194917996));
#9093=CARTESIAN_POINT('Ctrl Pts',(-0.0653756183348194,-0.141272218880717,
0.141992282973149));
#9094=CARTESIAN_POINT('Ctrl Pts',(-0.0790854035657697,-0.134274008029409,
0.140976151871489));
#9095=CARTESIAN_POINT('Ctrl Pts',(-0.0870461432685281,-0.129255440921728,
0.140364125473848));
#9096=CARTESIAN_POINT('Ctrl Pts',(-0.0947018146792362,-0.123399472859138,
0.139713436755087));
#9097=CARTESIAN_POINT('Ctrl Pts',(-0.094897796896862,-0.123248820475764,
0.139696735638923));
#9098=CARTESIAN_POINT('Ctrl Pts',(-0.0988960640349475,-0.120160144704847,
0.139355107221391));
#9099=CARTESIAN_POINT('Ctrl Pts',(-0.102560181859405,-0.117048251170178,
0.139025129970639));
#9100=CARTESIAN_POINT('Ctrl Pts',(-0.106746225794824,-0.1131454378215,0.138623658493219));
#9101=CARTESIAN_POINT('Ctrl Pts',(-0.107412724808465,-0.112512902842904,
0.138558956493561));
#9102=CARTESIAN_POINT('Ctrl Pts',(-0.108493486143699,-0.111468860443686,
0.138452728031849));
#9103=CARTESIAN_POINT('Ctrl Pts',(-0.108911111739892,-0.111060853170497,
0.138411353057405));
#9104=CARTESIAN_POINT('Ctrl Pts',(-0.109654962538559,-0.110325903559971,
0.138337064354729));
#9105=CARTESIAN_POINT('Ctrl Pts',(-0.109982049150166,-0.109999839372421,
0.138304189398948));
#9106=CARTESIAN_POINT('Ctrl Pts',(-0.110612332679272,-0.109365904511675,
0.13824043187762));
#9107=CARTESIAN_POINT('Ctrl Pts',(-0.110915708781466,-0.109058217246394,
0.138209557626091));
#9108=CARTESIAN_POINT('Ctrl Pts',(-0.111732858885005,-0.10822251847518,
0.138125889618168));
#9109=CARTESIAN_POINT('Ctrl Pts',(-0.112244164516321,-0.107692120218288,
0.138072989202101));
#9110=CARTESIAN_POINT('Ctrl Pts',(-0.114282925617486,-0.105546937631989,
0.137859818366441));
#9111=CARTESIAN_POINT('Ctrl Pts',(-0.115779387778606,-0.103903202772636,
0.137698235865585));
#9112=CARTESIAN_POINT('Ctrl Pts',(-0.119510575186018,-0.0996240972743058,
0.137281744278447));
#9113=CARTESIAN_POINT('Ctrl Pts',(-0.121693547429822,-0.0969454253964503,
0.137024860209447));
#9114=CARTESIAN_POINT('Ctrl Pts',(-0.127357582082388,-0.0895022097005319,
0.136321064310843));
#9115=CARTESIAN_POINT('Ctrl Pts',(-0.130659527387109,-0.0846089561619116,
0.135868700006317));
#9116=CARTESIAN_POINT('Ctrl Pts',(-0.139358985047391,-0.069988681580578,
0.134553029944301));
#9117=CARTESIAN_POINT('Ctrl Pts',(-0.14400283269987,-0.0598545485013284,
0.133681893259836));
#9118=CARTESIAN_POINT('Ctrl Pts',(-0.147891748703495,-0.0482198853745478,
0.132775143719688));
#9119=CARTESIAN_POINT('Ctrl Pts',(-0.14824443707268,-0.0471244497882592,
0.132690669564868));
#9120=CARTESIAN_POINT('Ctrl Pts',(-0.148709580649979,-0.0456228072575893,
0.132576187301951));
#9121=CARTESIAN_POINT('Ctrl Pts',(-0.148832578676592,-0.0452199453212849,
0.132545602567902));
#9122=CARTESIAN_POINT('Ctrl Pts',(-0.149025148762318,-0.0445799127353224,
0.132497221464874));
#9123=CARTESIAN_POINT('Ctrl Pts',(-0.14909579337474,-0.0443430714251948,
0.132479363601522));
#9124=CARTESIAN_POINT('Ctrl Pts',(-0.149240270165681,-0.0438544536130575,
0.132442616626082));
#9125=CARTESIAN_POINT('Ctrl Pts',(-0.149314029828064,-0.0436026586176383,
0.132423732196678));
#9126=CARTESIAN_POINT('Ctrl Pts',(-0.14948779402618,-0.0430038642967888,
0.132378944388203));
#9127=CARTESIAN_POINT('Ctrl Pts',(-0.149587228795776,-0.0426566981327582,
0.132353074050867));
#9128=CARTESIAN_POINT('Ctrl Pts',(-0.149795204919668,-0.0419209004237031,
0.132298441345078));
#9129=CARTESIAN_POINT('Ctrl Pts',(-0.149903445211676,-0.0415321855005446,
0.132269695981004));
#9130=CARTESIAN_POINT('Ctrl Pts',(-0.150195983137838,-0.0404655735940405,
0.132191128173938));
#9131=CARTESIAN_POINT('Ctrl Pts',(-0.15037720589022,-0.0397868319028949,
0.132141471370438));
#9132=CARTESIAN_POINT('Ctrl Pts',(-0.153859449839334,-0.0263808711836664,
0.131166952599816));
#9133=CARTESIAN_POINT('Ctrl Pts',(-0.155538655392449,-0.0132853806131935,
0.130322903296383));
#9134=CARTESIAN_POINT('Ctrl Pts',(-0.155549942714367,-0.000133497404892293,
0.12945317097425));
#9135=CARTESIAN_POINT('Ctrl Pts',(-0.155549942819317,-0.000133375062712872,
0.129453162883777));
#9136=CARTESIAN_POINT('Ctrl Pts',(-0.155555805801239,0.00670438369198078,
0.129000982730695));
#9137=CARTESIAN_POINT('Ctrl Pts',(-0.15511080758718,0.0135345765403181,
0.128543991051104));
#9138=CARTESIAN_POINT('Ctrl Pts',(-0.153889036609665,0.0228103386093192,
0.127900308785973));
#9139=CARTESIAN_POINT('Ctrl Pts',(-0.153499510118162,0.0252991361586018,
0.127725349529218));
#9140=CARTESIAN_POINT('Ctrl Pts',(-0.152927239502439,0.0284522860789925,
0.127500326413089));
#9141=CARTESIAN_POINT('Ctrl Pts',(-0.152800265776766,0.0291264813650497,
0.127452016581095));
#9142=CARTESIAN_POINT('Ctrl Pts',(-0.152575058385035,0.0302802523595054,
0.127368995110126));
#9143=CARTESIAN_POINT('Ctrl Pts',(-0.152479012274388,0.0307602491876375,
0.127334352818693));
#9144=CARTESIAN_POINT('Ctrl Pts',(-0.152294159988247,0.0316619175589571,
0.12726907925613));
#9145=CARTESIAN_POINT('Ctrl Pts',(-0.152205863943051,0.0320836900085918,
0.12723846445441));
#9146=CARTESIAN_POINT('Ctrl Pts',(-0.15201824844092,0.0329616844614085,
0.127174560832495));
#9147=CARTESIAN_POINT('Ctrl Pts',(-0.151918625268515,0.0334178363955861,
0.127141262607256));
#9148=CARTESIAN_POINT('Ctrl Pts',(-0.15168388345004,0.0344699200981673,
0.127064232807068));
#9149=CARTESIAN_POINT('Ctrl Pts',(-0.151547304691091,0.0350655145577277,
0.127020454924969));
#9150=CARTESIAN_POINT('Ctrl Pts',(-0.151170654181454,0.0366647057491829,
0.12690244209779));
#9151=CARTESIAN_POINT('Ctrl Pts',(-0.150924102806883,0.0376667284193124,
0.126828000522904));
#9152=CARTESIAN_POINT('Ctrl Pts',(-0.148639944313082,0.046567232605343,
0.126162222061261));
#9153=CARTESIAN_POINT('Ctrl Pts',(-0.145994319561966,0.0542950834051834,
0.125551126060616));
#9154=CARTESIAN_POINT('Ctrl Pts',(-0.140446089421772,0.0671156830038609,
0.124480997822295));
#9155=CARTESIAN_POINT('Ctrl Pts',(-0.137839138849583,0.072318636030586,
0.124029726649834));
#9156=CARTESIAN_POINT('Ctrl Pts',(-0.131829396085029,0.0828016316060835,
0.123092878355514));
#9157=CARTESIAN_POINT('Ctrl Pts',(-0.128385455108062,0.0880470720303393,
0.122608181432154));
#9158=CARTESIAN_POINT('Ctrl Pts',(-0.123043581632665,0.0952005544037684,
0.121936086612204));
#9159=CARTESIAN_POINT('Ctrl Pts',(-0.12139862353349,0.0972894909191922,
0.121738402845313));
#9160=CARTESIAN_POINT('Ctrl Pts',(-0.119352307386806,0.0997553357799539,
0.121504285668986));
#9161=CARTESIAN_POINT('Ctrl Pts',(-0.119001600882609,0.100173446114688,
0.121464561512281));
#9162=CARTESIAN_POINT('Ctrl Pts',(-0.118453381361028,0.100820088103071,
0.121403093998487));
#9163=CARTESIAN_POINT('Ctrl Pts',(-0.118257395637145,0.101049899071366,
0.121381242869438));
#9164=CARTESIAN_POINT('Ctrl Pts',(-0.117892967677068,0.101474711469062,
0.121340841395603));
#9165=CARTESIAN_POINT('Ctrl Pts',(-0.117724711838345,0.101669863381236,
0.121322278333307));
#9166=CARTESIAN_POINT('Ctrl Pts',(-0.117343725813944,0.102109537029153,
0.121280447758162));
#9167=CARTESIAN_POINT('Ctrl Pts',(-0.117130716333378,0.102353812027828,
0.121257201277273));
#9168=CARTESIAN_POINT('Ctrl Pts',(-0.116501310208449,0.103071064350553,
0.121188919361571));
#9169=CARTESIAN_POINT('Ctrl Pts',(-0.116082794324041,0.103542186981093,
0.121144037342716));
#9170=CARTESIAN_POINT('Ctrl Pts',(-0.113091338590442,0.106868727399821,
0.120826794204234));
#9171=CARTESIAN_POINT('Ctrl Pts',(-0.110415935172786,0.109630758853381,
0.120561605863823));
#9172=CARTESIAN_POINT('Ctrl Pts',(-0.106527884950608,0.113357789048688,
0.120196224490214));
#9173=CARTESIAN_POINT('Ctrl Pts',(-0.10539928090054,0.114407912574821,0.120092377707706));
#9174=CARTESIAN_POINT('Ctrl Pts',(-0.101295536149757,0.118114016999504,
0.119721818812999));
#9175=CARTESIAN_POINT('Ctrl Pts',(-0.0982340339323089,0.120672215885626,
0.119458303932637));
#9176=CARTESIAN_POINT('Ctrl Pts',(-0.0888463985780042,0.127922258405213,
0.1186767935642));
#9177=CARTESIAN_POINT('Ctrl Pts',(-0.0822592730425939,0.132254265392426,
0.118161557082653));
#9178=CARTESIAN_POINT('Ctrl Pts',(-0.0720657925292953,0.137900744710627,
0.117378082407623));
#9179=CARTESIAN_POINT('Ctrl Pts',(-0.0686934037247811,0.139611269791126,
0.117121065525822));
#9180=CARTESIAN_POINT('Ctrl Pts',(-0.0647390242514229,0.14143900980572,
0.116820229350733));
#9181=CARTESIAN_POINT('Ctrl Pts',(-0.0642144734262393,0.14167793092233,
0.116780334887106));
#9182=CARTESIAN_POINT('Ctrl Pts',(-0.0636886257863082,0.141913922662477,
0.116740348554263));
#9183=CARTESIAN_POINT('Ctrl Pts',(-0.0636886551490397,0.141913909484965,
0.102789135277549));
#9184=CARTESIAN_POINT('Ctrl Pts',(-0.0706385455446796,0.138794911676096,
0.103290767172019));
#9185=CARTESIAN_POINT('Ctrl Pts',(-0.0773589325761553,0.135165584427428,
0.103795169971365));
#9186=CARTESIAN_POINT('Ctrl Pts',(-0.0869787906224297,0.129014663481055,
0.104573891824348));
#9187=CARTESIAN_POINT('Ctrl Pts',(-0.0900881810529839,0.12686295364493,
0.104835181778715));
#9188=CARTESIAN_POINT('Ctrl Pts',(-0.0938384349741554,0.124060324867915,
0.105164181681259));
#9189=CARTESIAN_POINT('Ctrl Pts',(-0.0945562316998756,0.123514108790094,
0.105227803857689));
#9190=CARTESIAN_POINT('Ctrl Pts',(-0.0956845658241266,0.122639889221374,
0.105328874323912));
#9191=CARTESIAN_POINT('Ctrl Pts',(-0.0960982697677787,0.122315988736132,
0.105366160660117));
#9192=CARTESIAN_POINT('Ctrl Pts',(-0.0968715270618784,0.121704239348659,
0.105436288563915));
#9193=CARTESIAN_POINT('Ctrl Pts',(-0.0972314593618795,0.121416876638781,
0.105469110516049));
#9194=CARTESIAN_POINT('Ctrl Pts',(-0.0980350073753849,0.120769475653918,
0.105542791609919));
#9195=CARTESIAN_POINT('Ctrl Pts',(-0.098477924362814,0.120408584901165,
0.105583684721936));
#9196=CARTESIAN_POINT('Ctrl Pts',(-0.0995967513221978,0.119486657152731,
0.105687702708321));
#9197=CARTESIAN_POINT('Ctrl Pts',(-0.100269907734776,0.118922326143927,
0.105750960580353));
#9198=CARTESIAN_POINT('Ctrl Pts',(-0.104109502649637,0.115647680672805,
0.106115722098118));
#9199=CARTESIAN_POINT('Ctrl Pts',(-0.107170473938427,0.112816922366711,
0.106422163583893));
#9200=CARTESIAN_POINT('Ctrl Pts',(-0.111360857793215,0.108617120598283,
0.106865248268274));
#9201=CARTESIAN_POINT('Ctrl Pts',(-0.112586450099176,0.107346217333874,
0.1069979209144));
#9202=CARTESIAN_POINT('Ctrl Pts',(-0.12384338939518,0.0952682286987803,
0.108245627673472));
#9203=CARTESIAN_POINT('Ctrl Pts',(-0.132310477421477,0.0831088504158885,
0.109415149140087));
#9204=CARTESIAN_POINT('Ctrl Pts',(-0.140084268475597,0.0676659855061544,
0.110715156732754));
#9205=CARTESIAN_POINT('Ctrl Pts',(-0.141173384041356,0.0653633348979577,
0.110904371977293));
#9206=CARTESIAN_POINT('Ctrl Pts',(-0.142422875056337,0.0625445024681927,
0.111129599785222));
#9207=CARTESIAN_POINT('Ctrl Pts',(-0.142637675483297,0.0620530715100431,
0.111168633544894));
#9208=CARTESIAN_POINT('Ctrl Pts',(-0.14296862570722,0.0612851083708011,
0.111229259908833));
#9209=CARTESIAN_POINT('Ctrl Pts',(-0.143086521887947,0.0610093411109938,
0.111250955742889));
#9210=CARTESIAN_POINT('Ctrl Pts',(-0.143304259411854,0.0604959351692327,
0.11129120712845));
#9211=CARTESIAN_POINT('Ctrl Pts',(-0.143404306649491,0.0602583917290455,
0.111309774674413));
#9212=CARTESIAN_POINT('Ctrl Pts',(-0.143629797761343,0.0597192630568167,
0.111351789720478));
#9213=CARTESIAN_POINT('Ctrl Pts',(-0.143754882240401,0.0594175312712788,
0.111375215322197));
#9214=CARTESIAN_POINT('Ctrl Pts',(-0.144131302840691,0.0585013736832179,
0.111446080995303));
#9215=CARTESIAN_POINT('Ctrl Pts',(-0.144379661478246,0.0578857199578396,
0.11149334570905));
#9216=CARTESIAN_POINT('Ctrl Pts',(-0.146297497227193,0.0530424759419743,
0.11186252198048));
#9217=CARTESIAN_POINT('Ctrl Pts',(-0.147785087627223,0.0487446373652794,
0.112174367869767));
#9218=CARTESIAN_POINT('Ctrl Pts',(-0.153364496529452,0.0300052360032902,
0.113492463580175));
#9219=CARTESIAN_POINT('Ctrl Pts',(-0.155543053855193,0.0150793605078501,
0.114446301523442));
#9220=CARTESIAN_POINT('Ctrl Pts',(-0.155550077037969,-0.000130914471409132,
0.115485075421146));
#9221=CARTESIAN_POINT('Ctrl Pts',(-0.15554977427191,-0.000333650716531503,
0.115498931426319));
#9222=CARTESIAN_POINT('Ctrl Pts',(-0.155545683823176,-0.0015198766800267,
0.115580065613003));
#9223=CARTESIAN_POINT('Ctrl Pts',(-0.155532964948277,-0.00250330332611001,
0.115647577023153));
#9224=CARTESIAN_POINT('Ctrl Pts',(-0.155460202960187,-0.00574873535517704,
0.115871280317847));
#9225=CARTESIAN_POINT('Ctrl Pts',(-0.155360130892678,-0.00800946243452763,
0.116028569190131));
#9226=CARTESIAN_POINT('Ctrl Pts',(-0.15515259455218,-0.0111468487396825,
0.116249262821473));
#9227=CARTESIAN_POINT('Ctrl Pts',(-0.155086922608274,-0.0120260638629871,
0.116311372687011));
#9228=CARTESIAN_POINT('Ctrl Pts',(-0.154966303389103,-0.0134749703139348,
0.116414182947297));
#9229=CARTESIAN_POINT('Ctrl Pts',(-0.154915679293732,-0.0140450099368733,
0.116454747896279));
#9230=CARTESIAN_POINT('Ctrl Pts',(-0.154818637195961,-0.0150732946732276,
0.116528138660411));
#9231=CARTESIAN_POINT('Ctrl Pts',(-0.154773327121212,-0.015531639932309,
0.116560929371149));
#9232=CARTESIAN_POINT('Ctrl Pts',(-0.154672056728187,-0.0165115888872842,
0.116631205947826));
#9233=CARTESIAN_POINT('Ctrl Pts',(-0.154615492142895,-0.0170331229394871,
0.116668710403071));
#9234=CARTESIAN_POINT('Ctrl Pts',(-0.154454891891054,-0.0184471184536732,
0.116770678309198));
#9235=CARTESIAN_POINT('Ctrl Pts',(-0.154345761308043,-0.0193389687322384,
0.116835301005697));
#9236=CARTESIAN_POINT('Ctrl Pts',(-0.153743151429852,-0.0239331731630626,
0.117169831901331));
#9237=CARTESIAN_POINT('Ctrl Pts',(-0.153124203003052,-0.0276175197948567,
0.117443652502398));
#9238=CARTESIAN_POINT('Ctrl Pts',(-0.149374584530788,-0.0458854074301121,
0.118830662725052));
#9239=CARTESIAN_POINT('Ctrl Pts',(-0.144290258070929,-0.0599866995284198,
0.12000600546946));
#9240=CARTESIAN_POINT('Ctrl Pts',(-0.135162584725455,-0.077117738665688,
0.121489934379906));
#9241=CARTESIAN_POINT('Ctrl Pts',(-0.13287388269345,-0.0809975966507191,
0.121829326261002));
#9242=CARTESIAN_POINT('Ctrl Pts',(-0.130058755849486,-0.0853285498316267,
0.122207707320979));
#9243=CARTESIAN_POINT('Ctrl Pts',(-0.129694153688685,-0.0858817089419614,
0.122256024792016));
#9244=CARTESIAN_POINT('Ctrl Pts',(-0.129144677336626,-0.0867038714488613,
0.122327804337203));
#9245=CARTESIAN_POINT('Ctrl Pts',(-0.128962479095646,-0.0869746399787034,
0.122351438296505));
#9246=CARTESIAN_POINT('Ctrl Pts',(-0.128634863998955,-0.0874582225768048,
0.122393634613066));
#9247=CARTESIAN_POINT('Ctrl Pts',(-0.128489769814232,-0.0876712495002865,
0.122412218121612));
#9248=CARTESIAN_POINT('Ctrl Pts',(-0.12817456538751,-0.088131568544732,
0.122452363684521));
#9249=CARTESIAN_POINT('Ctrl Pts',(-0.128004269168859,-0.0883787285783763,
0.122473912839279));
#9250=CARTESIAN_POINT('Ctrl Pts',(-0.127527134651975,-0.0890669473196047,
0.122533903784023));
#9251=CARTESIAN_POINT('Ctrl Pts',(-0.127218720921191,-0.0895069173154188,
0.122572240524891));
#9252=CARTESIAN_POINT('Ctrl Pts',(-0.125426776620938,-0.0920352555871656,
0.122792517972867));
#9253=CARTESIAN_POINT('Ctrl Pts',(-0.123894007031203,-0.0940884777344814,
0.122971287695339));
#9254=CARTESIAN_POINT('Ctrl Pts',(-0.113207281920229,-0.107689555128207,
0.124161840311325));
#9255=CARTESIAN_POINT('Ctrl Pts',(-0.102502498883451,-0.11792487910962,
0.125095824726007));
#9256=CARTESIAN_POINT('Ctrl Pts',(-0.0890095334445175,-0.127579531110364,
0.126210421160723));
#9257=CARTESIAN_POINT('Ctrl Pts',(-0.0874839894727898,-0.12863042024781,
0.126335537418819));
#9258=CARTESIAN_POINT('Ctrl Pts',(-0.0825409520511248,-0.131906877151387,
0.126738774955476));
#9259=CARTESIAN_POINT('Ctrl Pts',(-0.0790548178875261,-0.134025235668758,
0.127019978917594));
#9260=CARTESIAN_POINT('Ctrl Pts',(-0.0747268648359269,-0.136427487850475,
0.127367469037761));
#9261=CARTESIAN_POINT('Ctrl Pts',(-0.0739604589619583,-0.13684448919969,
0.127428941143569));
#9262=CARTESIAN_POINT('Ctrl Pts',(-0.0726880633310731,-0.137522988267405,
0.127530916425332));
#9263=CARTESIAN_POINT('Ctrl Pts',(-0.0721840657197892,-0.137788197946449,
0.127571288046938));
#9264=CARTESIAN_POINT('Ctrl Pts',(-0.0712699716560731,-0.138262813737666,
0.127644477611306));
#9265=CARTESIAN_POINT('Ctrl Pts',(-0.0708603781886651,-0.138473179053262,
0.127677261372564));
#9266=CARTESIAN_POINT('Ctrl Pts',(-0.069980228040502,-0.138920292451442,
0.127747687074279));
#9267=CARTESIAN_POINT('Ctrl Pts',(-0.0695093919410487,-0.139156474483865,
0.127785348316346));
#9268=CARTESIAN_POINT('Ctrl Pts',(-0.0682237139890469,-0.139793246569915,
0.127888157680868));
#9269=CARTESIAN_POINT('Ctrl Pts',(-0.0674065608818435,-0.140189095232688,
0.127953469464895));
#9270=CARTESIAN_POINT('Ctrl Pts',(-0.0630960554115809,-0.142230807515395,
0.128297872962092));
#9271=CARTESIAN_POINT('Ctrl Pts',(-0.0595460741624127,-0.143753173753649,
0.128581157103115));
#9272=CARTESIAN_POINT('Ctrl Pts',(-0.0421081658824659,-0.150474436659898,
0.129972576881888));
#9273=CARTESIAN_POINT('Ctrl Pts',(-0.0275824082838605,-0.153800898223667,
0.13114129354303));
#9274=CARTESIAN_POINT('Ctrl Pts',(-0.00838123767623072,-0.155387607567937,
0.132613616267623));
#9275=CARTESIAN_POINT('Ctrl Pts',(-0.00393791286297731,-0.15556367088544,
0.132948527677967));
#9276=CARTESIAN_POINT('Ctrl Pts',(0.00116806411789234,-0.155547017669804,
0.133322537632243));
#9277=CARTESIAN_POINT('Ctrl Pts',(0.00182879797403608,-0.155540652627275,
0.133370726395007));
#9278=CARTESIAN_POINT('Ctrl Pts',(0.00281550095454516,-0.155524858999269,
0.133442356247465));
#9279=CARTESIAN_POINT('Ctrl Pts',(0.00314150183058143,-0.155518615554276,
0.133465968105366));
#9280=CARTESIAN_POINT('Ctrl Pts',(0.00372517554819278,-0.155505601200461,
0.13350814297036));
#9281=CARTESIAN_POINT('Ctrl Pts',(0.00398285225734731,-0.155499214882348,
0.1335267270211));
#9282=CARTESIAN_POINT('Ctrl Pts',(0.00454083203693389,-0.155483997890049,
0.133566893148311));
#9283=CARTESIAN_POINT('Ctrl Pts',(0.00484112495049768,-0.155474937751516,
0.133588462238073));
#9284=CARTESIAN_POINT('Ctrl Pts',(0.00567968161233166,-0.155447205790621,
0.133648565287772));
#9285=CARTESIAN_POINT('Ctrl Pts',(0.00621788457832035,-0.155426608100472,
0.133686993559254));
#9286=CARTESIAN_POINT('Ctrl Pts',(0.00933626859016975,-0.155291039856502,
0.133908853816108));
#9287=CARTESIAN_POINT('Ctrl Pts',(0.0119135682168439,-0.155114609135302,
0.134089061214026));
#9288=CARTESIAN_POINT('Ctrl Pts',(0.0291399058049222,-0.153503418054419,
0.135279603111998));
#9289=CARTESIAN_POINT('Ctrl Pts',(0.0435270414129684,-0.150059786605862,
0.13621260504786));
#9290=CARTESIAN_POINT('Ctrl Pts',(0.0589601803972402,-0.143954902099785,
0.137327611070788));
#9291=CARTESIAN_POINT('Ctrl Pts',(0.0606907156997419,-0.143233911310728,
0.137454243946822));
#9292=CARTESIAN_POINT('Ctrl Pts',(0.0661193951893142,-0.140856122829706,
0.137857310731186));
#9293=CARTESIAN_POINT('Ctrl Pts',(0.0697657881507205,-0.13908613041145,
0.138136764490696));
#9294=CARTESIAN_POINT('Ctrl Pts',(0.0741064250623704,-0.136765486042756,
0.138482306125629));
#9295=CARTESIAN_POINT('Ctrl Pts',(0.0748706950355498,-0.136348595071883,
0.138543643759503));
#9296=CARTESIAN_POINT('Ctrl Pts',(0.0761285374417257,-0.135648707823806,
0.138645440343138));
#9297=CARTESIAN_POINT('Ctrl Pts',(0.0766241359575988,-0.135369375858926,
0.138685768526715));
#9298=CARTESIAN_POINT('Ctrl Pts',(0.0775180035234204,-0.134859087870266,
0.138758909283748));
#9299=CARTESIAN_POINT('Ctrl Pts',(0.0779168026918441,-0.134629069302972,
0.138791687864545));
#9300=CARTESIAN_POINT('Ctrl Pts',(0.078770020180844,-0.13413189139421,0.138862135586966));
#9301=CARTESIAN_POINT('Ctrl Pts',(0.0792241121522437,-0.133864186432881,
0.138899824172253));
#9302=CARTESIAN_POINT('Ctrl Pts',(0.0804582186444308,-0.133128153684733,
0.139002792480867));
#9303=CARTESIAN_POINT('Ctrl Pts',(0.0812354882759923,-0.13265528873801,
0.139068236751931));
#9304=CARTESIAN_POINT('Ctrl Pts',(0.0853118684529381,-0.130126093320621,
0.13941464773595));
#9305=CARTESIAN_POINT('Ctrl Pts',(0.0885368940020133,-0.127953618400233,
0.139699865841379));
#9306=CARTESIAN_POINT('Ctrl Pts',(0.103637272725672,-0.116937183228877,
0.141091840840225));
#9307=CARTESIAN_POINT('Ctrl Pts',(0.11428966313307,-0.10654912072968,0.142258824418465));
#9308=CARTESIAN_POINT('Ctrl Pts',(0.1260177190381,-0.0912965134908927,0.143729114425927));
#9309=CARTESIAN_POINT('Ctrl Pts',(0.128572703051685,-0.0876617820074358,
0.144063723923184));
#9310=CARTESIAN_POINT('Ctrl Pts',(0.131325279211541,-0.0833661195061936,
0.144437433129076));
#9311=CARTESIAN_POINT('Ctrl Pts',(0.131678127393583,-0.082807666611234,
0.14448560873573));
#9312=CARTESIAN_POINT('Ctrl Pts',(0.132199785065882,-0.0819702726658703,
0.144557221078397));
#9313=CARTESIAN_POINT('Ctrl Pts',(0.132371286333957,-0.081693031110227,
0.144580828507199));
#9314=CARTESIAN_POINT('Ctrl Pts',(0.132676812490045,-0.0811956424406442,
0.144622997045343));
#9315=CARTESIAN_POINT('Ctrl Pts',(0.132811162379304,-0.0809757005209628,
0.144641579184054));
#9316=CARTESIAN_POINT('Ctrl Pts',(0.133100936291169,-0.0804986553469477,
0.144681743273674));
#9317=CARTESIAN_POINT('Ctrl Pts',(0.13325616190262,-0.0802414361374415,
0.144703312229576));
#9318=CARTESIAN_POINT('Ctrl Pts',(0.133687596400143,-0.0795218156850044,
0.144763417137694));
#9319=CARTESIAN_POINT('Ctrl Pts',(0.133962153944662,-0.0790584210221566,
0.144801847379823));
#9320=CARTESIAN_POINT('Ctrl Pts',(0.135539619336425,-0.076364181691027,
0.145023760204471));
#9321=CARTESIAN_POINT('Ctrl Pts',(0.136789294943068,-0.0741024125780319,
0.145204016194217));
#9322=CARTESIAN_POINT('Ctrl Pts',(0.144776204159051,-0.0587557354086258,
0.146394483986495));
#9323=CARTESIAN_POINT('Ctrl Pts',(0.149683989514654,-0.044801767878852,
0.147327385335938));
#9324=CARTESIAN_POINT('Ctrl Pts',(0.152922665071086,-0.0285299791630497,
0.148441992503164));
#9325=CARTESIAN_POINT('Ctrl Pts',(0.153254666718231,-0.026689097881679,
0.14856834276781));
#9326=CARTESIAN_POINT('Ctrl Pts',(0.154201303969297,-0.0208379144722291,
0.148971439284641));
#9327=CARTESIAN_POINT('Ctrl Pts',(0.154692251054584,-0.0168096217345331,
0.149251217219409));
#9328=CARTESIAN_POINT('Ctrl Pts',(0.155096657365621,-0.0118990686046017,
0.149597117011384));
#9329=CARTESIAN_POINT('Ctrl Pts',(0.155160845717928,-0.011030542182039,
0.149658476653839));
#9330=CARTESIAN_POINT('Ctrl Pts',(0.155254906593456,-0.00959376006181592,
0.149760301869139));
#9331=CARTESIAN_POINT('Ctrl Pts',(0.155288960858057,-0.00902578935509894,
0.149800636539955));
#9332=CARTESIAN_POINT('Ctrl Pts',(0.155344929875334,-0.00799795057847217,
0.149873783726313));
#9333=CARTESIAN_POINT('Ctrl Pts',(0.155367920773401,-0.00753814550303406,
0.1499065622167));
#9334=CARTESIAN_POINT('Ctrl Pts',(0.15541285306968,-0.00655174644955265,
0.149977003829522));
#9335=CARTESIAN_POINT('Ctrl Pts',(0.155434159908823,-0.0060251308377031,
0.150014686369657));
#9336=CARTESIAN_POINT('Ctrl Pts',(0.155484937423368,-0.0045895362622885,
0.15011762309413));
#9337=CARTESIAN_POINT('Ctrl Pts',(0.155509112833656,-0.00368040338539662,
0.150183041662213));
#9338=CARTESIAN_POINT('Ctrl Pts',(0.1555944850618,0.00111098136566404,0.150529081178344));
#9339=CARTESIAN_POINT('Ctrl Pts',(0.155518273397871,0.00499396816634459,
0.150813942742622));
#9340=CARTESIAN_POINT('Ctrl Pts',(0.154452482579347,0.0236545031885006,
0.152205798608921));
#9341=CARTESIAN_POINT('Ctrl Pts',(0.151500880857875,0.0382418732409599,
0.153373084026912));
#9342=CARTESIAN_POINT('Ctrl Pts',(0.145044118074665,0.0563713509820373,
0.154843732628452));
#9343=CARTESIAN_POINT('Ctrl Pts',(0.143375461416402,0.0604897642121254,
0.155178398590222));
#9344=CARTESIAN_POINT('Ctrl Pts',(0.141258570236774,0.0651325971259948,
0.155552163182417));
#9345=CARTESIAN_POINT('Ctrl Pts',(0.140980686608145,0.0657319170508707,
0.155600340546433));
#9346=CARTESIAN_POINT('Ctrl Pts',(0.14055997408423,0.0666243383575321,0.155671955038173));
#9347=CARTESIAN_POINT('Ctrl Pts',(0.140420033035468,0.0669187799033785,
0.155695562871136));
#9348=CARTESIAN_POINT('Ctrl Pts',(0.140167800177061,0.0674452127238864,
0.15573773207893));
#9349=CARTESIAN_POINT('Ctrl Pts',(0.140055857030071,0.0676773657950092,
0.155756314483062));
#9350=CARTESIAN_POINT('Ctrl Pts',(0.139812174826001,0.0681795315913519,
0.155796479226402));
#9351=CARTESIAN_POINT('Ctrl Pts',(0.13968023073895,0.068449440483249,0.155818048570095));
#9352=CARTESIAN_POINT('Ctrl Pts',(0.139309555190041,0.0692021707518959,
0.155878154041943));
#9353=CARTESIAN_POINT('Ctrl Pts',(0.139069093580581,0.0696841433729341,
0.155916584463651));
#9354=CARTESIAN_POINT('Ctrl Pts',(0.137660855033631,0.072470442480767,0.156138488983379));
#9355=CARTESIAN_POINT('Ctrl Pts',(0.136438234202659,0.0747468152831139,
0.15631873690612));
#9356=CARTESIAN_POINT('Ctrl Pts',(0.127874780907324,0.0897799784498791,
0.157509242008481));
#9357=CARTESIAN_POINT('Ctrl Pts',(0.118811545855129,0.101470833689925,0.158442183290816));
#9358=CARTESIAN_POINT('Ctrl Pts',(0.106893470341627,0.113018133323992,0.159557040303562));
#9359=CARTESIAN_POINT('Ctrl Pts',(0.105524545501431,0.11429734191863,0.159683595479395));
#9360=CARTESIAN_POINT('Ctrl Pts',(0.101121530682333,0.118265258634068,0.160086693782468));
#9361=CARTESIAN_POINT('Ctrl Pts',(0.0980054928101562,0.120860058956407,
0.160366260603895));
#9362=CARTESIAN_POINT('Ctrl Pts',(0.094101552809794,0.123860640956834,0.160711927862183));
#9363=CARTESIAN_POINT('Ctrl Pts',(0.0934067752787468,0.124385428795347,
0.160773273949869));
#9364=CARTESIAN_POINT('Ctrl Pts',(0.0922507889961369,0.125243435454709,
0.160875081962068));
#9365=CARTESIAN_POINT('Ctrl Pts',(0.0917920857036551,0.125580011074519,
0.160915413072385));
#9366=CARTESIAN_POINT('Ctrl Pts',(0.0909588761914181,0.126184378200024,
0.160988557380435));
#9367=CARTESIAN_POINT('Ctrl Pts',(0.0905850060835521,0.12645303920516,0.161021336574019));
#9368=CARTESIAN_POINT('Ctrl Pts',(0.0897805339143425,0.127025729993788,
0.161091783670405));
#9369=CARTESIAN_POINT('Ctrl Pts',(0.0893495692330081,0.127329237866431,
0.161129471008738));
#9370=CARTESIAN_POINT('Ctrl Pts',(0.0881706474560099,0.128150563790848,
0.16123243097855));
#9371=CARTESIAN_POINT('Ctrl Pts',(0.0874196874277055,0.128664013062905,
0.161297868107159));
#9372=CARTESIAN_POINT('Ctrl Pts',(0.0857538929141479,0.129781640612057,
0.161442720110232));
#9373=CARTESIAN_POINT('Ctrl Pts',(0.0848370946983941,0.130382788889746,
0.161522244269175));
#9374=CARTESIAN_POINT('Ctrl Pts',(0.0820218871204731,0.132186468348424,
0.16176587904077));
#9375=CARTESIAN_POINT('Ctrl Pts',(0.0801037812441496,0.133357548151939,
0.161931115291894));
#9376=CARTESIAN_POINT('Ctrl Pts',(0.0650421375642345,0.142111089809795,
0.163223215049242));
#9377=CARTESIAN_POINT('Ctrl Pts',(0.050879186398803,0.147774078272349,0.164418481600227));
#9378=CARTESIAN_POINT('Ctrl Pts',(0.0347539700387688,0.151624383686798,
0.165686709717775));
#9379=CARTESIAN_POINT('Ctrl Pts',(0.0333775532430762,0.15193331209725,0.165794162855451));
#9380=CARTESIAN_POINT('Ctrl Pts',(0.0287818774268354,0.152899314435191,
0.166149914789407));
#9381=CARTESIAN_POINT('Ctrl Pts',(0.0255457471264085,0.153473175890718,
0.166395528692922));
#9382=CARTESIAN_POINT('Ctrl Pts',(0.0217486045534025,0.154023062962571,
0.16667626967173));
#9383=CARTESIAN_POINT('Ctrl Pts',(0.0212032050239982,0.154099090994946,
0.166716414963485));
#9384=CARTESIAN_POINT('Ctrl Pts',(0.0203273623986443,0.154216444388624,
0.166780584531424));
#9385=CARTESIAN_POINT('Ctrl Pts',(0.0199971770621088,0.154259606822837,
0.166804707909536));
#9386=CARTESIAN_POINT('Ctrl Pts',(0.0194099426809959,0.154334454025935,
0.166847487464418));
#9387=CARTESIAN_POINT('Ctrl Pts',(0.01915295057938,0.154366557461666,0.166866166886917));
#9388=CARTESIAN_POINT('Ctrl Pts',(0.0186057947031262,0.154433520679718,
0.166905846112276));
#9389=CARTESIAN_POINT('Ctrl Pts',(0.0183156131141099,0.154468204579988,
0.166926835921389));
#9390=CARTESIAN_POINT('Ctrl Pts',(0.0175272744608783,0.154560177885348,
0.166983717073892));
#9391=CARTESIAN_POINT('Ctrl Pts',(0.017028929414945,0.154615877320389,0.167019520352928));
#9392=CARTESIAN_POINT('Ctrl Pts',(0.0145473139817467,0.154881100729164,
0.167197084292279));
#9393=CARTESIAN_POINT('Ctrl Pts',(0.0125602941128886,0.155054892639742,
0.167336952961936));
#9394=CARTESIAN_POINT('Ctrl Pts',(0.00675750056292725,0.155450133505772,
0.16774015847685));
#9395=CARTESIAN_POINT('Ctrl Pts',(0.00293604720025901,0.155569252188962,
0.167999091479927));
#9396=CARTESIAN_POINT('Ctrl Pts',(-0.0157568263655786,0.155462752540304,
0.169250138880972));
#9397=CARTESIAN_POINT('Ctrl Pts',(-0.0305377273157059,0.153246232063803,
0.170199377360572));
#9398=CARTESIAN_POINT('Ctrl Pts',(-0.0465836892157773,0.148422745643242,
0.171351101493234));
#9399=CARTESIAN_POINT('Ctrl Pts',(-0.0483777548045196,0.147847704941779,
0.171481521519002));
#9400=CARTESIAN_POINT('Ctrl Pts',(-0.0515087282835301,0.146781064760352,
0.17171233302246));
#9401=CARTESIAN_POINT('Ctrl Pts',(-0.0528501750027187,0.146303413587647,
0.171812271354078));
#9402=CARTESIAN_POINT('Ctrl Pts',(-0.0547165074119037,0.145609848661826,
0.171952870023323));
#9403=CARTESIAN_POINT('Ctrl Pts',(-0.0552470865653726,0.145409365658874,
0.171993018146018));
#9404=CARTESIAN_POINT('Ctrl Pts',(-0.0562163050216766,0.145037069284581,
0.17206668871895));
#9405=CARTESIAN_POINT('Ctrl Pts',(-0.0566552848764634,0.144866155825285,
0.172100180800954));
#9406=CARTESIAN_POINT('Ctrl Pts',(-0.0574960644800473,0.144534398606088,
0.172164572023355));
#9407=CARTESIAN_POINT('Ctrl Pts',(-0.0578979832298198,0.14437386654816,
0.172195460436706));
#9408=CARTESIAN_POINT('Ctrl Pts',(-0.0589058701179005,0.143966416677378,
0.172273192262356));
#9409=CARTESIAN_POINT('Ctrl Pts',(-0.0595109549000239,0.143717350685,0.172320107727856));
#9410=CARTESIAN_POINT('Ctrl Pts',(-0.0613123071259736,0.142962548624937,
0.172460533182733));
#9411=CARTESIAN_POINT('Ctrl Pts',(-0.0625037940408128,0.14244565559127,
0.172554418520559));
#9412=CARTESIAN_POINT('Ctrl Pts',(-0.0636886258390813,0.141913922638794,
0.172648810545196));
#9413=CARTESIAN_POINT('Origin',(0.,0.,-0.129405622560373));
#9414=CARTESIAN_POINT('',(-0.0636886236493968,0.141913923621488,0.256547255026181));
#9415=CARTESIAN_POINT('',(-0.0636886300394901,0.141913920753719,0.24285329779702));
#9416=CARTESIAN_POINT('',(-0.0636886258329924,0.141913922641526,-0.129405622560373));
#9417=CARTESIAN_POINT('Ctrl Pts',(-0.0636886236493968,0.141913923621488,
0.256547255026181));
#9418=CARTESIAN_POINT('Ctrl Pts',(-0.0596258587468564,0.143737225368426,
0.256203084221599));
#9419=CARTESIAN_POINT('Ctrl Pts',(-0.0554857265475,0.145385644314302,0.255861098235132));
#9420=CARTESIAN_POINT('Ctrl Pts',(-0.0487210271369214,0.147747786242891,
0.255321422368869));
#9421=CARTESIAN_POINT('Ctrl Pts',(-0.0461393551279011,0.148574254700172,
0.25511980497706));
#9422=CARTESIAN_POINT('Ctrl Pts',(-0.0430107014145476,0.149486396793805,
0.254881685933237));
#9423=CARTESIAN_POINT('Ctrl Pts',(-0.042483383832882,0.149637112325167,
0.254841762452393));
#9424=CARTESIAN_POINT('Ctrl Pts',(-0.0416638641902283,0.149866662404458,
0.254780053494691));
#9425=CARTESIAN_POINT('Ctrl Pts',(-0.0413722178174534,0.149947436379034,
0.254758158912198));
#9426=CARTESIAN_POINT('Ctrl Pts',(-0.0408318511512882,0.150095399012549,
0.25471771689295));
#9427=CARTESIAN_POINT('Ctrl Pts',(-0.0405832019144654,0.150162820290285,
0.254699156528942));
#9428=CARTESIAN_POINT('Ctrl Pts',(-0.0400220919321353,0.150313469826336,
0.254657382146159));
#9429=CARTESIAN_POINT('Ctrl Pts',(-0.0397095391888852,0.150396341565945,
0.25463418890867));
#9430=CARTESIAN_POINT('Ctrl Pts',(-0.0387905117082392,0.150636952264702,
0.254566209070282));
#9431=CARTESIAN_POINT('Ctrl Pts',(-0.03818332966159,0.150792004290077,0.254521573856897));
#9432=CARTESIAN_POINT('Ctrl Pts',(-0.0339295689682465,0.151850917634577,
0.254210701831179));
#9433=CARTESIAN_POINT('Ctrl Pts',(-0.0302518548848313,0.152626170763884,
0.253951313406448));
#9434=CARTESIAN_POINT('Ctrl Pts',(-0.0255057473517231,0.153448300871223,
0.253624265643544));
#9435=CARTESIAN_POINT('Ctrl Pts',(-0.0244603498923309,0.153618408929923,
0.253552702985084));
#9436=CARTESIAN_POINT('Ctrl Pts',(-0.00851377657193091,0.156046337069236,
0.252467194721703));
#9437=CARTESIAN_POINT('Ctrl Pts',(0.00663601846216799,0.156137586936553,
0.251508635130492));
#9438=CARTESIAN_POINT('Ctrl Pts',(0.0237559746747839,0.153741209671331,
0.250325505914376));
#9439=CARTESIAN_POINT('Ctrl Pts',(0.0259420532007912,0.153387466740599,
0.250172719422126));
#9440=CARTESIAN_POINT('Ctrl Pts',(0.0291867268719838,0.15279108081497,0.249942966645793));
#9441=CARTESIAN_POINT('Ctrl Pts',(0.030251599433257,0.152583813134891,0.249867082809595));
#9442=CARTESIAN_POINT('Ctrl Pts',(0.0321851572007719,0.152186427693648,
0.249728368169083));
#9443=CARTESIAN_POINT('Ctrl Pts',(0.033054553059676,0.151999965728812,0.249665654071608));
#9444=CARTESIAN_POINT('Ctrl Pts',(0.0344309252335927,0.151692404289917,
0.249565802787035));
#9445=CARTESIAN_POINT('Ctrl Pts',(0.0349389836902074,0.151576190539167,
0.249528821935665));
#9446=CARTESIAN_POINT('Ctrl Pts',(0.0354475720214446,0.151457162719788,
0.249491676815272));
#9447=CARTESIAN_POINT('Ctrl Pts',(0.0354487011050552,0.151456898460613,
0.249491594351204));
#9448=CARTESIAN_POINT('Ctrl Pts',(0.0354509655190462,0.151456368453513,
0.24949142896558));
#9449=CARTESIAN_POINT('Ctrl Pts',(0.0354521008360992,0.15145610270856,0.249491346044991));
#9450=CARTESIAN_POINT('Ctrl Pts',(0.0354543777614074,0.151455569719061,
0.24949117974306));
#9451=CARTESIAN_POINT('Ctrl Pts',(0.0354555193611961,0.151455302476347,
0.249491096362329));
#9452=CARTESIAN_POINT('Ctrl Pts',(0.0354578089034049,0.151454766478837,
0.249490929136336));
#9453=CARTESIAN_POINT('Ctrl Pts',(0.0354589568386282,0.151454497725573,
0.249490845291593));
#9454=CARTESIAN_POINT('Ctrl Pts',(0.0354612590898024,0.151453958697588,
0.249490677134772));
#9455=CARTESIAN_POINT('Ctrl Pts',(0.0354624134048996,0.151453688422913,
0.249490592822749));
#9456=CARTESIAN_POINT('Ctrl Pts',(0.035464728492523,0.151453146333684,0.249490423725745));
#9457=CARTESIAN_POINT('Ctrl Pts',(0.0354658892492579,0.151452874522671,
0.249490338941909));
#9458=CARTESIAN_POINT('Ctrl Pts',(0.0354682172506913,0.151452329353148,
0.249490168899028));
#9459=CARTESIAN_POINT('Ctrl Pts',(0.0354693844937416,0.151452055994865,
0.249490083640095));
#9460=CARTESIAN_POINT('Ctrl Pts',(0.035471725536426,0.151451507714256,0.249489912641983));
#9461=CARTESIAN_POINT('Ctrl Pts',(0.0354728993247909,0.151451232794408,
0.249489826903621));
#9462=CARTESIAN_POINT('Ctrl Pts',(0.0354752534239846,0.15145068139818,0.249489654949119));
#9463=CARTESIAN_POINT('Ctrl Pts',(0.0354764337314762,0.151450404922424,
0.249489568733218));
#9464=CARTESIAN_POINT('Ctrl Pts',(0.0359259530510062,0.151345103770182,
0.249456733205643));
#9465=CARTESIAN_POINT('Ctrl Pts',(0.0363738187839839,0.151238089899761,
0.249423920402388));
#9466=CARTESIAN_POINT('Ctrl Pts',(0.0373733284774284,0.150994568651274,
0.24935046878823));
#9467=CARTESIAN_POINT('Ctrl Pts',(0.0379247103895052,0.150857024263675,
0.24930979702264));
#9468=CARTESIAN_POINT('Ctrl Pts',(0.0393166063561113,0.150501697175272,
0.249206734811483));
#9469=CARTESIAN_POINT('Ctrl Pts',(0.0401560640196117,0.150279895041299,
0.249144215627597));
#9470=CARTESIAN_POINT('Ctrl Pts',(0.0448670077661596,0.148992876200802,
0.248791279934466));
#9471=CARTESIAN_POINT('Ctrl Pts',(0.0486976212035569,0.147785187826468,
0.248496291899387));
#9472=CARTESIAN_POINT('Ctrl Pts',(0.0542724639820242,0.14578731141018,0.248054556541746));
#9473=CARTESIAN_POINT('Ctrl Pts',(0.0560559470143578,0.14511089137054,0.247911321550669));
#9474=CARTESIAN_POINT('Ctrl Pts',(0.0714907385975114,0.138929949042804,
0.246655105097999));
#9475=CARTESIAN_POINT('Ctrl Pts',(0.084307089362347,0.131547304337279,0.245487849135746));
#9476=CARTESIAN_POINT('Ctrl Pts',(0.0979359571737378,0.12087627570952,0.244185706443168));
#9477=CARTESIAN_POINT('Ctrl Pts',(0.0999374137352741,0.119226847729202,
0.243992984120682));
#9478=CARTESIAN_POINT('Ctrl Pts',(0.102304333794042,0.11717472701326,0.243764139692011));
#9479=CARTESIAN_POINT('Ctrl Pts',(0.102709991048182,0.11681930972974,0.243724885080256));
#9480=CARTESIAN_POINT('Ctrl Pts',(0.103338892288381,0.116262488471385,0.243663985705807));
#9481=CARTESIAN_POINT('Ctrl Pts',(0.103563409379002,0.116062539722903,0.243642236295117));
#9482=CARTESIAN_POINT('Ctrl Pts',(0.103979378092587,0.115689921329102,0.243601927256693));
#9483=CARTESIAN_POINT('Ctrl Pts',(0.104170978245185,0.115517428377475,0.243583355411083));
#9484=CARTESIAN_POINT('Ctrl Pts',(0.104603862476082,0.115125760392618,0.243541383448499));
#9485=CARTESIAN_POINT('Ctrl Pts',(0.104844886554169,0.114906303219695,0.243518004977626));
#9486=CARTESIAN_POINT('Ctrl Pts',(0.105571883313801,0.11424016648358,0.243447454848087));
#9487=CARTESIAN_POINT('Ctrl Pts',(0.106055712961506,0.113791141897657,0.243400456155864));
#9488=CARTESIAN_POINT('Ctrl Pts',(0.109757603991422,0.110311430203864,0.243040360589159));
#9489=CARTESIAN_POINT('Ctrl Pts',(0.112848388530236,0.107147531994782,0.242736776146803));
#9490=CARTESIAN_POINT('Ctrl Pts',(0.125673865399182,0.0928469784568871,
0.241440426676367));
#9491=CARTESIAN_POINT('Ctrl Pts',(0.133927058098072,0.0804864806074241,
0.240500175752082));
#9492=CARTESIAN_POINT('Ctrl Pts',(0.142002245479188,0.0636121967864243,
0.239225803629711));
#9493=CARTESIAN_POINT('Ctrl Pts',(0.143559070248352,0.0600161493556608,
0.238955246419852));
#9494=CARTESIAN_POINT('Ctrl Pts',(0.145308947749686,0.0555152612595681,
0.238615950133217));
#9495=CARTESIAN_POINT('Ctrl Pts',(0.145631987607913,0.0546622232524051,
0.238551618546124));
#9496=CARTESIAN_POINT('Ctrl Pts',(0.14613005648988,0.0533112334902872,0.238449670528884));
#9497=CARTESIAN_POINT('Ctrl Pts',(0.146310089472281,0.0528151373388031,
0.238412220858117));
#9498=CARTESIAN_POINT('Ctrl Pts',(0.146642474551011,0.05188447944842,0.238341936945519));
#9499=CARTESIAN_POINT('Ctrl Pts',(0.146795428728212,0.0514501374750816,
0.238309123085164));
#9500=CARTESIAN_POINT('Ctrl Pts',(0.147132889565193,0.0504780988835804,
0.238235656765934));
#9501=CARTESIAN_POINT('Ctrl Pts',(0.147316380973068,0.0499400594697156,
0.23819497129149));
#9502=CARTESIAN_POINT('Ctrl Pts',(0.147772863138489,0.0485771383314743,
0.238091851192322));
#9503=CARTESIAN_POINT('Ctrl Pts',(0.148041896144577,0.0477509620593361,
0.238029287576418));
#9504=CARTESIAN_POINT('Ctrl Pts',(0.149517951399497,0.0430857277075011,
0.237675655393155));
#9505=CARTESIAN_POINT('Ctrl Pts',(0.150582446166689,0.0392035597913857,
0.237379994151165));
#9506=CARTESIAN_POINT('Ctrl Pts',(0.151926003049149,0.0334350038671785,
0.236938157212352));
#9507=CARTESIAN_POINT('Ctrl Pts',(0.152322908894079,0.0315775362257211,
0.236795520633883));
#9508=CARTESIAN_POINT('Ctrl Pts',(0.155498428181152,0.0152597312852637,
0.235539474234401));
#9509=CARTESIAN_POINT('Ctrl Pts',(0.15624439241789,0.000482274377844819,
0.234371745700547));
#9510=CARTESIAN_POINT('Ctrl Pts',(0.154666742041082,-0.0167537689945947,
0.233069796527146));
#9511=CARTESIAN_POINT('Ctrl Pts',(0.154366823993576,-0.0193229306758924,
0.232877599284345));
#9512=CARTESIAN_POINT('Ctrl Pts',(0.153927139774798,-0.0224171485201451,
0.232649294187079));
#9513=CARTESIAN_POINT('Ctrl Pts',(0.153848551614192,-0.0229502962151324,
0.232610070700915));
#9514=CARTESIAN_POINT('Ctrl Pts',(0.153721819580926,-0.0237801390687977,
0.232549209020646));
#9515=CARTESIAN_POINT('Ctrl Pts',(0.153675584934285,-0.0240771142101452,
0.232527466384051));
#9516=CARTESIAN_POINT('Ctrl Pts',(0.153588090315213,-0.0246285907801381,
0.232487163479456));
#9517=CARTESIAN_POINT('Ctrl Pts',(0.153547058770791,-0.0248831210898303,
0.232468591026818));
#9518=CARTESIAN_POINT('Ctrl Pts',(0.153452696495623,-0.0254593552739257,
0.232426609519356));
#9519=CARTESIAN_POINT('Ctrl Pts',(0.153398986985806,-0.0257809935757978,
0.232403222152111));
#9520=CARTESIAN_POINT('Ctrl Pts',(0.153233396958214,-0.0267537860532619,
0.232332618625719));
#9521=CARTESIAN_POINT('Ctrl Pts',(0.153118376956247,-0.0274044100732752,
0.232285575818465));
#9522=CARTESIAN_POINT('Ctrl Pts',(0.15219851451412,-0.0324210472492138,
0.231924090080054));
#9523=CARTESIAN_POINT('Ctrl Pts',(0.151211139808182,-0.0367520416818871,
0.231619242733859));
#9524=CARTESIAN_POINT('Ctrl Pts',(0.146129659764793,-0.0553317303273859,
0.230319548948886));
#9525=CARTESIAN_POINT('Ctrl Pts',(0.140196585757463,-0.0689959663259818,
0.229377205379866));
#9526=CARTESIAN_POINT('Ctrl Pts',(0.130388495262271,-0.0849094890022917,
0.228103274816019));
#9527=CARTESIAN_POINT('Ctrl Pts',(0.128235763064192,-0.0881269866405828,
0.227835911822118));
#9528=CARTESIAN_POINT('Ctrl Pts',(0.12543228587363,-0.0919965760411361,
0.22750015845956));
#9529=CARTESIAN_POINT('Ctrl Pts',(0.124892691580831,-0.0927277944839427,
0.227436063992362));
#9530=CARTESIAN_POINT('Ctrl Pts',(0.124030105616744,-0.0938755193746218,
0.227334407001755));
#9531=CARTESIAN_POINT('Ctrl Pts',(0.123711344706754,-0.0942951929610783,
0.227297009617457));
#9532=CARTESIAN_POINT('Ctrl Pts',(0.123110027680156,-0.0950785764644416,
0.227226772408556));
#9533=CARTESIAN_POINT('Ctrl Pts',(0.122827976138389,-0.0954426680645701,
0.227193952707544));
#9534=CARTESIAN_POINT('Ctrl Pts',(0.12219355263619,-0.0962541558679592,
0.227120406433537));
#9535=CARTESIAN_POINT('Ctrl Pts',(0.1218403338052,-0.0967008783310393,0.227079646514371));
#9536=CARTESIAN_POINT('Ctrl Pts',(0.120939961857918,-0.0978268309344642,
0.226976211906629));
#9537=CARTESIAN_POINT('Ctrl Pts',(0.120389540524285,-0.0985034095837423,
0.226913406849116));
#9538=CARTESIAN_POINT('Ctrl Pts',(0.117237690786658,-0.102311787731468,
0.226556120251975));
#9539=CARTESIAN_POINT('Ctrl Pts',(0.11452002201463,-0.105344847460616,0.226256934656299));
#9540=CARTESIAN_POINT('Ctrl Pts',(0.110394105753442,-0.109601062977842,
0.225814568179489));
#9541=CARTESIAN_POINT('Ctrl Pts',(0.109077725997197,-0.110911229363431,
0.225675066286808));
#9542=CARTESIAN_POINT('Ctrl Pts',(0.0970953577860628,-0.122417365791118,
0.224419809700923));
#9543=CARTESIAN_POINT('Ctrl Pts',(0.0850542719953016,-0.131069497372375,
0.223249495071439));
#9544=CARTESIAN_POINT('Ctrl Pts',(0.0697168198519296,-0.139075022750094,
0.221948578382555));
#9545=CARTESIAN_POINT('Ctrl Pts',(0.0674288166643111,-0.140198622146559,
0.221759229396775));
#9546=CARTESIAN_POINT('Ctrl Pts',(0.0646267639890398,-0.141490182649355,
0.221533852407647));
#9547=CARTESIAN_POINT('Ctrl Pts',(0.0641382974053375,-0.141712276245282,
0.221494799560585));
#9548=CARTESIAN_POINT('Ctrl Pts',(0.0633749083746817,-0.14205461454463,
0.221434144565686));
#9549=CARTESIAN_POINT('Ctrl Pts',(0.0631007771810436,-0.142176595993263,
0.221412439098915));
#9550=CARTESIAN_POINT('Ctrl Pts',(0.0625903893861014,-0.142401938731089,
0.221372169732452));
#9551=CARTESIAN_POINT('Ctrl Pts',(0.0623542311269034,-0.142505504666513,
0.221353593830727));
#9552=CARTESIAN_POINT('Ctrl Pts',(0.0618182166993383,-0.142738983358968,
0.221311559413954));
#9553=CARTESIAN_POINT('Ctrl Pts',(0.0615182085670214,-0.142868538545967,
0.221288122815917));
#9554=CARTESIAN_POINT('Ctrl Pts',(0.0606072280412788,-0.143258533839776,
0.221217223426876));
#9555=CARTESIAN_POINT('Ctrl Pts',(0.0599949829821342,-0.143516011887271,
0.221169936131201));
#9556=CARTESIAN_POINT('Ctrl Pts',(0.0551767173472634,-0.145506098425994,
0.220800483957709));
#9557=CARTESIAN_POINT('Ctrl Pts',(0.0508976762024639,-0.147057577975895,
0.220488398728771));
#9558=CARTESIAN_POINT('Ctrl Pts',(0.0322029590506205,-0.152921748668273,
0.219167604578315));
#9559=CARTESIAN_POINT('Ctrl Pts',(0.0172725964325838,-0.155318366635986,
0.218211498471092));
#9560=CARTESIAN_POINT('Ctrl Pts',(-0.00134619254742183,-0.155585281866863,
0.216939416396649));
#9561=CARTESIAN_POINT('Ctrl Pts',(-0.00492252785037709,-0.155513206634467,
0.216691943320553));
#9562=CARTESIAN_POINT('Ctrl Pts',(-0.00937815905213374,-0.155269567283624,
0.216378293833576));
#9563=CARTESIAN_POINT('Ctrl Pts',(-0.0102628952470384,-0.155213599000284,
0.216315752873355));
#9564=CARTESIAN_POINT('Ctrl Pts',(-0.0116678433714427,-0.155112657499286,
0.216216003096434));
#9565=CARTESIAN_POINT('Ctrl Pts',(-0.0121884006488223,-0.155072621577634,
0.216178948971282));
#9566=CARTESIAN_POINT('Ctrl Pts',(-0.0131683409589588,-0.154992289963757,
0.216109011449784));
#9567=CARTESIAN_POINT('Ctrl Pts',(-0.0136277667241898,-0.154952570541831,
0.216076146465476));
#9568=CARTESIAN_POINT('Ctrl Pts',(-0.0146612422527259,-0.15485859017616,
0.216002042014398));
#9569=CARTESIAN_POINT('Ctrl Pts',(-0.0152351778821357,-0.154803179276406,
0.21596076691561));
#9570=CARTESIAN_POINT('Ctrl Pts',(-0.0166993874260494,-0.154653594883159,
0.215855149643284));
#9571=CARTESIAN_POINT('Ctrl Pts',(-0.017589169990822,-0.154554925471253,
0.21579066735978));
#9572=CARTESIAN_POINT('Ctrl Pts',(-0.0228745183800269,-0.153922593036332,
0.215405803480896));
#9573=CARTESIAN_POINT('Ctrl Pts',(-0.0272460844993458,-0.153209176604658,
0.215079828086814));
#9574=CARTESIAN_POINT('Ctrl Pts',(-0.0422569970654817,-0.150096729167453,
0.213932546947964));
#9575=CARTESIAN_POINT('Ctrl Pts',(-0.0526695479242094,-0.146766949687107,
0.213084662781003));
#9576=CARTESIAN_POINT('Ctrl Pts',(-0.0693864159392888,-0.139411425143715,
0.211670861524967));
#9577=CARTESIAN_POINT('Ctrl Pts',(-0.0759079812786701,-0.135970686414469,
0.21110532117864));
#9578=CARTESIAN_POINT('Ctrl Pts',(-0.0828770836505378,-0.131635484747435,
0.21050200566044));
#9579=CARTESIAN_POINT('Ctrl Pts',(-0.0835886271819541,-0.131184806019123,
0.210440425484894));
#9580=CARTESIAN_POINT('Ctrl Pts',(-0.0845990160951622,-0.130533285207041,
0.210353046301048));
#9581=CARTESIAN_POINT('Ctrl Pts',(-0.0849008621752209,-0.130337161547275,
0.210326950719709));
#9582=CARTESIAN_POINT('Ctrl Pts',(-0.0854213789154936,-0.129996381725557,
0.21028196837972));
#9583=CARTESIAN_POINT('Ctrl Pts',(-0.0856403684051018,-0.129852218084454,
0.210263049211255));
#9584=CARTESIAN_POINT('Ctrl Pts',(-0.0860653638710163,-0.129570895226066,
0.210226344738713));
#9585=CARTESIAN_POINT('Ctrl Pts',(-0.0862714068031839,-0.129433798207739,
0.210208555346182));
#9586=CARTESIAN_POINT('Ctrl Pts',(-0.0868286530495609,-0.129061095457826,
0.210160455673437));
#9587=CARTESIAN_POINT('Ctrl Pts',(-0.0871792277184288,-0.128824545863323,
0.210130208182306));
#9588=CARTESIAN_POINT('Ctrl Pts',(-0.0884891728219151,-0.127932866602835,
0.210017217335792));
#9589=CARTESIAN_POINT('Ctrl Pts',(-0.0894421917464415,-0.127268403831028,
0.209935075911212));
#9590=CARTESIAN_POINT('Ctrl Pts',(-0.097507886421842,-0.121509491581732,
0.209239581405412));
#9591=CARTESIAN_POINT('Ctrl Pts',(-0.104187617431709,-0.115833208423761,
0.208661060256938));
#9592=CARTESIAN_POINT('Ctrl Pts',(-0.116882277964981,-0.103053911551563,
0.20747450593467));
#9593=CARTESIAN_POINT('Ctrl Pts',(-0.122808935963316,-0.095914150571156,
0.206868549556619));
#9594=CARTESIAN_POINT('Ctrl Pts',(-0.130514797297375,-0.0847367457109193,
0.205946608661568));
#9595=CARTESIAN_POINT('Ctrl Pts',(-0.132815269694958,-0.0810834549056396,
0.205649212796718));
#9596=CARTESIAN_POINT('Ctrl Pts',(-0.135427581208484,-0.0765248611403557,
0.205280209092682));
#9597=CARTESIAN_POINT('Ctrl Pts',(-0.135887031577635,-0.0757060017737411,
0.205214007796385));
#9598=CARTESIAN_POINT('Ctrl Pts',(-0.136595927150349,-0.0744153206732391,
0.205109766032161));
#9599=CARTESIAN_POINT('Ctrl Pts',(-0.136850411266116,-0.073946279070383,
0.205071905338756));
#9600=CARTESIAN_POINT('Ctrl Pts',(-0.137297911801987,-0.0731112652080053,
0.205004536943811));
#9601=CARTESIAN_POINT('Ctrl Pts',(-0.13749189210496,-0.072745812833661,
0.204975063728403));
#9602=CARTESIAN_POINT('Ctrl Pts',(-0.137936215592312,-0.0719005964696098,
0.204906921571));
#9603=CARTESIAN_POINT('Ctrl Pts',(-0.138185516512878,-0.0714202937337249,
0.204868216359888));
#9604=CARTESIAN_POINT('Ctrl Pts',(-0.138864267843637,-0.0700957543385004,
0.204761519373261));
#9605=CARTESIAN_POINT('Ctrl Pts',(-0.139288514952702,-0.0692488930493088,
0.2046933467738));
#9606=CARTESIAN_POINT('Ctrl Pts',(-0.140757040059304,-0.0662493958690764,
0.204452009153767));
#9607=CARTESIAN_POINT('Ctrl Pts',(-0.141759312481047,-0.0640766956419882,
0.204277409810209));
#9608=CARTESIAN_POINT('Ctrl Pts',(-0.14928409784167,-0.0467231450698623,
0.202883733406977));
#9609=CARTESIAN_POINT('Ctrl Pts',(-0.153399030139654,-0.0306151836416825,
0.201578915861666));
#9610=CARTESIAN_POINT('Ctrl Pts',(-0.155162654095302,-0.011333878156473,
0.200102186883096));
#9611=CARTESIAN_POINT('Ctrl Pts',(-0.155344101418235,-0.00849225672462064,
0.199887123865749));
#9612=CARTESIAN_POINT('Ctrl Pts',(-0.155486965269954,-0.00455962930237522,
0.199594346526066));
#9613=CARTESIAN_POINT('Ctrl Pts',(-0.155515059080838,-0.00347176520191675,
0.199513870672425));
#9614=CARTESIAN_POINT('Ctrl Pts',(-0.155543910366021,-0.00158924274323212,
0.199375595710535));
#9615=CARTESIAN_POINT('Ctrl Pts',(-0.155549999139583,-0.000794722658689682,
0.199317540579627));
#9616=CARTESIAN_POINT('Ctrl Pts',(-0.155550000342681,0.000316399235418375,
0.199236808123642));
#9617=CARTESIAN_POINT('Ctrl Pts',(-0.155549034291159,0.000632969976002597,
0.199213858398416));
#9618=CARTESIAN_POINT('Ctrl Pts',(-0.155545500768554,0.00121180770477676,
0.199171993106568));
#9619=CARTESIAN_POINT('Ctrl Pts',(-0.155543236412517,0.00147407517694016,
0.199153060811953));
#9620=CARTESIAN_POINT('Ctrl Pts',(-0.155537225019332,0.00201257227774423,
0.199114265051489));
#9621=CARTESIAN_POINT('Ctrl Pts',(-0.155533405467419,0.0022887989999451,
0.199094405706065));
#9622=CARTESIAN_POINT('Ctrl Pts',(-0.155521771441978,0.00299422378799091,
0.1990437911553));
#9623=CARTESIAN_POINT('Ctrl Pts',(-0.155512916086898,0.00342340627076611,
0.199013093580586));
#9624=CARTESIAN_POINT('Ctrl Pts',(-0.155469633330967,0.00517044689907013,
0.198888507771571));
#9625=CARTESIAN_POINT('Ctrl Pts',(-0.155420228645702,0.00648793083959554,
0.198795417662487));
#9626=CARTESIAN_POINT('Ctrl Pts',(-0.154901820251506,0.016806970299302,
0.198071936466645));
#9627=CARTESIAN_POINT('Ctrl Pts',(-0.153667860153803,0.0257543453427825,
0.19747768483264));
#9628=CARTESIAN_POINT('Ctrl Pts',(-0.149025949330323,0.0461337386908556,
0.196101592696785));
#9629=CARTESIAN_POINT('Ctrl Pts',(-0.145067540140679,0.0573795779779629,
0.195322362706915));
#9630=CARTESIAN_POINT('Ctrl Pts',(-0.139108203529722,0.0696256006050569,
0.194375803831849));
#9631=CARTESIAN_POINT('Ctrl Pts',(-0.138322478190227,0.0711737883865281,
0.19425429999787));
#9632=CARTESIAN_POINT('Ctrl Pts',(-0.137182550484042,0.073329695147618,
0.194082342792856));
#9633=CARTESIAN_POINT('Ctrl Pts',(-0.136849867339884,0.0739486992961989,
0.194032646061073));
#9634=CARTESIAN_POINT('Ctrl Pts',(-0.136305052632136,0.0749461361058689,
0.19395203023885));
#9635=CARTESIAN_POINT('Ctrl Pts',(-0.136095509439666,0.0753259782123471,
0.193921203362643));
#9636=CARTESIAN_POINT('Ctrl Pts',(-0.135655618494086,0.0761155477302487,
0.193856856391696));
#9637=CARTESIAN_POINT('Ctrl Pts',(-0.13542499734438,0.0765251169266757,
0.193823326765658));
#9638=CARTESIAN_POINT('Ctrl Pts',(-0.134875730528528,0.0774903224899755,
0.193743947605972));
#9639=CARTESIAN_POINT('Ctrl Pts',(-0.134555504345432,0.0780450446397574,
0.193698041582094));
#9640=CARTESIAN_POINT('Ctrl Pts',(-0.133483075168693,0.0798765746846046,
0.193545512743486));
#9641=CARTESIAN_POINT('Ctrl Pts',(-0.132716073458506,0.0811445753146967,
0.193438355998556));
#9642=CARTESIAN_POINT('Ctrl Pts',(-0.128566572611405,0.0877882525102592,
0.192868419126585));
#9643=CARTESIAN_POINT('Ctrl Pts',(-0.124875769773437,0.0929632321347478,
0.192394341750511));
#9644=CARTESIAN_POINT('Ctrl Pts',(-0.11529448917821,0.104793764352739,0.191235705825436));
#9645=CARTESIAN_POINT('Ctrl Pts',(-0.109129819953951,0.111198982606901,
0.190543835551954));
#9646=CARTESIAN_POINT('Ctrl Pts',(-0.0972553415262483,0.121593274999628,
0.189324169066063));
#9647=CARTESIAN_POINT('Ctrl Pts',(-0.0917591668694762,0.125792717316811,
0.188795656672878));
#9648=CARTESIAN_POINT('Ctrl Pts',(-0.0854152377620299,0.130002054799282,
0.188237493636357));
#9649=CARTESIAN_POINT('Ctrl Pts',(-0.0848265842732654,0.130386915543376,
0.188186170394339));
#9650=CARTESIAN_POINT('Ctrl Pts',(-0.0839541341241629,0.13094891271503,
0.188110815417013));
#9651=CARTESIAN_POINT('Ctrl Pts',(-0.0836723552062635,0.13112914000228,
0.188086586328329));
#9652=CARTESIAN_POINT('Ctrl Pts',(-0.0831717076586671,0.131447085974692,
0.18804373280791));
#9653=CARTESIAN_POINT('Ctrl Pts',(-0.0829530751686131,0.131585168959528,
0.18802508451289));
#9654=CARTESIAN_POINT('Ctrl Pts',(-0.0824843871801998,0.131879548541915,
0.187985248994558));
#9655=CARTESIAN_POINT('Ctrl Pts',(-0.0822342318788695,0.13203567913011,
0.187964072722744));
#9656=CARTESIAN_POINT('Ctrl Pts',(-0.081547611027205,0.13246151468995,0.187906177572484));
#9657=CARTESIAN_POINT('Ctrl Pts',(-0.0811102473070708,0.132729776387485,
0.187869552113901));
#9658=CARTESIAN_POINT('Ctrl Pts',(-0.0787891303430609,0.134137700643264,
0.187676465984875));
#9659=CARTESIAN_POINT('Ctrl Pts',(-0.0768825435241392,0.135239512115259,
0.187522329798283));
#9660=CARTESIAN_POINT('Ctrl Pts',(-0.0712721377913392,0.13832473211187,
0.187079641027565));
#9661=CARTESIAN_POINT('Ctrl Pts',(-0.0675141063018767,0.140197111154279,
0.186796543977972));
#9662=CARTESIAN_POINT('Ctrl Pts',(-0.063688595018437,0.141913936470586,
0.186516973639705));
#9663=CARTESIAN_POINT('',(-0.155549922407231,-0.000136919941883599,0.185534971438302));
#9664=CARTESIAN_POINT('Ctrl Pts',(-0.0636886258390813,0.141913922638794,
0.172648810545196));
#9665=CARTESIAN_POINT('Ctrl Pts',(-0.0639417182132668,0.141800338959176,
0.172668973661729));
#9666=CARTESIAN_POINT('Ctrl Pts',(-0.0641945069200826,0.141686078141358,
0.172689159868843));
#9667=CARTESIAN_POINT('Ctrl Pts',(-0.0664530499226049,0.140657928652624,
0.172869938830651));
#9668=CARTESIAN_POINT('Ctrl Pts',(-0.068439374571081,0.139702225593533,
0.173031938049245));
#9669=CARTESIAN_POINT('Ctrl Pts',(-0.0758515134502319,0.135939923572788,
0.173648113200886));
#9670=CARTESIAN_POINT('Ctrl Pts',(-0.0811301671444233,0.13285704690294,
0.174111221789556));
#9671=CARTESIAN_POINT('Ctrl Pts',(-0.0937175181050919,0.124475337870062,
0.175273711163105));
#9672=CARTESIAN_POINT('Ctrl Pts',(-0.100772789699689,0.118835700746529,
0.175979128346218));
#9673=CARTESIAN_POINT('Ctrl Pts',(-0.108069580434532,0.111883415748812,
0.1767505997933));
#9674=CARTESIAN_POINT('Ctrl Pts',(-0.108831817555137,0.111142109540443,
0.176831734698813));
#9675=CARTESIAN_POINT('Ctrl Pts',(-0.112215640062796,0.107783012044303,
0.177194182808041));
#9676=CARTESIAN_POINT('Ctrl Pts',(-0.114751068644906,0.105079614864521,
0.177471969523666));
#9677=CARTESIAN_POINT('Ctrl Pts',(-0.117562240940566,0.101858952975878,
0.177784917250049));
#9678=CARTESIAN_POINT('Ctrl Pts',(-0.117934367268449,0.101427865205498,
0.177826448339971));
#9679=CARTESIAN_POINT('Ctrl Pts',(-0.118523905850323,0.100737286171255,
0.177892398762503));
#9680=CARTESIAN_POINT('Ctrl Pts',(-0.118742848218726,0.100479117661241,
0.177916925959434));
#9681=CARTESIAN_POINT('Ctrl Pts',(-0.119128283924557,0.100021607277894,
0.177960162936685));
#9682=CARTESIAN_POINT('Ctrl Pts',(-0.119295122807983,0.0998225607353291,
0.177978897771885));
#9683=CARTESIAN_POINT('Ctrl Pts',(-0.119646643576512,0.0994010401302771,
0.178018411165874));
#9684=CARTESIAN_POINT('Ctrl Pts',(-0.11983120366099,0.0991784690897692,
0.178039180924485));
#9685=CARTESIAN_POINT('Ctrl Pts',(-0.120325243415529,0.0985792874081295,
0.1780948469974));
#9686=CARTESIAN_POINT('Ctrl Pts',(-0.12063357869763,0.098201730211959,0.178129661530982));
#9687=CARTESIAN_POINT('Ctrl Pts',(-0.122063964529137,0.0964333163224236,
0.178291543773438));
#9688=CARTESIAN_POINT('Ctrl Pts',(-0.123163828363868,0.0950245655411512,
0.178417107605077));
#9689=CARTESIAN_POINT('Ctrl Pts',(-0.128636549858209,0.0877601655425551,
0.17904937617282));
#9690=CARTESIAN_POINT('Ctrl Pts',(-0.132617635979318,0.0816198383153492,
0.179534711032005));
#9691=CARTESIAN_POINT('Ctrl Pts',(-0.139242256336471,0.06962914980104,0.18043828420425));
#9692=CARTESIAN_POINT('Ctrl Pts',(-0.141984421590115,0.0638517545748268,
0.180856422367196));
#9693=CARTESIAN_POINT('Ctrl Pts',(-0.147171965812737,0.0509224721587812,
0.181783073294908));
#9694=CARTESIAN_POINT('Ctrl Pts',(-0.149467234747206,0.0437287776299269,
0.182293263309149));
#9695=CARTESIAN_POINT('Ctrl Pts',(-0.151470288887039,0.0354061329755489,
0.182892819001806));
#9696=CARTESIAN_POINT('Ctrl Pts',(-0.151699172719634,0.0344122590999078,
0.182964551070705));
#9697=CARTESIAN_POINT('Ctrl Pts',(-0.152048761681122,0.0328229430008052,
0.183079506224629));
#9698=CARTESIAN_POINT('Ctrl Pts',(-0.152175783291413,0.0322289074697977,
0.183122527642506));
#9699=CARTESIAN_POINT('Ctrl Pts',(-0.15239413391884,0.0311776811385245,
0.183198763695134));
#9700=CARTESIAN_POINT('Ctrl Pts',(-0.152486893764593,0.03072079223285,0.183231932316995));
#9701=CARTESIAN_POINT('Ctrl Pts',(-0.152661409101821,0.0298409490938165,
0.183295875579051));
#9702=CARTESIAN_POINT('Ctrl Pts',(-0.152743464424159,0.0294180580697884,
0.183326640343285));
#9703=CARTESIAN_POINT('Ctrl Pts',(-0.152915246019541,0.0285126447769438,
0.183392576434651));
#9704=CARTESIAN_POINT('Ctrl Pts',(-0.153004447144712,0.0280300289172811,
0.183427764112988));
#9705=CARTESIAN_POINT('Ctrl Pts',(-0.15321345475542,0.0268684775677711,
0.183512556799489));
#9706=CARTESIAN_POINT('Ctrl Pts',(-0.153331033459057,0.026189157199468,
0.183562231826929));
#9707=CARTESIAN_POINT('Ctrl Pts',(-0.153844156489786,0.0231025828091486,
0.183788339211882));
#9708=CARTESIAN_POINT('Ctrl Pts',(-0.154187532123694,0.020687133824531,
0.183966401283114));
#9709=CARTESIAN_POINT('Ctrl Pts',(-0.155196166219536,0.01215661187438,0.184599556860343));
#9710=CARTESIAN_POINT('Ctrl Pts',(-0.155555358047335,0.00601193323586903,
0.185063661244219));
#9711=CARTESIAN_POINT('Ctrl Pts',(-0.155549939608074,-0.0001370690496796,
0.185534952791332));
#9712=CARTESIAN_POINT('Ctrl Pts',(-0.155549939737365,-0.000136922248412486,
0.18553494153972));
#9713=CARTESIAN_POINT('Ctrl Pts',(-0.155539040632619,-0.0125188039811671,
0.186483953207384));
#9714=CARTESIAN_POINT('Ctrl Pts',(-0.154049857623245,-0.0248552119677568,
0.187460691532931));
#9715=CARTESIAN_POINT('Ctrl Pts',(-0.150751720167338,-0.0383672971839581,
0.188503754085351));
#9716=CARTESIAN_POINT('Ctrl Pts',(-0.150368100501018,-0.0398442644059964,
0.188617331311801));
#9717=CARTESIAN_POINT('Ctrl Pts',(-0.149776773575888,-0.0419906071237111,
0.188781519094411));
#9718=CARTESIAN_POINT('Ctrl Pts',(-0.149586192350252,-0.0426645531431382,
0.188832948329596));
#9719=CARTESIAN_POINT('Ctrl Pts',(-0.149278893054669,-0.0437238685240643,
0.188913563499235));
#9720=CARTESIAN_POINT('Ctrl Pts',(-0.149165222518933,-0.0441101007792151,
0.188942909595204));
#9721=CARTESIAN_POINT('Ctrl Pts',(-0.148946938349915,-0.0448412978529119,
0.188998372175556));
#9722=CARTESIAN_POINT('Ctrl Pts',(-0.148842622927789,-0.0451863479829484,
0.189024504992108));
#9723=CARTESIAN_POINT('Ctrl Pts',(-0.148660359450103,-0.0457817515632065,
0.189069526069329));
#9724=CARTESIAN_POINT('Ctrl Pts',(-0.148582976562012,-0.0460322748563397,
0.189088446929479));
#9725=CARTESIAN_POINT('Ctrl Pts',(-0.148431400839802,-0.0465186291977152,
0.189125134358384));
#9726=CARTESIAN_POINT('Ctrl Pts',(-0.148357279329619,-0.0467544788223972,
0.189142905092716));
#9727=CARTESIAN_POINT('Ctrl Pts',(-0.148155160929256,-0.0473922856611791,
0.189190910152681));
#9728=CARTESIAN_POINT('Ctrl Pts',(-0.14802608940055,-0.0477939046130302,
0.189221082094392));
#9729=CARTESIAN_POINT('Ctrl Pts',(-0.147537417258178,-0.0492934866071408,
0.189333546493853));
#9730=CARTESIAN_POINT('Ctrl Pts',(-0.147167209420562,-0.0503879945550053,
0.18941524402898));
#9731=CARTESIAN_POINT('Ctrl Pts',(-0.143149849314013,-0.0618430598842776,
0.190267220108078));
#9732=CARTESIAN_POINT('Ctrl Pts',(-0.138426652492428,-0.0717954492526159,
0.190982359402924));
#9733=CARTESIAN_POINT('Ctrl Pts',(-0.130282029608854,-0.0851102105377999,
0.192010144725049));
#9734=CARTESIAN_POINT('Ctrl Pts',(-0.127696403078665,-0.088942571788872,
0.192315137291708));
#9735=CARTESIAN_POINT('Ctrl Pts',(-0.122354309116098,-0.0961463952623667,
0.19291508442459));
#9736=CARTESIAN_POINT('Ctrl Pts',(-0.119619403428955,-0.0995283860882286,
0.193209290599335));
#9737=CARTESIAN_POINT('Ctrl Pts',(-0.115004899189347,-0.104769377468851,
0.193690324877848));
#9738=CARTESIAN_POINT('Ctrl Pts',(-0.113213280178866,-0.106702863364689,
0.193873724654354));
#9739=CARTESIAN_POINT('Ctrl Pts',(-0.110826779967445,-0.109150541291889,
0.194114330936187));
#9740=CARTESIAN_POINT('Ctrl Pts',(-0.110275844173366,-0.10970712818174,
0.194169630695438));
#9741=CARTESIAN_POINT('Ctrl Pts',(-0.109412750689971,-0.110566004150522,
0.194255898309681));
#9742=CARTESIAN_POINT('Ctrl Pts',(-0.109103483664113,-0.110871191626771,
0.194286738370071));
#9743=CARTESIAN_POINT('Ctrl Pts',(-0.108497324292503,-0.11146436291253,
0.194347047854914));
#9744=CARTESIAN_POINT('Ctrl Pts',(-0.108200553692674,-0.111752466427655,
0.194376511702652));
#9745=CARTESIAN_POINT('Ctrl Pts',(-0.10751312742206,-0.112414511409432,
0.194444617820238));
#9746=CARTESIAN_POINT('Ctrl Pts',(-0.1071216656877,-0.112787604239748,0.194483296271171));
#9747=CARTESIAN_POINT('Ctrl Pts',(-0.106040065093725,-0.113807741608618,
0.194589882350488));
#9748=CARTESIAN_POINT('Ctrl Pts',(-0.105345966559504,-0.114450533905703,
0.194657970263093));
#9749=CARTESIAN_POINT('Ctrl Pts',(-0.101740745794513,-0.117728683008753,
0.195010087022277));
#9750=CARTESIAN_POINT('Ctrl Pts',(-0.0987367041809033,-0.120259221109373,
0.195298435400113));
#9751=CARTESIAN_POINT('Ctrl Pts',(-0.0949865095207073,-0.123183005964574,
0.195652880595562));
#9752=CARTESIAN_POINT('Ctrl Pts',(-0.0943285717427634,-0.123687551749149,
0.195714865043418));
#9753=CARTESIAN_POINT('Ctrl Pts',(-0.0849881302849278,-0.130732485279815,
0.196592016886436));
#9754=CARTESIAN_POINT('Ctrl Pts',(-0.0756482806278708,-0.136349707891492,
0.197438200822188));
#9755=CARTESIAN_POINT('Ctrl Pts',(-0.0611031768996177,-0.143140085480536,
0.198680184268759));
#9756=CARTESIAN_POINT('Ctrl Pts',(-0.0562982223114,-0.145097212887848,0.199078819580188));
#9757=CARTESIAN_POINT('Ctrl Pts',(-0.0491056384804594,-0.147615614205386,
0.199651193415899));
#9758=CARTESIAN_POINT('Ctrl Pts',(-0.046788377874307,-0.148366380235098,
0.199831988181158));
#9759=CARTESIAN_POINT('Ctrl Pts',(-0.0439445929522421,-0.149214470235712,
0.20004873305551));
#9760=CARTESIAN_POINT('Ctrl Pts',(-0.0434341267887402,-0.149363857843226,
0.200087439793114));
#9761=CARTESIAN_POINT('Ctrl Pts',(-0.0426355489305593,-0.149593120965101,
0.200147671155916));
#9762=CARTESIAN_POINT('Ctrl Pts',(-0.0423479628520096,-0.149674787185721,
0.200169296854877));
#9763=CARTESIAN_POINT('Ctrl Pts',(-0.0418118470724394,-0.149825359858296,
0.20020948808987));
#9764=CARTESIAN_POINT('Ctrl Pts',(-0.041563384092665,-0.149894476605321,
0.200228065262291));
#9765=CARTESIAN_POINT('Ctrl Pts',(-0.0409984699345812,-0.150050110245684,
0.20027019176312));
#9766=CARTESIAN_POINT('Ctrl Pts',(-0.0406819167577055,-0.150136244045255,
0.200293718732734));
#9767=CARTESIAN_POINT('Ctrl Pts',(-0.0397171973602681,-0.150395468036203,
0.20036518570801));
#9768=CARTESIAN_POINT('Ctrl Pts',(-0.0390681700670027,-0.150565370198937,
0.200412946014653));
#9769=CARTESIAN_POINT('Ctrl Pts',(-0.0368219814581839,-0.151137874468279,
0.200577199289516));
#9770=CARTESIAN_POINT('Ctrl Pts',(-0.0352194708975504,-0.151519321703812,
0.200692575539621));
#9771=CARTESIAN_POINT('Ctrl Pts',(-0.0332048303776652,-0.151965176593364,
0.20083571951493));
#9772=CARTESIAN_POINT('Ctrl Pts',(-0.0327981751398694,-0.152053462219372,
0.200864516449855));
#9773=CARTESIAN_POINT('Ctrl Pts',(-0.020153787612586,-0.15474549680438,
0.201757056412309));
#9774=CARTESIAN_POINT('Ctrl Pts',(-0.00764527844441893,-0.155865249716474,
0.202559841615445));
#9775=CARTESIAN_POINT('Ctrl Pts',(0.0122924810377385,-0.155241555213235,
0.203883259336207));
#9776=CARTESIAN_POINT('Ctrl Pts',(0.0196942376803756,-0.154477052668175,
0.204383650834542));
#9777=CARTESIAN_POINT('Ctrl Pts',(0.0280927467869705,-0.152996090114723,
0.204977436648777));
#9778=CARTESIAN_POINT('Ctrl Pts',(0.0291710553323685,-0.152794160348969,
0.205054160035188));
#9779=CARTESIAN_POINT('Ctrl Pts',(0.0311270520522133,-0.152406410130376,
0.205194268801548));
#9780=CARTESIAN_POINT('Ctrl Pts',(0.0320054474960424,-0.152224368905421,
0.205257533736885));
#9781=CARTESIAN_POINT('Ctrl Pts',(0.0333933507292141,-0.151924192019136,
0.205358064116007));
#9782=CARTESIAN_POINT('Ctrl Pts',(0.033903931901778,-0.151811064758285,
0.205395169551933));
#9783=CARTESIAN_POINT('Ctrl Pts',(0.0348172919223506,-0.15160385799833,
0.205461769859831));
#9784=CARTESIAN_POINT('Ctrl Pts',(0.0352202863708006,-0.151510742189058,
0.205491233613483));
#9785=CARTESIAN_POINT('Ctrl Pts',(0.0361493430622541,-0.15129216759957,
0.205559342127009));
#9786=CARTESIAN_POINT('Ctrl Pts',(0.036675129299857,-0.151165571007426,
0.205598023079656));
#9787=CARTESIAN_POINT('Ctrl Pts',(0.0381189568383495,-0.150809956155432,
0.205704622763903));
#9788=CARTESIAN_POINT('Ctrl Pts',(0.0390355720223534,-0.150575302720666,
0.205772721856004));
#9789=CARTESIAN_POINT('Ctrl Pts',(0.0437469016346806,-0.149323293186211,
0.206124989748362));
#9790=CARTESIAN_POINT('Ctrl Pts',(0.0475038953559363,-0.148170888050607,
0.206413482501409));
#9791=CARTESIAN_POINT('Ctrl Pts',(0.05308832834334,-0.146223720771394,0.206854316864829));
#9792=CARTESIAN_POINT('Ctrl Pts',(0.0549509344600306,-0.145533986854355,
0.207003406573533));
#9793=CARTESIAN_POINT('Ctrl Pts',(0.0704348690671795,-0.139460573714846,
0.208259923048057));
#9794=CARTESIAN_POINT('Ctrl Pts',(0.0832441977050638,-0.132214401296347,
0.209421037031592));
#9795=CARTESIAN_POINT('Ctrl Pts',(0.0969721060850179,-0.121652696283706,
0.210725124399454));
#9796=CARTESIAN_POINT('Ctrl Pts',(0.0990513773965682,-0.119965807017144,
0.210924210972425));
#9797=CARTESIAN_POINT('Ctrl Pts',(0.101499867628294,-0.117872284904401,
0.211159572001594));
#9798=CARTESIAN_POINT('Ctrl Pts',(0.101911653301926,-0.117516439795512,
0.211199187026749));
#9799=CARTESIAN_POINT('Ctrl Pts',(0.102548770129102,-0.116960007000574,
0.211260518436819));
#9800=CARTESIAN_POINT('Ctrl Pts',(0.102775394138162,-0.116760917504689,
0.21128234188055));
#9801=CARTESIAN_POINT('Ctrl Pts',(0.103194486828238,-0.116390578467316,
0.211322711688262));
#9802=CARTESIAN_POINT('Ctrl Pts',(0.103387107416474,-0.116219511656509,
0.211341270659615));
#9803=CARTESIAN_POINT('Ctrl Pts',(0.103821302796505,-0.115831967959875,
0.211383116384302));
#9804=CARTESIAN_POINT('Ctrl Pts',(0.104062625483538,-0.115615213957759,
0.211406381996453));
#9805=CARTESIAN_POINT('Ctrl Pts',(0.104771887443112,-0.114974141041409,
0.211474791185273));
#9806=CARTESIAN_POINT('Ctrl Pts',(0.105237929833943,-0.114547717861974,
0.211519780446197));
#9807=CARTESIAN_POINT('Ctrl Pts',(0.108552007508273,-0.111478078079297,
0.211840097204828));
#9808=CARTESIAN_POINT('Ctrl Pts',(0.111303018961708,-0.108731525560737,
0.212108092150111));
#9809=CARTESIAN_POINT('Ctrl Pts',(0.114742620665422,-0.105029968757704,
0.212450751858512));
#9810=CARTESIAN_POINT('Ctrl Pts',(0.115527081287693,-0.104166486649202,
0.212529447045909));
#9811=CARTESIAN_POINT('Ctrl Pts',(0.126194902614687,-0.0921552993154266,
0.213608545809946));
#9812=CARTESIAN_POINT('Ctrl Pts',(0.134436370571208,-0.079653286324288,
0.214557409736697));
#9813=CARTESIAN_POINT('Ctrl Pts',(0.142178070761036,-0.0631829780156148,
0.215803638933402));
#9814=CARTESIAN_POINT('Ctrl Pts',(0.143486370149046,-0.0601527335660158,
0.21603236352221));
#9815=CARTESIAN_POINT('Ctrl Pts',(0.145014113161251,-0.0562801478210873,
0.216325085975819));
#9816=CARTESIAN_POINT('Ctrl Pts',(0.14532428254892,-0.0554743265172514,
0.21638601734551));
#9817=CARTESIAN_POINT('Ctrl Pts',(0.145809375075496,-0.0541820617366619,
0.216483782936316));
#9818=CARTESIAN_POINT('Ctrl Pts',(0.145988613521935,-0.0536972474540742,
0.216520472952763));
#9819=CARTESIAN_POINT('Ctrl Pts',(0.146323398127622,-0.0527776363513783,
0.216590094185665));
#9820=CARTESIAN_POINT('Ctrl Pts',(0.146479431362818,-0.0523430216708083,
0.216623008796056));
#9821=CARTESIAN_POINT('Ctrl Pts',(0.146828557048109,-0.0513567805645438,
0.216697728280902));
#9822=CARTESIAN_POINT('Ctrl Pts',(0.147020479484016,-0.0508047504651751,
0.216739571343013));
#9823=CARTESIAN_POINT('Ctrl Pts',(0.147578621128321,-0.0491697072885763,
0.216863573141082));
#9824=CARTESIAN_POINT('Ctrl Pts',(0.147936009512592,-0.0480837445370402,
0.216946020730349));
#9825=CARTESIAN_POINT('Ctrl Pts',(0.15136369309761,-0.0372682781845446,
0.217768186914167));
#9826=CARTESIAN_POINT('Ctrl Pts',(0.153481040981572,-0.0272650307074598,
0.218539484931237));
#9827=CARTESIAN_POINT('Ctrl Pts',(0.155159659068066,-0.0121136537890807,
0.219716330160525));
#9828=CARTESIAN_POINT('Ctrl Pts',(0.155470921744708,-0.00707472707619059,
0.220108622139947));
#9829=CARTESIAN_POINT('Ctrl Pts',(0.155630367645457,0.0051437616091677,
0.221054161423279));
#9830=CARTESIAN_POINT('Ctrl Pts',(0.155227609625231,0.0123161003060405,
0.221604600471537));
#9831=CARTESIAN_POINT('Ctrl Pts',(0.154225810689665,0.0202709210587499,
0.222193957570673));
#9832=CARTESIAN_POINT('Ctrl Pts',(0.154113864242088,0.0211051618566121,
0.222255497506975));
#9833=CARTESIAN_POINT('Ctrl Pts',(0.153944403243728,0.0222946779221939,
0.222342824933219));
#9834=CARTESIAN_POINT('Ctrl Pts',(0.153892421774163,0.0226507059775128,
0.22236890859857));
#9835=CARTESIAN_POINT('Ctrl Pts',(0.153800441095285,0.0232657582659785,
0.222413872321446));
#9836=CARTESIAN_POINT('Ctrl Pts',(0.153761021927958,0.0235248661827032,
0.222432784752465));
#9837=CARTESIAN_POINT('Ctrl Pts',(0.153683117329499,0.024028382410436,0.222469477474416));
#9838=CARTESIAN_POINT('Ctrl Pts',(0.153644703714674,0.0242727982760551,
0.222487261845966));
#9839=CARTESIAN_POINT('Ctrl Pts',(0.153539063058975,0.0249346625191474,
0.222535350488864));
#9840=CARTESIAN_POINT('Ctrl Pts',(0.153470716147304,0.0253519343738573,
0.222565591990565));
#9841=CARTESIAN_POINT('Ctrl Pts',(0.153208222685584,0.0269145399586885,
0.222678573819157));
#9842=CARTESIAN_POINT('Ctrl Pts',(0.153002942919686,0.0280580047711293,
0.222760712225859));
#9843=CARTESIAN_POINT('Ctrl Pts',(0.151149541019614,0.0377559641137137,
0.223453601070469));
#9844=CARTESIAN_POINT('Ctrl Pts',(0.148797985581871,0.0461617040687934,
0.22402981835978));
#9845=CARTESIAN_POINT('Ctrl Pts',(0.142509464031649,0.063033131529343,0.225215937878361));
#9846=CARTESIAN_POINT('Ctrl Pts',(0.138491357502649,0.0714300384728149,
0.225823718626687));
#9847=CARTESIAN_POINT('Ctrl Pts',(0.1315410438247,0.0831351019374812,0.22674810901456));
#9848=CARTESIAN_POINT('Ctrl Pts',(0.129180047215683,0.0867582900619423,
0.22704599610356));
#9849=CARTESIAN_POINT('Ctrl Pts',(0.126126322670216,0.0910430411351392,
0.22741552848657));
#9850=CARTESIAN_POINT('Ctrl Pts',(0.125574320258971,0.0918029118922866,
0.227481747791953));
#9851=CARTESIAN_POINT('Ctrl Pts',(0.12469797974035,0.0929865638714944,0.227586004124916));
#9852=CARTESIAN_POINT('Ctrl Pts',(0.124378277615167,0.0934137637424796,
0.22762386121688));
#9853=CARTESIAN_POINT('Ctrl Pts',(0.123806864785654,0.0941691765304058,
0.227691216556504));
#9854=CARTESIAN_POINT('Ctrl Pts',(0.123556029690901,0.0944980481143688,
0.22772068030149));
#9855=CARTESIAN_POINT('Ctrl Pts',(0.122974180111206,0.095254637886217,0.227788790944785));
#9856=CARTESIAN_POINT('Ctrl Pts',(0.12264224224166,0.095681635736158,0.227827474045571));
#9857=CARTESIAN_POINT('Ctrl Pts',(0.121723412751251,0.0968509616772653,
0.227934085173705));
#9858=CARTESIAN_POINT('Ctrl Pts',(0.121131971932128,0.0975896679567658,
0.228002193624759));
#9859=CARTESIAN_POINT('Ctrl Pts',(0.118049496013169,0.101368468161948,0.228354586947536));
#9860=CARTESIAN_POINT('Ctrl Pts',(0.115450844851062,0.104318488833734,0.228643199428682));
#9861=CARTESIAN_POINT('Ctrl Pts',(0.111376150293414,0.108605223431768,0.229084051436817));
#9862=CARTESIAN_POINT('Ctrl Pts',(0.109981454016877,0.110017364946379,0.229233034262993));
#9863=CARTESIAN_POINT('Ctrl Pts',(0.098069786755476,0.121625129633186,0.23048952974803));
#9864=CARTESIAN_POINT('Ctrl Pts',(0.0861898460025061,0.130313420816375,
0.231650738469756));
#9865=CARTESIAN_POINT('Ctrl Pts',(0.0709113945192309,0.138472143661504,
0.232954787576607));
#9866=CARTESIAN_POINT('Ctrl Pts',(0.0685190535638948,0.139671407539156,
0.233153768794131));
#9867=CARTESIAN_POINT('Ctrl Pts',(0.0656042043121951,0.141039664511051,
0.233389021999629));
#9868=CARTESIAN_POINT('Ctrl Pts',(0.0651104125233813,0.141268300738876,
0.233428631059508));
#9869=CARTESIAN_POINT('Ctrl Pts',(0.0643410447789384,0.141619643548459,
0.233489955264347));
#9870=CARTESIAN_POINT('Ctrl Pts',(0.0640663012192808,0.141744144621015,
0.233511777428152));
#9871=CARTESIAN_POINT('Ctrl Pts',(0.0635562333071361,0.141973497795979,
0.233552146077209));
#9872=CARTESIAN_POINT('Ctrl Pts',(0.0633210128548923,0.142078563483618,
0.23357070516352));
#9873=CARTESIAN_POINT('Ctrl Pts',(0.0627890094543122,0.142314609309305,
0.233612552681419));
#9874=CARTESIAN_POINT('Ctrl Pts',(0.0624920777659436,0.142445245455279,
0.233635819964093));
#9875=CARTESIAN_POINT('Ctrl Pts',(0.0616156562571677,0.142827562285832,
0.233704238579944));
#9876=CARTESIAN_POINT('Ctrl Pts',(0.0610350297570965,0.143076646674438,
0.233749235534027));
#9877=CARTESIAN_POINT('Ctrl Pts',(0.0568701835940164,0.14483336680916,0.234069757140718));
#9878=CARTESIAN_POINT('Ctrl Pts',(0.0532316838368128,0.146209836283875,
0.234337938566508));
#9879=CARTESIAN_POINT('Ctrl Pts',(0.0378214697027433,0.151387909529295,
0.235440350439778));
#9880=CARTESIAN_POINT('Ctrl Pts',(0.0256693213776257,0.153915221001169,
0.236233154463579));
#9881=CARTESIAN_POINT('Ctrl Pts',(0.00893888478883866,0.155355912811346,
0.237355792582719));
#9882=CARTESIAN_POINT('Ctrl Pts',(0.00451858627127134,0.15554722916914,
0.237654887105966));
#9883=CARTESIAN_POINT('Ctrl Pts',(-0.00258099136772841,0.155551629629462,
0.238143804550222));
#9884=CARTESIAN_POINT('Ctrl Pts',(-0.00525784153340671,0.155484161887903,
0.238330076431399));
#9885=CARTESIAN_POINT('Ctrl Pts',(-0.00873399088828066,0.155306682406141,
0.23857505944318));
#9886=CARTESIAN_POINT('Ctrl Pts',(-0.00953615489689704,0.155259492151519,
0.238631805749427));
#9887=CARTESIAN_POINT('Ctrl Pts',(-0.0108404041280703,0.155172619250435,
0.238724433414779));
#9888=CARTESIAN_POINT('Ctrl Pts',(-0.0113427333478066,0.155136709118216,
0.238760196489967));
#9889=CARTESIAN_POINT('Ctrl Pts',(-0.0123085667496582,0.155062948345425,
0.238829131359007));
#9890=CARTESIAN_POINT('Ctrl Pts',(-0.0127720936900695,0.155025457197018,
0.238862291535787));
#9891=CARTESIAN_POINT('Ctrl Pts',(-0.0138331900592842,0.154934841990167,
0.238938380281671));
#9892=CARTESIAN_POINT('Ctrl Pts',(-0.0144306309811333,0.15488033858614,
0.238981351633487));
#9893=CARTESIAN_POINT('Ctrl Pts',(-0.0160171942645502,0.154726339850241,
0.239095820528831));
#9894=CARTESIAN_POINT('Ctrl Pts',(-0.0170056891878823,0.154620817503584,
0.239167505849375));
#9895=CARTESIAN_POINT('Ctrl Pts',(-0.0244280280647339,0.153756443872188,
0.239708614235448));
#9896=CARTESIAN_POINT('Ctrl Pts',(-0.0308089082765891,0.152605902959035,
0.240190287540344));
#9897=CARTESIAN_POINT('Ctrl Pts',(-0.0462225854363646,0.148820497931415,
0.241395185496132));
#9898=CARTESIAN_POINT('Ctrl Pts',(-0.0551222709238866,0.145758361620418,
0.242127760292114));
#9899=CARTESIAN_POINT('Ctrl Pts',(-0.0636886300394901,0.141913920753719,
0.24285329779702));
#9900=CARTESIAN_POINT('Origin',(0.,0.,-0.129405622560373));
#9901=CARTESIAN_POINT('',(-0.0636886254453755,0.141913922815482,0.326750756222096));
#9902=CARTESIAN_POINT('',(-0.0636886270244494,0.14191392210682,0.31288131537517));
#9903=CARTESIAN_POINT('',(-0.0636886258329924,0.141913922641526,-0.129405622560373));
#9904=CARTESIAN_POINT('',(-0.155549941229055,0.000135217002094367,0.269470366437021));
#9905=CARTESIAN_POINT('Ctrl Pts',(-0.0636886254453755,0.141913922815482,
0.326750756222096));
#9906=CARTESIAN_POINT('Ctrl Pts',(-0.0582901109833659,0.144336686972171,
0.326320925124822));
#9907=CARTESIAN_POINT('Ctrl Pts',(-0.0527581233471341,0.146449271766227,
0.325880672208058));
#9908=CARTESIAN_POINT('Ctrl Pts',(-0.0357824592924485,0.151845092873984,
0.324529867261289));
#9909=CARTESIAN_POINT('Ctrl Pts',(-0.0240708969387131,0.154135863142175,
0.323594999854329));
#9910=CARTESIAN_POINT('Ctrl Pts',(-0.0106728027741258,0.155191115319544,
0.322567035016699));
#9911=CARTESIAN_POINT('Ctrl Pts',(-0.00913032694338526,0.155289498749078,
0.322449370544501));
#9912=CARTESIAN_POINT('Ctrl Pts',(-0.00444993155897336,0.155518046297418,
0.322094838601657));
#9913=CARTESIAN_POINT('Ctrl Pts',(-0.00130905213082067,0.155576201956878,
0.321860318200235));
#9914=CARTESIAN_POINT('Ctrl Pts',(0.00237521922574042,0.155532814160507,
0.321590762491016));
#9915=CARTESIAN_POINT('Ctrl Pts',(0.00291870551660551,0.155523564544498,
0.321551140620584));
#9916=CARTESIAN_POINT('Ctrl Pts',(0.00379656517409258,0.155504020805235,
0.321487382551291));
#9917=CARTESIAN_POINT('Ctrl Pts',(0.00413096688544281,0.155495496758018,
0.32146315171864));
#9918=CARTESIAN_POINT('Ctrl Pts',(0.00472382364613329,0.155478470720674,
0.32142029625768));
#9919=CARTESIAN_POINT('Ctrl Pts',(0.00498228712648372,0.155470402927405,
0.321401647758151));
#9920=CARTESIAN_POINT('Ctrl Pts',(0.00553542999574471,0.155451756047836,
0.321361813063243));
#9921=CARTESIAN_POINT('Ctrl Pts',(0.00583009908345493,0.155440983631135,
0.321340637813952));
#9922=CARTESIAN_POINT('Ctrl Pts',(0.00663734268955308,0.155409173964979,
0.321282748383538));
#9923=CARTESIAN_POINT('Ctrl Pts',(0.00714985289851023,0.155386438577707,
0.321246127591292));
#9924=CARTESIAN_POINT('Ctrl Pts',(0.00986033728558172,0.155252760312061,
0.321053109776168));
#9925=CARTESIAN_POINT('Ctrl Pts',(0.0120560285610156,0.155097709046656,
0.320899035283374));
#9926=CARTESIAN_POINT('Ctrl Pts',(0.0282010883755749,0.153612634846923,
0.319778034047897));
#9927=CARTESIAN_POINT('Ctrl Pts',(0.0419186180543963,0.150449599533689,
0.318886327432832));
#9928=CARTESIAN_POINT('Ctrl Pts',(0.0613993227837462,0.143081521775237,
0.31749584890497));
#9929=CARTESIAN_POINT('Ctrl Pts',(0.0676043431192616,0.140256307234454,
0.317033233784034));
#9930=CARTESIAN_POINT('Ctrl Pts',(0.0744869323724657,0.13655952731255,0.316485905688618));
#9931=CARTESIAN_POINT('Ctrl Pts',(0.0753655114682721,0.136076622503357,
0.316415379815532));
#9932=CARTESIAN_POINT('Ctrl Pts',(0.0767645123763301,0.135289966905287,
0.316301987193396));
#9933=CARTESIAN_POINT('Ctrl Pts',(0.077287954531985,0.134991620374683,0.31625931341458));
#9934=CARTESIAN_POINT('Ctrl Pts',(0.0782127668251281,0.134457362564195,
0.316183470913544));
#9935=CARTESIAN_POINT('Ctrl Pts',(0.0786148384531749,0.134222674718234,
0.316150346580373));
#9936=CARTESIAN_POINT('Ctrl Pts',(0.0794488544196931,0.133730829411704,
0.316081318580144));
#9937=CARTESIAN_POINT('Ctrl Pts',(0.079880617183301,0.133473376338569,0.316045404472165));
#9938=CARTESIAN_POINT('Ctrl Pts',(0.0809953201807312,0.132801351213353,
0.315952213834214));
#9939=CARTESIAN_POINT('Ctrl Pts',(0.081676320486284,0.132383607002119,0.315894821977248));
#9940=CARTESIAN_POINT('Ctrl Pts',(0.0845877515648008,0.130566639701334,
0.315647448158808));
#9941=CARTESIAN_POINT('Ctrl Pts',(0.0867855525243568,0.129116232193679,
0.315455590180177));
#9942=CARTESIAN_POINT('Ctrl Pts',(0.0924897279614938,0.125140394179507,
0.314943519388029));
#9943=CARTESIAN_POINT('Ctrl Pts',(0.0959292991634937,0.122523594916081,
0.314620039179894));
#9944=CARTESIAN_POINT('Ctrl Pts',(0.108808669876982,0.111850018503915,0.313350719745203));
#9945=CARTESIAN_POINT('Ctrl Pts',(0.117379397400703,0.102819188601871,0.312373701995559));
#9946=CARTESIAN_POINT('Ctrl Pts',(0.125275761156514,0.0922087801849701,
0.311366054176543));
#9947=CARTESIAN_POINT('Ctrl Pts',(0.125760324472868,0.0915467984804432,
0.311303730131871));
#9948=CARTESIAN_POINT('Ctrl Pts',(0.128130719767829,0.0882541649237341,
0.310996514011709));
#9949=CARTESIAN_POINT('Ctrl Pts',(0.129939535236669,0.0855686863609178,
0.310754628481084));
#9950=CARTESIAN_POINT('Ctrl Pts',(0.131955386486013,0.0823643077774252,
0.310477636656397));
#9951=CARTESIAN_POINT('Ctrl Pts',(0.132244940280963,0.0818985898076804,
0.310437659282426));
#9952=CARTESIAN_POINT('Ctrl Pts',(0.132706027828015,0.0811481555372005,
0.310373702093419));
#9953=CARTESIAN_POINT('Ctrl Pts',(0.132879118949211,0.080864409488134,0.310349624232085));
#9954=CARTESIAN_POINT('Ctrl Pts',(0.133185461264069,0.080358586834402,0.310306890920478));
#9955=CARTESIAN_POINT('Ctrl Pts',(0.133319068612005,0.0801367301469652,
0.310288212448523));
#9956=CARTESIAN_POINT('Ctrl Pts',(0.133602538456296,0.0796633537755949,
0.310248496338573));
#9957=CARTESIAN_POINT('Ctrl Pts',(0.133752244808418,0.0794117449078804,
0.310227468866258));
#9958=CARTESIAN_POINT('Ctrl Pts',(0.13415750845334,0.0787262281996331,0.310170398344127));
#9959=CARTESIAN_POINT('Ctrl Pts',(0.134411673587953,0.0782914944490271,
0.310134444316195));
#9960=CARTESIAN_POINT('Ctrl Pts',(0.135703212854175,0.076057568342193,0.309950867426656));
#9961=CARTESIAN_POINT('Ctrl Pts',(0.136706654583689,0.07423885378224,0.309805305807871));
#9962=CARTESIAN_POINT('Ctrl Pts',(0.139552947965225,0.0688264719914708,
0.309381805733331));
#9963=CARTESIAN_POINT('Ctrl Pts',(0.141292739763657,0.0651803320972412,
0.309108787817847));
#9964=CARTESIAN_POINT('Ctrl Pts',(0.147014222448333,0.0518806514822679,
0.30814171923541));
#9965=CARTESIAN_POINT('Ctrl Pts',(0.150163855150907,0.0419000137475358,
0.30746699786141));
#9966=CARTESIAN_POINT('Ctrl Pts',(0.153611925935303,0.0253240905266897,
0.306334681780179));
#9967=CARTESIAN_POINT('Ctrl Pts',(0.154534618203243,0.0188935870117826,
0.305893080609385));
#9968=CARTESIAN_POINT('Ctrl Pts',(0.155132422106355,0.0114334299925759,
0.305368703045123));
#9969=CARTESIAN_POINT('Ctrl Pts',(0.155202354672146,0.0104412993850196,
0.305298730441605));
#9970=CARTESIAN_POINT('Ctrl Pts',(0.155299222545004,0.00884952964703879,
0.305186058417093));
#9971=CARTESIAN_POINT('Ctrl Pts',(0.15533221059567,0.00825027461614965,
0.305143548053034));
#9972=CARTESIAN_POINT('Ctrl Pts',(0.155384610726287,0.00718621328626032,
0.305067893831824));
#9973=CARTESIAN_POINT('Ctrl Pts',(0.155405407285597,0.00672147972893468,
0.305034793618392));
#9974=CARTESIAN_POINT('Ctrl Pts',(0.155444381178197,0.00575331483119456,
0.304965713044568));
#9975=CARTESIAN_POINT('Ctrl Pts',(0.155462198202698,0.0052498752740376,
0.30492972182303));
#9976=CARTESIAN_POINT('Ctrl Pts',(0.15550209362601,0.0039430129819499,0.304836107462004));
#9977=CARTESIAN_POINT('Ctrl Pts',(0.15552039086842,0.00313949877787785,
0.304778367008649));
#9978=CARTESIAN_POINT('Ctrl Pts',(0.155572667994231,-0.000341307548242315,
0.30452741782614));
#9979=CARTESIAN_POINT('Ctrl Pts',(0.15554374271425,-0.00301893436405565,
0.3043322650992));
#9980=CARTESIAN_POINT('Ctrl Pts',(0.155283834256495,-0.0101139993587367,
0.303809163172111));
#9981=CARTESIAN_POINT('Ctrl Pts',(0.154933531392658,-0.0145243350513768,
0.303477768604749));
#9982=CARTESIAN_POINT('Ctrl Pts',(0.152891807675056,-0.0311915515881011,
0.302202409464882));
#9983=CARTESIAN_POINT('Ctrl Pts',(0.149928786109605,-0.0432450630509603,
0.301228198694679));
#9984=CARTESIAN_POINT('Ctrl Pts',(0.144199783413796,-0.0584580099248424,
0.299990749377524));
#9985=CARTESIAN_POINT('Ctrl Pts',(0.14269360377312,-0.0620440031988351,
0.299698877066495));
#9986=CARTESIAN_POINT('Ctrl Pts',(0.140788092596793,-0.0661431384855975,
0.299367909198624));
#9987=CARTESIAN_POINT('Ctrl Pts',(0.140518231836121,-0.0667145287338506,
0.299321837031124));
#9988=CARTESIAN_POINT('Ctrl Pts',(0.140104534957726,-0.0675768234715042,
0.29925242069617));
#9989=CARTESIAN_POINT('Ctrl Pts',(0.139963262698345,-0.0678689390390178,
0.299228924410958));
#9990=CARTESIAN_POINT('Ctrl Pts',(0.139708153052337,-0.068392257463147,
0.299186869298371));
#9991=CARTESIAN_POINT('Ctrl Pts',(0.139594654845669,-0.0686236202205007,
0.299168289979218));
#9992=CARTESIAN_POINT('Ctrl Pts',(0.139347008278992,-0.0691252836335875,
0.299128034175251));
#9993=CARTESIAN_POINT('Ctrl Pts',(0.139212648582225,-0.0693954755922074,
0.299106371128295));
#9994=CARTESIAN_POINT('Ctrl Pts',(0.138833678231784,-0.0701520397109793,
0.299045759318072));
#9995=CARTESIAN_POINT('Ctrl Pts',(0.138587295899455,-0.0706375277448612,
0.299006919120298));
#9996=CARTESIAN_POINT('Ctrl Pts',(0.137113893931152,-0.0735034316300548,
0.29877790310948));
#9997=CARTESIAN_POINT('Ctrl Pts',(0.135828019537181,-0.0758533177111465,
0.298591199690355));
#9998=CARTESIAN_POINT('Ctrl Pts',(0.127120598043966,-0.0908335695765035,
0.297400263076346));
#9999=CARTESIAN_POINT('Ctrl Pts',(0.118006561187256,-0.102395998037373,
0.29647133687095));
#10000=CARTESIAN_POINT('Ctrl Pts',(0.105952252301966,-0.113903356353573,
0.295351500190367));
#10001=CARTESIAN_POINT('Ctrl Pts',(0.104469455841599,-0.115264854424969,
0.295215438622432));
#10002=CARTESIAN_POINT('Ctrl Pts',(0.100038150820563,-0.119177902442594,
0.294812886440002));
#10003=CARTESIAN_POINT('Ctrl Pts',(0.097019839541405,-0.121647648552644,
0.294543759461496));
#10004=CARTESIAN_POINT('Ctrl Pts',(0.0931596446242968,-0.124571161105423,
0.29420375564164));
#10005=CARTESIAN_POINT('Ctrl Pts',(0.0924019799560585,-0.125134198346578,
0.294137215917408));
#10006=CARTESIAN_POINT('Ctrl Pts',(0.0912025773697343,-0.126008668068039,
0.29403216089233));
#10007=CARTESIAN_POINT('Ctrl Pts',(0.0907642513720203,-0.126324760861218,
0.293993825977405));
#10008=CARTESIAN_POINT('Ctrl Pts',(0.0899874343255327,-0.126878821568116,
0.293925984398484));
#10009=CARTESIAN_POINT('Ctrl Pts',(0.0896496222738355,-0.12711773644577,
0.293896514407064));
#10010=CARTESIAN_POINT('Ctrl Pts',(0.0888733773329952,-0.127662096257359,
0.293828867189764));
#10011=CARTESIAN_POINT('Ctrl Pts',(0.0884343178420111,-0.127966634065507,
0.293790655899963));
#10012=CARTESIAN_POINT('Ctrl Pts',(0.0872167660204803,-0.128801886361493,
0.293684827713051));
#10013=CARTESIAN_POINT('Ctrl Pts',(0.0864350188683064,-0.129327791468073,
0.293617030608923));
#10014=CARTESIAN_POINT('Ctrl Pts',(0.0846927362010747,-0.13047702489966,
0.293466241470117));
#10015=CARTESIAN_POINT('Ctrl Pts',(0.0837300063831723,-0.131096908784045,
0.293383125858262));
#10016=CARTESIAN_POINT('Ctrl Pts',(0.0807394573813568,-0.132976088845127,
0.293125528260265));
#10017=CARTESIAN_POINT('Ctrl Pts',(0.0786895134417772,-0.13419932752562,
0.292949766076832));
#10018=CARTESIAN_POINT('Ctrl Pts',(0.063552779746995,-0.14276561937207,
0.291657361230243));
#10019=CARTESIAN_POINT('Ctrl Pts',(0.0494933861140353,-0.148226928899269,
0.290474937900805));
#10020=CARTESIAN_POINT('Ctrl Pts',(0.0304589108108244,-0.152605992650428,
0.288981512458593));
#10021=CARTESIAN_POINT('Ctrl Pts',(0.0260002458625941,-0.153428586160075,
0.288639849816666));
#10022=CARTESIAN_POINT('Ctrl Pts',(0.0208543036868468,-0.154147140419328,
0.288259233628864));
#10023=CARTESIAN_POINT('Ctrl Pts',(0.0201964709833297,-0.154234709077025,
0.288210833279952));
#10024=CARTESIAN_POINT('Ctrl Pts',(0.0192139972853612,-0.154359099255711,
0.288138948437671));
#10025=CARTESIAN_POINT('Ctrl Pts',(0.0188897797816933,-0.154399110877777,
0.288115291432368));
#10026=CARTESIAN_POINT('Ctrl Pts',(0.01830941677064,-0.154468877932902,
0.288073063649479));
#10027=CARTESIAN_POINT('Ctrl Pts',(0.0180533222193519,-0.154499017966925,
0.288054471637995));
#10028=CARTESIAN_POINT('Ctrl Pts',(0.0174989975029473,-0.154562859895225,
0.288014319166698));
#10029=CARTESIAN_POINT('Ctrl Pts',(0.0172007451990448,-0.154596335471925,
0.287992771565049));
#10030=CARTESIAN_POINT('Ctrl Pts',(0.016368637830235,-0.154687292612542,
0.287932807138131));
#10031=CARTESIAN_POINT('Ctrl Pts',(0.0158345721877104,-0.154742874299795,
0.287894495176426));
#10032=CARTESIAN_POINT('Ctrl Pts',(0.012797494639218,-0.155043063221851,
0.287677562492922));
#10033=CARTESIAN_POINT('Ctrl Pts',(0.0102889443697388,-0.155229722983398,
0.287501992906389));
#10034=CARTESIAN_POINT('Ctrl Pts',(-0.00698094676142714,-0.156094218921507,
0.286311219262086));
#10035=CARTESIAN_POINT('Ctrl Pts',(-0.0217701013512237,-0.154726578431675,
0.285374843717495));
#10036=CARTESIAN_POINT('Ctrl Pts',(-0.0379214800930314,-0.150867815742666,
0.284259310255825));
#10037=CARTESIAN_POINT('Ctrl Pts',(-0.0396897590620582,-0.150412297191286,
0.28413599582269));
#10038=CARTESIAN_POINT('Ctrl Pts',(-0.0454076550927831,-0.148831486265594,
0.283732711240773));
#10039=CARTESIAN_POINT('Ctrl Pts',(-0.0493205268322766,-0.147580984552771,
0.283449587823713));
#10040=CARTESIAN_POINT('Ctrl Pts',(-0.0540009166304922,-0.145878265405383,
0.283099965806389));
#10041=CARTESIAN_POINT('Ctrl Pts',(-0.0548202064040207,-0.145572360799852,
0.28303835237914));
#10042=CARTESIAN_POINT('Ctrl Pts',(-0.0561693576057605,-0.145055613195911,
0.282936185745965));
#10043=CARTESIAN_POINT('Ctrl Pts',(-0.0567007247238053,-0.144848733006444,
0.282895764924838));
#10044=CARTESIAN_POINT('Ctrl Pts',(-0.0576592421891808,-0.144469465484676,
0.282822515128432));
#10045=CARTESIAN_POINT('Ctrl Pts',(-0.0580867892668555,-0.144298092750948,
0.282789720534529));
#10046=CARTESIAN_POINT('Ctrl Pts',(-0.0589150986463811,-0.143961805547251,
0.282725946621811));
#10047=CARTESIAN_POINT('Ctrl Pts',(-0.0593159457971507,-0.143797110096527,
0.282694974945782));
#10048=CARTESIAN_POINT('Ctrl Pts',(-0.0604009629802681,-0.143346002008202,
0.28261084038669));
#10049=CARTESIAN_POINT('Ctrl Pts',(-0.0610837736383424,-0.143056370649525,
0.282557568958235));
#10050=CARTESIAN_POINT('Ctrl Pts',(-0.0639388245435889,-0.141821161829619,
0.282333435379573));
#10051=CARTESIAN_POINT('Ctrl Pts',(-0.0660912798635748,-0.140830951154788,
0.282161063258689));
#10052=CARTESIAN_POINT('Ctrl Pts',(-0.0715947836888051,-0.13814517552773,
0.281711175681017));
#10053=CARTESIAN_POINT('Ctrl Pts',(-0.0749083747560809,-0.136376807863524,
0.281431275603599));
#10054=CARTESIAN_POINT('Ctrl Pts',(-0.0845601198995792,-0.13076802635846,
0.280588694625293));
#10055=CARTESIAN_POINT('Ctrl Pts',(-0.0906910240442798,-0.126593084772745,
0.280016480914248));
#10056=CARTESIAN_POINT('Ctrl Pts',(-0.103643547390748,-0.116347596842595,
0.278735801803397));
#10057=CARTESIAN_POINT('Ctrl Pts',(-0.110277293779692,-0.110080440989303,
0.278028330146676));
#10058=CARTESIAN_POINT('Ctrl Pts',(-0.117096675653929,-0.102398838755052,
0.2772689420312));
#10059=CARTESIAN_POINT('Ctrl Pts',(-0.117858631760769,-0.101520917864376,
0.277183601606336));
#10060=CARTESIAN_POINT('Ctrl Pts',(-0.118884376945866,-0.100311945242677,
0.277068133461041));
#10061=CARTESIAN_POINT('Ctrl Pts',(-0.119156736679291,-0.0999882670891371,
0.277037416609493));
#10062=CARTESIAN_POINT('Ctrl Pts',(-0.119586356768663,-0.0994734488844824,
0.276988878023448));
#10063=CARTESIAN_POINT('Ctrl Pts',(-0.119744484389673,-0.099283040942448,
0.276970994096709));
#10064=CARTESIAN_POINT('Ctrl Pts',(-0.12006917201687,-0.0988901671757694,
0.276934235513077));
#10065=CARTESIAN_POINT('Ctrl Pts',(-0.120235674636361,-0.0986876576821558,
0.276915365392171));
#10066=CARTESIAN_POINT('Ctrl Pts',(-0.120629525014883,-0.0982061592484336,
0.276870679546228));
#10067=CARTESIAN_POINT('Ctrl Pts',(-0.120856419930169,-0.0979267981114251,
0.276844896448671));
#10068=CARTESIAN_POINT('Ctrl Pts',(-0.121334544872652,-0.0973339207221548,
0.276790474052623));
#10069=CARTESIAN_POINT('Ctrl Pts',(-0.121585534597569,-0.0970202127838668,
0.276761851491534));
#10070=CARTESIAN_POINT('Ctrl Pts',(-0.123637434388573,-0.0944351088812501,
0.276527378092782));
#10071=CARTESIAN_POINT('Ctrl Pts',(-0.125375899765741,-0.0921145571175439,
0.276325680582519));
#10072=CARTESIAN_POINT('Ctrl Pts',(-0.133332039786485,-0.0808515455563323,
0.275380348264986));
#10073=CARTESIAN_POINT('Ctrl Pts',(-0.138664588988016,-0.0713203237475915,
0.274676414146517));
#10074=CARTESIAN_POINT('Ctrl Pts',(-0.144190224994525,-0.0584359147975346,
0.273749490832387));
#10075=CARTESIAN_POINT('Ctrl Pts',(-0.145335548306044,-0.0555261590693752,
0.273541809798545));
#10076=CARTESIAN_POINT('Ctrl Pts',(-0.147116060408715,-0.0505692593613106,
0.273188656103198));
#10077=CARTESIAN_POINT('Ctrl Pts',(-0.147798046706393,-0.0485399015835882,
0.273044255500863));
#10078=CARTESIAN_POINT('Ctrl Pts',(-0.14966751215074,-0.0425718069201622,
0.272619128352821));
#10079=CARTESIAN_POINT('Ctrl Pts',(-0.150740815246993,-0.0385995395850642,
0.27233554217521));
#10080=CARTESIAN_POINT('Ctrl Pts',(-0.151849957232022,-0.0337366061969515,
0.271985408570263));
#10081=CARTESIAN_POINT('Ctrl Pts',(-0.152037324006107,-0.032881912390198,
0.27192376349765));
#10082=CARTESIAN_POINT('Ctrl Pts',(-0.152334896757062,-0.0314675554134114,
0.271821555198225));
#10083=CARTESIAN_POINT('Ctrl Pts',(-0.152449254762276,-0.0309087774003956,
0.271781124546243));
#10084=CARTESIAN_POINT('Ctrl Pts',(-0.152650408622758,-0.0298976156953686,
0.271707864204032));
#10085=CARTESIAN_POINT('Ctrl Pts',(-0.152738273503795,-0.0294454491505347,
0.271675068940467));
#10086=CARTESIAN_POINT('Ctrl Pts',(-0.152904899511301,-0.0285671489025245,
0.271611295578362));
#10087=CARTESIAN_POINT('Ctrl Pts',(-0.15298389089345,-0.0281410627210089,
0.271580325129715));
#10088=CARTESIAN_POINT('Ctrl Pts',(-0.153153087502518,-0.0272066322474014,
0.271512331805116));
#10089=CARTESIAN_POINT('Ctrl Pts',(-0.15324254409131,-0.0266981594553495,
0.271475285530647));
#10090=CARTESIAN_POINT('Ctrl Pts',(-0.153456080376488,-0.0254479748661856,
0.271384078522261));
#10091=CARTESIAN_POINT('Ctrl Pts',(-0.153577314645084,-0.0247057972702772,
0.27132982849307));
#10092=CARTESIAN_POINT('Ctrl Pts',(-0.154066536286533,-0.0215680138064688,
0.271100008084215));
#10093=CARTESIAN_POINT('Ctrl Pts',(-0.154383869571322,-0.0191649788829334,
0.270922860778074));
#10094=CARTESIAN_POINT('Ctrl Pts',(-0.155252803672957,-0.0111452131060672,
0.270327540589336));
#10095=CARTESIAN_POINT('Ctrl Pts',(-0.155554845593828,-0.00550663010602916,
0.269902092796786));
#10096=CARTESIAN_POINT('Ctrl Pts',(-0.155549941229055,0.000135217002094367,
0.269470366437021));
#10097=CARTESIAN_POINT('Ctrl Pts',(-0.155549941365104,0.000135060403868008,
0.269470378420255));
#10098=CARTESIAN_POINT('Ctrl Pts',(-0.155538361405763,0.0134717745324127,
0.26844982442386));
#10099=CARTESIAN_POINT('Ctrl Pts',(-0.153811734320124,0.0267516801702719,
0.267394858539501));
#10100=CARTESIAN_POINT('Ctrl Pts',(-0.150111277084165,0.0407896868427397,
0.266312817712502));
#10101=CARTESIAN_POINT('Ctrl Pts',(-0.149797613421265,0.0419269517450572,
0.266225448687747));
#10102=CARTESIAN_POINT('Ctrl Pts',(-0.149236792556411,0.0438736619999813,
0.266076519031741));
#10103=CARTESIAN_POINT('Ctrl Pts',(-0.148995916974571,0.0446848439766073,
0.26601464858016));
#10104=CARTESIAN_POINT('Ctrl Pts',(-0.148642949659393,0.0458389144450729,
0.265926932409377));
#10105=CARTESIAN_POINT('Ctrl Pts',(-0.148536272114212,0.0461834216411417,
0.265900787037438));
#10106=CARTESIAN_POINT('Ctrl Pts',(-0.148349939715738,0.0467778439441754,
0.265855746577269));
#10107=CARTESIAN_POINT('Ctrl Pts',(-0.148270849562501,0.0470279328930674,
0.265836818850273));
#10108=CARTESIAN_POINT('Ctrl Pts',(-0.148115965218899,0.0475134138773714,
0.265800119717081));
#10109=CARTESIAN_POINT('Ctrl Pts',(-0.148040242376818,0.0477488250155281,
0.26578234413627));
#10110=CARTESIAN_POINT('Ctrl Pts',(-0.147833805744105,0.0483853943933405,
0.265734329048688));
#10111=CARTESIAN_POINT('Ctrl Pts',(-0.14770201935289,0.0487862070844197,
0.265704151940773));
#10112=CARTESIAN_POINT('Ctrl Pts',(-0.147203281391342,0.0502825137170163,
0.265591684826262));
#10113=CARTESIAN_POINT('Ctrl Pts',(-0.146825747271535,0.0513744818662478,
0.265509989668008));
#10114=CARTESIAN_POINT('Ctrl Pts',(-0.142730112011315,0.0628065013125632,
0.264657703250813));
#10115=CARTESIAN_POINT('Ctrl Pts',(-0.137937851128568,0.0727308189373068,
0.263942295714118));
#10116=CARTESIAN_POINT('Ctrl Pts',(-0.12975729239478,0.0859023757296986,
0.262921291152447));
#10117=CARTESIAN_POINT('Ctrl Pts',(-0.12721036291946,0.0896308770702425,
0.262623406814871));
#10118=CARTESIAN_POINT('Ctrl Pts',(-0.121858548842607,0.0967770005487323,
0.26202649707633));
#10119=CARTESIAN_POINT('Ctrl Pts',(-0.119063032751312,0.10019622165393,
0.261727916813682));
#10120=CARTESIAN_POINT('Ctrl Pts',(-0.114352767742845,0.105481519166797,
0.261240360201995));
#10121=CARTESIAN_POINT('Ctrl Pts',(-0.112528713944862,0.107425292334628,
0.261054932654558));
#10122=CARTESIAN_POINT('Ctrl Pts',(-0.110103093240845,0.109880524439778,
0.260812031158641));
#10123=CARTESIAN_POINT('Ctrl Pts',(-0.109546243220104,0.110435688742401,
0.260756510024244));
#10124=CARTESIAN_POINT('Ctrl Pts',(-0.108674959710832,0.111291260711172,
0.260669996614128));
#10125=CARTESIAN_POINT('Ctrl Pts',(-0.108363429192316,0.111594618084951,
0.260639133535982));
#10126=CARTESIAN_POINT('Ctrl Pts',(-0.107752979622864,0.112184085736192,
0.260578790309104));
#10127=CARTESIAN_POINT('Ctrl Pts',(-0.107454182589295,0.112470317631217,
0.260549315785306));
#10128=CARTESIAN_POINT('Ctrl Pts',(-0.106762901911694,0.113127259065976,
0.260481264210018));
#10129=CARTESIAN_POINT('Ctrl Pts',(-0.106369625196915,0.113497122387658,
0.260442651310369));
#10130=CARTESIAN_POINT('Ctrl Pts',(-0.105285153294287,0.114506443705127,
0.260336448360013));
#10131=CARTESIAN_POINT('Ctrl Pts',(-0.104590074552427,0.115141675282488,
0.260268680218121));
#10132=CARTESIAN_POINT('Ctrl Pts',(-0.101008839438464,0.118355376651227,
0.259920994573663));
#10133=CARTESIAN_POINT('Ctrl Pts',(-0.0980331892901918,0.12083157574309,
0.259636886249868));
#10134=CARTESIAN_POINT('Ctrl Pts',(-0.086678510720647,0.129584735278999,
0.25856874917064));
#10135=CARTESIAN_POINT('Ctrl Pts',(-0.0777657023239636,0.135121428718178,
0.257758592970445));
#10136=CARTESIAN_POINT('Ctrl Pts',(-0.0668190495798515,0.140477699583313,
0.256813759178683));
#10137=CARTESIAN_POINT('Ctrl Pts',(-0.0652596210018785,0.141208885972023,
0.256680339621468));
#10138=CARTESIAN_POINT('Ctrl Pts',(-0.0636886236493968,0.141913923621488,
0.256547255026181));
#10139=CARTESIAN_POINT('Ctrl Pts',(-0.0636886300394901,0.141913920753719,
0.24285329779702));
#10140=CARTESIAN_POINT('Ctrl Pts',(-0.0646310252844373,0.141490989290846,
0.242933115031557));
#10141=CARTESIAN_POINT('Ctrl Pts',(-0.0655693880425395,0.141058589799998,
0.243012827267554));
#10142=CARTESIAN_POINT('Ctrl Pts',(-0.0701705969310746,0.138882485006915,
0.243404678902055));
#10143=CARTESIAN_POINT('Ctrl Pts',(-0.0737686816808534,0.137005270628566,
0.243714243232908));
#10144=CARTESIAN_POINT('Ctrl Pts',(-0.0790971242092449,0.133954417778686,
0.244173589806775));
#10145=CARTESIAN_POINT('Ctrl Pts',(-0.0808838855652834,0.132883179207204,
0.244327773649405));
#10146=CARTESIAN_POINT('Ctrl Pts',(-0.0830756240255447,0.131508544011537,
0.244516604484947));
#10147=CARTESIAN_POINT('Ctrl Pts',(-0.0835012477505949,0.13123870655549,
0.244553260016158));
#10148=CARTESIAN_POINT('Ctrl Pts',(-0.084172084477396,0.130808823958321,
0.244611001763488));
#10149=CARTESIAN_POINT('Ctrl Pts',(-0.0844181647311111,0.130650150011145,
0.244632176075007));
#10150=CARTESIAN_POINT('Ctrl Pts',(-0.0848809667469775,0.13034987916913,
0.24467198340744));
#10151=CARTESIAN_POINT('Ctrl Pts',(-0.0850977803515731,0.13020843788296,
0.24469062580215));
#10152=CARTESIAN_POINT('Ctrl Pts',(-0.08559190055342,0.129884330543777,
0.244733098503388));
#10153=CARTESIAN_POINT('Ctrl Pts',(-0.085868975841331,0.129701317474722,
0.244756905315376));
#10154=CARTESIAN_POINT('Ctrl Pts',(-0.0866013419250812,0.129214201380808,
0.244819812346093));
#10155=CARTESIAN_POINT('Ctrl Pts',(-0.0870556223805546,0.128908575732652,
0.24485881330213));
#10156=CARTESIAN_POINT('Ctrl Pts',(-0.0901716165641117,0.12678824798451,
0.245126262904502));
#10157=CARTESIAN_POINT('Ctrl Pts',(-0.0927782537850686,0.124893473607168,
0.245349667757981));
#10158=CARTESIAN_POINT('Ctrl Pts',(-0.0959900452419526,0.122402709515645,
0.245627154765004));
#10159=CARTESIAN_POINT('Ctrl Pts',(-0.0966515095238083,0.121881080732186,
0.245684425565424));
#10160=CARTESIAN_POINT('Ctrl Pts',(-0.0980100135738502,0.120791753799071,
0.245802378344208));
#10161=CARTESIAN_POINT('Ctrl Pts',(-0.0987064355934165,0.120223334560066,
0.245863029049646));
#10162=CARTESIAN_POINT('Ctrl Pts',(-0.110933337841073,0.110065878648549,
0.246931902287378));
#10163=CARTESIAN_POINT('Ctrl Pts',(-0.121022191170155,0.0988654033982793,
0.247886286394423));
#10164=CARTESIAN_POINT('Ctrl Pts',(-0.131205465187675,0.0836185598499964,
0.249141409538127));
#10165=CARTESIAN_POINT('Ctrl Pts',(-0.132968919682436,0.0807849070926952,
0.249372643878607));
#10166=CARTESIAN_POINT('Ctrl Pts',(-0.135073785434927,0.077146782413369,
0.249668171050736));
#10167=CARTESIAN_POINT('Ctrl Pts',(-0.135501495390457,0.076393050999492,
0.249729324185004));
#10168=CARTESIAN_POINT('Ctrl Pts',(-0.136174555111127,0.075183515096626,
0.249827362145157));
#10169=CARTESIAN_POINT('Ctrl Pts',(-0.136423971337927,0.0747299835046003,
0.249864101335422));
#10170=CARTESIAN_POINT('Ctrl Pts',(-0.136891557240927,0.0738695957861169,
0.249933762654057));
#10171=CARTESIAN_POINT('Ctrl Pts',(-0.137110188769411,0.0734629958048693,
0.249966667923186));
#10172=CARTESIAN_POINT('Ctrl Pts',(-0.137600944887211,0.0725404899020796,
0.250041293699401));
#10173=CARTESIAN_POINT('Ctrl Pts',(-0.137871982856152,0.0720240170724891,
0.250083052018111));
#10174=CARTESIAN_POINT('Ctrl Pts',(-0.138663139207676,0.070495608776675,
0.250206573047868));
#10175=CARTESIAN_POINT('Ctrl Pts',(-0.139175056893584,0.0694794965617869,
0.250288621284287));
#10176=CARTESIAN_POINT('Ctrl Pts',(-0.144387811887925,0.0588438251891433,
0.251146868886069));
#10177=CARTESIAN_POINT('Ctrl Pts',(-0.148093635503412,0.0487710897163048,
0.251958081617822));
#10178=CARTESIAN_POINT('Ctrl Pts',(-0.152625356991953,0.0309821951729422,
0.253377140340226));
#10179=CARTESIAN_POINT('Ctrl Pts',(-0.153964934328477,0.0234350101372198,
0.253974383355005));
#10180=CARTESIAN_POINT('Ctrl Pts',(-0.15504708924477,0.0128497394444634,
0.254787005803065));
#10181=CARTESIAN_POINT('Ctrl Pts',(-0.155265173507138,0.00987137877698549,
0.25501284781695));
#10182=CARTESIAN_POINT('Ctrl Pts',(-0.1554471956716,0.00576508064528757,
0.255318874111009));
#10183=CARTESIAN_POINT('Ctrl Pts',(-0.155484809544134,0.00464122617924813,
0.25540207951625));
#10184=CARTESIAN_POINT('Ctrl Pts',(-0.155528663351504,0.0027021669107826,
0.255544581490408));
#10185=CARTESIAN_POINT('Ctrl Pts',(-0.155540687778674,0.00188715468499464,
0.255604154823418));
#10186=CARTESIAN_POINT('Ctrl Pts',(-0.155548753196391,0.000716937102396059,
0.25568919446813));
#10187=CARTESIAN_POINT('Ctrl Pts',(-0.155549984658848,0.000361799947529685,
0.25571493649624));
#10188=CARTESIAN_POINT('Ctrl Pts',(-0.155550011041026,-0.000254663437624176,
0.255759502982025));
#10189=CARTESIAN_POINT('Ctrl Pts',(-0.155549363710134,-0.000515986568123264,
0.25577835824537));
#10190=CARTESIAN_POINT('Ctrl Pts',(-0.155546638232264,-0.00106138237633014,
0.255817632196304));
#10191=CARTESIAN_POINT('Ctrl Pts',(-0.155544440473662,-0.00134545129377664,
0.255838044120524));
#10192=CARTESIAN_POINT('Ctrl Pts',(-0.155536595733541,-0.0020942519099721,
0.255891737721539));
#10193=CARTESIAN_POINT('Ctrl Pts',(-0.155529644058057,-0.00255897196269481,
0.255924947411003));
#10194=CARTESIAN_POINT('Ctrl Pts',(-0.155488728703524,-0.00466343375498688,
0.256074849985892));
#10195=CARTESIAN_POINT('Ctrl Pts',(-0.155430914162649,-0.00630268759477646,
0.256190279496122));
#10196=CARTESIAN_POINT('Ctrl Pts',(-0.155201019275601,-0.0108001549157698,
0.256504064543988));
#10197=CARTESIAN_POINT('Ctrl Pts',(-0.154975932195845,-0.0136551260960159,
0.256700027510645));
#10198=CARTESIAN_POINT('Ctrl Pts',(-0.15288775239119,-0.0332269647460581,
0.258031182991192));
#10199=CARTESIAN_POINT('Ctrl Pts',(-0.148402991951509,-0.0495511847403122,
0.259092852227158));
#10200=CARTESIAN_POINT('Ctrl Pts',(-0.140835635852098,-0.0660522538505316,
0.260346101737872));
#10201=CARTESIAN_POINT('Ctrl Pts',(-0.140264899314354,-0.0672557388049182,
0.260438531145712));
#10202=CARTESIAN_POINT('Ctrl Pts',(-0.139053280586148,-0.0697281011010006,
0.260630662994696));
#10203=CARTESIAN_POINT('Ctrl Pts',(-0.13841032142666,-0.0709958140481729,
0.260730427351576));
#10204=CARTESIAN_POINT('Ctrl Pts',(-0.13748681737535,-0.0727564347766701,
0.260870821827192));
#10205=CARTESIAN_POINT('Ctrl Pts',(-0.137220798580539,-0.0732569189562833,
0.260910941735121));
#10206=CARTESIAN_POINT('Ctrl Pts',(-0.13672873428624,-0.074170597539528,
0.260984576785553));
#10207=CARTESIAN_POINT('Ctrl Pts',(-0.136503535144281,-0.0745842423242739,
0.261018061667909));
#10208=CARTESIAN_POINT('Ctrl Pts',(-0.136043867976956,-0.0754195015726712,
0.261085981348318));
#10209=CARTESIAN_POINT('Ctrl Pts',(-0.135809310302092,-0.0758410604963707,
0.261120419062224));
#10210=CARTESIAN_POINT('Ctrl Pts',(-0.13522700051705,-0.0768762532084486,
0.261205380375507));
#10211=CARTESIAN_POINT('Ctrl Pts',(-0.134877031455413,-0.0774886206587898,
0.261255983084047));
#10212=CARTESIAN_POINT('Ctrl Pts',(-0.133574035952822,-0.0797329989666328,
0.261442733736896));
#10213=CARTESIAN_POINT('Ctrl Pts',(-0.132595489764074,-0.0813499214125757,
0.26157979973297));
#10214=CARTESIAN_POINT('Ctrl Pts',(-0.126189131654329,-0.0915128278749574,
0.262457941517948));
#10215=CARTESIAN_POINT('Ctrl Pts',(-0.119968364155803,-0.0995279482857881,
0.263228849318606));
#10216=CARTESIAN_POINT('Ctrl Pts',(-0.105583413615441,-0.11473844762226,
0.264848980466173));
#10217=CARTESIAN_POINT('Ctrl Pts',(-0.0973523903873451,-0.121800336528475,
0.2656954993498));
#10218=CARTESIAN_POINT('Ctrl Pts',(-0.0875174985688326,-0.128599330470599,
0.266579087403249));
#10219=CARTESIAN_POINT('Ctrl Pts',(-0.0865732676975356,-0.129236875070932,
0.266662706865862));
#10220=CARTESIAN_POINT('Ctrl Pts',(-0.0852719532568076,-0.130094859111347,
0.266776212351666));
#10221=CARTESIAN_POINT('Ctrl Pts',(-0.0849208879832633,-0.130324292342802,
0.266806662810959));
#10222=CARTESIAN_POINT('Ctrl Pts',(-0.0843618096442823,-0.130686450912175,
0.266854879919869));
#10223=CARTESIAN_POINT('Ctrl Pts',(-0.0841544048335969,-0.130820103684079,
0.266872707371933));
#10224=CARTESIAN_POINT('Ctrl Pts',(-0.0837256941361658,-0.13109492570158,
0.266909432174851));
#10225=CARTESIAN_POINT('Ctrl Pts',(-0.0835043488151082,-0.131236028336217,
0.266928324706472));
#10226=CARTESIAN_POINT('Ctrl Pts',(-0.0829767495209032,-0.131570485726683,
0.266973196221415));
#10227=CARTESIAN_POINT('Ctrl Pts',(-0.0826701727770193,-0.131763334109334,
0.266999141789122));
#10228=CARTESIAN_POINT('Ctrl Pts',(-0.0816371804463011,-0.132408100834492,
0.267086143429506));
#10229=CARTESIAN_POINT('Ctrl Pts',(-0.0809076931497814,-0.132855107825965,
0.267146886832381));
#10230=CARTESIAN_POINT('Ctrl Pts',(-0.0791491681472426,-0.133912820203145,
0.267291749900795));
#10231=CARTESIAN_POINT('Ctrl Pts',(-0.0781166826918304,-0.13451772497603,
0.267375532259073));
#10232=CARTESIAN_POINT('Ctrl Pts',(-0.0742375753964356,-0.136730659220493,
0.267685996099241));
#10233=CARTESIAN_POINT('Ctrl Pts',(-0.0713472830942073,-0.138260837545,
0.267908761299697));
#10234=CARTESIAN_POINT('Ctrl Pts',(-0.0635493598096736,-0.142079489259363,
0.268493146901523));
#10235=CARTESIAN_POINT('Ctrl Pts',(-0.058566809500545,-0.144204845116762,
0.268849738536345));
#10236=CARTESIAN_POINT('Ctrl Pts',(-0.0425734801544572,-0.150060937094764,
0.2699708356569));
#10237=CARTESIAN_POINT('Ctrl Pts',(-0.0312520119154191,-0.152820319826965,
0.270733762018313));
#10238=CARTESIAN_POINT('Ctrl Pts',(-0.0179990143981319,-0.154514989613307,
0.271662290042638));
#10239=CARTESIAN_POINT('Ctrl Pts',(-0.0162648526853695,-0.154707144865804,
0.271784388974812));
#10240=CARTESIAN_POINT('Ctrl Pts',(-0.013826894949649,-0.154935842165196,
0.271957042354235));
#10241=CARTESIAN_POINT('Ctrl Pts',(-0.0131254769140946,-0.154996838799361,
0.272006831718319));
#10242=CARTESIAN_POINT('Ctrl Pts',(-0.0119911094886615,-0.15508773036931,
0.272087550688457));
#10243=CARTESIAN_POINT('Ctrl Pts',(-0.0115584006573708,-0.155120579502367,
0.272118387559271));
#10244=CARTESIAN_POINT('Ctrl Pts',(-0.0106570961333128,-0.1551852099674,
0.272182717976255));
#10245=CARTESIAN_POINT('Ctrl Pts',(-0.0101884833019987,-0.155216680449379,
0.272216220911841));
#10246=CARTESIAN_POINT('Ctrl Pts',(-0.00908190995427605,-0.155285961481448,
0.272295469506566));
#10247=CARTESIAN_POINT('Ctrl Pts',(-0.00844384900640427,-0.155321963395448,
0.272341271206601));
#10248=CARTESIAN_POINT('Ctrl Pts',(-0.00633310829019463,-0.155428015249109,
0.27249314860609));
#10249=CARTESIAN_POINT('Ctrl Pts',(-0.00485969507336507,-0.15548105759351,
0.272599752115084));
#10250=CARTESIAN_POINT('Ctrl Pts',(0.00290524697204107,-0.155650114129601,
0.273164815382534));
#10251=CARTESIAN_POINT('Ctrl Pts',(0.00919791101476006,-0.155405202570579,
0.273634358054969));
#10252=CARTESIAN_POINT('Ctrl Pts',(0.0233073754734391,-0.153996105058492,
0.274713118147876));
#10253=CARTESIAN_POINT('Ctrl Pts',(0.0310855464860249,-0.152616205180488,
0.275326287983536));
#10254=CARTESIAN_POINT('Ctrl Pts',(0.0401852769142114,-0.15027714336649,
0.276054126084955));
#10255=CARTESIAN_POINT('Ctrl Pts',(0.0416401932374928,-0.149880521437169,
0.27617079471762));
#10256=CARTESIAN_POINT('Ctrl Pts',(0.0492948719477864,-0.147673728709153,
0.276785618193729));
#10257=CARTESIAN_POINT('Ctrl Pts',(0.0553840608470555,-0.145499632773997,
0.277278437823852));
#10258=CARTESIAN_POINT('Ctrl Pts',(0.0619644296493473,-0.14267691452889,
0.277803342523287));
#10259=CARTESIAN_POINT('Ctrl Pts',(0.062605874614149,-0.142396618621266,
0.277854423407324));
#10260=CARTESIAN_POINT('Ctrl Pts',(0.063550366001855,-0.14197628284294,
0.277929486769382));
#10261=CARTESIAN_POINT('Ctrl Pts',(0.0638548766492982,-0.141839587713198,
0.277953664505873));
#10262=CARTESIAN_POINT('Ctrl Pts',(0.0643943788385472,-0.141595315120732,
0.277996455990822));
#10263=CARTESIAN_POINT('Ctrl Pts',(0.0646295441600475,-0.141488131359905,
0.278015093388228));
#10264=CARTESIAN_POINT('Ctrl Pts',(0.0651327072876176,-0.141257283185047,
0.278054937176998));
#10265=CARTESIAN_POINT('Ctrl Pts',(0.0654006199441148,-0.141133442267647,
0.27807613248833));
#10266=CARTESIAN_POINT('Ctrl Pts',(0.0661346353465462,-0.140791609391587,
0.278134152559328));
#10267=CARTESIAN_POINT('Ctrl Pts',(0.0666000172412687,-0.140572063337675,
0.27817088318408));
#10268=CARTESIAN_POINT('Ctrl Pts',(0.06907051370596,-0.139391572456316,
0.278365619318536));
#10269=CARTESIAN_POINT('Ctrl Pts',(0.0710560733276606,-0.13838996408166,
0.278521252640042));
#10270=CARTESIAN_POINT('Ctrl Pts',(0.085442687186578,-0.130741365023255,
0.279647470213097));
#10271=CARTESIAN_POINT('Ctrl Pts',(0.0969137479924993,-0.12248098898627,
0.280542528707925));
#10272=CARTESIAN_POINT('Ctrl Pts',(0.112000299278424,-0.108152963710786,
0.281932174259887));
#10273=CARTESIAN_POINT('Ctrl Pts',(0.116575335321449,-0.10320514803952,
0.28238963041825));
#10274=CARTESIAN_POINT('Ctrl Pts',(0.121445238991837,-0.0972000881196913,
0.282931300033196));
#10275=CARTESIAN_POINT('Ctrl Pts',(0.122067812613842,-0.0964170744483435,
0.283001673473434));
#10276=CARTESIAN_POINT('Ctrl Pts',(0.123052722857573,-0.0951535181142867,
0.283114860599021));
#10277=CARTESIAN_POINT('Ctrl Pts',(0.123419905908483,-0.0946767733887699,
0.28315748236073));
#10278=CARTESIAN_POINT('Ctrl Pts',(0.124066097656561,-0.0938276208576194,
0.283233256203632));
#10279=CARTESIAN_POINT('Ctrl Pts',(0.12434622068369,-0.0934560667725696,
0.283266364099166));
#10280=CARTESIAN_POINT('Ctrl Pts',(0.124925538895744,-0.0926804457119648,
0.283335381670927));
#10281=CARTESIAN_POINT('Ctrl Pts',(0.125224450115931,-0.0922761744329278,
0.283371301878818));
#10282=CARTESIAN_POINT('Ctrl Pts',(0.12599375043568,-0.0912250896556484,
0.28346455983454));
#10283=CARTESIAN_POINT('Ctrl Pts',(0.126461115214211,-0.0905760919115208,
0.283522013291596));
#10284=CARTESIAN_POINT('Ctrl Pts',(0.128450954116115,-0.0877675143207924,
0.283770122406445));
#10285=CARTESIAN_POINT('Ctrl Pts',(0.129923185590691,-0.0855730590658979,
0.283962668267544));
#10286=CARTESIAN_POINT('Ctrl Pts',(0.133665161212532,-0.079676097035106,
0.2844770645729));
#10287=CARTESIAN_POINT('Ctrl Pts',(0.135836842557997,-0.0759144359912381,
0.284802220036776));
#10288=CARTESIAN_POINT('Ctrl Pts',(0.143623831697038,-0.0610196899979001,
0.286077862006308));
#10289=CARTESIAN_POINT('Ctrl Pts',(0.148049881740416,-0.0493193241638953,
0.287059743420964));
#10290=CARTESIAN_POINT('Ctrl Pts',(0.151968596788088,-0.0334165830217562,
0.288306761327306));
#10291=CARTESIAN_POINT('Ctrl Pts',(0.152761406010202,-0.0295817817380417,
0.288600668104189));
#10292=CARTESIAN_POINT('Ctrl Pts',(0.153513382011395,-0.0250967019825401,
0.288933640833726));
#10293=CARTESIAN_POINT('Ctrl Pts',(0.153614207458862,-0.0244719882861227,
0.28897977828202));
#10294=CARTESIAN_POINT('Ctrl Pts',(0.153760984325288,-0.0235258914771595,
0.289049268936782));
#10295=CARTESIAN_POINT('Ctrl Pts',(0.153809744929723,-0.0232049615462851,
0.289072774787922));
#10296=CARTESIAN_POINT('Ctrl Pts',(0.153895403157591,-0.0226290468669152,
0.289114834625351));
#10297=CARTESIAN_POINT('Ctrl Pts',(0.153932672073063,-0.0223741222631823,
0.289133409170077));
#10298=CARTESIAN_POINT('Ctrl Pts',(0.154012177092988,-0.021820694096564,
0.289173640102508));
#10299=CARTESIAN_POINT('Ctrl Pts',(0.154054178723935,-0.021522160804094,
0.289195283125781));
#10300=CARTESIAN_POINT('Ctrl Pts',(0.154169453977875,-0.0206851936174956,
0.289255802205561));
#10301=CARTESIAN_POINT('Ctrl Pts',(0.154240775493627,-0.0201464878695059,
0.289294570187238));
#10302=CARTESIAN_POINT('Ctrl Pts',(0.154644917814789,-0.0169659090896126,
0.289522432224591));
#10303=CARTESIAN_POINT('Ctrl Pts',(0.154912707033697,-0.0143160109146303,
0.289708094139946));
#10304=CARTESIAN_POINT('Ctrl Pts',(0.156210854054824,0.00295267182807369,
0.290898586001891));
#10305=CARTESIAN_POINT('Ctrl Pts',(0.155239073871537,0.0176489329047987,
0.291827839142038));
#10306=CARTESIAN_POINT('Ctrl Pts',(0.151819417137384,0.0339196315765692,
0.292944983517349));
#10307=CARTESIAN_POINT('Ctrl Pts',(0.151378059572506,0.0358379610517775,
0.293078003662129));
#10308=CARTESIAN_POINT('Ctrl Pts',(0.149942329211882,0.041577499447648,
0.293480712748644));
#10309=CARTESIAN_POINT('Ctrl Pts',(0.148838827467336,0.0453694769943925,
0.293753162661909));
#10310=CARTESIAN_POINT('Ctrl Pts',(0.14731974376163,0.0499343678096255,
0.294090949216627));
#10311=CARTESIAN_POINT('Ctrl Pts',(0.147040306983594,0.0507513158369499,
0.294151787702763));
#10312=CARTESIAN_POINT('Ctrl Pts',(0.146566229569858,0.0521005180172448,
0.294252926876222));
#10313=CARTESIAN_POINT('Ctrl Pts',(0.146375452887546,0.052634118255503,
0.294293099763111));
#10314=CARTESIAN_POINT('Ctrl Pts',(0.146024461501181,0.053599169345844,
0.294366074939678));
#10315=CARTESIAN_POINT('Ctrl Pts',(0.145865238830342,0.0540309763366914,
0.294398843952769));
#10316=CARTESIAN_POINT('Ctrl Pts',(0.145518967244312,0.0549573677624412,
0.294469400454367));
#10317=CARTESIAN_POINT('Ctrl Pts',(0.145331308507367,0.055451716420817,
0.294507207948635));
#10318=CARTESIAN_POINT('Ctrl Pts',(0.144811234732413,0.056800969658985,
0.294610832821411));
#10319=CARTESIAN_POINT('Ctrl Pts',(0.144473777195233,0.0576538940134264,
0.294676818303378));
#10320=CARTESIAN_POINT('Ctrl Pts',(0.142627136278012,0.0622032445389931,
0.295031400098233));
#10321=CARTESIAN_POINT('Ctrl Pts',(0.140983731906166,0.0658431891837452,
0.295324490298526));
#10322=CARTESIAN_POINT('Ctrl Pts',(0.132627942421066,0.0825994351494228,
0.296720070694461));
#10323=CARTESIAN_POINT('Ctrl Pts',(0.124214216050099,0.0947814562636385,
0.297881489930009));
#10324=CARTESIAN_POINT('Ctrl Pts',(0.111232668608358,0.108822867128473,
0.299342370443203));
#10325=CARTESIAN_POINT('Ctrl Pts',(0.108112950676369,0.111922838344334,
0.2996735046566));
#10326=CARTESIAN_POINT('Ctrl Pts',(0.104378960751211,0.115331129579707,
0.300043810890028));
#10327=CARTESIAN_POINT('Ctrl Pts',(0.103889337413758,0.115772373695358,
0.300091877948775));
#10328=CARTESIAN_POINT('Ctrl Pts',(0.1031535815779,0.116427003698748,0.300163361286699));
#10329=CARTESIAN_POINT('Ctrl Pts',(0.102909568127296,0.11664274249072,0.300186947363945));
#10330=CARTESIAN_POINT('Ctrl Pts',(0.102471268558987,0.117027808811723,
0.300229093287804));
#10331=CARTESIAN_POINT('Ctrl Pts',(0.102277238527927,0.117197420611471,
0.300247674063303));
#10332=CARTESIAN_POINT('Ctrl Pts',(0.10185593445929,0.117563861394978,0.300287852937023));
#10333=CARTESIAN_POINT('Ctrl Pts',(0.101628511655836,0.117760513388253,
0.300309437961563));
#10334=CARTESIAN_POINT('Ctrl Pts',(0.100991303662769,0.118308284951478,
0.300369631660898));
#10335=CARTESIAN_POINT('Ctrl Pts',(0.100580253925784,0.118657937985371,
0.300408134124878));
#10336=CARTESIAN_POINT('Ctrl Pts',(0.0981781804688915,0.12067977322723,
0.300631294968168));
#10337=CARTESIAN_POINT('Ctrl Pts',(0.0961471496060811,0.122304090499185,
0.300812684276459));
#10338=CARTESIAN_POINT('Ctrl Pts',(0.08236634025872,0.13276969477891,0.302003169420193));
#10339=CARTESIAN_POINT('Ctrl Pts',(0.069453676464604,0.139958212658715,
0.302935319667781));
#10340=CARTESIAN_POINT('Ctrl Pts',(0.0539557821117858,0.145904611552168,
0.304050541410017));
#10341=CARTESIAN_POINT('Ctrl Pts',(0.0521771960635938,0.146550066207702,
0.304178356842817));
#10342=CARTESIAN_POINT('Ctrl Pts',(0.0465718731327349,0.148469281190261,
0.304581362194133));
#10343=CARTESIAN_POINT('Ctrl Pts',(0.0427073732836244,0.149626676319463,
0.304859524558478));
#10344=CARTESIAN_POINT('Ctrl Pts',(0.03796073761188,0.150849396932931,0.305203637499376));
#10345=CARTESIAN_POINT('Ctrl Pts',(0.0371171469334411,0.151059178814054,
0.30526488485908));
#10346=CARTESIAN_POINT('Ctrl Pts',(0.0357190294658757,0.151394440539131,
0.305366562605688));
#10347=CARTESIAN_POINT('Ctrl Pts',(0.0351654858523942,0.151523972629209,
0.305406862764935));
#10348=CARTESIAN_POINT('Ctrl Pts',(0.0341624375822613,0.151752898768408,
0.305479973631794));
#10349=CARTESIAN_POINT('Ctrl Pts',(0.0337131759131925,0.151853337756109,
0.305512750476149));
#10350=CARTESIAN_POINT('Ctrl Pts',(0.03326228799292,0.151952040785781,0.305545678324688));
#10351=CARTESIAN_POINT('Ctrl Pts',(0.033261096582728,0.151952301580466,
0.305545765332291));
#10352=CARTESIAN_POINT('Ctrl Pts',(0.0332587207255954,0.151952821616339,
0.305545938839424));
#10353=CARTESIAN_POINT('Ctrl Pts',(0.0332575360529371,0.151953080907093,
0.305546025355438));
#10354=CARTESIAN_POINT('Ctrl Pts',(0.033255173324262,0.151953598011456,
0.305546197904702));
#10355=CARTESIAN_POINT('Ctrl Pts',(0.0332539952612068,0.151953855826765,
0.305546283938464));
#10356=CARTESIAN_POINT('Ctrl Pts',(0.0332516457020982,0.151954369991586,
0.305546455526842));
#10357=CARTESIAN_POINT('Ctrl Pts',(0.0332504741961427,0.151954626343423,
0.305546541082179));
#10358=CARTESIAN_POINT('Ctrl Pts',(0.0332481376978107,0.151955137593465,
0.305546711717601));
#10359=CARTESIAN_POINT('Ctrl Pts',(0.0332469726959516,0.151955392493903,
0.305546796798376));
#10360=CARTESIAN_POINT('Ctrl Pts',(0.0332446491540944,0.151955900852935,
0.305546966488444));
#10361=CARTESIAN_POINT('Ctrl Pts',(0.0332434906051759,0.151956154313635,
0.305547051098386));
#10362=CARTESIAN_POINT('Ctrl Pts',(0.0332411799101148,0.151956659806583,
0.305547219851097));
#10363=CARTESIAN_POINT('Ctrl Pts',(0.0332400277596687,0.151956911839925,
0.305547303994177));
#10364=CARTESIAN_POINT('Ctrl Pts',(0.0332377298150578,0.151957414488784,
0.305547471816552));
#10365=CARTESIAN_POINT('Ctrl Pts',(0.0332365840137241,0.151957665106021,
0.305547555496368));
#10366=CARTESIAN_POINT('Ctrl Pts',(0.0332342987097748,0.151958164935713,
0.305547722396412));
#10367=CARTESIAN_POINT('Ctrl Pts',(0.033233159203392,0.151958414149141,
0.305547805616913));
#10368=CARTESIAN_POINT('Ctrl Pts',(0.0327233048205491,0.152069914806779,
0.305585041426369));
#10369=CARTESIAN_POINT('Ctrl Pts',(0.0322140402765985,0.152178609747234,
0.305622275459916));
#10370=CARTESIAN_POINT('Ctrl Pts',(0.0308364365117833,0.152465413837663,
0.305723113685092));
#10371=CARTESIAN_POINT('Ctrl Pts',(0.0299671163995292,0.152638658627842,
0.305786871857615));
#10372=CARTESIAN_POINT('Ctrl Pts',(0.028033802189224,0.153006792148099,
0.305928963410166));
#10373=CARTESIAN_POINT('Ctrl Pts',(0.0269691689366109,0.153198029770798,
0.306007409271551));
#10374=CARTESIAN_POINT('Ctrl Pts',(0.0237278501052427,0.153745426894165,
0.306246882292746));
#10375=CARTESIAN_POINT('Ctrl Pts',(0.0215455896880002,0.154066394179012,
0.306408991000768));
#10376=CARTESIAN_POINT('Ctrl Pts',(0.0044431140174602,0.156211377083595,
0.307686718837038));
#10377=CARTESIAN_POINT('Ctrl Pts',(-0.0106621158301532,0.155909861711717,
0.308869548094476));
#10378=CARTESIAN_POINT('Ctrl Pts',(-0.026345427090253,0.153305194294345,
0.310087247990286));
#10379=CARTESIAN_POINT('Ctrl Pts',(-0.0272051420288109,0.153154968647471,
0.310153928453098));
#10380=CARTESIAN_POINT('Ctrl Pts',(-0.0288359658101667,0.152855834886191,
0.310280234987703));
#10381=CARTESIAN_POINT('Ctrl Pts',(-0.0296073003428357,0.152708306881315,
0.310339896785407));
#10382=CARTESIAN_POINT('Ctrl Pts',(-0.0335717377101413,0.151918888434002,
0.310646042062632));
#10383=CARTESIAN_POINT('Ctrl Pts',(-0.0367455246038526,0.151182606979643,
0.310889473506111));
#10384=CARTESIAN_POINT('Ctrl Pts',(-0.0404250154250893,0.150206265884471,
0.311168015035298));
#10385=CARTESIAN_POINT('Ctrl Pts',(-0.0409551614627046,0.150062583467118,
0.311208057133632));
#10386=CARTESIAN_POINT('Ctrl Pts',(-0.0418050735753087,0.149827397122019,
0.311272093664716));
#10387=CARTESIAN_POINT('Ctrl Pts',(-0.0421253201090561,0.149737672335052,
0.311296186562792));
#10388=CARTESIAN_POINT('Ctrl Pts',(-0.0426943871336672,0.149576264339099,
0.311338931666725));
#10389=CARTESIAN_POINT('Ctrl Pts',(-0.0429433188117957,0.149504986270929,
0.311357606982288));
#10390=CARTESIAN_POINT('Ctrl Pts',(-0.0434730621661568,0.149351869471086,
0.31139729944714));
#10391=CARTESIAN_POINT('Ctrl Pts',(-0.0437538207588134,0.149269860392073,
0.311418306509449));
#10392=CARTESIAN_POINT('Ctrl Pts',(-0.0445163297165142,0.149044796729112,
0.311475283258547));
#10393=CARTESIAN_POINT('Ctrl Pts',(-0.0449976265962869,0.148900196987338,
0.311511164377631));
#10394=CARTESIAN_POINT('Ctrl Pts',(-0.0474112023001512,0.14816229631183,
0.311690722839279));
#10395=CARTESIAN_POINT('Ctrl Pts',(-0.0493326039622012,0.147533668668207,
0.311832453904321));
#10396=CARTESIAN_POINT('Ctrl Pts',(-0.0549178007752948,0.145585024772356,
0.312242392109044));
#10397=CARTESIAN_POINT('Ctrl Pts',(-0.0585451262568406,0.14416461936081,
0.312506024919305));
#10398=CARTESIAN_POINT('Ctrl Pts',(-0.0626412936682278,0.142380474849873,
0.312804839115273));
#10399=CARTESIAN_POINT('Ctrl Pts',(-0.0631656457855339,0.142148627458991,
0.312843111303748));
#10400=CARTESIAN_POINT('Ctrl Pts',(-0.0636886270244494,0.14191392210682,
0.31288131537517));
#10401=CARTESIAN_POINT('Origin',(0.,0.,-0.129405622560373));
#10402=CARTESIAN_POINT('',(-0.0636886207929056,0.141913924903434,0.396608754846595));
#10403=CARTESIAN_POINT('',(-0.0636886258329921,0.141913922641526,0.382796071549385));
#10404=CARTESIAN_POINT('',(-0.0636886258329924,0.141913922641526,-0.129405622560373));
#10405=CARTESIAN_POINT('Ctrl Pts',(-0.0636886207929056,0.141913924903434,
0.396608754846595));
#10406=CARTESIAN_POINT('Ctrl Pts',(-0.0591354711488871,0.143957303108135,
0.396280149747421));
#10407=CARTESIAN_POINT('Ctrl Pts',(-0.0544854027433177,0.145780922739278,
0.395950672078547));
#10408=CARTESIAN_POINT('Ctrl Pts',(-0.0458237033067888,0.148705081971013,
0.395338079499676));
#10409=CARTESIAN_POINT('Ctrl Pts',(-0.0418418461088594,0.149874176190154,
0.395056901137322));
#10410=CARTESIAN_POINT('Ctrl Pts',(-0.0353378727723009,0.151504376525937,
0.394594616688936));
#10411=CARTESIAN_POINT('Ctrl Pts',(-0.0328426610223724,0.152064787711378,
0.394416579065734));
#10412=CARTESIAN_POINT('Ctrl Pts',(-0.0295595151424556,0.152717590803652,
0.394180923169887));
#10413=CARTESIAN_POINT('Ctrl Pts',(-0.0287829885131883,0.152865846437844,
0.394125085341324));
#10414=CARTESIAN_POINT('Ctrl Pts',(-0.0275127108832061,0.153098347777723,
0.394033564052576));
#10415=CARTESIAN_POINT('Ctrl Pts',(-0.0270196162337983,0.153186140627323,
0.393997993485945));
#10416=CARTESIAN_POINT('Ctrl Pts',(-0.0260667273767181,0.153351053398406,
0.393929165705241));
#10417=CARTESIAN_POINT('Ctrl Pts',(-0.0256069929010297,0.153428490706252,
0.39389591894561));
#10418=CARTESIAN_POINT('Ctrl Pts',(-0.0245481922785319,0.153601942869539,
0.393819254137818));
#10419=CARTESIAN_POINT('Ctrl Pts',(-0.0239489019942723,0.153696521338003,
0.393775791177357));
#10420=CARTESIAN_POINT('Ctrl Pts',(-0.0223436573269114,0.153940240538981,
0.39365917685131));
#10421=CARTESIAN_POINT('Ctrl Pts',(-0.0213367831270878,0.154083023965586,
0.393585826435465));
#10422=CARTESIAN_POINT('Ctrl Pts',(-0.0129940613902414,0.155182753992489,
0.392976266209449));
#10423=CARTESIAN_POINT('Ctrl Pts',(-0.00560113016398566,0.155624958516443,
0.392423930633981));
#10424=CARTESIAN_POINT('Ctrl Pts',(0.0117238713532809,0.155425111399385,
0.391101724465564));
#10425=CARTESIAN_POINT('Ctrl Pts',(0.0216195989182905,0.154359927374671,
0.390324268914821));
#10426=CARTESIAN_POINT('Ctrl Pts',(0.0349944030782908,0.151608292096276,
0.389275222631333));
#10427=CARTESIAN_POINT('Ctrl Pts',(0.038615707523504,0.1507266198929,0.388991622031633));
#10428=CARTESIAN_POINT('Ctrl Pts',(0.0434601339677926,0.149361064610111,
0.388615587028682));
#10429=CARTESIAN_POINT('Ctrl Pts',(0.0447136869116124,0.148990594827376,
0.388518595072565));
#10430=CARTESIAN_POINT('Ctrl Pts',(0.0465613753970196,0.14841911541535,
0.3883762392744));
#10431=CARTESIAN_POINT('Ctrl Pts',(0.0471591677446034,0.148230254778108,
0.388330276870934));
#10432=CARTESIAN_POINT('Ctrl Pts',(0.0482397725726555,0.147881660224996,
0.388247384344753));
#10433=CARTESIAN_POINT('Ctrl Pts',(0.0487229709107621,0.147723164107304,
0.388210388325363));
#10434=CARTESIAN_POINT('Ctrl Pts',(0.0494822059590996,0.147469993352559,
0.38815237704341));
#10435=CARTESIAN_POINT('Ctrl Pts',(0.0497587624318069,0.14737690867659,
0.388131271075488));
#10436=CARTESIAN_POINT('Ctrl Pts',(0.0502718638027505,0.147202597661875,
0.388092161343756));
#10437=CARTESIAN_POINT('Ctrl Pts',(0.0505084722090288,0.14712157994426,
0.388074146029746));
#10438=CARTESIAN_POINT('Ctrl Pts',(0.0510528421066504,0.146933712749406,
0.388032741750722));
#10439=CARTESIAN_POINT('Ctrl Pts',(0.0513604636238838,0.146826466997955,
0.388009376481895));
#10440=CARTESIAN_POINT('Ctrl Pts',(0.0522894613393386,0.146499314649221,
0.387938905543215));
#10441=CARTESIAN_POINT('Ctrl Pts',(0.0529097898187304,0.146276420323115,
0.387891972268997));
#10442=CARTESIAN_POINT('Ctrl Pts',(0.0576761658799279,0.144529493735014,
0.387532164477043));
#10443=CARTESIAN_POINT('Ctrl Pts',(0.0617574983698718,0.142833242585835,
0.387228790084258));
#10444=CARTESIAN_POINT('Ctrl Pts',(0.0791557975828898,0.134716788601274,
0.385933130595585));
#10445=CARTESIAN_POINT('Ctrl Pts',(0.0915912323790402,0.126591264585131,
0.38499336037026));
#10446=CARTESIAN_POINT('Ctrl Pts',(0.105644319033502,0.114238842820077,
0.383718880371709));
#10447=CARTESIAN_POINT('Ctrl Pts',(0.108495410459469,0.111534643764521,
0.383447582577348));
#10448=CARTESIAN_POINT('Ctrl Pts',(0.111879032373547,0.108072744340735,
0.383107465105336));
#10449=CARTESIAN_POINT('Ctrl Pts',(0.112511380428234,0.107414268907066,
0.383043079009707));
#10450=CARTESIAN_POINT('Ctrl Pts',(0.113500187767364,0.106366294398961,
0.382941064096871));
#10451=CARTESIAN_POINT('Ctrl Pts',(0.113860530570887,0.105980473545882,
0.382903602412488));
#10452=CARTESIAN_POINT('Ctrl Pts',(0.114531483318713,0.105254709461171,
0.382833307733877));
#10453=CARTESIAN_POINT('Ctrl Pts',(0.114842562251683,0.104915205866627,
0.382800495180288));
#10454=CARTESIAN_POINT('Ctrl Pts',(0.115534144312808,0.104153669596703,
0.382727047060551));
#10455=CARTESIAN_POINT('Ctrl Pts',(0.11591384986254,0.103730924929615,0.382686378554194));
#10456=CARTESIAN_POINT('Ctrl Pts',(0.116867775723354,0.1026570949005,0.382583330106278));
#10457=CARTESIAN_POINT('Ctrl Pts',(0.117438871039729,0.102003272732052,
0.382520821486495));
#10458=CARTESIAN_POINT('Ctrl Pts',(0.120619165552353,0.0983001796953169,
0.382168051212617));
#10459=CARTESIAN_POINT('Ctrl Pts',(0.123114830981151,0.0951558791407954,
0.38187322304819));
#10460=CARTESIAN_POINT('Ctrl Pts',(0.126614192964098,0.0903786144783409,
0.381431511679175));
#10461=CARTESIAN_POINT('Ctrl Pts',(0.127713938225963,0.0888177756493666,
0.381288134440068));
#10462=CARTESIAN_POINT('Ctrl Pts',(0.137038856553683,0.0750517793050917,
0.38003187667353));
#10463=CARTESIAN_POINT('Ctrl Pts',(0.143520768099879,0.0617586354025572,
0.378864732072268));
#10464=CARTESIAN_POINT('Ctrl Pts',(0.148834886832389,0.0452847731455561,
0.377562543551511));
#10465=CARTESIAN_POINT('Ctrl Pts',(0.14956957840972,0.042795765935048,0.377369697281248));
#10466=CARTESIAN_POINT('Ctrl Pts',(0.150381423032445,0.0397683426615026,
0.377140725561483));
#10467=CARTESIAN_POINT('Ctrl Pts',(0.150518430487696,0.0392465995726382,
0.377101463617054));
#10468=CARTESIAN_POINT('Ctrl Pts',(0.150727573656063,0.0384329472951513,
0.377040555362658));
#10469=CARTESIAN_POINT('Ctrl Pts',(0.150801580000325,0.0381415307981588,
0.377018804356258));
#10470=CARTESIAN_POINT('Ctrl Pts',(0.150937473850377,0.037599839789361,
0.376978493872609));
#10471=CARTESIAN_POINT('Ctrl Pts',(0.150999583502159,0.0373496284927104,
0.376959922169652));
#10472=CARTESIAN_POINT('Ctrl Pts',(0.151138808317416,0.036782731709718,
0.376917952452996));
#10473=CARTESIAN_POINT('Ctrl Pts',(0.151215550232206,0.036465958164934,
0.376894576075642));
#10474=CARTESIAN_POINT('Ctrl Pts',(0.151444657814457,0.0355070923864214,
0.376824038504343));
#10475=CARTESIAN_POINT('Ctrl Pts',(0.151593936325631,0.0348642582177862,
0.376777050186271));
#10476=CARTESIAN_POINT('Ctrl Pts',(0.152710636894445,0.0299126276891752,
0.376417279520102));
#10477=CARTESIAN_POINT('Ctrl Pts',(0.153498377268147,0.0255648431689894,
0.376113990227377));
#10478=CARTESIAN_POINT('Ctrl Pts',(0.156113409732975,0.00654659047186478,
0.374818410627166));
#10479=CARTESIAN_POINT('Ctrl Pts',(0.156029742918761,-0.00830798203150761,
0.373878638037471));
#10480=CARTESIAN_POINT('Ctrl Pts',(0.153271835687203,-0.026813789611275,
0.37260415857605));
#10481=CARTESIAN_POINT('Ctrl Pts',(0.152545846269266,-0.030675645257038,
0.372332864431312));
#10482=CARTESIAN_POINT('Ctrl Pts',(0.151472018559481,-0.0353958124737809,
0.371992751005912));
#10483=CARTESIAN_POINT('Ctrl Pts',(0.151261673780469,-0.0362841829013968,
0.371928365178482));
#10484=CARTESIAN_POINT('Ctrl Pts',(0.150917370453587,-0.0376832655415541,
0.371826350594796));
#10485=CARTESIAN_POINT('Ctrl Pts',(0.150788608228567,-0.0381952460718942,
0.371788888969522));
#10486=CARTESIAN_POINT('Ctrl Pts',(0.150542661134858,-0.0391525441504082,
0.371718594343923));
#10487=CARTESIAN_POINT('Ctrl Pts',(0.15042609996145,-0.0395980173371105,
0.371685781783945));
#10488=CARTESIAN_POINT('Ctrl Pts',(0.150161283275421,-0.0405920484693481,
0.371612333574844));
#10489=CARTESIAN_POINT('Ctrl Pts',(0.150011997028421,-0.0411403223803712,
0.371571664985144));
#10490=CARTESIAN_POINT('Ctrl Pts',(0.149627052085371,-0.0425241275821229,
0.371468616185309));
#10491=CARTESIAN_POINT('Ctrl Pts',(0.149387399268055,-0.0433585173351884,
0.371406107295415));
#10492=CARTESIAN_POINT('Ctrl Pts',(0.148000631683482,-0.048038753995225,
0.371053332793077));
#10493=CARTESIAN_POINT('Ctrl Pts',(0.146712102408559,-0.0518407406068074,
0.370758500542132));
#10494=CARTESIAN_POINT('Ctrl Pts',(0.144595845262558,-0.0573715012970494,
0.370316788560117));
#10495=CARTESIAN_POINT('Ctrl Pts',(0.143880807506569,-0.059141866161648,
0.370173414957269));
#10496=CARTESIAN_POINT('Ctrl Pts',(0.137371268870141,-0.0744416097236432,
0.36891715825066));
#10497=CARTESIAN_POINT('Ctrl Pts',(0.129717303886049,-0.0870962799570504,
0.36775001080692));
#10498=CARTESIAN_POINT('Ctrl Pts',(0.118757648883784,-0.100494551256526,
0.366447823457123));
#10499=CARTESIAN_POINT('Ctrl Pts',(0.117064812744389,-0.102461533113913,
0.366254980351734));
#10500=CARTESIAN_POINT('Ctrl Pts',(0.114961440124734,-0.104785307906241,
0.366026011882111));
#10501=CARTESIAN_POINT('Ctrl Pts',(0.114597368278322,-0.10518334789989,
0.365986750124842));
#10502=CARTESIAN_POINT('Ctrl Pts',(0.114027151715282,-0.105800290970308,
0.365925842097099));
#10503=CARTESIAN_POINT('Ctrl Pts',(0.11382243533742,-0.106020498563939,
0.365904091131427));
#10504=CARTESIAN_POINT('Ctrl Pts',(0.113440997979261,-0.106428421683388,
0.36586378068468));
#10505=CARTESIAN_POINT('Ctrl Pts',(0.113264450574062,-0.106616289574125,
0.3658452089781));
#10506=CARTESIAN_POINT('Ctrl Pts',(0.112863640692477,-0.107040680779638,
0.365803239204184));
#10507=CARTESIAN_POINT('Ctrl Pts',(0.112639101822718,-0.107276938239204,
0.36577986277344));
#10508=CARTESIAN_POINT('Ctrl Pts',(0.111957697656428,-0.107989406567054,
0.365709324881809));
#10509=CARTESIAN_POINT('Ctrl Pts',(0.111498534867578,-0.108463425905312,
0.365662336299106));
#10510=CARTESIAN_POINT('Ctrl Pts',(0.107943644453324,-0.112086906195201,
0.365302557353279));
#10511=CARTESIAN_POINT('Ctrl Pts',(0.104717715343248,-0.115106533812928,
0.364999260539068));
#10512=CARTESIAN_POINT('Ctrl Pts',(0.0901563580736357,-0.127616971474278,
0.363703661381624));
#10513=CARTESIAN_POINT('Ctrl Pts',(0.0776299566863628,-0.135601986811538,
0.362763876658843));
#10514=CARTESIAN_POINT('Ctrl Pts',(0.0605858387280864,-0.143319883110265,
0.361489399953024));
#10515=CARTESIAN_POINT('Ctrl Pts',(0.0569476690540846,-0.144803975211418,
0.361218124536059));
#10516=CARTESIAN_POINT('Ctrl Pts',(0.0523997468572953,-0.146461266007262,
0.360878031875576));
#10517=CARTESIAN_POINT('Ctrl Pts',(0.0515392906741986,-0.146766267801874,
0.360813647424466));
#10518=CARTESIAN_POINT('Ctrl Pts',(0.0501770952732396,-0.147235662500156,
0.360711634529874));
#10519=CARTESIAN_POINT('Ctrl Pts',(0.0496771081464612,-0.147405108851847,
0.360674173207941));
#10520=CARTESIAN_POINT('Ctrl Pts',(0.0487394178499021,-0.147717580819097,
0.360603878854384));
#10521=CARTESIAN_POINT('Ctrl Pts',(0.0483019221113363,-0.147861214817721,
0.360571066261615));
#10522=CARTESIAN_POINT('Ctrl Pts',(0.0473231264180402,-0.148177755100382,
0.360497617593915));
#10523=CARTESIAN_POINT('Ctrl Pts',(0.046781506150068,-0.148349641277132,
0.360456948576507));
#10524=CARTESIAN_POINT('Ctrl Pts',(0.0454100613849526,-0.148776619468472,
0.36035389797066));
#10525=CARTESIAN_POINT('Ctrl Pts',(0.0445790300259477,-0.149027736346607,
0.360291387694576));
#10526=CARTESIAN_POINT('Ctrl Pts',(0.0398943925850023,-0.150400626825541,
0.359938591491321));
#10527=CARTESIAN_POINT('Ctrl Pts',(0.0360009469321137,-0.151379778847063,
0.359643738267843));
#10528=CARTESIAN_POINT('Ctrl Pts',(0.0302063665586847,-0.152600858744321,
0.359202023139442));
#10529=CARTESIAN_POINT('Ctrl Pts',(0.028331402036626,-0.152960052963473,
0.359058668197927));
#10530=CARTESIAN_POINT('Ctrl Pts',(0.0119466540993918,-0.155787359212479,
0.357802416928715));
#10531=CARTESIAN_POINT('Ctrl Pts',(-0.00283654316817243,-0.156218756873579,
0.356635254894959));
#10532=CARTESIAN_POINT('Ctrl Pts',(-0.0200368803470148,-0.154275909703786,
0.355333073554957));
#10533=CARTESIAN_POINT('Ctrl Pts',(-0.0226073099168896,-0.153920253953389,
0.355140246693816));
#10534=CARTESIAN_POINT('Ctrl Pts',(-0.0257001295377401,-0.15341315718086,
0.354911294906176));
#10535=CARTESIAN_POINT('Ctrl Pts',(-0.026231977268921,-0.153323112563649,
0.354872034109604));
#10536=CARTESIAN_POINT('Ctrl Pts',(-0.0270595319050074,-0.153178571050486,
0.354811127245268));
#10537=CARTESIAN_POINT('Ctrl Pts',(-0.0273555602952314,-0.153125981535161,
0.354789376488655));
#10538=CARTESIAN_POINT('Ctrl Pts',(-0.027905139099566,-0.153026704128821,
0.354749066231342));
#10539=CARTESIAN_POINT('Ctrl Pts',(-0.0281587234021228,-0.152980244681817,
0.354730494506161));
#10540=CARTESIAN_POINT('Ctrl Pts',(-0.0287326505477795,-0.152873619461138,
0.354688524438306));
#10541=CARTESIAN_POINT('Ctrl Pts',(-0.0290529198960198,-0.152813077272343,
0.354665147733501));
#10542=CARTESIAN_POINT('Ctrl Pts',(-0.0300210675994438,-0.152626909556827,
0.354594608197535));
#10543=CARTESIAN_POINT('Ctrl Pts',(-0.0306683504579261,-0.152498165045919,
0.354547618256416));
#10544=CARTESIAN_POINT('Ctrl Pts',(-0.0356411192274561,-0.151476138995254,
0.354187796801346));
#10545=CARTESIAN_POINT('Ctrl Pts',(-0.0399281132623178,-0.150403008460899,
0.353884461370454));
#10546=CARTESIAN_POINT('Ctrl Pts',(-0.058337109069451,-0.144951963177837,
0.352588761758896));
#10547=CARTESIAN_POINT('Ctrl Pts',(-0.0718396701616462,-0.138756622887168,
0.3516489147026));
#10548=CARTESIAN_POINT('Ctrl Pts',(-0.087566179370972,-0.128621093876159,
0.350374452128954));
#10549=CARTESIAN_POINT('Ctrl Pts',(-0.0907847952954962,-0.12636984611009,
0.35010327289934));
#10550=CARTESIAN_POINT('Ctrl Pts',(-0.0946422495902132,-0.12344829005988,
0.349763286890065));
#10551=CARTESIAN_POINT('Ctrl Pts',(-0.0953650344051116,-0.122890788408527,
0.349698909509598));
#10552=CARTESIAN_POINT('Ctrl Pts',(-0.096498005842365,-0.122000885434624,
0.349596905292492));
#10553=CARTESIAN_POINT('Ctrl Pts',(-0.0969114873115889,-0.121672695346751,
0.349559445528945));
#10554=CARTESIAN_POINT('Ctrl Pts',(-0.0976824958721955,-0.121054304085085,
0.349489152572844));
#10555=CARTESIAN_POINT('Ctrl Pts',(-0.0980404214898577,-0.120764606913884,
0.349456339811474));
#10556=CARTESIAN_POINT('Ctrl Pts',(-0.0988371794682913,-0.120113851781497,
0.3493828887871));
#10557=CARTESIAN_POINT('Ctrl Pts',(-0.0992753282308914,-0.119751971273283,
0.349342217571856));
#10558=CARTESIAN_POINT('Ctrl Pts',(-0.100377872324346,-0.118831136883617,
0.34923915768544));
#10559=CARTESIAN_POINT('Ctrl Pts',(-0.101039581340861,-0.118269012387253,
0.349176640286103));
#10560=CARTESIAN_POINT('Ctrl Pts',(-0.10473459587014,-0.115076440155669,
0.348823732547575));
#10561=CARTESIAN_POINT('Ctrl Pts',(-0.107669601004868,-0.1123350977175,
0.348528771530388));
#10562=CARTESIAN_POINT('Ctrl Pts',(-0.111837779702478,-0.108128408754094,
0.348087040218821));
#10563=CARTESIAN_POINT('Ctrl Pts',(-0.113155403896522,-0.106748750776543,
0.347943781180044));
#10564=CARTESIAN_POINT('Ctrl Pts',(-0.124415590152557,-0.0945156644537806,
0.346687557766949));
#10565=CARTESIAN_POINT('Ctrl Pts',(-0.132794930127446,-0.0823278724373318,
0.345520320657869));
#10566=CARTESIAN_POINT('Ctrl Pts',(-0.14048939314704,-0.0668225828946814,
0.344218170218855));
#10567=CARTESIAN_POINT('Ctrl Pts',(-0.141583953763048,-0.0644710272572081,
0.344025426923031));
#10568=CARTESIAN_POINT('Ctrl Pts',(-0.142834574585835,-0.0615985201508543,
0.343796560954731));
#10569=CARTESIAN_POINT('Ctrl Pts',(-0.143047299183293,-0.0611028935602491,
0.343757305101806));
#10570=CARTESIAN_POINT('Ctrl Pts',(-0.143374584429493,-0.0603292750398509,
0.343696404224281));
#10571=CARTESIAN_POINT('Ctrl Pts',(-0.143490921431259,-0.0600520470771563,
0.343674654543487));
#10572=CARTESIAN_POINT('Ctrl Pts',(-0.143705525649564,-0.0595364666674289,
0.343634345260886));
#10573=CARTESIAN_POINT('Ctrl Pts',(-0.143804003096175,-0.0592982095920591,
0.343615773439877));
#10574=CARTESIAN_POINT('Ctrl Pts',(-0.144025650315872,-0.05875815516773,
0.343573801858931));
#10575=CARTESIAN_POINT('Ctrl Pts',(-0.144148463861312,-0.0584562154037349,
0.343550423743441));
#10576=CARTESIAN_POINT('Ctrl Pts',(-0.144517090990275,-0.0575417115089637,
0.343479875743202));
#10577=CARTESIAN_POINT('Ctrl Pts',(-0.144759960019966,-0.0569279559462022,
0.34343287880955));
#10578=CARTESIAN_POINT('Ctrl Pts',(-0.146598967263648,-0.0521927139463801,
0.343072838336293));
#10579=CARTESIAN_POINT('Ctrl Pts',(-0.148022884216022,-0.0480059524947524,
0.342769303942075));
#10580=CARTESIAN_POINT('Ctrl Pts',(-0.153426818966979,-0.0295745516656521,
0.341473085969551));
#10581=CARTESIAN_POINT('Ctrl Pts',(-0.15554270412961,-0.0148646774897879,
0.34053291696168));
#10582=CARTESIAN_POINT('Ctrl Pts',(-0.155551875192911,0.00377240964231844,
0.339263323416171));
#10583=CARTESIAN_POINT('Ctrl Pts',(-0.155410911248689,0.00761980084480383,
0.338997568250853));
#10584=CARTESIAN_POINT('Ctrl Pts',(-0.15505820770871,0.0123950842303167,
0.338661337111921));
#10585=CARTESIAN_POINT('Ctrl Pts',(-0.154980483131377,0.013331754203132,
0.338595081553473));
#10586=CARTESIAN_POINT('Ctrl Pts',(-0.154844793031477,0.0148048509162445,
0.338490377958999));
#10587=CARTESIAN_POINT('Ctrl Pts',(-0.154792515958477,0.0153417902974159,
0.338452108308192));
#10588=CARTESIAN_POINT('Ctrl Pts',(-0.154695208360985,0.0162900653490015,
0.338384329994491));
#10589=CARTESIAN_POINT('Ctrl Pts',(-0.154651327425278,0.016701516052533,
0.338354857695168));
#10590=CARTESIAN_POINT('Ctrl Pts',(-0.154546920691025,0.0176447809281248,
0.338287142703986));
#10591=CARTESIAN_POINT('Ctrl Pts',(-0.154485290872378,0.0181764650009163,
0.338248865662852));
#10592=CARTESIAN_POINT('Ctrl Pts',(-0.154307104528458,0.0196472781321917,
0.338142671966467));
#10593=CARTESIAN_POINT('Ctrl Pts',(-0.154184721716883,0.0205856639802072,
0.338074573047169));
#10594=CARTESIAN_POINT('Ctrl Pts',(-0.153440237542671,0.0259144459705404,
0.337685828332761));
#10595=CARTESIAN_POINT('Ctrl Pts',(-0.152639249564241,0.0302773369576339,
0.337359596198671));
#10596=CARTESIAN_POINT('Ctrl Pts',(-0.14948715934694,0.0440931945675072,
0.336299659137388));
#10597=CARTESIAN_POINT('Ctrl Pts',(-0.146434817648429,0.0533611876740401,
0.335546078973155));
#10598=CARTESIAN_POINT('Ctrl Pts',(-0.139000414404946,0.0703754381062482,
0.334106366647411));
#10599=CARTESIAN_POINT('Ctrl Pts',(-0.134780408387858,0.0781543454835109,
0.333423529591988));
#10600=CARTESIAN_POINT('Ctrl Pts',(-0.129542511915241,0.0861104924450523,
0.332725362760499));
#10601=CARTESIAN_POINT('Ctrl Pts',(-0.129158969563395,0.0866847156743254,
0.332674980489749));
#10602=CARTESIAN_POINT('Ctrl Pts',(-0.128585372740147,0.0875312209319739,
0.33260074047546));
#10603=CARTESIAN_POINT('Ctrl Pts',(-0.12839825715358,0.0878054684292402,
0.33257669354251));
#10604=CARTESIAN_POINT('Ctrl Pts',(-0.128063985103896,0.0882920435464803,
0.332534041000714));
#10605=CARTESIAN_POINT('Ctrl Pts',(-0.127917176729224,0.0885046051669697,
0.332515412364162));
#10606=CARTESIAN_POINT('Ctrl Pts',(-0.127600752928645,0.0889603183435611,
0.332475483909656));
#10607=CARTESIAN_POINT('Ctrl Pts',(-0.127430972153441,0.089203350429118,
0.332454195625835));
#10608=CARTESIAN_POINT('Ctrl Pts',(-0.126961342157553,0.0898715235608675,
0.332395678200694));
#10609=CARTESIAN_POINT('Ctrl Pts',(-0.126660049537383,0.0902956533920446,
0.33235854585871));
#10610=CARTESIAN_POINT('Ctrl Pts',(-0.125014424034513,0.0925877571447012,
0.332157891703847));
#10611=CARTESIAN_POINT('Ctrl Pts',(-0.123630797913218,0.0944273600073881,
0.331996915939853));
#10612=CARTESIAN_POINT('Ctrl Pts',(-0.113344052392295,0.107490180992172,
0.330848798709652));
#10613=CARTESIAN_POINT('Ctrl Pts',(-0.102968214487035,0.117467748648099,
0.329938812661447));
#10614=CARTESIAN_POINT('Ctrl Pts',(-0.0889586129320677,0.127636435131847,
0.328780496157874));
#10615=CARTESIAN_POINT('Ctrl Pts',(-0.0864956177248851,0.129318215944089,
0.328579379734413));
#10616=CARTESIAN_POINT('Ctrl Pts',(-0.0808705594660266,0.132926498929271,
0.328123569780184));
#10617=CARTESIAN_POINT('Ctrl Pts',(-0.0776851114311599,0.134812911772795,
0.327867795298827));
#10618=CARTESIAN_POINT('Ctrl Pts',(-0.0736212035253429,0.137027665775012,
0.327542742600306));
#10619=CARTESIAN_POINT('Ctrl Pts',(-0.0728028370025879,0.137464212266892,
0.327477349763916));
#10620=CARTESIAN_POINT('Ctrl Pts',(-0.0715049029263191,0.138141736426061,
0.327373713428127));
#10621=CARTESIAN_POINT('Ctrl Pts',(-0.0710278985778237,0.138387600946786,
0.327335642300027));
#10622=CARTESIAN_POINT('Ctrl Pts',(-0.0701437110260563,0.138837566073509,
0.327265097861832));
#10623=CARTESIAN_POINT('Ctrl Pts',(-0.0697368838007441,0.139042356781615,
0.327232649157847));
#10624=CARTESIAN_POINT('Ctrl Pts',(-0.0688320734181299,0.139492854751347,
0.327160499505217));
#10625=CARTESIAN_POINT('Ctrl Pts',(-0.0683336641663858,0.139737687058772,
0.327120768594766));
#10626=CARTESIAN_POINT('Ctrl Pts',(-0.0668984475443242,0.140433190254196,
0.327006387841378));
#10627=CARTESIAN_POINT('Ctrl Pts',(-0.0659584350150779,0.140877137824565,
0.326931506862302));
#10628=CARTESIAN_POINT('Ctrl Pts',(-0.0645731589023019,0.141514469913206,
0.326821186335112));
#10629=CARTESIAN_POINT('Ctrl Pts',(-0.0641313410607403,0.141715239356901,
0.326786005352217));
#10630=CARTESIAN_POINT('Ctrl Pts',(-0.0636886254453755,0.141913922815482,
0.326750756222096));
#10631=CARTESIAN_POINT('',(-0.155549941519498,0.000134882470554111,0.325594377439629));
#10632=CARTESIAN_POINT('Ctrl Pts',(-0.0636886270244492,0.14191392210682,
0.31288131537517));
#10633=CARTESIAN_POINT('Ctrl Pts',(-0.0738457763258268,0.137355561067371,
0.313623300801195));
#10634=CARTESIAN_POINT('Ctrl Pts',(-0.0834857012421142,0.1317192952549,
0.314342086516591));
#10635=CARTESIAN_POINT('Ctrl Pts',(-0.0968652474729675,0.121832535428259,
0.315461554910601));
#10636=CARTESIAN_POINT('Ctrl Pts',(-0.101111003997252,0.118332566954402,
0.315837738301656));
#10637=CARTESIAN_POINT('Ctrl Pts',(-0.105865281244906,0.113970413452104,
0.316290101255649));
#10638=CARTESIAN_POINT('Ctrl Pts',(-0.106562377892366,0.113318897195196,
0.316357260196019));
#10639=CARTESIAN_POINT('Ctrl Pts',(-0.107683980767327,0.112251129959869,
0.316466704596343));
#10640=CARTESIAN_POINT('Ctrl Pts',(-0.108112179851629,0.111838778789471,
0.316508822519532));
#10641=CARTESIAN_POINT('Ctrl Pts',(-0.108869604911422,0.111100971770551,
0.316583928744778));
#10642=CARTESIAN_POINT('Ctrl Pts',(-0.109199763457013,0.110776479698431,
0.316616874810544));
#10643=CARTESIAN_POINT('Ctrl Pts',(-0.109834725548014,0.1101468183604,0.316680642564838));
#10644=CARTESIAN_POINT('Ctrl Pts',(-0.110139718372898,0.109841845218271,
0.316711455435337));
#10645=CARTESIAN_POINT('Ctrl Pts',(-0.110949479491181,0.109025372840118,
0.316793757617018));
#10646=CARTESIAN_POINT('Ctrl Pts',(-0.111451972970211,0.108511642744849,
0.316845345886176));
#10647=CARTESIAN_POINT('Ctrl Pts',(-0.113402359182437,0.106489803286914,
0.317047631907775));
#10648=CARTESIAN_POINT('Ctrl Pts',(-0.114823286229012,0.104956111877036,
0.317199480043754));
#10649=CARTESIAN_POINT('Ctrl Pts',(-0.118328635821682,0.101016180364589,
0.317585822048543));
#10650=CARTESIAN_POINT('Ctrl Pts',(-0.120370815262059,0.0985738248010755,
0.317821949653995));
#10651=CARTESIAN_POINT('Ctrl Pts',(-0.126103629237698,0.0912736544734109,
0.318518332383104));
#10652=CARTESIAN_POINT('Ctrl Pts',(-0.129584964943485,0.0862596582650869,
0.318985314453582));
#10653=CARTESIAN_POINT('Ctrl Pts',(-0.138706886644305,0.0713185072492202,
0.320338306441304));
#10654=CARTESIAN_POINT('Ctrl Pts',(-0.143562443411091,0.0609573245357439,
0.321233351895657));
#10655=CARTESIAN_POINT('Ctrl Pts',(-0.147600249513271,0.0491040492620575,
0.322158377065807));
#10656=CARTESIAN_POINT('Ctrl Pts',(-0.147947841727943,0.048046619336895,
0.322240048576568));
#10657=CARTESIAN_POINT('Ctrl Pts',(-0.148409540769718,0.046589518786747,
0.322351341330326));
#10658=CARTESIAN_POINT('Ctrl Pts',(-0.148533430148211,0.0461930210253136,
0.322381499554538));
#10659=CARTESIAN_POINT('Ctrl Pts',(-0.148728143983151,0.0455609721252862,
0.322429368423441));
#10660=CARTESIAN_POINT('Ctrl Pts',(-0.148799999445464,0.0453257450133406,
0.322447138344701));
#10661=CARTESIAN_POINT('Ctrl Pts',(-0.148947533565676,0.0448386430564463,
0.322483840851225));
#10662=CARTESIAN_POINT('Ctrl Pts',(-0.149023131458458,0.0445867464390801,
0.322502768284357));
#10663=CARTESIAN_POINT('Ctrl Pts',(-0.149202137990535,0.0439847448979742,
0.322547879271261));
#10664=CARTESIAN_POINT('Ctrl Pts',(-0.14930495462334,0.0436344622627188,
0.322574028439805));
#10665=CARTESIAN_POINT('Ctrl Pts',(-0.149520379158446,0.042890862529187,
0.322629335570863));
#10666=CARTESIAN_POINT('Ctrl Pts',(-0.149632670740083,0.0424974555624741,
0.322658475653757));
#10667=CARTESIAN_POINT('Ctrl Pts',(-0.149937403644339,0.0414136589348379,
0.322738434101334));
#10668=CARTESIAN_POINT('Ctrl Pts',(-0.150126630744275,0.0407223642402907,
0.322789079273793));
#10669=CARTESIAN_POINT('Ctrl Pts',(-0.153777084537168,0.0270149747521514,
0.323786727562734));
#10670=CARTESIAN_POINT('Ctrl Pts',(-0.155538566952624,0.0136034147113705,
0.324649336154599));
#10671=CARTESIAN_POINT('Ctrl Pts',(-0.155549944528231,0.000131366907260993,
0.325541276351331));
#10672=CARTESIAN_POINT('Ctrl Pts',(-0.155549941519498,0.000134882470554111,
0.325594377439629));
#10673=CARTESIAN_POINT('Ctrl Pts',(-0.15555880784338,-0.0100899907526335,
0.326325391658143));
#10674=CARTESIAN_POINT('Ctrl Pts',(-0.154555154411991,-0.0203335588299377,
0.327056405876658));
#10675=CARTESIAN_POINT('Ctrl Pts',(-0.152554318723264,-0.0303806243991271,
0.327787420095172));
#10676=CARTESIAN_POINT('Ctrl Pts',(-0.150554603080401,-0.0404220657312509,
0.328518025099948));
#10677=CARTESIAN_POINT('Ctrl Pts',(-0.147559001477363,-0.0502663007971989,
0.329248630104723));
#10678=CARTESIAN_POINT('Ctrl Pts',(-0.143633978489968,-0.0597083136853105,
0.329979235109499));
#10679=CARTESIAN_POINT('Ctrl Pts',(-0.139699463917864,-0.0691731594754049,
0.330711606880817));
#10680=CARTESIAN_POINT('Ctrl Pts',(-0.134831446328035,-0.0782329877699992,
0.331443978652135));
#10681=CARTESIAN_POINT('Ctrl Pts',(-0.129143803565775,-0.0867045587069356,
0.332176350423453));
#10682=CARTESIAN_POINT('Ctrl Pts',(-0.125869021867529,-0.091582246462531,
0.332598029100064));
#10683=CARTESIAN_POINT('Ctrl Pts',(-0.122323365373555,-0.0962654239148562,
0.333019707776675));
#10684=CARTESIAN_POINT('Ctrl Pts',(-0.118534587709285,-0.100724148130375,
0.333441386453285));
#10685=CARTESIAN_POINT('Ctrl Pts',(-0.111909869255113,-0.108520275327589,
0.334178696150029));
#10686=CARTESIAN_POINT('Ctrl Pts',(-0.104487883553983,-0.11568924989458,
0.334916005846774));
#10687=CARTESIAN_POINT('Ctrl Pts',(-0.0964115024798472,-0.122068114958733,
0.335653315543518));
#10688=CARTESIAN_POINT('Ctrl Pts',(-0.0882848547000145,-0.128486681533985,
0.336395214192813));
#10689=CARTESIAN_POINT('Ctrl Pts',(-0.0794962614522086,-0.134104547200687,
0.337137112842109));
#10690=CARTESIAN_POINT('Ctrl Pts',(-0.0702284668008892,-0.138793965829918,
0.337879011491404));
#10691=CARTESIAN_POINT('Ctrl Pts',(-0.0610391862679532,-0.143443657039276,
0.33861462498651));
#10692=CARTESIAN_POINT('Ctrl Pts',(-0.0513796418104073,-0.147180168478902,
0.339350238481616));
#10693=CARTESIAN_POINT('Ctrl Pts',(-0.0414531982586966,-0.149924763978888,
0.340085851976721));
#10694=CARTESIAN_POINT('Ctrl Pts',(-0.0313995359392024,-0.152704534620479,
0.340830893203111));
#10695=CARTESIAN_POINT('Ctrl Pts',(-0.0210730073372121,-0.154466474556329,
0.341575934429501));
#10696=CARTESIAN_POINT('Ctrl Pts',(-0.0106975876470872,-0.155181713222057,
0.342320975655891));
#10697=CARTESIAN_POINT('Ctrl Pts',(-0.000322167956962707,-0.155896951887786,
0.343066016882281));
#10698=CARTESIAN_POINT('Ctrl Pts',(0.0101011639815613,-0.15556555558113,
0.343811058108671));
#10699=CARTESIAN_POINT('Ctrl Pts',(0.0203502550655604,-0.154213065655173,
0.344556099335061));
#10700=CARTESIAN_POINT('Ctrl Pts',(0.0304929880736154,-0.152874610947079,
0.345293409031827));
#10701=CARTESIAN_POINT('Ctrl Pts',(0.0405411244634621,-0.150526202297159,
0.346030718728593));
#10702=CARTESIAN_POINT('Ctrl Pts',(0.0502802718650486,-0.14719951345428,
0.346768028425358));
#10703=CARTESIAN_POINT('Ctrl Pts',(0.0600800348875177,-0.143852119584423,
0.347509927074648));
#10704=CARTESIAN_POINT('Ctrl Pts',(0.0695660042342812,-0.139514358471281,
0.348251825723938));
#10705=CARTESIAN_POINT('Ctrl Pts',(0.0785317499687253,-0.134270498423331,
0.348993724373228));
#10706=CARTESIAN_POINT('Ctrl Pts',(0.0874215404575554,-0.129071062864954,
0.349729337868355));
#10707=CARTESIAN_POINT('Ctrl Pts',(0.0957990883436117,-0.122981316705354,
0.350464951363482));
#10708=CARTESIAN_POINT('Ctrl Pts',(0.103487959801753,-0.116129430705876,
0.351200564858609));
#10709=CARTESIAN_POINT('Ctrl Pts',(0.111275372972575,-0.109189729923024,
0.35194560608498));
#10710=CARTESIAN_POINT('Ctrl Pts',(0.118355571950899,-0.101468822740119,
0.352690647311352));
#10711=CARTESIAN_POINT('Ctrl Pts',(0.124582843579175,-0.0931392376269359,
0.353435688537723));
#10712=CARTESIAN_POINT('Ctrl Pts',(0.130810115207451,-0.0848096525137527,
0.354180729764095));
#10713=CARTESIAN_POINT('Ctrl Pts',(0.136183984389138,-0.075872247844273,
0.354925770990466));
#10714=CARTESIAN_POINT('Ctrl Pts',(0.140605443003462,-0.0665275273687531,
0.355670812216837));
#10715=CARTESIAN_POINT('Ctrl Pts',(0.144981018736611,-0.057279780027348,
0.35640812191363));
#10716=CARTESIAN_POINT('Ctrl Pts',(0.14845673252472,-0.0475638404553147,
0.357145431610422));
#10717=CARTESIAN_POINT('Ctrl Pts',(0.150942937142596,-0.0375770172680896,
0.357882741307214));
#10718=CARTESIAN_POINT('Ctrl Pts',(0.15344461568537,-0.0275280369475157,
0.358624639956497));
#10719=CARTESIAN_POINT('Ctrl Pts',(0.154944024042579,-0.0172056554152167,
0.359366538605781));
#10720=CARTESIAN_POINT('Ctrl Pts',(0.155400022831297,-0.00682901193674878,
0.360108437255064));
#10721=CARTESIAN_POINT('Ctrl Pts',(0.155852158528107,0.0034597235725403,
0.360844050750219));
#10722=CARTESIAN_POINT('Ctrl Pts',(0.155278477933672,0.0138008650692228,
0.361579664245374));
#10723=CARTESIAN_POINT('Ctrl Pts',(0.153690994693365,0.0239766688713038,
0.362315277740529));
#10724=CARTESIAN_POINT('Ctrl Pts',(0.152083166033404,0.0342828872777153,
0.363060318966876));
#10725=CARTESIAN_POINT('Ctrl Pts',(0.14943546241944,0.0444185318484303,
0.363805360193224));
#10726=CARTESIAN_POINT('Ctrl Pts',(0.14581382593986,0.0541676163845165,
0.364550401419571));
#10727=CARTESIAN_POINT('Ctrl Pts',(0.14219218946028,0.0639167009206027,
0.365295442645918));
#10728=CARTESIAN_POINT('Ctrl Pts',(0.137597083689187,0.0732783607708785,
0.366040483872266));
#10729=CARTESIAN_POINT('Ctrl Pts',(0.132143282539398,0.0820606810824336,
0.366785525098613));
#10730=CARTESIAN_POINT('Ctrl Pts',(0.126746077217331,0.090751864465138,
0.367522834795384));
#10731=CARTESIAN_POINT('Ctrl Pts',(0.120467523852922,0.0989408714713713,
0.368260144492155));
#10732=CARTESIAN_POINT('Ctrl Pts',(0.113424787979095,0.10644538492531,0.368997454188926));
#10733=CARTESIAN_POINT('Ctrl Pts',(0.106338218719297,0.113996605829399,
0.369739352838215));
#10734=CARTESIAN_POINT('Ctrl Pts',(0.0984784316869404,0.120853976588515,
0.370481251487504));
#10735=CARTESIAN_POINT('Ctrl Pts',(0.0900072391288423,0.126864098169669,
0.371223150136792));
#10736=CARTESIAN_POINT('Ctrl Pts',(0.0816078121025456,0.132823303711729,
0.371958763631925));
#10737=CARTESIAN_POINT('Ctrl Pts',(0.0726080793179316,0.137949035530561,
0.372694377127058));
#10738=CARTESIAN_POINT('Ctrl Pts',(0.0631975039910557,0.142133310625274,
0.373429990622192));
#10739=CARTESIAN_POINT('Ctrl Pts',(0.0536663213404706,0.146371212007785,
0.374175031848558));
#10740=CARTESIAN_POINT('Ctrl Pts',(0.0437145572080062,0.149642911252742,
0.374920073074924));
#10741=CARTESIAN_POINT('Ctrl Pts',(0.0335594421983349,0.151886689144693,
0.375665114301291));
#10742=CARTESIAN_POINT('Ctrl Pts',(0.0234043271886633,0.154130467036644,
0.376410155527657));
#10743=CARTESIAN_POINT('Ctrl Pts',(0.0130468391673053,0.15534624419272,
0.377155196754023));
#10744=CARTESIAN_POINT('Ctrl Pts',(0.00271046422415448,0.155526383239917,
0.37790023798039));
#10745=CARTESIAN_POINT('Ctrl Pts',(-0.00751912685898194,0.155704661292045,
0.37863758227447));
#10746=CARTESIAN_POINT('Ctrl Pts',(-0.0178047266851457,0.154870016604413,
0.37937492656855));
#10747=CARTESIAN_POINT('Ctrl Pts',(-0.0279295856847137,0.153022026987883,
0.380112270862631));
#10748=CARTESIAN_POINT('Ctrl Pts',(-0.0380325437573131,0.151178034729303,
0.380848020218595));
#10749=CARTESIAN_POINT('Ctrl Pts',(-0.0479745335382852,0.148325135029611,
0.38158376957456));
#10750=CARTESIAN_POINT('Ctrl Pts',(-0.0575442136137484,0.144514587428312,
0.382319518930524));
#10751=CARTESIAN_POINT('Ctrl Pts',(-0.0596103411904147,0.143691876802757,
0.382478369803478));
#10752=CARTESIAN_POINT('Ctrl Pts',(-0.0616591580438317,0.142824714283798,
0.382637220676431));
#10753=CARTESIAN_POINT('Ctrl Pts',(-0.0636886258329921,0.141913922641526,
0.382796071549385));
#10754=CARTESIAN_POINT('Origin',(0.,0.,-0.129405622560373));
#10755=CARTESIAN_POINT('',(-0.0637865765496296,0.142129738084048,0.466608809190139));
#10756=CARTESIAN_POINT('',(-0.0636704081198525,0.141871577573868,0.452783997775559));
#10757=CARTESIAN_POINT('',(-0.0636886258329924,0.141913922641526,-0.129405622560373));
#10758=CARTESIAN_POINT('',(-0.155747148273957,-8.48283479504535E-5,0.40940562256037));
#10759=CARTESIAN_POINT('Ctrl Pts',(-0.155747148273957,-8.48283479504535E-5,
0.40940562256037));
#10760=CARTESIAN_POINT('Ctrl Pts',(-0.155779482799656,-0.00500404714443213,
0.409759213094268));
#10761=CARTESIAN_POINT('Ctrl Pts',(-0.153336323268121,-0.0614340654297066,
0.413817707922091));
#10762=CARTESIAN_POINT('Ctrl Pts',(-0.0845632241029054,-0.163255983359439,
0.42158110704384));
#10763=CARTESIAN_POINT('Ctrl Pts',(0.0913113927969153,-0.159579712115361,
0.432695819925616));
#10764=CARTESIAN_POINT('Ctrl Pts',(0.183594933073833,-0.00981608490943425,
0.443810532807392));
#10765=CARTESIAN_POINT('Ctrl Pts',(0.107806367033371,0.148933683901261,
0.454925245689169));
#10766=CARTESIAN_POINT('Ctrl Pts',(-0.0114902447342972,0.16425485410465,
0.462524671150084));
#10767=CARTESIAN_POINT('Ctrl Pts',(-0.0613862033991981,0.143219630774059,
0.466419192317074));
#10768=CARTESIAN_POINT('Ctrl Pts',(-0.0637865765496296,0.142129738084048,
0.466608809190139));
#10769=CARTESIAN_POINT('Ctrl Pts',(-0.15554997258092,-9.23584055120413E-5,
0.409292448061377));
#10770=CARTESIAN_POINT('Ctrl Pts',(-0.155557537435976,0.0126483660585973,
0.408427759124959));
#10771=CARTESIAN_POINT('Ctrl Pts',(-0.153999806552126,0.0253430736269646,
0.407612305561652));
#10772=CARTESIAN_POINT('Ctrl Pts',(-0.149882798880593,0.0418201330599853,
0.406475148577664));
#10773=CARTESIAN_POINT('Ctrl Pts',(-0.148687414650298,0.0458892688006899,
0.406188013833792));
#10774=CARTESIAN_POINT('Ctrl Pts',(-0.14649406783911,0.0523644696222185,
0.405716850546238));
#10775=CARTESIAN_POINT('Ctrl Pts',(-0.145599273192537,0.0548032833110541,
0.405536046470926));
#10776=CARTESIAN_POINT('Ctrl Pts',(-0.144351432928983,0.0579577294100021,
0.405297249788426));
#10777=CARTESIAN_POINT('Ctrl Pts',(-0.144053322372908,0.0586947600576042,
0.40524109849527));
#10778=CARTESIAN_POINT('Ctrl Pts',(-0.143557846676748,0.059893230008936,
0.405149192967831));
#10779=CARTESIAN_POINT('Ctrl Pts',(-0.143363872462857,0.0603560635318725,
0.405113553465428));
#10780=CARTESIAN_POINT('Ctrl Pts',(-0.142985521260094,0.0612467160773643,
0.405044683000883));
#10781=CARTESIAN_POINT('Ctrl Pts',(-0.142801455094546,0.0616746620135198,
0.405011462892062));
#10782=CARTESIAN_POINT('Ctrl Pts',(-0.142374158583935,0.062655939886744,
0.404934989247679));
#10783=CARTESIAN_POINT('Ctrl Pts',(-0.142129621211477,0.0632086907851109,
0.40489169152825));
#10784=CARTESIAN_POINT('Ctrl Pts',(-0.141468225648485,0.0646804606617182,
0.404775807944452));
#10785=CARTESIAN_POINT('Ctrl Pts',(-0.141045641411174,0.0655968582265392,
0.404703026930829));
#10786=CARTESIAN_POINT('Ctrl Pts',(-0.137591525234734,0.0728995883620714,
0.404117909179039));
#10787=CARTESIAN_POINT('Ctrl Pts',(-0.134137241223736,0.0790755959048336,
0.403590896643744));
#10788=CARTESIAN_POINT('Ctrl Pts',(-0.124704628610565,0.0935334474189555,
0.402275888788921));
#10789=CARTESIAN_POINT('Ctrl Pts',(-0.118307773153663,0.101503675713296,
0.401477575043163));
#10790=CARTESIAN_POINT('Ctrl Pts',(-0.108533763554301,0.111492238453883,
0.400403532777939));
#10791=CARTESIAN_POINT('Ctrl Pts',(-0.105791642054227,0.114097458434855,
0.400115603687116));
#10792=CARTESIAN_POINT('Ctrl Pts',(-0.101967647376471,0.117474012903218,
0.399734386913506));
#10793=CARTESIAN_POINT('Ctrl Pts',(-0.100967075944991,0.118335094879871,
0.399636417229969));
#10794=CARTESIAN_POINT('Ctrl Pts',(-0.0994718924935058,0.119589061732261,
0.399492765935777));
#10795=CARTESIAN_POINT('Ctrl Pts',(-0.0989856845943892,0.119991813732151,
0.399446473643626));
#10796=CARTESIAN_POINT('Ctrl Pts',(-0.0981049607053237,0.120712368013654,
0.399363393766964));
#10797=CARTESIAN_POINT('Ctrl Pts',(-0.0977113220410934,0.121031221883824,
0.399326536594244));
#10798=CARTESIAN_POINT('Ctrl Pts',(-0.0970869351904872,0.121531953930878,
0.399268516574676));
#10799=CARTESIAN_POINT('Ctrl Pts',(-0.0968572221164068,0.121715107274073,
0.399247264743596));
#10800=CARTESIAN_POINT('Ctrl Pts',(-0.0966263276692074,0.121898134940101,
0.399225998682503));
#10801=CARTESIAN_POINT('Ctrl Pts',(-0.0966256664104302,0.121898659104406,
0.399225937779395));
#10802=CARTESIAN_POINT('Ctrl Pts',(-0.0966243412313925,0.121899709525155,
0.399225815729616));
#10803=CARTESIAN_POINT('Ctrl Pts',(-0.096623677311036,0.121900235781603,
0.399225754582941));
#10804=CARTESIAN_POINT('Ctrl Pts',(-0.0966223467903276,0.1219012904011,
0.399225632044343));
#10805=CARTESIAN_POINT('Ctrl Pts',(-0.0966216801867385,0.121901818766642,
0.399225570652127));
#10806=CARTESIAN_POINT('Ctrl Pts',(-0.0966203442745582,0.121902877623932,
0.399225447620162));
#10807=CARTESIAN_POINT('Ctrl Pts',(-0.096619674968368,0.121903408113704,
0.39922538598064));
#10808=CARTESIAN_POINT('Ctrl Pts',(-0.0966183336272404,0.121904471238058,
0.399225262451894));
#10809=CARTESIAN_POINT('Ctrl Pts',(-0.0966176615937382,0.121905003871429,
0.39922520056281));
#10810=CARTESIAN_POINT('Ctrl Pts',(-0.0966163147788525,0.121906071297926,
0.399225076533197));
#10811=CARTESIAN_POINT('Ctrl Pts',(-0.0966156399939986,0.121906606093728,
0.399225014392356));
#10812=CARTESIAN_POINT('Ctrl Pts',(-0.0966142876526094,0.121907677863727,
0.399224889857058));
#10813=CARTESIAN_POINT('Ctrl Pts',(-0.0966136100963429,0.121908214837636,
0.399224827462632));
#10814=CARTESIAN_POINT('Ctrl Pts',(-0.0966122521868786,0.121909290983635,
0.399224702417861));
#10815=CARTESIAN_POINT('Ctrl Pts',(-0.0966115718352112,0.121909830154436,
0.399224639767663));
#10816=CARTESIAN_POINT('Ctrl Pts',(-0.0966101471332454,0.121910959194794,
0.39922450857568));
#10817=CARTESIAN_POINT('Ctrl Pts',(-0.09660940278153,0.121911549063647,
0.399224440033928));
#10818=CARTESIAN_POINT('Ctrl Pts',(-0.0966079004402631,0.121912739586392,
0.399224301696613));
#10819=CARTESIAN_POINT('Ctrl Pts',(-0.0966071424489415,0.121913340241277,
0.399224231900924));
#10820=CARTESIAN_POINT('Ctrl Pts',(-0.0966056125263574,0.121914552574241,
0.399224091028028));
#10821=CARTESIAN_POINT('Ctrl Pts',(-0.0966048405972114,0.121915164250217,
0.399224019951054));
#10822=CARTESIAN_POINT('Ctrl Pts',(-0.0966032824931897,0.121916398866383,
0.399223876487547));
#10823=CARTESIAN_POINT('Ctrl Pts',(-0.0966024963151156,0.121917021808664,
0.399223804100759));
#10824=CARTESIAN_POINT('Ctrl Pts',(-0.096600909394848,0.121918279208378,
0.399223657988428));
#10825=CARTESIAN_POINT('Ctrl Pts',(-0.096600108654989,0.1219189136635,0.399223584263141));
#10826=CARTESIAN_POINT('Ctrl Pts',(-0.0965984922879632,0.121920194343575,
0.39922343544418));
#10827=CARTESIAN_POINT('Ctrl Pts',(-0.0965976766573522,0.121920840570776,
0.399223360350232));
#10828=CARTESIAN_POINT('Ctrl Pts',(-0.0965960301729118,0.121922145059696,
0.399223208763152));
#10829=CARTESIAN_POINT('Ctrl Pts',(-0.0965951993210838,0.121922803319329,
0.399223132270249));
#10830=CARTESIAN_POINT('Ctrl Pts',(-0.0965935220492247,0.12192413214492,
0.399222977853633));
#10831=CARTESIAN_POINT('Ctrl Pts',(-0.0965926756306571,0.121924802709198,
0.399222899930101));
#10832=CARTESIAN_POINT('Ctrl Pts',(-0.0965909668741902,0.121926156420677,
0.399222742620042));
#10833=CARTESIAN_POINT('Ctrl Pts',(-0.0965901045349775,0.121926839568376,
0.399222663233442));
#10834=CARTESIAN_POINT('Ctrl Pts',(-0.0965883635749518,0.121928218732045,
0.399222502964044));
#10835=CARTESIAN_POINT('Ctrl Pts',(-0.0965874849529363,0.121928914748401,
0.399222422081185));
#10836=CARTESIAN_POINT('Ctrl Pts',(-0.0965857110534585,0.12193031994382,
0.399222258785007));
#10837=CARTESIAN_POINT('Ctrl Pts',(-0.0965848157753737,0.121931029122786,
0.399222176371682));
#10838=CARTESIAN_POINT('Ctrl Pts',(-0.0963904279118336,0.122085006604115,
0.399204282632976));
#10839=CARTESIAN_POINT('Ctrl Pts',(-0.096196573136442,0.122237812270272,
0.399186505003034));
#10840=CARTESIAN_POINT('Ctrl Pts',(-0.0957419364928956,0.122594427433828,
0.39914496751221));
#10841=CARTESIAN_POINT('Ctrl Pts',(-0.095480867346312,0.122797866502447,
0.399121234049922));
#10842=CARTESIAN_POINT('Ctrl Pts',(-0.0946772604466527,0.123419967880696,
0.399048536354677));
#10843=CARTESIAN_POINT('Ctrl Pts',(-0.0941325936993364,0.123835887234364,
0.398999760930253));
#10844=CARTESIAN_POINT('Ctrl Pts',(-0.0863119302969718,0.129726501274908,
0.398306195051271));
#10845=CARTESIAN_POINT('Ctrl Pts',(-0.078570331258783,0.13455659010774,
0.397702516207297));
#10846=CARTESIAN_POINT('Ctrl Pts',(-0.0682213415125348,0.139813789530708,
0.396937441118992));
#10847=CARTESIAN_POINT('Ctrl Pts',(-0.0659671172503672,0.140891373402896,
0.396773196082423));
#10848=CARTESIAN_POINT('Ctrl Pts',(-0.0636886207929056,0.141913924903434,
0.396608754846595));
#10849=CARTESIAN_POINT('',(-0.155542147809967,-7.47474344319557E-5,0.395594379955244));
#10850=CARTESIAN_POINT('Ctrl Pts',(-0.0636886258329921,0.141913922641526,
0.382796071549385));
#10851=CARTESIAN_POINT('Ctrl Pts',(-0.0730861195942185,0.137696482570911,
0.383531633895099));
#10852=CARTESIAN_POINT('Ctrl Pts',(-0.082066691787089,0.132539942042728,
0.384267196240812));
#10853=CARTESIAN_POINT('Ctrl Pts',(-0.0904421818323631,0.126554392438199,
0.385002758586526));
#10854=CARTESIAN_POINT('Ctrl Pts',(-0.0988383308873284,0.120554078858474,
0.385740135272601));
#10855=CARTESIAN_POINT('Ctrl Pts',(-0.106625672314012,0.113721234620129,
0.386477511958675));
#10856=CARTESIAN_POINT('Ctrl Pts',(-0.113647151506982,0.106207944403181,
0.38721488864475));
#10857=CARTESIAN_POINT('Ctrl Pts',(-0.119360694143706,0.100094203577801,
0.387814909383888));
#10858=CARTESIAN_POINT('Ctrl Pts',(-0.124567633470123,0.0935308734025379,
0.388414930123027));
#10859=CARTESIAN_POINT('Ctrl Pts',(-0.129203650408045,0.0866153521105563,
0.389014950862166));
#10860=CARTESIAN_POINT('Ctrl Pts',(-0.134996062412211,0.0779748425776694,
0.3897646390921));
#10861=CARTESIAN_POINT('Ctrl Pts',(-0.13993845508717,0.0687205532039445,
0.390514327322034));
#10862=CARTESIAN_POINT('Ctrl Pts',(-0.143909921737381,0.0590401297893296,
0.391264015551968));
#10863=CARTESIAN_POINT('Ctrl Pts',(-0.147872374669165,0.0493816772531327,
0.392012002274825));
#10864=CARTESIAN_POINT('Ctrl Pts',(-0.150867858811146,0.0392997867614514,
0.392759988997682));
#10865=CARTESIAN_POINT('Ctrl Pts',(-0.152821662629263,0.029005894766889,
0.393507975720539));
#10866=CARTESIAN_POINT('Ctrl Pts',(-0.1546382811691,0.0194347828307725,
0.394203442960236));
#10867=CARTESIAN_POINT('Ctrl Pts',(-0.155554668148968,0.00968118809725694,
0.394898910199932));
#10868=CARTESIAN_POINT('Ctrl Pts',(-0.15554998205569,-7.47159587813949E-5,
0.395594377439629));
#10869=CARTESIAN_POINT('Ctrl Pts',(-0.155329803440314,-7.56005704470291E-5,
0.395594448140074));
#10870=CARTESIAN_POINT('Ctrl Pts',(-0.155421485368252,-0.021252058778351,
0.397106186674697));
#10871=CARTESIAN_POINT('Ctrl Pts',(-0.141514608041042,-0.0942113101233241,
0.402322829503245));
#10872=CARTESIAN_POINT('Ctrl Pts',(-0.030390408656302,-0.18132809188354,
0.411244376625719));
#10873=CARTESIAN_POINT('Ctrl Pts',(0.135872146613563,-0.123863689671489,
0.422359089507495));
#10874=CARTESIAN_POINT('Ctrl Pts',(0.177750452880091,0.0469918114711103,
0.433473802389271));
#10875=CARTESIAN_POINT('Ctrl Pts',(0.0674866542632175,0.163636701374273,
0.443615438478625));
#10876=CARTESIAN_POINT('Ctrl Pts',(-0.0287035209048353,0.157155007295605,
0.450052170274054));
#10877=CARTESIAN_POINT('Ctrl Pts',(-0.0636704081198332,0.141871577573876,
0.452783997775557));
#10878=CARTESIAN_POINT('Origin',(0.,0.,-0.129405622560373));
#10879=CARTESIAN_POINT('',(-0.0636886258329926,0.141913922641526,0.536610014060325));
#10880=CARTESIAN_POINT('',(-0.0636886260274623,0.141913922554251,0.522938154987668));
#10881=CARTESIAN_POINT('',(-0.0636886258329924,0.141913922641526,-0.129405622560373));
#10882=CARTESIAN_POINT('',(-0.155549938719811,0.000138073397279943,0.479405624672607));
#10883=CARTESIAN_POINT('Ctrl Pts',(-0.155549938719811,0.000138073397279943,
0.479405624672607));
#10884=CARTESIAN_POINT('Ctrl Pts',(-0.1555590802874,-0.0101605815668361,
0.480144271311098));
#10885=CARTESIAN_POINT('Ctrl Pts',(-0.154540807560027,-0.0204920682189847,
0.480882917949589));
#10886=CARTESIAN_POINT('Ctrl Pts',(-0.152503881605263,-0.0306328026032212,
0.48162156458808));
#10887=CARTESIAN_POINT('Ctrl Pts',(-0.150503926990696,-0.0405894770122334,
0.482346804378819));
#10888=CARTESIAN_POINT('Ctrl Pts',(-0.147522245248312,-0.050361310081166,
0.483072044169558));
#10889=CARTESIAN_POINT('Ctrl Pts',(-0.143619085953899,-0.0597441264876015,
0.483797283960298));
#10890=CARTESIAN_POINT('Ctrl Pts',(-0.139607695430838,-0.0693871202711947,
0.484542634022664));
#10891=CARTESIAN_POINT('Ctrl Pts',(-0.134623217858585,-0.0786181617347638,
0.485287984085031));
#10892=CARTESIAN_POINT('Ctrl Pts',(-0.128783351950023,-0.0872390437849736,
0.486033334147398));
#10893=CARTESIAN_POINT('Ctrl Pts',(-0.12294348604146,-0.0958599258351837,
0.486778684209764));
#10894=CARTESIAN_POINT('Ctrl Pts',(-0.11624896051622,-0.103869838725253,
0.487524034272131));
#10895=CARTESIAN_POINT('Ctrl Pts',(-0.108861606859135,-0.111107844241741,
0.488269384334498));
#10896=CARTESIAN_POINT('Ctrl Pts',(-0.101553943306264,-0.118267770727406,
0.489006694031275));
#10897=CARTESIAN_POINT('Ctrl Pts',(-0.093509487166098,-0.124730494109114,
0.489744003728051));
#10898=CARTESIAN_POINT('Ctrl Pts',(-0.0848853671140475,-0.130346756576117,
0.490481313424828));
#10899=CARTESIAN_POINT('Ctrl Pts',(-0.0762075712761837,-0.135997974180504,
0.491223212074115));
#10900=CARTESIAN_POINT('Ctrl Pts',(-0.0669435581198422,-0.140791495449943,
0.491965110723402));
#10901=CARTESIAN_POINT('Ctrl Pts',(-0.0572869535805678,-0.144616760610442,
0.492707009372689));
#10902=CARTESIAN_POINT('Ctrl Pts',(-0.0477121570458454,-0.148409619213502,
0.493442622867828));
#10903=CARTESIAN_POINT('Ctrl Pts',(-0.0377522780015032,-0.151250239972536,
0.494178236362967));
#10904=CARTESIAN_POINT('Ctrl Pts',(-0.0276170107185682,-0.153078748423713,
0.494913849858106));
#10905=CARTESIAN_POINT('Ctrl Pts',(-0.0173518483529004,-0.154930691309317,
0.495658891084467));
#10906=CARTESIAN_POINT('Ctrl Pts',(-0.00690771718440615,-0.155744171137756,
0.496403932310828));
#10907=CARTESIAN_POINT('Ctrl Pts',(0.00348970852022084,-0.155510849893002,
0.49714897353719));
#10908=CARTESIAN_POINT('Ctrl Pts',(0.0138871342248475,-0.155277528648248,
0.497894014763551));
#10909=CARTESIAN_POINT('Ctrl Pts',(0.0242368857416045,-0.153997561560528,
0.498639055989912));
#10910=CARTESIAN_POINT('Ctrl Pts',(0.0343200622446376,-0.151716630029553,
0.499384097216273));
#10911=CARTESIAN_POINT('Ctrl Pts',(0.0442986024206074,-0.149459368449967,
0.50012140691305));
#10912=CARTESIAN_POINT('Ctrl Pts',(0.0540908956050945,-0.146204977218319,
0.500858716609827));
#10913=CARTESIAN_POINT('Ctrl Pts',(0.0634863282952233,-0.142004537320436,
0.501596026306604));
#10914=CARTESIAN_POINT('Ctrl Pts',(0.0729402373550734,-0.137777954243781,
0.502337924955891));
#10915=CARTESIAN_POINT('Ctrl Pts',(0.0819913996524141,-0.132593723636582,
0.503079823605178));
#10916=CARTESIAN_POINT('Ctrl Pts',(0.090441924285109,-0.126554576494122,
0.503821722254466));
#10917=CARTESIAN_POINT('Ctrl Pts',(0.0988208584788675,-0.120566591286989,
0.504557335749605));
#10918=CARTESIAN_POINT('Ctrl Pts',(0.106608541702961,-0.113738684808734,
0.505292949244743));
#10919=CARTESIAN_POINT('Ctrl Pts',(0.113640955466632,-0.106214574050038,
0.506028562739883));
#10920=CARTESIAN_POINT('Ctrl Pts',(0.120763497683961,-0.0985940331763595,
0.506773603966244));
#10921=CARTESIAN_POINT('Ctrl Pts',(0.127110572156788,-0.0902599902839601,
0.507518645192605));
#10922=CARTESIAN_POINT('Ctrl Pts',(0.132552795837115,-0.081397535686065,
0.508263686418966));
#10923=CARTESIAN_POINT('Ctrl Pts',(0.137995019517441,-0.0725350810881702,
0.509008727645328));
#10924=CARTESIAN_POINT('Ctrl Pts',(0.142531997515425,-0.0631451128853464,
0.509753768871688));
#10925=CARTESIAN_POINT('Ctrl Pts',(0.146083407030714,-0.0534363236974505,
0.51049881009805));
#10926=CARTESIAN_POINT('Ctrl Pts',(0.149597962440805,-0.043828285700466,
0.511236119794826));
#10927=CARTESIAN_POINT('Ctrl Pts',(0.152173731215626,-0.0338360145212888,
0.511973429491603));
#10928=CARTESIAN_POINT('Ctrl Pts',(0.153739421299251,-0.0236641678191169,
0.51271073918838));
#10929=CARTESIAN_POINT('Ctrl Pts',(0.155314856104085,-0.0134290124127974,
0.513452637837667));
#10930=CARTESIAN_POINT('Ctrl Pts',(0.155867274863009,-0.00301293736332606,
0.514194536486954));
#10931=CARTESIAN_POINT('Ctrl Pts',(0.15537568106821,0.00736208072422352,
0.514936435136241));
#10932=CARTESIAN_POINT('Ctrl Pts',(0.15488825191609,0.0176492046121652,
0.51567204863138));
#10933=CARTESIAN_POINT('Ctrl Pts',(0.15337449941722,0.0278950266995725,
0.516407662126519));
#10934=CARTESIAN_POINT('Ctrl Pts',(0.150866231699999,0.0378838043580931,
0.517143275621658));
#10935=CARTESIAN_POINT('Ctrl Pts',(0.14832581765318,0.0480005996666759,
0.51788831684802));
#10936=CARTESIAN_POINT('Ctrl Pts',(0.144765401788514,0.0578527600473534,
0.518633358074381));
#10937=CARTESIAN_POINT('Ctrl Pts',(0.14027033607596,0.0672312079107413,
0.519378399300742));
#10938=CARTESIAN_POINT('Ctrl Pts',(0.135775270363406,0.0766096557741292,
0.520123440527103));
#10939=CARTESIAN_POINT('Ctrl Pts',(0.130346095249456,0.0855135723160958,
0.520868481753464));
#10940=CARTESIAN_POINT('Ctrl Pts',(0.124114597521458,0.0937623014973852,
0.521613522979826));
#10941=CARTESIAN_POINT('Ctrl Pts',(0.117947766025789,0.101925430994467,
0.522350832676602));
#10942=CARTESIAN_POINT('Ctrl Pts',(0.110949021114648,0.109508150675974,
0.523088142373379));
#10943=CARTESIAN_POINT('Ctrl Pts',(0.103251656540129,0.116339580202609,
0.523825452070156));
#10944=CARTESIAN_POINT('Ctrl Pts',(0.0955063842266478,0.123213527962508,
0.524567350719443));
#10945=CARTESIAN_POINT('Ctrl Pts',(0.0870543473186811,0.129326044467828,
0.525309249368731));
#10946=CARTESIAN_POINT('Ctrl Pts',(0.0780706649700945,0.134539116137751,
0.526051148018018));
#10947=CARTESIAN_POINT('Ctrl Pts',(0.0691630898208316,0.139708024148578,
0.526786761513157));
#10948=CARTESIAN_POINT('Ctrl Pts',(0.0597336673533617,0.143992217048598,
0.527522375008296));
#10949=CARTESIAN_POINT('Ctrl Pts',(0.0499809135424709,0.147301428307603,
0.528257988503435));
#10950=CARTESIAN_POINT('Ctrl Pts',(0.0401031669980127,0.150653050906958,
0.529003029729796));
#10951=CARTESIAN_POINT('Ctrl Pts',(0.0298946459200571,0.15300416185647,
0.529748070956157));
#10952=CARTESIAN_POINT('Ctrl Pts',(0.0195773017775878,0.154313096511959,
0.530493112182519));
#10953=CARTESIAN_POINT('Ctrl Pts',(0.0092599576351189,0.155622031167448,
0.53123815340888));
#10954=CARTESIAN_POINT('Ctrl Pts',(-0.00116522854114558,0.155888799596017,
0.531983194635241));
#10955=CARTESIAN_POINT('Ctrl Pts',(-0.0114750046802433,0.155126164032984,
0.532728235861602));
#10956=CARTESIAN_POINT('Ctrl Pts',(-0.0216784195161703,0.154371396236549,
0.53346559083419));
#10957=CARTESIAN_POINT('Ctrl Pts',(-0.031845294325765,0.152602787151973,
0.534202945806778));
#10958=CARTESIAN_POINT('Ctrl Pts',(-0.0417597337363428,0.149839671443412,
0.534940300779366));
#10959=CARTESIAN_POINT('Ctrl Pts',(-0.0492433618270808,0.147754013396778,
0.535496871873019));
#10960=CARTESIAN_POINT('Ctrl Pts',(-0.0565829658107906,0.145102825562585,
0.536053442966672));
#10961=CARTESIAN_POINT('Ctrl Pts',(-0.0636886258329926,0.141913922641526,
0.536610014060325));
#10962=CARTESIAN_POINT('Ctrl Pts',(-0.0637865765496296,0.142129738084048,
0.466608809190139));
#10963=CARTESIAN_POINT('Ctrl Pts',(-0.108286843876662,0.121924331247818,
0.470124096610999));
#10964=CARTESIAN_POINT('Ctrl Pts',(-0.150204862388095,0.0699946174511132,
0.474389701067743));
#10965=CARTESIAN_POINT('Ctrl Pts',(-0.155693983092541,0.0106028137662625,
0.478655305524487));
#10966=CARTESIAN_POINT('Ctrl Pts',(-0.155597581791774,0.000138145146615299,
0.47940562256037));
#10967=CARTESIAN_POINT('',(-0.155730189438309,-9.40385839890952E-5,0.465594279708133));
#10968=CARTESIAN_POINT('Ctrl Pts',(-0.0636704081198332,0.141871577573876,
0.452783997775557));
#10969=CARTESIAN_POINT('Ctrl Pts',(-0.0761256112515922,0.136427620822346,
0.453757074567979));
#10970=CARTESIAN_POINT('Ctrl Pts',(-0.127520786042802,0.105560469046302,
0.458027168545505));
#10971=CARTESIAN_POINT('Ctrl Pts',(-0.155398933057417,0.0457878287565685,
0.462297262523029));
#10972=CARTESIAN_POINT('Ctrl Pts',(-0.155730189438309,-9.40385839890952E-5,
0.465594279708133));
#10973=CARTESIAN_POINT('Ctrl Pts',(-0.155549975452665,-8.73880735471365E-5,
0.465697707969148));
#10974=CARTESIAN_POINT('Ctrl Pts',(-0.155548164875887,-0.00331019825709863,
0.465944108543144));
#10975=CARTESIAN_POINT('Ctrl Pts',(-0.155446195038996,-0.00653246011159423,
0.466188084566158));
#10976=CARTESIAN_POINT('Ctrl Pts',(-0.155155744776936,-0.0111573908270398,
0.466532880105807));
#10977=CARTESIAN_POINT('Ctrl Pts',(-0.155048174695573,-0.0125640916787875,
0.466637030835553));
#10978=CARTESIAN_POINT('Ctrl Pts',(-0.154883554325798,-0.0143897677691079,
0.466771103469191));
#10979=CARTESIAN_POINT('Ctrl Pts',(-0.154843918718361,-0.0148101878428167,
0.466801902094296));
#10980=CARTESIAN_POINT('Ctrl Pts',(-0.154774299441659,-0.0155177995442651,
0.466853605932392));
#10981=CARTESIAN_POINT('Ctrl Pts',(-0.154745227618446,-0.0158050752386271,
0.466874559530526));
#10982=CARTESIAN_POINT('Ctrl Pts',(-0.15469031679173,-0.0163330024566513,
0.4669129957944));
#10983=CARTESIAN_POINT('Ctrl Pts',(-0.154664715795774,-0.0165736769722737,
0.466930491496732));
#10984=CARTESIAN_POINT('Ctrl Pts',(-0.154610555425915,-0.0170717818417858,
0.466966644029411));
#10985=CARTESIAN_POINT('Ctrl Pts',(-0.154581915234115,-0.0173291969883696,
0.466985295485207));
#10986=CARTESIAN_POINT('Ctrl Pts',(-0.154514967182694,-0.017917544348447,
0.467027854072288));
#10987=CARTESIAN_POINT('Ctrl Pts',(-0.154476239093041,-0.0182484256919927,
0.467051737361886));
#10988=CARTESIAN_POINT('Ctrl Pts',(-0.15437061608041,-0.0191263998087611,
0.467114980254563));
#10989=CARTESIAN_POINT('Ctrl Pts',(-0.154301875072465,-0.0196732725305804,
0.467154238895342));
#10990=CARTESIAN_POINT('Ctrl Pts',(-0.153801795329305,-0.0234877262749171,
0.467427205988928));
#10991=CARTESIAN_POINT('Ctrl Pts',(-0.153269564534123,-0.026741545112331,
0.467655632166634));
#10992=CARTESIAN_POINT('Ctrl Pts',(-0.152246948752375,-0.0319485348496029,
0.468017626718562));
#10993=CARTESIAN_POINT('Ctrl Pts',(-0.151821408491984,-0.0339131660570124,
0.468153384709735));
#10994=CARTESIAN_POINT('Ctrl Pts',(-0.148682919453986,-0.0471567511957541,
0.469066254280379));
#10995=CARTESIAN_POINT('Ctrl Pts',(-0.144753683561463,-0.0581099049338928,
0.46981278092554));
#10996=CARTESIAN_POINT('Ctrl Pts',(-0.13786812908316,-0.0721416220458392,
0.470861248283143));
#10997=CARTESIAN_POINT('Ctrl Pts',(-0.135953539177746,-0.0756879497399387,
0.471134588221908));
#10998=CARTESIAN_POINT('Ctrl Pts',(-0.132629730486719,-0.0813106596315096,
0.471585145436031));
#10999=CARTESIAN_POINT('Ctrl Pts',(-0.131304118296203,-0.0834343817743867,
0.471759492773676));
#11000=CARTESIAN_POINT('Ctrl Pts',(-0.129496671811696,-0.0861802160342242,
0.471990942536704));
#11001=CARTESIAN_POINT('Ctrl Pts',(-0.129060496691806,-0.0868320551364464,
0.472046343993481));
#11002=CARTESIAN_POINT('Ctrl Pts',(-0.128338573174079,-0.0878934725014694,
0.472137323055854));
#11003=CARTESIAN_POINT('Ctrl Pts',(-0.128055744863998,-0.0883050285626444,
0.472172790276873));
#11004=CARTESIAN_POINT('Ctrl Pts',(-0.127504846408535,-0.0890984529819978,
0.472241540611045));
#11005=CARTESIAN_POINT('Ctrl Pts',(-0.127237029916742,-0.0894804916766432,
0.472274813813889));
#11006=CARTESIAN_POINT('Ctrl Pts',(-0.12661531116442,-0.0903589350395661,
0.472351716572051));
#11007=CARTESIAN_POINT('Ctrl Pts',(-0.126260203267138,-0.0908544727247875,
0.47239539201171));
#11008=CARTESIAN_POINT('Ctrl Pts',(-0.125298872028597,-0.0921794480044028,
0.472512972880781));
#11009=CARTESIAN_POINT('Ctrl Pts',(-0.124687338396307,-0.0930049757566399,
0.472587082654436));
#11010=CARTESIAN_POINT('Ctrl Pts',(-0.119292433485654,-0.10013887270268,
0.47323508061539));
#11011=CARTESIAN_POINT('Ctrl Pts',(-0.114042947506785,-0.106078486715775,
0.473827534466485));
#11012=CARTESIAN_POINT('Ctrl Pts',(-0.101551535814027,-0.118208685514831,
0.475159817809064));
#11013=CARTESIAN_POINT('Ctrl Pts',(-0.0941466666919652,-0.124186952003432,
0.475903099373365));
#11014=CARTESIAN_POINT('Ctrl Pts',(-0.0832040702968274,-0.131477070797758,
0.476912729319627));
#11015=CARTESIAN_POINT('Ctrl Pts',(-0.0800944336132139,-0.133394240125578,
0.477190543098319));
#11016=CARTESIAN_POINT('Ctrl Pts',(-0.0757991533018811,-0.135837968557607,
0.477559629399006));
#11017=CARTESIAN_POINT('Ctrl Pts',(-0.0746704080736929,-0.136461700741375,
0.477655295354975));
#11018=CARTESIAN_POINT('Ctrl Pts',(-0.0729869354279448,-0.137364825033823,
0.47779588855457));
#11019=CARTESIAN_POINT('Ctrl Pts',(-0.0724381147288619,-0.137655030666191,
0.477841398138763));
#11020=CARTESIAN_POINT('Ctrl Pts',(-0.0714412843417732,-0.13817452241102,
0.477923452672274));
#11021=CARTESIAN_POINT('Ctrl Pts',(-0.0709938748025159,-0.138404933117785,
0.477960062473078));
#11022=CARTESIAN_POINT('Ctrl Pts',(-0.0702858420787814,-0.138765225051959,
0.478017644218082));
#11023=CARTESIAN_POINT('Ctrl Pts',(-0.0700259643329782,-0.138896550005705,
0.478038704287792));
#11024=CARTESIAN_POINT('Ctrl Pts',(-0.0695350018513293,-0.139142921669729,
0.47807834795028));
#11025=CARTESIAN_POINT('Ctrl Pts',(-0.0693040021660714,-0.139258121553617,
0.478096940620944));
#11026=CARTESIAN_POINT('Ctrl Pts',(-0.0687764063239815,-0.139519596451617,
0.478139270607487));
#11027=CARTESIAN_POINT('Ctrl Pts',(-0.0684796301671491,-0.139665500817273,
0.478162984694788));
#11028=CARTESIAN_POINT('Ctrl Pts',(-0.0675673988751837,-0.140110375309755,
0.478235587443016));
#11029=CARTESIAN_POINT('Ctrl Pts',(-0.0669504231951391,-0.140406237540617,
0.478284287954387));
#11030=CARTESIAN_POINT('Ctrl Pts',(-0.0580752564643582,-0.144590398040235,
0.478979364980513));
#11031=CARTESIAN_POINT('Ctrl Pts',(-0.0494908820139851,-0.147749213291722,
0.479584420753534));
#11032=CARTESIAN_POINT('Ctrl Pts',(-0.0338469873846071,-0.151987719206044,
0.480652654654553));
#11033=CARTESIAN_POINT('Ctrl Pts',(-0.0268982386528548,-0.15337002830477,
0.481115843765348));
#11034=CARTESIAN_POINT('Ctrl Pts',(-0.0155100653906487,-0.154837498087777,
0.481883591788931));
#11035=CARTESIAN_POINT('Ctrl Pts',(-0.0111188455925274,-0.155214622642025,
0.482181575334059));
#11036=CARTESIAN_POINT('Ctrl Pts',(-0.00405027554779986,-0.155520181340613,
0.482668845916792));
#11037=CARTESIAN_POINT('Ctrl Pts',(-0.00138036420720576,-0.155566785149004,
0.482854612961654));
#11038=CARTESIAN_POINT('Ctrl Pts',(0.00209202504326187,-0.15553800293797,
0.483099024303547));
#11039=CARTESIAN_POINT('Ctrl Pts',(0.00289468207103836,-0.15552513526461,
0.483155715347063));
#11040=CARTESIAN_POINT('Ctrl Pts',(0.00420048694823484,-0.155494089470242,
0.483248275232321));
#11041=CARTESIAN_POINT('Ctrl Pts',(0.00470371715538929,-0.155479680295672,
0.483284026118819));
#11042=CARTESIAN_POINT('Ctrl Pts',(0.00567170286170136,-0.155447259882393,
0.483352952999139));
#11043=CARTESIAN_POINT('Ctrl Pts',(0.00613646566108345,-0.155429606571105,
0.483386117444879));
#11044=CARTESIAN_POINT('Ctrl Pts',(0.00720090180359724,-0.155384393937088,
0.483462237883674));
#11045=CARTESIAN_POINT('Ctrl Pts',(0.00780050550932397,-0.15535544715613,
0.483505236780354));
#11046=CARTESIAN_POINT('Ctrl Pts',(0.00939387042019223,-0.155269277474624,
0.483619826887047));
#11047=CARTESIAN_POINT('Ctrl Pts',(0.0103872609876461,-0.155205985878364,
0.483691606506616));
#11048=CARTESIAN_POINT('Ctrl Pts',(0.0178920778310046,-0.154655462241151,
0.484236525968052));
#11049=CARTESIAN_POINT('Ctrl Pts',(0.0243666784582232,-0.153768269754051,
0.484722117126193));
#11050=CARTESIAN_POINT('Ctrl Pts',(0.0410630567821762,-0.150399409257983,
0.486015561510219));
#11051=CARTESIAN_POINT('Ctrl Pts',(0.0511231205686958,-0.147283911548327,
0.486837855955399));
#11052=CARTESIAN_POINT('Ctrl Pts',(0.0644392496848606,-0.14163012766054,
0.487950976873036));
#11053=CARTESIAN_POINT('Ctrl Pts',(0.068027086086083,-0.139942239918318,
0.48825322014786));
#11054=CARTESIAN_POINT('Ctrl Pts',(0.0727560866326421,-0.137492578644091,
0.488651505730209));
#11055=CARTESIAN_POINT('Ctrl Pts',(0.073957161220585,-0.136850268324908,
0.488752650540117));
#11056=CARTESIAN_POINT('Ctrl Pts',(0.0757149476048539,-0.135880337076171,
0.488900497519645));
#11057=CARTESIAN_POINT('Ctrl Pts',(0.0762782668814876,-0.135564911882608,
0.488947850524431));
#11058=CARTESIAN_POINT('Ctrl Pts',(0.0772918840699767,-0.134989028169367,
0.489032984083087));
#11059=CARTESIAN_POINT('Ctrl Pts',(0.0777428666557943,-0.134729802843178,
0.489070836139389));
#11060=CARTESIAN_POINT('Ctrl Pts',(0.0784472258989971,-0.134320222009398,
0.489129904028981));
#11061=CARTESIAN_POINT('Ctrl Pts',(0.0787014844571805,-0.134171403958061,
0.489151215858852));
#11062=CARTESIAN_POINT('Ctrl Pts',(0.0791773683102057,-0.133891049978019,
0.4891910824759));
#11063=CARTESIAN_POINT('Ctrl Pts',(0.0793990872681636,-0.133759686974749,
0.489209647567011));
#11064=CARTESIAN_POINT('Ctrl Pts',(0.0799002911315223,-0.133461050739314,
0.489251594870398));
#11065=CARTESIAN_POINT('Ctrl Pts',(0.08017957721249,-0.133293450666705,
0.489274955498335));
#11066=CARTESIAN_POINT('Ctrl Pts',(0.081022439578012,-0.132784039817386,
0.489345421054062));
#11067=CARTESIAN_POINT('Ctrl Pts',(0.0815843816311355,-0.132439516990278,
0.489392353571305));
#11068=CARTESIAN_POINT('Ctrl Pts',(0.0858776605068247,-0.129769641485927,
0.489750695234669));
#11069=CARTESIAN_POINT('Ctrl Pts',(0.089511521009019,-0.127290333644916,
0.490052695432413));
#11070=CARTESIAN_POINT('Ctrl Pts',(0.10484180971496,-0.115849092683232,
0.491343893714127));
#11071=CARTESIAN_POINT('Ctrl Pts',(0.115336420249136,-0.105405770913032,
0.492280662351702));
#11072=CARTESIAN_POINT('Ctrl Pts',(0.12660778001882,-0.0904554742995251,
0.493555391767838));
#11073=CARTESIAN_POINT('Ctrl Pts',(0.128886111333087,-0.0871784858382005,
0.493830845358089));
#11074=CARTESIAN_POINT('Ctrl Pts',(0.131529973887771,-0.0830452256196419,
0.49417555558678));
#11075=CARTESIAN_POINT('Ctrl Pts',(0.132017287071481,-0.0822683376463375,
0.494240230570442));
#11076=CARTESIAN_POINT('Ctrl Pts',(0.132774677104978,-0.0810368260556379,
0.494342592506802));
#11077=CARTESIAN_POINT('Ctrl Pts',(0.133049360016668,-0.0805850472736843,
0.494380110308273));
#11078=CARTESIAN_POINT('Ctrl Pts',(0.133558821153511,-0.0797374166033444,
0.494450443594424));
#11079=CARTESIAN_POINT('Ctrl Pts',(0.133794156892778,-0.079341904990258,
0.494483238316564));
#11080=CARTESIAN_POINT('Ctrl Pts',(0.134315362871283,-0.0784570391010249,
0.494556560300084));
#11081=CARTESIAN_POINT('Ctrl Pts',(0.134600319671333,-0.0779671572933243,
0.494597120056372));
#11082=CARTESIAN_POINT('Ctrl Pts',(0.135312722173778,-0.0767268890445578,
0.494699731659987));
#11083=CARTESIAN_POINT('Ctrl Pts',(0.13573660288336,-0.0759744882595893,
0.494761910347876));
#11084=CARTESIAN_POINT('Ctrl Pts',(0.138064530579706,-0.0717606759675843,
0.495109796803931));
#11085=CARTESIAN_POINT('Ctrl Pts',(0.139842271893258,-0.0682315394491492,
0.495399924999162));
#11086=CARTESIAN_POINT('Ctrl Pts',(0.142300711081877,-0.0628504271923861,
0.495840983464642));
#11087=CARTESIAN_POINT('Ctrl Pts',(0.143083764667252,-0.061046738526805,
0.495988596044243));
#11088=CARTESIAN_POINT('Ctrl Pts',(0.149414031658429,-0.0456741817785139,
0.497244582644813));
#11089=CARTESIAN_POINT('Ctrl Pts',(0.153050942097622,-0.0314008743230206,
0.498406742355253));
#11090=CARTESIAN_POINT('Ctrl Pts',(0.154924694426822,-0.0141853042412813,
0.499710367010844));
#11091=CARTESIAN_POINT('Ctrl Pts',(0.155144717481925,-0.0115326815911267,
0.499908258261993));
#11092=CARTESIAN_POINT('Ctrl Pts',(0.155327579760841,-0.00833310466792126,
0.500142395278582));
#11093=CARTESIAN_POINT('Ctrl Pts',(0.155355738177683,-0.0077905267289172,
0.500181942085597));
#11094=CARTESIAN_POINT('Ctrl Pts',(0.155395099642321,-0.00694668107853892,
0.500243190936549));
#11095=CARTESIAN_POINT('Ctrl Pts',(0.155408270309878,-0.00664551686200445,
0.50026499958461));
#11096=CARTESIAN_POINT('Ctrl Pts',(0.155431073642886,-0.00608688946849056,
0.500305355847305));
#11097=CARTESIAN_POINT('Ctrl Pts',(0.155440942071776,-0.00582944310631814,
0.500323915996993));
#11098=CARTESIAN_POINT('Ctrl Pts',(0.155461799888879,-0.00524753886955188,
0.500365781886261));
#11099=CARTESIAN_POINT('Ctrl Pts',(0.155472413197397,-0.00492307106106822,
0.500389066396508));
#11100=CARTESIAN_POINT('Ctrl Pts',(0.155500721623952,-0.00396593599087978,
0.50045758255323));
#11101=CARTESIAN_POINT('Ctrl Pts',(0.155515571620106,-0.00333318080103419,
0.500502659162807));
#11102=CARTESIAN_POINT('Ctrl Pts',(0.155594566512995,0.00121654713528559,
0.50082531643342));
#11103=CARTESIAN_POINT('Ctrl Pts',(0.155514588212892,0.00513503335253237,
0.501095442046556));
#11104=CARTESIAN_POINT('Ctrl Pts',(0.155224819022421,0.0101089143053874,
0.501433209105386));
#11105=CARTESIAN_POINT('Ctrl Pts',(0.155152039359066,0.0111704682524216,
0.501504999509196));
#11106=CARTESIAN_POINT('Ctrl Pts',(0.154158416206782,0.0237677088421316,
0.502354247233721));
#11107=CARTESIAN_POINT('Ctrl Pts',(0.151963932812225,0.0351668696930953,
0.503098801121396));
#11108=CARTESIAN_POINT('Ctrl Pts',(0.146632486672816,0.052300049104295,
0.504300374314306));
#11109=CARTESIAN_POINT('Ctrl Pts',(0.144368162367733,0.0582597473445544,
0.504734403320023));
#11110=CARTESIAN_POINT('Ctrl Pts',(0.141317601395188,0.0650093513068715,
0.505253859661951));
#11111=CARTESIAN_POINT('Ctrl Pts',(0.140880595348656,0.0659510271546518,
0.50532697711584));
#11112=CARTESIAN_POINT('Ctrl Pts',(0.140195597801441,0.067389203563851,
0.505439673701972));
#11113=CARTESIAN_POINT('Ctrl Pts',(0.139954314025153,0.067888882529719,
0.505479021149259));
#11114=CARTESIAN_POINT('Ctrl Pts',(0.139510188859246,0.0687961991023488,
0.505550824406271));
#11115=CARTESIAN_POINT('Ctrl Pts',(0.139308220465525,0.0692042593278585,
0.505583249573012));
#11116=CARTESIAN_POINT('Ctrl Pts',(0.138864296785653,0.0700913517546344,
0.505654031086156));
#11117=CARTESIAN_POINT('Ctrl Pts',(0.138621648894121,0.0705700287452655,
0.505692411327243));
#11118=CARTESIAN_POINT('Ctrl Pts',(0.137952627848658,0.0718730569520019,
0.505797404005634));
#11119=CARTESIAN_POINT('Ctrl Pts',(0.137521352297071,0.0726948515301451,
0.505864187992973));
#11120=CARTESIAN_POINT('Ctrl Pts',(0.135329385860168,0.0767823182649117,
0.506199256833229));
#11121=CARTESIAN_POINT('Ctrl Pts',(0.133459752358724,0.0799878567360161,
0.506471379390095));
#11122=CARTESIAN_POINT('Ctrl Pts',(0.129883640070248,0.0856442538859851,
0.506969282705803));
#11123=CARTESIAN_POINT('Ctrl Pts',(0.1282177271067,0.0881187304214564,0.507193581156044));
#11124=CARTESIAN_POINT('Ctrl Pts',(0.120411447203032,0.0990234409545753,
0.508211271586583));
#11125=CARTESIAN_POINT('Ctrl Pts',(0.113503947172465,0.106870849970884,
0.509027138066551));
#11126=CARTESIAN_POINT('Ctrl Pts',(0.102857147538016,0.116760679644628,
0.510146181466628));
#11127=CARTESIAN_POINT('Ctrl Pts',(0.0997402815676494,0.119434210948601,
0.510459519811949));
#11128=CARTESIAN_POINT('Ctrl Pts',(0.09487486750574,0.123284097739597,0.510923764924525));
#11129=CARTESIAN_POINT('Ctrl Pts',(0.0932023539512702,0.124553328511343,
0.511079175914049));
#11130=CARTESIAN_POINT('Ctrl Pts',(0.0910960020863834,0.12608559053669,
0.511269295003979));
#11131=CARTESIAN_POINT('Ctrl Pts',(0.0906860015093899,0.126380801099234,
0.511306043821766));
#11132=CARTESIAN_POINT('Ctrl Pts',(0.0900358894915702,0.12684410510161,
0.511363898933324));
#11133=CARTESIAN_POINT('Ctrl Pts',(0.0897967337674781,0.127013522918407,
0.511385093896668));
#11134=CARTESIAN_POINT('Ctrl Pts',(0.0893454814969487,0.127331278256141,
0.511424917969795));
#11135=CARTESIAN_POINT('Ctrl Pts',(0.0891334962161335,0.127479760511008,
0.511443556558521));
#11136=CARTESIAN_POINT('Ctrl Pts',(0.0886490671948899,0.127817273241531,
0.511485992441576));
#11137=CARTESIAN_POINT('Ctrl Pts',(0.0883763891443588,0.128005961973545,
0.511509766390563));
#11138=CARTESIAN_POINT('Ctrl Pts',(0.0876531826104626,0.128502996559307,
0.511572529269652));
#11139=CARTESIAN_POINT('Ctrl Pts',(0.0872016251804054,0.128809848753669,
0.511611419662326));
#11140=CARTESIAN_POINT('Ctrl Pts',(0.0841006168665344,0.130893333112102,
0.511876534584703));
#11141=CARTESIAN_POINT('Ctrl Pts',(0.0813984343165668,0.132590637159455,
0.51209781452478));
#11142=CARTESIAN_POINT('Ctrl Pts',(0.0778791106639981,0.134653021236762,
0.512376398738253));
#11143=CARTESIAN_POINT('Ctrl Pts',(0.0771086542724344,0.13509569757276,
0.512436814285568));
#11144=CARTESIAN_POINT('Ctrl Pts',(0.0655367818292574,0.141613227791855,
0.513336351889971));
#11145=CARTESIAN_POINT('Ctrl Pts',(0.0540505877705848,0.146382902925483,
0.514130696433513));
#11146=CARTESIAN_POINT('Ctrl Pts',(0.0379624645776529,0.150908252378661,
0.515248958307355));
#11147=CARTESIAN_POINT('Ctrl Pts',(0.0337590056200117,0.151903831450294,
0.515541228482873));
#11148=CARTESIAN_POINT('Ctrl Pts',(0.0269357746227456,0.153222692128533,
0.516020018771936));
#11149=CARTESIAN_POINT('Ctrl Pts',(0.0243395976488883,0.153656473652998,
0.516203176168421));
#11150=CARTESIAN_POINT('Ctrl Pts',(0.020942987189616,0.154135757097126,
0.516444630632217));
#11151=CARTESIAN_POINT('Ctrl Pts',(0.0201513455757505,0.15424125115262,
0.516501033693001));
#11152=CARTESIAN_POINT('Ctrl Pts',(0.0188603177378919,0.154403184715411,
0.51659324040369));
#11153=CARTESIAN_POINT('Ctrl Pts',(0.0183614009725772,0.154463309491148,
0.516628927805409));
#11154=CARTESIAN_POINT('Ctrl Pts',(0.0173998799815613,0.154574458689163,
0.516697813577958));
#11155=CARTESIAN_POINT('Ctrl Pts',(0.0169373202021491,0.154625826685374,
0.516731000761746));
#11156=CARTESIAN_POINT('Ctrl Pts',(0.015875617953295,0.154738909241769,
0.516807288675343));
#11157=CARTESIAN_POINT('Ctrl Pts',(0.0152763369178987,0.154799220896665,
0.516850432947526));
#11158=CARTESIAN_POINT('Ctrl Pts',(0.0136789591696513,0.154950614913672,
0.516965663510083));
#11159=CARTESIAN_POINT('Ctrl Pts',(0.01268032153837,0.155035532521845,0.517037941569458));
#11160=CARTESIAN_POINT('Ctrl Pts',(0.00489320014901267,0.155621958577393,
0.517603499032958));
#11161=CARTESIAN_POINT('Ctrl Pts',(-0.0019197227178117,0.155686950441743,
0.518110349161898));
#11162=CARTESIAN_POINT('Ctrl Pts',(-0.022709745869486,0.154520431489838,
0.519694167932434));
#11163=CARTESIAN_POINT('Ctrl Pts',(-0.0365335872077338,0.151847146766974,
0.520804791631584));
#11164=CARTESIAN_POINT('Ctrl Pts',(-0.0518989612148523,0.14665317734524,
0.522019864148303));
#11165=CARTESIAN_POINT('Ctrl Pts',(-0.0539710667562702,0.145903330712485,
0.522183113000258));
#11166=CARTESIAN_POINT('Ctrl Pts',(-0.0565053145224866,0.144924860436067,
0.522381436127547));
#11167=CARTESIAN_POINT('Ctrl Pts',(-0.0569830405300083,0.144737689817398,
0.522418762312211));
#11168=CARTESIAN_POINT('Ctrl Pts',(-0.0577338071554716,0.144439249961131,
0.522477318770632));
#11169=CARTESIAN_POINT('Ctrl Pts',(-0.0580074665675729,0.144329564692631,
0.522498641301715));
#11170=CARTESIAN_POINT('Ctrl Pts',(-0.0585204821753058,0.14412224840889,
0.522538570638093));
#11171=CARTESIAN_POINT('Ctrl Pts',(-0.0587599039628375,0.144024799976349,
0.52255718756815));
#11172=CARTESIAN_POINT('Ctrl Pts',(-0.0593084114202115,0.143799953387588,
0.522599798650671));
#11173=CARTESIAN_POINT('Ctrl Pts',(-0.0596173298069143,0.143672155450658,
0.522623768388046));
#11174=CARTESIAN_POINT('Ctrl Pts',(-0.0605742888472609,0.143272648488029,
0.522697939199957));
#11175=CARTESIAN_POINT('Ctrl Pts',(-0.0612209145136707,0.142997538265821,
0.522747940134679));
#11176=CARTESIAN_POINT('Ctrl Pts',(-0.0624750809416945,0.142453880004019,
0.522844734101855));
#11177=CARTESIAN_POINT('Ctrl Pts',(-0.0630827451941917,0.142185831871624,
0.522891546874463));
#11178=CARTESIAN_POINT('Ctrl Pts',(-0.0636886260274623,0.141913922554251,
0.522938154987668));
#11179=CARTESIAN_POINT('Origin',(0.,0.,-0.129405622560373));
#11180=CARTESIAN_POINT('',(-0.0636886258321223,0.141913922641917,0.606695238001095));
#11181=CARTESIAN_POINT('',(-0.063688625907641,0.141913922608025,0.592717731153444));
#11182=CARTESIAN_POINT('',(-0.0636886258329924,0.141913922641526,-0.129405622560373));
#11183=CARTESIAN_POINT('',(-0.155549999999463,-4.08543441352296E-7,0.54940562255668));
#11184=CARTESIAN_POINT('Ctrl Pts',(-0.0636886258321223,0.141913922641917,
0.606695238001095));
#11185=CARTESIAN_POINT('Ctrl Pts',(-0.0636228496240879,0.14194344191828,
0.606690392871029));
#11186=CARTESIAN_POINT('Ctrl Pts',(-0.0635570512475328,0.14197291620284,
0.606685546573706));
#11187=CARTESIAN_POINT('Ctrl Pts',(-0.0583496585560615,0.144301214160662,
0.60630203832958));
#11188=CARTESIAN_POINT('Ctrl Pts',(-0.0530876043388053,0.146318888920545,
0.605917040173728));
#11189=CARTESIAN_POINT('Ctrl Pts',(-0.0468144616707361,0.148341263218698,
0.605454986388314));
#11190=CARTESIAN_POINT('Ctrl Pts',(-0.0458980334977013,0.148627368417361,
0.605387417318009));
#11191=CARTESIAN_POINT('Ctrl Pts',(-0.0444081656620055,0.149077405893748,
0.605277428635648));
#11192=CARTESIAN_POINT('Ctrl Pts',(-0.0438363181890301,0.149246558805094,
0.605235179268839));
#11193=CARTESIAN_POINT('Ctrl Pts',(-0.0428185119163103,0.149541272472045,
0.605159916262343));
#11194=CARTESIAN_POINT('Ctrl Pts',(-0.0423729355252007,0.149668137764049,
0.605126945431326));
#11195=CARTESIAN_POINT('Ctrl Pts',(-0.0414351677004477,0.149930617351041,
0.605057504686982));
#11196=CARTESIAN_POINT('Ctrl Pts',(-0.0409428629847105,0.150065802569334,
0.605021021313407));
#11197=CARTESIAN_POINT('Ctrl Pts',(-0.0396442999892002,0.150415517988506,
0.604924707635625));
#11198=CARTESIAN_POINT('Ctrl Pts',(-0.0388369753361092,0.150625986701401,
0.604864747064989));
#11199=CARTESIAN_POINT('Ctrl Pts',(-0.0351396480552566,0.151558175603332,
0.604589737204761));
#11200=CARTESIAN_POINT('Ctrl Pts',(-0.032231162169451,0.152203237054385,
0.604372252406214));
#11201=CARTESIAN_POINT('Ctrl Pts',(-0.0242527408110029,0.153733807643722,
0.603772016513123));
#11202=CARTESIAN_POINT('Ctrl Pts',(-0.0191548954397207,0.154451801169225,
0.603384420198587));
#11203=CARTESIAN_POINT('Ctrl Pts',(-0.00144627765254581,0.156055737879248,
0.602026066894407));
#11204=CARTESIAN_POINT('Ctrl Pts',(0.0112299305269262,0.155657820024943,
0.601028703700662));
#11205=CARTESIAN_POINT('Ctrl Pts',(0.0263353323862714,0.153327316201151,
0.59987773287967));
#11206=CARTESIAN_POINT('Ctrl Pts',(0.0289420747006572,0.152856711330897,
0.599680701166667));
#11207=CARTESIAN_POINT('Ctrl Pts',(0.0320409827575366,0.152215124572108,
0.59944934011767));
#11208=CARTESIAN_POINT('Ctrl Pts',(0.032545723287219,0.152108003209668,
0.59941174860009));
#11209=CARTESIAN_POINT('Ctrl Pts',(0.0333686425723911,0.151929070860057,
0.599350620327875));
#11210=CARTESIAN_POINT('Ctrl Pts',(0.0336871394586741,0.151858768334015,
0.599327000937595));
#11211=CARTESIAN_POINT('Ctrl Pts',(0.0342570023710706,0.151731100176208,
0.599284813700123));
#11212=CARTESIAN_POINT('Ctrl Pts',(0.0345084479197196,0.15167411116551,
0.599266224792553));
#11213=CARTESIAN_POINT('Ctrl Pts',(0.0350526537515696,0.151549345965948,
0.599226048746406));
#11214=CARTESIAN_POINT('Ctrl Pts',(0.0353453588916062,0.151481346728645,
0.599204474599771));
#11215=CARTESIAN_POINT('Ctrl Pts',(0.036162193650409,0.151289088824309,
0.599144361502053));
#11216=CARTESIAN_POINT('Ctrl Pts',(0.036685884571956,0.151162953606365,
0.599105928259505));
#11217=CARTESIAN_POINT('Ctrl Pts',(0.0397160170218915,0.150416446973662,
0.598884110716867));
#11218=CARTESIAN_POINT('Ctrl Pts',(0.0422075457645097,0.149736417451604,
0.598703949270332));
#11219=CARTESIAN_POINT('Ctrl Pts',(0.0587852181785379,0.144765030107717,
0.597513020807236));
#11220=CARTESIAN_POINT('Ctrl Pts',(0.0722186342837146,0.13855393980055,
0.596579658534424));
#11221=CARTESIAN_POINT('Ctrl Pts',(0.0861695532009537,0.129515252754879,
0.595462850214944));
#11222=CARTESIAN_POINT('Ctrl Pts',(0.0877407240458845,0.128456052936871,
0.595334845684996));
#11223=CARTESIAN_POINT('Ctrl Pts',(0.0925914559234453,0.125055429738614,
0.594931882655904));
#11224=CARTESIAN_POINT('Ctrl Pts',(0.0957994071019434,0.122615280463015,
0.594653960190692));
#11225=CARTESIAN_POINT('Ctrl Pts',(0.099579670333836,0.11950082552985,0.594310100331516));
#11226=CARTESIAN_POINT('Ctrl Pts',(0.100245878746327,0.118942514627391,
0.594248857339703));
#11227=CARTESIAN_POINT('Ctrl Pts',(0.101340066812819,0.118009815855463,
0.594147178516757));
#11228=CARTESIAN_POINT('Ctrl Pts',(0.101770741751611,0.117638607130564,
0.594106872854714));
#11229=CARTESIAN_POINT('Ctrl Pts',(0.102546522857291,0.116962494872795,
0.594033746325486));
#11230=CARTESIAN_POINT('Ctrl Pts',(0.1028923302962,0.116658402675708,0.594000959308965));
#11231=CARTESIAN_POINT('Ctrl Pts',(0.103631486434597,0.116002568777306,
0.593930463874316));
#11232=CARTESIAN_POINT('Ctrl Pts',(0.104024404747847,0.115650352994551,
0.5938927358718));
#11233=CARTESIAN_POINT('Ctrl Pts',(0.105091360867665,0.114684086748224,
0.59378958423956));
#11234=CARTESIAN_POINT('Ctrl Pts',(0.10576179443667,0.114066106508724,0.593723995148152));
#11235=CARTESIAN_POINT('Ctrl Pts',(0.109280168161355,0.110765317267864,
0.593375618965678));
#11236=CARTESIAN_POINT('Ctrl Pts',(0.112031316967832,0.107981894709485,
0.593088523407152));
#11237=CARTESIAN_POINT('Ctrl Pts',(0.124669916825852,0.0941916737298453,
0.591695220831876));
#11238=CARTESIAN_POINT('Ctrl Pts',(0.133057561929886,0.08191580412155,0.590529038508831));
#11239=CARTESIAN_POINT('Ctrl Pts',(0.141535641214404,0.0646762977072758,
0.58906112746275));
#11240=CARTESIAN_POINT('Ctrl Pts',(0.143317416693748,0.0606258055950618,
0.588727897502056));
#11241=CARTESIAN_POINT('Ctrl Pts',(0.145164090562029,0.0558894004613202,
0.588355527009997));
#11242=CARTESIAN_POINT('Ctrl Pts',(0.145399975062929,0.0552728284622067,
0.588307383158202));
#11243=CARTESIAN_POINT('Ctrl Pts',(0.14574646879012,0.0543495684879227,
0.58823580379183));
#11244=CARTESIAN_POINT('Ctrl Pts',(0.145860046609496,0.054044015098693,
0.588212197872362));
#11245=CARTESIAN_POINT('Ctrl Pts',(0.146061729855145,0.0534961684307075,
0.588170025135612));
#11246=CARTESIAN_POINT('Ctrl Pts',(0.146150193816012,0.0532540122067559,
0.588151437320121));
#11247=CARTESIAN_POINT('Ctrl Pts',(0.146340512909937,0.0527289973380136,
0.588111252742142));
#11248=CARTESIAN_POINT('Ctrl Pts',(0.146442149932301,0.0524460637835971,
0.588089669019786));
#11249=CARTESIAN_POINT('Ctrl Pts',(0.146723809301793,0.0516547877635206,
0.588029502264383));
#11250=CARTESIAN_POINT('Ctrl Pts',(0.146902011740119,0.051145794398306,
0.587991025245594));
#11251=CARTESIAN_POINT('Ctrl Pts',(0.147921394689084,0.0481848824878102,
0.587768447572583));
#11252=CARTESIAN_POINT('Ctrl Pts',(0.148703890567598,0.0457129846195717,
0.58758759565725));
#11253=CARTESIAN_POINT('Ctrl Pts',(0.153513528761999,0.0290856049325191,
0.586396676589063));
#11254=CARTESIAN_POINT('Ctrl Pts',(0.155576383426343,0.014438626043585,
0.585463789960434));
#11255=CARTESIAN_POINT('Ctrl Pts',(0.155546295269917,-0.00218796301726947,
0.58434672181089));
#11256=CARTESIAN_POINT('Ctrl Pts',(0.155507796055369,-0.00409415555346438,
0.584217918350292));
#11257=CARTESIAN_POINT('Ctrl Pts',(0.155279377172575,-0.0100123907218766,
0.583815005829561));
#11258=CARTESIAN_POINT('Ctrl Pts',(0.154969120707362,-0.0140178386724394,
0.583537965206974));
#11259=CARTESIAN_POINT('Ctrl Pts',(0.154403745968478,-0.0188690151277756,
0.583195081118856));
#11260=CARTESIAN_POINT('Ctrl Pts',(0.154296009048926,-0.0197306370431628,
0.583133900104402));
#11261=CARTESIAN_POINT('Ctrl Pts',(0.15410583541604,-0.0211545966022298,
0.583032302909887));
#11262=CARTESIAN_POINT('Ctrl Pts',(0.154027519622246,-0.0217174733830872,
0.582992016529782));
#11263=CARTESIAN_POINT('Ctrl Pts',(0.153880166473009,-0.022735630745161,
0.582918910591882));
#11264=CARTESIAN_POINT('Ctrl Pts',(0.153812188264794,-0.0231910601736626,
0.582886124795862));
#11265=CARTESIAN_POINT('Ctrl Pts',(0.153661943070413,-0.0241679210650832,
0.582815615997633));
#11266=CARTESIAN_POINT('Ctrl Pts',(0.153579042173131,-0.0246892476451226,
0.58277787334162));
#11267=CARTESIAN_POINT('Ctrl Pts',(0.153345564860988,-0.0261107888514442,
0.582674640793021));
#11268=CARTESIAN_POINT('Ctrl Pts',(0.153189718277372,-0.0270101037597491,
0.582608985001122));
#11269=CARTESIAN_POINT('Ctrl Pts',(0.152321687257459,-0.0317697209022288,
0.582259607901591));
#11270=CARTESIAN_POINT('Ctrl Pts',(0.15147154203859,-0.0356030670275371,
0.58197154859614));
#11271=CARTESIAN_POINT('Ctrl Pts',(0.146732535953112,-0.0537024556087539,
0.580577816547525));
#11272=CARTESIAN_POINT('Ctrl Pts',(0.140967667305219,-0.0673970505989316,
0.579412328963373));
#11273=CARTESIAN_POINT('Ctrl Pts',(0.131086073568716,-0.0838555672583985,
0.577945561714988));
#11274=CARTESIAN_POINT('Ctrl Pts',(0.128651744106631,-0.0875445747450963,
0.577612738592707));
#11275=CARTESIAN_POINT('Ctrl Pts',(0.125676769017241,-0.0916601755032032,
0.57724076655518));
#11276=CARTESIAN_POINT('Ctrl Pts',(0.125286739093392,-0.0921925761278503,
0.577192635467388));
#11277=CARTESIAN_POINT('Ctrl Pts',(0.124699032105828,-0.0929841928976501,
0.577121071306377));
#11278=CARTESIAN_POINT('Ctrl Pts',(0.124503916508397,-0.0932452868316977,
0.57709746793281));
#11279=CARTESIAN_POINT('Ctrl Pts',(0.12415300458986,-0.0937117944285697,
0.577055297935442));
#11280=CARTESIAN_POINT('Ctrl Pts',(0.123997517683928,-0.0939174348854666,
0.577036710325181));
#11281=CARTESIAN_POINT('Ctrl Pts',(0.123659590254208,-0.0943620614048785,
0.576996524129416));
#11282=CARTESIAN_POINT('Ctrl Pts',(0.123476968387237,-0.0946009047339768,
0.576974938593164));
#11283=CARTESIAN_POINT('Ctrl Pts',(0.122964785637752,-0.0952667567131231,
0.576914761671966));
#11284=CARTESIAN_POINT('Ctrl Pts',(0.122633690129042,-0.0956925885841168,
0.576876276359242));
#11285=CARTESIAN_POINT('Ctrl Pts',(0.120697442856023,-0.0981562996950603,
0.57665355429208));
#11286=CARTESIAN_POINT('Ctrl Pts',(0.119043607125714,-0.100155646942024,
0.576472571206104));
#11287=CARTESIAN_POINT('Ctrl Pts',(0.107680620676554,-0.113213137062743,
0.575281653641704));
#11288=CARTESIAN_POINT('Ctrl Pts',(0.096493776444301,-0.122887715270571,
0.57434885716864));
#11289=CARTESIAN_POINT('Ctrl Pts',(0.0792849207766551,-0.133950149332071,
0.57297438307565));
#11290=CARTESIAN_POINT('Ctrl Pts',(0.0742896539082768,-0.136783682501102,
0.572582295298205));
#11291=CARTESIAN_POINT('Ctrl Pts',(0.0682088221361338,-0.139801510721322,
0.572106437513219));
#11292=CARTESIAN_POINT('Ctrl Pts',(0.067263247175454,-0.140258908096826,
0.572032488594585));
#11293=CARTESIAN_POINT('Ctrl Pts',(0.0658087321236649,-0.14094440111431,
0.571918775317686));
#11294=CARTESIAN_POINT('Ctrl Pts',(0.0653030631271205,-0.141179401332923,
0.57187924927641));
#11295=CARTESIAN_POINT('Ctrl Pts',(0.0644001080599986,-0.141593143760605,
0.571808675958053));
#11296=CARTESIAN_POINT('Ctrl Pts',(0.0640033118394637,-0.141772946448386,
0.571777665461824));
#11297=CARTESIAN_POINT('Ctrl Pts',(0.0632117003290168,-0.142127653574691,
0.571715801367291));
#11298=CARTESIAN_POINT('Ctrl Pts',(0.0628169015662974,-0.142302585499374,
0.571684949042528));
#11299=CARTESIAN_POINT('Ctrl Pts',(0.061714924764121,-0.142785382455695,
0.571598832446714));
#11300=CARTESIAN_POINT('Ctrl Pts',(0.0610061861341762,-0.143089631333867,
0.571543445805745));
#11301=CARTESIAN_POINT('Ctrl Pts',(0.0580919589163292,-0.144315070443383,
0.571315677331949));
#11302=CARTESIAN_POINT('Ctrl Pts',(0.0558677516706189,-0.145190593327374,
0.571141769268236));
#11303=CARTESIAN_POINT('Ctrl Pts',(0.0500746385180267,-0.147318135892371,
0.570688333058454));
#11304=CARTESIAN_POINT('Ctrl Pts',(0.046478842937778,-0.148491802528006,
0.570406393919639));
#11305=CARTESIAN_POINT('Ctrl Pts',(0.0353359879743188,-0.151684443058084,
0.569531267476946));
#11306=CARTESIAN_POINT('Ctrl Pts',(0.0276771766279245,-0.153266937053795,
0.568927145015773));
#11307=CARTESIAN_POINT('Ctrl Pts',(0.0113399063064241,-0.155377857221553,
0.567649605839236));
#11308=CARTESIAN_POINT('Ctrl Pts',(0.00266832128430588,-0.155768374592577,
0.566977973686294));
#11309=CARTESIAN_POINT('Ctrl Pts',(-0.00715261114397514,-0.1553898092933,
0.566251387244432));
#11310=CARTESIAN_POINT('Ctrl Pts',(-0.00831322979201837,-0.15533204146457,
0.566166077189831));
#11311=CARTESIAN_POINT('Ctrl Pts',(-0.00989530206442547,-0.155235512635428,
0.566050643659634));
#11312=CARTESIAN_POINT('Ctrl Pts',(-0.0103173662344781,-0.155208032496642,
0.566019931492819));
#11313=CARTESIAN_POINT('Ctrl Pts',(-0.0109862204691736,-0.155161743711987,
0.565971398494046));
#11314=CARTESIAN_POINT('Ctrl Pts',(-0.0112330824516254,-0.15514406728241,
0.565953515494623));
#11315=CARTESIAN_POINT('Ctrl Pts',(-0.0117413654193336,-0.155106452395721,
0.565916757325326));
#11316=CARTESIAN_POINT('Ctrl Pts',(-0.0120027781935027,-0.155086442197625,
0.565897886696641));
#11317=CARTESIAN_POINT('Ctrl Pts',(-0.0126229524521631,-0.15503739265832,
0.565853197251119));
#11318=CARTESIAN_POINT('Ctrl Pts',(-0.0129816690795313,-0.155007768598415,
0.565827411076315));
#11319=CARTESIAN_POINT('Ctrl Pts',(-0.0141792421804365,-0.154904682487028,
0.565741523969575));
#11320=CARTESIAN_POINT('Ctrl Pts',(-0.0150176245902908,-0.154825652271663,
0.565681724821987));
#11321=CARTESIAN_POINT('Ctrl Pts',(-0.02515584389605,-0.153786843985333,
0.56496211148084));
#11322=CARTESIAN_POINT('Ctrl Pts',(-0.0343531694731221,-0.151997136882406,
0.564344490736005));
#11323=CARTESIAN_POINT('Ctrl Pts',(-0.0550549351542557,-0.145991999442293,
0.562924871311521));
#11324=CARTESIAN_POINT('Ctrl Pts',(-0.0663321685042083,-0.141225721967393,
0.562126286630674));
#11325=CARTESIAN_POINT('Ctrl Pts',(-0.0784320973250131,-0.13433976176749,
0.561158522064545));
#11326=CARTESIAN_POINT('Ctrl Pts',(-0.0799138460732735,-0.133463636530446,
0.561038040599918));
#11327=CARTESIAN_POINT('Ctrl Pts',(-0.0819663793336351,-0.132203583362628,
0.560868212987029));
#11328=CARTESIAN_POINT('Ctrl Pts',(-0.0825496601606235,-0.131840162223192,
0.560819614476925));
#11329=CARTESIAN_POINT('Ctrl Pts',(-0.0835313938487909,-0.131219410556196,
0.560737234379471));
#11330=CARTESIAN_POINT('Ctrl Pts',(-0.0839311168765511,-0.130964098423174,
0.560703527541403));
#11331=CARTESIAN_POINT('Ctrl Pts',(-0.0846963427535504,-0.130470389157694,
0.560638678537535));
#11332=CARTESIAN_POINT('Ctrl Pts',(-0.0850620229337815,-0.130232273918793,
0.560607547082493));
#11333=CARTESIAN_POINT('Ctrl Pts',(-0.0858131449618687,-0.129738662295228,
0.560543306096664));
#11334=CARTESIAN_POINT('Ctrl Pts',(-0.0861984586774024,-0.129482979790762,
0.560510189811726));
#11335=CARTESIAN_POINT('Ctrl Pts',(-0.0875221592688026,-0.128596085229633,
0.560395859201348));
#11336=CARTESIAN_POINT('Ctrl Pts',(-0.088454778928397,-0.127956373262866,
0.560314325677068));
#11337=CARTESIAN_POINT('Ctrl Pts',(-0.0983836808740542,-0.120985417633,
0.55943551362049));
#11338=CARTESIAN_POINT('Ctrl Pts',(-0.106689080910222,-0.113728451407107,
0.558601108919804));
#11339=CARTESIAN_POINT('Ctrl Pts',(-0.121642185123988,-0.0975723848635565,
0.556898317575468));
#11340=CARTESIAN_POINT('Ctrl Pts',(-0.128246305142112,-0.0887136817832488,
0.556035138823591));
#11341=CARTESIAN_POINT('Ctrl Pts',(-0.134447582447173,-0.0782367206849143,
0.555135180266414));
#11342=CARTESIAN_POINT('Ctrl Pts',(-0.135024904544559,-0.0772360813042496,
0.555050376911829));
#11343=CARTESIAN_POINT('Ctrl Pts',(-0.135797800454722,-0.0758613068925079,
0.554935520383834));
#11344=CARTESIAN_POINT('Ctrl Pts',(-0.136003059105635,-0.0754927043956593,
0.554904885841469));
#11345=CARTESIAN_POINT('Ctrl Pts',(-0.136326244569571,-0.0749067332774861,
0.554856445414567));
#11346=CARTESIAN_POINT('Ctrl Pts',(-0.13644515502325,-0.0746899144582098,
0.554838577772579));
#11347=CARTESIAN_POINT('Ctrl Pts',(-0.136689130198624,-0.0742425281514594,
0.554801826374327));
#11348=CARTESIAN_POINT('Ctrl Pts',(-0.136814128794541,-0.0740119278505793,
0.554782947245642));
#11349=CARTESIAN_POINT('Ctrl Pts',(-0.137109611852291,-0.0734635073364975,
0.5547381977602));
#11350=CARTESIAN_POINT('Ctrl Pts',(-0.137279576835164,-0.0731454056213762,
0.554712360288195));
#11351=CARTESIAN_POINT('Ctrl Pts',(-0.137844637208956,-0.0720789471289757,
0.554626124892199));
#11352=CARTESIAN_POINT('Ctrl Pts',(-0.138234741335024,-0.0713279398287831,
0.554566032109108));
#11353=CARTESIAN_POINT('Ctrl Pts',(-0.139153994011338,-0.0695223733999668,
0.554422979475206));
#11354=CARTESIAN_POINT('Ctrl Pts',(-0.139677320218167,-0.0684648879000127,
0.554340345784201));
#11355=CARTESIAN_POINT('Ctrl Pts',(-0.141576080191444,-0.0645156519965605,
0.55403560803146));
#11356=CARTESIAN_POINT('Ctrl Pts',(-0.142874242108495,-0.0615874162646004,
0.553817265486979));
#11357=CARTESIAN_POINT('Ctrl Pts',(-0.148533561568301,-0.0476776978490142,
0.552805796688296));
#11358=CARTESIAN_POINT('Ctrl Pts',(-0.15172489064108,-0.0362625009691681,
0.552046512952225));
#11359=CARTESIAN_POINT('Ctrl Pts',(-0.154592044357726,-0.018357808113916,
0.550832585222723));
#11360=CARTESIAN_POINT('Ctrl Pts',(-0.155209887669435,-0.0120658091122547,
0.550402388706692));
#11361=CARTESIAN_POINT('Ctrl Pts',(-0.155483355582146,-0.00467842002347808,
0.549884384452491));
#11362=CARTESIAN_POINT('Ctrl Pts',(-0.155512009975409,-0.00360223917708829,
0.549808612953919));
#11363=CARTESIAN_POINT('Ctrl Pts',(-0.15553847222879,-0.00197283667481611,
0.549693384679298));
#11364=CARTESIAN_POINT('Ctrl Pts',(-0.155544503861204,-0.00141976478831956,
0.549654184370811));
#11365=CARTESIAN_POINT('Ctrl Pts',(-0.155549213861576,-0.000574435365012869,
0.549594130454558));
#11366=CARTESIAN_POINT('Ctrl Pts',(-0.155550018564031,-0.000282189959955681,
0.549573343335134));
#11367=CARTESIAN_POINT('Ctrl Pts',(-0.155549999675089,1.00538485301794E-5,
0.549552530512073));
#11368=CARTESIAN_POINT('Ctrl Pts',(-0.0636886258329926,0.141913922641526,
0.536610014060325));
#11369=CARTESIAN_POINT('Ctrl Pts',(-0.0730814786960769,0.137698565329387,
0.537345736058591));
#11370=CARTESIAN_POINT('Ctrl Pts',(-0.0820642535703313,0.132542130691616,
0.538081458056857));
#11371=CARTESIAN_POINT('Ctrl Pts',(-0.0904466417708162,0.126551205021452,
0.538817180055122));
#11372=CARTESIAN_POINT('Ctrl Pts',(-0.0988275438342714,0.120561341499243,
0.539552771615179));
#11373=CARTESIAN_POINT('Ctrl Pts',(-0.106607530543232,0.113737839536412,
0.540288363175235));
#11374=CARTESIAN_POINT('Ctrl Pts',(-0.113627370286093,0.106229107225219,
0.541023954735291));
#11375=CARTESIAN_POINT('Ctrl Pts',(-0.120663580662677,0.0987028641572448,
0.541761261733369));
#11376=CARTESIAN_POINT('Ctrl Pts',(-0.126935523776145,0.0904889250916622,
0.542498568731447));
#11377=CARTESIAN_POINT('Ctrl Pts',(-0.132323914233961,0.0817690908705926,
0.543235875729525));
#11378=CARTESIAN_POINT('Ctrl Pts',(-0.133802785515336,0.0793758878336476,
0.543438233400809));
#11379=CARTESIAN_POINT('Ctrl Pts',(-0.135215366375327,0.0769447282492072,
0.543640591072093));
#11380=CARTESIAN_POINT('Ctrl Pts',(-0.136559806045013,0.0744796742269222,
0.543842948743377));
#11381=CARTESIAN_POINT('Ctrl Pts',(-0.141705683718826,0.0650446160803692,
0.544617477973856));
#11382=CARTESIAN_POINT('Ctrl Pts',(-0.145885002942362,0.0550465854919305,
0.545392007204334));
#11383=CARTESIAN_POINT('Ctrl Pts',(-0.148989921630324,0.0446968203856833,
0.546166536434813));
#11384=CARTESIAN_POINT('Ctrl Pts',(-0.152081349398532,0.0343920251690047,
0.546937700323798));
#11385=CARTESIAN_POINT('Ctrl Pts',(-0.15410734778821,0.0237392552038595,
0.547708864212783));
#11386=CARTESIAN_POINT('Ctrl Pts',(-0.155008465445465,0.012968351485135,
0.548480028101768));
#11387=CARTESIAN_POINT('Ctrl Pts',(-0.155368989547926,0.00865906915711002,
0.548788559586739));
#11388=CARTESIAN_POINT('Ctrl Pts',(-0.155550011375819,0.00433105777467094,
0.549097091071709));
#11389=CARTESIAN_POINT('Ctrl Pts',(-0.155549999999463,-4.08543441352294E-7,
0.54940562255668));
#11390=CARTESIAN_POINT('Ctrl Pts',(-0.0636886260274623,0.141913922554251,
0.522938154987668));
#11391=CARTESIAN_POINT('Ctrl Pts',(-0.0693125037711184,0.139390019049978,
0.523370778560055));
#11392=CARTESIAN_POINT('Ctrl Pts',(-0.0747827181519514,0.136533442705235,
0.523785861625993));
#11393=CARTESIAN_POINT('Ctrl Pts',(-0.0881720709049043,0.128494339908574,
0.524823008133113));
#11394=CARTESIAN_POINT('Ctrl Pts',(-0.0958138441722195,0.122901661705836,
0.525436271246095));
#11395=CARTESIAN_POINT('Ctrl Pts',(-0.106154319408019,0.113779985617878,
0.526358747946524));
#11396=CARTESIAN_POINT('Ctrl Pts',(-0.109286072117201,0.110775331897159,
0.526652340563003));
#11397=CARTESIAN_POINT('Ctrl Pts',(-0.114115429594705,0.105737622239116,
0.527133095389452));
#11398=CARTESIAN_POINT('Ctrl Pts',(-0.115893938886627,0.103785208557242,
0.527316858833636));
#11399=CARTESIAN_POINT('Ctrl Pts',(-0.118145049350833,0.101183937358877,
0.527559000245081));
#11400=CARTESIAN_POINT('Ctrl Pts',(-0.118663613682811,0.100575288269287,
0.527615470531124));
#11401=CARTESIAN_POINT('Ctrl Pts',(-0.119500535509174,0.0995774937518589,
0.527707759678011));
#11402=CARTESIAN_POINT('Ctrl Pts',(-0.119821744516277,0.0991907494635538,
0.527743461893031));
#11403=CARTESIAN_POINT('Ctrl Pts',(-0.120436640666833,0.0984430526750521,
0.527812357178973));
#11404=CARTESIAN_POINT('Ctrl Pts',(-0.120730594469286,0.0980823255512263,
0.527845538978341));
#11405=CARTESIAN_POINT('Ctrl Pts',(-0.121401012161318,0.0972520383144402,
0.527921787440167));
#11406=CARTESIAN_POINT('Ctrl Pts',(-0.121776376259455,0.0967816040184198,
0.527964897494571));
#11407=CARTESIAN_POINT('Ctrl Pts',(-0.122768537492344,0.0955232430470036,
0.528079977202787));
#11408=CARTESIAN_POINT('Ctrl Pts',(-0.123380468652547,0.0947315344976719,
0.528152137831722));
#11409=CARTESIAN_POINT('Ctrl Pts',(-0.128056496002495,0.0885595849195694,
0.528712908761808));
#11410=CARTESIAN_POINT('Ctrl Pts',(-0.131773904598353,0.0829269526565161,
0.529214825829898));
#11411=CARTESIAN_POINT('Ctrl Pts',(-0.142082778030083,0.0648545460312558,
0.530796773084979));
#11412=CARTESIAN_POINT('Ctrl Pts',(-0.147361903220405,0.0517499558580485,
0.531911261649214));
#11413=CARTESIAN_POINT('Ctrl Pts',(-0.151352150844595,0.035961937829689,
0.533131441400601));
#11414=CARTESIAN_POINT('Ctrl Pts',(-0.151850193278327,0.0337972591956748,
0.533296019281844));
#11415=CARTESIAN_POINT('Ctrl Pts',(-0.152406305096423,0.0311188887216352,
0.533495729511515));
#11416=CARTESIAN_POINT('Ctrl Pts',(-0.152508375606618,0.0306147425012116,
0.533533150547508));
#11417=CARTESIAN_POINT('Ctrl Pts',(-0.152665069153205,0.0298205675109193,
0.533591822177884));
#11418=CARTESIAN_POINT('Ctrl Pts',(-0.152721369540717,0.029530880037654,
0.533613165624603));
#11419=CARTESIAN_POINT('Ctrl Pts',(-0.152825430129839,0.0289871902928638,
0.533653112515148));
#11420=CARTESIAN_POINT('Ctrl Pts',(-0.152873381138254,0.0287332322634315,
0.533671726189034));
#11421=CARTESIAN_POINT('Ctrl Pts',(-0.152981823220601,0.0281509452489734,
0.533714301494299));
#11422=CARTESIAN_POINT('Ctrl Pts',(-0.153041890338123,0.0278225405328822,
0.533738238860759));
#11423=CARTESIAN_POINT('Ctrl Pts',(-0.153196620213558,0.0269609222069499,
0.533800852382747));
#11424=CARTESIAN_POINT('Ctrl Pts',(-0.153289557658122,0.0264273969038806,
0.533839433249556));
#11425=CARTESIAN_POINT('Ctrl Pts',(-0.153896325876387,0.0228331999091928,
0.534098128723025));
#11426=CARTESIAN_POINT('Ctrl Pts',(-0.154321290711703,0.0197579567617597,
0.534313566233528));
#11427=CARTESIAN_POINT('Ctrl Pts',(-0.155245941276463,0.0111805388222644,
0.534903316546242));
#11428=CARTESIAN_POINT('Ctrl Pts',(-0.155545066027013,0.00566119306105173,
0.53527023616306));
#11429=CARTESIAN_POINT('Ctrl Pts',(-0.155561771596661,-0.0132742945436004,
0.536520045667977));
#11430=CARTESIAN_POINT('Ctrl Pts',(-0.153839235067069,-0.0266292059187267,
0.537391592974479));
#11431=CARTESIAN_POINT('Ctrl Pts',(-0.150008356577863,-0.0411823023591037,
0.538438671652821));
#11432=CARTESIAN_POINT('Ctrl Pts',(-0.149566095899624,-0.042760632256689,
0.538553469462463));
#11433=CARTESIAN_POINT('Ctrl Pts',(-0.148922893840937,-0.0449238909266402,
0.538712653086854));
#11434=CARTESIAN_POINT('Ctrl Pts',(-0.148743271099596,-0.0455150916585728,
0.538756347441353));
#11435=CARTESIAN_POINT('Ctrl Pts',(-0.148429384043841,-0.0465264982652633,
0.538831433186879));
#11436=CARTESIAN_POINT('Ctrl Pts',(-0.148296844728414,-0.0469472355389249,
0.538862768041952));
#11437=CARTESIAN_POINT('Ctrl Pts',(-0.14802078951082,-0.0478107204855038,
0.538927285240482));
#11438=CARTESIAN_POINT('Ctrl Pts',(-0.147877072678076,-0.0482533987223313,
0.538960473889777));
#11439=CARTESIAN_POINT('Ctrl Pts',(-0.147539533466966,-0.0492774196686756,
0.539037512847962));
#11440=CARTESIAN_POINT('Ctrl Pts',(-0.147344259241144,-0.0498582718677507,
0.539081410518519));
#11441=CARTESIAN_POINT('Ctrl Pts',(-0.146714689743651,-0.0516949516154911,
0.539220859009577));
#11442=CARTESIAN_POINT('Ctrl Pts',(-0.146267742511014,-0.0529463455401811,
0.539316825654902));
#11443=CARTESIAN_POINT('Ctrl Pts',(-0.142400915940452,-0.0633501656378722,
0.540122905774491));
#11444=CARTESIAN_POINT('Ctrl Pts',(-0.138142413652402,-0.0721655577750554,
0.540861584510963));
#11445=CARTESIAN_POINT('Ctrl Pts',(-0.126822870264277,-0.0908744721940083,
0.542548868396242));
#11446=CARTESIAN_POINT('Ctrl Pts',(-0.119372412477284,-0.10046131888096,
0.543500752540934));
#11447=CARTESIAN_POINT('Ctrl Pts',(-0.11015969864138,-0.109825837202611,
0.544469936043691));
#11448=CARTESIAN_POINT('Ctrl Pts',(-0.109426476438798,-0.110556411533628,
0.544545815320775));
#11449=CARTESIAN_POINT('Ctrl Pts',(-0.108397557470002,-0.111561348991582,
0.54465049827888));
#11450=CARTESIAN_POINT('Ctrl Pts',(-0.108108025918828,-0.111841941131645,
0.544679761096987));
#11451=CARTESIAN_POINT('Ctrl Pts',(-0.107641822430754,-0.112290248458939,
0.544726564703862));
#11452=CARTESIAN_POINT('Ctrl Pts',(-0.107465844555686,-0.112458677261316,
0.544744160180144));
#11453=CARTESIAN_POINT('Ctrl Pts',(-0.107097768355951,-0.112809310838233,
0.544780812731165));
#11454=CARTESIAN_POINT('Ctrl Pts',(-0.106905599877627,-0.112991439122484,
0.54479986358994));
#11455=CARTESIAN_POINT('Ctrl Pts',(-0.106440345862733,-0.11343013564948,
0.544845784904675));
#11456=CARTESIAN_POINT('Ctrl Pts',(-0.106166793917122,-0.113686211908599,
0.544872617676915));
#11457=CARTESIAN_POINT('Ctrl Pts',(-0.105210563100172,-0.114574893138384,
0.544965845410856));
#11458=CARTESIAN_POINT('Ctrl Pts',(-0.104523115705746,-0.115202374635666,
0.545031863601993));
#11459=CARTESIAN_POINT('Ctrl Pts',(-0.10046826675944,-0.11883734144804,
0.545415733863223));
#11460=CARTESIAN_POINT('Ctrl Pts',(-0.0969764752657212,-0.121703569171678,
0.545724251167426));
#11461=CARTESIAN_POINT('Ctrl Pts',(-0.0884836528162996,-0.128076870265841,
0.546438066479018));
#11462=CARTESIAN_POINT('Ctrl Pts',(-0.0833912005378006,-0.131449446043761,
0.54683875943586));
#11463=CARTESIAN_POINT('Ctrl Pts',(-0.0688114013467321,-0.13991605661537,
0.547948398322483));
#11464=CARTESIAN_POINT('Ctrl Pts',(-0.058975438721653,-0.144337677161704,
0.548658324127951));
#11465=CARTESIAN_POINT('Ctrl Pts',(-0.0470954517241333,-0.148259582951455,
0.549527651141724));
#11466=CARTESIAN_POINT('Ctrl Pts',(-0.0454189706477286,-0.148781726627143,
0.54965051885225));
#11467=CARTESIAN_POINT('Ctrl Pts',(-0.0430565765930316,-0.149473850905517,
0.549824084939934));
#11468=CARTESIAN_POINT('Ctrl Pts',(-0.0423777519413163,-0.149667721981832,
0.549874007337901));
#11469=CARTESIAN_POINT('Ctrl Pts',(-0.0412792271964498,-0.149973386061135,
0.549954884570839));
#11470=CARTESIAN_POINT('Ctrl Pts',(-0.0408603315021957,-0.150088055577804,
0.549985745957495));
#11471=CARTESIAN_POINT('Ctrl Pts',(-0.0399876933493037,-0.150323009648652,
0.550050082098602));
#11472=CARTESIAN_POINT('Ctrl Pts',(-0.0395338762873895,-0.150442997397799,
0.550083566077444));
#11473=CARTESIAN_POINT('Ctrl Pts',(-0.0384623869174121,-0.150721112702892,
0.550162688381621));
#11474=CARTESIAN_POINT('Ctrl Pts',(-0.037844275835988,-0.15087749926949,
0.5502083822503));
#11475=CARTESIAN_POINT('Ctrl Pts',(-0.0358019864413543,-0.151380873770935,
0.550359536614289));
#11476=CARTESIAN_POINT('Ctrl Pts',(-0.0343739032366468,-0.151711521248621,
0.550465518022388));
#11477=CARTESIAN_POINT('Ctrl Pts',(-0.0268574250332789,-0.153340255712135,
0.551025005229703));
#11478=CARTESIAN_POINT('Ctrl Pts',(-0.0207006495548377,-0.15429199289901,
0.551489350421596));
#11479=CARTESIAN_POINT('Ctrl Pts',(-0.00415077271920622,-0.155841926362421,
0.552753384634826));
#11480=CARTESIAN_POINT('Ctrl Pts',(0.00627339725513827,-0.155770825443758,
0.553567563328912));
#11481=CARTESIAN_POINT('Ctrl Pts',(0.0187372909922365,-0.15443214955363,
0.554531483828088));
#11482=CARTESIAN_POINT('Ctrl Pts',(0.0208585245858162,-0.154159973800621,
0.55469509530889));
#11483=CARTESIAN_POINT('Ctrl Pts',(0.02645734918772,-0.153323901271539,
0.555124793947395));
#11484=CARTESIAN_POINT('Ctrl Pts',(0.0299228350788113,-0.152685424671255,
0.555388573096077));
#11485=CARTESIAN_POINT('Ctrl Pts',(0.0339128536530036,-0.151809211373921,
0.555687567446266));
#11486=CARTESIAN_POINT('Ctrl Pts',(0.0344610902840289,-0.151685699995515,
0.555728545343533));
#11487=CARTESIAN_POINT('Ctrl Pts',(0.0353363367607763,-0.15148352685256,
0.555793785451161));
#11488=CARTESIAN_POINT('Ctrl Pts',(0.0356637747607796,-0.1514067725664,
0.55581815198941));
#11489=CARTESIAN_POINT('Ctrl Pts',(0.0362433417141194,-0.151268932626566,
0.555861206189086));
#11490=CARTESIAN_POINT('Ctrl Pts',(0.0364955696305209,-0.151208277545038,
0.555879918186122));
#11491=CARTESIAN_POINT('Ctrl Pts',(0.0370297634157288,-0.151078401545684,
0.555919493958265));
#11492=CARTESIAN_POINT('Ctrl Pts',(0.037311687081137,-0.15100902225746,
0.555940348468868));
#11493=CARTESIAN_POINT('Ctrl Pts',(0.0380716396381659,-0.150819745517151,
0.555996482087961));
#11494=CARTESIAN_POINT('Ctrl Pts',(0.038549301225703,-0.150698363545474,
0.556031677021169));
#11495=CARTESIAN_POINT('Ctrl Pts',(0.0409102182154071,-0.150086454293043,
0.556205237886987));
#11496=CARTESIAN_POINT('Ctrl Pts',(0.0427848393735488,-0.149562856959651,
0.556341801440567));
#11497=CARTESIAN_POINT('Ctrl Pts',(0.0481602952309036,-0.147952096144847,
0.556731115449568));
#11498=CARTESIAN_POINT('Ctrl Pts',(0.051633341615043,-0.146776153148321,
0.556979838778363));
#11499=CARTESIAN_POINT('Ctrl Pts',(0.064024622280468,-0.142086203195988,
0.557867870622627));
#11500=CARTESIAN_POINT('Ctrl Pts',(0.0726549765943762,-0.137872806403243,
0.558488735123943));
#11501=CARTESIAN_POINT('Ctrl Pts',(0.0875190128081615,-0.128830465016337,
0.559644579137773));
#11502=CARTESIAN_POINT('Ctrl Pts',(0.0938785881956358,-0.124272480144846,
0.560172389791356));
#11503=CARTESIAN_POINT('Ctrl Pts',(0.100654469344356,-0.118598194769974,
0.560791343911244));
#11504=CARTESIAN_POINT('Ctrl Pts',(0.101434094282203,-0.1179320924507,0.560863461331539));
#11505=CARTESIAN_POINT('Ctrl Pts',(0.102666203566894,-0.116858136747144,
0.560978917589372));
#11506=CARTESIAN_POINT('Ctrl Pts',(0.103122986361702,-0.116455240945192,
0.561022051956307));
#11507=CARTESIAN_POINT('Ctrl Pts',(0.103925401992304,-0.115739063921458,
0.561098419233729));
#11508=CARTESIAN_POINT('Ctrl Pts',(0.104272016163796,-0.115426889125279,
0.561131605613918));
#11509=CARTESIAN_POINT('Ctrl Pts',(0.104986945006736,-0.114777147043085,
0.561200472242016));
#11510=CARTESIAN_POINT('Ctrl Pts',(0.105355047501936,-0.114439355382329,
0.56123616174279));
#11511=CARTESIAN_POINT('Ctrl Pts',(0.106297601602329,-0.113566012527091,
0.561328150041716));
#11512=CARTESIAN_POINT('Ctrl Pts',(0.106869629941809,-0.113027879135312,
0.561384558662525));
#11513=CARTESIAN_POINT('Ctrl Pts',(0.109254497547434,-0.110750034851705,
0.561622220382414));
#11514=CARTESIAN_POINT('Ctrl Pts',(0.111029027113239,-0.108970955866384,
0.561805171668631));
#11515=CARTESIAN_POINT('Ctrl Pts',(0.11554913318028,-0.10421419968529,0.562287871917499));
#11516=CARTESIAN_POINT('Ctrl Pts',(0.118222720882528,-0.101171066098921,
0.56259044114648));
#11517=CARTESIAN_POINT('Ctrl Pts',(0.125839483265111,-0.0917868518480665,
0.563505312772759));
#11518=CARTESIAN_POINT('Ctrl Pts',(0.13041291285108,-0.0851636777831778,
0.564128483714476));
#11519=CARTESIAN_POINT('Ctrl Pts',(0.136261706820665,-0.0751097640991976,
0.565030292753454));
#11520=CARTESIAN_POINT('Ctrl Pts',(0.137961396377216,-0.071940141979813,
0.565308622955537));
#11521=CARTESIAN_POINT('Ctrl Pts',(0.140106264183853,-0.0675842011487671,
0.565681164445715));
#11522=CARTESIAN_POINT('Ctrl Pts',(0.140649029198706,-0.0664472740911736,
0.565777506874568));
#11523=CARTESIAN_POINT('Ctrl Pts',(0.142826587703963,-0.061739692689556,
0.566172457221779));
#11524=CARTESIAN_POINT('Ctrl Pts',(0.144339862352576,-0.0581139789411102,
0.566467360911001));
#11525=CARTESIAN_POINT('Ctrl Pts',(0.145936017904574,-0.0538412687175233,
0.56680132077099));
#11526=CARTESIAN_POINT('Ctrl Pts',(0.14615401237522,-0.0532466735353458,
0.566847494981841));
#11527=CARTESIAN_POINT('Ctrl Pts',(0.146478284494606,-0.0523452014197282,
0.566917029975448));
#11528=CARTESIAN_POINT('Ctrl Pts',(0.14658723892096,-0.0520393056345255,
0.566940543688161));
#11529=CARTESIAN_POINT('Ctrl Pts',(0.146780922706548,-0.0514900923321722,
0.566982611944645));
#11530=CARTESIAN_POINT('Ctrl Pts',(0.146866005739974,-0.0512469046910303,
0.567001187083172));
#11531=CARTESIAN_POINT('Ctrl Pts',(0.147049308861439,-0.0507187746132098,
0.567041412837719));
#11532=CARTESIAN_POINT('Ctrl Pts',(0.147147304892852,-0.0504337585538178,
0.567063050118036));
#11533=CARTESIAN_POINT('Ctrl Pts',(0.147419539488799,-0.0496344310634207,
0.567123536955249));
#11534=CARTESIAN_POINT('Ctrl Pts',(0.147591916549682,-0.0491194825170829,
0.567162278622683));
#11535=CARTESIAN_POINT('Ctrl Pts',(0.148591637926296,-0.0460801946676753,
0.567389669026069));
#11536=CARTESIAN_POINT('Ctrl Pts',(0.149356968406698,-0.0435357033627789,
0.567574902170907));
#11537=CARTESIAN_POINT('Ctrl Pts',(0.15391810093453,-0.0268311733729513,
0.568765389268736));
#11538=CARTESIAN_POINT('Ctrl Pts',(0.155761446085182,-0.0122135808111399,
0.569694930178027));
#11539=CARTESIAN_POINT('Ctrl Pts',(0.155499901656167,0.00440750625721281,
0.570811857355879));
#11540=CARTESIAN_POINT('Ctrl Pts',(0.155432007072187,0.00636680891806572,
0.570944334246211));
#11541=CARTESIAN_POINT('Ctrl Pts',(0.155115349972588,0.0122755013757389,
0.571347068131));
#11542=CARTESIAN_POINT('Ctrl Pts',(0.154752922132215,0.0162169124391543,
0.571620108153867));
#11543=CARTESIAN_POINT('Ctrl Pts',(0.154128797092813,0.0209967378612288,
0.571958550284801));
#11544=CARTESIAN_POINT('Ctrl Pts',(0.154009787734688,0.0218525587142995,
0.572019433297928));
#11545=CARTESIAN_POINT('Ctrl Pts',(0.15380090287758,0.0232681354354257,
0.572120631130542));
#11546=CARTESIAN_POINT('Ctrl Pts',(0.153715085226818,0.0238284789878695,
0.572160817886219));
#11547=CARTESIAN_POINT('Ctrl Pts',(0.153554047141098,0.0248428848968651,
0.572233807818604));
#11548=CARTESIAN_POINT('Ctrl Pts',(0.153479870395448,0.025297108499979,
0.572266577654775));
#11549=CARTESIAN_POINT('Ctrl Pts',(0.153316167097562,0.0262723209686628,
0.57233712428238));
#11550=CARTESIAN_POINT('Ctrl Pts',(0.153225998612155,0.0267931946422494,
0.572374921028864));
#11551=CARTESIAN_POINT('Ctrl Pts',(0.152972231815096,0.0282159337340021,
0.572478486498202));
#11552=CARTESIAN_POINT('Ctrl Pts',(0.152803316620583,0.0291168162049528,
0.572544423001337));
#11553=CARTESIAN_POINT('Ctrl Pts',(0.151857865829933,0.0339242571912706,
0.572898255308876));
#11554=CARTESIAN_POINT('Ctrl Pts',(0.150939529743546,0.0378010532882317,
0.573190622452226));
#11555=CARTESIAN_POINT('Ctrl Pts',(0.145928221523231,0.0558389479353133,
0.574585869721996));
#11556=CARTESIAN_POINT('Ctrl Pts',(0.139984618828454,0.0694060379413062,
0.575747797526563));
#11557=CARTESIAN_POINT('Ctrl Pts',(0.129906718422113,0.0856703163387146,
0.577209533666793));
#11558=CARTESIAN_POINT('Ctrl Pts',(0.12743150627182,0.0893105743709335,
0.577540981851726));
#11559=CARTESIAN_POINT('Ctrl Pts',(0.124411527018555,0.0933702791090407,
0.577911595776505));
#11560=CARTESIAN_POINT('Ctrl Pts',(0.12401469572336,0.0938967111370229,
0.577959672801102));
#11561=CARTESIAN_POINT('Ctrl Pts',(0.123416798135735,0.0946794726338518,
0.578031168012147));
#11562=CARTESIAN_POINT('Ctrl Pts',(0.123218261005705,0.0949377098961141,
0.57805475607818));
#11563=CARTESIAN_POINT('Ctrl Pts',(0.122861192975882,0.0953991413846882,
0.578096904140811));
#11564=CARTESIAN_POINT('Ctrl Pts',(0.122702967686102,0.0956025660792466,
0.578115485075473));
#11565=CARTESIAN_POINT('Ctrl Pts',(0.122359070869421,0.0960424419440706,
0.57815566268024));
#11566=CARTESIAN_POINT('Ctrl Pts',(0.122173219725323,0.0962787477314077,
0.578177246283805));
#11567=CARTESIAN_POINT('Ctrl Pts',(0.121651912165297,0.0969376390825866,
0.578237432017959));
#11568=CARTESIAN_POINT('Ctrl Pts',(0.121314935987773,0.0973590259488018,
0.578275927983178));
#11569=CARTESIAN_POINT('Ctrl Pts',(0.119342324291338,0.099799622042576,
0.578498975345491));
#11570=CARTESIAN_POINT('Ctrl Pts',(0.117658365088442,0.101779497897026,
0.578680261555918));
#11571=CARTESIAN_POINT('Ctrl Pts',(0.106120526202603,0.114675522262285,
0.57987074767686));
#11572=CARTESIAN_POINT('Ctrl Pts',(0.0948102604855902,0.124190034508338,
0.580802968658051));
#11573=CARTESIAN_POINT('Ctrl Pts',(0.0805585735780984,0.133080732784228,
0.581931485852659));
#11574=CARTESIAN_POINT('Ctrl Pts',(0.0787643933659321,0.134150419339113,
0.58207267139487));
#11575=CARTESIAN_POINT('Ctrl Pts',(0.0735939059578258,0.13709356614276,
0.582477920900257));
#11576=CARTESIAN_POINT('Ctrl Pts',(0.0701688606252284,0.138877772169655,
0.582744481637431));
#11577=CARTESIAN_POINT('Ctrl Pts',(0.0658383334649136,0.140932561071735,
0.583081059724209));
#11578=CARTESIAN_POINT('Ctrl Pts',(0.0649918760668528,0.141324905453235,
0.583146824538289));
#11579=CARTESIAN_POINT('Ctrl Pts',(0.0636582524998469,0.14192854291008,
0.583250426735509));
#11580=CARTESIAN_POINT('Ctrl Pts',(0.0631734360664162,0.142145001202198,
0.58328808694569));
#11581=CARTESIAN_POINT('Ctrl Pts',(0.0623023098357494,0.142528600130034,
0.583355755340711));
#11582=CARTESIAN_POINT('Ctrl Pts',(0.0619164099142628,0.142696663741093,
0.583385731702458));
#11583=CARTESIAN_POINT('Ctrl Pts',(0.0610514947559166,0.143069174672798,
0.583452920093837));
#11584=CARTESIAN_POINT('Ctrl Pts',(0.0605721272073822,0.143272785785984,
0.583490160102854));
#11585=CARTESIAN_POINT('Ctrl Pts',(0.0592464988251205,0.143828003738642,
0.583593152954099));
#11586=CARTESIAN_POINT('Ctrl Pts',(0.0583981514064706,0.144174540498715,
0.583659075957717));
#11587=CARTESIAN_POINT('Ctrl Pts',(0.0538488911843001,0.145986103479568,
0.584012702045417));
#11588=CARTESIAN_POINT('Ctrl Pts',(0.0500961601432995,0.147316037378406,
0.584304870274994));
#11589=CARTESIAN_POINT('Ctrl Pts',(0.032224297022644,0.152887810891637,
0.585700026177644));
#11590=CARTESIAN_POINT('Ctrl Pts',(0.017600403115368,0.155251960987593,
0.586862094208258));
#11591=CARTESIAN_POINT('Ctrl Pts',(-0.00153278850207716,0.155604688009956,
0.58832406579133));
#11592=CARTESIAN_POINT('Ctrl Pts',(-0.0059346966032725,0.155499056735746,
0.588655600127666));
#11593=CARTESIAN_POINT('Ctrl Pts',(-0.0109844704383491,0.155163070780574,
0.589026298474553));
#11594=CARTESIAN_POINT('Ctrl Pts',(-0.0116420078729264,0.155115121181916,
0.589074378230013));
#11595=CARTESIAN_POINT('Ctrl Pts',(-0.0126239542045381,0.155037235480348,
0.589145876694541));
#11596=CARTESIAN_POINT('Ctrl Pts',(-0.0129485945608784,0.155010459354629,
0.589169465305529));
#11597=CARTESIAN_POINT('Ctrl Pts',(-0.0135299268060048,0.154960672421424,
0.58921161395427));
#11598=CARTESIAN_POINT('Ctrl Pts',(-0.0137866466142657,0.154938043408745,
0.589230194932599));
#11599=CARTESIAN_POINT('Ctrl Pts',(-0.0143427124966196,0.154887634992414,
0.589270372189876));
#11600=CARTESIAN_POINT('Ctrl Pts',(-0.0146420338248949,0.154859625871129,
0.589291955404241));
#11601=CARTESIAN_POINT('Ctrl Pts',(-0.0154782965400792,0.154778925934398,
0.589352138956825));
#11602=CARTESIAN_POINT('Ctrl Pts',(-0.0160150549304179,0.154724308419198,
0.589390633142117));
#11603=CARTESIAN_POINT('Ctrl Pts',(-0.0191349079331047,0.154390440360469,
0.589613649436506));
#11604=CARTESIAN_POINT('Ctrl Pts',(-0.0217111616717617,0.154049279045929,
0.589794907421937));
#11605=CARTESIAN_POINT('Ctrl Pts',(-0.0378786016877545,0.151494597106192,
0.590921004805059));
#11606=CARTESIAN_POINT('Ctrl Pts',(-0.0511309123138129,0.14754961718002,
0.591797849353644));
#11607=CARTESIAN_POINT('Ctrl Pts',(-0.0636886259076391,0.141913922608026,
0.592717731153444));
#11608=CARTESIAN_POINT('Origin',(0.,0.,-0.129405622560373));
#11609=CARTESIAN_POINT('',(-0.0636886255638827,0.141913922762298,0.676466729580158));
#11610=CARTESIAN_POINT('',(-0.063688650901166,0.141913911391341,0.662679920979917));
#11611=CARTESIAN_POINT('',(-0.0636886258329924,0.141913922641526,-0.129405622560373));
#11612=CARTESIAN_POINT('Ctrl Pts',(-0.0636886255638827,0.141913922762298,
0.676466729580158));
#11613=CARTESIAN_POINT('Ctrl Pts',(-0.0607908715473581,0.143214386923548,
0.676246520920293));
#11614=CARTESIAN_POINT('Ctrl Pts',(-0.0578533659458898,0.144426060804552,
0.676030425544921));
#11615=CARTESIAN_POINT('Ctrl Pts',(-0.0408568520024256,0.15083479002351,
0.674809111787695));
#11616=CARTESIAN_POINT('Ctrl Pts',(-0.0261433107887304,0.154068097680774,
0.67385525957657));
#11617=CARTESIAN_POINT('Ctrl Pts',(-0.0078701255115844,0.155386513139834,
0.672601056777744));
#11618=CARTESIAN_POINT('Ctrl Pts',(-0.00453975603769017,0.155519436523196,
0.67237013173076));
#11619=CARTESIAN_POINT('Ctrl Pts',(-0.000341490133210229,0.155552038151604,
0.672074937499572));
#11620=CARTESIAN_POINT('Ctrl Pts',(0.000524931679086567,0.15555152709313,
0.672013798845211));
#11621=CARTESIAN_POINT('Ctrl Pts',(0.00190891973239365,0.155539147769742,
0.671915771196146));
#11622=CARTESIAN_POINT('Ctrl Pts',(0.00242651880768871,0.155531933885506,
0.671879027710959));
#11623=CARTESIAN_POINT('Ctrl Pts',(0.00340580789169315,0.155513395738248,
0.671809349983256));
#11624=CARTESIAN_POINT('Ctrl Pts',(0.00386750335110679,0.15550259866258,
0.671776432571904));
#11625=CARTESIAN_POINT('Ctrl Pts',(0.00491255867777641,0.155473502273566,
0.671701767952502));
#11626=CARTESIAN_POINT('Ctrl Pts',(0.0054958745005055,0.155453975466281,
0.671659982850067));
#11627=CARTESIAN_POINT('Ctrl Pts',(0.00721718720756023,0.1553866533049,
0.671536346550711));
#11628=CARTESIAN_POINT('Ctrl Pts',(0.00835476284272535,0.155329641813805,
0.671454209125888));
#11629=CARTESIAN_POINT('Ctrl Pts',(0.0198533780149537,0.154626692247295,
0.670619448973276));
#11630=CARTESIAN_POINT('Ctrl Pts',(0.0301234881892788,0.152957712150837,
0.669834050183851));
#11631=CARTESIAN_POINT('Ctrl Pts',(0.0470126485828665,0.148445566887118,
0.668483817470187));
#11632=CARTESIAN_POINT('Ctrl Pts',(0.0537426513860412,0.146143778992174,
0.667929810837915));
#11633=CARTESIAN_POINT('Ctrl Pts',(0.0635997597744231,0.141999121179274,
0.667109106033747));
#11634=CARTESIAN_POINT('Ctrl Pts',(0.0668588781187584,0.140494036329267,
0.66683623820975));
#11635=CARTESIAN_POINT('Ctrl Pts',(0.0712011965062588,0.138303350058065,
0.666473088430787));
#11636=CARTESIAN_POINT('Ctrl Pts',(0.0723320966343983,0.137715268133416,
0.66637855216442));
#11637=CARTESIAN_POINT('Ctrl Pts',(0.0739984014708397,0.136822579119382,
0.666239454945605));
#11638=CARTESIAN_POINT('Ctrl Pts',(0.0745393992203288,0.136528603499958,
0.666194325393266));
#11639=CARTESIAN_POINT('Ctrl Pts',(0.0755172149347744,0.13598971838742,
0.666112832243787));
#11640=CARTESIAN_POINT('Ctrl Pts',(0.0759546196334397,0.135745898772536,
0.666076405632637));
#11641=CARTESIAN_POINT('Ctrl Pts',(0.0766436851665365,0.135357424138557,
0.666019073651056));
#11642=CARTESIAN_POINT('Ctrl Pts',(0.0768961263943522,0.135214172684108,
0.665998081143176));
#11643=CARTESIAN_POINT('Ctrl Pts',(0.0771487200101584,0.135069898575509,
0.665977088361396));
#11644=CARTESIAN_POINT('Ctrl Pts',(0.0771492720245886,0.135069583276473,
0.665977042484134));
#11645=CARTESIAN_POINT('Ctrl Pts',(0.0771501308440659,0.135069092729863,
0.665976971108763));
#11646=CARTESIAN_POINT('Ctrl Pts',(0.0771504376505049,0.135068917484595,
0.665976945610496));
#11647=CARTESIAN_POINT('Ctrl Pts',(0.0771510513544071,0.135068566939294,
0.665976894606436));
#11648=CARTESIAN_POINT('Ctrl Pts',(0.0771513582558655,0.135068391636978,
0.665976869100309));
#11649=CARTESIAN_POINT('Ctrl Pts',(0.0771519721411672,0.135068040982512,
0.665976818081246));
#11650=CARTESIAN_POINT('Ctrl Pts',(0.0771522791404123,0.135067865621564,
0.665976792567029));
#11651=CARTESIAN_POINT('Ctrl Pts',(0.0771528932496153,0.135067514833651,
0.665976741529432));
#11652=CARTESIAN_POINT('Ctrl Pts',(0.0771532003271718,0.135067339425193,
0.665976716008743));
#11653=CARTESIAN_POINT('Ctrl Pts',(0.0773655494028303,0.134946040691334,
0.665959068054596));
#11654=CARTESIAN_POINT('Ctrl Pts',(0.077577303495344,0.134824419585031,
0.665941478558442));
#11655=CARTESIAN_POINT('Ctrl Pts',(0.0780710238609456,0.134539302677585,
0.665900487357142));
#11656=CARTESIAN_POINT('Ctrl Pts',(0.0783527630941476,0.134375419078258,
0.665877110976581));
#11657=CARTESIAN_POINT('Ctrl Pts',(0.0792033740451375,0.133877046316535,
0.665806573386037));
#11658=CARTESIAN_POINT('Ctrl Pts',(0.079770644310064,0.133539815554879,
0.665759585052068));
#11659=CARTESIAN_POINT('Ctrl Pts',(0.0841173711352894,0.130918191637871,
0.665399805444364));
#11660=CARTESIAN_POINT('Ctrl Pts',(0.0878005854559817,0.128477123788497,
0.665096507782301));
#11661=CARTESIAN_POINT('Ctrl Pts',(0.103336613985805,0.117199850045557,
0.663800907098825));
#11662=CARTESIAN_POINT('Ctrl Pts',(0.113999507537604,0.106857014813201,
0.662861121678506));
#11663=CARTESIAN_POINT('Ctrl Pts',(0.12544618821654,0.0920569741290184,
0.661586645131116));
#11664=CARTESIAN_POINT('Ctrl Pts',(0.12773062221633,0.0888600938032811,
0.661315370790834));
#11665=CARTESIAN_POINT('Ctrl Pts',(0.13039374320141,0.0848180855891804,
0.660975279324153));
#11666=CARTESIAN_POINT('Ctrl Pts',(0.130889278264255,0.0840513692992772,
0.660910894952173));
#11667=CARTESIAN_POINT('Ctrl Pts',(0.131660672036104,0.0828344652946929,
0.660808882154693));
#11668=CARTESIAN_POINT('Ctrl Pts',(0.131941042702394,0.0823871497247103,
0.660771420850201));
#11669=CARTESIAN_POINT('Ctrl Pts',(0.132461689178739,0.0815470136505976,
0.660701126512285));
#11670=CARTESIAN_POINT('Ctrl Pts',(0.132702508990537,0.0811545355150301,
0.660668313917629));
#11671=CARTESIAN_POINT('Ctrl Pts',(0.133236610303401,0.0802753453795863,
0.660594865223563));
#11672=CARTESIAN_POINT('Ctrl Pts',(0.133528973289228,0.0797880860619735,
0.660554196181564));
#11673=CARTESIAN_POINT('Ctrl Pts',(0.134261236267001,0.0785523813350681,
0.660451145471877));
#11674=CARTESIAN_POINT('Ctrl Pts',(0.1346975474557,0.0778018433584267,0.660388635116091));
#11675=CARTESIAN_POINT('Ctrl Pts',(0.137115563779064,0.0735610862337354,
0.660035837665069));
#11676=CARTESIAN_POINT('Ctrl Pts',(0.138967708229039,0.0699991558691533,
0.659740983235701));
#11677=CARTESIAN_POINT('Ctrl Pts',(0.141494432897997,0.0646434225112803,
0.659299267926378));
#11678=CARTESIAN_POINT('Ctrl Pts',(0.142277062937266,0.0629021736573755,
0.659155914057853));
#11679=CARTESIAN_POINT('Ctrl Pts',(0.148813127614827,0.0476138338661142,
0.65789966310097));
#11680=CARTESIAN_POINT('Ctrl Pts',(0.15264810577264,0.0333301975951108,
0.656732500227976));
#11681=CARTESIAN_POINT('Ctrl Pts',(0.154731474706446,0.0161463172334283,
0.655430319233572));
#11682=CARTESIAN_POINT('Ctrl Pts',(0.154979265361752,0.0135632696176046,
0.655237493306741));
#11683=CARTESIAN_POINT('Ctrl Pts',(0.155200396084705,0.0104369779531962,
0.655008542478591));
#11684=CARTESIAN_POINT('Ctrl Pts',(0.155235656017167,0.00989871596476052,
0.654969281737277));
#11685=CARTESIAN_POINT('Ctrl Pts',(0.155286208205535,0.00906015656793316,
0.654908374939859));
#11686=CARTESIAN_POINT('Ctrl Pts',(0.155303430507879,0.00875998701815042,
0.654886624195271));
#11687=CARTESIAN_POINT('Ctrl Pts',(0.155333803735065,0.008202340025924,
0.654846313948852));
#11688=CARTESIAN_POINT('Ctrl Pts',(0.155347184752105,0.00794488238741016,
0.6548277422226));
#11689=CARTESIAN_POINT('Ctrl Pts',(0.155376033967548,0.00736184781897832,
0.654785772137834));
#11690=CARTESIAN_POINT('Ctrl Pts',(0.155391118953179,0.00703625543535908,
0.654762395417264));
#11691=CARTESIAN_POINT('Ctrl Pts',(0.155433651256396,0.00605128740409831,
0.654691855786703));
#11692=CARTESIAN_POINT('Ctrl Pts',(0.155457926377431,0.00539177058821119,
0.654644865767439));
#11693=CARTESIAN_POINT('Ctrl Pts',(0.155612369792172,0.000317377488226763,
0.654285041866687));
#11694=CARTESIAN_POINT('Ctrl Pts',(0.15555865896183,-0.00410159738035948,
0.653981704214066));
#11695=CARTESIAN_POINT('Ctrl Pts',(0.154507946121226,-0.0232720049461217,
0.652685998820199));
#11696=CARTESIAN_POINT('Ctrl Pts',(0.151599564718293,-0.0378406168766032,
0.651746148175031));
#11697=CARTESIAN_POINT('Ctrl Pts',(0.145371370846084,-0.0554831997448552,
0.650471686413573));
#11698=CARTESIAN_POINT('Ctrl Pts',(0.143924621975196,-0.0591347580392705,
0.650200512720392));
#11699=CARTESIAN_POINT('Ctrl Pts',(0.141973291618426,-0.0635627263621239,
0.649860532849883));
#11700=CARTESIAN_POINT('Ctrl Pts',(0.141597853050832,-0.0643947487261666,
0.64979615587648));
#11701=CARTESIAN_POINT('Ctrl Pts',(0.140993768041352,-0.0657026525380222,
0.649694152158946));
#11702=CARTESIAN_POINT('Ctrl Pts',(0.140769980015533,-0.0661807667752452,
0.649656692485117));
#11703=CARTESIAN_POINT('Ctrl Pts',(0.140346437926841,-0.0670737795170796,
0.64958639960946));
#11704=CARTESIAN_POINT('Ctrl Pts',(0.140147266288204,-0.0674889493252753,
0.649553586838374));
#11705=CARTESIAN_POINT('Ctrl Pts',(0.139698183198175,-0.0684144944302647,
0.649480135678284));
#11706=CARTESIAN_POINT('Ctrl Pts',(0.139447313508257,-0.0689243946400924,
0.649439464336476));
#11707=CARTESIAN_POINT('Ctrl Pts',(0.138806098136054,-0.0702098531222488,
0.64933640391563));
#11708=CARTESIAN_POINT('Ctrl Pts',(0.138412046943202,-0.0709835301980151,
0.649273886106094));
#11709=CARTESIAN_POINT('Ctrl Pts',(0.136159428374096,-0.0753162225599389,
0.648920971943723));
#11710=CARTESIAN_POINT('Ctrl Pts',(0.134170251038917,-0.0788052127745625,
0.648626004718085));
#11711=CARTESIAN_POINT('Ctrl Pts',(0.131040288860471,-0.0838324767647021,
0.648184272473799));
#11712=CARTESIAN_POINT('Ctrl Pts',(0.130002392221593,-0.0854331256406525,
0.648041018957942));
#11713=CARTESIAN_POINT('Ctrl Pts',(0.120701593641929,-0.0992148007876205,
0.64678479714447));
#11714=CARTESIAN_POINT('Ctrl Pts',(0.110779271900926,-0.110183149655123,
0.645617555706887));
#11715=CARTESIAN_POINT('Ctrl Pts',(0.0974710130631162,-0.121251509081323,
0.644315407048281));
#11716=CARTESIAN_POINT('Ctrl Pts',(0.0954359874559907,-0.122859681293083,
0.644122668569318));
#11717=CARTESIAN_POINT('Ctrl Pts',(0.0929301613535089,-0.124740043644849,
0.643893807547915));
#11718=CARTESIAN_POINT('Ctrl Pts',(0.0924970894832599,-0.125061512217034,
0.643854551980029));
#11719=CARTESIAN_POINT('Ctrl Pts',(0.0918200125798306,-0.125558664282855,
0.643793651447691));
#11720=CARTESIAN_POINT('Ctrl Pts',(0.0915771612033927,-0.125735899554454,
0.643771901828927));
#11721=CARTESIAN_POINT('Ctrl Pts',(0.0911251070491711,-0.126063808568441,
0.643731592602523));
#11722=CARTESIAN_POINT('Ctrl Pts',(0.0909160456278558,-0.126214664816518,
0.643713020775984));
#11723=CARTESIAN_POINT('Ctrl Pts',(0.0904418049924492,-0.126555081518211,
0.643671049107775));
#11724=CARTESIAN_POINT('Ctrl Pts',(0.0901764049153119,-0.126744328276266,
0.64364767091093));
#11725=CARTESIAN_POINT('Ctrl Pts',(0.0893717952875931,-0.127314258299297,
0.643577122422535));
#11726=CARTESIAN_POINT('Ctrl Pts',(0.088830746239289,-0.127692351859156,
0.643530125085603));
#11727=CARTESIAN_POINT('Ctrl Pts',(0.0846483040597585,-0.130575659077068,
0.643170071970541));
#11728=CARTESIAN_POINT('Ctrl Pts',(0.0809036065800154,-0.1329283780899,
0.642866526092058));
#11729=CARTESIAN_POINT('Ctrl Pts',(0.0642187845658998,-0.142444373853295,
0.641570277701066));
#11730=CARTESIAN_POINT('Ctrl Pts',(0.0503953289308302,-0.147901356878928,
0.640630089722447));
#11731=CARTESIAN_POINT('Ctrl Pts',(0.032196106401791,-0.152231965299856,
0.639355703699344));
#11732=CARTESIAN_POINT('Ctrl Pts',(0.028351012720224,-0.152994693151566,
0.639085049759057));
#11733=CARTESIAN_POINT('Ctrl Pts',(0.0235805968941704,-0.153754967936899,
0.638745646210428));
#11734=CARTESIAN_POINT('Ctrl Pts',(0.0226784799631589,-0.153890614393438,
0.63868130749526));
#11735=CARTESIAN_POINT('Ctrl Pts',(0.0212526578672108,-0.154092198320615,
0.638579350730771));
#11736=CARTESIAN_POINT('Ctrl Pts',(0.0207297100636731,-0.154163420297706,
0.638541899489654));
#11737=CARTESIAN_POINT('Ctrl Pts',(0.0197498307992688,-0.154291797356417,
0.638471614171795));
#11738=CARTESIAN_POINT('Ctrl Pts',(0.0192929870464523,-0.154349587594285,
0.638438800484267));
#11739=CARTESIAN_POINT('Ctrl Pts',(0.0182716410912885,-0.154474181517958,
0.638365336552078));
#11740=CARTESIAN_POINT('Ctrl Pts',(0.0177070182382793,-0.154539920774733,
0.638324653301721));
#11741=CARTESIAN_POINT('Ctrl Pts',(0.0162785674698841,-0.154698304831259,
0.638221542592591));
#11742=CARTESIAN_POINT('Ctrl Pts',(0.0154143100420053,-0.154786809081192,
0.638158986183661));
#11743=CARTESIAN_POINT('Ctrl Pts',(0.0105441372580052,-0.155244346647751,
0.637805467043103));
#11744=CARTESIAN_POINT('Ctrl Pts',(0.00652618807877941,-0.155465074350251,
0.637509915072673));
#11745=CARTESIAN_POINT('Ctrl Pts',(0.000604153676276382,-0.155560437911898,
0.637068094691197));
#11746=CARTESIAN_POINT('Ctrl Pts',(-0.00129654682107055,-0.155556206215626,
0.636925361052969));
#11747=CARTESIAN_POINT('Ctrl Pts',(-0.0179173481626891,-0.155214568757071,
0.635669287651216));
#11748=CARTESIAN_POINT('Ctrl Pts',(-0.0325182388025824,-0.152823689406662,
0.634501636400603));
#11749=CARTESIAN_POINT('Ctrl Pts',(-0.0490328363497881,-0.147642394584557,
0.633199655730459));
#11750=CARTESIAN_POINT('Ctrl Pts',(-0.0514818191483435,-0.146806403639578,
0.633007372754232));
#11751=CARTESIAN_POINT('Ctrl Pts',(-0.0544145526411711,-0.145722851476748,
0.632778979587384));
#11752=CARTESIAN_POINT('Ctrl Pts',(-0.0549191492589548,-0.14553343275501,
0.632739751012789));
#11753=CARTESIAN_POINT('Ctrl Pts',(-0.0557035989922428,-0.14523430000448,
0.63267888317044));
#11754=CARTESIAN_POINT('Ctrl Pts',(-0.0559841291480127,-0.145126393623628,
0.632657139426609));
#11755=CARTESIAN_POINT('Ctrl Pts',(-0.0565047083184651,-0.144924417913407,
0.632616835520038));
#11756=CARTESIAN_POINT('Ctrl Pts',(-0.0567448338330358,-0.144830565851271,
0.632598263167226));
#11757=CARTESIAN_POINT('Ctrl Pts',(-0.0572881290252687,-0.144616662567373,
0.632556283222664));
#11758=CARTESIAN_POINT('Ctrl Pts',(-0.0575911546703196,-0.144496255066921,
0.632532897311704));
#11759=CARTESIAN_POINT('Ctrl Pts',(-0.0585069326082267,-0.144129031471325,
0.632462302527958));
#11760=CARTESIAN_POINT('Ctrl Pts',(-0.0591185042088403,-0.143879259720847,
0.632415266943923));
#11761=CARTESIAN_POINT('Ctrl Pts',(-0.0638248048292751,-0.141922086362662,
0.632054009768443));
#11762=CARTESIAN_POINT('Ctrl Pts',(-0.0678468677682815,-0.140043907651936,
0.63174937006357));
#11763=CARTESIAN_POINT('Ctrl Pts',(-0.0849274118718202,-0.131158857950281,
0.630450232114783));
#11764=CARTESIAN_POINT('Ctrl Pts',(-0.0970271056562661,-0.122478979117119,
0.629508238081551));
#11765=CARTESIAN_POINT('Ctrl Pts',(-0.11051456227126,-0.109532521859507,
0.628234236968684));
#11766=CARTESIAN_POINT('Ctrl Pts',(-0.113210666198235,-0.106743536275944,
0.627966343848601));
#11767=CARTESIAN_POINT('Ctrl Pts',(-0.116406710207291,-0.103179974764915,
0.627630002365092));
#11768=CARTESIAN_POINT('Ctrl Pts',(-0.117007885388992,-0.102497727134985,
0.627565868316161));
#11769=CARTESIAN_POINT('Ctrl Pts',(-0.117948050701247,-0.101411723703796,
0.627464162743053));
#11770=CARTESIAN_POINT('Ctrl Pts',(-0.118291036434266,-0.1010114402217,
0.627426756627974));
#11771=CARTESIAN_POINT('Ctrl Pts',(-0.118929859962621,-0.100258181788982,
0.627356511638086));
#11772=CARTESIAN_POINT('Ctrl Pts',(-0.119226178431301,-0.099905620335656,
0.627323692929973));
#11773=CARTESIAN_POINT('Ctrl Pts',(-0.119885291193279,-0.09911429557228,
0.627250160092359));
#11774=CARTESIAN_POINT('Ctrl Pts',(-0.120247249493325,-0.0986748478825366,
0.627209412672188));
#11775=CARTESIAN_POINT('Ctrl Pts',(-0.121157242471216,-0.0975575976021249,
0.627106030886133));
#11776=CARTESIAN_POINT('Ctrl Pts',(-0.121702001186741,-0.0968771650223936,
0.627043266383169));
#11777=CARTESIAN_POINT('Ctrl Pts',(-0.124753527481387,-0.0929992869566213,
0.626686628009328));
#11778=CARTESIAN_POINT('Ctrl Pts',(-0.12713975376476,-0.089709460591384,
0.626388070035682));
#11779=CARTESIAN_POINT('Ctrl Pts',(-0.130429154726752,-0.0847792123557415,
0.625945803074513));
#11780=CARTESIAN_POINT('Ctrl Pts',(-0.131435999614898,-0.0832097155762332,
0.62580574826096));
#11781=CARTESIAN_POINT('Ctrl Pts',(-0.14015403988719,-0.069066643317702,
0.624550365582026));
#11782=CARTESIAN_POINT('Ctrl Pts',(-0.146067498189948,-0.0554758003983858,
0.623380521592489));
#11783=CARTESIAN_POINT('Ctrl Pts',(-0.150656624586409,-0.0387932093447793,
0.622079420292723));
#11784=CARTESIAN_POINT('Ctrl Pts',(-0.151273595703449,-0.036312985647016,
0.621889556083399));
#11785=CARTESIAN_POINT('Ctrl Pts',(-0.151945968216113,-0.0332943479732488,
0.621663649105777));
#11786=CARTESIAN_POINT('Ctrl Pts',(-0.152060004988231,-0.0327695860510881,
0.621624565164134));
#11787=CARTESIAN_POINT('Ctrl Pts',(-0.152233539435988,-0.0319506189485235,
0.621563872501541));
#11788=CARTESIAN_POINT('Ctrl Pts',(-0.152294905531702,-0.031656821281618,
0.621542160257309));
#11789=CARTESIAN_POINT('Ctrl Pts',(-0.152407413130354,-0.0311102782967215,
0.621501884788927));
#11790=CARTESIAN_POINT('Ctrl Pts',(-0.152458776004204,-0.0308575860024739,
0.621483309529429));
#11791=CARTESIAN_POINT('Ctrl Pts',(-0.152573781388118,-0.0302844916740415,
0.62144128482264));
#11792=CARTESIAN_POINT('Ctrl Pts',(-0.152637043040253,-0.0299640167578431,
0.621417857250302));
#11793=CARTESIAN_POINT('Ctrl Pts',(-0.152825743846724,-0.028991977868985,
0.621347012160336));
#11794=CARTESIAN_POINT('Ctrl Pts',(-0.152948026217467,-0.0283397967778022,
0.621299769743629));
#11795=CARTESIAN_POINT('Ctrl Pts',(-0.153872143155152,-0.023230834555012,
0.620931815243988));
#11796=CARTESIAN_POINT('Ctrl Pts',(-0.154483282768341,-0.0187412167743094,
0.620621090821166));
#11797=CARTESIAN_POINT('Ctrl Pts',(-0.155328034334317,-0.00954638373917771,
0.619998531446841));
#11798=CARTESIAN_POINT('Ctrl Pts',(-0.155545705223899,-0.00484457768735938,
0.619687425983483));
#11799=CARTESIAN_POINT('Ctrl Pts',(-0.155561285277832,0.0124761902052128,
0.618546004554368));
#11800=CARTESIAN_POINT('Ctrl Pts',(-0.154037873253815,0.0250450339594314,
0.617722353371123));
#11801=CARTESIAN_POINT('Ctrl Pts',(-0.150606091338229,0.0389422576042399,
0.616727048739471));
#11802=CARTESIAN_POINT('Ctrl Pts',(-0.150171387750559,0.040586304077064,
0.616608004950626));
#11803=CARTESIAN_POINT('Ctrl Pts',(-0.149520700253385,0.0428934515853061,
0.616438959710814));
#11804=CARTESIAN_POINT('Ctrl Pts',(-0.149327065559149,0.0435627760385117,
0.616389680669495));
#11805=CARTESIAN_POINT('Ctrl Pts',(-0.149005902063342,0.0446456144275852,
0.616309561045339));
#11806=CARTESIAN_POINT('Ctrl Pts',(-0.148881131480382,0.0450599425159485,
0.616278810453712));
#11807=CARTESIAN_POINT('Ctrl Pts',(-0.148616973300796,0.0459240621782781,
0.616214477289995));
#11808=CARTESIAN_POINT('Ctrl Pts',(-0.148477268975909,0.046373751503711,
0.616180884657429));
#11809=CARTESIAN_POINT('Ctrl Pts',(-0.148141258858153,0.0474382380989754,
0.616101092214698));
#11810=CARTESIAN_POINT('Ctrl Pts',(-0.1479431658435,0.0480524574497901,
0.61605483428233));
#11811=CARTESIAN_POINT('Ctrl Pts',(-0.147268845329349,0.0500995982376279,
0.615899922479334));
#11812=CARTESIAN_POINT('Ctrl Pts',(-0.146775589642696,0.0515267749263192,
0.615790711473049));
#11813=CARTESIAN_POINT('Ctrl Pts',(-0.144022803320651,0.0591311884418498,
0.615202078251652));
#11814=CARTESIAN_POINT('Ctrl Pts',(-0.141394268527936,0.0651667365848729,
0.614710512034069));
#11815=CARTESIAN_POINT('Ctrl Pts',(-0.133806050313894,0.0799540043047982,
0.613443751824431));
#11816=CARTESIAN_POINT('Ctrl Pts',(-0.12836520930498,0.0884254022824461,
0.612657426108371));
#11817=CARTESIAN_POINT('Ctrl Pts',(-0.120926640201696,0.0978592414262875,
0.61173390126183));
#11818=CARTESIAN_POINT('Ctrl Pts',(-0.11967754293255,0.0993829446681807,
0.611583163824499));
#11819=CARTESIAN_POINT('Ctrl Pts',(-0.117510817061786,0.101925900652144,
0.611329370879208));
#11820=CARTESIAN_POINT('Ctrl Pts',(-0.116608054918576,0.102957482120815,
0.611225772688831));
#11821=CARTESIAN_POINT('Ctrl Pts',(-0.114103164856635,0.105744589132956,
0.610944379228456));
#11822=CARTESIAN_POINT('Ctrl Pts',(-0.112474164039244,0.107475645877367,
0.610767943271088));
#11823=CARTESIAN_POINT('Ctrl Pts',(-0.110456489777317,0.109523579167342,
0.610557860882373));
#11824=CARTESIAN_POINT('Ctrl Pts',(-0.110105256347507,0.109876672093618,
0.610521589758884));
#11825=CARTESIAN_POINT('Ctrl Pts',(-0.109525097647989,0.110454326789766,
0.610462177472418));
#11826=CARTESIAN_POINT('Ctrl Pts',(-0.109297166699943,0.110679874764104,
0.610438961102276));
#11827=CARTESIAN_POINT('Ctrl Pts',(-0.108884959714948,0.111085257088982,
0.610397202943737));
#11828=CARTESIAN_POINT('Ctrl Pts',(-0.108700934457395,0.111265338924405,
0.610378641961056));
#11829=CARTESIAN_POINT('Ctrl Pts',(-0.108298097466243,0.111657590315717,
0.610338189005064));
#11830=CARTESIAN_POINT('Ctrl Pts',(-0.108079109647944,0.111869573396744,
0.610316311532879));
#11831=CARTESIAN_POINT('Ctrl Pts',(-0.107457153254402,0.112468104420445,
0.61025449140292));
#11832=CARTESIAN_POINT('Ctrl Pts',(-0.107052718689288,0.112853133515076,
0.610214664377523));
#11833=CARTESIAN_POINT('Ctrl Pts',(-0.104513542140358,0.115244542576148,
0.609966861853852));
#11834=CARTESIAN_POINT('Ctrl Pts',(-0.102324367148768,0.117192627600569,
0.609763056576974));
#11835=CARTESIAN_POINT('Ctrl Pts',(-0.0890659403496413,0.128335926790838,
0.608576120101917));
#11836=CARTESIAN_POINT('Ctrl Pts',(-0.0768187175676357,0.136021354216421,
0.607662411453918));
#11837=CARTESIAN_POINT('Ctrl Pts',(-0.0636886258321226,0.141913922641918,
0.606695238001095));
#11838=CARTESIAN_POINT('',(-0.155549956956732,1.69517297940555E-6,0.605448024839579));
#11839=CARTESIAN_POINT('Ctrl Pts',(-0.0636886259076389,0.141913922608026,
0.592717731153444));
#11840=CARTESIAN_POINT('Ctrl Pts',(-0.0645421680723216,0.141530866973851,
0.592780255107091));
#11841=CARTESIAN_POINT('Ctrl Pts',(-0.06539250273425,0.141139999457564,
0.592842952041328));
#11842=CARTESIAN_POINT('Ctrl Pts',(-0.071439591683574,0.138293954046624,
0.593291964667332));
#11843=CARTESIAN_POINT('Ctrl Pts',(-0.0764994376252857,0.135560526283284,
0.593684591834827));
#11844=CARTESIAN_POINT('Ctrl Pts',(-0.0822897660030893,0.132004912109664,
0.594160907074483));
#11845=CARTESIAN_POINT('Ctrl Pts',(-0.083177890784753,0.131447102664529,
0.594234742969407));
#11846=CARTESIAN_POINT('Ctrl Pts',(-0.0845290725455758,0.130579281686744,
0.594348309736595));
#11847=CARTESIAN_POINT('Ctrl Pts',(-0.084996230379702,0.130275683524707,
0.594387803158546));
#11848=CARTESIAN_POINT('Ctrl Pts',(-0.0858254862657522,0.129730404782106,
0.594458322638973));
#11849=CARTESIAN_POINT('Ctrl Pts',(-0.0861882217733486,0.129489700123871,
0.594489311994601));
#11850=CARTESIAN_POINT('Ctrl Pts',(-0.0865582548510905,0.129241909291469,
0.594521072341359));
#11851=CARTESIAN_POINT('Ctrl Pts',(-0.0865665704554396,0.129236339625331,
0.594521786155287));
#11852=CARTESIAN_POINT('Ctrl Pts',(-0.0865815823983888,0.129226282753808,
0.594523074922943));
#11853=CARTESIAN_POINT('Ctrl Pts',(-0.086588278926626,0.129221795829886,
0.594523649866084));
#11854=CARTESIAN_POINT('Ctrl Pts',(-0.0866004540151363,0.129213636694708,
0.594524695271622));
#11855=CARTESIAN_POINT('Ctrl Pts',(-0.0866059326907217,0.129209964655478,
0.594525165727521));
#11856=CARTESIAN_POINT('Ctrl Pts',(-0.0866200706884921,0.129200487470459,
0.594526379848355));
#11857=CARTESIAN_POINT('Ctrl Pts',(-0.0866287296598549,0.129194681803096,
0.594527123532947));
#11858=CARTESIAN_POINT('Ctrl Pts',(-0.0866457235385286,0.129183285270245,
0.594528583232527));
#11859=CARTESIAN_POINT('Ctrl Pts',(-0.086654058488704,0.129177694468374,
0.594529299245118));
#11860=CARTESIAN_POINT('Ctrl Pts',(-0.0866704443701546,0.129166701075337,
0.594530707023049));
#11861=CARTESIAN_POINT('Ctrl Pts',(-0.0866784953374954,0.129161298538042,
0.594531398786348));
#11862=CARTESIAN_POINT('Ctrl Pts',(-0.0866943476260553,0.129150658836807,
0.594532761004112));
#11863=CARTESIAN_POINT('Ctrl Pts',(-0.0867021489779531,0.129145421718671,
0.594533431456842));
#11864=CARTESIAN_POINT('Ctrl Pts',(-0.0867175318159114,0.129135093058236,
0.594534753600041));
#11865=CARTESIAN_POINT('Ctrl Pts',(-0.0867251133285815,0.129130001554818,
0.59453540528906));
#11866=CARTESIAN_POINT('Ctrl Pts',(-0.0867400825157907,0.129119946810574,
0.594536692131201));
#11867=CARTESIAN_POINT('Ctrl Pts',(-0.086747470212533,0.12911498360352,
0.594537327283026));
#11868=CARTESIAN_POINT('Ctrl Pts',(-0.0867620746966495,0.129105170190584,
0.594538583012691));
#11869=CARTESIAN_POINT('Ctrl Pts',(-0.0867692915036335,0.129100320013406,
0.59453920358946));
#11870=CARTESIAN_POINT('Ctrl Pts',(-0.0867835745623629,0.129090719103583,
0.594540431911215));
#11871=CARTESIAN_POINT('Ctrl Pts',(-0.0867906408311332,0.129085968395572,
0.594541039655289));
#11872=CARTESIAN_POINT('Ctrl Pts',(-0.0868046410138762,0.129076554293483,
0.594542243870061));
#11873=CARTESIAN_POINT('Ctrl Pts',(-0.0868115749418122,0.129071890921101,
0.594542840339913));
#11874=CARTESIAN_POINT('Ctrl Pts',(-0.0868253268241844,0.129062640564179,
0.594544023409412));
#11875=CARTESIAN_POINT('Ctrl Pts',(-0.0868321447919833,0.129058053597398,
0.594544610008447));
#11876=CARTESIAN_POINT('Ctrl Pts',(-0.0868456796034278,0.129048946139709,
0.594545774608762));
#11877=CARTESIAN_POINT('Ctrl Pts',(-0.0868523964570442,0.129044425665037,
0.594546352609389));
#11878=CARTESIAN_POINT('Ctrl Pts',(-0.0868657425806166,0.129035442145885,
0.594547501173671));
#11879=CARTESIAN_POINT('Ctrl Pts',(-0.0868723718592643,0.12903097911514,
0.594548071736783));
#11880=CARTESIAN_POINT('Ctrl Pts',(-0.0868855552573491,0.12902210217657,
0.594549206491615));
#11881=CARTESIAN_POINT('Ctrl Pts',(-0.0868921093849075,0.129017688279865,
0.59454977068294));
#11882=CARTESIAN_POINT('Ctrl Pts',(-0.0869051539532847,0.129008901931611,
0.594550893678592));
#11883=CARTESIAN_POINT('Ctrl Pts',(-0.0869116444004273,0.129004529489696,
0.594551452482547));
#11884=CARTESIAN_POINT('Ctrl Pts',(-0.0869245722610375,0.128995818914783,
0.594552565617997));
#11885=CARTESIAN_POINT('Ctrl Pts',(-0.0869310096799614,0.128991480789555,
0.594553119949207));
#11886=CARTESIAN_POINT('Ctrl Pts',(-0.0874011603812284,0.128674598805235,
0.59459360837186));
#11887=CARTESIAN_POINT('Ctrl Pts',(-0.087863179528361,0.128359560928423,
0.594633636409742));
#11888=CARTESIAN_POINT('Ctrl Pts',(-0.0892459848900351,0.127405700887843,
0.594754169434339));
#11889=CARTESIAN_POINT('Ctrl Pts',(-0.0901615584427469,0.126759424480668,
0.594834956732482));
#11890=CARTESIAN_POINT('Ctrl Pts',(-0.0991541728784745,0.120265084962037,
0.595638380511613));
#11891=CARTESIAN_POINT('Ctrl Pts',(-0.106656456765969,0.11366426583745,
0.59639113301573));
#11892=CARTESIAN_POINT('Ctrl Pts',(-0.12184721546711,0.097462354411212,
0.598104197824594));
#11893=CARTESIAN_POINT('Ctrl Pts',(-0.129137025742495,0.0875746634344515,
0.599067737899218));
#11894=CARTESIAN_POINT('Ctrl Pts',(-0.135698187044565,0.0760450565832941,
0.600046258588611));
#11895=CARTESIAN_POINT('Ctrl Pts',(-0.136195290257886,0.0751511254689562,
0.600121232097949));
#11896=CARTESIAN_POINT('Ctrl Pts',(-0.136875068465791,0.0738997908593797,
0.600224875334224));
#11897=CARTESIAN_POINT('Ctrl Pts',(-0.137065218072634,0.0735465122287305,
0.600253992554515));
#11898=CARTESIAN_POINT('Ctrl Pts',(-0.137368440603421,0.0729778951207177,
0.600300623244457));
#11899=CARTESIAN_POINT('Ctrl Pts',(-0.137482377253485,0.0727630235561555,
0.600318190667547));
#11900=CARTESIAN_POINT('Ctrl Pts',(-0.137719445165092,0.0723133956714605,
0.600354838007231));
#11901=CARTESIAN_POINT('Ctrl Pts',(-0.137842480726941,0.0720785909876796,
0.600373911528016));
#11902=CARTESIAN_POINT('Ctrl Pts',(-0.138138764495207,0.0715096211907438,
0.600419976686285));
#11903=CARTESIAN_POINT('Ctrl Pts',(-0.138311402800424,0.0711751364067545,
0.60044693005095));
#11904=CARTESIAN_POINT('Ctrl Pts',(-0.138911504267425,0.070002017823152,
0.60054102882373));
#11905=CARTESIAN_POINT('Ctrl Pts',(-0.139332579561854,0.0691601106604629,
0.600607787988364));
#11906=CARTESIAN_POINT('Ctrl Pts',(-0.141771901241083,0.0641701609473671,
0.600999240119817));
#11907=CARTESIAN_POINT('Ctrl Pts',(-0.143612686445219,0.059937363228163,
0.601314192319064));
#11908=CARTESIAN_POINT('Ctrl Pts',(-0.149088721203819,0.0456377976915111,
0.602342702975756));
#11909=CARTESIAN_POINT('Ctrl Pts',(-0.151873915082035,0.0352787489918909,
0.603033133129283));
#11910=CARTESIAN_POINT('Ctrl Pts',(-0.15461481200792,0.0182476766811929,
0.604183449687493));
#11911=CARTESIAN_POINT('Ctrl Pts',(-0.155245963313012,0.0117214143171901,
0.604627295046638));
#11912=CARTESIAN_POINT('Ctrl Pts',(-0.15550216665472,0.00402527617589184,
0.605164580373047));
#11913=CARTESIAN_POINT('Ctrl Pts',(-0.155527688746032,0.00287482029818528,
0.60524524757909));
#11914=CARTESIAN_POINT('Ctrl Pts',(-0.155546808207301,0.00115006330512711,
0.605366757610222));
#11915=CARTESIAN_POINT('Ctrl Pts',(-0.155549993637752,0.00057589038162694,
0.60540730368657));
#11916=CARTESIAN_POINT('Ctrl Pts',(-0.155549999990479,1.72103705376068E-6,
0.605447948317266));
#11917=CARTESIAN_POINT('Ctrl Pts',(-0.15554999999082,1.68991234156361E-6,
0.60544795052054));
#11918=CARTESIAN_POINT('Ctrl Pts',(-0.15555000269116,-0.000246866046467027,
0.605465545444643));
#11919=CARTESIAN_POINT('Ctrl Pts',(-0.155549409633897,-0.000495420636813976,
0.605483158784546));
#11920=CARTESIAN_POINT('Ctrl Pts',(-0.155546180294664,-0.00117060485290016,
0.605531055424233));
#11921=CARTESIAN_POINT('Ctrl Pts',(-0.155542384543066,-0.00159722384704611,
0.605561374528306));
#11922=CARTESIAN_POINT('Ctrl Pts',(-0.155530851940917,-0.00248354092000977,
0.605624481252254));
#11923=CARTESIAN_POINT('Ctrl Pts',(-0.155522831979431,-0.00294323049001169,
0.605657277404107));
#11924=CARTESIAN_POINT('Ctrl Pts',(-0.155499307288224,-0.00401831901967739,
0.6057341359501));
#11925=CARTESIAN_POINT('Ctrl Pts',(-0.155482187168788,-0.00463367110368875,
0.605778248329937));
#11926=CARTESIAN_POINT('Ctrl Pts',(-0.155416544985987,-0.00657785597660333,
0.605918011214128));
#11927=CARTESIAN_POINT('Ctrl Pts',(-0.155354637239221,-0.00790614499603027,
0.606014077205768));
#11928=CARTESIAN_POINT('Ctrl Pts',(-0.1551945530319,-0.0105982283447777,
0.606210003052721));
#11929=CARTESIAN_POINT('Ctrl Pts',(-0.155095408538991,-0.0119618462158238,
0.60630988477302));
#11930=CARTESIAN_POINT('Ctrl Pts',(-0.154643381828647,-0.0172196250270301,
0.606697545663322));
#11931=CARTESIAN_POINT('Ctrl Pts',(-0.154161718860842,-0.0211009642599832,
0.606989160605566));
#11932=CARTESIAN_POINT('Ctrl Pts',(-0.151181792927924,-0.0394313218854205,
0.608392180677955));
#11933=CARTESIAN_POINT('Ctrl Pts',(-0.146795550196754,-0.0534953471628895,
0.609554571603185));
#11934=CARTESIAN_POINT('Ctrl Pts',(-0.139366153735788,-0.0691371137296447,
0.610858094242812));
#11935=CARTESIAN_POINT('Ctrl Pts',(-0.138164521207684,-0.0715082700154811,
0.611055721580055));
#11936=CARTESIAN_POINT('Ctrl Pts',(-0.136644786718346,-0.0743256329052478,
0.611289588245654));
#11937=CARTESIAN_POINT('Ctrl Pts',(-0.136384448237238,-0.0748022709999217,
0.611329119918695));
#11938=CARTESIAN_POINT('Ctrl Pts',(-0.135975751214151,-0.0755413027792245,
0.611390350450682));
#11939=CARTESIAN_POINT('Ctrl Pts',(-0.13582912088118,-0.0758046388336279,
0.611412155813021));
#11940=CARTESIAN_POINT('Ctrl Pts',(-0.13555573156068,-0.0762922834914956,
0.611452509069153));
#11941=CARTESIAN_POINT('Ctrl Pts',(-0.135429181920111,-0.0765167012204078,
0.611471069481943));
#11942=CARTESIAN_POINT('Ctrl Pts',(-0.13514188300577,-0.0770232392531501,
0.611512939857842));
#11943=CARTESIAN_POINT('Ctrl Pts',(-0.134980807949059,-0.0773051707069598,
0.611536228572002));
#11944=CARTESIAN_POINT('Ctrl Pts',(-0.134503023709644,-0.0781353955398286,
0.611604768540353));
#11945=CARTESIAN_POINT('Ctrl Pts',(-0.134183842933698,-0.078682270909785,
0.611649864596857));
#11946=CARTESIAN_POINT('Ctrl Pts',(-0.131862372778803,-0.0826045992384129,
0.611973046242618));
#11947=CARTESIAN_POINT('Ctrl Pts',(-0.129736096224094,-0.0859055128545022,
0.612243649193784));
#11948=CARTESIAN_POINT('Ctrl Pts',(-0.12676314900073,-0.0901582087722229,
0.612595392087857));
#11949=CARTESIAN_POINT('Ctrl Pts',(-0.126026704905546,-0.0911848032890401,
0.612680551745414));
#11950=CARTESIAN_POINT('Ctrl Pts',(-0.119166425518087,-0.100506051418135,
0.613457201707674));
#11951=CARTESIAN_POINT('Ctrl Pts',(-0.112244448397571,-0.108181816691158,
0.614123508150869));
#11952=CARTESIAN_POINT('Ctrl Pts',(-0.100972321942327,-0.118425509933041,
0.615137940013221));
#11953=CARTESIAN_POINT('Ctrl Pts',(-0.0971763914055755,-0.121559670309547,
0.6154693778377));
#11954=CARTESIAN_POINT('Ctrl Pts',(-0.0909275861478394,-0.126239107451906,
0.616005942718959));
#11955=CARTESIAN_POINT('Ctrl Pts',(-0.0885689952328414,-0.127904923240541,
0.616206547746189));
#11956=CARTESIAN_POINT('Ctrl Pts',(-0.0856597052565283,-0.129840619772417,
0.616452408325497));
#11957=CARTESIAN_POINT('Ctrl Pts',(-0.0851519040148387,-0.130174209701628,
0.616495264475898));
#11958=CARTESIAN_POINT('Ctrl Pts',(-0.0842566150031015,-0.130754871837227,
0.616570729711796));
#11959=CARTESIAN_POINT('Ctrl Pts',(-0.0838699597391991,-0.131003219525641,
0.616603291222935));
#11960=CARTESIAN_POINT('Ctrl Pts',(-0.083094567585844,-0.131496412121985,
0.616668532658772));
#11961=CARTESIAN_POINT('Ctrl Pts',(-0.082705835195802,-0.131741255419529,
0.616701212219627));
#11962=CARTESIAN_POINT('Ctrl Pts',(-0.0819467749141003,-0.132214666224297,
0.616764972139161));
#11963=CARTESIAN_POINT('Ctrl Pts',(-0.081576560870931,-0.13244340902062,
0.616796045667784));
#11964=CARTESIAN_POINT('Ctrl Pts',(-0.0806205312927279,-0.13302857833316,
0.616876230805559));
#11965=CARTESIAN_POINT('Ctrl Pts',(-0.0800333153543437,-0.133382686750331,
0.616925426476372));
#11966=CARTESIAN_POINT('Ctrl Pts',(-0.0779710051651543,-0.134607798404192,
0.617098022535319));
#11967=CARTESIAN_POINT('Ctrl Pts',(-0.0764839294410919,-0.135458278221593,
0.617222159068087));
#11968=CARTESIAN_POINT('Ctrl Pts',(-0.0641464353693927,-0.142246341310883,
0.61824988006041));
#11969=CARTESIAN_POINT('Ctrl Pts',(-0.052639496067444,-0.146893639503891,
0.619200111178757));
#11970=CARTESIAN_POINT('Ctrl Pts',(-0.0360660659531262,-0.151387456761871,
0.620531846263102));
#11971=CARTESIAN_POINT('Ctrl Pts',(-0.0313692226170196,-0.152429978537289,
0.620904672542681));
#11972=CARTESIAN_POINT('Ctrl Pts',(-0.0234788234335609,-0.153801127306779,
0.621517469190521));
#11973=CARTESIAN_POINT('Ctrl Pts',(-0.0203097676359398,-0.154251606995086,
0.621759995265127));
#11974=CARTESIAN_POINT('Ctrl Pts',(-0.0159568541404281,-0.154733873944736,
0.622086414105963));
#11975=CARTESIAN_POINT('Ctrl Pts',(-0.0147833729024979,-0.154850395653898,
0.622173747161028));
#11976=CARTESIAN_POINT('Ctrl Pts',(-0.0127660483161376,-0.155027565103629,
0.622322617529598));
#11977=CARTESIAN_POINT('Ctrl Pts',(-0.0119228444483672,-0.155094693004722,
0.622384464417819));
#11978=CARTESIAN_POINT('Ctrl Pts',(-0.0107195098600563,-0.15518061921468,
0.62247214820256));
#11979=CARTESIAN_POINT('Ctrl Pts',(-0.0103598167694378,-0.155205047195995,
0.622498284529464));
#11980=CARTESIAN_POINT('Ctrl Pts',(-0.0097383726893711,-0.155245081563896,
0.622543309724848));
#11981=CARTESIAN_POINT('Ctrl Pts',(-0.00947666267635023,-0.155261276953991,
0.622562231208876));
#11982=CARTESIAN_POINT('Ctrl Pts',(-0.00896813589807324,-0.155291455493855,
0.622598918283943));
#11983=CARTESIAN_POINT('Ctrl Pts',(-0.00872132697857542,-0.155305512036626,
0.622616688046706));
#11984=CARTESIAN_POINT('Ctrl Pts',(-0.00805333736016125,-0.155341958753017,
0.622664687214997));
#11985=CARTESIAN_POINT('Ctrl Pts',(-0.00763209313398832,-0.15536322459792,
0.622694854263577));
#11986=CARTESIAN_POINT('Ctrl Pts',(-0.0060571073442633,-0.155436314076149,
0.622807282176867));
#11987=CARTESIAN_POINT('Ctrl Pts',(-0.00490284763192702,-0.15547700337552,
0.622888948610456));
#11988=CARTESIAN_POINT('Ctrl Pts',(0.0072041728738317,-0.15576882384188,
0.623738926678597));
#11989=CARTESIAN_POINT('Ctrl Pts',(0.0181556956324896,-0.154875040171725,
0.624452376272599));
#11990=CARTESIAN_POINT('Ctrl Pts',(0.0387287316436798,-0.150981679344767,
0.625831087940597));
#11991=CARTESIAN_POINT('Ctrl Pts',(0.0483309570722019,-0.148187251400893,
0.626492121962202));
#11992=CARTESIAN_POINT('Ctrl Pts',(0.0593417735998711,-0.143798043556098,
0.627315016725813));
#11993=CARTESIAN_POINT('Ctrl Pts',(0.0610720186803714,-0.143071770194556,
0.627446258026023));
#11994=CARTESIAN_POINT('Ctrl Pts',(0.0632775987228548,-0.142098675642065,
0.627616237449259));
#11995=CARTESIAN_POINT('Ctrl Pts',(0.0637654373707554,-0.141880432419188,
0.627654004726327));
#11996=CARTESIAN_POINT('Ctrl Pts',(0.0647151513481073,-0.141449673638688,
0.62772786833199));
#11997=CARTESIAN_POINT('Ctrl Pts',(0.0651771290020639,-0.141237398837473,
0.627763956078891));
#11998=CARTESIAN_POINT('Ctrl Pts',(0.0660456204977071,-0.140833165875177,
0.627832100821028));
#11999=CARTESIAN_POINT('Ctrl Pts',(0.0664523600041686,-0.140641702348329,
0.627864140498651));
#12000=CARTESIAN_POINT('Ctrl Pts',(0.0673772326442361,-0.140201431472514,
0.627937284387844));
#12001=CARTESIAN_POINT('Ctrl Pts',(0.0678948255296149,-0.139951511301741,
0.627978426791504));
#12002=CARTESIAN_POINT('Ctrl Pts',(0.0693780426016128,-0.139225174101158,
0.628096932716961));
#12003=CARTESIAN_POINT('Ctrl Pts',(0.0703401037478813,-0.138741600088303,
0.628174544275768));
#12004=CARTESIAN_POINT('Ctrl Pts',(0.0770090342113652,-0.135302311771293,
0.628717861141329));
#12005=CARTESIAN_POINT('Ctrl Pts',(0.082532122390359,-0.132005810682738,
0.629195563973366));
#12006=CARTESIAN_POINT('Ctrl Pts',(0.0996490245700216,-0.120294574061155,
0.630769478042835));
#12007=CARTESIAN_POINT('Ctrl Pts',(0.110289499669239,-0.110620468326615,
0.631904303893878));
#12008=CARTESIAN_POINT('Ctrl Pts',(0.12092907832483,-0.0978633959929492,
0.633150063928951));
#12009=CARTESIAN_POINT('Ctrl Pts',(0.122362141603887,-0.0960655718432342,
0.633320516656308));
#12010=CARTESIAN_POINT('Ctrl Pts',(0.124069915037214,-0.0938228597556935,
0.63352634502795));
#12011=CARTESIAN_POINT('Ctrl Pts',(0.124382834881437,-0.0934076187350562,
0.633564175279617));
#12012=CARTESIAN_POINT('Ctrl Pts',(0.124870825867942,-0.0927532595643639,
0.633623343633234));
#12013=CARTESIAN_POINT('Ctrl Pts',(0.125047301839897,-0.0925152020985207,
0.633644777172721));
#12014=CARTESIAN_POINT('Ctrl Pts',(0.125376301016954,-0.0920687370261534,
0.63368480058021));
#12015=CARTESIAN_POINT('Ctrl Pts',(0.125528983744005,-0.0918604563240144,
0.633703401130076));
#12016=CARTESIAN_POINT('Ctrl Pts',(0.125876725061937,-0.0913836022620748,
0.63374582645333));
#12017=CARTESIAN_POINT('Ctrl Pts',(0.126071442956404,-0.0911147844818143,
0.633769627593949));
#12018=CARTESIAN_POINT('Ctrl Pts',(0.126668560435871,-0.0902848551013026,
0.633842762147437));
#12019=CARTESIAN_POINT('Ctrl Pts',(0.127068093109419,-0.089721675332436,
0.633891903386442));
#12020=CARTESIAN_POINT('Ctrl Pts',(0.132495237580992,-0.0819626227478519,
0.634562570956439));
#12021=CARTESIAN_POINT('Ctrl Pts',(0.136909582294586,-0.0743550885261985,
0.63514593798261));
#12022=CARTESIAN_POINT('Ctrl Pts',(0.144078785040856,-0.0591714727061843,
0.636253396297089));
#12023=CARTESIAN_POINT('Ctrl Pts',(0.146934007696836,-0.0516754351668931,
0.63677669614464));
#12024=CARTESIAN_POINT('Ctrl Pts',(0.150336621149422,-0.0401357114992056,
0.637583784302255));
#12025=CARTESIAN_POINT('Ctrl Pts',(0.151323898543774,-0.0362360131282377,
0.637856638393564));
#12026=CARTESIAN_POINT('Ctrl Pts',(0.152678077918459,-0.0298572696393413,
0.638306468207153));
#12027=CARTESIAN_POINT('Ctrl Pts',(0.153138172830518,-0.027399832463768,
0.638480586071073));
#12028=CARTESIAN_POINT('Ctrl Pts',(0.153664486387855,-0.0241586976034388,
0.638711774762485));
#12029=CARTESIAN_POINT('Ctrl Pts',(0.153784285989732,-0.0233839771845434,
0.638767149506014));
#12030=CARTESIAN_POINT('Ctrl Pts',(0.153970791512132,-0.0221144104595091,
0.638858095843171));
#12031=CARTESIAN_POINT('Ctrl Pts',(0.154040980901334,-0.0216200828213467,
0.638893557207049));
#12032=CARTESIAN_POINT('Ctrl Pts',(0.154172157427217,-0.020663157708806,
0.638962304098659));
#12033=CARTESIAN_POINT('Ctrl Pts',(0.15423344549532,-0.0202006062824941,
0.638995579750602));
#12034=CARTESIAN_POINT('Ctrl Pts',(0.154370034304574,-0.0191328753607649,
0.639072499629973));
#12035=CARTESIAN_POINT('Ctrl Pts',(0.154443858595634,-0.018527518270096,
0.639116189806916));
#12036=CARTESIAN_POINT('Ctrl Pts',(0.154632568422074,-0.0169005381023726,
0.639233836117936));
#12037=CARTESIAN_POINT('Ctrl Pts',(0.154740886905871,-0.0158781998400958,
0.639307996951977));
#12038=CARTESIAN_POINT('Ctrl Pts',(0.155905784530694,-0.00373595508885958,
0.640191745011383));
#12039=CARTESIAN_POINT('Ctrl Pts',(0.155771534038834,0.00746302211110987,
0.641039755092854));
#12040=CARTESIAN_POINT('Ctrl Pts',(0.153955256975544,0.0225856981260099,
0.642218384041977));
#12041=CARTESIAN_POINT('Ctrl Pts',(0.153312303551222,0.0266021113264362,
0.64253428099494));
#12042=CARTESIAN_POINT('Ctrl Pts',(0.151094189137307,0.0376614446459579,
0.643407165187042));
#12043=CARTESIAN_POINT('Ctrl Pts',(0.149185165957373,0.0446279338210357,
0.643960757063796));
#12044=CARTESIAN_POINT('Ctrl Pts',(0.146520772639784,0.0522319274084485,
0.644553027592142));
#12045=CARTESIAN_POINT('Ctrl Pts',(0.146235966693505,0.0530240811911721,
0.644614573337361));
#12046=CARTESIAN_POINT('Ctrl Pts',(0.145820256044093,0.0541514994325331,
0.644701907512446));
#12047=CARTESIAN_POINT('Ctrl Pts',(0.145694603734264,0.0544886631635209,
0.6447279921791));
#12048=CARTESIAN_POINT('Ctrl Pts',(0.145475405058326,0.0550706610921606,
0.64477295707184));
#12049=CARTESIAN_POINT('Ctrl Pts',(0.145382408268418,0.0553156990422736,
0.644791869676017));
#12050=CARTESIAN_POINT('Ctrl Pts',(0.14520041924754,0.0557915940060938,
0.644828562288324));
#12051=CARTESIAN_POINT('Ctrl Pts',(0.145111495669539,0.0560224735110557,
0.644846346378823));
#12052=CARTESIAN_POINT('Ctrl Pts',(0.14486911791217,0.056647329489976,0.644894433311514));
#12053=CARTESIAN_POINT('Ctrl Pts',(0.144714606110117,0.0570408980704138,
0.644924673391923));
#12054=CARTESIAN_POINT('Ctrl Pts',(0.144129614889571,0.0585132957016289,
0.645037644724764));
#12055=CARTESIAN_POINT('Ctrl Pts',(0.143688646228143,0.0595879586938149,
0.645119774198944));
#12056=CARTESIAN_POINT('Ctrl Pts',(0.139833568364228,0.0686912602035709,
0.645813539009813));
#12057=CARTESIAN_POINT('Ctrl Pts',(0.13576107391466,0.0764257411053781,
0.64639053895324));
#12058=CARTESIAN_POINT('Ctrl Pts',(0.126061897274138,0.0915988074250569,
0.647576828755047));
#12059=CARTESIAN_POINT('Ctrl Pts',(0.120373612641557,0.0989551429633502,
0.648184012387952));
#12060=CARTESIAN_POINT('Ctrl Pts',(0.111126181632568,0.108928608662527,
0.649107596055885));
#12061=CARTESIAN_POINT('Ctrl Pts',(0.108058091947769,0.111972822201948,
0.649405317010247));
#12062=CARTESIAN_POINT('Ctrl Pts',(0.104173958406753,0.115518270006524,
0.64977466579892));
#12063=CARTESIAN_POINT('Ctrl Pts',(0.103474695562522,0.11614504563118,0.649840874181854));
#12064=CARTESIAN_POINT('Ctrl Pts',(0.102369298586383,0.117117948591452,
0.649945117115342));
#12065=CARTESIAN_POINT('Ctrl Pts',(0.101966976729068,0.11746839072352,0.649982971807506));
#12066=CARTESIAN_POINT('Ctrl Pts',(0.101249585405843,0.118086811418107,
0.650050324697209));
#12067=CARTESIAN_POINT('Ctrl Pts',(0.100935233331135,0.11835561770392,0.650079788402867));
#12068=CARTESIAN_POINT('Ctrl Pts',(0.100207337834258,0.118973041045461,
0.650147901580778));
#12069=CARTESIAN_POINT('Ctrl Pts',(0.0997930428047233,0.119320759491201,
0.650186587267329));
#12070=CARTESIAN_POINT('Ctrl Pts',(0.0986488259489147,0.120270974986987,
0.650293212268211));
#12071=CARTESIAN_POINT('Ctrl Pts',(0.0979152161774744,0.120868973077282,
0.650361332083289));
#12072=CARTESIAN_POINT('Ctrl Pts',(0.094105730667767,0.123916813277471,
0.650713878246627));
#12073=CARTESIAN_POINT('Ctrl Pts',(0.0909434855293611,0.126255860982809,
0.651002636668619));
#12074=CARTESIAN_POINT('Ctrl Pts',(0.086058565355115,0.129590345660602,
0.651443508412847));
#12075=CARTESIAN_POINT('Ctrl Pts',(0.0843996863067313,0.130676802528019,
0.65159235915422));
#12076=CARTESIAN_POINT('Ctrl Pts',(0.0703149981521815,0.139521275882966,
0.652848801711777));
#12077=CARTESIAN_POINT('Ctrl Pts',(0.0568732990107603,0.145518848342843,
0.654010097842982));
#12078=CARTESIAN_POINT('Ctrl Pts',(0.0402215194448914,0.150283674043558,
0.65531410674233));
#12079=CARTESIAN_POINT('Ctrl Pts',(0.0376318420634051,0.150952973182189,
0.655512986768204));
#12080=CARTESIAN_POINT('Ctrl Pts',(0.0344959019302548,0.151677721677948,
0.655748136363642));
#12081=CARTESIAN_POINT('Ctrl Pts',(0.0339651626271346,0.151797451411035,
0.655787739653547));
#12082=CARTESIAN_POINT('Ctrl Pts',(0.0331392298437318,0.151979225281166,
0.655849056870482));
#12083=CARTESIAN_POINT('Ctrl Pts',(0.0328444728524854,0.152043198068726,
0.655870877777938));
#12084=CARTESIAN_POINT('Ctrl Pts',(0.0322976091319414,0.152160222508194,
0.65591124527159));
#12085=CARTESIAN_POINT('Ctrl Pts',(0.0320455590713309,0.152213504706742,
0.655929804452719));
#12086=CARTESIAN_POINT('Ctrl Pts',(0.0314758044893956,0.152332470200553,
0.655971653661496));
#12087=CARTESIAN_POINT('Ctrl Pts',(0.0311580268202946,0.152397785796019,
0.655994922532799));
#12088=CARTESIAN_POINT('Ctrl Pts',(0.0302207039556695,0.152587387514851,
0.656063350141667));
#12089=CARTESIAN_POINT('Ctrl Pts',(0.0296005929177064,0.152708895325904,
0.656108354439541));
#12090=CARTESIAN_POINT('Ctrl Pts',(0.0251568271563583,0.153551544291862,
0.656429072115368));
#12091=CARTESIAN_POINT('Ctrl Pts',(0.0213076378996552,0.154132844498649,
0.656697432037));
#12092=CARTESIAN_POINT('Ctrl Pts',(0.0162346410105878,0.154705239273233,
0.65704361564081));
#12093=CARTESIAN_POINT('Ctrl Pts',(0.0150274012392898,0.154827168063572,
0.657125444389107));
#12094=CARTESIAN_POINT('Ctrl Pts',(-0.000984437347845478,0.156255282855507,
0.658204853940127));
#12095=CARTESIAN_POINT('Ctrl Pts',(-0.0159000904905725,0.155447415966817,
0.659151709054206));
#12096=CARTESIAN_POINT('Ctrl Pts',(-0.0336969953422569,0.151891771155205,
0.660394642152622));
#12097=CARTESIAN_POINT('Ctrl Pts',(-0.0368974923166192,0.151146187488856,
0.660622387523984));
#12098=CARTESIAN_POINT('Ctrl Pts',(-0.0409048996753446,0.150077763450468,
0.660914015232223));
#12099=CARTESIAN_POINT('Ctrl Pts',(-0.0417361283034552,0.149848728524489,
0.660974859388766));
#12100=CARTESIAN_POINT('Ctrl Pts',(-0.0430622885310259,0.149471431030984,
0.66107251787399));
#12101=CARTESIAN_POINT('Ctrl Pts',(-0.0435584690630845,0.14932759004664,
0.661109188559251));
#12102=CARTESIAN_POINT('Ctrl Pts',(-0.0444968367759962,0.149050485746035,
0.661178794136787));
#12103=CARTESIAN_POINT('Ctrl Pts',(-0.0449391659758202,0.148917719352486,
0.661211712522855));
#12104=CARTESIAN_POINT('Ctrl Pts',(-0.045940356248095,0.148612342308135,
0.661286469325993));
#12105=CARTESIAN_POINT('Ctrl Pts',(-0.046498845344745,0.148438546149006,
0.661328346080184));
#12106=CARTESIAN_POINT('Ctrl Pts',(-0.0481480985568903,0.147915094314029,
0.661452539222409));
#12107=CARTESIAN_POINT('Ctrl Pts',(-0.0492359744271794,0.147556542424474,
0.66153514579337));
#12108=CARTESIAN_POINT('Ctrl Pts',(-0.0548577449395311,0.145634578815814,
0.661965692596482));
#12109=CARTESIAN_POINT('Ctrl Pts',(-0.0593186914332088,0.143875077990713,
0.662319887710196));
#12110=CARTESIAN_POINT('Ctrl Pts',(-0.063688650901166,0.141913911391341,
0.662679920979917));
#12111=CARTESIAN_POINT('Origin',(0.,0.,-0.129405622560373));
#12112=CARTESIAN_POINT('',(-0.0636886011499548,0.141913933718863,0.746625191472247));
#12113=CARTESIAN_POINT('',(-0.0636886287602419,0.141913921327825,0.732917465391055));
#12114=CARTESIAN_POINT('',(-0.0636886258329924,0.141913922641526,-0.129405622560373));
#12115=CARTESIAN_POINT('',(-0.155549981000406,7.68815545762296E-5,0.689293189475146));
#12116=CARTESIAN_POINT('Ctrl Pts',(-0.0636886011499548,0.141913933718863,
0.746625191472247));
#12117=CARTESIAN_POINT('Ctrl Pts',(-0.0573143785489615,0.144774578267551,
0.746084397578596));
#12118=CARTESIAN_POINT('Ctrl Pts',(-0.0507472492709453,0.147205842133469,
0.745539423472764));
#12119=CARTESIAN_POINT('Ctrl Pts',(-0.0397917799989713,0.15043919305941,
0.744666654528811));
#12120=CARTESIAN_POINT('Ctrl Pts',(-0.0355009023210546,0.151509179577591,
0.744333640805331));
#12121=CARTESIAN_POINT('Ctrl Pts',(-0.0305231620975979,0.152527291743769,
0.743961482087081));
#12122=CARTESIAN_POINT('Ctrl Pts',(-0.0298756598046069,0.15265543928807,
0.743913345014964));
#12123=CARTESIAN_POINT('Ctrl Pts',(-0.0289071952940793,0.152840710570873,
0.743841773724966));
#12124=CARTESIAN_POINT('Ctrl Pts',(-0.0285868488441498,0.152900951030528,
0.743818169157724));
#12125=CARTESIAN_POINT('Ctrl Pts',(-0.0280127969741062,0.153007033073725,
0.743775997876012));
#12126=CARTESIAN_POINT('Ctrl Pts',(-0.0277591659544253,0.153053251103599,
0.743757410169573));
#12127=CARTESIAN_POINT('Ctrl Pts',(-0.0272095078935997,0.153152001512819,
0.743717224732536));
#12128=CARTESIAN_POINT('Ctrl Pts',(-0.0269134439098565,0.153204306167541,
0.743695640046914));
#12129=CARTESIAN_POINT('Ctrl Pts',(-0.0260858465783675,0.153348042017064,
0.743635467893048));
#12130=CARTESIAN_POINT('Ctrl Pts',(-0.0255539795268914,0.153437568853032,
0.743596986469842));
#12131=CARTESIAN_POINT('Ctrl Pts',(-0.0224622143758307,0.153941469810441,
0.743374332132695));
#12132=CARTESIAN_POINT('Ctrl Pts',(-0.0198925461309444,0.154294575207567,
0.743193410574441));
#12133=CARTESIAN_POINT('Ctrl Pts',(-0.0026908929065488,0.156221352204686,
0.742002492315798));
#12134=CARTESIAN_POINT('Ctrl Pts',(0.0120931029397263,0.155776178144092,
0.741069653561887));
#12135=CARTESIAN_POINT('Ctrl Pts',(0.0284752546072518,0.152933323964381,
0.739952558378447));
#12136=CARTESIAN_POINT('Ctrl Pts',(0.03034861823162,0.152572614396229,0.739823673621564));
#12137=CARTESIAN_POINT('Ctrl Pts',(0.0361427178619844,0.151346047875282,
0.739420766145229));
#12138=CARTESIAN_POINT('Ctrl Pts',(0.0400366230296828,0.150362848847467,
0.739143815162361));
#12139=CARTESIAN_POINT('Ctrl Pts',(0.0447208406822449,0.148985243405018,
0.738801030264824));
#12140=CARTESIAN_POINT('Ctrl Pts',(0.0455517259364031,0.14873330680643,
0.738739855559981));
#12141=CARTESIAN_POINT('Ctrl Pts',(0.0469228679489378,0.148304989458365,
0.738638266675863));
#12142=CARTESIAN_POINT('Ctrl Pts',(0.0474643529357969,0.148132577847127,
0.73859798225899));
#12143=CARTESIAN_POINT('Ctrl Pts',(0.0484428727011502,0.147815096055153,
0.738524878416856));
#12144=CARTESIAN_POINT('Ctrl Pts',(0.0488802332889404,0.147671044293031,
0.738492092744318));
#12145=CARTESIAN_POINT('Ctrl Pts',(0.0498176088711473,0.147357683969654,
0.738421582581683));
#12146=CARTESIAN_POINT('Ctrl Pts',(0.0503174131703332,0.147187768166038,
0.738383838430702));
#12147=CARTESIAN_POINT('Ctrl Pts',(0.0516790663679986,0.146717108161522,
0.738280597626148));
#12148=CARTESIAN_POINT('Ctrl Pts',(0.0525391363779293,0.146411320636833,
0.73821493502858));
#12149=CARTESIAN_POINT('Ctrl Pts',(0.0570845946160769,0.144750029256393,
0.737865455598671));
#12150=CARTESIAN_POINT('Ctrl Pts',(0.0607200382423781,0.143263022853464,
0.737577297743301));
#12151=CARTESIAN_POINT('Ctrl Pts',(0.0777568437991727,0.135529467967245,
0.736183521620348));
#12152=CARTESIAN_POINT('Ctrl Pts',(0.0902777091810642,0.127530990518193,
0.73501810489613));
#12153=CARTESIAN_POINT('Ctrl Pts',(0.1048258504892,0.11500804823815,0.733551454573456));
#12154=CARTESIAN_POINT('Ctrl Pts',(0.108049403465252,0.1119850234781,0.73321867317898));
#12155=CARTESIAN_POINT('Ctrl Pts',(0.111601947867011,0.10835701755164,0.732846742012679));
#12156=CARTESIAN_POINT('Ctrl Pts',(0.112060671854064,0.107882546715695,
0.73279861223607));
#12157=CARTESIAN_POINT('Ctrl Pts',(0.112741427880196,0.107169394764387,
0.732727049637053));
#12158=CARTESIAN_POINT('Ctrl Pts',(0.112965743862985,0.106932920344534,
0.732703446525034));
#12159=CARTESIAN_POINT('Ctrl Pts',(0.113366152962936,0.106508142064163,
0.732661276809071));
#12160=CARTESIAN_POINT('Ctrl Pts',(0.113542521938729,0.106320104772796,
0.732642689219873));
#12161=CARTESIAN_POINT('Ctrl Pts',(0.113923566490701,0.105911821313951,
0.73260250285781));
#12162=CARTESIAN_POINT('Ctrl Pts',(0.114128070697715,0.105691420555265,
0.732580917135136));
#12163=CARTESIAN_POINT('Ctrl Pts',(0.114697677639162,0.105073955853852,
0.73252073916913));
#12164=CARTESIAN_POINT('Ctrl Pts',(0.1150613608363,0.104675578432192,0.732482253003976));
#12165=CARTESIAN_POINT('Ctrl Pts',(0.117162101998996,0.102350255315176,
0.73225951608949));
#12166=CARTESIAN_POINT('Ctrl Pts',(0.118852939359672,0.100381840210238,
0.732078519515728));
#12167=CARTESIAN_POINT('Ctrl Pts',(0.129799662769605,0.0869734059699074,
0.730887602100889));
#12168=CARTESIAN_POINT('Ctrl Pts',(0.137441959338346,0.0743111202246647,
0.729954814894502));
#12169=CARTESIAN_POINT('Ctrl Pts',(0.143937072388668,0.0590047947843232,
0.728837690423271));
#12170=CARTESIAN_POINT('Ctrl Pts',(0.144650328733272,0.0572339811682892,
0.728708717953214));
#12171=CARTESIAN_POINT('Ctrl Pts',(0.146761533152933,0.0517007072550992,
0.728305815900108));
#12172=CARTESIAN_POINT('Ctrl Pts',(0.148046487873488,0.0478972171677788,
0.728028961613457));
#12173=CARTESIAN_POINT('Ctrl Pts',(0.149428703404376,0.0432159550750357,
0.727686283715507));
#12174=CARTESIAN_POINT('Ctrl Pts',(0.149667564788807,0.0423813186433418,
0.727625115818986));
#12175=CARTESIAN_POINT('Ctrl Pts',(0.150051190884273,0.0409971403223736,
0.727523535902164));
#12176=CARTESIAN_POINT('Ctrl Pts',(0.150199955253999,0.0404487184784621,
0.727483253603748));
#12177=CARTESIAN_POINT('Ctrl Pts',(0.150463823585566,0.0394544335581914,
0.727410152022919));
#12178=CARTESIAN_POINT('Ctrl Pts',(0.150579959600077,0.0390088489174813,
0.727377366483463));
#12179=CARTESIAN_POINT('Ctrl Pts',(0.150824992727465,0.0380513175959221,
0.727306854847761));
#12180=CARTESIAN_POINT('Ctrl Pts',(0.150953265141815,0.0375392185902024,
0.72726910908299));
#12181=CARTESIAN_POINT('Ctrl Pts',(0.15129623311734,0.0361398084808301,
0.72716585936613));
#12182=CARTESIAN_POINT('Ctrl Pts',(0.151505725112019,0.035251256783263,
0.727100189421808));
#12183=CARTESIAN_POINT('Ctrl Pts',(0.152575112309186,0.030529791735562,
0.726750599483291));
#12184=CARTESIAN_POINT('Ctrl Pts',(0.153297331418468,0.0266675102533206,
0.72646233519781));
#12185=CARTESIAN_POINT('Ctrl Pts',(0.156037704955779,0.0081589522504735,
0.725068511443441));
#12186=CARTESIAN_POINT('Ctrl Pts',(0.156106799749517,-0.00669745341819393,
0.723903171207325));
#12187=CARTESIAN_POINT('Ctrl Pts',(0.153474088293961,-0.0257100987288768,
0.722436647152494));
#12188=CARTESIAN_POINT('Ctrl Pts',(0.15268226752861,-0.0300572639444694,
0.722103910848615));
#12189=CARTESIAN_POINT('Ctrl Pts',(0.151560596950402,-0.0350089052533985,
0.721732023847998));
#12190=CARTESIAN_POINT('Ctrl Pts',(0.151410704451113,-0.0356516004475047,
0.721683895488664));
#12191=CARTESIAN_POINT('Ctrl Pts',(0.151180675191396,-0.0366102742517521,
0.72161233457803));
#12192=CARTESIAN_POINT('Ctrl Pts',(0.151103630809113,-0.0369269751498208,
0.721588731748727));
#12193=CARTESIAN_POINT('Ctrl Pts',(0.15096386417344,-0.0374937418411552,
0.721546562336935));
#12194=CARTESIAN_POINT('Ctrl Pts',(0.150901515460847,-0.0377438948517119,
0.721527974770501));
#12195=CARTESIAN_POINT('Ctrl Pts',(0.150765105280708,-0.0382854532088609,
0.721487788228665));
#12196=CARTESIAN_POINT('Ctrl Pts',(0.150690820978907,-0.0385767983973127,
0.721466202304468));
#12197=CARTESIAN_POINT('Ctrl Pts',(0.150480905628401,-0.0393902336871026,
0.721406023209));
#12198=CARTESIAN_POINT('Ctrl Pts',(0.150343401098537,-0.0399118433277011,
0.721367536122352));
#12199=CARTESIAN_POINT('Ctrl Pts',(0.149528780023052,-0.0429380712438971,
0.721144783156171));
#12200=CARTESIAN_POINT('Ctrl Pts',(0.148791746389422,-0.0454263398781971,
0.720963772000498));
#12201=CARTESIAN_POINT('Ctrl Pts',(0.143462005232925,-0.0618948608962483,
0.719772854746293));
#12202=CARTESIAN_POINT('Ctrl Pts',(0.136967398017042,-0.0751821893527464,
0.718840077557524));
#12203=CARTESIAN_POINT('Ctrl Pts',(0.127629077402446,-0.0889396771574107,
0.717722947372951));
#12204=CARTESIAN_POINT('Ctrl Pts',(0.126527868172901,-0.0904994239460685,
0.717593957835289));
#12205=CARTESIAN_POINT('Ctrl Pts',(0.123023644878245,-0.095273770286096,
0.717191056835136));
#12206=CARTESIAN_POINT('Ctrl Pts',(0.12052490920674,-0.0984156999940041,
0.716914221361773));
#12207=CARTESIAN_POINT('Ctrl Pts',(0.117341438995376,-0.102115340843822,
0.71657156428182));
#12208=CARTESIAN_POINT('Ctrl Pts',(0.116769717040258,-0.102768620060293,
0.716510397710175));
#12209=CARTESIAN_POINT('Ctrl Pts',(0.115814775525421,-0.103841529089779,
0.716408819538363));
#12210=CARTESIAN_POINT('Ctrl Pts',(0.115434665751914,-0.104263911881839,
0.716368537652197));
#12211=CARTESIAN_POINT('Ctrl Pts',(0.1147423594554,-0.105024785082451,0.716295436511397));
#12212=CARTESIAN_POINT('Ctrl Pts',(0.114430956485173,-0.105363991593605,
0.716262650997818));
#12213=CARTESIAN_POINT('Ctrl Pts',(0.113759309866574,-0.10608911643179,
0.716192139075365));
#12214=CARTESIAN_POINT('Ctrl Pts',(0.11339859944167,-0.106474592455557,
0.716154392996477));
#12215=CARTESIAN_POINT('Ctrl Pts',(0.112408779293291,-0.107521636363341,
0.716051141544854));
#12216=CARTESIAN_POINT('Ctrl Pts',(0.111775805241721,-0.108179504736383,
0.715985470170497));
#12217=CARTESIAN_POINT('Ctrl Pts',(0.108388515998469,-0.111638545556464,
0.71563585871652));
#12218=CARTESIAN_POINT('Ctrl Pts',(0.105534852986288,-0.114339953218292,
0.715347573709146));
#12219=CARTESIAN_POINT('Ctrl Pts',(0.0914698378970639,-0.12667910983429,
0.713953740676999));
#12220=CARTESIAN_POINT('Ctrl Pts',(0.0790250668364783,-0.134793256058008,
0.712788415328505));
#12221=CARTESIAN_POINT('Ctrl Pts',(0.0616220930406426,-0.142891681479338,
0.711321820428744));
#12222=CARTESIAN_POINT('Ctrl Pts',(0.0575391416232965,-0.144584131753525,
0.710989000140358));
#12223=CARTESIAN_POINT('Ctrl Pts',(0.052770145372486,-0.1463268557379,0.710617093930375));
#12224=CARTESIAN_POINT('Ctrl Pts',(0.0521496093558077,-0.146549156389626,
0.710569023775148));
#12225=CARTESIAN_POINT('Ctrl Pts',(0.0512202836077782,-0.146875427406823,
0.710497532206486));
#12226=CARTESIAN_POINT('Ctrl Pts',(0.0509125608467141,-0.146982379155182,
0.710473940991376));
#12227=CARTESIAN_POINT('Ctrl Pts',(0.0503680306711304,-0.147169720129574,
0.710432341750079));
#12228=CARTESIAN_POINT('Ctrl Pts',(0.050131364257746,-0.147250505458193,
0.710414310626498));
#12229=CARTESIAN_POINT('Ctrl Pts',(0.049618126105051,-0.147424316866571,
0.710375314436903));
#12230=CARTESIAN_POINT('Ctrl Pts',(0.0493414878458612,-0.147517135352908,
0.710354361703613));
#12231=CARTESIAN_POINT('Ctrl Pts',(0.0485842181361713,-0.147768848197215,
0.710297182923058));
#12232=CARTESIAN_POINT('Ctrl Pts',(0.0481030638050704,-0.147926177605941,
0.710261047509789));
#12233=CARTESIAN_POINT('Ctrl Pts',(0.0470262035404419,-0.148272483072258,
0.710180590190179));
#12234=CARTESIAN_POINT('Ctrl Pts',(0.0464301055718878,-0.148460224929537,
0.710136336509763));
#12235=CARTESIAN_POINT('Ctrl Pts',(0.0445892835085485,-0.149027822437778,
0.710000501050794));
#12236=CARTESIAN_POINT('Ctrl Pts',(0.0433408744485835,-0.149395665725621,
0.709909538731034));
#12237=CARTESIAN_POINT('Ctrl Pts',(0.0385245689866483,-0.150749330955579,
0.709562515940091));
#12238=CARTESIAN_POINT('Ctrl Pts',(0.0349262837168794,-0.151623422729105,
0.709311430658154));
#12239=CARTESIAN_POINT('Ctrl Pts',(0.0217032330639749,-0.154339741465093,
0.70840696172466));
#12240=CARTESIAN_POINT('Ctrl Pts',(0.0119414849742218,-0.155400135168206,
0.707772694690845));
#12241=CARTESIAN_POINT('Ctrl Pts',(-0.00541271749503033,-0.155639416076207,
0.706618332509503));
#12242=CARTESIAN_POINT('Ctrl Pts',(-0.0129664430829459,-0.155192690348088,
0.706107115285203));
#12243=CARTESIAN_POINT('Ctrl Pts',(-0.021468665427403,-0.154064727335743,
0.705506414511639));
#12244=CARTESIAN_POINT('Ctrl Pts',(-0.0224788782829936,-0.153920576102233,
0.705434643730842));
#12245=CARTESIAN_POINT('Ctrl Pts',(-0.0240883403744863,-0.153674733425446,
0.705319631136846));
#12246=CARTESIAN_POINT('Ctrl Pts',(-0.0246885511904395,-0.153579449330068,
0.705276591235092));
#12247=CARTESIAN_POINT('Ctrl Pts',(-0.0257483514866636,-0.153404831741451,
0.705200325103425));
#12248=CARTESIAN_POINT('Ctrl Pts',(-0.0262081744201329,-0.153326943460039,
0.705167144937081));
#12249=CARTESIAN_POINT('Ctrl Pts',(-0.0271606444975024,-0.153161197137391,
0.705098225856666));
#12250=CARTESIAN_POINT('Ctrl Pts',(-0.0276532311613021,-0.153073027387669,
0.705062477418416));
#12251=CARTESIAN_POINT('Ctrl Pts',(-0.0289209465170841,-0.152839795923415,
0.704970198329306));
#12252=CARTESIAN_POINT('Ctrl Pts',(-0.0296954046940716,-0.15269121540844,
0.704913556584084));
#12253=CARTESIAN_POINT('Ctrl Pts',(-0.032959060693673,-0.152039311467853,
0.704673703735599));
#12254=CARTESIAN_POINT('Ctrl Pts',(-0.0354367337068162,-0.15148098363632,
0.704488755382251));
#12255=CARTESIAN_POINT('Ctrl Pts',(-0.0418850008861716,-0.149861055280161,
0.703999543462196));
#12256=CARTESIAN_POINT('Ctrl Pts',(-0.0458289086256457,-0.148702370045862,
0.703692364136736));
#12257=CARTESIAN_POINT('Ctrl Pts',(-0.0568361538246493,-0.144989050748367,
0.702812542890346));
#12258=CARTESIAN_POINT('Ctrl Pts',(-0.0637666235067489,-0.142077347630461,
0.702231166674509));
#12259=CARTESIAN_POINT('Ctrl Pts',(-0.0786196394803076,-0.134530810630353,
0.700939165071838));
#12260=CARTESIAN_POINT('Ctrl Pts',(-0.0863993512298343,-0.129671832192135,
0.700230367496002));
#12261=CARTESIAN_POINT('Ctrl Pts',(-0.0942535311948483,-0.123743859101679,
0.699509230520571));
#12262=CARTESIAN_POINT('Ctrl Pts',(-0.0947970337430191,-0.123327990529874,
0.699459303614591));
#12263=CARTESIAN_POINT('Ctrl Pts',(-0.0955991563778857,-0.122705799441843,
0.699385603908957));
#12264=CARTESIAN_POINT('Ctrl Pts',(-0.0958598813393453,-0.12250222476332,
0.699361645813828));
#12265=CARTESIAN_POINT('Ctrl Pts',(-0.0963139517615069,-0.122145348157204,
0.69931991971239));
#12266=CARTESIAN_POINT('Ctrl Pts',(-0.0965075833881976,-0.121992416700293,
0.699302125893107));
#12267=CARTESIAN_POINT('Ctrl Pts',(-0.0967017462591082,-0.121838314054877,
0.699284283190461));
#12268=CARTESIAN_POINT('Ctrl Pts',(-0.0967026378563213,-0.121837606398537,
0.699284201256644));
#12269=CARTESIAN_POINT('Ctrl Pts',(-0.0967044044783999,-0.121836204207641,
0.699284038911921));
#12270=CARTESIAN_POINT('Ctrl Pts',(-0.0967052795046704,-0.121835509672557,
0.699283958500886));
#12271=CARTESIAN_POINT('Ctrl Pts',(-0.0967070133576984,-0.121834133429989,
0.699283799167468));
#12272=CARTESIAN_POINT('Ctrl Pts',(-0.0967078721846693,-0.121833451722899,
0.699283720245065));
#12273=CARTESIAN_POINT('Ctrl Pts',(-0.0967095739965852,-0.121832100854239,
0.699283563856058));
#12274=CARTESIAN_POINT('Ctrl Pts',(-0.0967104169828092,-0.121831431692193,
0.699283486389338));
#12275=CARTESIAN_POINT('Ctrl Pts',(-0.096712087473058,-0.121830105629601,
0.69928333287863));
#12276=CARTESIAN_POINT('Ctrl Pts',(-0.0967129149730638,-0.121829448732764,
0.699283256835012));
#12277=CARTESIAN_POINT('Ctrl Pts',(-0.0967145548245948,-0.121828146937218,
0.699283106139844));
#12278=CARTESIAN_POINT('Ctrl Pts',(-0.0967153671779748,-0.121827502037534,
0.699283031488123));
#12279=CARTESIAN_POINT('Ctrl Pts',(-0.0967169770662906,-0.121826223975774,
0.69928288354642));
#12280=CARTESIAN_POINT('Ctrl Pts',(-0.0967177746039718,-0.121825590811998,
0.699282810256186));
#12281=CARTESIAN_POINT('Ctrl Pts',(-0.0967193551859499,-0.121824335965413,
0.699282665007585));
#12282=CARTESIAN_POINT('Ctrl Pts',(-0.0967201382306162,-0.121823714282771,
0.699282593049185));
#12283=CARTESIAN_POINT('Ctrl Pts',(-0.0967216901463187,-0.121822482145962,
0.699282450434868));
#12284=CARTESIAN_POINT('Ctrl Pts',(-0.0967224590141659,-0.121821871694769,
0.699282379779244));
#12285=CARTESIAN_POINT('Ctrl Pts',(-0.0967239828807618,-0.121820661780387,
0.699282239742497));
#12286=CARTESIAN_POINT('Ctrl Pts',(-0.0967247378780507,-0.121820062318781,
0.699282170361507));
#12287=CARTESIAN_POINT('Ctrl Pts',(-0.0967262342990919,-0.121818874150164,
0.699282032846867));
#12288=CARTESIAN_POINT('Ctrl Pts',(-0.0967269757237147,-0.121818285442869,
0.699281964713136));
#12289=CARTESIAN_POINT('Ctrl Pts',(-0.096728396462962,-0.121817157323821,
0.699281834153307));
#12290=CARTESIAN_POINT('Ctrl Pts',(-0.0967290757812409,-0.121816617910938,
0.699281771726873));
#12291=CARTESIAN_POINT('Ctrl Pts',(-0.0967304316296409,-0.121815541280617,
0.699281647130216));
#12292=CARTESIAN_POINT('Ctrl Pts',(-0.0967311081595325,-0.121815004063437,
0.699281584960014));
#12293=CARTESIAN_POINT('Ctrl Pts',(-0.0967324584536179,-0.121813931806913,
0.699281460873757));
#12294=CARTESIAN_POINT('Ctrl Pts',(-0.0967331322178909,-0.121813396767582,
0.699281398957695));
#12295=CARTESIAN_POINT('Ctrl Pts',(-0.0967344770057696,-0.121812328847102,
0.699281275377418));
#12296=CARTESIAN_POINT('Ctrl Pts',(-0.0967351480288432,-0.12181179596645,
0.699281213713252));
#12297=CARTESIAN_POINT('Ctrl Pts',(-0.0967364873495007,-0.121810732351498,
0.699281090635371));
#12298=CARTESIAN_POINT('Ctrl Pts',(-0.0967371556506375,-0.121810201614449,
0.699281029221331));
#12299=CARTESIAN_POINT('Ctrl Pts',(-0.0967384895595116,-0.121809142261436,
0.699280906640753));
#12300=CARTESIAN_POINT('Ctrl Pts',(-0.0967391551647717,-0.121808613647511,
0.699280845474443));
#12301=CARTESIAN_POINT('Ctrl Pts',(-0.0967404836959832,-0.121807558529772,
0.699280723388032));
#12302=CARTESIAN_POINT('Ctrl Pts',(-0.0967411466243366,-0.121807032024121,
0.69928066246771));
#12303=CARTESIAN_POINT('Ctrl Pts',(-0.0967424698314265,-0.121805981099561,
0.699280540870546));
#12304=CARTESIAN_POINT('Ctrl Pts',(-0.0967431301077306,-0.121805456682653,
0.699280480193928));
#12305=CARTESIAN_POINT('Ctrl Pts',(-0.0969739056985227,-0.121622162747296,
0.699259272885091));
#12306=CARTESIAN_POINT('Ctrl Pts',(-0.0972035052171123,-0.121438739433352,
0.699238173118612));
#12307=CARTESIAN_POINT('Ctrl Pts',(-0.0978276944467504,-0.120937180411758,
0.699180805485452));
#12308=CARTESIAN_POINT('Ctrl Pts',(-0.0982212559773331,-0.12061776113037,
0.699144627896046));
#12309=CARTESIAN_POINT('Ctrl Pts',(-0.0991018854580417,-0.119895863152338,
0.699063644506462));
#12310=CARTESIAN_POINT('Ctrl Pts',(-0.099588080074217,-0.119492326298826,
0.699018910908785));
#12311=CARTESIAN_POINT('Ctrl Pts',(-0.101083450683968,-0.118235716266999,
0.698881205651762));
#12312=CARTESIAN_POINT('Ctrl Pts',(-0.102084255965751,-0.11737271220482,
0.698788873359521));
#12313=CARTESIAN_POINT('Ctrl Pts',(-0.10591016440817,-0.113987633321759,
0.69843467673692));
#12314=CARTESIAN_POINT('Ctrl Pts',(-0.108653999531667,-0.111375295883887,
0.698178010346829));
#12315=CARTESIAN_POINT('Ctrl Pts',(-0.11844027040805,-0.101351742704892,
0.697240172004058));
#12316=CARTESIAN_POINT('Ctrl Pts',(-0.124842511012778,-0.093352211292088,
0.696579335331345));
#12317=CARTESIAN_POINT('Ctrl Pts',(-0.134248632985664,-0.0788835020583746,
0.695428563669994));
#12318=CARTESIAN_POINT('Ctrl Pts',(-0.137678259648649,-0.072732233019689,
0.694951309978228));
#12319=CARTESIAN_POINT('Ctrl Pts',(-0.141109804188978,-0.0654587067498898,
0.694387931426037));
#12320=CARTESIAN_POINT('Ctrl Pts',(-0.141531134578908,-0.0645426757093185,
0.69431700659571));
#12321=CARTESIAN_POINT('Ctrl Pts',(-0.142190640742558,-0.0630713026462111,
0.694203094601393));
#12322=CARTESIAN_POINT('Ctrl Pts',(-0.142434542903887,-0.0625185452596902,
0.694160303252533));
#12323=CARTESIAN_POINT('Ctrl Pts',(-0.142860776174381,-0.0615371279369823,
0.694084324979772));
#12324=CARTESIAN_POINT('Ctrl Pts',(-0.143044414786842,-0.0611090408493635,
0.694051182981923));
#12325=CARTESIAN_POINT('Ctrl Pts',(-0.143421937037418,-0.0602179577078676,
0.693982191268251));
#12326=CARTESIAN_POINT('Ctrl Pts',(-0.143615507670087,-0.059754835786256,
0.693946331409538));
#12327=CARTESIAN_POINT('Ctrl Pts',(-0.144110065923122,-0.0585553096000549,
0.693853439062178));
#12328=CARTESIAN_POINT('Ctrl Pts',(-0.144407648515963,-0.0578175266608104,
0.69379629263784));
#12329=CARTESIAN_POINT('Ctrl Pts',(-0.145654356664466,-0.0546569451104951,
0.693551405221163));
#12330=CARTESIAN_POINT('Ctrl Pts',(-0.146548215135496,-0.0522129522661191,
0.693361834721557));
#12331=CARTESIAN_POINT('Ctrl Pts',(-0.148739539438872,-0.0457210490005038,
0.692857372415726));
#12332=CARTESIAN_POINT('Ctrl Pts',(-0.149933042137028,-0.04164062662355,
0.692539332812466));
#12333=CARTESIAN_POINT('Ctrl Pts',(-0.15401454500164,-0.0252177077964493,
0.691256012606266));
#12334=CARTESIAN_POINT('Ctrl Pts',(-0.155556243311404,-0.0125932883211169,
0.690257429517547));
#12335=CARTESIAN_POINT('Ctrl Pts',(-0.155549981000406,7.68815545762296E-5,
0.689293189475146));
#12336=CARTESIAN_POINT('Ctrl Pts',(-0.155549980890396,7.71038094666679E-5,
0.68929317256085));
#12337=CARTESIAN_POINT('Ctrl Pts',(-0.155548056574785,0.00395923698251686,
0.688997730089396));
#12338=CARTESIAN_POINT('Ctrl Pts',(-0.15540079960715,0.00784042716544082,
0.688706369629833));
#12339=CARTESIAN_POINT('Ctrl Pts',(-0.155075286701211,0.0121511941037518,
0.688389983467841));
#12340=CARTESIAN_POINT('Ctrl Pts',(-0.155040297377641,0.0125897682665448,
0.688357878401912));
#12341=CARTESIAN_POINT('Ctrl Pts',(-0.15497865262095,0.0133231891107395,
0.68830433629505));
#12342=CARTESIAN_POINT('Ctrl Pts',(-0.154953015720463,0.0136181151163825,
0.688282845453773));
#12343=CARTESIAN_POINT('Ctrl Pts',(-0.154904757642047,0.0141554883212025,
0.688243762381385));
#12344=CARTESIAN_POINT('Ctrl Pts',(-0.154882408930206,0.0143979580482441,
0.688226155275795));
#12345=CARTESIAN_POINT('Ctrl Pts',(-0.154835217158718,0.0148971319366596,
0.688189965794114));
#12346=CARTESIAN_POINT('Ctrl Pts',(-0.154810305346525,0.0151538237033385,
0.68817138804088));
#12347=CARTESIAN_POINT('Ctrl Pts',(-0.154752344408021,0.0157359912993524,
0.68812932610603));
#12348=CARTESIAN_POINT('Ctrl Pts',(-0.154718906907653,0.0160614249862333,
0.688105863960416));
#12349=CARTESIAN_POINT('Ctrl Pts',(-0.154629746679346,0.0169030620505461,
0.688045311430264));
#12350=CARTESIAN_POINT('Ctrl Pts',(-0.154572465116616,0.0174191019555854,
0.688008306387435));
#12351=CARTESIAN_POINT('Ctrl Pts',(-0.154201181055804,0.0206177932842343,
0.687779631978769));
#12352=CARTESIAN_POINT('Ctrl Pts',(-0.153819910266708,0.0232923853163874,
0.687591491639772));
#12353=CARTESIAN_POINT('Ctrl Pts',(-0.153044980709305,0.0278713163664628,
0.687272560353994));
#12354=CARTESIAN_POINT('Ctrl Pts',(-0.152684951868742,0.029780572569399,
0.687140533614673));
#12355=CARTESIAN_POINT('Ctrl Pts',(-0.149850644858165,0.0434042532131832,
0.686202102441212));
#12356=CARTESIAN_POINT('Ctrl Pts',(-0.146066886193278,0.0548054974957794,
0.685433189541829));
#12357=CARTESIAN_POINT('Ctrl Pts',(-0.139216402343899,0.0695176245208165,
0.684346709819848));
#12358=CARTESIAN_POINT('Ctrl Pts',(-0.137262951775136,0.0732992780673955,
0.684058575602304));
#12359=CARTESIAN_POINT('Ctrl Pts',(-0.133867993735918,0.0792587214602847,
0.683585924482481));
#12360=CARTESIAN_POINT('Ctrl Pts',(-0.132522354160731,0.0814887043504419,
0.683404658647205));
#12361=CARTESIAN_POINT('Ctrl Pts',(-0.130693321582756,0.084354558036373,
0.683165338058722));
#12362=CARTESIAN_POINT('Ctrl Pts',(-0.130260068153889,0.0850220581387679,
0.683109134882886));
#12363=CARTESIAN_POINT('Ctrl Pts',(-0.129545185613298,0.0861051647237944,
0.683017165748169));
#12364=CARTESIAN_POINT('Ctrl Pts',(-0.129266628529204,0.0865227903249757,
0.682981514826514));
#12365=CARTESIAN_POINT('Ctrl Pts',(-0.128725717600621,0.087325306151855,
0.682912637185019));
#12366=CARTESIAN_POINT('Ctrl Pts',(-0.128463646509426,0.0877103812734499,
0.682879421384209));
#12367=CARTESIAN_POINT('Ctrl Pts',(-0.127857749995387,0.0885921167593224,
0.682802978899054));
#12368=CARTESIAN_POINT('Ctrl Pts',(-0.12751275505738,0.0890879602662635,
0.682759708149617));
#12369=CARTESIAN_POINT('Ctrl Pts',(-0.126584451991756,0.0904057233087287,
0.682643943686541));
#12370=CARTESIAN_POINT('Ctrl Pts',(-0.125996037532316,0.0912239920758776,
0.682571255456006));
#12371=CARTESIAN_POINT('Ctrl Pts',(-0.121246579160543,0.0976951311066141,
0.681989871605733));
#12372=CARTESIAN_POINT('Ctrl Pts',(-0.116715854506798,0.103065285289254,
0.681466714900051));
#12373=CARTESIAN_POINT('Ctrl Pts',(-0.104725685928213,0.115468931355165,
0.680152935583966));
#12374=CARTESIAN_POINT('Ctrl Pts',(-0.0969039435813654,0.122107098736112,
0.679351573746187));
#12375=CARTESIAN_POINT('Ctrl Pts',(-0.0853706033661158,0.130084705134222,
0.678273735803344));
#12376=CARTESIAN_POINT('Ctrl Pts',(-0.082175160234284,0.132126522617949,
0.677985047102469));
#12377=CARTESIAN_POINT('Ctrl Pts',(-0.0777686033058295,0.134720433213035,
0.677602921839187));
#12378=CARTESIAN_POINT('Ctrl Pts',(-0.0766205822576034,0.135376650302601,
0.67750478131097));
#12379=CARTESIAN_POINT('Ctrl Pts',(-0.0749115506911382,0.136324838650471,
0.677360903756288));
#12380=CARTESIAN_POINT('Ctrl Pts',(-0.0743569380349156,0.136628137150924,
0.677314553919367));
#12381=CARTESIAN_POINT('Ctrl Pts',(-0.0733506689532501,0.137170488695617,
0.677231093725719));
#12382=CARTESIAN_POINT('Ctrl Pts',(-0.0728996576866927,0.137410711132035,
0.677193915534618));
#12383=CARTESIAN_POINT('Ctrl Pts',(-0.0721883460888214,0.137785089647908,
0.677135648498658));
#12384=CARTESIAN_POINT('Ctrl Pts',(-0.0719288423143392,0.137920737699267,
0.677114467982603));
#12385=CARTESIAN_POINT('Ctrl Pts',(-0.0714399602564044,0.138174531476272,
0.677074712035956));
#12386=CARTESIAN_POINT('Ctrl Pts',(-0.0712106735813902,0.138292837992195,
0.677056126966165));
#12387=CARTESIAN_POINT('Ctrl Pts',(-0.0706887849509646,0.13856047810894,
0.677013961093206));
#12388=CARTESIAN_POINT('Ctrl Pts',(-0.0703960041067318,0.138709455419689,
0.676990402773698));
#12389=CARTESIAN_POINT('Ctrl Pts',(-0.0695021677941161,0.139160712145041,
0.676918769035741));
#12390=CARTESIAN_POINT('Ctrl Pts',(-0.0688996103649754,0.139460026058571,
0.676870874489821));
#12391=CARTESIAN_POINT('Ctrl Pts',(-0.0667713643040441,0.14050004870385,
0.676703030614361));
#12392=CARTESIAN_POINT('Ctrl Pts',(-0.0652356599949374,0.141219639250885,
0.676584293174888));
#12393=CARTESIAN_POINT('Ctrl Pts',(-0.0636886255638827,0.141913922762298,
0.676466729580158));
#12394=CARTESIAN_POINT('Ctrl Pts',(-0.063688650901166,0.141913911391341,
0.662679920979917));
#12395=CARTESIAN_POINT('Ctrl Pts',(-0.068017198513575,0.13997132975792,
0.663036542399741));
#12396=CARTESIAN_POINT('Ctrl Pts',(-0.0722564768373429,0.137830888847813,
0.663398887752939));
#12397=CARTESIAN_POINT('Ctrl Pts',(-0.0823242436398772,0.132154769206293,
0.664289282501908));
#12398=CARTESIAN_POINT('Ctrl Pts',(-0.0880293688476399,0.128425043328055,
0.664819914915556));
#12399=CARTESIAN_POINT('Ctrl Pts',(-0.096980935203349,0.12169542033187,
0.665683656014293));
#12400=CARTESIAN_POINT('Ctrl Pts',(-0.100377194888951,0.118909638481955,
0.666019496001153));
#12401=CARTESIAN_POINT('Ctrl Pts',(-0.105287253112897,0.114521660550206,
0.66651276070101));
#12402=CARTESIAN_POINT('Ctrl Pts',(-0.106892224411513,0.113025086184047,
0.666675320035616));
#12403=CARTESIAN_POINT('Ctrl Pts',(-0.108832375128955,0.111137658665867,
0.666872923066296));
#12404=CARTESIAN_POINT('Ctrl Pts',(-0.109197889274138,0.110778545070602,
0.666910199700956));
#12405=CARTESIAN_POINT('Ctrl Pts',(-0.109770801141017,0.110210074616639,
0.666968695988504));
#12406=CARTESIAN_POINT('Ctrl Pts',(-0.10997938538448,0.110001927821948,
0.666990007588517));
#12407=CARTESIAN_POINT('Ctrl Pts',(-0.110369854245646,0.109610057054866,
0.667029927782906));
#12408=CARTESIAN_POINT('Ctrl Pts',(-0.110551870131244,0.10942647461075,
0.667048546446941));
#12409=CARTESIAN_POINT('Ctrl Pts',(-0.110968381864329,0.109004278111474,
0.667091176375138));
#12410=CARTESIAN_POINT('Ctrl Pts',(-0.111202565996398,0.10876536094595,
0.667115163145199));
#12411=CARTESIAN_POINT('Ctrl Pts',(-0.111927105996519,0.108021391223322,
0.667189439115347));
#12412=CARTESIAN_POINT('Ctrl Pts',(-0.112414815037905,0.107513754602276,
0.667239527358037));
#12413=CARTESIAN_POINT('Ctrl Pts',(-0.117790473135738,0.10184187731401,
0.667792873615856));
#12414=CARTESIAN_POINT('Ctrl Pts',(-0.122323032149567,0.0963507700116848,
0.668271257306462));
#12415=CARTESIAN_POINT('Ctrl Pts',(-0.131528878105711,0.083496195099452,
0.669319885775283));
#12416=CARTESIAN_POINT('Ctrl Pts',(-0.135991181485854,0.0760122343812776,
0.669885513167569));
#12417=CARTESIAN_POINT('Ctrl Pts',(-0.142578586869586,0.0625074910798073,
0.670888272363713));
#12418=CARTESIAN_POINT('Ctrl Pts',(-0.145002715499442,0.0566571867506787,
0.671317233501453));
#12419=CARTESIAN_POINT('Ctrl Pts',(-0.147545489508619,0.0492779641791501,
0.671861516353689));
#12420=CARTESIAN_POINT('Ctrl Pts',(-0.148007272575461,0.0478731263711093,
0.671965256782573));
#12421=CARTESIAN_POINT('Ctrl Pts',(-0.148640062992512,0.0458513203841124,
0.672114826235472));
#12422=CARTESIAN_POINT('Ctrl Pts',(-0.148827410435187,0.045239515784646,
0.672160121225386));
#12423=CARTESIAN_POINT('Ctrl Pts',(-0.149145760143502,0.0441765259790005,
0.672238888096389));
#12424=CARTESIAN_POINT('Ctrl Pts',(-0.149278503926231,0.0437258673218194,
0.672272302819173));
#12425=CARTESIAN_POINT('Ctrl Pts',(-0.149529880770881,0.0428579679601338,
0.672336698404793));
#12426=CARTESIAN_POINT('Ctrl Pts',(-0.149648814251913,0.0424408181707076,
0.672367669154412));
#12427=CARTESIAN_POINT('Ctrl Pts',(-0.149955946836966,0.0413462313604879,
0.672448989485316));
#12428=CARTESIAN_POINT('Ctrl Pts',(-0.150141298564831,0.0406680129175078,
0.67249943073348));
#12429=CARTESIAN_POINT('Ctrl Pts',(-0.150769090616767,0.0383080640462042,
0.67267515177128));
#12430=CARTESIAN_POINT('Ctrl Pts',(-0.1511879085321,0.0366202445901691,
0.672801187063284));
#12431=CARTESIAN_POINT('Ctrl Pts',(-0.154228616276149,0.0234235497555797,
0.673789832264847));
#12432=CARTESIAN_POINT('Ctrl Pts',(-0.155560517056396,0.0116593737878267,
0.674694483054675));
#12433=CARTESIAN_POINT('Ctrl Pts',(-0.155544977013624,-0.00567160696188913,
0.676038358415671));
#12434=CARTESIAN_POINT('Ctrl Pts',(-0.155244895077116,-0.0111997338309086,
0.676467881282379));
#12435=CARTESIAN_POINT('Ctrl Pts',(-0.154171825791168,-0.0211367527301333,
0.67723176138205));
#12436=CARTESIAN_POINT('Ctrl Pts',(-0.153502005772645,-0.0255510788692451,
0.677568072100292));
#12437=CARTESIAN_POINT('Ctrl Pts',(-0.152515935877645,-0.0305798805954947,
0.67794344683171));
#12438=CARTESIAN_POINT('Ctrl Pts',(-0.152384551991569,-0.0312280026626399,
0.677991675472776));
#12439=CARTESIAN_POINT('Ctrl Pts',(-0.152182202474545,-0.0321945044890838,
0.678063351289277));
#12440=CARTESIAN_POINT('Ctrl Pts',(-0.152114364642188,-0.0325135194051921,
0.678086969586603));
#12441=CARTESIAN_POINT('Ctrl Pts',(-0.151991120312434,-0.0330842602826696,
0.678129150189201));
#12442=CARTESIAN_POINT('Ctrl Pts',(-0.151936091315621,-0.0333360629282256,
0.678147733572009));
#12443=CARTESIAN_POINT('Ctrl Pts',(-0.151815586118259,-0.0338809756018943,
0.678187892017362));
#12444=CARTESIAN_POINT('Ctrl Pts',(-0.151749887030346,-0.0341740323433377,
0.678209454121508));
#12445=CARTESIAN_POINT('Ctrl Pts',(-0.151564095228498,-0.0349916724720893,
0.678269519380939));
#12446=CARTESIAN_POINT('Ctrl Pts',(-0.15144212677316,-0.0355158326118633,
0.678307917057136));
#12447=CARTESIAN_POINT('Ctrl Pts',(-0.150720649827556,-0.0385450774292413,
0.678529257147511));
#12448=CARTESIAN_POINT('Ctrl Pts',(-0.150061666619405,-0.0410357841172182,
0.678708992518197));
#12449=CARTESIAN_POINT('Ctrl Pts',(-0.145222769189471,-0.0576448396847631,
0.679899500002206));
#12450=CARTESIAN_POINT('Ctrl Pts',(-0.139118076193454,-0.0711255991963758,
0.680832789825957));
#12451=CARTESIAN_POINT('Ctrl Pts',(-0.130206582842128,-0.08512064414634,
0.68194741897197));
#12452=CARTESIAN_POINT('Ctrl Pts',(-0.129177055985994,-0.0866750604225387,
0.682073351012123));
#12453=CARTESIAN_POINT('Ctrl Pts',(-0.125815431985952,-0.0915575919891249,
0.682476466585702));
#12454=CARTESIAN_POINT('Ctrl Pts',(-0.12338091746222,-0.0948127620834062,
0.68275669834497));
#12455=CARTESIAN_POINT('Ctrl Pts',(-0.120273046910367,-0.098645609184231,
0.683103111027972));
#12456=CARTESIAN_POINT('Ctrl Pts',(-0.119718484239365,-0.0993179062447148,
0.683164513302434));
#12457=CARTESIAN_POINT('Ctrl Pts',(-0.118792444629253,-0.10042151947745,
0.683266395062366));
#12458=CARTESIAN_POINT('Ctrl Pts',(-0.118424191953835,-0.100855526470347,
0.683306743395405));
#12459=CARTESIAN_POINT('Ctrl Pts',(-0.117753774679885,-0.101636917605477,
0.683379905781965));
#12460=CARTESIAN_POINT('Ctrl Pts',(-0.117452432537582,-0.101985001614719,
0.683412685750271));
#12461=CARTESIAN_POINT('Ctrl Pts',(-0.116802903639582,-0.102728583422733,
0.683483119938));
#12462=CARTESIAN_POINT('Ctrl Pts',(-0.116454244598768,-0.103123659036102,
0.683520793529576));
#12463=CARTESIAN_POINT('Ctrl Pts',(-0.115498747311813,-0.104195335346355,
0.683623678845034));
#12464=CARTESIAN_POINT('Ctrl Pts',(-0.114887983981592,-0.104868391854024,
0.683689054668293));
#12465=CARTESIAN_POINT('Ctrl Pts',(-0.111642695206594,-0.108382296460608,
0.68403444839281));
#12466=CARTESIAN_POINT('Ctrl Pts',(-0.108908836611452,-0.111129086813327,
0.684318687967596));
#12467=CARTESIAN_POINT('Ctrl Pts',(-0.0952395680371516,-0.123873791632705,
0.685710298570283));
#12468=CARTESIAN_POINT('Ctrl Pts',(-0.0830164219644928,-0.132376046640035,
0.686878067383553));
#12469=CARTESIAN_POINT('Ctrl Pts',(-0.0658083933527459,-0.141013497902221,
0.688349445391028));
#12470=CARTESIAN_POINT('Ctrl Pts',(-0.0617526037190603,-0.142836186894842,
0.688684336672733));
#12471=CARTESIAN_POINT('Ctrl Pts',(-0.0570101957502238,-0.144727594430487,
0.689058322529715));
#12472=CARTESIAN_POINT('Ctrl Pts',(-0.0563949464308064,-0.144968441628414,
0.689106507441296));
#12473=CARTESIAN_POINT('Ctrl Pts',(-0.055473824203223,-0.145322275030348,
0.689178131172802));
#12474=CARTESIAN_POINT('Ctrl Pts',(-0.0551691112552447,-0.145438227300577,
0.689201740755889));
#12475=CARTESIAN_POINT('Ctrl Pts',(-0.0546228605468499,-0.145644128042777,
0.689243911973408));
#12476=CARTESIAN_POINT('Ctrl Pts',(-0.0543814628258599,-0.145734434613504,
0.689262494645179));
#12477=CARTESIAN_POINT('Ctrl Pts',(-0.0538582053854122,-0.145928703349405,
0.689302658588828));
#12478=CARTESIAN_POINT('Ctrl Pts',(-0.0535762693818314,-0.146032448831979,
0.68932422687121));
#12479=CARTESIAN_POINT('Ctrl Pts',(-0.0527880776877376,-0.146319894031104,
0.689384326743801));
#12480=CARTESIAN_POINT('Ctrl Pts',(-0.0522811592007497,-0.146501784804078,
0.689422752657956));
#12481=CARTESIAN_POINT('Ctrl Pts',(-0.0493382173653042,-0.147540540710993,
0.689644581509973));
#12482=CARTESIAN_POINT('Ctrl Pts',(-0.0468819191985013,-0.148339335988197,
0.689824760815528));
#12483=CARTESIAN_POINT('Ctrl Pts',(-0.0303010697154155,-0.15327840894129,
0.691015260900772));
#12484=CARTESIAN_POINT('Ctrl Pts',(-0.0156691863389914,-0.155457426698968,
0.691948243831195));
#12485=CARTESIAN_POINT('Ctrl Pts',(0.000923992207560616,-0.155558515738684,
0.69306302336376));
#12486=CARTESIAN_POINT('Ctrl Pts',(0.00279560811795781,-0.155536136534543,
0.693189453402145));
#12487=CARTESIAN_POINT('Ctrl Pts',(0.00872016387768964,-0.155358326918353,
0.693592551480902));
#12488=CARTESIAN_POINT('Ctrl Pts',(0.0127673665477948,-0.155078175287072,
0.693872248081887));
#12489=CARTESIAN_POINT('Ctrl Pts',(0.0176644519419164,-0.154546200123709,
0.694218058525394));
#12490=CARTESIAN_POINT('Ctrl Pts',(0.0185293621350384,-0.154444888290468,
0.694279413225571));
#12491=CARTESIAN_POINT('Ctrl Pts',(0.0199578980157496,-0.154265383483883,
0.694381232335576));
#12492=CARTESIAN_POINT('Ctrl Pts',(0.0205220350325007,-0.154191349618434,
0.694421565877277));
#12493=CARTESIAN_POINT('Ctrl Pts',(0.0215418854419725,-0.154051814754689,
0.694494712436008));
#12494=CARTESIAN_POINT('Ctrl Pts',(0.0219977405802601,-0.153987382140934,
0.694527491435966));
#12495=CARTESIAN_POINT('Ctrl Pts',(0.0229748573558366,-0.153844844703004,
0.694597935721334));
#12496=CARTESIAN_POINT('Ctrl Pts',(0.0234960201244876,-0.153766112449707,
0.694635620431662));
#12497=CARTESIAN_POINT('Ctrl Pts',(0.024915422524783,-0.153544298248632,
0.694738567113799));
#12498=CARTESIAN_POINT('Ctrl Pts',(0.0258128110277106,-0.153395986015988,
0.69480399351563));
#12499=CARTESIAN_POINT('Ctrl Pts',(0.0305352080194024,-0.152572899030745,
0.695150138013753));
#12500=CARTESIAN_POINT('Ctrl Pts',(0.0343349179965368,-0.151762962761304,
0.695435099683119));
#12501=CARTESIAN_POINT('Ctrl Pts',(0.0524572277745169,-0.147184667285636,
0.696827025332424));
#12502=CARTESIAN_POINT('Ctrl Pts',(0.0662218406495348,-0.141525996856218,
0.697994265901072));
#12503=CARTESIAN_POINT('Ctrl Pts',(0.0828004875208679,-0.131755820335562,
0.699464785448405));
#12504=CARTESIAN_POINT('Ctrl Pts',(0.0865279212759689,-0.129338489521177,
0.699799377249114));
#12505=CARTESIAN_POINT('Ctrl Pts',(0.0906855103241419,-0.126381869980952,
0.700173069982034));
#12506=CARTESIAN_POINT('Ctrl Pts',(0.0912214013173557,-0.12599561431374,
0.700221245611605));
#12507=CARTESIAN_POINT('Ctrl Pts',(0.0920180708579799,-0.125413649220629,
0.700292858286985));
#12508=CARTESIAN_POINT('Ctrl Pts',(0.0922807116386719,-0.125220521640903,
0.700316466019855));
#12509=CARTESIAN_POINT('Ctrl Pts',(0.0927499054741206,-0.124873231563961,
0.700358635245281));
#12510=CARTESIAN_POINT('Ctrl Pts',(0.0929566833736199,-0.124719380797038,
0.700377217766641));
#12511=CARTESIAN_POINT('Ctrl Pts',(0.0934036705001353,-0.124385075860508,
0.700417382880235));
#12512=CARTESIAN_POINT('Ctrl Pts',(0.0936437389667213,-0.124204440002033,
0.700438952476365));
#12513=CARTESIAN_POINT('Ctrl Pts',(0.0943127491122702,-0.123698011227758,
0.700499059709901));
#12514=CARTESIAN_POINT('Ctrl Pts',(0.0947405298629848,-0.123370679867716,
0.700537491629346));
#12515=CARTESIAN_POINT('Ctrl Pts',(0.0972103351503213,-0.12146039992029,
0.700759424604099));
#12516=CARTESIAN_POINT('Ctrl Pts',(0.0992145216248112,-0.119828873039177,
0.700939698487263));
#12517=CARTESIAN_POINT('Ctrl Pts',(0.112355582129889,-0.10857539188738,
0.702130197129907));
#12518=CARTESIAN_POINT('Ctrl Pts',(0.122119935124537,-0.0974639593988757,
0.703063114775693));
#12519=CARTESIAN_POINT('Ctrl Pts',(0.131203062074052,-0.0835767189661042,
0.704177927175531));
#12520=CARTESIAN_POINT('Ctrl Pts',(0.132199986392239,-0.0819906986190413,
0.704304464028192));
#12521=CARTESIAN_POINT('Ctrl Pts',(0.135263033294116,-0.0769165038369862,
0.704707554756115));
#12522=CARTESIAN_POINT('Ctrl Pts',(0.137221418644689,-0.0733656193836609,
0.704987132868446));
#12523=CARTESIAN_POINT('Ctrl Pts',(0.139429156431116,-0.0689642731076854,
0.705332812218683));
#12524=CARTESIAN_POINT('Ctrl Pts',(0.139812998036409,-0.0681827408774246,
0.705394158646061));
#12525=CARTESIAN_POINT('Ctrl Pts',(0.140436766469974,-0.0668852810136515,
0.705495966861504));
#12526=CARTESIAN_POINT('Ctrl Pts',(0.140680463639622,-0.0663711784387937,
0.705536297830852));
#12527=CARTESIAN_POINT('Ctrl Pts',(0.141116247230638,-0.0654386676416063,
0.705609441637799));
#12528=CARTESIAN_POINT('Ctrl Pts',(0.141309307831825,-0.0650207195200458,
0.705642220470181));
#12529=CARTESIAN_POINT('Ctrl Pts',(0.14171942205374,-0.0641224278479023,
0.705712666515595));
#12530=CARTESIAN_POINT('Ctrl Pts',(0.141935894624611,-0.0636418270073892,
0.705750353162732));
#12531=CARTESIAN_POINT('Ctrl Pts',(0.142519289510958,-0.0623288227238584,
0.705853310535296));
#12532=CARTESIAN_POINT('Ctrl Pts',(0.142881354083872,-0.0614942974160983,
0.705918745748376));
#12533=CARTESIAN_POINT('Ctrl Pts',(0.144751316558782,-0.0570785238603094,
0.706265021247061));
#12534=CARTESIAN_POINT('Ctrl Pts',(0.146131817579184,-0.0534451908844771,
0.706550108933191));
#12535=CARTESIAN_POINT('Ctrl Pts',(0.152111900153953,-0.0357354340290918,
0.70794208972485));
#12536=CARTESIAN_POINT('Ctrl Pts',(0.154821087855728,-0.0211029662831042,
0.709109238293607));
#12537=CARTESIAN_POINT('Ctrl Pts',(0.155602013593444,-0.00187731027392902,
0.710579608063287));
#12538=CARTESIAN_POINT('Ctrl Pts',(0.155592231567148,0.00256466499622176,
0.710914147470928));
#12539=CARTESIAN_POINT('Ctrl Pts',(0.15536265919091,0.00766047926721451,
0.711287788919633));
#12540=CARTESIAN_POINT('Ctrl Pts',(0.155328727619254,0.00832017016775597,
0.711335962923356));
#12541=CARTESIAN_POINT('Ctrl Pts',(0.155271774790372,0.00930509139248887,
0.711407573662109));
#12542=CARTESIAN_POINT('Ctrl Pts',(0.155251932392416,0.00963048628550986,
0.711431181070874));
#12543=CARTESIAN_POINT('Ctrl Pts',(0.15521457096105,0.0102130254034281,
0.711473349947363));
#12544=CARTESIAN_POINT('Ctrl Pts',(0.155197435745348,0.0104701894976847,
0.711491932442396));
#12545=CARTESIAN_POINT('Ctrl Pts',(0.155158941812179,0.0110270366554358,
0.711532097761023));
#12546=CARTESIAN_POINT('Ctrl Pts',(0.155137354088246,0.0113266999756158,
0.711553667587355));
#12547=CARTESIAN_POINT('Ctrl Pts',(0.155074637691405,0.0121634447318391,
0.711613776110747));
#12548=CARTESIAN_POINT('Ctrl Pts',(0.155031586738179,0.0127003850033983,
0.711652209082502));
#12549=CARTESIAN_POINT('Ctrl Pts',(0.154765856369803,0.0158116718584473,
0.711874160309211));
#12550=CARTESIAN_POINT('Ctrl Pts',(0.154481830883446,0.0183805685041798,
0.712054450771302));
#12551=CARTESIAN_POINT('Ctrl Pts',(0.152152610299058,0.0355242166807686,
0.71324494916589));
#12552=CARTESIAN_POINT('Ctrl Pts',(0.148111738869294,0.0497534819534633,
0.714177855371147));
#12553=CARTESIAN_POINT('Ctrl Pts',(0.141369157485213,0.0649158978496598,
0.715292673562299));
#12554=CARTESIAN_POINT('Ctrl Pts',(0.140577064666596,0.0666138197572454,
0.715419229164823));
#12555=CARTESIAN_POINT('Ctrl Pts',(0.137974711268721,0.0719389552762498,
0.715822318605974));
#12556=CARTESIAN_POINT('Ctrl Pts',(0.136053369318516,0.0755096685069591,
0.716101875922684));
#12557=CARTESIAN_POINT('Ctrl Pts',(0.133552716758185,0.0797510654385667,
0.716447532265028));
#12558=CARTESIAN_POINT('Ctrl Pts',(0.133104230248,0.0804973566478612,0.71650887724018));
#12559=CARTESIAN_POINT('Ctrl Pts',(0.132352370400346,0.0817250037313298,
0.716610683543158));
#12560=CARTESIAN_POINT('Ctrl Pts',(0.132052574800892,0.0822085376243107,
0.716651014060941));
#12561=CARTESIAN_POINT('Ctrl Pts',(0.131505395881217,0.0830803545301993,
0.716724157384853));
#12562=CARTESIAN_POINT('Ctrl Pts',(0.13125892735468,0.0834692065140469,
0.716756936187843));
#12563=CARTESIAN_POINT('Ctrl Pts',(0.130726573604193,0.0843009092418634,
0.716827382542345));
#12564=CARTESIAN_POINT('Ctrl Pts',(0.130440157072864,0.0847434112806142,
0.716865069529576));
#12565=CARTESIAN_POINT('Ctrl Pts',(0.129653314814835,0.0859456108310081,
0.716968028779353));
#12566=CARTESIAN_POINT('Ctrl Pts',(0.129148471793413,0.0867023773128583,
0.717033465539673));
#12567=CARTESIAN_POINT('Ctrl Pts',(0.126452185197167,0.0906683444717917,
0.717379764048225));
#12568=CARTESIAN_POINT('Ctrl Pts',(0.124147878108818,0.0937987377124655,
0.717664873869456));
#12569=CARTESIAN_POINT('Ctrl Pts',(0.112510817896961,0.108426754153507,
0.719056864351944));
#12570=CARTESIAN_POINT('Ctrl Pts',(0.101685834197047,0.118637638695264,
0.720223996766467));
#12571=CARTESIAN_POINT('Ctrl Pts',(0.0859561132231783,0.129719145390344,
0.721694342009498));
#12572=CARTESIAN_POINT('Ctrl Pts',(0.0822187321792526,0.132119639955574,
0.722028873941542));
#12573=CARTESIAN_POINT('Ctrl Pts',(0.0778128282158,0.13469002395874,0.722402506895644));
#12574=CARTESIAN_POINT('Ctrl Pts',(0.0772401708133397,0.135019238790746,
0.722450679531708));
#12575=CARTESIAN_POINT('Ctrl Pts',(0.0763817739542957,0.135505473607316,
0.722522288641374));
#12576=CARTESIAN_POINT('Ctrl Pts',(0.0760976199348284,0.135665253530529,
0.722545895777497));
#12577=CARTESIAN_POINT('Ctrl Pts',(0.0755922805287867,0.135947318832112,
0.722587703039956));
#12578=CARTESIAN_POINT('Ctrl Pts',(0.0753712983987127,0.136069959044185,
0.722605925603602));
#12579=CARTESIAN_POINT('Ctrl Pts',(0.0748947144111918,0.136332935403301,
0.722645097131703));
#12580=CARTESIAN_POINT('Ctrl Pts',(0.0746390173088581,0.136473091198937,
0.722666034555502));
#12581=CARTESIAN_POINT('Ctrl Pts',(0.0741084946162756,0.136761950719259,
0.722709315728716));
#12582=CARTESIAN_POINT('Ctrl Pts',(0.0738336116769774,0.136910547183552,
0.722731652718698));
#12583=CARTESIAN_POINT('Ctrl Pts',(0.0731355265874104,0.137285204772479,
0.72278815984087));
#12584=CARTESIAN_POINT('Ctrl Pts',(0.0727117188291189,0.137510140205285,
0.722822261778076));
#12585=CARTESIAN_POINT('Ctrl Pts',(0.071490863686974,0.138150885147711,
0.722919935026978));
#12586=CARTESIAN_POINT('Ctrl Pts',(0.070691227261039,0.138561759304666,
0.722983222341033));
#12587=CARTESIAN_POINT('Ctrl Pts',(0.0615260607739091,0.143171066941971,
0.723701319482948));
#12588=CARTESIAN_POINT('Ctrl Pts',(0.0528002153092404,0.146613783699978,
0.724316828381261));
#12589=CARTESIAN_POINT('Ctrl Pts',(0.0327889707256326,0.152488605101206,
0.725689542534843));
#12590=CARTESIAN_POINT('Ctrl Pts',(0.0214381869515838,0.154493521305979,
0.726444795148573));
#12591=CARTESIAN_POINT('Ctrl Pts',(0.00822654953847539,0.155342143845186,
0.727364808355722));
#12592=CARTESIAN_POINT('Ctrl Pts',(0.00648051060938771,0.155424773837839,
0.727487129460105));
#12593=CARTESIAN_POINT('Ctrl Pts',(0.00402922224027828,0.155499403050392,
0.72766004637409));
#12594=CARTESIAN_POINT('Ctrl Pts',(0.00332480763725275,0.155516058995937,
0.727709873957952));
#12595=CARTESIAN_POINT('Ctrl Pts',(0.00218631863673489,0.155535240111994,
0.727790638388596));
#12596=CARTESIAN_POINT('Ctrl Pts',(0.00175229812578089,0.155540735340245,
0.727821482295465));
#12597=CARTESIAN_POINT('Ctrl Pts',(0.000848684763719505,0.15554839361092,
0.72788581431212));
#12598=CARTESIAN_POINT('Ctrl Pts',(0.000379094422689995,0.155550246863475,
0.727919311763792));
#12599=CARTESIAN_POINT('Ctrl Pts',(-0.000729141509548038,0.155549602138571,
0.727998523893856));
#12600=CARTESIAN_POINT('Ctrl Pts',(-0.0013677732940302,0.155545297410417,
0.728044294469447));
#12601=CARTESIAN_POINT('Ctrl Pts',(-0.00347811302031817,0.155518075063737,
0.728195962925053));
#12602=CARTESIAN_POINT('Ctrl Pts',(-0.00494948184701168,0.155478201990687,
0.728302386616676));
#12603=CARTESIAN_POINT('Ctrl Pts',(-0.0126876976832074,0.15515855012282,
0.728865835223222));
#12604=CARTESIAN_POINT('Ctrl Pts',(-0.0189330890713884,0.154520780887436,
0.729333872232452));
#12605=CARTESIAN_POINT('Ctrl Pts',(-0.0343353319763814,0.152000139872101,
0.730521081495637));
#12606=CARTESIAN_POINT('Ctrl Pts',(-0.0433935718138847,0.149666067153807,
0.731249759660826));
#12607=CARTESIAN_POINT('Ctrl Pts',(-0.0560812712273453,0.145147451604106,
0.732289502199682));
#12608=CARTESIAN_POINT('Ctrl Pts',(-0.0599181983650028,0.143606028342147,
0.732606338978805));
#12609=CARTESIAN_POINT('Ctrl Pts',(-0.0636886287602419,0.141913921327825,
0.732917465391055));
#12610=CARTESIAN_POINT('Origin',(0.,0.,-0.129405622560373));
#12611=CARTESIAN_POINT('',(-0.0636886258329888,0.141913922641528,0.816746504307747));
#12612=CARTESIAN_POINT('',(-0.0636886325197553,0.141913919640617,0.802807733721352));
#12613=CARTESIAN_POINT('',(-0.0636886258329924,0.141913922641526,-0.129405622560373));
#12614=CARTESIAN_POINT('Ctrl Pts',(-0.0636886258329888,0.141913922641528,
0.816746504307747));
#12615=CARTESIAN_POINT('Ctrl Pts',(-0.0626085849357707,0.14239862716739,
0.816663661869299));
#12616=CARTESIAN_POINT('Ctrl Pts',(-0.061523072900136,0.142870974281785,
0.816580416551277));
#12617=CARTESIAN_POINT('Ctrl Pts',(-0.0598935254377186,0.143558037018761,
0.816455425860265));
#12618=CARTESIAN_POINT('Ctrl Pts',(-0.0593534800960053,0.143782157327041,
0.816413999010022));
#12619=CARTESIAN_POINT('Ctrl Pts',(-0.0583832635698295,0.144178402337241,
0.816339560473828));
#12620=CARTESIAN_POINT('Ctrl Pts',(-0.0579535603104242,0.144351660899428,
0.816306587444798));
#12621=CARTESIAN_POINT('Ctrl Pts',(-0.0570488798741372,0.144711742125908,
0.816237154243));
#12622=CARTESIAN_POINT('Ctrl Pts',(-0.056573745295578,0.144898151595469,
0.816200680660453));
#12623=CARTESIAN_POINT('Ctrl Pts',(-0.055320109028202,0.145382884469277,
0.816104420640522));
#12624=CARTESIAN_POINT('Ctrl Pts',(-0.0545401206827073,0.145677289737176,
0.816044504199232));
#12625=CARTESIAN_POINT('Ctrl Pts',(-0.0512584627898476,0.146885896426461,
0.81579227986365));
#12626=CARTESIAN_POINT('Ctrl Pts',(-0.048736031798294,0.14774198507016,
0.815598065871951));
#12627=CARTESIAN_POINT('Ctrl Pts',(-0.0315718790675979,0.153079954475024,
0.81427322900165));
#12628=CARTESIAN_POINT('Ctrl Pts',(-0.0163612209060666,0.155442490040404,
0.813071153392481));
#12629=CARTESIAN_POINT('Ctrl Pts',(0.00426227194055146,0.155582527565222,
0.811487537108713));
#12630=CARTESIAN_POINT('Ctrl Pts',(0.00957980275595861,0.155345845516234,
0.811084657667849));
#12631=CARTESIAN_POINT('Ctrl Pts',(0.0155236950559502,0.154774809316907,
0.810647354029034));
#12632=CARTESIAN_POINT('Ctrl Pts',(0.0161716398631995,0.154708451002783,
0.810599859752694));
#12633=CARTESIAN_POINT('Ctrl Pts',(0.0171414634305739,0.154602968397244,
0.810529054691374));
#12634=CARTESIAN_POINT('Ctrl Pts',(0.0174636565176181,0.154566905617053,
0.810505578784916));
#12635=CARTESIAN_POINT('Ctrl Pts',(0.0180417315800823,0.154500371592342,
0.810463545457661));
#12636=CARTESIAN_POINT('Ctrl Pts',(0.018297651351116,0.15447027176465,0.810444967639323));
#12637=CARTESIAN_POINT('Ctrl Pts',(0.0188533090009909,0.154403518164273,
0.810404698237779));
#12638=CARTESIAN_POINT('Ctrl Pts',(0.0191530144861062,0.154366627617865,
0.810383020167474));
#12639=CARTESIAN_POINT('Ctrl Pts',(0.0199792050220714,0.154262489187437,
0.810323372053753));
#12640=CARTESIAN_POINT('Ctrl Pts',(0.020505463007932,0.154193418187613,
0.810285502740853));
#12641=CARTESIAN_POINT('Ctrl Pts',(0.0231937495080265,0.153826575893572,
0.810092644510992));
#12642=CARTESIAN_POINT('Ctrl Pts',(0.0253498308491427,0.153486002113901,
0.809939918326207));
#12643=CARTESIAN_POINT('Ctrl Pts',(0.0413045518527728,0.150620389460298,
0.808819457603409));
#12644=CARTESIAN_POINT('Ctrl Pts',(0.0547137116318943,0.146284266570763,
0.80792688339334));
#12645=CARTESIAN_POINT('Ctrl Pts',(0.0714805038753536,0.13822889498148,
0.806684765406559));
#12646=CARTESIAN_POINT('Ctrl Pts',(0.0755104611525617,0.136069300286315,
0.80637606028091));
#12647=CARTESIAN_POINT('Ctrl Pts',(0.0809988836628154,0.132809163889201,
0.805936707844174));
#12648=CARTESIAN_POINT('Ctrl Pts',(0.0825421222573581,0.131855567813592,
0.805810992977536));
#12649=CARTESIAN_POINT('Ctrl Pts',(0.0848592039434004,0.130367180249647,
0.805618674622934));
#12650=CARTESIAN_POINT('Ctrl Pts',(0.0856454910997768,0.129851977138239,
0.805552775382605));
#12651=CARTESIAN_POINT('Ctrl Pts',(0.0870953527582119,0.128883079271673,
0.80543004021721));
#12652=CARTESIAN_POINT('Ctrl Pts',(0.0877601768812447,0.128431304224809,
0.80537327658187));
#12653=CARTESIAN_POINT('Ctrl Pts',(0.0888359245777928,0.127688036998965,
0.805280620159881));
#12654=CARTESIAN_POINT('Ctrl Pts',(0.0892489924009949,0.127399661038663,
0.805244845728522));
#12655=CARTESIAN_POINT('Ctrl Pts',(0.0900407870163033,0.126841143089946,
0.805175888606833));
#12656=CARTESIAN_POINT('Ctrl Pts',(0.0904197176996317,0.12657129828423,
0.805142717539861));
#12657=CARTESIAN_POINT('Ctrl Pts',(0.0912847066690999,0.125949454079457,
0.805066603235888));
#12658=CARTESIAN_POINT('Ctrl Pts',(0.0917699470874756,0.125596335326539,
0.805023617185629));
#12659=CARTESIAN_POINT('Ctrl Pts',(0.0930538170499614,0.124650626144344,
0.804909107669234));
#12660=CARTESIAN_POINT('Ctrl Pts',(0.0938488161834835,0.124053178440869,
0.804837396287636));
#12661=CARTESIAN_POINT('Ctrl Pts',(0.0997841511117801,0.119503023061095,
0.804295830195685));
#12662=CARTESIAN_POINT('Ctrl Pts',(0.104677797073148,0.115240556817054,
0.803813702258976));
#12663=CARTESIAN_POINT('Ctrl Pts',(0.11672015718757,0.103349980929197,0.802528909301267));
#12664=CARTESIAN_POINT('Ctrl Pts',(0.123391803047791,0.0952850644481384,
0.801711899434893));
#12665=CARTESIAN_POINT('Ctrl Pts',(0.131455646399825,0.0832559801104097,
0.800597074853583));
#12666=CARTESIAN_POINT('Ctrl Pts',(0.133575094106209,0.0798113065309945,
0.800288597757142));
#12667=CARTESIAN_POINT('Ctrl Pts',(0.136577370427651,0.0744764658864343,
0.799830652367178));
#12668=CARTESIAN_POINT('Ctrl Pts',(0.137560344625351,0.0726448540707293,
0.799676812357502));
#12669=CARTESIAN_POINT('Ctrl Pts',(0.138735614427269,0.0703454724372923,
0.799488334681132));
#12670=CARTESIAN_POINT('Ctrl Pts',(0.138962678204106,0.0698958531548797,
0.799451697553405));
#12671=CARTESIAN_POINT('Ctrl Pts',(0.139318278893569,0.0691831294363092,
0.799393973926168));
#12672=CARTESIAN_POINT('Ctrl Pts',(0.139448261067244,0.0689207568274182,
0.799372799462109));
#12673=CARTESIAN_POINT('Ctrl Pts',(0.139691812633638,0.0684256315443816,
0.799332984548816));
#12674=CARTESIAN_POINT('Ctrl Pts',(0.139805540188643,0.0681929652020945,
0.799314334754582));
#12675=CARTESIAN_POINT('Ctrl Pts',(0.14006388166321,0.0676610818179139,
0.799271835528155));
#12676=CARTESIAN_POINT('Ctrl Pts',(0.140208118034519,0.0673616848225591,
0.799248009657173));
#12677=CARTESIAN_POINT('Ctrl Pts',(0.140587751108258,0.0665671637603513,
0.799185032373793));
#12678=CARTESIAN_POINT('Ctrl Pts',(0.140821494548802,0.0660712475263667,
0.799145980539543));
#12679=CARTESIAN_POINT('Ctrl Pts',(0.142415816649116,0.0626417941857988,
0.798877616826963));
#12680=CARTESIAN_POINT('Ctrl Pts',(0.143687376820304,0.0596674187302281,
0.798653387365905));
#12681=CARTESIAN_POINT('Ctrl Pts',(0.145165924370437,0.0558868299186629,
0.798376278328924));
#12682=CARTESIAN_POINT('Ctrl Pts',(0.145460347577447,0.0551159748852266,
0.7983201810209));
#12683=CARTESIAN_POINT('Ctrl Pts',(0.15008170145632,0.0427213984830013,
0.797424109162421));
#12684=CARTESIAN_POINT('Ctrl Pts',(0.15300952956646,0.0306229239145531,
0.796629134099632));
#12685=CARTESIAN_POINT('Ctrl Pts',(0.154977757385461,0.0140132086590769,
0.795510002567479));
#12686=CARTESIAN_POINT('Ctrl Pts',(0.155307185208447,0.00970302182048626,
0.79521753718701));
#12687=CARTESIAN_POINT('Ctrl Pts',(0.155547925680275,0.00275317695041912,
0.794738445293535));
#12688=CARTESIAN_POINT('Ctrl Pts',(0.155572238601344,0.000119635029152116,
0.794555186514293));
#12689=CARTESIAN_POINT('Ctrl Pts',(0.155516788792295,-0.00331198555048525,
0.79431360584295));
#12690=CARTESIAN_POINT('Ctrl Pts',(0.155497725947619,-0.00411072097472965,
0.794257180163994));
#12691=CARTESIAN_POINT('Ctrl Pts',(0.155456645201601,-0.00541171655463531,
0.794164938212319));
#12692=CARTESIAN_POINT('Ctrl Pts',(0.155438343978517,-0.00591408689546025,
0.794129238289805));
#12693=CARTESIAN_POINT('Ctrl Pts',(0.155398404274547,-0.00688151059171137,
0.794060329517132));
#12694=CARTESIAN_POINT('Ctrl Pts',(0.155377112495579,-0.00734657355316305,
0.794027131866808));
#12695=CARTESIAN_POINT('Ctrl Pts',(0.155323477785036,-0.00841324720877495,
0.793950821495057));
#12696=CARTESIAN_POINT('Ctrl Pts',(0.155289726863767,-0.00901477628714574,
0.793907665212274));
#12697=CARTESIAN_POINT('Ctrl Pts',(0.155190510014185,-0.0106166402521328,
0.793792405864537));
#12698=CARTESIAN_POINT('Ctrl Pts',(0.155118867785877,-0.0116165493168872,
0.793720110953034));
#12699=CARTESIAN_POINT('Ctrl Pts',(0.154485427316412,-0.0194010770670998,
0.793154472652925));
#12700=CARTESIAN_POINT('Ctrl Pts',(0.153488524643234,-0.0261418498296094,
0.792647555200766));
#12701=CARTESIAN_POINT('Ctrl Pts',(0.149098247854497,-0.0464974245144076,
0.791063655255003));
#12702=CARTESIAN_POINT('Ctrl Pts',(0.14430465426185,-0.059736316186918,
0.789953025093026));
#12703=CARTESIAN_POINT('Ctrl Pts',(0.136781677907786,-0.0741041370850376,
0.788738067490588));
#12704=CARTESIAN_POINT('Ctrl Pts',(0.135718961954988,-0.076032988018343,
0.788574922000234));
#12705=CARTESIAN_POINT('Ctrl Pts',(0.134358495576523,-0.0783827813864158,
0.788376698583588));
#12706=CARTESIAN_POINT('Ctrl Pts',(0.134099214983862,-0.0788255435261533,
0.788339371711147));
#12707=CARTESIAN_POINT('Ctrl Pts',(0.133687475256215,-0.0795207420331388,
0.788280810163883));
#12708=CARTESIAN_POINT('Ctrl Pts',(0.133536484198099,-0.0797740361637073,
0.788259483245344));
#12709=CARTESIAN_POINT('Ctrl Pts',(0.133251734654675,-0.0802486422257836,
0.788219542989181));
#12710=CARTESIAN_POINT('Ctrl Pts',(0.133118146222098,-0.0804700473184797,
0.788200919533595));
#12711=CARTESIAN_POINT('Ctrl Pts',(0.132810494090436,-0.0809770772155301,
0.788158289600803));
#12712=CARTESIAN_POINT('Ctrl Pts',(0.132636060972183,-0.0812624741832928,
0.788134307575406));
#12713=CARTESIAN_POINT('Ctrl Pts',(0.13209202594785,-0.0821461730290882,
0.788060084684401));
#12714=CARTESIAN_POINT('Ctrl Pts',(0.131719279150754,-0.0827425441493287,
0.788010044305072));
#12715=CARTESIAN_POINT('Ctrl Pts',(0.127644534946307,-0.089164553880836,
0.787471486488151));
#12716=CARTESIAN_POINT('Ctrl Pts',(0.123562153832671,-0.0947410595434836,
0.787006390933967));
#12717=CARTESIAN_POINT('Ctrl Pts',(0.113412838903229,-0.106827684865006,
0.785958630532125));
#12718=CARTESIAN_POINT('Ctrl Pts',(0.107131986916895,-0.113125441977779,
0.785381687976477));
#12719=CARTESIAN_POINT('Ctrl Pts',(0.0967835193588346,-0.12186269964518,
0.784477970004902));
#12720=CARTESIAN_POINT('Ctrl Pts',(0.0930855587242266,-0.124710224258607,
0.784163084549768));
#12721=CARTESIAN_POINT('Ctrl Pts',(0.0877587324118492,-0.128442954097473,
0.783715585541222));
#12722=CARTESIAN_POINT('Ctrl Pts',(0.0862334300851427,-0.129471937620841,
0.783588117719509));
#12723=CARTESIAN_POINT('Ctrl Pts',(0.0835357942098381,-0.131222970597773,
0.783363566231928));
#12724=CARTESIAN_POINT('Ctrl Pts',(0.0823714390042258,-0.131956973098525,
0.783266926512843));
#12725=CARTESIAN_POINT('Ctrl Pts',(0.0806672503466133,-0.132999938862592,
0.783125808822505));
#12726=CARTESIAN_POINT('Ctrl Pts',(0.080135037936016,-0.133321283712045,
0.78308178401757));
#12727=CARTESIAN_POINT('Ctrl Pts',(0.0791997804380966,-0.133878360019871,
0.783004491590087));
#12728=CARTESIAN_POINT('Ctrl Pts',(0.0787975708131618,-0.134115485042924,
0.782971275056694));
#12729=CARTESIAN_POINT('Ctrl Pts',(0.0780154280004287,-0.13457186895908,
0.782906723474683));
#12730=CARTESIAN_POINT('Ctrl Pts',(0.0776356224819512,-0.13479133887533,
0.782875396443397));
#12731=CARTESIAN_POINT('Ctrl Pts',(0.0767269771719916,-0.135311283453173,
0.782800491922773));
#12732=CARTESIAN_POINT('Ctrl Pts',(0.0761972968241275,-0.135610266546859,
0.782756861383812));
#12733=CARTESIAN_POINT('Ctrl Pts',(0.0742888151924397,-0.136672815728198,
0.782599767334483));
#12734=CARTESIAN_POINT('Ctrl Pts',(0.0729002228940245,-0.137418498696092,
0.78248567167684));
#12735=CARTESIAN_POINT('Ctrl Pts',(0.0706118758295029,-0.138602910796911,
0.782297911750962));
#12736=CARTESIAN_POINT('Ctrl Pts',(0.0697187671307334,-0.139054296277507,
0.782224697044403));
#12737=CARTESIAN_POINT('Ctrl Pts',(0.0681303428149257,-0.13983795142238,
0.782094585367641));
#12738=CARTESIAN_POINT('Ctrl Pts',(0.0674367890467702,-0.140173734039405,
0.782037809160768));
#12739=CARTESIAN_POINT('Ctrl Pts',(0.0662166273033565,-0.140753321432988,
0.781937980280856));
#12740=CARTESIAN_POINT('Ctrl Pts',(0.0656910917040262,-0.140999360567433,
0.781895001367356));
#12741=CARTESIAN_POINT('Ctrl Pts',(0.0650242859477797,-0.141307000814208,
0.781840491854575));
#12742=CARTESIAN_POINT('Ctrl Pts',(0.0648842785343968,-0.141371343068167,
0.781829047898492));
#12743=CARTESIAN_POINT('Ctrl Pts',(0.0646896543854195,-0.141460435143653,
0.781813141411207));
#12744=CARTESIAN_POINT('Ctrl Pts',(0.0646351182220086,-0.141485361744407,
0.781808684400974));
#12745=CARTESIAN_POINT('Ctrl Pts',(0.0515529581325114,-0.147455623864881,
0.780739580222501));
#12746=CARTESIAN_POINT('Ctrl Pts',(0.0377679009634067,-0.151572796241196,
0.779614413181161));
#12747=CARTESIAN_POINT('Ctrl Pts',(0.0201187780993151,-0.154284075085249,
0.778244404138055));
#12748=CARTESIAN_POINT('Ctrl Pts',(0.0166012349691905,-0.154702113430027,
0.77797525350488));
#12749=CARTESIAN_POINT('Ctrl Pts',(0.0111778435190974,-0.15515950686183,
0.777568955580236));
#12750=CARTESIAN_POINT('Ctrl Pts',(0.0092805598676607,-0.155284541596335,
0.777428446666504));
#12751=CARTESIAN_POINT('Ctrl Pts',(0.0068927935365231,-0.155397976564714,
0.777254037794324));
#12752=CARTESIAN_POINT('Ctrl Pts',(0.00640412442419206,-0.155418882156921,
0.777218471633737));
#12753=CARTESIAN_POINT('Ctrl Pts',(0.00562600500076877,-0.15544849440568,
0.777162050264291));
#12754=CARTESIAN_POINT('Ctrl Pts',(0.00533662056392088,-0.155458698148318,
0.777141113570064));
#12755=CARTESIAN_POINT('Ctrl Pts',(0.00478762127951809,-0.15547652117854,
0.777101484377287));
#12756=CARTESIAN_POINT('Ctrl Pts',(0.00452801919361408,-0.155484298238487,
0.777082783758662));
#12757=CARTESIAN_POINT('Ctrl Pts',(0.00393051748116529,-0.155500700250034,
0.777039829415925));
#12758=CARTESIAN_POINT('Ctrl Pts',(0.00359260825401031,-0.155508874080279,
0.777015601080654));
#12759=CARTESIAN_POINT('Ctrl Pts',(0.00268722705150434,-0.155527822090269,
0.776950849349461));
#12760=CARTESIAN_POINT('Ctrl Pts',(0.00211971098721477,-0.155536592109872,
0.776910434681687));
#12761=CARTESIAN_POINT('Ctrl Pts',(-0.00210115335165072,-0.155578711893932,
0.776611056855797));
#12762=CARTESIAN_POINT('Ctrl Pts',(-0.00575498535910577,-0.15548644970198,
0.776358597155457));
#12763=CARTESIAN_POINT('Ctrl Pts',(-0.0112980827973848,-0.155150772185236,
0.775981161612917));
#12764=CARTESIAN_POINT('Ctrl Pts',(-0.0131914376173044,-0.15500127500968,
0.775853232195567));
#12765=CARTESIAN_POINT('Ctrl Pts',(-0.0295991060914255,-0.153402908098742,
0.774749637375592));
#12766=CARTESIAN_POINT('Ctrl Pts',(-0.0438448907086237,-0.149953998417868,
0.773818113933568));
#12767=CARTESIAN_POINT('Ctrl Pts',(-0.0603302557095414,-0.143408467471548,
0.772601907898211));
#12768=CARTESIAN_POINT('Ctrl Pts',(-0.063222220694162,-0.142157225304195,
0.772383351094607));
#12769=CARTESIAN_POINT('Ctrl Pts',(-0.0668438866724197,-0.140457895692484,
0.772101996903965));
#12770=CARTESIAN_POINT('Ctrl Pts',(-0.0676107458562194,-0.14009037312098,
0.772041978666779));
#12771=CARTESIAN_POINT('Ctrl Pts',(-0.0688363051439574,-0.139490608601823,
0.771945327069034));
#12772=CARTESIAN_POINT('Ctrl Pts',(-0.069296942507977,-0.139262344305525,
0.77190883204996));
#12773=CARTESIAN_POINT('Ctrl Pts',(-0.0701698145683913,-0.138824398154907,
0.771839353218202));
#12774=CARTESIAN_POINT('Ctrl Pts',(-0.0705822630678265,-0.138615152603784,
0.771806384945972));
#12775=CARTESIAN_POINT('Ctrl Pts',(-0.0715185099331964,-0.138134908839416,
0.771731229221048));
#12776=CARTESIAN_POINT('Ctrl Pts',(-0.0720417098791794,-0.137862766268129,
0.771689001910026));
#12777=CARTESIAN_POINT('Ctrl Pts',(-0.0736318896006051,-0.137024109968243,
0.771559952344894));
#12778=CARTESIAN_POINT('Ctrl Pts',(-0.0746938060136661,-0.136448147912775,
0.771472797511643));
#12779=CARTESIAN_POINT('Ctrl Pts',(-0.0772647476860239,-0.135014715655852,
0.771259350217379));
#12780=CARTESIAN_POINT('Ctrl Pts',(-0.0787663059520426,-0.134144262922644,
0.77113260313));
#12781=CARTESIAN_POINT('Ctrl Pts',(-0.0925912967294179,-0.125817769953142,
0.769945723517359));
#12782=CARTESIAN_POINT('Ctrl Pts',(-0.10383574540402,-0.116709988593688,
0.768821737720165));
#12783=CARTESIAN_POINT('Ctrl Pts',(-0.116738583117244,-0.10289890668422,
0.767363211441435));
#12784=CARTESIAN_POINT('Ctrl Pts',(-0.119668737455807,-0.0994760356110558,
0.767018462642592));
#12785=CARTESIAN_POINT('Ctrl Pts',(-0.123822150326273,-0.094174591394553,
0.766513781260716));
#12786=CARTESIAN_POINT('Ctrl Pts',(-0.125160038838041,-0.0923890938442791,
0.76634845656961));
#12787=CARTESIAN_POINT('Ctrl Pts',(-0.126759137757643,-0.0901564690941939,
0.766147959126184));
#12788=CARTESIAN_POINT('Ctrl Pts',(-0.127057053304051,-0.0897361306863186,
0.7661104770143));
#12789=CARTESIAN_POINT('Ctrl Pts',(-0.127522463560698,-0.0890725042688893,
0.76605172697451));
#12790=CARTESIAN_POINT('Ctrl Pts',(-0.127691359454263,-0.0888302113811323,
0.766030365828257));
#12791=CARTESIAN_POINT('Ctrl Pts',(-0.128006789729661,-0.0883749461662716,
0.765990396820721));
#12792=CARTESIAN_POINT('Ctrl Pts',(-0.128153481558411,-0.0881620921527741,
0.765971778669144));
#12793=CARTESIAN_POINT('Ctrl Pts',(-0.128488338955865,-0.0876736028043386,
0.765929207171701));
#12794=CARTESIAN_POINT('Ctrl Pts',(-0.128676148384388,-0.0873977271955276,
0.765905278032215));
#12795=CARTESIAN_POINT('Ctrl Pts',(-0.129254798523519,-0.0865418322503385,
0.765831381176145));
#12796=CARTESIAN_POINT('Ctrl Pts',(-0.1296426237012,-0.0859597687272538,
0.765781611419586));
#12797=CARTESIAN_POINT('Ctrl Pts',(-0.133444714767209,-0.0801691728839793,
0.765291049750526));
#12798=CARTESIAN_POINT('Ctrl Pts',(-0.136547691992521,-0.0747618785240991,
0.764869276763085));
#12799=CARTESIAN_POINT('Ctrl Pts',(-0.140424437915346,-0.0669549424434565,
0.76428857545107));
#12800=CARTESIAN_POINT('Ctrl Pts',(-0.141476951996176,-0.0647013112755856,
0.764124074343465));
#12801=CARTESIAN_POINT('Ctrl Pts',(-0.145695951793674,-0.0550718725152586,
0.763430601390425));
#12802=CARTESIAN_POINT('Ctrl Pts',(-0.148342966282279,-0.0474824152885466,
0.762906312659745));
#12803=CARTESIAN_POINT('Ctrl Pts',(-0.15195045667767,-0.0338242616384623,
0.76195880842185));
#12804=CARTESIAN_POINT('Ctrl Pts',(-0.153159867661364,-0.0278399330092353,
0.761542520224111));
#12805=CARTESIAN_POINT('Ctrl Pts',(-0.154158837767367,-0.0207825048141482,
0.761042573029926));
#12806=CARTESIAN_POINT('Ctrl Pts',(-0.154292845160762,-0.0197630364581568,
0.760970145401697));
#12807=CARTESIAN_POINT('Ctrl Pts',(-0.154483351593567,-0.0181934679079019,
0.760858283341127));
#12808=CARTESIAN_POINT('Ctrl Pts',(-0.15454704279997,-0.0176442551995465,
0.760819075118087));
#12809=CARTESIAN_POINT('Ctrl Pts',(-0.154657849414168,-0.0166420997802093,
0.760747405397276));
#12810=CARTESIAN_POINT('Ctrl Pts',(-0.154705906630079,-0.016189265461627,
0.760714973859669));
#12811=CARTESIAN_POINT('Ctrl Pts',(-0.154806477594729,-0.0152002385909582,
0.760644035308861));
#12812=CARTESIAN_POINT('Ctrl Pts',(-0.154858195272737,-0.0146639729231184,
0.760605503745893));
#12813=CARTESIAN_POINT('Ctrl Pts',(-0.154992201550675,-0.0131945981169751,
0.760499735612869));
#12814=CARTESIAN_POINT('Ctrl Pts',(-0.155068847639527,-0.0122610106195149,
0.7604323233414));
#12815=CARTESIAN_POINT('Ctrl Pts',(-0.155414542529894,-0.00752621732812435,
0.760089314549051));
#12816=CARTESIAN_POINT('Ctrl Pts',(-0.155552250998398,-0.00371705200902001,
0.7598096602253));
#12817=CARTESIAN_POINT('Ctrl Pts',(-0.155541110402596,0.0149096492034718,
0.758422610536678));
#12818=CARTESIAN_POINT('Ctrl Pts',(-0.153415077015676,0.029647957652074,
0.757254684268284));
#12819=CARTESIAN_POINT('Ctrl Pts',(-0.147988193807677,0.0481141380828599,
0.755783922740216));
#12820=CARTESIAN_POINT('Ctrl Pts',(-0.146555982731543,0.0523147091798366,
0.755449689641221));
#12821=CARTESIAN_POINT('Ctrl Pts',(-0.144706278994157,0.0570642765115517,
0.755076336933976));
#12822=CARTESIAN_POINT('Ctrl Pts',(-0.144462640524784,0.0576782833369183,
0.75502816176344));
#12823=CARTESIAN_POINT('Ctrl Pts',(-0.144092904592088,0.0585930342396851,
0.754956545089647));
#12824=CARTESIAN_POINT('Ctrl Pts',(-0.143969765240692,0.058894953239144,
0.754932932924854));
#12825=CARTESIAN_POINT('Ctrl Pts',(-0.143747561398075,0.0594349018711088,
0.754890753466581));
#12826=CARTESIAN_POINT('Ctrl Pts',(-0.143648854107371,0.0596730733706338,
0.75487216514607));
#12827=CARTESIAN_POINT('Ctrl Pts',(-0.143433787027275,0.0601883840977885,
0.754831984529495));
#12828=CARTESIAN_POINT('Ctrl Pts',(-0.14331721631369,0.0604654310623273,
0.754810405251202));
#12829=CARTESIAN_POINT('Ctrl Pts',(-0.142989368791817,0.0612383329075057,
0.754750263399946));
#12830=CARTESIAN_POINT('Ctrl Pts',(-0.142776313920289,0.0617334367346935,
0.754711806699295));
#12831=CARTESIAN_POINT('Ctrl Pts',(-0.141525570992927,0.0645988412845397,
0.754489582247166));
#12832=CARTESIAN_POINT('Ctrl Pts',(-0.14043136454327,0.0669442417802616,
0.754309051192415));
#12833=CARTESIAN_POINT('Ctrl Pts',(-0.132724621279661,0.082441871521703,
0.753118128068271));
#12834=CARTESIAN_POINT('Ctrl Pts',(-0.124331899563472,0.094626504330818,
0.752185020633095));
#12835=CARTESIAN_POINT('Ctrl Pts',(-0.113061510702215,0.106848074958021,
0.751068075083847));
#12836=CARTESIAN_POINT('Ctrl Pts',(-0.111747307059217,0.108221787466916,
0.750939644489558));
#12837=CARTESIAN_POINT('Ctrl Pts',(-0.107574890917782,0.112426086162214,
0.750536708609445));
#12838=CARTESIAN_POINT('Ctrl Pts',(-0.104632046356623,0.115169927026694,
0.750259256634307));
#12839=CARTESIAN_POINT('Ctrl Pts',(-0.100928498481501,0.118363826468811,
0.749915917372416));
#12840=CARTESIAN_POINT('Ctrl Pts',(-0.100265875354558,0.118925654956956,
0.749854707426298));
#12841=CARTESIAN_POINT('Ctrl Pts',(-0.0991619669570246,0.119845859010989,
0.749753072126332));
#12842=CARTESIAN_POINT('Ctrl Pts',(-0.0987233548899906,0.120207424049308,
0.7497127767447));
#12843=CARTESIAN_POINT('Ctrl Pts',(-0.0979258540281336,0.12085752628741,
0.749639661195743));
#12844=CARTESIAN_POINT('Ctrl Pts',(-0.0975676452605391,0.121146890745929,
0.74960687483169));
#12845=CARTESIAN_POINT('Ctrl Pts',(-0.0967961294994244,0.121764487314958,
0.749536372280422));
#12846=CARTESIAN_POINT('Ctrl Pts',(-0.0963824273403182,0.122092214102517,
0.749498636471835));
#12847=CARTESIAN_POINT('Ctrl Pts',(-0.095249097409192,0.122980666028845,
0.749395441736298));
#12848=CARTESIAN_POINT('Ctrl Pts',(-0.0945262017524837,0.123537168052934,
0.749329817114607));
#12849=CARTESIAN_POINT('Ctrl Pts',(-0.0906718212744912,0.126450722236682,
0.748980908209767));
#12850=CARTESIAN_POINT('Ctrl Pts',(-0.0874572513636142,0.128694943135836,
0.748693299755616));
#12851=CARTESIAN_POINT('Ctrl Pts',(-0.077615623880683,0.135026678807705,
0.747821586081134));
#12852=CARTESIAN_POINT('Ctrl Pts',(-0.0707711937600463,0.138735384551554,
0.74722608401625));
#12853=CARTESIAN_POINT('Ctrl Pts',(-0.0636886011499548,0.141913933718863,
0.746625191472247));
#12854=CARTESIAN_POINT('',(-0.155550013165998,8.25752365483191E-5,0.745715654272581));
#12855=CARTESIAN_POINT('Ctrl Pts',(-0.0636886287602419,0.141913921327825,
0.732917465391055));
#12856=CARTESIAN_POINT('Ctrl Pts',(-0.0658868196071155,0.140927409507978,
0.733098854558852));
#12857=CARTESIAN_POINT('Ctrl Pts',(-0.0680624092442903,0.139889680523272,
0.733278291559734));
#12858=CARTESIAN_POINT('Ctrl Pts',(-0.0708388259518219,0.138485212855949,
0.733506388586994));
#12859=CARTESIAN_POINT('Ctrl Pts',(-0.071461926926368,0.138164707837504,
0.733557520036753));
#12860=CARTESIAN_POINT('Ctrl Pts',(-0.0723787520957292,0.137685257899643,
0.733632643283517));
#12861=CARTESIAN_POINT('Ctrl Pts',(-0.0726741524091138,0.137529566185343,
0.733656830780006));
#12862=CARTESIAN_POINT('Ctrl Pts',(-0.0731883917908159,0.137256415116443,
0.733698903986489));
#12863=CARTESIAN_POINT('Ctrl Pts',(-0.0734074529175393,0.137139381810263,
0.733716816203875));
#12864=CARTESIAN_POINT('Ctrl Pts',(-0.0736269661597238,0.137021430275701,
0.733734754444373));
#12865=CARTESIAN_POINT('Ctrl Pts',(-0.0736276946533431,0.137021038825177,
0.733734813975475));
#12866=CARTESIAN_POINT('Ctrl Pts',(-0.0736291513747163,0.13702025605188,
0.733734933015738));
#12867=CARTESIAN_POINT('Ctrl Pts',(-0.0736298762907878,0.137019866508793,
0.733734992254266));
#12868=CARTESIAN_POINT('Ctrl Pts',(-0.0736313216189784,0.137019089828089,
0.733735110363035));
#12869=CARTESIAN_POINT('Ctrl Pts',(-0.0736320419228137,0.137018702748759,
0.733735169224429));
#12870=CARTESIAN_POINT('Ctrl Pts',(-0.0736334780672034,0.137017930973993,
0.733735286582259));
#12871=CARTESIAN_POINT('Ctrl Pts',(-0.0736341937935272,0.137017546340039,
0.73373534506936));
#12872=CARTESIAN_POINT('Ctrl Pts',(-0.0736356208233877,0.13701677943454,
0.73373546168192));
#12873=CARTESIAN_POINT('Ctrl Pts',(-0.0736363320090056,0.137016397226459,
0.733735519797743));
#12874=CARTESIAN_POINT('Ctrl Pts',(-0.0736377499825418,0.137015635159494,
0.733735635669798));
#12875=CARTESIAN_POINT('Ctrl Pts',(-0.0736384566581405,0.137015255361068,
0.733735693416853));
#12876=CARTESIAN_POINT('Ctrl Pts',(-0.0736398656455024,0.137014498095477,
0.733735808554144));
#12877=CARTESIAN_POINT('Ctrl Pts',(-0.0736405678422688,0.137014120690211,
0.733735865934984));
#12878=CARTESIAN_POINT('Ctrl Pts',(-0.0736419693503222,0.137013367416629,
0.733735980460655));
#12879=CARTESIAN_POINT('Ctrl Pts',(-0.0736426685448713,0.137012991611061,
0.733736037595963));
#12880=CARTESIAN_POINT('Ctrl Pts',(-0.0736440569327213,0.137012245361901,
0.733736151049072));
#12881=CARTESIAN_POINT('Ctrl Pts',(-0.0736447503153976,0.137011872666577,
0.733736207709228));
#12882=CARTESIAN_POINT('Ctrl Pts',(-0.0736461327094075,0.137011129612014,
0.733736320672119));
#12883=CARTESIAN_POINT('Ctrl Pts',(-0.0736468217146804,0.137010759256118,
0.733736376974361));
#12884=CARTESIAN_POINT('Ctrl Pts',(-0.0736481953872075,0.137010020862753,
0.733736489224152));
#12885=CARTESIAN_POINT('Ctrl Pts',(-0.0736488800500122,0.137009652827759,
0.733736545171339));
#12886=CARTESIAN_POINT('Ctrl Pts',(-0.0736502450542464,0.137008919067505,
0.733736656712383));
#12887=CARTESIAN_POINT('Ctrl Pts',(-0.073650925401184,0.137008553339366,
0.733736712306692));
#12888=CARTESIAN_POINT('Ctrl Pts',(-0.0736522818143393,0.137007824171214,
0.733736823145308));
#12889=CARTESIAN_POINT('Ctrl Pts',(-0.0736529578801308,0.137007460731512,
0.733736878389581));
#12890=CARTESIAN_POINT('Ctrl Pts',(-0.0736543057557409,0.137006736127176,
0.733736988530151));
#12891=CARTESIAN_POINT('Ctrl Pts',(-0.0736549775684109,0.13700637496109,
0.733737043426682));
#12892=CARTESIAN_POINT('Ctrl Pts',(-0.07365631697955,0.13700565488177,0.733737152875184));
#12893=CARTESIAN_POINT('Ctrl Pts',(-0.0736569845740336,0.137005295970758,
0.733737207426831));
#12894=CARTESIAN_POINT('Ctrl Pts',(-0.0736583155734067,0.137004580388598,
0.73373731618758));
#12895=CARTESIAN_POINT('Ctrl Pts',(-0.0736589789788319,0.137004223717239,
0.733737370396727));
#12896=CARTESIAN_POINT('Ctrl Pts',(-0.073660301632553,0.137003512597165,
0.733737478475132));
#12897=CARTESIAN_POINT('Ctrl Pts',(-0.0736609608805821,0.13700315814867,
0.733737532344371));
#12898=CARTESIAN_POINT('Ctrl Pts',(-0.0736622752456853,0.137002451460484,
0.733737639745101));
#12899=CARTESIAN_POINT('Ctrl Pts',(-0.0736629303647093,0.137002099219819,
0.733737693276754));
#12900=CARTESIAN_POINT('Ctrl Pts',(-0.0736642365069524,0.137001396928623,
0.73373780000519));
#12901=CARTESIAN_POINT('Ctrl Pts',(-0.0736648875282756,0.137001046879186,
0.73373785320182));
#12902=CARTESIAN_POINT('Ctrl Pts',(-0.0736661855103606,0.137000348951719,
0.733737959263092));
#12903=CARTESIAN_POINT('Ctrl Pts',(-0.0736668324687862,0.137000001075019,
0.733738012127545));
#12904=CARTESIAN_POINT('Ctrl Pts',(-0.0739239134974,0.136861763415723,0.733759018769638));
#12905=CARTESIAN_POINT('Ctrl Pts',(-0.0741799627949866,0.136723152375748,
0.733779926514437));
#12906=CARTESIAN_POINT('Ctrl Pts',(-0.0748786279704719,0.136342392942848,
0.733836940432022));
#12907=CARTESIAN_POINT('Ctrl Pts',(-0.0753204626956025,0.136098805866748,
0.733872956663408));
#12908=CARTESIAN_POINT('Ctrl Pts',(-0.0763041978149138,0.135550206797253,
0.733953076125712));
#12909=CARTESIAN_POINT('Ctrl Pts',(-0.0768454737280182,0.135244084409275,
0.733997112211482));
#12910=CARTESIAN_POINT('Ctrl Pts',(-0.0785060874229395,0.134291724297996,
0.734132112599383));
#12911=CARTESIAN_POINT('Ctrl Pts',(-0.0796192512344375,0.133634756243729,
0.734222466151496));
#12912=CARTESIAN_POINT('Ctrl Pts',(-0.0838562748442795,0.131062404452488,
0.734566350561137));
#12913=CARTESIAN_POINT('Ctrl Pts',(-0.0869204983846739,0.129050610064148,
0.734815001678183));
#12914=CARTESIAN_POINT('Ctrl Pts',(-0.0977256739393813,0.121396888921269,
0.735702516373472));
#12915=CARTESIAN_POINT('Ctrl Pts',(-0.105012667391308,0.115151494326533,
0.736322957523172));
#12916=CARTESIAN_POINT('Ctrl Pts',(-0.117124236043512,0.10265917083873,
0.737478845861239));
#12917=CARTESIAN_POINT('Ctrl Pts',(-0.122137070180012,0.0966410904870666,
0.73800717596665));
#12918=CARTESIAN_POINT('Ctrl Pts',(-0.127270881815958,0.0894369999562729,
0.738626702342981));
#12919=CARTESIAN_POINT('Ctrl Pts',(-0.127857782842325,0.088595945713987,
0.738698830534396));
#12920=CARTESIAN_POINT('Ctrl Pts',(-0.128779932887381,0.0872462172202169,
0.738814300794546));
#12921=CARTESIAN_POINT('Ctrl Pts',(-0.129120592126282,0.0867412600990741,
0.738857438314034));
#12922=CARTESIAN_POINT('Ctrl Pts',(-0.129716881011497,0.0858460883448823,
0.738933809255411));
#12923=CARTESIAN_POINT('Ctrl Pts',(-0.12997373932828,0.0854566976884622,
0.738966996132539));
#12924=CARTESIAN_POINT('Ctrl Pts',(-0.130502050164645,0.0846479000879931,
0.739035861903078));
#12925=CARTESIAN_POINT('Ctrl Pts',(-0.13077324105906,0.0842283295492287,
0.739071550041686));
#12926=CARTESIAN_POINT('Ctrl Pts',(-0.131465500655869,0.0831459037549432,
0.739163530832447));
#12927=CARTESIAN_POINT('Ctrl Pts',(-0.131883574980984,0.0824811601651463,
0.739219933272772));
#12928=CARTESIAN_POINT('Ctrl Pts',(-0.133617705970058,0.0796769749716854,
0.739457534509738));
#12929=CARTESIAN_POINT('Ctrl Pts',(-0.13488680548366,0.077509096415319,
0.739640430414));
#12930=CARTESIAN_POINT('Ctrl Pts',(-0.138062650781598,0.0717697191835356,
0.740122949748545));
#12931=CARTESIAN_POINT('Ctrl Pts',(-0.139883330741691,0.068153038618028,
0.740425390804462));
#12932=CARTESIAN_POINT('Ctrl Pts',(-0.147000785032031,0.0525247438556022,
0.741725257506989));
#12933=CARTESIAN_POINT('Ctrl Pts',(-0.150906399022489,0.0399409552940836,
0.742760508761882));
#12934=CARTESIAN_POINT('Ctrl Pts',(-0.153513178247386,0.0251606928274965,
0.743901568080885));
#12935=CARTESIAN_POINT('Ctrl Pts',(-0.153806848468763,0.0232982913102516,
0.744043910567974));
#12936=CARTESIAN_POINT('Ctrl Pts',(-0.154146351899127,0.0208576066405569,
0.744228218212873));
#12937=CARTESIAN_POINT('Ctrl Pts',(-0.154222902538861,0.0202838338052238,
0.744271385766656));
#12938=CARTESIAN_POINT('Ctrl Pts',(-0.154491345450532,0.0181823372761071,
0.74442887259747));
#12939=CARTESIAN_POINT('Ctrl Pts',(-0.154663763591989,0.0166521448237655,
0.744542351714121));
#12940=CARTESIAN_POINT('Ctrl Pts',(-0.154859417385346,0.0146487914606559,
0.744689150924813));
#12941=CARTESIAN_POINT('Ctrl Pts',(-0.154903248054186,0.0141777996257191,
0.744723536089202));
#12942=CARTESIAN_POINT('Ctrl Pts',(-0.154970124340366,0.0134218035172789,
0.744778515905987));
#12943=CARTESIAN_POINT('Ctrl Pts',(-0.154994533366409,0.0131369280225778,
0.744799185147332));
#12944=CARTESIAN_POINT('Ctrl Pts',(-0.155038717563621,0.0126039867289663,
0.7448377605169));
#12945=CARTESIAN_POINT('Ctrl Pts',(-0.155058682692638,0.0123559438278507,
0.744855676729856));
#12946=CARTESIAN_POINT('Ctrl Pts',(-0.155097922028982,0.011853364064749,
0.744891903455346));
#12947=CARTESIAN_POINT('Ctrl Pts',(-0.155117164896952,0.0115988281403929,
0.744910212052376));
#12948=CARTESIAN_POINT('Ctrl Pts',(-0.15516028559773,0.0110091401994567,
0.744952540600203));
#12949=CARTESIAN_POINT('Ctrl Pts',(-0.155183704369946,0.0106739542026328,
0.744976535382325));
#12950=CARTESIAN_POINT('Ctrl Pts',(-0.155241700513122,0.00980330706539756,
0.745038698609322));
#12951=CARTESIAN_POINT('Ctrl Pts',(-0.155274594083551,0.00926773227578935,
0.74507677770032));
#12952=CARTESIAN_POINT('Ctrl Pts',(-0.155466653342219,0.00585181955296553,
0.745318687248882));
#12953=CARTESIAN_POINT('Ctrl Pts',(-0.155548450466375,0.00296749491786026,
0.745518602194368));
#12954=CARTESIAN_POINT('Ctrl Pts',(-0.155549978192756,8.23664555785925E-5,
0.745715729333107));
#12955=CARTESIAN_POINT('Ctrl Pts',(-0.155549978079878,8.25793517535353E-5,
0.745715714786916));
#12956=CARTESIAN_POINT('Ctrl Pts',(-0.155556853675459,-0.0128685848205831,
0.746600607013714));
#12957=CARTESIAN_POINT('Ctrl Pts',(-0.15394629247449,-0.0257717735182719,
0.747428745924574));
#12958=CARTESIAN_POINT('Ctrl Pts',(-0.149220890194732,-0.0443581414932631,
0.748709406296978));
#12959=CARTESIAN_POINT('Ctrl Pts',(-0.147327452226894,-0.0502904133857493,
0.74913151030482));
#12960=CARTESIAN_POINT('Ctrl Pts',(-0.144555614530026,-0.0574597637479467,
0.749667613277752));
#12961=CARTESIAN_POINT('Ctrl Pts',(-0.144007872702005,-0.058819065656376,
0.749770433443441));
#12962=CARTESIAN_POINT('Ctrl Pts',(-0.143194412099914,-0.0607582857442818,
0.749918909348949));
#12963=CARTESIAN_POINT('Ctrl Pts',(-0.142944192343963,-0.0613446558102792,
0.749964041898562));
#12964=CARTESIAN_POINT('Ctrl Pts',(-0.142503493861355,-0.0623600599469477,
0.750042617960528));
#12965=CARTESIAN_POINT('Ctrl Pts',(-0.142314663107363,-0.0627898040694738,
0.750076005092705));
#12966=CARTESIAN_POINT('Ctrl Pts',(-0.141947373841504,-0.0636155185224228,
0.750140412923053));
#12967=CARTESIAN_POINT('Ctrl Pts',(-0.141769196103932,-0.0640116096217815,
0.750171423764564));
#12968=CARTESIAN_POINT('Ctrl Pts',(-0.141297017472815,-0.0650496261149102,
0.750252997356559));
#12969=CARTESIAN_POINT('Ctrl Pts',(-0.141000303660039,-0.065690298687884,
0.750303652880535));
#12970=CARTESIAN_POINT('Ctrl Pts',(-0.139950321550031,-0.0679175577687259,
0.750480846203047));
#12971=CARTESIAN_POINT('Ctrl Pts',(-0.139174577777274,-0.0694933348297017,
0.750608156344875));
#12972=CARTESIAN_POINT('Ctrl Pts',(-0.13349409367168,-0.0805554064374866,
0.751516153660548));
#12973=CARTESIAN_POINT('Ctrl Pts',(-0.127651511328569,-0.0895257062755262,
0.752330599354084));
#12974=CARTESIAN_POINT('Ctrl Pts',(-0.117010113811023,-0.102681266320282,
0.753641065290989));
#12975=CARTESIAN_POINT('Ctrl Pts',(-0.112793330642627,-0.107296213723833,
0.754127125459592));
#12976=CARTESIAN_POINT('Ctrl Pts',(-0.105919506967761,-0.113964718411044,
0.754860723414654));
#12977=CARTESIAN_POINT('Ctrl Pts',(-0.103454519627854,-0.116206990704938,
0.755113481581829));
#12978=CARTESIAN_POINT('Ctrl Pts',(-0.0999970293591358,-0.119154795676602,
0.755452335202484));
#12979=CARTESIAN_POINT('Ctrl Pts',(-0.0990656156982189,-0.119930293191213,
0.755542138252442));
#12980=CARTESIAN_POINT('Ctrl Pts',(-0.0976644579142919,-0.121069437740297,
0.755674931246396));
#12981=CARTESIAN_POINT('Ctrl Pts',(-0.0972015665344496,-0.121441387455473,
0.755718434035197));
#12982=CARTESIAN_POINT('Ctrl Pts',(-0.0963591599275317,-0.122110388752919,
0.755796924755105));
#12983=CARTESIAN_POINT('Ctrl Pts',(-0.0959803753407263,-0.122408342482916,
0.755831972000189));
#12984=CARTESIAN_POINT('Ctrl Pts',(-0.0953729661787505,-0.122881580411988,
0.755887773470156));
#12985=CARTESIAN_POINT('Ctrl Pts',(-0.0951452330586423,-0.123057994913729,
0.755908605872835));
#12986=CARTESIAN_POINT('Ctrl Pts',(-0.0947224800282469,-0.123383607369907,
0.755947111653722));
#12987=CARTESIAN_POINT('Ctrl Pts',(-0.0945275992113327,-0.123532974460131,
0.755964796656662));
#12988=CARTESIAN_POINT('Ctrl Pts',(-0.0940711323089854,-0.123881122464299,
0.756006068536476));
#12989=CARTESIAN_POINT('Ctrl Pts',(-0.0938092696723706,-0.124079536450808,
0.756029629529322));
#12990=CARTESIAN_POINT('Ctrl Pts',(-0.0930088493814255,-0.124682034621621,
0.756101302298344));
#12991=CARTESIAN_POINT('Ctrl Pts',(-0.0924682853137486,-0.12508346044055,
0.75614923285879));
#12992=CARTESIAN_POINT('Ctrl Pts',(-0.0879959686971424,-0.128359789228604,
0.756542059500712));
#12993=CARTESIAN_POINT('Ctrl Pts',(-0.0839332856556553,-0.131052437568517,
0.756875381402291));
#12994=CARTESIAN_POINT('Ctrl Pts',(-0.0707747838078598,-0.138910125620825,
0.757905854604968));
#12995=CARTESIAN_POINT('Ctrl Pts',(-0.0612813702914252,-0.143351694687048,
0.758581099640804));
#12996=CARTESIAN_POINT('Ctrl Pts',(-0.0450135437998744,-0.149048884657759,
0.759728422725725));
#12997=CARTESIAN_POINT('Ctrl Pts',(-0.0384744050131824,-0.150869118422769,
0.760186842136539));
#12998=CARTESIAN_POINT('Ctrl Pts',(-0.0303357676596908,-0.152570963627185,
0.760766282235592));
#12999=CARTESIAN_POINT('Ctrl Pts',(-0.0288290612976303,-0.152862823052504,
0.760873897590779));
#13000=CARTESIAN_POINT('Ctrl Pts',(-0.0266789515540542,-0.15324639590601,
0.761028062431324));
#13001=CARTESIAN_POINT('Ctrl Pts',(-0.0260388746616454,-0.153356451763358,
0.761074031013052));
#13002=CARTESIAN_POINT('Ctrl Pts',(-0.0249329514654142,-0.153539482723705,
0.761153592257944));
#13003=CARTESIAN_POINT('Ctrl Pts',(-0.0244674240336009,-0.153614354720019,
0.761187124514826));
#13004=CARTESIAN_POINT('Ctrl Pts',(-0.0235750981601126,-0.153753710716794,
0.761251482506231));
#13005=CARTESIAN_POINT('Ctrl Pts',(-0.0231483569175283,-0.153818537171378,
0.761282297088505));
#13006=CARTESIAN_POINT('Ctrl Pts',(-0.0220373166845191,-0.153982587598456,
0.761362621923545));
#13007=CARTESIAN_POINT('Ctrl Pts',(-0.0213526226194976,-0.15407902546687,
0.761412219528569));
#13008=CARTESIAN_POINT('Ctrl Pts',(-0.0190128809935731,-0.154392678609546,
0.76158204843877));
#13009=CARTESIAN_POINT('Ctrl Pts',(-0.0173550432431517,-0.154587809746761,
0.761702969280892));
#13010=CARTESIAN_POINT('Ctrl Pts',(-0.00270078989406502,-0.156073955986166,
0.762777420994795));
#13011=CARTESIAN_POINT('Ctrl Pts',(0.010404389635215,-0.155749711482677,
0.763783662581983));
#13012=CARTESIAN_POINT('Ctrl Pts',(0.0312462930030291,-0.152590559824126,
0.76541814411691));
#13013=CARTESIAN_POINT('Ctrl Pts',(0.0390770468872219,-0.150775409498959,
0.766038588046395));
#13014=CARTESIAN_POINT('Ctrl Pts',(0.0475331000389493,-0.14811181502562,
0.76669462996299));
#13015=CARTESIAN_POINT('Ctrl Pts',(0.0483307028768224,-0.147853469990355,
0.766756362153185));
#13016=CARTESIAN_POINT('Ctrl Pts',(0.0495594885391126,-0.147444457797167,
0.766851197318819));
#13017=CARTESIAN_POINT('Ctrl Pts',(0.0499921468907001,-0.147298324166876,
0.766884537127157));
#13018=CARTESIAN_POINT('Ctrl Pts',(0.0507106981471287,-0.14705209735635,
0.766939813726873));
#13019=CARTESIAN_POINT('Ctrl Pts',(0.0509969496684277,-0.146953072006535,
0.766961809657108));
#13020=CARTESIAN_POINT('Ctrl Pts',(0.0515511604380897,-0.146759534916859,
0.767004345389014));
#13021=CARTESIAN_POINT('Ctrl Pts',(0.0518191533043671,-0.14666512395893,
0.76702489090427));
#13022=CARTESIAN_POINT('Ctrl Pts',(0.0523231756130922,-0.14648600846526,
0.767063486229943));
#13023=CARTESIAN_POINT('Ctrl Pts',(0.0525592559546091,-0.14640146856186,
0.767081545004875));
#13024=CARTESIAN_POINT('Ctrl Pts',(0.0531098822975063,-0.146202786791173,
0.767123621745067));
#13025=CARTESIAN_POINT('Ctrl Pts',(0.0534242651829672,-0.146088200613596,
0.767147613066528));
#13026=CARTESIAN_POINT('Ctrl Pts',(0.0543991799857938,-0.145729295964849,
0.767221917151304));
#13027=CARTESIAN_POINT('Ctrl Pts',(0.055058436845694,-0.145481500775259,
0.767272028738349));
#13028=CARTESIAN_POINT('Ctrl Pts',(0.0624055939506118,-0.142662824135343,
0.767829243674299));
#13029=CARTESIAN_POINT('Ctrl Pts',(0.068910965225607,-0.139636852474163,
0.76831108731601));
#13030=CARTESIAN_POINT('Ctrl Pts',(0.0827584142275593,-0.131991220583771,
0.769359922734358));
#13031=CARTESIAN_POINT('Ctrl Pts',(0.0899693779636657,-0.127185490687428,
0.769922567487994));
#13032=CARTESIAN_POINT('Ctrl Pts',(0.101693326904764,-0.117873776491494,
0.770921776088418));
#13033=CARTESIAN_POINT('Ctrl Pts',(0.106398382466766,-0.113644747375297,
0.771350325729344));
#13034=CARTESIAN_POINT('Ctrl Pts',(0.111869795767525,-0.108088554786076,
0.771894117673135));
#13035=CARTESIAN_POINT('Ctrl Pts',(0.112891715704575,-0.107020779021166,
0.771997803076025));
#13036=CARTESIAN_POINT('Ctrl Pts',(0.114333916121706,-0.105470220226416,
0.772147307165418));
#13037=CARTESIAN_POINT('Ctrl Pts',(0.114766697052267,-0.104999128358048,
0.772192592469312));
#13038=CARTESIAN_POINT('Ctrl Pts',(0.115512233795035,-0.104177478551907,
0.772271347954059));
#13039=CARTESIAN_POINT('Ctrl Pts',(0.115826332675114,-0.103828145721331,
0.77230476102306));
#13040=CARTESIAN_POINT('Ctrl Pts',(0.116427425445298,-0.103153503543321,
0.772369157302719));
#13041=CARTESIAN_POINT('Ctrl Pts',(0.116714650808961,-0.102828405455886,
0.772400130415386));
#13042=CARTESIAN_POINT('Ctrl Pts',(0.117463938886023,-0.101973134434213,
0.772481465697885));
#13043=CARTESIAN_POINT('Ctrl Pts',(0.117923768022064,-0.101441027155288,
0.772531919599824));
#13044=CARTESIAN_POINT('Ctrl Pts',(0.11950870162044,-0.0995816262723197,
0.772707728197258));
#13045=CARTESIAN_POINT('Ctrl Pts',(0.120615094335134,-0.0982386309734471,
0.772833839393779));
#13046=CARTESIAN_POINT('Ctrl Pts',(0.129031178712947,-0.0876662341274678,
0.77382035741648));
#13047=CARTESIAN_POINT('Ctrl Pts',(0.135292697004802,-0.0776542807933108,
0.774722566529805));
#13048=CARTESIAN_POINT('Ctrl Pts',(0.142639297104381,-0.0622711754104519,
0.77604442713586));
#13049=CARTESIAN_POINT('Ctrl Pts',(0.144670329487358,-0.0573948408394731,
0.776454280726952));
#13050=CARTESIAN_POINT('Ctrl Pts',(0.147922236439142,-0.0483105401481043,
0.7771929533274));
#13051=CARTESIAN_POINT('Ctrl Pts',(0.14922108313896,-0.0441358460368841,
0.777523220145323));
#13052=CARTESIAN_POINT('Ctrl Pts',(0.15057723397387,-0.0390273751942305,
0.777912244373114));
#13053=CARTESIAN_POINT('Ctrl Pts',(0.150804166019929,-0.0381410936575152,
0.777979193991493));
#13054=CARTESIAN_POINT('Ctrl Pts',(0.151112391534664,-0.0368915450473225,
0.778072773973506));
#13055=CARTESIAN_POINT('Ctrl Pts',(0.151200214830678,-0.0365299331270809,
0.778099760315207));
#13056=CARTESIAN_POINT('Ctrl Pts',(0.15134818898269,-0.0359109737036286,
0.778145785365745));
#13057=CARTESIAN_POINT('Ctrl Pts',(0.15140898285055,-0.0356537832095708,
0.778164860615984));
#13058=CARTESIAN_POINT('Ctrl Pts',(0.151524688081587,-0.0351586551006461,
0.778201487260176));
#13059=CARTESIAN_POINT('Ctrl Pts',(0.151579694723989,-0.0349207427806138,
0.77821904423203));
#13060=CARTESIAN_POINT('Ctrl Pts',(0.151724730578397,-0.0342866402606119,
0.778265728072107));
#13061=CARTESIAN_POINT('Ctrl Pts',(0.151813769042295,-0.0338902214313781,
0.778294798544624));
#13062=CARTESIAN_POINT('Ctrl Pts',(0.152128235824517,-0.0324640352510709,
0.778398988106287));
#13063=CARTESIAN_POINT('Ctrl Pts',(0.152344755071913,-0.0314323000054422,
0.778473619215755));
#13064=CARTESIAN_POINT('Ctrl Pts',(0.152612994249233,-0.0300861736746981,
0.778570123937446));
#13065=CARTESIAN_POINT('Ctrl Pts',(0.152674253895215,-0.0297737478619322,
0.77859246128141));
#13066=CARTESIAN_POINT('Ctrl Pts',(0.15281520101481,-0.029043039524621,
0.77864456734425));
#13067=CARTESIAN_POINT('Ctrl Pts',(0.152894131498634,-0.0286246112407429,
0.778674300258396));
#13068=CARTESIAN_POINT('Ctrl Pts',(0.153133495662976,-0.0273264462662894,
0.778766236433758));
#13069=CARTESIAN_POINT('Ctrl Pts',(0.153288065097442,-0.0264456298460426,
0.77882817589768));
#13070=CARTESIAN_POINT('Ctrl Pts',(0.153654327342955,-0.0242472828642634,
0.778981781069904));
#13071=CARTESIAN_POINT('Ctrl Pts',(0.153856682283298,-0.0229282485285171,
0.779073068593096));
#13072=CARTESIAN_POINT('Ctrl Pts',(0.154748899773841,-0.0165673141999273,
0.77950978665694));
#13073=CARTESIAN_POINT('Ctrl Pts',(0.155208085289536,-0.0114958824002954,
0.779847459529292));
#13074=CARTESIAN_POINT('Ctrl Pts',(0.155750349392639,0.00165039431151851,
0.780715614663966));
#13075=CARTESIAN_POINT('Ctrl Pts',(0.155455190247727,0.00972487931033154,
0.781242438282852));
#13076=CARTESIAN_POINT('Ctrl Pts',(0.153830882395702,0.0238744926984932,
0.782197292971392));
#13077=CARTESIAN_POINT('Ctrl Pts',(0.152762090744374,0.0299609729633764,
0.782618468815589));
#13078=CARTESIAN_POINT('Ctrl Pts',(0.151096219339256,0.0369702268929665,
0.783123778231147));
#13079=CARTESIAN_POINT('Ctrl Pts',(0.150847898004737,0.0379707354645114,
0.783196388881908));
#13080=CARTESIAN_POINT('Ctrl Pts',(0.150451030483555,0.0395043809974338,
0.783308466792793));
#13081=CARTESIAN_POINT('Ctrl Pts',(0.150309549378168,0.0400393311996677,
0.783347706370615));
#13082=CARTESIAN_POINT('Ctrl Pts',(0.150046471007586,0.0410130015107262,
0.783419398180742));
#13083=CARTESIAN_POINT('Ctrl Pts',(0.149925795750907,0.0414519663601781,
0.783451820268677));
#13084=CARTESIAN_POINT('Ctrl Pts',(0.149658305003929,0.0424085334404736,
0.783522696273284));
#13085=CARTESIAN_POINT('Ctrl Pts',(0.149510728046123,0.0429259146775495,
0.783561174536549));
#13086=CARTESIAN_POINT('Ctrl Pts',(0.149099628430607,0.0443393234998059,
0.783666690344779));
#13087=CARTESIAN_POINT('Ctrl Pts',(0.148830718840912,0.0452337469723748,
0.783733902286087));
#13088=CARTESIAN_POINT('Ctrl Pts',(0.147432924375321,0.0497355269152193,
0.78407446898486));
#13089=CARTESIAN_POINT('Ctrl Pts',(0.14618096609324,0.0533030053836293,
0.784351813502948));
#13090=CARTESIAN_POINT('Ctrl Pts',(0.144409475143314,0.0578173977539785,
0.78471284232296));
#13091=CARTESIAN_POINT('Ctrl Pts',(0.144008247882034,0.0588096288020261,
0.784792828435677));
#13092=CARTESIAN_POINT('Ctrl Pts',(0.13908194124866,0.0706395641171971,
0.785754076635668));
#13093=CARTESIAN_POINT('Ctrl Pts',(0.133354060236117,0.0809342850009497,
0.786671678836341));
#13094=CARTESIAN_POINT('Ctrl Pts',(0.123916329447004,0.09413097579025,0.787923552299801));
#13095=CARTESIAN_POINT('Ctrl Pts',(0.121152069317364,0.0976630940760973,
0.788266680825109));
#13096=CARTESIAN_POINT('Ctrl Pts',(0.116793819120748,0.102761628635682,
0.788769278904082));
#13097=CARTESIAN_POINT('Ctrl Pts',(0.115312571246287,0.104421074562778,
0.788934093877867));
#13098=CARTESIAN_POINT('Ctrl Pts',(0.113445312365403,0.106424754669651,
0.789134051440653));
#13099=CARTESIAN_POINT('Ctrl Pts',(0.113092610202952,0.106799479595455,
0.789171489307682));
#13100=CARTESIAN_POINT('Ctrl Pts',(0.112534689739361,0.107386373536638,
0.789230181373474));
#13101=CARTESIAN_POINT('Ctrl Pts',(0.112330720464652,0.107599715891554,
0.789251528530322));
#13102=CARTESIAN_POINT('Ctrl Pts',(0.111947017038074,0.107998771601096,
0.789291478543127));
#13103=CARTESIAN_POINT('Ctrl Pts',(0.111767429463248,0.108184615374602,
0.789310091647807));
#13104=CARTESIAN_POINT('Ctrl Pts',(0.111354843299807,0.108609450666968,
0.789352660645121));
#13105=CARTESIAN_POINT('Ctrl Pts',(0.111121538323439,0.108848140208246,
0.789376592299338));
#13106=CARTESIAN_POINT('Ctrl Pts',(0.110507870358779,0.109471941927973,
0.789439181082622));
#13107=CARTESIAN_POINT('Ctrl Pts',(0.11012625787481,0.109855827474938,0.789477743044949));
#13108=CARTESIAN_POINT('Ctrl Pts',(0.107546896565529,0.112423604842781,
0.789736052218443));
#13109=CARTESIAN_POINT('Ctrl Pts',(0.105286131660525,0.114543597972723,
0.78995113818279));
#13110=CARTESIAN_POINT('Ctrl Pts',(0.10227824088442,0.117199826536193,0.790225472673442));
#13111=CARTESIAN_POINT('Ctrl Pts',(0.101587804607612,0.117798794222096,
0.79028766996987));
#13112=CARTESIAN_POINT('Ctrl Pts',(0.0915458374841799,0.126356452460334,
0.791181881236259));
#13113=CARTESIAN_POINT('Ctrl Pts',(0.0812888453034642,0.133186943557129,
0.791969342723043));
#13114=CARTESIAN_POINT('Ctrl Pts',(0.0663738002059899,0.140748145014673,
0.793087125375898));
#13115=CARTESIAN_POINT('Ctrl Pts',(0.0623291906936536,0.142585372432512,
0.793387385172353));
#13116=CARTESIAN_POINT('Ctrl Pts',(0.0557217693590248,0.14525183942048,
0.793878029224762));
#13117=CARTESIAN_POINT('Ctrl Pts',(0.0532062908837309,0.146192002284986,
0.794064829713856));
#13118=CARTESIAN_POINT('Ctrl Pts',(0.0499073590577501,0.147328561509932,
0.794310411203595));
#13119=CARTESIAN_POINT('Ctrl Pts',(0.0491448422838382,0.147584667082986,
0.794367215226336));
#13120=CARTESIAN_POINT('Ctrl Pts',(0.047901577854178,0.147991537425799,
0.794459913687363));
#13121=CARTESIAN_POINT('Ctrl Pts',(0.0474220163572628,0.14814590329908,
0.794495689498111));
#13122=CARTESIAN_POINT('Ctrl Pts',(0.0464984133227592,0.148438257428172,
0.794564632754068));
#13123=CARTESIAN_POINT('Ctrl Pts',(0.0460544856375709,0.148576589858141,
0.794597788510254));
#13124=CARTESIAN_POINT('Ctrl Pts',(0.0450367710393607,0.148888720828842,
0.794673844323989));
#13125=CARTESIAN_POINT('Ctrl Pts',(0.044462589310013,0.149061195718147,
0.79471678703855));
#13126=CARTESIAN_POINT('Ctrl Pts',(0.0429349999975343,0.149510447326604,
0.794831129950518));
#13127=CARTESIAN_POINT('Ctrl Pts',(0.0419799291292653,0.149781419241201,
0.794902717268526));
#13128=CARTESIAN_POINT('Ctrl Pts',(0.0348225602128495,0.151738269304934,
0.795440016857477));
#13129=CARTESIAN_POINT('Ctrl Pts',(0.0285245959452449,0.153047178533373,
0.795917780370095));
#13130=CARTESIAN_POINT('Ctrl Pts',(0.0080011785399801,0.15600173438768,
0.797491389239621));
#13131=CARTESIAN_POINT('Ctrl Pts',(-0.00637404542214832,0.156076522523706,
0.798625780759763));
#13132=CARTESIAN_POINT('Ctrl Pts',(-0.022833188343903,0.153882179321186,
0.7998710130445));
#13133=CARTESIAN_POINT('Ctrl Pts',(-0.0251033999956616,0.153528174743988,
0.800041356368757));
#13134=CARTESIAN_POINT('Ctrl Pts',(-0.0278768176971603,0.153032531702818,
0.800247071002812));
#13135=CARTESIAN_POINT('Ctrl Pts',(-0.028388089491437,0.152938514181768,
0.800284893780436));
#13136=CARTESIAN_POINT('Ctrl Pts',(-0.0291900412426293,0.152786883572281,
0.800344053064149));
#13137=CARTESIAN_POINT('Ctrl Pts',(-0.0294810378070146,0.152731001153364,
0.800365484960294));
#13138=CARTESIAN_POINT('Ctrl Pts',(-0.0300253575047191,0.1526248574209,
0.800405506959248));
#13139=CARTESIAN_POINT('Ctrl Pts',(-0.0302787122072849,0.152574797344376,
0.8004241077357));
#13140=CARTESIAN_POINT('Ctrl Pts',(-0.0308574497311752,0.152458946912431,
0.800466535736156));
#13141=CARTESIAN_POINT('Ctrl Pts',(-0.031182747021868,0.152392745861793,
0.800490339316069));
#13142=CARTESIAN_POINT('Ctrl Pts',(-0.032184173411267,0.152185605390961,
0.800563488802791));
#13143=CARTESIAN_POINT('Ctrl Pts',(-0.0328595903921099,0.152041201235197,
0.800612642422108));
#13144=CARTESIAN_POINT('Ctrl Pts',(-0.042148116187281,0.149990525887887,
0.80128638672946));
#13145=CARTESIAN_POINT('Ctrl Pts',(-0.0505863797026703,0.147359064157851,
0.80187243974495));
#13146=CARTESIAN_POINT('Ctrl Pts',(-0.0604135697152416,0.14334993345218,
0.802572387203032));
#13147=CARTESIAN_POINT('Ctrl Pts',(-0.0620576279375163,0.142645887665595,
0.80269007939709));
#13148=CARTESIAN_POINT('Ctrl Pts',(-0.0636886325197553,0.141913919640617,
0.802807733721352));
#13149=CARTESIAN_POINT('Origin',(0.,0.,-0.129405622560373));
#13150=CARTESIAN_POINT('',(-0.0636885883104208,0.141913939481031,0.886533246392299));
#13151=CARTESIAN_POINT('',(-0.0636886258347646,0.141913922640731,0.87264646002013));
#13152=CARTESIAN_POINT('',(-0.0636886258329924,0.141913922641526,-0.129405622560373));
#13153=CARTESIAN_POINT('',(-0.155549948690716,-0.000126342057708579,0.829469708790686));
#13154=CARTESIAN_POINT('Ctrl Pts',(-0.0636885883104107,0.141913939481036,
0.886533246392299));
#13155=CARTESIAN_POINT('Ctrl Pts',(-0.0557309582408581,0.145485189967631,
0.885954834675078));
#13156=CARTESIAN_POINT('Ctrl Pts',(-0.0474779691464282,0.148384890244849,
0.885387010768159));
#13157=CARTESIAN_POINT('Ctrl Pts',(-0.0324099555367,0.152289041749862,0.88434789329685));
#13158=CARTESIAN_POINT('Ctrl Pts',(-0.0257003671515546,0.153563761069064,
0.883884516764253));
#13159=CARTESIAN_POINT('Ctrl Pts',(-0.0179340183461664,0.154515951193323,
0.883336355006266));
#13160=CARTESIAN_POINT('Ctrl Pts',(-0.0169374964047631,0.154628358716609,
0.883265808559678));
#13161=CARTESIAN_POINT('Ctrl Pts',(-0.0153405636421684,0.154792870369464,
0.883152389149448));
#13162=CARTESIAN_POINT('Ctrl Pts',(-0.014740803744391,0.154851135922697,
0.883109709302275));
#13163=CARTESIAN_POINT('Ctrl Pts',(-0.0136770867155704,0.154948238304049,
0.883033859799711));
#13164=CARTESIAN_POINT('Ctrl Pts',(-0.0132132624224909,0.154988480030233,
0.883000734561069));
#13165=CARTESIAN_POINT('Ctrl Pts',(-0.0122483026607682,0.155067837563457,
0.882931708464853));
#13166=CARTESIAN_POINT('Ctrl Pts',(-0.0117471450188714,0.155106607653069,
0.882895797181827));
#13167=CARTESIAN_POINT('Ctrl Pts',(-0.0104491585834692,0.155200694518073,
0.882802622072632));
#13168=CARTESIAN_POINT('Ctrl Pts',(-0.00965208463037596,0.155252303403557,
0.882745242992048));
#13169=CARTESIAN_POINT('Ctrl Pts',(-0.00622756059518912,0.155447560575373,
0.882497999231447));
#13170=CARTESIAN_POINT('Ctrl Pts',(-0.00359724039065065,0.155530655786621,
0.88230626098265));
#13171=CARTESIAN_POINT('Ctrl Pts',(0.00335036183627117,0.155573812660352,
0.881794589444205));
#13172=CARTESIAN_POINT('Ctrl Pts',(0.00766579282231143,0.15542092993162,
0.881471395099634));
#13173=CARTESIAN_POINT('Ctrl Pts',(0.0243262636164154,0.154135162763463,
0.880203431210545));
#13174=CARTESIAN_POINT('Ctrl Pts',(0.0365238279629842,0.151708208869297,
0.879227542470186));
#13175=CARTESIAN_POINT('Ctrl Pts',(0.0491519596285416,0.147582804468907,
0.878215292317797));
#13176=CARTESIAN_POINT('Ctrl Pts',(0.0499980865010896,0.147298305208132,
0.878147483289698));
#13177=CARTESIAN_POINT('Ctrl Pts',(0.0538547442220192,0.145964492626417,
0.877838606861723));
#13178=CARTESIAN_POINT('Ctrl Pts',(0.056835295690395,0.144829967604943,
0.877600439671863));
#13179=CARTESIAN_POINT('Ctrl Pts',(0.0602831581317987,0.14339470498393,
0.877327199666263));
#13180=CARTESIAN_POINT('Ctrl Pts',(0.0607860925730163,0.143182231946716,
0.877287400392466));
#13181=CARTESIAN_POINT('Ctrl Pts',(0.0615927333595057,0.142836436848808,
0.877223672571824));
#13182=CARTESIAN_POINT('Ctrl Pts',(0.0618971440517604,0.142704786388414,
0.877199647075541));
#13183=CARTESIAN_POINT('Ctrl Pts',(0.0624384277052468,0.142468636095738,
0.877156972506382));
#13184=CARTESIAN_POINT('Ctrl Pts',(0.0626754630306191,0.142364517571019,
0.877138300646802));
#13185=CARTESIAN_POINT('Ctrl Pts',(0.0631803986298991,0.142141217454963,
0.877098560322931));
#13186=CARTESIAN_POINT('Ctrl Pts',(0.0634482216213194,0.142021870314343,
0.877077502187409));
#13187=CARTESIAN_POINT('Ctrl Pts',(0.0641768760939549,0.141694695131272,
0.877020261922814));
#13188=CARTESIAN_POINT('Ctrl Pts',(0.0646370400312778,0.141485374256706,
0.876984169713385));
#13189=CARTESIAN_POINT('Ctrl Pts',(0.0670051412948642,0.140394199923349,
0.876798681558541));
#13190=CARTESIAN_POINT('Ctrl Pts',(0.0688962019565898,0.1394759293378,0.876651398413019));
#13191=CARTESIAN_POINT('Ctrl Pts',(0.0744298143608292,0.136648864523816,
0.876221200489449));
#13192=CARTESIAN_POINT('Ctrl Pts',(0.0780161417610215,0.134633564841213,
0.87594339282131));
#13193=CARTESIAN_POINT('Ctrl Pts',(0.0904043013319887,0.127010686872075,
0.874972431110522));
#13194=CARTESIAN_POINT('Ctrl Pts',(0.0987173285323472,0.120662965108255,
0.87429801680404));
#13195=CARTESIAN_POINT('Ctrl Pts',(0.10850943998619,0.111491706516617,0.873400276261083));
#13196=CARTESIAN_POINT('Ctrl Pts',(0.110627235799444,0.109390641089544,
0.873199097977098));
#13197=CARTESIAN_POINT('Ctrl Pts',(0.115230988208832,0.104552766152732,
0.872743580914815));
#13198=CARTESIAN_POINT('Ctrl Pts',(0.117682317588431,0.101785705819696,
0.87248817161644));
#13199=CARTESIAN_POINT('Ctrl Pts',(0.120622271904033,0.0982187836493397,
0.872163528261071));
#13200=CARTESIAN_POINT('Ctrl Pts',(0.121205489450828,0.0974981599900408,
0.872098167603466));
#13201=CARTESIAN_POINT('Ctrl Pts',(0.122116015281513,0.0963523179964739,
0.871994571084442));
#13202=CARTESIAN_POINT('Ctrl Pts',(0.122447631540451,0.0959305367885992,
0.871956507371756));
#13203=CARTESIAN_POINT('Ctrl Pts',(0.123056712850689,0.0951475452999969,
0.871885969955472));
#13204=CARTESIAN_POINT('Ctrl Pts',(0.123334787277894,0.0947868144482662,
0.871853520822379));
#13205=CARTESIAN_POINT('Ctrl Pts',(0.123948433597489,0.0939834921825097,
0.871781361880888));
#13206=CARTESIAN_POINT('Ctrl Pts',(0.124283225954363,0.0935403160443579,
0.871741622071087));
#13207=CARTESIAN_POINT('Ctrl Pts',(0.125238155691429,0.0922620657407525,
0.871627190502249));
#13208=CARTESIAN_POINT('Ctrl Pts',(0.12585228937465,0.0914225660173952,
0.87155226728676));
#13209=CARTESIAN_POINT('Ctrl Pts',(0.130196115274874,0.0853579871591274,
0.871012562893483));
#13210=CARTESIAN_POINT('Ctrl Pts',(0.133607064566514,0.0799133597275997,
0.870535776563866));
#13211=CARTESIAN_POINT('Ctrl Pts',(0.142409037449887,0.063716915419631,
0.869137732793021));
#13212=CARTESIAN_POINT('Ctrl Pts',(0.146903239258912,0.0525316376017849,
0.868193035165235));
#13213=CARTESIAN_POINT('Ctrl Pts',(0.151238106539499,0.0366427548870334,
0.866934350184584));
#13214=CARTESIAN_POINT('Ctrl Pts',(0.152225777953326,0.0322951710133692,
0.866598541750189));
#13215=CARTESIAN_POINT('Ctrl Pts',(0.153144115564801,0.0272602196725307,
0.866223647285724));
#13216=CARTESIAN_POINT('Ctrl Pts',(0.15325861341003,0.0266089677823639,
0.866175423371968));
#13217=CARTESIAN_POINT('Ctrl Pts',(0.153423390178777,0.0256353710281211,
0.866103748638998));
#13218=CARTESIAN_POINT('Ctrl Pts',(0.153476811598263,0.0253135775551344,
0.866080126758472));
#13219=CARTESIAN_POINT('Ctrl Pts',(0.153570644680489,0.024737139403579,
0.866037936839227));
#13220=CARTESIAN_POINT('Ctrl Pts',(0.153611435677005,0.0244825612680901,
0.86601934772864));
#13221=CARTESIAN_POINT('Ctrl Pts',(0.153698394706228,0.023931072844203,
0.865979173254531));
#13222=CARTESIAN_POINT('Ctrl Pts',(0.153744335359232,0.0236341306558906,
0.86595760087406));
#13223=CARTESIAN_POINT('Ctrl Pts',(0.153870212378724,0.0228046106373711,
0.865897497671507));
#13224=CARTESIAN_POINT('Ctrl Pts',(0.153948244878478,0.0222717409634943,
0.865859072501626));
#13225=CARTESIAN_POINT('Ctrl Pts',(0.154384098287754,0.019183589710003,
0.865637394767268));
#13226=CARTESIAN_POINT('Ctrl Pts',(0.1546810907192,0.0166199335255763,0.865457360307288));
#13227=CARTESIAN_POINT('Ctrl Pts',(0.156244297755291,-0.000616012416733156,
0.864266429844491));
#13228=CARTESIAN_POINT('Ctrl Pts',(0.155485289398982,-0.0153978724115204,
0.863332979896753));
#13229=CARTESIAN_POINT('Ctrl Pts',(0.152295039607863,-0.0317112821963661,
0.862216217731747));
#13230=CARTESIAN_POINT('Ctrl Pts',(0.151897940870372,-0.0335618781605787,
0.862088358726973));
#13231=CARTESIAN_POINT('Ctrl Pts',(0.150549521551592,-0.0393306370886721,
0.861685386311132));
#13232=CARTESIAN_POINT('Ctrl Pts',(0.149479646316607,-0.0432190695091235,
0.861407303034985));
#13233=CARTESIAN_POINT('Ctrl Pts',(0.147997002703635,-0.0478899312834811,
0.861063265241731));
#13234=CARTESIAN_POINT('Ctrl Pts',(0.147727035230681,-0.0487163354011653,
0.861002010965989));
#13235=CARTESIAN_POINT('Ctrl Pts',(0.147269059704246,-0.0500794358067639,
0.860900317281739));
#13236=CARTESIAN_POINT('Ctrl Pts',(0.147085008124732,-0.0506174496222945,
0.860860008109573));
#13237=CARTESIAN_POINT('Ctrl Pts',(0.14674657211634,-0.0515893218831334,
0.860786877830356));
#13238=CARTESIAN_POINT('Ctrl Pts',(0.146593202367092,-0.0520235290196553,
0.860754090590148));
#13239=CARTESIAN_POINT('Ctrl Pts',(0.146259968857814,-0.0529537762068859,
0.860683597581025));
#13240=CARTESIAN_POINT('Ctrl Pts',(0.146079505183643,-0.0534495936139159,
0.860645872240338));
#13241=CARTESIAN_POINT('Ctrl Pts',(0.145580370926055,-0.0547995363058094,
0.860542735305214));
#13242=CARTESIAN_POINT('Ctrl Pts',(0.145256713087452,-0.0556517817827719,
0.860477158328525));
#13243=CARTESIAN_POINT('Ctrl Pts',(0.143505258188574,-0.0601442705812009,
0.860128963553767));
#13244=CARTESIAN_POINT('Ctrl Pts',(0.141948190634919,-0.0637322406613657,
0.859842042628733));
#13245=CARTESIAN_POINT('Ctrl Pts',(0.133860409900367,-0.0805983812626829,
0.858448817575511));
#13246=CARTESIAN_POINT('Ctrl Pts',(0.125592608505698,-0.0929572975477284,
0.857282509017944));
#13247=CARTESIAN_POINT('Ctrl Pts',(0.112751227511238,-0.107249849862203,
0.855814390644805));
#13248=CARTESIAN_POINT('Ctrl Pts',(0.109655499419823,-0.110413088288794,
0.855481087202818));
#13249=CARTESIAN_POINT('Ctrl Pts',(0.10594733564764,-0.113892055838166,
0.855108644749989));
#13250=CARTESIAN_POINT('Ctrl Pts',(0.105463006786398,-0.114340686351543,
0.855060498596647));
#13251=CARTESIAN_POINT('Ctrl Pts',(0.104735271038529,-0.115006224893193,
0.854988916488554));
#13252=CARTESIAN_POINT('Ctrl Pts',(0.10449402326186,-0.115225465377872,
0.854965310110057));
#13253=CARTESIAN_POINT('Ctrl Pts',(0.104060748222832,-0.1156167360056,0.854923136879356));
#13254=CARTESIAN_POINT('Ctrl Pts',(0.103868981746331,-0.115789047840443,
0.854904549026821));
#13255=CARTESIAN_POINT('Ctrl Pts',(0.103452669206257,-0.116161259076944,
0.85486436474035));
#13256=CARTESIAN_POINT('Ctrl Pts',(0.10322797238731,-0.116360983999005,
0.8548427813449));
#13257=CARTESIAN_POINT('Ctrl Pts',(0.102598611931363,-0.116917142121499,
0.854782616421558));
#13258=CARTESIAN_POINT('Ctrl Pts',(0.102192666368243,-0.117272129065913,
0.854744140897477));
#13259=CARTESIAN_POINT('Ctrl Pts',(0.0998249606595039,-0.119320984493836,
0.854521589233907));
#13260=CARTESIAN_POINT('Ctrl Pts',(0.0978228074341549,-0.120967849372446,
0.854340760945773));
#13261=CARTESIAN_POINT('Ctrl Pts',(0.0841843914425153,-0.131625880267573,
0.853149841597209));
#13262=CARTESIAN_POINT('Ctrl Pts',(0.071360144898193,-0.138997204756141,
0.852216938722345));
#13263=CARTESIAN_POINT('Ctrl Pts',(0.0559194062181418,-0.145163547839768,
0.851099879710145));
#13264=CARTESIAN_POINT('Ctrl Pts',(0.0541364776695639,-0.14583784484268,
0.850971103800745));
#13265=CARTESIAN_POINT('Ctrl Pts',(0.0485591677040739,-0.147830794478288,
0.850568189566551));
#13266=CARTESIAN_POINT('Ctrl Pts',(0.0447260570270535,-0.149035269705835,
0.850291118561336));
#13267=CARTESIAN_POINT('Ctrl Pts',(0.0400130168388674,-0.150318046280951,
0.849948200853536));
#13268=CARTESIAN_POINT('Ctrl Pts',(0.0391732550245654,-0.150539073301947,
0.849887017700901));
#13269=CARTESIAN_POINT('Ctrl Pts',(0.0377809163812575,-0.150893100686792,
0.849785417690192));
#13270=CARTESIAN_POINT('Ctrl Pts',(0.0372293745907179,-0.151030126562594,
0.849745130644801));
#13271=CARTESIAN_POINT('Ctrl Pts',(0.0362296067076135,-0.151272701230479,
0.849672023996671));
#13272=CARTESIAN_POINT('Ctrl Pts',(0.0357816370948312,-0.151379288471737,
0.849639238158773));
#13273=CARTESIAN_POINT('Ctrl Pts',(0.0353320238176394,-0.15148415954951,
0.849606301747618));
#13274=CARTESIAN_POINT('Ctrl Pts',(0.0353308424402875,-0.151484435087998,
0.849606215205634));
#13275=CARTESIAN_POINT('Ctrl Pts',(0.035328486592679,-0.151484984524953,
0.849606042627233));
#13276=CARTESIAN_POINT('Ctrl Pts',(0.0353273118913456,-0.15148525847747,
0.849605956573888));
#13277=CARTESIAN_POINT('Ctrl Pts',(0.0353249690444817,-0.15148580482489,
0.849605784947035));
#13278=CARTESIAN_POINT('Ctrl Pts',(0.0353238008911775,-0.151486077221765,
0.849605699372959));
#13279=CARTESIAN_POINT('Ctrl Pts',(0.0353214710870273,-0.151486620470821,
0.849605528700742));
#13280=CARTESIAN_POINT('Ctrl Pts',(0.0353203094287292,-0.151486891324896,
0.849605443602057));
#13281=CARTESIAN_POINT('Ctrl Pts',(0.0353179925598226,-0.151487431501596,
0.849605273876617));
#13282=CARTESIAN_POINT('Ctrl Pts',(0.0353168373425601,-0.151487700825927,
0.849605189249377));
#13283=CARTESIAN_POINT('Ctrl Pts',(0.0353145333101644,-0.151488237954226,
0.849605020463495));
#13284=CARTESIAN_POINT('Ctrl Pts',(0.0353133844851565,-0.15148850576065,
0.849604936304132));
#13285=CARTESIAN_POINT('Ctrl Pts',(0.0353110931748767,-0.151489039868139,
0.84960476844944));
#13286=CARTESIAN_POINT('Ctrl Pts',(0.0353099506864661,-0.151489306170089,
0.849604684753884));
#13287=CARTESIAN_POINT('Ctrl Pts',(0.0353076720066047,-0.151489837279055,
0.849604517823679));
#13288=CARTESIAN_POINT('Ctrl Pts',(0.0353065358064704,-0.151490102088245,
0.849604434588396));
#13289=CARTESIAN_POINT('Ctrl Pts',(0.0353042696469616,-0.151490630225239,
0.849604268574626));
#13290=CARTESIAN_POINT('Ctrl Pts',(0.0353031396815149,-0.151490893554606,
0.849604185795697));
#13291=CARTESIAN_POINT('Ctrl Pts',(0.0347944456962448,-0.151609434599421,
0.849566919841226));
#13292=CARTESIAN_POINT('Ctrl Pts',(0.034286296228128,-0.151725159382405,
0.84952965508757));
#13293=CARTESIAN_POINT('Ctrl Pts',(0.0329098126447955,-0.15203136853186,
0.849428601607333));
#13294=CARTESIAN_POINT('Ctrl Pts',(0.032040423038703,-0.152216963629336,
0.849364657668824));
#13295=CARTESIAN_POINT('Ctrl Pts',(0.0301068652700983,-0.152612435957079,
0.849222161993263));
#13296=CARTESIAN_POINT('Ctrl Pts',(0.029042005195906,-0.152818653208929,
0.849143497237425));
#13297=CARTESIAN_POINT('Ctrl Pts',(0.0257974275122641,-0.153411850931766,
0.848903199282392));
#13298=CARTESIAN_POINT('Ctrl Pts',(0.0236116116832879,-0.153763435657424,
0.848740476003865));
#13299=CARTESIAN_POINT('Ctrl Pts',(0.00649163142723672,-0.156143518667789,
0.847459033540093));
#13300=CARTESIAN_POINT('Ctrl Pts',(-0.00865689128124857,-0.156037903576278,
0.846272748448176));
#13301=CARTESIAN_POINT('Ctrl Pts',(-0.0245910061659342,-0.153597515877808,
0.845038443564618));
#13302=CARTESIAN_POINT('Ctrl Pts',(-0.0256317216626494,-0.153427277235785,
0.844957943113218));
#13303=CARTESIAN_POINT('Ctrl Pts',(-0.030379704097775,-0.152600949820218,
0.844591420359134));
#13304=CARTESIAN_POINT('Ctrl Pts',(-0.0340645062244877,-0.151820919592666,
0.844309010648112));
#13305=CARTESIAN_POINT('Ctrl Pts',(-0.0383259850394866,-0.150755810720089,
0.843987435419375));
#13306=CARTESIAN_POINT('Ctrl Pts',(-0.0389333361683257,-0.150600102808235,
0.843941725396808));
#13307=CARTESIAN_POINT('Ctrl Pts',(-0.0398525381522708,-0.150358512569947,
0.843872746074385));
#13308=CARTESIAN_POINT('Ctrl Pts',(-0.0401650800514967,-0.15027532548313,
0.843849327449929));
#13309=CARTESIAN_POINT('Ctrl Pts',(-0.0407261209372963,-0.15012412180567,
0.843807355222793));
#13310=CARTESIAN_POINT('Ctrl Pts',(-0.0409747110358075,-0.150056462484769,
0.843788781487636));
#13311=CARTESIAN_POINT('Ctrl Pts',(-0.0415148857965436,-0.149907999465116,
0.843748473247666));
#13312=CARTESIAN_POINT('Ctrl Pts',(-0.0418064023507024,-0.149826962770641,
0.84372675246862));
#13313=CARTESIAN_POINT('Ctrl Pts',(-0.0426253928067726,-0.149596720798495,
0.84366581610499));
#13314=CARTESIAN_POINT('Ctrl Pts',(-0.0431523243307589,-0.149445575092002,
0.843626710963861));
#13315=CARTESIAN_POINT('Ctrl Pts',(-0.0462751467000908,-0.148531926765663,
0.843395494773945));
#13316=CARTESIAN_POINT('Ctrl Pts',(-0.048851788521746,-0.147704528110391,
0.843206926862309));
#13317=CARTESIAN_POINT('Ctrl Pts',(-0.0572192549931257,-0.144774652656276,
0.842597793534907));
#13318=CARTESIAN_POINT('Ctrl Pts',(-0.0629073052769641,-0.142395324942774,
0.842188738504685));
#13319=CARTESIAN_POINT('Ctrl Pts',(-0.0777792221583317,-0.135108701157259,
0.841096069980007));
#13320=CARTESIAN_POINT('Ctrl Pts',(-0.0866355455706651,-0.129607995757295,
0.840418448221008));
#13321=CARTESIAN_POINT('Ctrl Pts',(-0.098004429180422,-0.120857413649837,
0.839441918038446));
#13322=CARTESIAN_POINT('Ctrl Pts',(-0.10103931436128,-0.118331884902855,
0.839169537002037));
#13323=CARTESIAN_POINT('Ctrl Pts',(-0.104616937976521,-0.115116655839939,
0.838831814887102));
#13324=CARTESIAN_POINT('Ctrl Pts',(-0.105254369837748,-0.114534124783255,
0.838770969424666));
#13325=CARTESIAN_POINT('Ctrl Pts',(-0.106302116421647,-0.113560485278865,
0.838669814239373));
#13326=CARTESIAN_POINT('Ctrl Pts',(-0.106715208618646,-0.1131723818188,
0.838629632325799));
#13327=CARTESIAN_POINT('Ctrl Pts',(-0.107459962228186,-0.112464976608252,
0.838556637702664));
#13328=CARTESIAN_POINT('Ctrl Pts',(-0.10779234641724,-0.112146442168666,
0.838523858273135));
#13329=CARTESIAN_POINT('Ctrl Pts',(-0.108435155383258,-0.111524919816016,
0.838460068305689));
#13330=CARTESIAN_POINT('Ctrl Pts',(-0.108745736797507,-0.111222099352119,
0.838429065236399));
#13331=CARTESIAN_POINT('Ctrl Pts',(-0.109603790271067,-0.110378457461784,
0.838342901456648));
#13332=CARTESIAN_POINT('Ctrl Pts',(-0.110148515197611,-0.109834872757619,
0.838287619677268));
#13333=CARTESIAN_POINT('Ctrl Pts',(-0.112453922919354,-0.107499892096503,
0.83805113004833));
#13334=CARTESIAN_POINT('Ctrl Pts',(-0.114175016550804,-0.105670127320208,
0.837868217802818));
#13335=CARTESIAN_POINT('Ctrl Pts',(-0.118565873240046,-0.100769481917354,
0.83738414451957));
#13336=CARTESIAN_POINT('Ctrl Pts',(-0.121160616010215,-0.0976342900634126,
0.837080119314934));
#13337=CARTESIAN_POINT('Ctrl Pts',(-0.12655911307234,-0.0905643367086734,
0.83640666176002));
#13338=CARTESIAN_POINT('Ctrl Pts',(-0.129308509468712,-0.086593369292964,
0.836035943440676));
#13339=CARTESIAN_POINT('Ctrl Pts',(-0.137825176806334,-0.072980468047344,
0.834794437583796));
#13340=CARTESIAN_POINT('Ctrl Pts',(-0.142733522471522,-0.0628419460443651,
0.833913836437172));
#13341=CARTESIAN_POINT('Ctrl Pts',(-0.146890228136033,-0.0511894658104013,
0.83299954343689));
#13342=CARTESIAN_POINT('Ctrl Pts',(-0.147261234641557,-0.0501121692644601,
0.832915918039014));
#13343=CARTESIAN_POINT('Ctrl Pts',(-0.147752606139395,-0.0486327650302099,
0.832802400043315));
#13344=CARTESIAN_POINT('Ctrl Pts',(-0.14788321852574,-0.0482341387922267,
0.83277194296649));
#13345=CARTESIAN_POINT('Ctrl Pts',(-0.148088117217248,-0.0476001360567745,
0.832723714123265));
#13346=CARTESIAN_POINT('Ctrl Pts',(-0.148163457305142,-0.0473651067273554,
0.832705881533063));
#13347=CARTESIAN_POINT('Ctrl Pts',(-0.148317799287829,-0.0468796530098195,
0.832669144943366));
#13348=CARTESIAN_POINT('Ctrl Pts',(-0.148396726501924,-0.0466292077633217,
0.832650245770599));
#13349=CARTESIAN_POINT('Ctrl Pts',(-0.148583054959099,-0.0460327010982864,
0.83260535619198));
#13350=CARTESIAN_POINT('Ctrl Pts',(-0.14868988284744,-0.0456864590156303,
0.832579399237554));
#13351=CARTESIAN_POINT('Ctrl Pts',(-0.149045020267678,-0.0445209752363483,
0.832492348755955));
#13352=CARTESIAN_POINT('Ctrl Pts',(-0.14928778277448,-0.0437000378200648,
0.832431568301207));
#13353=CARTESIAN_POINT('Ctrl Pts',(-0.149853825699472,-0.0417260973803592,
0.832286609177381));
#13354=CARTESIAN_POINT('Ctrl Pts',(-0.150170599403682,-0.0405712653102088,
0.83220276833904));
#13355=CARTESIAN_POINT('Ctrl Pts',(-0.153833038689739,-0.0265884656197295,
0.831197937906557));
#13356=CARTESIAN_POINT('Ctrl Pts',(-0.155539178755421,-0.013386082424089,
0.830349973974934));
#13357=CARTESIAN_POINT('Ctrl Pts',(-0.155549948690716,-0.000126342057708579,
0.829469708790686));
#13358=CARTESIAN_POINT('Ctrl Pts',(-0.155549948817025,-0.00012618645330382,
0.829469698460683));
#13359=CARTESIAN_POINT('Ctrl Pts',(-0.155554514228924,0.00550159346059295,
0.829096090860219));
#13360=CARTESIAN_POINT('Ctrl Pts',(-0.155253663330696,0.0111251091990293,
0.828718226575423));
#13361=CARTESIAN_POINT('Ctrl Pts',(-0.154386614564261,0.0191448636797682,
0.828163896303848));
#13362=CARTESIAN_POINT('Ctrl Pts',(-0.154067426800833,0.021563382051133,
0.827994722731987));
#13363=CARTESIAN_POINT('Ctrl Pts',(-0.153572980556294,0.0247332517364343,
0.827769883097865));
#13364=CARTESIAN_POINT('Ctrl Pts',(-0.153448805689968,0.0254923143944479,
0.827715807379159));
#13365=CARTESIAN_POINT('Ctrl Pts',(-0.153230687766271,0.0267662609700567,
0.827624640217435));
#13366=CARTESIAN_POINT('Ctrl Pts',(-0.153139765358742,0.0272816541554971,
0.827587643867501));
#13367=CARTESIAN_POINT('Ctrl Pts',(-0.152968574006925,0.0282242233515341,
0.827519771134307));
#13368=CARTESIAN_POINT('Ctrl Pts',(-0.152889111905139,0.0286515422165518,
0.827488920516889));
#13369=CARTESIAN_POINT('Ctrl Pts',(-0.152730514015063,0.0294849754697185,
0.827428590891142));
#13370=CARTESIAN_POINT('Ctrl Pts',(-0.152651546715168,0.0298911185664314,
0.827399117465349));
#13371=CARTESIAN_POINT('Ctrl Pts',(-0.152465607102645,0.0308274833278512,
0.827330992915194));
#13372=CARTESIAN_POINT('Ctrl Pts',(-0.152357488162434,0.031357469041479,
0.827292305603255));
#13373=CARTESIAN_POINT('Ctrl Pts',(-0.152052661911768,0.0328128880619441,
0.827185704437716));
#13374=CARTESIAN_POINT('Ctrl Pts',(-0.151850275055325,0.0337370939700421,
0.827117610291581));
#13375=CARTESIAN_POINT('Ctrl Pts',(-0.150764802056544,0.0384861854608708,
0.826765580276784));
#13376=CARTESIAN_POINT('Ctrl Pts',(-0.149745663954339,0.0422781621984397,
0.826477327948062));
#13377=CARTESIAN_POINT('Ctrl Pts',(-0.147850600286118,0.0483957719252788,
0.825999963242419));
#13378=CARTESIAN_POINT('Ctrl Pts',(-0.147060404198409,0.0507463015557448,
0.825813512639377));
#13379=CARTESIAN_POINT('Ctrl Pts',(-0.145134407212981,0.0560519777310876,
0.825385821812431));
#13380=CARTESIAN_POINT('Ctrl Pts',(-0.143963907809761,0.0589933198393297,
0.825143780320487));
#13381=CARTESIAN_POINT('Ctrl Pts',(-0.138437605606369,0.0717343465129827,
0.82407504923337));
#13382=CARTESIAN_POINT('Ctrl Pts',(-0.133164900959068,0.0811042719230291,
0.8232329413188));
#13383=CARTESIAN_POINT('Ctrl Pts',(-0.125293506205099,0.0922267032027333,
0.822204733871579));
#13384=CARTESIAN_POINT('Ctrl Pts',(-0.123550617045382,0.0945487992668807,
0.821988476892715));
#13385=CARTESIAN_POINT('Ctrl Pts',(-0.121493465401088,0.0971354820417315,
0.821746930237558));
#13386=CARTESIAN_POINT('Ctrl Pts',(-0.121242097156666,0.0974490528080551,
0.8217176377196));
#13387=CARTESIAN_POINT('Ctrl Pts',(-0.120763269050626,0.0980416489744151,
0.821662264391206));
#13388=CARTESIAN_POINT('Ctrl Pts',(-0.120536050914056,0.0983208651433942,
0.821636167364445));
#13389=CARTESIAN_POINT('Ctrl Pts',(-0.120141671882216,0.098802074455135,
0.821591183339302));
#13390=CARTESIAN_POINT('Ctrl Pts',(-0.119974966776974,0.0990044372268701,
0.821572263924446));
#13391=CARTESIAN_POINT('Ctrl Pts',(-0.119649911896764,0.0993969935569465,
0.82153555961722));
#13392=CARTESIAN_POINT('Ctrl Pts',(-0.119491620056914,0.0995872305247231,
0.821517770633871));
#13393=CARTESIAN_POINT('Ctrl Pts',(-0.119061618976135,0.100101509545521,
0.821469673446606));
#13394=CARTESIAN_POINT('Ctrl Pts',(-0.118789038484718,0.100424825982833,
0.821439428020346));
#13395=CARTESIAN_POINT('Ctrl Pts',(-0.117762841439244,0.101632006807619,
0.821326452422786));
#13396=CARTESIAN_POINT('Ctrl Pts',(-0.117000625615171,0.102508562819539,
0.821244323976098));
#13397=CARTESIAN_POINT('Ctrl Pts',(-0.110154046709239,0.110206330196331,
0.820521361599731));
#13398=CARTESIAN_POINT('Ctrl Pts',(-0.103488277063102,0.116488533027217,
0.819918595295257));
#13399=CARTESIAN_POINT('Ctrl Pts',(-0.0903949159700552,0.126811937635072,
0.818820801400127));
#13400=CARTESIAN_POINT('Ctrl Pts',(-0.0841511108279415,0.131038506765125,
0.818326983037018));
#13401=CARTESIAN_POINT('Ctrl Pts',(-0.074456218456099,0.136621570717291,
0.817573901214445));
#13402=CARTESIAN_POINT('Ctrl Pts',(-0.0712232535120552,0.138334475174034,
0.817324955649504));
#13403=CARTESIAN_POINT('Ctrl Pts',(-0.0665360277114172,0.140609997373972,
0.816964938170145));
#13404=CARTESIAN_POINT('Ctrl Pts',(-0.0651289138466826,0.141267259595859,
0.816856979135929));
#13405=CARTESIAN_POINT('Ctrl Pts',(-0.0637043666304979,0.141906857644826,
0.81674771167595));
#13406=CARTESIAN_POINT('Ctrl Pts',(-0.0636964963770145,0.141910390471292,
0.816747108002534));
#13407=CARTESIAN_POINT('Ctrl Pts',(-0.0636886258329888,0.141913922641528,
0.816746504307747));
#13408=CARTESIAN_POINT('Ctrl Pts',(-0.0636886325197553,0.141913919640617,
0.802807733721352));
#13409=CARTESIAN_POINT('Ctrl Pts',(-0.0709427906615581,0.138658372804173,
0.803331020463499));
#13410=CARTESIAN_POINT('Ctrl Pts',(-0.0779386900738588,0.13485051276678,
0.803854275908225));
#13411=CARTESIAN_POINT('Ctrl Pts',(-0.0883369135816863,0.128109604884196,
0.804695024206573));
#13412=CARTESIAN_POINT('Ctrl Pts',(-0.0919539666028445,0.125538611030549,
0.805000505086495));
#13413=CARTESIAN_POINT('Ctrl Pts',(-0.0962030810829642,0.122236103760248,
0.805378425520191));
#13414=CARTESIAN_POINT('Ctrl Pts',(-0.0969448704452268,0.121648632939773,
0.805445135611587));
#13415=CARTESIAN_POINT('Ctrl Pts',(-0.0980976888416617,0.120718400825775,
0.805549993675264));
#13416=CARTESIAN_POINT('Ctrl Pts',(-0.0985123967086169,0.120380216546245,
0.805587958223667));
#13417=CARTESIAN_POINT('Ctrl Pts',(-0.0992445678226578,0.119776831509414,
0.805655423274368));
#13418=CARTESIAN_POINT('Ctrl Pts',(-0.099562735511347,0.11951249014297,
0.805684888789684));
#13419=CARTESIAN_POINT('Ctrl Pts',(-0.100293243548118,0.118900624874036,
0.805752886526086));
#13420=CARTESIAN_POINT('Ctrl Pts',(-0.100704836599187,0.118552221273332,
0.80579145442426));
#13421=CARTESIAN_POINT('Ctrl Pts',(-0.101828423077946,0.117591059006142,
0.805897449177747));
#13422=CARTESIAN_POINT('Ctrl Pts',(-0.102536680289723,0.116973988681051,
0.805965053053673));
#13423=CARTESIAN_POINT('Ctrl Pts',(-0.10611526359444,0.113798667284445,
0.806310737500681));
#13424=CARTESIAN_POINT('Ctrl Pts',(-0.108895374065997,0.111141254791816,
0.806592952223893));
#13425=CARTESIAN_POINT('Ctrl Pts',(-0.113011389155491,0.106904088324655,
0.807032961552413));
#13426=CARTESIAN_POINT('Ctrl Pts',(-0.114419155327026,0.105395988561302,
0.807187758456438));
#13427=CARTESIAN_POINT('Ctrl Pts',(-0.125546393482391,0.0929899625007461,
0.808446588180703));
#13428=CARTESIAN_POINT('Ctrl Pts',(-0.133715683730569,0.0808026459482706,
0.809603952325363));
#13429=CARTESIAN_POINT('Ctrl Pts',(-0.14125501705106,0.065194313414932,
0.810909774768515));
#13430=CARTESIAN_POINT('Ctrl Pts',(-0.142379234602237,0.0627011513930527,
0.811113217928002));
#13431=CARTESIAN_POINT('Ctrl Pts',(-0.143649058715307,0.05967453594177,
0.811353034189395));
#13432=CARTESIAN_POINT('Ctrl Pts',(-0.143858232142606,0.0591684998854224,
0.811392893765217));
#13433=CARTESIAN_POINT('Ctrl Pts',(-0.144178764846738,0.0583813129063918,
0.811454521108485));
#13434=CARTESIAN_POINT('Ctrl Pts',(-0.1442919809195,0.0581009309390728,
0.811476397570913));
#13435=CARTESIAN_POINT('Ctrl Pts',(-0.144500117926105,0.0575811145710233,
0.811516816215091));
#13436=CARTESIAN_POINT('Ctrl Pts',(-0.144595260912915,0.0573417767373752,
0.811535371262656));
#13437=CARTESIAN_POINT('Ctrl Pts',(-0.144808541586246,0.0568013502459086,
0.811577146044424));
#13438=CARTESIAN_POINT('Ctrl Pts',(-0.14492633467931,0.0565001294483033,
0.811600344949062));
#13439=CARTESIAN_POINT('Ctrl Pts',(-0.145269826322503,0.0556136095581081,
0.811668377051388));
#13440=CARTESIAN_POINT('Ctrl Pts',(-0.145492928506876,0.0550273004801538,
0.811713058462969));
#13441=CARTESIAN_POINT('Ctrl Pts',(-0.147034079437659,0.0509022748581949,
0.812025339882027));
#13442=CARTESIAN_POINT('Ctrl Pts',(-0.148226566933849,0.0473175752641455,
0.812286019783897));
#13443=CARTESIAN_POINT('Ctrl Pts',(-0.150546706777027,0.0393902057793274,
0.812846743677707));
#13444=CARTESIAN_POINT('Ctrl Pts',(-0.151619423201953,0.035035050228785,
0.813144787003368));
#13445=CARTESIAN_POINT('Ctrl Pts',(-0.154523603333601,0.0205799691305764,
0.814118814957486));
#13446=CARTESIAN_POINT('Ctrl Pts',(-0.155544297372826,0.0103459061205155,
0.814786177014324));
#13447=CARTESIAN_POINT('Ctrl Pts',(-0.155552455097302,-0.00439252726531829,
0.815785205400792));
#13448=CARTESIAN_POINT('Ctrl Pts',(-0.155361511363309,-0.00886875882136496,
0.816093330688297));
#13449=CARTESIAN_POINT('Ctrl Pts',(-0.154900791593397,-0.0142251221010313,
0.816470581476357));
#13450=CARTESIAN_POINT('Ctrl Pts',(-0.154816066085496,-0.0151193570196231,
0.816533846500607));
#13451=CARTESIAN_POINT('Ctrl Pts',(-0.154664159269177,-0.0165871566664824,
0.816638179465917));
#13452=CARTESIAN_POINT('Ctrl Pts',(-0.154601519529247,-0.0171611792037266,
0.816679104912957));
#13453=CARTESIAN_POINT('Ctrl Pts',(-0.154483115989479,-0.0181929099523547,
0.816752890858028));
#13454=CARTESIAN_POINT('Ctrl Pts',(-0.154428510129127,-0.0186507466140799,
0.816785714614313));
#13455=CARTESIAN_POINT('Ctrl Pts',(-0.154307836239588,-0.01962564367355,
0.816855783631093));
#13456=CARTESIAN_POINT('Ctrl Pts',(-0.154241203240571,-0.020142627068871,
0.816893046291902));
#13457=CARTESIAN_POINT('Ctrl Pts',(-0.154054671119672,-0.0215346432984295,
0.816993668450051));
#13458=CARTESIAN_POINT('Ctrl Pts',(-0.153929917372611,-0.0224089944816921,
0.817057180053865));
#13459=CARTESIAN_POINT('Ctrl Pts',(-0.153268283597083,-0.0267796160757041,
0.817376247106298));
#13460=CARTESIAN_POINT('Ctrl Pts',(-0.152619741702651,-0.030257647847939,
0.81763529468849));
#13461=CARTESIAN_POINT('Ctrl Pts',(-0.148587157058356,-0.0484230483110955,
0.819016926138375));
#13462=CARTESIAN_POINT('Ctrl Pts',(-0.143200185747883,-0.0625817613357571,
0.820204298025277));
#13463=CARTESIAN_POINT('Ctrl Pts',(-0.135054226686732,-0.0771940898268286,
0.821483759793902));
#13464=CARTESIAN_POINT('Ctrl Pts',(-0.134220652250412,-0.0786345251007929,
0.821610391617838));
#13465=CARTESIAN_POINT('Ctrl Pts',(-0.131812124365683,-0.0826465874672812,
0.821964030214036));
#13466=CARTESIAN_POINT('Ctrl Pts',(-0.130185166594307,-0.0851863849767095,
0.822188999421818));
#13467=CARTESIAN_POINT('Ctrl Pts',(-0.128182609646554,-0.0881209928235368,
0.822448873342377));
#13468=CARTESIAN_POINT('Ctrl Pts',(-0.127877663750674,-0.0885629376675909,
0.822488007609831));
#13469=CARTESIAN_POINT('Ctrl Pts',(-0.12738020199926,-0.0892759607469687,
0.822551131123704));
#13470=CARTESIAN_POINT('Ctrl Pts',(-0.12718909831537,-0.0895480111672114,
0.82257521207778));
#13471=CARTESIAN_POINT('Ctrl Pts',(-0.126847969571038,-0.0900303384188775,
0.82261789677546));
#13472=CARTESIAN_POINT('Ctrl Pts',(-0.126698291884646,-0.0902408558108802,
0.822636523724232));
#13473=CARTESIAN_POINT('Ctrl Pts',(-0.126375972988033,-0.090691805360956,
0.822676416878256));
#13474=CARTESIAN_POINT('Ctrl Pts',(-0.12620317014697,-0.090932117302656,
0.822697671694038));
#13475=CARTESIAN_POINT('Ctrl Pts',(-0.125725852467355,-0.0915919277272215,
0.822756022354877));
#13476=CARTESIAN_POINT('Ctrl Pts',(-0.125419921178669,-0.0920104048217402,
0.822793022270224));
#13477=CARTESIAN_POINT('Ctrl Pts',(-0.123759236309898,-0.0942583479850944,
0.8229917778906));
#13478=CARTESIAN_POINT('Ctrl Pts',(-0.122366446299144,-0.0960595598146429,
0.823151043812595));
#13479=CARTESIAN_POINT('Ctrl Pts',(-0.111982900638586,-0.108895431375117,
0.824291448241559));
#13480=CARTESIAN_POINT('Ctrl Pts',(-0.101553880412221,-0.118681529749294,
0.82519605490586));
#13481=CARTESIAN_POINT('Ctrl Pts',(-0.0846187913805061,-0.130682682624514,
0.826584003385049));
#13482=CARTESIAN_POINT('Ctrl Pts',(-0.0790686870865399,-0.134113490818743,
0.827027473250179));
#13483=CARTESIAN_POINT('Ctrl Pts',(-0.0724426566541869,-0.137654837279197,
0.827553875014385));
#13484=CARTESIAN_POINT('Ctrl Pts',(-0.0715605733508693,-0.138115448048711,
0.827623883288218));
#13485=CARTESIAN_POINT('Ctrl Pts',(-0.0701394623203017,-0.138840262839448,
0.827736594791734));
#13486=CARTESIAN_POINT('Ctrl Pts',(-0.0696032084020613,-0.139109870684167,
0.827779108678171));
#13487=CARTESIAN_POINT('Ctrl Pts',(-0.0686486856653592,-0.139582867008537,
0.827854758252922));
#13488=CARTESIAN_POINT('Ctrl Pts',(-0.0682310372095184,-0.139787497146982,
0.827887850247378));
#13489=CARTESIAN_POINT('Ctrl Pts',(-0.0673593652842269,-0.140209742529195,
0.827956902629154));
#13490=CARTESIAN_POINT('Ctrl Pts',(-0.0669051910952876,-0.140427032244889,
0.827992873825742));
#13491=CARTESIAN_POINT('Ctrl Pts',(-0.0657239834923578,-0.140985124092878,
0.828086411938883));
#13492=CARTESIAN_POINT('Ctrl Pts',(-0.0649953599545144,-0.141322504793454,
0.828144095878418));
#13493=CARTESIAN_POINT('Ctrl Pts',(-0.0618310977143198,-0.142758033364856,
0.828394570910129));
#13494=CARTESIAN_POINT('Ctrl Pts',(-0.0593701409965125,-0.143798906282152,
0.828589297226851));
#13495=CARTESIAN_POINT('Ctrl Pts',(-0.0527794287756847,-0.146388456857322,
0.829110996714711));
#13496=CARTESIAN_POINT('Ctrl Pts',(-0.0486087857251568,-0.147825666584394,
0.829441392899277));
#13497=CARTESIAN_POINT('Ctrl Pts',(-0.0324785437779717,-0.152627732754861,
0.830719496252659));
#13498=CARTESIAN_POINT('Ctrl Pts',(-0.0201937776026256,-0.154732834173996,
0.831697851186547));
#13499=CARTESIAN_POINT('Ctrl Pts',(-0.00393590476244397,-0.155548075948361,
0.832936736987945));
#13500=CARTESIAN_POINT('Ctrl Pts',(-7.53493148768674E-5,-0.155597866005134,
0.833226408301307));
#13501=CARTESIAN_POINT('Ctrl Pts',(0.0044138863096793,-0.155488642039542,
0.833555183720977));
#13502=CARTESIAN_POINT('Ctrl Pts',(0.00504424633625328,-0.155469469064192,
0.833601163124359));
#13503=CARTESIAN_POINT('Ctrl Pts',(0.00599841733932474,-0.15543463758223,
0.833670463127406));
#13504=CARTESIAN_POINT('Ctrl Pts',(0.00632231426643907,-0.155421800010246,
0.833693935148018));
#13505=CARTESIAN_POINT('Ctrl Pts',(0.00690353988906549,-0.155396943329064,
0.833735958797997));
#13506=CARTESIAN_POINT('Ctrl Pts',(0.0071608796303466,-0.155385297455609,
0.833754530829436));
#13507=CARTESIAN_POINT('Ctrl Pts',(0.00771967261606659,-0.155358618204026,
0.833794784235462));
#13508=CARTESIAN_POINT('Ctrl Pts',(0.0080211105724575,-0.155343346767629,
0.833816452121388));
#13509=CARTESIAN_POINT('Ctrl Pts',(0.00886673077742968,-0.155298038032034,
0.833877110850549));
#13510=CARTESIAN_POINT('Ctrl Pts',(0.00941080975329047,-0.155266017578841,
0.833915992814396));
#13511=CARTESIAN_POINT('Ctrl Pts',(0.0126394141179972,-0.155058972439274,
0.834145912635973));
#13512=CARTESIAN_POINT('Ctrl Pts',(0.0153194110167562,-0.154817175170915,
0.834333445651806));
#13513=CARTESIAN_POINT('Ctrl Pts',(0.032526643533326,-0.152813417442147,
0.835523968622352));
#13514=CARTESIAN_POINT('Ctrl Pts',(0.0467510858564298,-0.149078380392629,
0.836451973434921));
#13515=CARTESIAN_POINT('Ctrl Pts',(0.0620926028731287,-0.14263353916533,
0.83757012416017));
#13516=CARTESIAN_POINT('Ctrl Pts',(0.0639248085375822,-0.141821846693957,
0.837705565229497));
#13517=CARTESIAN_POINT('Ctrl Pts',(0.0692837532519598,-0.139322814073107,
0.838108170870832));
#13518=CARTESIAN_POINT('Ctrl Pts',(0.0727629080939486,-0.137537775797823,
0.838377997886358));
#13519=CARTESIAN_POINT('Ctrl Pts',(0.0769945146879745,-0.135161161205173,
0.838718771506387));
#13520=CARTESIAN_POINT('Ctrl Pts',(0.0778138720512623,-0.13469111342838,
0.838785356458359));
#13521=CARTESIAN_POINT('Ctrl Pts',(0.0790952059883833,-0.133940445661322,
0.83889045999301));
#13522=CARTESIAN_POINT('Ctrl Pts',(0.079560098018765,-0.133664824782526,
0.838928797836794));
#13523=CARTESIAN_POINT('Ctrl Pts',(0.0803782271988722,-0.133173999623865,
0.838996632307444));
#13524=CARTESIAN_POINT('Ctrl Pts',(0.0807320621206994,-0.13295979739428,
0.839026092213123));
#13525=CARTESIAN_POINT('Ctrl Pts',(0.0815407046839779,-0.132465848757613,
0.839093701593312));
#13526=CARTESIAN_POINT('Ctrl Pts',(0.0819949324661616,-0.132185168018858,
0.839131885042975));
#13527=CARTESIAN_POINT('Ctrl Pts',(0.0832455603812954,-0.131403441636436,
0.839237593024821));
#13528=CARTESIAN_POINT('Ctrl Pts',(0.0840388617350304,-0.13089750739833,
0.839305297166802));
#13529=CARTESIAN_POINT('Ctrl Pts',(0.0884737547136953,-0.128012186217781,
0.839687532650347));
#13530=CARTESIAN_POINT('Ctrl Pts',(0.0920185161390474,-0.125488289565871,
0.840007432816153));
#13531=CARTESIAN_POINT('Ctrl Pts',(0.1028726715123,-0.11705267662579,0.841034965171198));
#13532=CARTESIAN_POINT('Ctrl Pts',(0.109753981186708,-0.110626101523787,
0.841760971940625));
#13533=CARTESIAN_POINT('Ctrl Pts',(0.119829474337633,-0.099345516845188,
0.842933955167288));
#13534=CARTESIAN_POINT('Ctrl Pts',(0.123407606928729,-0.0948641356758045,
0.843378004460806));
#13535=CARTESIAN_POINT('Ctrl Pts',(0.128835816830005,-0.0872371376000215,
0.844089218141352));
#13536=CARTESIAN_POINT('Ctrl Pts',(0.130837181388826,-0.0842058382742902,
0.844361327493607));
#13537=CARTESIAN_POINT('Ctrl Pts',(0.133026188114896,-0.0806235494867982,
0.844668630867109));
#13538=CARTESIAN_POINT('Ctrl Pts',(0.133318951404708,-0.080138509338658,
0.844709945323327));
#13539=CARTESIAN_POINT('Ctrl Pts',(0.133781960304958,-0.0793618523010465,
0.844775617713906));
#13540=CARTESIAN_POINT('Ctrl Pts',(0.133953913974725,-0.0790712681092836,
0.844800082121021));
#13541=CARTESIAN_POINT('Ctrl Pts',(0.134256399066179,-0.0785562804696079,
0.844843247585486));
#13542=CARTESIAN_POINT('Ctrl Pts',(0.134387316463537,-0.0783321075256524,
0.844861973416464));
#13543=CARTESIAN_POINT('Ctrl Pts',(0.134663092547841,-0.0778571632652931,
0.844901510768642));
#13544=CARTESIAN_POINT('Ctrl Pts',(0.134807812090975,-0.0776063152665721,
0.844922313309607));
#13545=CARTESIAN_POINT('Ctrl Pts',(0.13519527533038,-0.0769303559597684,
0.844978160074161));
#13546=CARTESIAN_POINT('Ctrl Pts',(0.135436716976263,-0.0765044956311639,
0.845013121595415));
#13547=CARTESIAN_POINT('Ctrl Pts',(0.136608966385062,-0.0744139130601118,
0.845183700495456));
#13548=CARTESIAN_POINT('Ctrl Pts',(0.137511166073088,-0.0727332128514912,
0.845317589070989));
#13549=CARTESIAN_POINT('Ctrl Pts',(0.14000720524231,-0.0678707992849482,
0.845696979603526));
#13550=CARTESIAN_POINT('Ctrl Pts',(0.141523173141172,-0.0646502775005473,
0.845938695814096));
#13551=CARTESIAN_POINT('Ctrl Pts',(0.148684157789354,-0.0479755392683395,
0.847156338429439));
#13552=CARTESIAN_POINT('Ctrl Pts',(0.152526471659468,-0.0338279864847041,
0.848086812223037));
#13553=CARTESIAN_POINT('Ctrl Pts',(0.15446835579267,-0.0183403555419018,
0.849154448954754));
#13554=CARTESIAN_POINT('Ctrl Pts',(0.154585224745113,-0.0173277176048889,
0.849224433192257));
#13555=CARTESIAN_POINT('Ctrl Pts',(0.154919424531863,-0.014158782569299,
0.849444090304843));
#13556=CARTESIAN_POINT('Ctrl Pts',(0.155101642279014,-0.0119991245545318,
0.849594730634901));
#13557=CARTESIAN_POINT('Ctrl Pts',(0.15529624999085,-0.00892783001396077,
0.849810637341172));
#13558=CARTESIAN_POINT('Ctrl Pts',(0.155345843864133,-0.00801873690103627,
0.849874752560793));
#13559=CARTESIAN_POINT('Ctrl Pts',(0.155414015532305,-0.00652870903575065,
0.849980203060855));
#13560=CARTESIAN_POINT('Ctrl Pts',(0.155437323399908,-0.00594800329527819,
0.850021390534172));
#13561=CARTESIAN_POINT('Ctrl Pts',(0.155473298004804,-0.00490602040753982,
0.850095463174784));
#13562=CARTESIAN_POINT('Ctrl Pts',(0.155487167538701,-0.00444478920921299,
0.850128310394621));
#13563=CARTESIAN_POINT('Ctrl Pts',(0.15551227255689,-0.00346479740739736,
0.850198230833581));
#13564=CARTESIAN_POINT('Ctrl Pts',(0.155522964970464,-0.0029460298091664,
0.850235320609249));
#13565=CARTESIAN_POINT('Ctrl Pts',(0.155544675222567,-0.00155488572332244,
0.850334992998728));
#13566=CARTESIAN_POINT('Ctrl Pts',(0.155550949349555,-0.00068246506152315,
0.85039772280156));
#13567=CARTESIAN_POINT('Ctrl Pts',(0.155545725178648,0.00359569501132507,
0.850706469466919));
#13568=CARTESIAN_POINT('Ctrl Pts',(0.15542971592967,0.00700011914161767,
0.850955712691444));
#13569=CARTESIAN_POINT('Ctrl Pts',(0.154187477041494,0.0255423929228684,
0.852334013408533));
#13570=CARTESIAN_POINT('Ctrl Pts',(0.150961455966671,0.0404556384175158,
0.853529659254922));
#13571=CARTESIAN_POINT('Ctrl Pts',(0.145139469463207,0.0559667988643988,
0.854797088651043));
#13572=CARTESIAN_POINT('Ctrl Pts',(0.144631747907989,0.0572660971600335,
0.854903354439001));
#13573=CARTESIAN_POINT('Ctrl Pts',(0.142863363931482,0.0616179186166481,
0.8552592567934));
#13574=CARTESIAN_POINT('Ctrl Pts',(0.141522883046087,0.0646373450244673,
0.855506170260098));
#13575=CARTESIAN_POINT('Ctrl Pts',(0.13984744555462,0.0681087263205664,
0.855788219469132));
#13576=CARTESIAN_POINT('Ctrl Pts',(0.139605092773141,0.0686041159511367,
0.855828425231567));
#13577=CARTESIAN_POINT('Ctrl Pts',(0.139212079184579,0.0693967618156155,
0.855892672430234));
#13578=CARTESIAN_POINT('Ctrl Pts',(0.1390630919076,0.0696948349315154,0.855916813346368));
#13579=CARTESIAN_POINT('Ctrl Pts',(0.138796597856358,0.0702237425100022,
0.855959612467863));
#13580=CARTESIAN_POINT('Ctrl Pts',(0.138679471242554,0.0704547645557252,
0.855978293998204));
#13581=CARTESIAN_POINT('Ctrl Pts',(0.138429029649834,0.0709456945210096,
0.856017964958107));
#13582=CARTESIAN_POINT('Ctrl Pts',(0.138295559756299,0.0712055192832181,
0.856038944448093));
#13583=CARTESIAN_POINT('Ctrl Pts',(0.137931281503052,0.0719097689075282,
0.856095768671674));
#13584=CARTESIAN_POINT('Ctrl Pts',(0.137699054842487,0.0723534629124167,
0.856131525639183));
#13585=CARTESIAN_POINT('Ctrl Pts',(0.136508579364141,0.0746015020393035,
0.856312511341029));
#13586=CARTESIAN_POINT('Ctrl Pts',(0.135516934222805,0.0763880747952177,
0.856455747372342));
#13587=CARTESIAN_POINT('Ctrl Pts',(0.132510650857198,0.0815613524984651,
0.856870307278052));
#13588=CARTESIAN_POINT('Ctrl Pts',(0.130402097041442,0.0848918432503784,
0.857136953144764));
#13589=CARTESIAN_POINT('Ctrl Pts',(0.1222134458951,0.0967995525154898,0.858103081685175));
#13590=CARTESIAN_POINT('Ctrl Pts',(0.115395229838299,0.104834312919997,
0.858782169934589));
#13591=CARTESIAN_POINT('Ctrl Pts',(0.103094447859705,0.116663161575551,
0.859923095134347));
#13592=CARTESIAN_POINT('Ctrl Pts',(0.0980884836985785,0.120902398137326,
0.860368849358707));
#13593=CARTESIAN_POINT('Ctrl Pts',(0.092031441662467,0.125407368982369,
0.860897742754843));
#13594=CARTESIAN_POINT('Ctrl Pts',(0.0912266068626585,0.125994049733277,
0.860967811126981));
#13595=CARTESIAN_POINT('Ctrl Pts',(0.0899275998023373,0.126921983353701,
0.861080600919101));
#13596=CARTESIAN_POINT('Ctrl Pts',(0.089436979016023,0.1272681807477,0.861123132572274));
#13597=CARTESIAN_POINT('Ctrl Pts',(0.0885627884640505,0.127877485668954,
0.861198802598185));
#13598=CARTESIAN_POINT('Ctrl Pts',(0.0881800175851144,0.128141731421221,
0.861231897196103));
#13599=CARTESIAN_POINT('Ctrl Pts',(0.0877948238505663,0.128405106624818,
0.861265164810487));
#13600=CARTESIAN_POINT('Ctrl Pts',(0.0877935766114245,0.128405959394635,
0.86126527252907));
#13601=CARTESIAN_POINT('Ctrl Pts',(0.0877910927589434,0.128407657616026,
0.861265487047772));
#13602=CARTESIAN_POINT('Ctrl Pts',(0.0877898561428815,0.128408503069914,
0.861265593848131));
#13603=CARTESIAN_POINT('Ctrl Pts',(0.0877873934459118,0.128410186722777,
0.861265806538233));
#13604=CARTESIAN_POINT('Ctrl Pts',(0.0877861673595772,0.128411024925908,
0.861265912428451));
#13605=CARTESIAN_POINT('Ctrl Pts',(0.0877837256161923,0.128412694150966,
0.861266123307431));
#13606=CARTESIAN_POINT('Ctrl Pts',(0.0877825099604475,0.128413525172438,
0.861266228296087));
#13607=CARTESIAN_POINT('Ctrl Pts',(0.0877800889905027,0.128415180095466,
0.861266437379541));
#13608=CARTESIAN_POINT('Ctrl Pts',(0.0877788836737805,0.128416003999176,
0.861266541474563));
#13609=CARTESIAN_POINT('Ctrl Pts',(0.087776483278764,0.128417644758453,
0.861266748779673));
#13610=CARTESIAN_POINT('Ctrl Pts',(0.0877752882036578,0.128418461612263,
0.861266851989492));
#13611=CARTESIAN_POINT('Ctrl Pts',(0.0877729082047907,0.128420088332524,
0.861267057531733));
#13612=CARTESIAN_POINT('Ctrl Pts',(0.0877717232793406,0.128420898200545,
0.861267159864309));
#13613=CARTESIAN_POINT('Ctrl Pts',(0.0877693634909101,0.128422511011214,
0.861267363659757));
#13614=CARTESIAN_POINT('Ctrl Pts',(0.0877681886245434,0.128423313956585,
0.861267465122928));
#13615=CARTESIAN_POINT('Ctrl Pts',(0.087765848859657,0.128424912987841,
0.861267667187758));
#13616=CARTESIAN_POINT('Ctrl Pts',(0.0877646839608254,0.128425709074341,
0.861267767789449));
#13617=CARTESIAN_POINT('Ctrl Pts',(0.0877623640347443,0.128427294454839,
0.86126796813965));
#13618=CARTESIAN_POINT('Ctrl Pts',(0.0877612090095433,0.128428083747832,
0.861268067887988));
#13619=CARTESIAN_POINT('Ctrl Pts',(0.0877589087537019,0.128429655595129,
0.861268266538151));
#13620=CARTESIAN_POINT('Ctrl Pts',(0.0877577635171766,0.12843043815384,
0.86126836544049));
#13621=CARTESIAN_POINT('Ctrl Pts',(0.0877554827392267,0.128431996601691,
0.861268562407259));
#13622=CARTESIAN_POINT('Ctrl Pts',(0.0877543471980134,0.128432772491066,
0.861268660471678));
#13623=CARTESIAN_POINT('Ctrl Pts',(0.0877520857370583,0.128434317651691,
0.861268855768982));
#13624=CARTESIAN_POINT('Ctrl Pts',(0.0877509598099265,0.128435086928363,
0.861268953002512));
#13625=CARTESIAN_POINT('Ctrl Pts',(0.0877487174695555,0.128436618938199,
0.861269146647345));
#13626=CARTESIAN_POINT('Ctrl Pts',(0.0877476010615809,0.128437381668133,
0.861269243058199));
#13627=CARTESIAN_POINT('Ctrl Pts',(0.0877453776883554,0.128438900634212,
0.861269435063842));
#13628=CARTESIAN_POINT('Ctrl Pts',(0.0877442707177036,0.128439656874407,
0.861269530659104));
#13629=CARTESIAN_POINT('Ctrl Pts',(0.0877420661286834,0.128441162923872,
0.861269721041388));
#13630=CARTESIAN_POINT('Ctrl Pts',(0.0877409685077732,0.128441912735231,
0.861269815828635));
#13631=CARTESIAN_POINT('Ctrl Pts',(0.0877387825411712,0.128443405980728,
0.861270004601562));
#13632=CARTESIAN_POINT('Ctrl Pts',(0.0877376941896687,0.128444149419183,
0.861270098587747));
#13633=CARTESIAN_POINT('Ctrl Pts',(0.0877355266612734,0.128445629988633,
0.861270285767254));
#13634=CARTESIAN_POINT('Ctrl Pts',(0.0877344474885076,0.128446367117152,
0.861270378960224));
#13635=CARTESIAN_POINT('Ctrl Pts',(0.0877322982490207,0.128447835114586,
0.861270564559233));
#13636=CARTESIAN_POINT('Ctrl Pts',(0.0877312281761717,0.128448565988023,
0.861270656965807));
#13637=CARTESIAN_POINT('Ctrl Pts',(0.0877290970522117,0.128450021533881,
0.86127084099932));
#13638=CARTESIAN_POINT('Ctrl Pts',(0.0877280359977181,0.128450746208942,
0.861270932626556));
#13639=CARTESIAN_POINT('Ctrl Pts',(0.0877259228208885,0.128452189420214,
0.861271115109143));
#13640=CARTESIAN_POINT('Ctrl Pts',(0.0877248707003412,0.128452907955529,
0.861271205964345));
#13641=CARTESIAN_POINT('Ctrl Pts',(0.0877227753123451,0.12845433894227,
0.861271386909705));
#13642=CARTESIAN_POINT('Ctrl Pts',(0.0877217320434193,0.128455051395024,
0.861271476999995));
#13643=CARTESIAN_POINT('Ctrl Pts',(0.0877196542919911,0.128456470263131,
0.861271656421302));
#13644=CARTESIAN_POINT('Ctrl Pts',(0.0877186198002404,0.128457176685111,
0.861271745753123));
#13645=CARTESIAN_POINT('Ctrl Pts',(0.0877165595105252,0.128458583555865,
0.861271923665505));
#13646=CARTESIAN_POINT('Ctrl Pts',(0.0877155337124031,0.128459284005053,
0.861272012246084));
#13647=CARTESIAN_POINT('Ctrl Pts',(0.0877134907367074,0.128460678981151,
0.861272188662321));
#13648=CARTESIAN_POINT('Ctrl Pts',(0.0877124735553404,0.128461373510953,
0.86127227649831));
#13649=CARTESIAN_POINT('Ctrl Pts',(0.0877104477309279,0.128462756705325,
0.86127245143248));
#13650=CARTESIAN_POINT('Ctrl Pts',(0.0877094390854991,0.12846344537182,
0.861272538530871));
#13651=CARTESIAN_POINT('Ctrl Pts',(0.0877074302697687,0.128464816883613,
0.861272711995315));
#13652=CARTESIAN_POINT('Ctrl Pts',(0.0877064300894679,0.128465499736029,
0.861272798362234));
#13653=CARTESIAN_POINT('Ctrl Pts',(0.0877044381113941,0.128466859683759,
0.861272970371744));
#13654=CARTESIAN_POINT('Ctrl Pts',(0.087703446314811,0.128467536778546,
0.861273056014235));
#13655=CARTESIAN_POINT('Ctrl Pts',(0.0877014710344858,0.128468885259447,
0.861273226580917));
#13656=CARTESIAN_POINT('Ctrl Pts',(0.0877004875479138,0.128469556647775,
0.861273311505356));
#13657=CARTESIAN_POINT('Ctrl Pts',(0.0876985288094731,0.128470893769944,
0.861273480642693));
#13658=CARTESIAN_POINT('Ctrl Pts',(0.0876975535564825,0.128471559504826,
0.861273564855692));
#13659=CARTESIAN_POINT('Ctrl Pts',(0.087695611214741,0.12847288536903,0.861273732576245));
#13660=CARTESIAN_POINT('Ctrl Pts',(0.0876946441219777,0.128473545501362,
0.86127381608415));
#13661=CARTESIAN_POINT('Ctrl Pts',(0.087692718027213,0.128474860211434,
0.861273982400871));
#13662=CARTESIAN_POINT('Ctrl Pts',(0.0876917590208031,0.128475514792451,
0.861274065210072));
#13663=CARTESIAN_POINT('Ctrl Pts',(0.0876898490282865,0.128476818448784,
0.861274230135481));
#13664=CARTESIAN_POINT('Ctrl Pts',(0.0876888980361884,0.128477467528452,
0.861274312252211));
#13665=CARTESIAN_POINT('Ctrl Pts',(0.0876870040011461,0.128478760231434,
0.861274475798832));
#13666=CARTESIAN_POINT('Ctrl Pts',(0.0876860609528391,0.128479403858666,
0.86127455722919));
#13667=CARTESIAN_POINT('Ctrl Pts',(0.0876841827247945,0.128480685712548,
0.861274719410038));
#13668=CARTESIAN_POINT('Ctrl Pts',(0.0876832475450118,0.128481323939481,
0.861274800160536));
#13669=CARTESIAN_POINT('Ctrl Pts',(0.0876813849900348,0.128482595037186,
0.861274960987198));
#13670=CARTESIAN_POINT('Ctrl Pts',(0.0876804576085012,0.128483227912534,
0.861275041063914));
#13671=CARTESIAN_POINT('Ctrl Pts',(0.0876786105905786,0.12848448834838,
0.861275200548155));
#13672=CARTESIAN_POINT('Ctrl Pts',(0.087677690942862,0.128485115916853,
0.861275279956663));
#13673=CARTESIAN_POINT('Ctrl Pts',(0.0876758593060191,0.128486365798749,
0.861275438111973));
#13674=CARTESIAN_POINT('Ctrl Pts',(0.0876749473174137,0.128486988112055,
0.861275516858734));
#13675=CARTESIAN_POINT('Ctrl Pts',(0.0876731309353678,0.128488227527615,
0.861275673696038));
#13676=CARTESIAN_POINT('Ctrl Pts',(0.0876722265382817,0.128488844632593,
0.861275751786898));
#13677=CARTESIAN_POINT('Ctrl Pts',(0.0876704252715704,0.128490073678399,
0.861275907318257));
#13678=CARTESIAN_POINT('Ctrl Pts',(0.0876695283974716,0.128490685622513,
0.861275984759145));
#13679=CARTESIAN_POINT('Ctrl Pts',(0.087667943279937,0.128491767136107,
0.861276121626291));
#13680=CARTESIAN_POINT('Ctrl Pts',(0.0876672550322583,0.128492236714143,
0.861276181052995));
#13681=CARTESIAN_POINT('Ctrl Pts',(0.0876658796485813,0.128493175095536,
0.861276299810186));
#13682=CARTESIAN_POINT('Ctrl Pts',(0.0876651926736389,0.128493643789042,
0.861276359126766));
#13683=CARTESIAN_POINT('Ctrl Pts',(0.0876638200525214,0.128494580253363,
0.861276477644964));
#13684=CARTESIAN_POINT('Ctrl Pts',(0.0876631344019249,0.128495048027225,
0.861276536846963));
#13685=CARTESIAN_POINT('Ctrl Pts',(0.0876617644256033,0.128495982655008,
0.861276655136339));
#13686=CARTESIAN_POINT('Ctrl Pts',(0.087661080096343,0.128496449511373,
0.86127671422402));
#13687=CARTESIAN_POINT('Ctrl Pts',(0.087659712755036,0.128497382309478,
0.861276832285421));
#13688=CARTESIAN_POINT('Ctrl Pts',(0.0876590297427072,0.128497848251442,
0.861276891259165));
#13689=CARTESIAN_POINT('Ctrl Pts',(0.0876576650304796,0.128498779224104,
0.861277009093106));
#13690=CARTESIAN_POINT('Ctrl Pts',(0.0876569833317044,0.128499244254066,
0.861277067953206));
#13691=CARTESIAN_POINT('Ctrl Pts',(0.0876556212358863,0.128500173410113,
0.861277185560784));
#13692=CARTESIAN_POINT('Ctrl Pts',(0.0876549408425665,0.128500637533689,
0.861277244307941));
#13693=CARTESIAN_POINT('Ctrl Pts',(0.0876535813695065,0.128501564868973,
0.86127736168861));
#13694=CARTESIAN_POINT('Ctrl Pts',(0.0876529022830971,0.128502028085262,
0.861277420322699));
#13695=CARTESIAN_POINT('Ctrl Pts',(0.0876515454120886,0.128502953614093,
0.861277537478251));
#13696=CARTESIAN_POINT('Ctrl Pts',(0.0876508676260698,0.128503415927633,
0.861277595999836));
#13697=CARTESIAN_POINT('Ctrl Pts',(0.0876495133582066,0.128504339649445,
0.861277712930177));
#13698=CARTESIAN_POINT('Ctrl Pts',(0.0876488368718639,0.128504801060816,
0.861277771339322));
#13699=CARTESIAN_POINT('Ctrl Pts',(0.0876474851919838,0.128505722986133,
0.861277888045766));
#13700=CARTESIAN_POINT('Ctrl Pts',(0.0876468099999454,0.128506183499088,
0.861277946342935));
#13701=CARTESIAN_POINT('Ctrl Pts',(0.0876454609008248,0.128507103633018,
0.861278062826107));
#13702=CARTESIAN_POINT('Ctrl Pts',(0.0876447869963007,0.128507563252279,
0.861278121011888));
#13703=CARTESIAN_POINT('Ctrl Pts',(0.087643440482064,0.128508481592188,
0.861278237271435));
#13704=CARTESIAN_POINT('Ctrl Pts',(0.0876427678667361,0.128508940316696,
0.861278295345685));
#13705=CARTESIAN_POINT('Ctrl Pts',(0.0876414239146435,0.128509856878272,
0.861278411383572));
#13706=CARTESIAN_POINT('Ctrl Pts',(0.0876407525802623,0.128510314713744,
0.861278469347003));
#13707=CARTESIAN_POINT('Ctrl Pts',(0.0876394111951554,0.128511229493862,
0.861278585162816));
#13708=CARTESIAN_POINT('Ctrl Pts',(0.08763874114114,0.128511686440782,0.861278643015481));
#13709=CARTESIAN_POINT('Ctrl Pts',(0.087637402309562,0.128512599448798,
0.861278758610382));
#13710=CARTESIAN_POINT('Ctrl Pts',(0.0876367335323633,0.128513055509675,
0.861278816352588));
#13711=CARTESIAN_POINT('Ctrl Pts',(0.087635397241258,0.128513966754667,
0.86127893172771));
#13712=CARTESIAN_POINT('Ctrl Pts',(0.0876347297317331,0.128514421935823,
0.861278989360247));
#13713=CARTESIAN_POINT('Ctrl Pts',(0.0876333959916878,0.128515331410747,
0.861279104514676));
#13714=CARTESIAN_POINT('Ctrl Pts',(0.0876327297531324,0.128515785710023,
0.861279162037262));
#13715=CARTESIAN_POINT('Ctrl Pts',(0.0876313985378597,0.12851669343298,
0.861279276973271));
#13716=CARTESIAN_POINT('Ctrl Pts',(0.0876307335615464,0.128517146856413,
0.86127933438666));
#13717=CARTESIAN_POINT('Ctrl Pts',(0.0876294048798295,0.128518052821587,
0.861279449103494));
#13718=CARTESIAN_POINT('Ctrl Pts',(0.0876287411680163,0.128518505367725,
0.861279506407492));
#13719=CARTESIAN_POINT('Ctrl Pts',(0.0876274149972206,0.128519409590722,
0.861279620907107));
#13720=CARTESIAN_POINT('Ctrl Pts',(0.0876267525426929,0.12851986126457,
0.861279678102338));
#13721=CARTESIAN_POINT('Ctrl Pts',(0.0876254288821741,0.128520763746001,
0.861279792384792));
#13722=CARTESIAN_POINT('Ctrl Pts',(0.0876247676807267,0.128521214550513,
0.861279849471622));
#13723=CARTESIAN_POINT('Ctrl Pts',(0.0876234465214615,0.128522115296701,
0.861279963537696));
#13724=CARTESIAN_POINT('Ctrl Pts',(0.0876227865665,0.128522565236457,0.861280020516694));
#13725=CARTESIAN_POINT('Ctrl Pts',(0.0876214679117838,0.128523464245327,
0.861280134366106));
#13726=CARTESIAN_POINT('Ctrl Pts',(0.0876208092042186,0.128523913319792,
0.861280191237196));
#13727=CARTESIAN_POINT('Ctrl Pts',(0.0876194930407674,0.128524810600568,
0.861280304871096));
#13728=CARTESIAN_POINT('Ctrl Pts',(0.0876188355799287,0.128525258810284,
0.861280361634335));
#13729=CARTESIAN_POINT('Ctrl Pts',(0.0876175218870788,0.128526154377224,
0.86128047505451));
#13730=CARTESIAN_POINT('Ctrl Pts',(0.087616865661705,0.128526601729951,
0.861280531710873));
#13731=CARTESIAN_POINT('Ctrl Pts',(0.0876155544518105,0.128527495574799,
0.861280644916258));
#13732=CARTESIAN_POINT('Ctrl Pts',(0.0876148994624468,0.12852794207025,
0.861280701465699));
#13733=CARTESIAN_POINT('Ctrl Pts',(0.0876135907205038,0.128528834203403,
0.861280814457592));
#13734=CARTESIAN_POINT('Ctrl Pts',(0.0876129369639253,0.128529279843859,
0.86128087090039));
#13735=CARTESIAN_POINT('Ctrl Pts',(0.0876116306808378,0.128530170271684,
0.861280983679579));
#13736=CARTESIAN_POINT('Ctrl Pts',(0.0876109781521583,0.128530615060559,
0.861281040016157));
#13737=CARTESIAN_POINT('Ctrl Pts',(0.0876096743280367,0.128531503783145,
0.861281152582634));
#13738=CARTESIAN_POINT('Ctrl Pts',(0.0876090230282226,0.128531947719863,
0.861281208812911));
#13739=CARTESIAN_POINT('Ctrl Pts',(0.0871812073418933,0.128823549200173,
0.861318144414142));
#13740=CARTESIAN_POINT('Ctrl Pts',(0.0867525989968188,0.129112572189949,
0.861355104045547));
#13741=CARTESIAN_POINT('Ctrl Pts',(0.0855910672287118,0.129887431733229,
0.861455150813779));
#13742=CARTESIAN_POINT('Ctrl Pts',(0.0848554614192455,0.130369192372853,
0.861518389363862));
#13743=CARTESIAN_POINT('Ctrl Pts',(0.0832204400110838,0.131420294888535,
0.861658700150327));
#13744=CARTESIAN_POINT('Ctrl Pts',(0.0823191920591894,0.13198668894343,
0.861735877643107));
#13745=CARTESIAN_POINT('Ctrl Pts',(0.0795743140512054,0.13367267244437,
0.8619704756261));
#13746=CARTESIAN_POINT('Ctrl Pts',(0.0777132127266061,0.134763164587089,
0.862128927159207));
#13747=CARTESIAN_POINT('Ctrl Pts',(0.0628779988512285,0.143046194644541,
0.863387624077439));
#13748=CARTESIAN_POINT('Ctrl Pts',(0.0489592455952193,0.148386933290451,
0.86455338930693));
#13749=CARTESIAN_POINT('Ctrl Pts',(0.0332946637113915,0.151949977996143,
0.865785739690024));
#13750=CARTESIAN_POINT('Ctrl Pts',(0.0320860979303089,0.152209766104469,
0.865880255471062));
#13751=CARTESIAN_POINT('Ctrl Pts',(0.0270405618503047,0.153231565775232,
0.866272203081998));
#13752=CARTESIAN_POINT('Ctrl Pts',(0.0231782342824295,0.153863188342659,
0.866565935525092));
#13753=CARTESIAN_POINT('Ctrl Pts',(0.0186680098006594,0.154427031980521,
0.866898735600778));
#13754=CARTESIAN_POINT('Ctrl Pts',(0.0180397194148179,0.154501687228857,
0.866944866603948));
#13755=CARTESIAN_POINT('Ctrl Pts',(0.0170884270230544,0.154608840368648,
0.86701434948501));
#13756=CARTESIAN_POINT('Ctrl Pts',(0.0167657604544999,0.154644162967363,
0.867037853957583));
#13757=CARTESIAN_POINT('Ctrl Pts',(0.0161867927283748,0.154705709706023,
0.867079912319031));
#13758=CARTESIAN_POINT('Ctrl Pts',(0.0159305361579924,0.154732307213625,
0.867098486759973));
#13759=CARTESIAN_POINT('Ctrl Pts',(0.0153742592741097,0.154788647982125,
0.867138718601952));
#13760=CARTESIAN_POINT('Ctrl Pts',(0.0150742190333812,0.154818155644297,
0.867160362633513));
#13761=CARTESIAN_POINT('Ctrl Pts',(0.0142330908995031,0.154898408543729,
0.867220887374982));
#13762=CARTESIAN_POINT('Ctrl Pts',(0.013691812799435,0.15494719142898,0.867259659977492));
#13763=CARTESIAN_POINT('Ctrl Pts',(0.0105339611448528,0.155215117043182,
0.86748489524559));
#13764=CARTESIAN_POINT('Ctrl Pts',(0.00791223073821961,0.155370832859545,
0.867668025095678));
#13765=CARTESIAN_POINT('Ctrl Pts',(-0.00938443492379959,0.155959138381236,
0.868858253106924));
#13766=CARTESIAN_POINT('Ctrl Pts',(-0.0240546187594827,0.154378764784856,
0.869789041449628));
#13767=CARTESIAN_POINT('Ctrl Pts',(-0.0401545510479763,0.150290142989394,
0.870905093455021));
#13768=CARTESIAN_POINT('Ctrl Pts',(-0.0420130401465986,0.149781237418863,
0.871035281904662));
#13769=CARTESIAN_POINT('Ctrl Pts',(-0.0476935630183817,0.148111712342661,
0.871438140633943));
#13770=CARTESIAN_POINT('Ctrl Pts',(-0.0514804665691437,0.146838387871464,
0.871713687029259));
#13771=CARTESIAN_POINT('Ctrl Pts',(-0.0560241298396049,0.145113233177457,
0.872054905275818));
#13772=CARTESIAN_POINT('Ctrl Pts',(-0.056831737219131,0.144798850679256,
0.872115968445238));
#13773=CARTESIAN_POINT('Ctrl Pts',(-0.0581639338038398,0.144267396061234,
0.872217403594079));
#13774=CARTESIAN_POINT('Ctrl Pts',(-0.0586900447208019,0.144054168273587,
0.872257646441696));
#13775=CARTESIAN_POINT('Ctrl Pts',(-0.0596406100690489,0.143662841417161,
0.872330696129825));
#13776=CARTESIAN_POINT('Ctrl Pts',(-0.0600654656211035,0.143485728226998,
0.872363469371213));
#13777=CARTESIAN_POINT('Ctrl Pts',(-0.0604930733683425,0.143305235735787,
0.87239658139186));
#13778=CARTESIAN_POINT('Ctrl Pts',(-0.0604966220396954,0.143303737692402,
0.87239685619382));
#13779=CARTESIAN_POINT('Ctrl Pts',(-0.0605035930545927,0.143300794628937,
0.872397396032431));
#13780=CARTESIAN_POINT('Ctrl Pts',(-0.0605070160446262,0.143299349346655,
0.872397661118549));
#13781=CARTESIAN_POINT('Ctrl Pts',(-0.0605137412126719,0.143296509508395,
0.872398181950845));
#13782=CARTESIAN_POINT('Ctrl Pts',(-0.0605170434629638,0.143295114931893,
0.872398437702057));
#13783=CARTESIAN_POINT('Ctrl Pts',(-0.0605235317047551,0.143292374611977,
0.872398940215497));
#13784=CARTESIAN_POINT('Ctrl Pts',(-0.0605267177710916,0.143291028846237,
0.872399186982998));
#13785=CARTESIAN_POINT('Ctrl Pts',(-0.0605329780071209,0.143288384332856,
0.872399671865314));
#13786=CARTESIAN_POINT('Ctrl Pts',(-0.0605360522575128,0.143287085559744,
0.872399909985893));
#13787=CARTESIAN_POINT('Ctrl Pts',(-0.0605420926507131,0.143284533456456,
0.872400377866405));
#13788=CARTESIAN_POINT('Ctrl Pts',(-0.0605450588802291,0.143283280097737,
0.872400607632582));
#13789=CARTESIAN_POINT('Ctrl Pts',(-0.0605508891893127,0.143280816329487,
0.872401059264462));
#13790=CARTESIAN_POINT('Ctrl Pts',(-0.0605537521743916,0.143279606389964,
0.872401281044945));
#13791=CARTESIAN_POINT('Ctrl Pts',(-0.0605593783858018,0.143277228471676,
0.872401716889391));
#13792=CARTESIAN_POINT('Ctrl Pts',(-0.0605621416162174,0.143276060498106,
0.872401930953278));
#13793=CARTESIAN_POINT('Ctrl Pts',(-0.0605675720198831,0.143273764967636,
0.872402351650126));
#13794=CARTESIAN_POINT('Ctrl Pts',(-0.0605702391954167,0.143272637416204,
0.872402558282899));
#13795=CARTESIAN_POINT('Ctrl Pts',(-0.0610598249756475,0.143065648366848,
0.872440488634159));
#13796=CARTESIAN_POINT('Ctrl Pts',(-0.0615456853657312,0.142857308419279,
0.872478296295375));
#13797=CARTESIAN_POINT('Ctrl Pts',(-0.0625846159187864,0.142405524813775,
0.872559502527816));
#13798=CARTESIAN_POINT('Ctrl Pts',(-0.0631373441878761,0.142161328743564,
0.872602926138957));
#13799=CARTESIAN_POINT('Ctrl Pts',(-0.0636886258347646,0.141913922640731,
0.87264646002013));
#13800=CARTESIAN_POINT('Origin',(0.,0.,-0.129405622560373));
#13801=CARTESIAN_POINT('',(-0.0636886228436576,0.14191392398309,0.956529730343417));
#13802=CARTESIAN_POINT('',(-0.0636886279045103,0.141913921711863,0.942835077379979));
#13803=CARTESIAN_POINT('',(-0.0636886258329924,0.141913922641526,-0.129405622560373));
#13804=CARTESIAN_POINT('Ctrl Pts',(-0.0636886228436577,0.14191392398309,
0.956529730343417));
#13805=CARTESIAN_POINT('Ctrl Pts',(-0.0605616421227201,0.143317261232781,
0.95626580888382));
#13806=CARTESIAN_POINT('Ctrl Pts',(-0.0573883432362314,0.144617218288781,
0.956003754733755));
#13807=CARTESIAN_POINT('Ctrl Pts',(-0.0516595524775657,0.146745655762337,
0.955543579904026));
#13808=CARTESIAN_POINT('Ctrl Pts',(-0.0491212969258761,0.147614692335739,
0.955344073949756));
#13809=CARTESIAN_POINT('Ctrl Pts',(-0.0460398608689767,0.148581401105557,
0.955108111206096));
#13810=CARTESIAN_POINT('Ctrl Pts',(-0.0455172163110459,0.148742342951681,
0.95506830310435));
#13811=CARTESIAN_POINT('Ctrl Pts',(-0.0447043650646508,0.148987964673378,
0.955006733736637));
#13812=CARTESIAN_POINT('Ctrl Pts',(-0.0444147490985092,0.149074558326085,
0.954984864139642));
#13813=CARTESIAN_POINT('Ctrl Pts',(-0.0438778053492266,0.149233398022506,
0.954944445212162));
#13814=CARTESIAN_POINT('Ctrl Pts',(-0.0436305527662352,0.149305873142629,
0.954925883076122));
#13815=CARTESIAN_POINT('Ctrl Pts',(-0.0430721755460429,0.149468040169477,
0.954884075616488));
#13816=CARTESIAN_POINT('Ctrl Pts',(-0.0427609509344645,0.149557375006153,
0.954860851219839));
#13817=CARTESIAN_POINT('Ctrl Pts',(-0.0418446251520368,0.149817305706711,
0.954792695463313));
#13818=CARTESIAN_POINT('Ctrl Pts',(-0.0412387561642388,0.149985208501964,
0.954747916666911));
#13819=CARTESIAN_POINT('Ctrl Pts',(-0.0369572440978493,0.151143826569018,
0.954433376674147));
#13820=CARTESIAN_POINT('Ctrl Pts',(-0.0332469560861469,0.152003092786986,
0.954170649527741));
#13821=CARTESIAN_POINT('Ctrl Pts',(-0.028501874617075,0.152919903096122,
0.953842670361788));
#13822=CARTESIAN_POINT('Ctrl Pts',(-0.027493332379588,0.153104442705289,
0.953773415504164));
#13823=CARTESIAN_POINT('Ctrl Pts',(-0.0116456296118653,0.155842554439753,
0.95269128757154));
#13824=CARTESIAN_POINT('Ctrl Pts',(0.00348505447402093,0.156238328516161,
0.951733510985633));
#13825=CARTESIAN_POINT('Ctrl Pts',(0.0206331190770367,0.154191331757608,
0.950551500627717));
#13826=CARTESIAN_POINT('Ctrl Pts',(0.0228229056783667,0.153882443979089,
0.950398919571636));
#13827=CARTESIAN_POINT('Ctrl Pts',(0.0260749588618998,0.153352774974058,
0.950169449389325));
#13828=CARTESIAN_POINT('Ctrl Pts',(0.0271427664052125,0.153167382954111,
0.950093639526612));
#13829=CARTESIAN_POINT('Ctrl Pts',(0.0290814589951995,0.152809879150505,
0.949955105425714));
#13830=CARTESIAN_POINT('Ctrl Pts',(0.029952981008281,0.152641440289458,
0.949892497992219));
#13831=CARTESIAN_POINT('Ctrl Pts',(0.0313338949610883,0.152362269641473,
0.949792750707262));
#13832=CARTESIAN_POINT('Ctrl Pts',(0.0318442640754913,0.152256418640378,
0.949755766364858));
#13833=CARTESIAN_POINT('Ctrl Pts',(0.0323552245392878,0.152147763527324,
0.949718617420224));
#13834=CARTESIAN_POINT('Ctrl Pts',(0.0323563631412977,0.152147521391651,
0.94971853463853));
#13835=CARTESIAN_POINT('Ctrl Pts',(0.0323586466220602,0.152147035758696,
0.949718368617576));
#13836=CARTESIAN_POINT('Ctrl Pts',(0.0323597914947508,0.152146792262557,
0.949718285378751));
#13837=CARTESIAN_POINT('Ctrl Pts',(0.0323620875712343,0.152146303896665,
0.949718118439563));
#13838=CARTESIAN_POINT('Ctrl Pts',(0.0323632387665168,0.152146059028573,
0.949718034739813));
#13839=CARTESIAN_POINT('Ctrl Pts',(0.0323655475365981,0.152145567908027,
0.949717866875234));
#13840=CARTESIAN_POINT('Ctrl Pts',(0.0323667051044633,0.152145321656897,
0.949717782710902));
#13841=CARTESIAN_POINT('Ctrl Pts',(0.0323690266744545,0.152144827758173,
0.949717613913161));
#13842=CARTESIAN_POINT('Ctrl Pts',(0.0323701906679437,0.152144580112262,
0.949717529280371));
#13843=CARTESIAN_POINT('Ctrl Pts',(0.0323725251373474,0.152144083413267,
0.94971735954219));
#13844=CARTESIAN_POINT('Ctrl Pts',(0.032373695607215,0.152143834361314,
0.949717274437232));
#13845=CARTESIAN_POINT('Ctrl Pts',(0.0323760430834124,0.152143334838265,
0.949717103750761));
#13846=CARTESIAN_POINT('Ctrl Pts',(0.0323772200821449,0.152143084368629,
0.949717018169795));
#13847=CARTESIAN_POINT('Ctrl Pts',(0.032379580671995,0.15214258199784,0.949716846527222));
#13848=CARTESIAN_POINT('Ctrl Pts',(0.0323807642534029,0.152142330098593,
0.949716760466315));
#13849=CARTESIAN_POINT('Ctrl Pts',(0.0323831379893035,0.152141824872209,
0.94971658786524));
#13850=CARTESIAN_POINT('Ctrl Pts',(0.0323843281337768,0.152141571547047,
0.949716501325796));
#13851=CARTESIAN_POINT('Ctrl Pts',(0.032835900190565,0.152045447789354,
0.949683665736758));
#13852=CARTESIAN_POINT('Ctrl Pts',(0.0332858494498373,0.151947578963342,
0.949650853196147));
#13853=CARTESIAN_POINT('Ctrl Pts',(0.0342900624437464,0.151724477285312,
0.949577405257927));
#13854=CARTESIAN_POINT('Ctrl Pts',(0.0348440854145153,0.15159820277853,
0.949536736920863));
#13855=CARTESIAN_POINT('Ctrl Pts',(0.0362427354886735,0.151271346418091,
0.949433689187789));
#13856=CARTESIAN_POINT('Ctrl Pts',(0.0370863887693582,0.151066726429398,
0.949371181116677));
#13857=CARTESIAN_POINT('Ctrl Pts',(0.0418202506969962,0.149876529749583,
0.949018419431836));
#13858=CARTESIAN_POINT('Ctrl Pts',(0.0456725421758692,0.148747843499238,
0.948723599568112));
#13859=CARTESIAN_POINT('Ctrl Pts',(0.0512867919273554,0.14686426783951,
0.948281889444133));
#13860=CARTESIAN_POINT('Ctrl Pts',(0.0530855958110184,0.146223688864191,
0.948138504818793));
#13861=CARTESIAN_POINT('Ctrl Pts',(0.0686437175628241,0.140358312249086,
0.946882244898241));
#13862=CARTESIAN_POINT('Ctrl Pts',(0.0816067039213671,0.133239197660704,
0.945715106069722));
#13863=CARTESIAN_POINT('Ctrl Pts',(0.0954507241606839,0.122848255642365,
0.944412915170613));
#13864=CARTESIAN_POINT('Ctrl Pts',(0.0974867403277383,0.121238905752293,
0.944220062472617));
#13865=CARTESIAN_POINT('Ctrl Pts',(0.0998963733384406,0.11923425711897,
0.94399108415196));
#13866=CARTESIAN_POINT('Ctrl Pts',(0.100309266152085,0.118887108738101,
0.943951821827424));
#13867=CARTESIAN_POINT('Ctrl Pts',(0.100949475516749,0.118343129465159,
0.943890913112717));
#13868=CARTESIAN_POINT('Ctrl Pts',(0.10117803588526,0.118147780162392,0.943869162023602));
#13869=CARTESIAN_POINT('Ctrl Pts',(0.101601523124038,0.11778369778257,0.943828851465));
#13870=CARTESIAN_POINT('Ctrl Pts',(0.101796594989769,0.117615144495934,
0.943810279769402));
#13871=CARTESIAN_POINT('Ctrl Pts',(0.102237341433666,0.117232396321224,
0.943768310169039));
#13872=CARTESIAN_POINT('Ctrl Pts',(0.102482761931622,0.11701791419601,0.943744933900112));
#13873=CARTESIAN_POINT('Ctrl Pts',(0.103223036059529,0.116366845823294,
0.943674396979351));
#13874=CARTESIAN_POINT('Ctrl Pts',(0.103715796035067,0.115927872724899,
0.943627409198699));
#13875=CARTESIAN_POINT('Ctrl Pts',(0.107484211303136,0.112527535302619,
0.94326765534566));
#13876=CARTESIAN_POINT('Ctrl Pts',(0.110635599865423,0.109430685989414,
0.942964381326475));
#13877=CARTESIAN_POINT('Ctrl Pts',(0.1237422794111,0.0954048800150995,0.941668841431201));
#13878=CARTESIAN_POINT('Ctrl Pts',(0.132242906875762,0.0832232246797103,
0.940729093471332));
#13879=CARTESIAN_POINT('Ctrl Pts',(0.140665790789191,0.0665159729279089,
0.939454608411167));
#13880=CARTESIAN_POINT('Ctrl Pts',(0.142300806178678,0.062942159239021,
0.939183276244309));
#13881=CARTESIAN_POINT('Ctrl Pts',(0.144146801727768,0.0584665337771078,
0.938843120661047));
#13882=CARTESIAN_POINT('Ctrl Pts',(0.144487470350992,0.0576195007644558,
0.938778732039682));
#13883=CARTESIAN_POINT('Ctrl Pts',(0.145013331761929,0.056278013709661,
0.938676714027132));
#13884=CARTESIAN_POINT('Ctrl Pts',(0.145203501328331,0.0557855214665347,
0.938639251786081));
#13885=CARTESIAN_POINT('Ctrl Pts',(0.145554838070132,0.0548616774134873,
0.938568956608212));
#13886=CARTESIAN_POINT('Ctrl Pts',(0.145716604577305,0.0544305582952572,
0.938536144114774));
#13887=CARTESIAN_POINT('Ctrl Pts',(0.146073710701386,0.0534658435094093,
0.938462696836499));
#13888=CARTESIAN_POINT('Ctrl Pts',(0.146268044641094,0.0529318852986887,
0.93842202911494));
#13889=CARTESIAN_POINT('Ctrl Pts',(0.146751860597336,0.0515795258457461,
0.938318983980847));
#13890=CARTESIAN_POINT('Ctrl Pts',(0.147037422034294,0.0507597531511795,
0.938256477904554));
#13891=CARTESIAN_POINT('Ctrl Pts',(0.148604337422754,0.0461373515406115,
0.937903747445434));
#13892=CARTESIAN_POINT('Ctrl Pts',(0.149744918301528,0.0422889851955426,
0.937608957759007));
#13893=CARTESIAN_POINT('Ctrl Pts',(0.15120684129218,0.0365505228376165,
0.93716725216043));
#13894=CARTESIAN_POINT('Ctrl Pts',(0.151644164357749,0.0346914465339953,
0.93702384068137));
#13895=CARTESIAN_POINT('Ctrl Pts',(0.155152896367734,0.0184387429981322,
0.935767572922593));
#13896=CARTESIAN_POINT('Ctrl Pts',(0.156200950457405,0.00368696476256723,
0.93460045507406));
#13897=CARTESIAN_POINT('Ctrl Pts',(0.154977838413255,-0.0135796118118842,
0.933298255529385));
#13898=CARTESIAN_POINT('Ctrl Pts',(0.154729720408327,-0.0161632926673331,
0.933105379469176));
#13899=CARTESIAN_POINT('Ctrl Pts',(0.154352057576583,-0.0192752644350223,
0.932876377157122));
#13900=CARTESIAN_POINT('Ctrl Pts',(0.154284282256396,-0.0198104459562377,
0.932837113451182));
#13901=CARTESIAN_POINT('Ctrl Pts',(0.154174396726348,-0.0206433595920402,
0.932776203063593));
#13902=CARTESIAN_POINT('Ctrl Pts',(0.154134206010954,-0.0209413333562646,
0.932754451673873));
#13903=CARTESIAN_POINT('Ctrl Pts',(0.154057949533934,-0.0214945841933946,
0.932714140842873));
#13904=CARTESIAN_POINT('Ctrl Pts',(0.154022113485362,-0.0217498855996991,
0.932695569174006));
#13905=CARTESIAN_POINT('Ctrl Pts',(0.153939534570932,-0.0223277500680519,
0.932653599996227));
#13906=CARTESIAN_POINT('Ctrl Pts',(0.153892412619383,-0.0226502554175331,
0.932630224121317));
#13907=CARTESIAN_POINT('Ctrl Pts',(0.153746821260097,-0.0236252597032322,
0.932559689564563));
#13908=CARTESIAN_POINT('Ctrl Pts',(0.153645211395646,-0.0242772939247841,
0.932512703736852));
#13909=CARTESIAN_POINT('Ctrl Pts',(0.15283190250593,-0.029286585055981,
0.932153010964684));
#13910=CARTESIAN_POINT('Ctrl Pts',(0.15193905196086,-0.0336129154550012,
0.931849792433107));
#13911=CARTESIAN_POINT('Ctrl Pts',(0.147262842354895,-0.052228877496125,
0.930554396683378));
#13912=CARTESIAN_POINT('Ctrl Pts',(0.141638449781161,-0.0659757428550496,
0.929614738110709));
#13913=CARTESIAN_POINT('Ctrl Pts',(0.13216892268605,-0.0821135268963821,
0.928340232676168));
#13914=CARTESIAN_POINT('Ctrl Pts',(0.130051807652998,-0.0854270345897545,
0.928068762459612));
#13915=CARTESIAN_POINT('Ctrl Pts',(0.127291190612526,-0.089406873773799,
0.927728453812722));
#13916=CARTESIAN_POINT('Ctrl Pts',(0.126764167278465,-0.0901525491389225,
0.92766405505106));
#13917=CARTESIAN_POINT('Ctrl Pts',(0.125922108611989,-0.0913219788017271,
0.927562024593833));
#13918=CARTESIAN_POINT('Ctrl Pts',(0.125611422188316,-0.0917488520521021,
0.927524560117915));
#13919=CARTESIAN_POINT('Ctrl Pts',(0.125025712463918,-0.0925450471626755,
0.927454262935369));
#13920=CARTESIAN_POINT('Ctrl Pts',(0.124751209957878,-0.0929147466074473,
0.927421450683122));
#13921=CARTESIAN_POINT('Ctrl Pts',(0.12413433430201,-0.0937378919021104,
0.927348006781666));
#13922=CARTESIAN_POINT('Ctrl Pts',(0.123791111546934,-0.0941906896513171,
0.927307342209724));
#13923=CARTESIAN_POINT('Ctrl Pts',(0.122917333295667,-0.0953303991769037,
0.927204310374685));
#13924=CARTESIAN_POINT('Ctrl Pts',(0.122383500943652,-0.0960147617387886,
0.927141814505881));
#13925=CARTESIAN_POINT('Ctrl Pts',(0.119350839044903,-0.0998361908755614,
0.926789243787177));
#13926=CARTESIAN_POINT('Ctrl Pts',(0.116737363938768,-0.102879882271182,
0.926494608473505));
#13927=CARTESIAN_POINT('Ctrl Pts',(0.112709002933879,-0.107220041460402,
0.926052926001055));
#13928=CARTESIAN_POINT('Ctrl Pts',(0.111382909454409,-0.108596977794657,
0.925909377126475));
#13929=CARTESIAN_POINT('Ctrl Pts',(0.0996297614469436,-0.120358971129495,
0.92465306908851));
#13930=CARTESIAN_POINT('Ctrl Pts',(0.0878048483710721,-0.129238546997106,
0.923486058390957));
#13931=CARTESIAN_POINT('Ctrl Pts',(0.0726341946255662,-0.137574773123402,
0.922183814643931));
#13932=CARTESIAN_POINT('Ctrl Pts',(0.0703274574803643,-0.138768135060366,
0.921990819221544));
#13933=CARTESIAN_POINT('Ctrl Pts',(0.0675064796765401,-0.140139105186311,
0.921761694337139));
#13934=CARTESIAN_POINT('Ctrl Pts',(0.0670199806256607,-0.140372418305302,
0.921722423576472));
#13935=CARTESIAN_POINT('Ctrl Pts',(0.0662604721912255,-0.140731811395884,
0.921661504645653));
#13936=CARTESIAN_POINT('Ctrl Pts',(0.0659883010491051,-0.140859635959385,
0.921639751720815));
#13937=CARTESIAN_POINT('Ctrl Pts',(0.065482090202286,-0.141095587549365,
0.921599439498538));
#13938=CARTESIAN_POINT('Ctrl Pts',(0.0652481546746922,-0.141203920896554,
0.921580867965983));
#13939=CARTESIAN_POINT('Ctrl Pts',(0.0647178797071554,-0.141447887063497,
0.921538900945333));
#13940=CARTESIAN_POINT('Ctrl Pts',(0.0644213832595874,-0.141583170231193,
0.92151552708186));
#13941=CARTESIAN_POINT('Ctrl Pts',(0.0635233883146044,-0.141989495716967,
0.921445004592581));
#13942=CARTESIAN_POINT('Ctrl Pts',(0.0629205779461682,-0.142257648895638,
0.921398028733891));
#13943=CARTESIAN_POINT('Ctrl Pts',(0.05827477706551,-0.144288971096523,
0.921038647351752));
#13944=CARTESIAN_POINT('Ctrl Pts',(0.054159676708548,-0.145883499154976,
0.920735711694544));
#13945=CARTESIAN_POINT('Ctrl Pts',(0.035994210136798,-0.152047367186302,
0.919441048389864));
#13946=CARTESIAN_POINT('Ctrl Pts',(0.0214018054862157,-0.154777248216127,
0.918501843308454));
#13947=CARTESIAN_POINT('Ctrl Pts',(0.00270480659069758,-0.155576416194499,
0.917227233169775));
#13948=CARTESIAN_POINT('Ctrl Pts',(-0.00123766647162131,-0.155594989931657,
0.916955061156382));
#13949=CARTESIAN_POINT('Ctrl Pts',(-0.00608967229243966,-0.155433437599074,
0.916613974435584));
#13950=CARTESIAN_POINT('Ctrl Pts',(-0.00700271842718297,-0.155394979016254,
0.91654952421732));
#13951=CARTESIAN_POINT('Ctrl Pts',(-0.00844280089516923,-0.155321603564634,
0.916447430610745));
#13952=CARTESIAN_POINT('Ctrl Pts',(-0.00897009996397641,-0.155292043308623,
0.916409954795012));
#13953=CARTESIAN_POINT('Ctrl Pts',(-0.00995682681477347,-0.155231685287383,
0.916339647433335));
#13954=CARTESIAN_POINT('Ctrl Pts',(-0.0104162895345085,-0.155201531633367,
0.916306836397572));
#13955=CARTESIAN_POINT('Ctrl Pts',(-0.011442179105327,-0.155129628433983,
0.91623340959511));
#13956=CARTESIAN_POINT('Ctrl Pts',(-0.0120085223198687,-0.155086815869748,
0.916192760976546));
#13957=CARTESIAN_POINT('Ctrl Pts',(-0.013439009589307,-0.154970796024108,
0.916089796497695));
#13958=CARTESIAN_POINT('Ctrl Pts',(-0.0143027896319657,-0.154893462583821,
0.916027352325525));
#13959=CARTESIAN_POINT('Ctrl Pts',(-0.0191470381299152,-0.154418895567225,
0.915675589544445));
#13960=CARTESIAN_POINT('Ctrl Pts',(-0.02311131681086,-0.153875488563329,
0.9153817349092));
#13961=CARTESIAN_POINT('Ctrl Pts',(-0.0289415957922071,-0.152845924076965,
0.914940168790301));
#13962=CARTESIAN_POINT('Ctrl Pts',(-0.0308268360618294,-0.152476877315448,
0.914795924471245));
#13963=CARTESIAN_POINT('Ctrl Pts',(-0.0470858212228406,-0.148980234222072,
0.913539408146966));
#13964=CARTESIAN_POINT('Ctrl Pts',(-0.0609533191626043,-0.143863823529639,
0.912372934983359));
#13965=CARTESIAN_POINT('Ctrl Pts',(-0.0761868591312057,-0.135639773197008,
0.911070468307069));
#13966=CARTESIAN_POINT('Ctrl Pts',(-0.0784473977661218,-0.134345053999845,
0.910876872969576));
#13967=CARTESIAN_POINT('Ctrl Pts',(-0.0811362380198341,-0.132713997002593,
0.910647132148336));
#13968=CARTESIAN_POINT('Ctrl Pts',(-0.0815964977205298,-0.132431513256563,
0.910607826009885));
#13969=CARTESIAN_POINT('Ctrl Pts',(-0.0823108237584191,-0.131987958803547,
0.910546864238203));
#13970=CARTESIAN_POINT('Ctrl Pts',(-0.0825659036352816,-0.131828542197799,
0.910525103616403));
#13971=CARTESIAN_POINT('Ctrl Pts',(-0.0830387372779375,-0.13153112585634,
0.910484784413295));
#13972=CARTESIAN_POINT('Ctrl Pts',(-0.0832566082599744,-0.131393326088713,
0.910466213559127));
#13973=CARTESIAN_POINT('Ctrl Pts',(-0.0837490165790518,-0.131080169507045,
0.910424257331071));
#13974=CARTESIAN_POINT('Ctrl Pts',(-0.0840233457276077,-0.130904491878477,
0.910400893534863));
#13975=CARTESIAN_POINT('Ctrl Pts',(-0.0848509908067295,-0.130370802645779,
0.910330431426925));
#13976=CARTESIAN_POINT('Ctrl Pts',(-0.0854025950839007,-0.130010128904104,
0.910283505447237));
#13977=CARTESIAN_POINT('Ctrl Pts',(-0.0896104064106475,-0.127220459128954,
0.909925672045913));
#13978=CARTESIAN_POINT('Ctrl Pts',(-0.0931650377193367,-0.124640903690957,
0.909624142582147));
#13979=CARTESIAN_POINT('Ctrl Pts',(-0.108155378818288,-0.112762384688307,
0.908333062392606));
#13980=CARTESIAN_POINT('Ctrl Pts',(-0.11834572893592,-0.102016072679374,
0.907396058604052));
#13981=CARTESIAN_POINT('Ctrl Pts',(-0.129182080549085,-0.0867394478478589,
0.906120907876402));
#13982=CARTESIAN_POINT('Ctrl Pts',(-0.131365529719357,-0.083395651189083,
0.905845294811318));
#13983=CARTESIAN_POINT('Ctrl Pts',(-0.133889486022727,-0.0791849084518531,
0.905500394190824));
#13984=CARTESIAN_POINT('Ctrl Pts',(-0.134354182049451,-0.0783938638885485,
0.90543569390499));
#13985=CARTESIAN_POINT('Ctrl Pts',(-0.135075704019467,-0.0771403684027894,
0.905333293424861));
#13986=CARTESIAN_POINT('Ctrl Pts',(-0.135337220731513,-0.0766806294038661,
0.90529576252288));
#13987=CARTESIAN_POINT('Ctrl Pts',(-0.135821971898118,-0.0758182458312662,
0.905225405541033));
#13988=CARTESIAN_POINT('Ctrl Pts',(-0.136045774026821,-0.0754159254554385,
0.905192600241969));
#13989=CARTESIAN_POINT('Ctrl Pts',(-0.136541167955571,-0.0745159937917177,
0.905119255675079));
#13990=CARTESIAN_POINT('Ctrl Pts',(-0.136811830904436,-0.0740178815306377,
0.905078683896796));
#13991=CARTESIAN_POINT('Ctrl Pts',(-0.137488031273642,-0.0727570610716043,
0.904976043704369));
#13992=CARTESIAN_POINT('Ctrl Pts',(-0.13788994484764,-0.0719924421952539,
0.904913848388818));
#13993=CARTESIAN_POINT('Ctrl Pts',(-0.140094706927866,-0.0677118025913985,
0.904565890159978));
#13994=CARTESIAN_POINT('Ctrl Pts',(-0.14176928475754,-0.0641317376980251,
0.904275705197761));
#13995=CARTESIAN_POINT('Ctrl Pts',(-0.144252364957401,-0.0582493262404351,
0.903799684121174));
#13996=CARTESIAN_POINT('Ctrl Pts',(-0.145146257010626,-0.0559847461395491,
0.903616622534871));
#13997=CARTESIAN_POINT('Ctrl Pts',(-0.151003890944027,-0.0400604906779335,
0.902331084345073));
#13998=CARTESIAN_POINT('Ctrl Pts',(-0.154084384812384,-0.0257868058292971,
0.901178461611881));
#13999=CARTESIAN_POINT('Ctrl Pts',(-0.155310168662362,-0.008948893428367,
0.899911655934367));
#14000=CARTESIAN_POINT('Ctrl Pts',(-0.155427707712362,-0.00660003721258554,
0.899737223210819));
#14001=CARTESIAN_POINT('Ctrl Pts',(-0.155506255650117,-0.00372575001372523,
0.899527253607195));
#14002=CARTESIAN_POINT('Ctrl Pts',(-0.155517918253579,-0.00320216845602306,
0.899489146753876));
#14003=CARTESIAN_POINT('Ctrl Pts',(-0.155532054575551,-0.00238135235045557,
0.899429638536462));
#14004=CARTESIAN_POINT('Ctrl Pts',(-0.155536320914119,-0.00208415931666893,
0.899408139988824));
#14005=CARTESIAN_POINT('Ctrl Pts',(-0.155542701881444,-0.00152874781286528,
0.899368053463317));
#14006=CARTESIAN_POINT('Ctrl Pts',(-0.155545025346779,-0.00127053923554435,
0.899349454507506));
#14007=CARTESIAN_POINT('Ctrl Pts',(-0.155548858987973,-0.000681486019007851,
0.899307107999714));
#14008=CARTESIAN_POINT('Ctrl Pts',(-0.155549956642077,-0.000350642004559851,
0.899283383702997));
#14009=CARTESIAN_POINT('Ctrl Pts',(-0.155550085855824,0.00066483591721158,
0.899210741903766));
#14010=CARTESIAN_POINT('Ctrl Pts',(-0.155545653043982,0.00134947466596592,
0.899162012788569));
#14011=CARTESIAN_POINT('Ctrl Pts',(-0.155524923765982,0.00293454784667604,
0.899049718708714));
#14012=CARTESIAN_POINT('Ctrl Pts',(-0.155505327669386,0.00383492449214596,
0.898986322870997));
#14013=CARTESIAN_POINT('Ctrl Pts',(-0.155191940176796,0.0141250482928698,
0.898265738327592));
#14014=CARTESIAN_POINT('Ctrl Pts',(-0.154055860259594,0.0234712885827232,
0.897648125621407));
#14015=CARTESIAN_POINT('Ctrl Pts',(-0.149678020877209,0.0438575256198832,
0.896275750927973));
#14016=CARTESIAN_POINT('Ctrl Pts',(-0.1460441175715,0.0547545526085629,
0.895522902063312));
#14017=CARTESIAN_POINT('Ctrl Pts',(-0.14051488865648,0.066741497240731,
0.894605550974665));
#14018=CARTESIAN_POINT('Ctrl Pts',(-0.13975561378378,0.0683171235622771,
0.894483158627786));
#14019=CARTESIAN_POINT('Ctrl Pts',(-0.138653280561385,0.0705093412341997,
0.894310148075968));
#14020=CARTESIAN_POINT('Ctrl Pts',(-0.138332328586955,0.0711369541796008,
0.894260299051709));
#14021=CARTESIAN_POINT('Ctrl Pts',(-0.137806804231475,0.07214759696694,
0.894179502113146));
#14022=CARTESIAN_POINT('Ctrl Pts',(-0.137604871688499,0.0725319951553056,
0.894148647228026));
#14023=CARTESIAN_POINT('Ctrl Pts',(-0.137181139545749,0.0733304718904287,
0.894084294067337));
#14024=CARTESIAN_POINT('Ctrl Pts',(-0.136959068744773,0.0737444006986513,
0.894050786450422));
#14025=CARTESIAN_POINT('Ctrl Pts',(-0.13643058577915,0.0747188452038213,
0.893971553365648));
#14026=CARTESIAN_POINT('Ctrl Pts',(-0.136122590990758,0.0752784880563611,
0.893925771983588));
#14027=CARTESIAN_POINT('Ctrl Pts',(-0.135093488069912,0.0771214554592928,
0.893774081035787));
#14028=CARTESIAN_POINT('Ctrl Pts',(-0.134357629866733,0.0783964057253749,
0.893667645576543));
#14029=CARTESIAN_POINT('Ctrl Pts',(-0.130391362333879,0.0850484761478511,
0.89310419930309));
#14030=CARTESIAN_POINT('Ctrl Pts',(-0.126856409538407,0.0902362580492424,
0.892636177407088));
#14031=CARTESIAN_POINT('Ctrl Pts',(-0.117609748200653,0.102185401155856,
0.891486857489979));
#14032=CARTESIAN_POINT('Ctrl Pts',(-0.111615500045129,0.108700817805921,
0.890798062324915));
#14033=CARTESIAN_POINT('Ctrl Pts',(-0.0999139986189095,0.119425730706921,
0.889570868028963));
#14034=CARTESIAN_POINT('Ctrl Pts',(-0.0944094498375184,0.123823243297438,
0.889032161706746));
#14035=CARTESIAN_POINT('Ctrl Pts',(-0.0880468611393628,0.128234348516339,
0.888464555949552));
#14036=CARTESIAN_POINT('Ctrl Pts',(-0.0874657018089413,0.128631446207753,
0.88841319069226));
#14037=CARTESIAN_POINT('Ctrl Pts',(-0.0866043173201996,0.129211480423492,
0.888337785972354));
#14038=CARTESIAN_POINT('Ctrl Pts',(-0.086326176412109,0.129397471859048,
0.888313548788249));
#14039=CARTESIAN_POINT('Ctrl Pts',(-0.0858320072469462,0.12972561776396,
0.888270686291535));
#14040=CARTESIAN_POINT('Ctrl Pts',(-0.0856162228560454,0.129868132196046,
0.888252037078596));
#14041=CARTESIAN_POINT('Ctrl Pts',(-0.0851536755377225,0.130171966852737,
0.888212205495706));
#14042=CARTESIAN_POINT('Ctrl Pts',(-0.0849068096903753,0.130333123510633,
0.888191034051918));
#14043=CARTESIAN_POINT('Ctrl Pts',(-0.0842293227602283,0.130772652371244,
0.888133165738373));
#14044=CARTESIAN_POINT('Ctrl Pts',(-0.0837977757505891,0.131049602135839,
0.888096562143742));
#14045=CARTESIAN_POINT('Ctrl Pts',(-0.0815096338915462,0.132502116651127,
0.88790379493374));
#14046=CARTESIAN_POINT('Ctrl Pts',(-0.0796295319257737,0.133640451638179,
0.887749946698035));
#14047=CARTESIAN_POINT('Ctrl Pts',(-0.0731663819296115,0.137368807356439,
0.887234032347461));
#14048=CARTESIAN_POINT('Ctrl Pts',(-0.0684810578985275,0.139763159764089,
0.886881593895257));
#14049=CARTESIAN_POINT('Ctrl Pts',(-0.0636885883104107,0.141913939481036,
0.886533246392299));
#14050=CARTESIAN_POINT('',(-0.155549945051201,-0.000130746198511629,0.885519163677599));
#14051=CARTESIAN_POINT('Ctrl Pts',(-0.0636886258347646,0.141913922640731,
0.87264646002013));
#14052=CARTESIAN_POINT('Ctrl Pts',(-0.0639839808243548,0.14178137219698,
0.872669783758718));
#14053=CARTESIAN_POINT('Ctrl Pts',(-0.0642789205766795,0.141647900346939,
0.87269313914274));
#14054=CARTESIAN_POINT('Ctrl Pts',(-0.0656103611131948,0.141040356252537,
0.872798865345358));
#14055=CARTESIAN_POINT('Ctrl Pts',(-0.0666420232472574,0.140555832985705,
0.872881593105514));
#14056=CARTESIAN_POINT('Ctrl Pts',(-0.0698040541603743,0.139028137482075,
0.873137691865879));
#14057=CARTESIAN_POINT('Ctrl Pts',(-0.0719158695679871,0.137947582673369,
0.873312326119224));
#14058=CARTESIAN_POINT('Ctrl Pts',(-0.0800256953822378,0.133561183197557,
0.873997314592906));
#14059=CARTESIAN_POINT('Ctrl Pts',(-0.0858268567636554,0.129909317770408,
0.874518923921789));
#14060=CARTESIAN_POINT('Ctrl Pts',(-0.101196557961316,0.118754146378466,
0.875984139080918));
#14061=CARTESIAN_POINT('Ctrl Pts',(-0.110156432495108,0.110493846410477,
0.876939696515992));
#14062=CARTESIAN_POINT('Ctrl Pts',(-0.118736569029378,0.100491270105243,
0.877911926478186));
#14063=CARTESIAN_POINT('Ctrl Pts',(-0.119400897564014,0.0997010230989174,
0.877987607296685));
#14064=CARTESIAN_POINT('Ctrl Pts',(-0.120313412303396,0.098593344214222,
0.878092062446794));
#14065=CARTESIAN_POINT('Ctrl Pts',(-0.120568287415644,0.098281497663267,
0.878121293353105));
#14066=CARTESIAN_POINT('Ctrl Pts',(-0.120975316662894,0.0977795201094749,
0.878168059052301));
#14067=CARTESIAN_POINT('Ctrl Pts',(-0.121128238137576,0.0975900185595753,
0.87818564837152));
#14068=CARTESIAN_POINT('Ctrl Pts',(-0.121446543938576,0.0971936705813331,
0.878222299705275));
#14069=CARTESIAN_POINT('Ctrl Pts',(-0.121611845556675,0.0969867602178439,
0.878241355464605));
#14070=CARTESIAN_POINT('Ctrl Pts',(-0.122009978867162,0.0964857929167504,
0.878287307996225));
#14071=CARTESIAN_POINT('Ctrl Pts',(-0.122242279153235,0.0961913113192382,
0.878314166957051));
#14072=CARTESIAN_POINT('Ctrl Pts',(-0.123048706878283,0.0951613825374254,
0.878407583331032));
#14073=CARTESIAN_POINT('Ctrl Pts',(-0.123617296309055,0.0944215926465238,
0.878473761932663));
#14074=CARTESIAN_POINT('Ctrl Pts',(-0.126620195467169,0.0904409056087231,
0.878825239610829));
#14075=CARTESIAN_POINT('Ctrl Pts',(-0.128934029129705,0.0871105864426254,
0.879103107677789));
#14076=CARTESIAN_POINT('Ctrl Pts',(-0.136585451272144,0.075123745866676,
0.880062527809272));
#14077=CARTESIAN_POINT('Ctrl Pts',(-0.1412025418034,0.0660380972084901,
0.880720022333444));
#14078=CARTESIAN_POINT('Ctrl Pts',(-0.145990188285565,0.0537740880269545,
0.88159360466118));
#14079=CARTESIAN_POINT('Ctrl Pts',(-0.146999267897609,0.0509509727517754,
0.88179367257103));
#14080=CARTESIAN_POINT('Ctrl Pts',(-0.148330356843338,0.0468574069364056,
0.882083811666845));
#14081=CARTESIAN_POINT('Ctrl Pts',(-0.148718894265833,0.0456092282163969,
0.882172281006354));
#14082=CARTESIAN_POINT('Ctrl Pts',(-0.15025511847033,0.040445631031379,
0.88253858622068));
#14083=CARTESIAN_POINT('Ctrl Pts',(-0.151264177651802,0.0364910025913579,
0.882819927379395));
#14084=CARTESIAN_POINT('Ctrl Pts',(-0.152298897269656,0.0316482199489744,
0.88316756658446));
#14085=CARTESIAN_POINT('Ctrl Pts',(-0.152474036970631,0.0307933747767094,
0.883229045223125));
#14086=CARTESIAN_POINT('Ctrl Pts',(-0.152751582879789,0.0293782366564353,
0.883331027541352));
#14087=CARTESIAN_POINT('Ctrl Pts',(-0.152858122392891,0.0288187658339247,
0.883371399611584));
#14088=CARTESIAN_POINT('Ctrl Pts',(-0.153045231729836,0.0278059622976841,
0.883444587415596));
#14089=CARTESIAN_POINT('Ctrl Pts',(-0.153126866151747,0.0273528307260728,
0.883477368954808));
#14090=CARTESIAN_POINT('Ctrl Pts',(-0.153281414580556,0.0264725929609248,
0.883541124167507));
#14091=CARTESIAN_POINT('Ctrl Pts',(-0.153354558281646,0.0260455309241754,
0.88357209022907));
#14092=CARTESIAN_POINT('Ctrl Pts',(-0.153510990332421,0.0251086674382806,
0.883640099179537));
#14093=CARTESIAN_POINT('Ctrl Pts',(-0.153593525114088,0.0245987472131566,
0.883677165569534));
#14094=CARTESIAN_POINT('Ctrl Pts',(-0.153790103046173,0.0233446670990093,
0.883768453066955));
#14095=CARTESIAN_POINT('Ctrl Pts',(-0.153901285466897,0.0226000790149197,
0.883822763757642));
#14096=CARTESIAN_POINT('Ctrl Pts',(-0.154331458681031,0.0195687112015811,
0.884044341677169));
#14097=CARTESIAN_POINT('Ctrl Pts',(-0.154604904771191,0.017275877942892,
0.88421302417564));
#14098=CARTESIAN_POINT('Ctrl Pts',(-0.155313044927032,0.00995581101386103,
0.884755291129623));
#14099=CARTESIAN_POINT('Ctrl Pts',(-0.155554185082819,0.00491365809576992,
0.88513451871578));
#14100=CARTESIAN_POINT('Ctrl Pts',(-0.155549945051201,-0.000130746198511629,
0.885519163677599));
#14101=CARTESIAN_POINT('Ctrl Pts',(-0.155549945196739,-0.000130572935765169,
0.885519150466002));
#14102=CARTESIAN_POINT('Ctrl Pts',(-0.155538152527638,-0.0141790357481969,
0.886590370869597));
#14103=CARTESIAN_POINT('Ctrl Pts',(-0.153623404595727,-0.02816081303895,
0.88770398506701));
#14104=CARTESIAN_POINT('Ctrl Pts',(-0.149541044889883,-0.0428330689818887,
0.888839113490999));
#14105=CARTESIAN_POINT('Ctrl Pts',(-0.14921167976298,-0.0439667003155691,
0.888926541329305));
#14106=CARTESIAN_POINT('Ctrl Pts',(-0.148624005230768,-0.0459066900059983,
0.889075557530823));
#14107=CARTESIAN_POINT('Ctrl Pts',(-0.148371964239863,-0.0467148737807904,
0.88913745624345));
#14108=CARTESIAN_POINT('Ctrl Pts',(-0.148003154703567,-0.0478643787865776,
0.889225200174473));
#14109=CARTESIAN_POINT('Ctrl Pts',(-0.147891783724052,-0.0482073943796404,
0.889251345374466));
#14110=CARTESIAN_POINT('Ctrl Pts',(-0.147697373281028,-0.0487991515199586,
0.889296380933229));
#14111=CARTESIAN_POINT('Ctrl Pts',(-0.147614896387343,-0.0490480747041561,
0.889315303948344));
#14112=CARTESIAN_POINT('Ctrl Pts',(-0.147453455386157,-0.0495312233690396,
0.889351990095693));
#14113=CARTESIAN_POINT('Ctrl Pts',(-0.147374562564733,-0.0497654690015451,
0.889369757414952));
#14114=CARTESIAN_POINT('Ctrl Pts',(-0.147159594330047,-0.0503987503815633,
0.889417741607176));
#14115=CARTESIAN_POINT('Ctrl Pts',(-0.147022453058591,-0.0507974266202238,
0.889447896192181));
#14116=CARTESIAN_POINT('Ctrl Pts',(-0.146503960123012,-0.052285019992407,
0.889560230750206));
#14117=CARTESIAN_POINT('Ctrl Pts',(-0.146112105248525,-0.0533702778440294,
0.889641817552013));
#14118=CARTESIAN_POINT('Ctrl Pts',(-0.141836509487951,-0.0648115369460556,
0.890499077902331));
#14119=CARTESIAN_POINT('Ctrl Pts',(-0.136870190233698,-0.0747312810406909,
0.891218827987436));
#14120=CARTESIAN_POINT('Ctrl Pts',(-0.128452526781656,-0.0878415956347108,
0.892244842947308));
#14121=CARTESIAN_POINT('Ctrl Pts',(-0.125848290294038,-0.0915336157035162,
0.892542982466153));
#14122=CARTESIAN_POINT('Ctrl Pts',(-0.120416653634604,-0.0985632261996008,
0.893137154663758));
#14123=CARTESIAN_POINT('Ctrl Pts',(-0.117601898405325,-0.10190519367907,
0.893432662166524));
#14124=CARTESIAN_POINT('Ctrl Pts',(-0.112862942599354,-0.107073593066328,
0.893915666907023));
#14125=CARTESIAN_POINT('Ctrl Pts',(-0.111026109819991,-0.108977060128182,
0.894099700781088));
#14126=CARTESIAN_POINT('Ctrl Pts',(-0.108583291972478,-0.111382608533483,
0.894340998330812));
#14127=CARTESIAN_POINT('Ctrl Pts',(-0.108020707526251,-0.111928296174413,
0.894396340733983));
#14128=CARTESIAN_POINT('Ctrl Pts',(-0.107139837867773,-0.112769882812272,
0.894482654388813));
#14129=CARTESIAN_POINT('Ctrl Pts',(-0.106824389843949,-0.113068744820656,
0.894513497571105));
#14130=CARTESIAN_POINT('Ctrl Pts',(-0.106206245705339,-0.113649491664343,
0.89457381038687));
#14131=CARTESIAN_POINT('Ctrl Pts',(-0.105903669113949,-0.113931498912837,
0.894603274432736));
#14132=CARTESIAN_POINT('Ctrl Pts',(-0.105203102553521,-0.114579238383775,
0.894671361523234));
#14133=CARTESIAN_POINT('Ctrl Pts',(-0.104804325864619,-0.114944107817372,
0.894710020661181));
#14134=CARTESIAN_POINT('Ctrl Pts',(-0.103703250385203,-0.115941067435139,
0.894816503521015));
#14135=CARTESIAN_POINT('Ctrl Pts',(-0.102997091527054,-0.116568839413521,
0.894884506956097));
#14136=CARTESIAN_POINT('Ctrl Pts',(-0.0993377146315612,-0.119762797563676,
0.895235492625419));
#14137=CARTESIAN_POINT('Ctrl Pts',(-0.0962944153694092,-0.122223114463218,
0.895522761485409));
#14138=CARTESIAN_POINT('Ctrl Pts',(-0.0915594053831049,-0.125764390743432,
0.895963432868851));
#14139=CARTESIAN_POINT('Ctrl Pts',(-0.0899340338873895,-0.126931775506413,
0.896113632875983));
#14140=CARTESIAN_POINT('Ctrl Pts',(-0.0762350741093716,-0.136375513611164,
0.897370590085317));
#14141=CARTESIAN_POINT('Ctrl Pts',(-0.0630731348671237,-0.142939738315851,
0.898530964540429));
#14142=CARTESIAN_POINT('Ctrl Pts',(-0.0466421964116437,-0.148416694220697,
0.89983512805926));
#14143=CARTESIAN_POINT('Ctrl Pts',(-0.0440735887868415,-0.149199633862116,
0.900034814035675));
#14144=CARTESIAN_POINT('Ctrl Pts',(-0.0409587490884475,-0.150061595442215,
0.900270951339052));
#14145=CARTESIAN_POINT('Ctrl Pts',(-0.0404309230539648,-0.150204667166823,
0.900310760132925));
#14146=CARTESIAN_POINT('Ctrl Pts',(-0.039610233016664,-0.150422482624979,
0.900372326036213));
#14147=CARTESIAN_POINT('Ctrl Pts',(-0.0393178944033794,-0.150499159541276,
0.900394191499956));
#14148=CARTESIAN_POINT('Ctrl Pts',(-0.0387759987737597,-0.150639605553741,
0.900434599984482));
#14149=CARTESIAN_POINT('Ctrl Pts',(-0.0385265091388475,-0.150703606253555,
0.900453155817519));
#14150=CARTESIAN_POINT('Ctrl Pts',(-0.037963184115895,-0.150846623705276,
0.900494945184646));
#14151=CARTESIAN_POINT('Ctrl Pts',(-0.0376492611025511,-0.150925280768664,
0.900518157824987));
#14152=CARTESIAN_POINT('Ctrl Pts',(-0.0367252543927661,-0.151153739038354,
0.900586267489426));
#14153=CARTESIAN_POINT('Ctrl Pts',(-0.0361144960830717,-0.151300827308021,
0.900631012208815));
#14154=CARTESIAN_POINT('Ctrl Pts',(-0.0318048501361557,-0.152311131412774,
0.900944915754908));
#14155=CARTESIAN_POINT('Ctrl Pts',(-0.0280759420180833,-0.15304240194071,
0.901207072237295));
#14156=CARTESIAN_POINT('Ctrl Pts',(-0.0233044485662321,-0.153797821599284,
0.901534949012357));
#14157=CARTESIAN_POINT('Ctrl Pts',(-0.0222836737543572,-0.153949034486008,
0.901604654843597));
#14158=CARTESIAN_POINT('Ctrl Pts',(-0.00634423143215172,-0.156148369163235,
0.902687340657683));
#14159=CARTESIAN_POINT('Ctrl Pts',(0.00879251396618733,-0.156029781423452,
0.903645188548648));
#14160=CARTESIAN_POINT('Ctrl Pts',(0.0258633314586502,-0.153400732166274,
0.90482734189002));
#14161=CARTESIAN_POINT('Ctrl Pts',(0.0280422740574947,-0.153017406214281,
0.904979986524117));
#14162=CARTESIAN_POINT('Ctrl Pts',(0.0312755885443407,-0.152377213371051,
0.905209537944045));
#14163=CARTESIAN_POINT('Ctrl Pts',(0.0323367082795656,-0.152155561148261,
0.905285364420942));
#14164=CARTESIAN_POINT('Ctrl Pts',(0.0342636527589544,-0.151731983727192,
0.905424008634687));
#14165=CARTESIAN_POINT('Ctrl Pts',(0.0351302350894301,-0.151533690346781,
0.905486710100899));
#14166=CARTESIAN_POINT('Ctrl Pts',(0.0365017470432344,-0.151207460880876,
0.905586523910935));
#14167=CARTESIAN_POINT('Ctrl Pts',(0.0370078256185217,-0.151084395601389,
0.905623479907294));
#14168=CARTESIAN_POINT('Ctrl Pts',(0.0375143946125529,-0.150958513168994,
0.905660599930424));
#14169=CARTESIAN_POINT('Ctrl Pts',(0.0375155181777817,-0.150958233949633,
0.905660682262917));
#14170=CARTESIAN_POINT('Ctrl Pts',(0.0375177715377327,-0.150957673936097,
0.905660847385655));
#14171=CARTESIAN_POINT('Ctrl Pts',(0.0375189013217255,-0.150957393144441,
0.905660930175122));
#14172=CARTESIAN_POINT('Ctrl Pts',(0.0375211671584859,-0.150956829976105,
0.905661096214708));
#14173=CARTESIAN_POINT('Ctrl Pts',(0.0375223032079665,-0.150956547600093,
0.905661179464594));
#14174=CARTESIAN_POINT('Ctrl Pts',(0.0375245816304175,-0.150955981248996,
0.90566134642905));
#14175=CARTESIAN_POINT('Ctrl Pts',(0.0375257239959067,-0.150955697275618,
0.90566143014308));
#14176=CARTESIAN_POINT('Ctrl Pts',(0.0375280151120727,-0.150955127713995,
0.905661598040365));
#14177=CARTESIAN_POINT('Ctrl Pts',(0.0375291638492502,-0.150954842128952,
0.90566168222264));
#14178=CARTESIAN_POINT('Ctrl Pts',(0.0375314677528195,-0.150954269332587,
0.905661851059665));
#14179=CARTESIAN_POINT('Ctrl Pts',(0.0375326229117475,-0.150953982122966,
0.905661935713875));
#14180=CARTESIAN_POINT('Ctrl Pts',(0.0375349397125162,-0.150953406063626,
0.90566210549873));
#14181=CARTESIAN_POINT('Ctrl Pts',(0.0375361013465343,-0.150953117215694,
0.905662190628808));
#14182=CARTESIAN_POINT('Ctrl Pts',(0.0375384311483642,-0.150952537866602,
0.90566236136915));
#14183=CARTESIAN_POINT('Ctrl Pts',(0.0375395993097859,-0.150952247366872,
0.905662446978952));
#14184=CARTESIAN_POINT('Ctrl Pts',(0.0375419422235694,-0.150951664699489,
0.905662618682953));
#14185=CARTESIAN_POINT('Ctrl Pts',(0.0375431169680617,-0.150951372533632,
0.905662704776582));
#14186=CARTESIAN_POINT('Ctrl Pts',(0.0375454730244149,-0.150950786539369,
0.905662877446533));
#14187=CARTESIAN_POINT('Ctrl Pts',(0.0375466543323981,-0.150950492711769,
0.905662964022576));
#14188=CARTESIAN_POINT('Ctrl Pts',(0.0379946072117565,-0.150839067478026,
0.905695793989544));
#14189=CARTESIAN_POINT('Ctrl Pts',(0.0384408785224315,-0.150725954317339,
0.905728600849246));
#14190=CARTESIAN_POINT('Ctrl Pts',(0.039437506318027,-0.15046863222028,
0.905802093732532));
#14191=CARTESIAN_POINT('Ctrl Pts',(0.0399875845606474,-0.150323382252826,
0.905842812959197));
#14192=CARTESIAN_POINT('Ctrl Pts',(0.041377450014223,-0.14994821515961,
0.905946097830702));
#14193=CARTESIAN_POINT('Ctrl Pts',(0.0422161169291542,-0.14971426122234,
0.906008793251438));
#14194=CARTESIAN_POINT('Ctrl Pts',(0.0469481021403496,-0.148351308466123,
0.906364689873562));
#14195=CARTESIAN_POINT('Ctrl Pts',(0.0507977291912003,-0.147077598833341,
0.906662553400032));
#14196=CARTESIAN_POINT('Ctrl Pts',(0.0563472049523658,-0.144997602950568,
0.907104757222454));
#14197=CARTESIAN_POINT('Ctrl Pts',(0.0580894069109226,-0.144308463630955,
0.907245471279747));
#14198=CARTESIAN_POINT('Ctrl Pts',(0.0734068482554405,-0.137927228729949,
0.908499274335655));
#14199=CARTESIAN_POINT('Ctrl Pts',(0.0861206404782316,-0.130367340786665,
0.909666635362832));
#14200=CARTESIAN_POINT('Ctrl Pts',(0.0995941270883413,-0.119513551085416,
0.910968053158101));
#14201=CARTESIAN_POINT('Ctrl Pts',(0.101565801392122,-0.117842560889508,
0.911160091223221));
#14202=CARTESIAN_POINT('Ctrl Pts',(0.103897190805273,-0.115764702664121,
0.911388223901601));
#14203=CARTESIAN_POINT('Ctrl Pts',(0.104297451607449,-0.115404221116141,
0.91142742919177));
#14204=CARTESIAN_POINT('Ctrl Pts',(0.104918035565521,-0.114839446944071,
0.911488264545976));
#14205=CARTESIAN_POINT('Ctrl Pts',(0.105139647727574,-0.114636587707616,
0.911509998950918));
#14206=CARTESIAN_POINT('Ctrl Pts',(0.105550281072221,-0.114258509937979,
0.911550287647352));
#14207=CARTESIAN_POINT('Ctrl Pts',(0.105739452623241,-0.11408346544723,
0.911568854110377));
#14208=CARTESIAN_POINT('Ctrl Pts',(0.106166916390006,-0.113685947403785,
0.911610823054837));
#14209=CARTESIAN_POINT('Ctrl Pts',(0.106404944387432,-0.113463194860919,
0.911634203857901));
#14210=CARTESIAN_POINT('Ctrl Pts',(0.107123146368127,-0.112786835803873,
0.911704790470792));
#14211=CARTESIAN_POINT('Ctrl Pts',(0.107601141438976,-0.112330909464413,
0.911751822997039));
#14212=CARTESIAN_POINT('Ctrl Pts',(0.11126914501455,-0.10878735788026,0.912113297600198));
#14213=CARTESIAN_POINT('Ctrl Pts',(0.114328926059272,-0.105567124513092,
0.912418143880914));
#14214=CARTESIAN_POINT('Ctrl Pts',(0.126976025685611,-0.0910608150511777,
0.913716712003752));
#14215=CARTESIAN_POINT('Ctrl Pts',(0.135062192365374,-0.0785699397450294,
0.914658043892356));
#14216=CARTESIAN_POINT('Ctrl Pts',(0.142887838763237,-0.061595167144369,
0.915931718983082));
#14217=CARTESIAN_POINT('Ctrl Pts',(0.144381634668728,-0.0580072261681909,
0.916200111106546));
#14218=CARTESIAN_POINT('Ctrl Pts',(0.14605740588081,-0.0535150836206767,
0.916536992617766));
#14219=CARTESIAN_POINT('Ctrl Pts',(0.146367860098708,-0.052660036601624,
0.91660115020794));
#14220=CARTESIAN_POINT('Ctrl Pts',(0.146846329847733,-0.0513053188852416,
0.916702877184828));
#14221=CARTESIAN_POINT('Ctrl Pts',(0.147019339300464,-0.0508074226356638,
0.916740280968632));
#14222=CARTESIAN_POINT('Ctrl Pts',(0.147338713021705,-0.0498730197670068,
0.916810511878994));
#14223=CARTESIAN_POINT('Ctrl Pts',(0.147485676886321,-0.0494367227937805,
0.916843318803807));
#14224=CARTESIAN_POINT('Ctrl Pts',(0.147809923926955,-0.0484598038430126,
0.916916812574511));
#14225=CARTESIAN_POINT('Ctrl Pts',(0.147986181431481,-0.0479188510841113,
0.916957532627149));
#14226=CARTESIAN_POINT('Ctrl Pts',(0.148424668123391,-0.046547594522173,
0.917060820988422));
#14227=CARTESIAN_POINT('Ctrl Pts',(0.148682897596839,-0.0457160427884443,
0.917123519088245));
#14228=CARTESIAN_POINT('Ctrl Pts',(0.150103940030121,-0.0410005686224286,
0.917479458000172));
#14229=CARTESIAN_POINT('Ctrl Pts',(0.151121433621259,-0.0370748713999017,
0.917777362433376));
#14230=CARTESIAN_POINT('Ctrl Pts',(0.152383102129157,-0.0312841929979406,
0.918219572617918));
#14231=CARTESIAN_POINT('Ctrl Pts',(0.152748730191014,-0.0294471641232828,
0.918360250509824));
#14232=CARTESIAN_POINT('Ctrl Pts',(0.155693402670874,-0.0131171781642028,
0.919614044045814));
#14233=CARTESIAN_POINT('Ctrl Pts',(0.156235868854734,0.00166485672163923,
0.920781434448465));
#14234=CARTESIAN_POINT('Ctrl Pts',(0.154422681920322,0.0188709335403455,
0.922082840303305));
#14235=CARTESIAN_POINT('Ctrl Pts',(0.15408794558242,0.0214332446269605,
0.922274845808125));
#14236=CARTESIAN_POINT('Ctrl Pts',(0.153606447379172,0.0245183999341052,
0.922502945035628));
#14237=CARTESIAN_POINT('Ctrl Pts',(0.153520625463669,0.0250501535346767,
0.922542148391032));
#14238=CARTESIAN_POINT('Ctrl Pts',(0.153382633387528,0.0258778000031592,
0.922602981402059));
#14239=CARTESIAN_POINT('Ctrl Pts',(0.153332366319068,0.0261739985685697,
0.922624715385827));
#14240=CARTESIAN_POINT('Ctrl Pts',(0.153237381674115,0.0267240301159189,
0.922665003701198));
#14241=CARTESIAN_POINT('Ctrl Pts',(0.153192891833672,0.0269778950522651,
0.922683570202268));
#14242=CARTESIAN_POINT('Ctrl Pts',(0.153090697794654,0.0275526228643031,
0.922725539741502));
#14243=CARTESIAN_POINT('Ctrl Pts',(0.153032615863719,0.0278734150248027,
0.922748921098714));
#14244=CARTESIAN_POINT('Ctrl Pts',(0.152853791936818,0.0288436675983817,
0.92281951103822));
#14245=CARTESIAN_POINT('Ctrl Pts',(0.152729918811505,0.0294925551867561,
0.922866546312915));
#14246=CARTESIAN_POINT('Ctrl Pts',(0.151741442733016,0.0344972031778821,
0.923228107995185));
#14247=CARTESIAN_POINT('Ctrl Pts',(0.150694703707889,0.0388154350206104,
0.923533033384837));
#14248=CARTESIAN_POINT('Ctrl Pts',(0.145363318004187,0.0573110100873105,
0.924831812301412));
#14249=CARTESIAN_POINT('Ctrl Pts',(0.139251900616261,0.0708801971536447,
0.925773276471871));
#14250=CARTESIAN_POINT('Ctrl Pts',(0.129232756085471,0.0866589332077304,
0.927046924325926));
#14251=CARTESIAN_POINT('Ctrl Pts',(0.127029785747986,0.0898571373224586,
0.927315115286679));
#14252=CARTESIAN_POINT('Ctrl Pts',(0.12416608844301,0.0936985169473646,
0.927651773656477));
#14253=CARTESIAN_POINT('Ctrl Pts',(0.123616153997182,0.0944228574316695,
0.927715916275253));
#14254=CARTESIAN_POINT('Ctrl Pts',(0.122737536594645,0.0955592873380829,
0.927817624876976));
#14255=CARTESIAN_POINT('Ctrl Pts',(0.122413049996471,0.0959746084337265,
0.927855025359208));
#14256=CARTESIAN_POINT('Ctrl Pts',(0.121801176163229,0.0967496147028431,
0.927925253323625));
#14257=CARTESIAN_POINT('Ctrl Pts',(0.121514289808375,0.0971096896498648,
0.927958060620348));
#14258=CARTESIAN_POINT('Ctrl Pts',(0.120869266403979,0.0979119334542896,
0.928031559454399));
#14259=CARTESIAN_POINT('Ctrl Pts',(0.12051029471596,0.0983534194899055,
0.928072284219391));
#14260=CARTESIAN_POINT('Ctrl Pts',(0.119595764393611,0.0994656431550907,
0.928175592491053));
#14261=CARTESIAN_POINT('Ctrl Pts',(0.119036986151855,0.100133695126451,
0.928238305876175));
#14262=CARTESIAN_POINT('Ctrl Pts',(0.115843451124629,0.103887244260346,
0.928594486152816));
#14263=CARTESIAN_POINT('Ctrl Pts',(0.113094612837865,0.106873137746962,
0.92889262406594));
#14264=CARTESIAN_POINT('Ctrl Pts',(0.10891292461344,0.111073286686013,0.9293348706252));
#14265=CARTESIAN_POINT('Ctrl Pts',(0.107569660273376,0.112374676230265,
0.929475342163363));
#14266=CARTESIAN_POINT('Ctrl Pts',(0.0954464200580246,0.123703416634404,
0.930729081834463));
#14267=CARTESIAN_POINT('Ctrl Pts',(0.0833187671933404,0.132175867318789,
0.931896640345904));
#14268=CARTESIAN_POINT('Ctrl Pts',(0.0678789658641286,0.139981820714347,
0.93319797798148));
#14269=CARTESIAN_POINT('Ctrl Pts',(0.0655467783845755,0.14108892975694,
0.933389797258561));
#14270=CARTESIAN_POINT('Ctrl Pts',(0.0626958992149843,0.14235630183139,
0.933617705153987));
#14271=CARTESIAN_POINT('Ctrl Pts',(0.0622027173212019,0.14257248833633,
0.933656897435981));
#14272=CARTESIAN_POINT('Ctrl Pts',(0.0614326658553099,0.142905284381127,
0.933717717035966));
#14273=CARTESIAN_POINT('Ctrl Pts',(0.061156570877564,0.143023657416573,
0.933739448609067));
#14274=CARTESIAN_POINT('Ctrl Pts',(0.0606429527111171,0.143242106994375,
0.933779734743845));
#14275=CARTESIAN_POINT('Ctrl Pts',(0.0604055260906377,0.14334239201737,
0.933798301463162));
#14276=CARTESIAN_POINT('Ctrl Pts',(0.05986717704097,0.143568206509304,0.933840274408923));
#14277=CARTESIAN_POINT('Ctrl Pts',(0.0595661090887147,0.143693380016156,
0.933863658939628));
#14278=CARTESIAN_POINT('Ctrl Pts',(0.0586536810408798,0.14406937518277,
0.933934267931659));
#14279=CARTESIAN_POINT('Ctrl Pts',(0.058041103329471,0.144317253061305,
0.933981318947773));
#14280=CARTESIAN_POINT('Ctrl Pts',(0.0532935766457031,0.146203208140537,
0.934343380401504));
#14281=CARTESIAN_POINT('Ctrl Pts',(0.0490911842966859,0.147667356909277,
0.93464875982257));
#14282=CARTESIAN_POINT('Ctrl Pts',(0.0306409878440384,0.153220561271546,
0.935948755156329));
#14283=CARTESIAN_POINT('Ctrl Pts',(0.0159131608208337,0.155442046342665,
0.936890984581909));
#14284=CARTESIAN_POINT('Ctrl Pts',(-0.00277245758209385,0.15557331520756,
0.938164478424675));
#14285=CARTESIAN_POINT('Ctrl Pts',(-0.00663700638285604,0.15545638864657,
0.938431509426429));
#14286=CARTESIAN_POINT('Ctrl Pts',(-0.0113990712733975,0.155134420799282,
0.938766880965891));
#14287=CARTESIAN_POINT('Ctrl Pts',(-0.0123046394880982,0.1550652221718,
0.938830937000372));
#14288=CARTESIAN_POINT('Ctrl Pts',(-0.0137344108026052,0.154943363710533,
0.93893253933082));
#14289=CARTESIAN_POINT('Ctrl Pts',(-0.0142590521131872,0.154895963208998,
0.938969920716547));
#14290=CARTESIAN_POINT('Ctrl Pts',(-0.0152417710738129,0.154802141134066,
0.939040131662229));
#14291=CARTESIAN_POINT('Ctrl Pts',(-0.0156999043182575,0.1547563487589,
0.939072941130983));
#14292=CARTESIAN_POINT('Ctrl Pts',(-0.0167241312670081,0.154649378067233,
0.93914646935182));
#14293=CARTESIAN_POINT('Ctrl Pts',(-0.017290103427844,0.154587124336835,
0.939187221452907));
#14294=CARTESIAN_POINT('Ctrl Pts',(-0.018722103348753,0.154421650034999,
0.939290645241007));
#14295=CARTESIAN_POINT('Ctrl Pts',(-0.0195876184459121,0.154314251770064,
0.939353447313268));
#14296=CARTESIAN_POINT('Ctrl Pts',(-0.0244901941423557,0.153664001605169,
0.93971088110266));
#14297=CARTESIAN_POINT('Ctrl Pts',(-0.0285052403014864,0.152970064208931,
0.940010221954393));
#14298=CARTESIAN_POINT('Ctrl Pts',(-0.0432248145238853,0.149826409029404,
0.941133473445246));
#14299=CARTESIAN_POINT('Ctrl Pts',(-0.0536831418144325,0.146404218878681,
0.941985602790749));
#14300=CARTESIAN_POINT('Ctrl Pts',(-0.0636886279045124,0.141913921711862,
0.942835077379979));
#14301=CARTESIAN_POINT('Origin',(0.,0.,-0.129405622560373));
#14302=CARTESIAN_POINT('',(-0.0636886257384703,0.141913922683946,1.02674653231234));
#14303=CARTESIAN_POINT('',(-0.0636886260608369,0.141913922539273,1.01289638536134));
#14304=CARTESIAN_POINT('',(-0.0636886258329924,0.141913922641526,-0.129405622560373));
#14305=CARTESIAN_POINT('',(-0.155549936890276,0.00014011934593126,0.969453892031266));
#14306=CARTESIAN_POINT('Ctrl Pts',(-0.0636886257384703,0.141913922683946,
1.02674653231234));
#14307=CARTESIAN_POINT('Ctrl Pts',(-0.0630352306679285,0.142207155605143,
1.02669405911617));
#14308=CARTESIAN_POINT('Ctrl Pts',(-0.0623798065897889,0.142495877757158,
1.0266414348019));
#14309=CARTESIAN_POINT('Ctrl Pts',(-0.0576415668584197,0.144544171545589,
1.02626107071648));
#14310=CARTESIAN_POINT('Ctrl Pts',(-0.0534873655959961,0.146132346438471,
1.02592788080371));
#14311=CARTESIAN_POINT('Ctrl Pts',(-0.0376529200786634,0.151420271184699,
1.02465969010187));
#14312=CARTESIAN_POINT('Ctrl Pts',(-0.0256183551010184,0.153913939049909,
1.02369533159991));
#14313=CARTESIAN_POINT('Ctrl Pts',(-0.0126319359965695,0.155038243789787,
1.02270248284392));
#14314=CARTESIAN_POINT('Ctrl Pts',(-0.0118467337456412,0.155100218522508,
1.02264265376301));
#14315=CARTESIAN_POINT('Ctrl Pts',(-0.00783342961095387,0.155386326824878,
1.02233798649972));
#14316=CARTESIAN_POINT('Ctrl Pts',(-0.00459907048430397,0.155515676572398,
1.02209616941057));
#14317=CARTESIAN_POINT('Ctrl Pts',(-0.000814431946987157,0.155548834359067,
1.02181924660198));
#14318=CARTESIAN_POINT('Ctrl Pts',(-0.000266086682487207,0.155550738962588,
1.0217792724826));
#14319=CARTESIAN_POINT('Ctrl Pts',(0.000614623215861104,0.155549140783889,
1.0217153194843));
#14320=CARTESIAN_POINT('Ctrl Pts',(0.000946979797115376,0.155547472480817,
1.02169124257916));
#14321=CARTESIAN_POINT('Ctrl Pts',(0.00153830136032678,0.155542608947653,
1.02164851034128));
#14322=CARTESIAN_POINT('Ctrl Pts',(0.00179726617478012,0.155539832222134,
1.02162983199114));
#14323=CARTESIAN_POINT('Ctrl Pts',(0.00234898534973309,0.155532538361492,
1.02159011544398));
#14324=CARTESIAN_POINT('Ctrl Pts',(0.00264173362726414,0.155527841458206,
1.02156908741561));
#14325=CARTESIAN_POINT('Ctrl Pts',(0.00343798422600656,0.155512817417418,
1.02151201381604));
#14326=CARTESIAN_POINT('Ctrl Pts',(0.0039414584958467,0.155500871510094,
1.02147605728297));
#14327=CARTESIAN_POINT('Ctrl Pts',(0.00652129801348688,0.155427121916947,
1.0212924459474));
#14328=CARTESIAN_POINT('Ctrl Pts',(0.00859646117933128,0.155326171485528,
1.02114685331092));
#14329=CARTESIAN_POINT('Ctrl Pts',(0.0146989950671047,0.154906613003737,
1.02072323300142));
#14330=CARTESIAN_POINT('Ctrl Pts',(0.0187169036301496,0.154472658424671,
1.02045012918477));
#14331=CARTESIAN_POINT('Ctrl Pts',(0.0330399681741005,0.152358519906227,
1.01948306500855));
#14332=CARTESIAN_POINT('Ctrl Pts',(0.0431866612744261,0.149798802724692,
1.01880841875851));
#14333=CARTESIAN_POINT('Ctrl Pts',(0.0591025861724015,0.144030586955267,
1.01767622026813));
#14334=CARTESIAN_POINT('Ctrl Pts',(0.065059301505784,0.141439723788827,
1.01723465794199));
#14335=CARTESIAN_POINT('Ctrl Pts',(0.0717217606801996,0.138031810554476,
1.01671032275089));
#14336=CARTESIAN_POINT('Ctrl Pts',(0.0726028389250547,0.137570416073688,
1.01664035119534));
#14337=CARTESIAN_POINT('Ctrl Pts',(0.0740083912343247,0.136817106823851,
1.01652768053613));
#14338=CARTESIAN_POINT('Ctrl Pts',(0.0745357162886557,0.136530544830826,
1.01648517048202));
#14339=CARTESIAN_POINT('Ctrl Pts',(0.0754688162561447,0.136016457402152,
1.01640951661746));
#14340=CARTESIAN_POINT('Ctrl Pts',(0.0758752561609753,0.135790148410093,
1.01637641644931));
#14341=CARTESIAN_POINT('Ctrl Pts',(0.0767196976671625,0.13531498166623,
1.01630733577342));
#14342=CARTESIAN_POINT('Ctrl Pts',(0.077157517068472,0.135065812929438,
1.01627134440373));
#14343=CARTESIAN_POINT('Ctrl Pts',(0.0782907064869744,0.134413592192337,
1.01617772922887));
#14344=CARTESIAN_POINT('Ctrl Pts',(0.0789841689900054,0.134007274027301,
1.01611998810601));
#14345=CARTESIAN_POINT('Ctrl Pts',(0.0819741119203691,0.132224116386185,
1.01586903200626));
#14346=CARTESIAN_POINT('Ctrl Pts',(0.0842378465335957,0.130793560755221,
1.0156738728988));
#14347=CARTESIAN_POINT('Ctrl Pts',(0.090140015025796,0.126846921983579,
1.01515074952546));
#14348=CARTESIAN_POINT('Ctrl Pts',(0.0937097478716353,0.124233008385915,
1.01481933954105));
#14349=CARTESIAN_POINT('Ctrl Pts',(0.106822161809964,0.113744550049465,
1.01354402700956));
#14350=CARTESIAN_POINT('Ctrl Pts',(0.115524243844455,0.104894731285634,
1.01256988475825));
#14351=CARTESIAN_POINT('Ctrl Pts',(0.125463452194823,0.0920317474293646,
1.01133245658215));
#14352=CARTESIAN_POINT('Ctrl Pts',(0.127724876853017,0.0888666564937184,
1.011040545508));
#14353=CARTESIAN_POINT('Ctrl Pts',(0.130213332602004,0.0850922430263657,
1.01070953922736));
#14354=CARTESIAN_POINT('Ctrl Pts',(0.130557946694873,0.0845625472781061,
1.0106634656141));
#14355=CARTESIAN_POINT('Ctrl Pts',(0.131074622092326,0.0837576935708865,
1.01059404753511));
#14356=CARTESIAN_POINT('Ctrl Pts',(0.131249060443669,0.0834840818769859,
1.01057055094043));
#14357=CARTESIAN_POINT('Ctrl Pts',(0.131560498636436,0.0829921930598325,
1.01052849549684));
#14358=CARTESIAN_POINT('Ctrl Pts',(0.131697812672667,0.0827741206599731,
1.01050991615471));
#14359=CARTESIAN_POINT('Ctrl Pts',(0.131994735435516,0.0822999597150525,
1.01046966055638));
#14360=CARTESIAN_POINT('Ctrl Pts',(0.132154140707772,0.0820437483894939,
1.0104479977369));
#14361=CARTESIAN_POINT('Ctrl Pts',(0.132599042640065,0.0813239986832844,
1.01038738720437));
#14362=CARTESIAN_POINT('Ctrl Pts',(0.132882856741106,0.0808594167606562,
1.01034854804946));
#14363=CARTESIAN_POINT('Ctrl Pts',(0.134548197872611,0.0781009313201563,
1.01011955087143));
#14364=CARTESIAN_POINT('Ctrl Pts',(0.135872851223409,0.0757729744201464,
1.00993286457653));
#14365=CARTESIAN_POINT('Ctrl Pts',(0.144050328767804,0.06049704387074,1.00874192826109));
#14366=CARTESIAN_POINT('Ctrl Pts',(0.149105563105364,0.0466693227503142,
1.00781299064504));
#14367=CARTESIAN_POINT('Ctrl Pts',(0.152570019515499,0.030368440483885,
1.00669316346403));
#14368=CARTESIAN_POINT('Ctrl Pts',(0.152950155307709,0.028391944930931,
1.00655712433383));
#14369=CARTESIAN_POINT('Ctrl Pts',(0.15395382947274,0.0225660196310106,
1.00615457127069));
#14370=CARTESIAN_POINT('Ctrl Pts',(0.154471057883322,0.0187001267212292,
1.00588542005788));
#14371=CARTESIAN_POINT('Ctrl Pts',(0.154932419211424,0.0138794487615835,
1.0055453891294));
#14372=CARTESIAN_POINT('Ctrl Pts',(0.155013794859819,0.0129389703509694,
1.00547884737501));
#14373=CARTESIAN_POINT('Ctrl Pts',(0.155128287171852,0.0114590171259123,
1.00537378983941));
#14374=CARTESIAN_POINT('Ctrl Pts',(0.155167161982236,0.0109199992374513,
1.00533545445845));
#14375=CARTESIAN_POINT('Ctrl Pts',(0.155230839539519,0.00996795639691497,
1.00526761242679));
#14376=CARTESIAN_POINT('Ctrl Pts',(0.155256804798304,0.00955501212076111,
1.00523814245089));
#14377=CARTESIAN_POINT('Ctrl Pts',(0.155312525769058,0.00860856270042894,
1.00517049571296));
#14378=CARTESIAN_POINT('Ctrl Pts',(0.155341180519754,0.00807500056360406,
1.00513228488903));
#14379=CARTESIAN_POINT('Ctrl Pts',(0.155412762250503,0.00660026360220895,
1.00502645929071));
#14380=CARTESIAN_POINT('Ctrl Pts',(0.155449887627298,0.00565884387846968,
1.00495866432382));
#14381=CARTESIAN_POINT('Ctrl Pts',(0.155610880917971,0.000352479944241274,
1.00457512625096));
#14382=CARTESIAN_POINT('Ctrl Pts',(0.155559442127116,-0.00401539858204799,
1.00425397169674));
#14383=CARTESIAN_POINT('Ctrl Pts',(0.154814887628769,-0.0178241302734176,
1.00322016677576));
#14384=CARTESIAN_POINT('Ctrl Pts',(0.15344426084606,-0.027205923441768,
1.0024888594306));
#14385=CARTESIAN_POINT('Ctrl Pts',(0.150503608444309,-0.0394221428117864,
1.00151441813805));
#14386=CARTESIAN_POINT('Ctrl Pts',(0.149686795644279,-0.0424182200064618,
1.00127377356817));
#14387=CARTESIAN_POINT('Ctrl Pts',(0.147962610875359,-0.0480700728279184,
1.00081840104725));
#14388=CARTESIAN_POINT('Ctrl Pts',(0.147071949488602,-0.0507297669582083,
1.00060349993731));
#14389=CARTESIAN_POINT('Ctrl Pts',(0.144948043181759,-0.0565449858653637,
1.00013409988177));
#14390=CARTESIAN_POINT('Ctrl Pts',(0.143682574022113,-0.0596874610987846,
0.999880749735729));
#14391=CARTESIAN_POINT('Ctrl Pts',(0.142091102582054,-0.0632947851830865,
0.999592214849562));
#14392=CARTESIAN_POINT('Ctrl Pts',(0.141864085888583,-0.0638019782167183,
0.999551700719325));
#14393=CARTESIAN_POINT('Ctrl Pts',(0.141496054848492,-0.0646125441648346,
0.999487052780408));
#14394=CARTESIAN_POINT('Ctrl Pts',(0.141356774152863,-0.0649166912892718,
0.99946281758712));
#14395=CARTESIAN_POINT('Ctrl Pts',(0.141107811279407,-0.0654557507488711,
0.999419907080047));
#14396=CARTESIAN_POINT('Ctrl Pts',(0.140998521862669,-0.0656908406618156,
0.999401208039142));
#14397=CARTESIAN_POINT('Ctrl Pts',(0.140765094829428,-0.0661896937195439,
0.99936156143802));
#14398=CARTESIAN_POINT('Ctrl Pts',(0.140640803609722,-0.0664533809587728,
0.999340623563209));
#14399=CARTESIAN_POINT('Ctrl Pts',(0.140302232723181,-0.06716646380878,
0.999284048552469));
#14400=CARTESIAN_POINT('Ctrl Pts',(0.140086533082748,-0.0676151879000025,
0.999248497839715));
#14401=CARTESIAN_POINT('Ctrl Pts',(0.138991126633436,-0.0698662395727306,
0.999070370663153));
#14402=CARTESIAN_POINT('Ctrl Pts',(0.138078723254914,-0.0716525779654174,
0.998929712154224));
#14403=CARTESIAN_POINT('Ctrl Pts',(0.135323120697832,-0.0767993589792354,
0.99852501722293));
#14404=CARTESIAN_POINT('Ctrl Pts',(0.133389886847989,-0.0801101206653924,
0.998265397545028));
#14405=CARTESIAN_POINT('Ctrl Pts',(0.125778548189099,-0.0921039779726331,
0.99731481138957));
#14406=CARTESIAN_POINT('Ctrl Pts',(0.119358859612558,-0.100283910033483,
0.996644490199267));
#14407=CARTESIAN_POINT('Ctrl Pts',(0.107440462666309,-0.112689859593906,
0.995496083866646));
#14408=CARTESIAN_POINT('Ctrl Pts',(0.102389696044359,-0.117297858863065,
0.995032228321061));
#14409=CARTESIAN_POINT('Ctrl Pts',(0.096269161267774,-0.122184520909687,
0.994483542016292));
#14410=CARTESIAN_POINT('Ctrl Pts',(0.0954793016760473,-0.122802733801713,
0.994412982603241));
#14411=CARTESIAN_POINT('Ctrl Pts',(0.0942053998639343,-0.123780080434601,
0.994299546310084));
#14412=CARTESIAN_POINT('Ctrl Pts',(0.09372514356311,-0.12414412237997,0.994256862638636));
#14413=CARTESIAN_POINT('Ctrl Pts',(0.0928701324047044,-0.124784445222554,
0.994181008723361));
#14414=CARTESIAN_POINT('Ctrl Pts',(0.0924962274448928,-0.12506185334547,
0.994147882913742));
#14415=CARTESIAN_POINT('Ctrl Pts',(0.0917160795285165,-0.125635249416698,
0.994078858015699));
#14416=CARTESIAN_POINT('Ctrl Pts',(0.0913096366509977,-0.125930954827646,
0.994042948511566));
#14417=CARTESIAN_POINT('Ctrl Pts',(0.0902537015299882,-0.126691395434084,
0.993949783181154));
#14418=CARTESIAN_POINT('Ctrl Pts',(0.0896020577111059,-0.127153102701747,
0.993892412146157));
#14419=CARTESIAN_POINT('Ctrl Pts',(0.0867890177829316,-0.129113855311558,
0.993645250250577));
#14420=CARTESIAN_POINT('Ctrl Pts',(0.084593463939754,-0.130562879600856,
0.993453587361467));
#14421=CARTESIAN_POINT('Ctrl Pts',(0.0787024285672941,-0.134239874011988,
0.992942167061363));
#14422=CARTESIAN_POINT('Ctrl Pts',(0.0749493885211219,-0.136370814095713,
0.992619152581192));
#14423=CARTESIAN_POINT('Ctrl Pts',(0.0582705078776675,-0.144944326988716,
0.991196164483745));
#14424=CARTESIAN_POINT('Ctrl Pts',(0.0445730419396786,-0.149724754493238,
0.990050930265348));
#14425=CARTESIAN_POINT('Ctrl Pts',(0.030168111211927,-0.152596691593575,
0.988950502576982));
#14426=CARTESIAN_POINT('Ctrl Pts',(0.0299223868857948,-0.15264506537789,
0.988931763350734));
#14427=CARTESIAN_POINT('Ctrl Pts',(0.0290873360485386,-0.152807361284316,
0.988868193157962));
#14428=CARTESIAN_POINT('Ctrl Pts',(0.0284974585208203,-0.152918467376053,
0.988823476261369));
#14429=CARTESIAN_POINT('Ctrl Pts',(0.0264779803126232,-0.153286753833623,
0.988671062692387));
#14430=CARTESIAN_POINT('Ctrl Pts',(0.0250453674192803,-0.153527334131997,
0.988564098787129));
#14431=CARTESIAN_POINT('Ctrl Pts',(0.0231521718021301,-0.15381805338242,
0.988424448638687));
#14432=CARTESIAN_POINT('Ctrl Pts',(0.022694498350447,-0.153886244885385,
0.988390819451182));
#14433=CARTESIAN_POINT('Ctrl Pts',(0.0219557574399018,-0.153992946874617,
0.988336755862827));
#14434=CARTESIAN_POINT('Ctrl Pts',(0.021674881811729,-0.154032731826293,
0.988316251189596));
#14435=CARTESIAN_POINT('Ctrl Pts',(0.0211347852625754,-0.15410772785524,
0.988276922248808));
#14436=CARTESIAN_POINT('Ctrl Pts',(0.0208755842678257,-0.154143053412833,
0.988258091934976));
#14437=CARTESIAN_POINT('Ctrl Pts',(0.0202630193151008,-0.154224964199205,
0.98821369298856));
#14438=CARTESIAN_POINT('Ctrl Pts',(0.0199095792797009,-0.154270989475555,
0.988188155824479));
#14439=CARTESIAN_POINT('Ctrl Pts',(0.018792791402094,-0.154412516660218,
0.988107708892055));
#14440=CARTESIAN_POINT('Ctrl Pts',(0.0180288755335209,-0.154503572844977,
0.988053041332966));
#14441=CARTESIAN_POINT('Ctrl Pts',(0.0116014473685904,-0.155221379692399,
0.987595867133344));
#14442=CARTESIAN_POINT('Ctrl Pts',(0.00590733513091148,-0.155542248908363,
0.987208968863565));
#14443=CARTESIAN_POINT('Ctrl Pts',(-0.0137828839692928,-0.155568547137174,
0.985894090575662));
#14444=CARTESIAN_POINT('Ctrl Pts',(-0.0277114019557472,-0.153699792994551,
0.984997969551863));
#14445=CARTESIAN_POINT('Ctrl Pts',(-0.042777412245691,-0.149561234221445,
0.983928331536351));
#14446=CARTESIAN_POINT('Ctrl Pts',(-0.044345296853919,-0.149103870196441,
0.983815848658988));
#14447=CARTESIAN_POINT('Ctrl Pts',(-0.046750282563141,-0.148361029444013,
0.983641321803609));
#14448=CARTESIAN_POINT('Ctrl Pts',(-0.0475926670679483,-0.148092950421283,
0.983579811398731));
#14449=CARTESIAN_POINT('Ctrl Pts',(-0.0495926861862118,-0.147437640996896,
0.983432826465254));
#14450=CARTESIAN_POINT('Ctrl Pts',(-0.0507481220980271,-0.147043940577151,
0.983347152450299));
#14451=CARTESIAN_POINT('Ctrl Pts',(-0.0524684626897892,-0.146435064513183,
0.983218396428757));
#14452=CARTESIAN_POINT('Ctrl Pts',(-0.0530369616348882,-0.146230121308723,
0.983175651419479));
#14453=CARTESIAN_POINT('Ctrl Pts',(-0.0540150689540782,-0.145871060689959,
0.983101761635701));
#14454=CARTESIAN_POINT('Ctrl Pts',(-0.0544252509966532,-0.145718516557564,
0.9830706693382));
#14455=CARTESIAN_POINT('Ctrl Pts',(-0.0552722627075692,-0.145399443004196,
0.983006243090929));
#14456=CARTESIAN_POINT('Ctrl Pts',(-0.0557089957467054,-0.145232671375499,
0.9829729013307));
#14457=CARTESIAN_POINT('Ctrl Pts',(-0.0567165572734705,-0.144842708786945,
0.982895693200521));
#14458=CARTESIAN_POINT('Ctrl Pts',(-0.0572868283126382,-0.144618108961725,
0.982851780008853));
#14459=CARTESIAN_POINT('Ctrl Pts',(-0.0590973254702236,-0.143892660086581,
0.982711671492993));
#14460=CARTESIAN_POINT('Ctrl Pts',(-0.0603323957121858,-0.14337919418218,
0.982615053426657));
#14461=CARTESIAN_POINT('Ctrl Pts',(-0.0632071085482083,-0.142140346744301,
0.982387659790866));
#14462=CARTESIAN_POINT('Ctrl Pts',(-0.0648411051055526,-0.141402430452105,
0.98225647098647));
#14463=CARTESIAN_POINT('Ctrl Pts',(-0.0705242220952803,-0.13871670541187,
0.981793213513812));
#14464=CARTESIAN_POINT('Ctrl Pts',(-0.0745010504269431,-0.136622021439553,
0.981456361686497));
#14465=CARTESIAN_POINT('Ctrl Pts',(-0.0845558187773673,-0.130756319092542,
0.980571701250823));
#14466=CARTESIAN_POINT('Ctrl Pts',(-0.0904742448205335,-0.126733177547743,
0.980017594534704));
#14467=CARTESIAN_POINT('Ctrl Pts',(-0.103106691198302,-0.116808940856877,
0.978771907112906));
#14468=CARTESIAN_POINT('Ctrl Pts',(-0.109633067609805,-0.110706604689759,
0.978082237452275));
#14469=CARTESIAN_POINT('Ctrl Pts',(-0.116061570381856,-0.103566345555614,
0.97737807830484));
#14470=CARTESIAN_POINT('Ctrl Pts',(-0.11651862141399,-0.103051865399575,
0.977327869846842));
#14471=CARTESIAN_POINT('Ctrl Pts',(-0.117190791718214,-0.102285046562854,
0.977253836011245));
#14472=CARTESIAN_POINT('Ctrl Pts',(-0.117408534255182,-0.102035035666798,
0.977229822934923));
#14473=CARTESIAN_POINT('Ctrl Pts',(-0.117794487531771,-0.101589014751518,
0.977187207578976));
#14474=CARTESIAN_POINT('Ctrl Pts',(-0.117963010565243,-0.101393280611942,
0.977168582427088));
#14475=CARTESIAN_POINT('Ctrl Pts',(-0.118324115173727,-0.100971750186091,
0.977128635918741));
#14476=CARTESIAN_POINT('Ctrl Pts',(-0.118516537873616,-0.100745822850169,
0.977107326207094));
#14477=CARTESIAN_POINT('Ctrl Pts',(-0.119045392234047,-0.10012127231349,
0.977048689559062));
#14478=CARTESIAN_POINT('Ctrl Pts',(-0.11938047146774,-0.0997215003639668,
0.977011460075556));
#14479=CARTESIAN_POINT('Ctrl Pts',(-0.12117147603577,-0.0975627467969924,
0.976811999801817));
#14480=CARTESIAN_POINT('Ctrl Pts',(-0.122590646726793,-0.0957734357162094,
0.976652271643523));
#14481=CARTESIAN_POINT('Ctrl Pts',(-0.12795122684845,-0.0887002363019829,
0.976039328255174));
#14482=CARTESIAN_POINT('Ctrl Pts',(-0.131594973069662,-0.0831987388151121,
0.975601336925232));
#14483=CARTESIAN_POINT('Ctrl Pts',(-0.137842295687083,-0.0723235505690146,
0.974773767496741));
#14484=CARTESIAN_POINT('Ctrl Pts',(-0.140507236782163,-0.0669993277992513,
0.974384313582742));
#14485=CARTESIAN_POINT('Ctrl Pts',(-0.146072524104153,-0.0540789901738317,
0.973450940480724));
#14486=CARTESIAN_POINT('Ctrl Pts',(-0.148695198689844,-0.0463834788812116,
0.9729034867842));
#14487=CARTESIAN_POINT('Ctrl Pts',(-0.15096062193687,-0.0375200830573085,
0.972262854614899));
#14488=CARTESIAN_POINT('Ctrl Pts',(-0.151206048609356,-0.036518444402699,
0.972190331305487));
#14489=CARTESIAN_POINT('Ctrl Pts',(-0.151580964764115,-0.0349197192255328,
0.972074340434997));
#14490=CARTESIAN_POINT('Ctrl Pts',(-0.15171693064462,-0.0343241694163665,
0.972031080281636));
#14491=CARTESIAN_POINT('Ctrl Pts',(-0.15195061745934,-0.0332720653735112,
0.971954558171104));
#14492=CARTESIAN_POINT('Ctrl Pts',(-0.152049798125487,-0.0328158401049746,
0.971921343288194));
#14493=CARTESIAN_POINT('Ctrl Pts',(-0.152236568023895,-0.0319376823317655,
0.971857344567772));
#14494=CARTESIAN_POINT('Ctrl Pts',(-0.152324460921639,-0.0315158181626794,
0.971826570757795));
#14495=CARTESIAN_POINT('Ctrl Pts',(-0.15250846787461,-0.0306138765536068,
0.971760712137446));
#14496=CARTESIAN_POINT('Ctrl Pts',(-0.152604070325346,-0.0301337007531674,
0.971725611364373));
#14497=CARTESIAN_POINT('Ctrl Pts',(-0.152828228193531,-0.0289794086288356,
0.971641135507136));
#14498=CARTESIAN_POINT('Ctrl Pts',(-0.152954591495778,-0.0283048824329136,
0.971591691354873));
#14499=CARTESIAN_POINT('Ctrl Pts',(-0.153522877886142,-0.0251563955149873,
0.971360512478664));
#14500=CARTESIAN_POINT('Ctrl Pts',(-0.15390924373343,-0.0226729265187878,
0.971177038246144));
#14501=CARTESIAN_POINT('Ctrl Pts',(-0.155117025923269,-0.0134424784721329,
0.970490528255298));
#14502=CARTESIAN_POINT('Ctrl Pts',(-0.155556057183704,-0.00665416912435971,
0.969976199532121));
#14503=CARTESIAN_POINT('Ctrl Pts',(-0.155549936890276,0.00014011934593126,
0.969453892031266));
#14504=CARTESIAN_POINT('Ctrl Pts',(-0.155549937001753,0.00013999553845127,
0.969453901548902));
#14505=CARTESIAN_POINT('Ctrl Pts',(-0.155538063581429,0.0133326287020923,
0.968439724690961));
#14506=CARTESIAN_POINT('Ctrl Pts',(-0.153847975061747,0.0264709038583835,
0.96739735679523));
#14507=CARTESIAN_POINT('Ctrl Pts',(-0.150341752135942,0.0399206228266964,
0.966372199424086));
#14508=CARTESIAN_POINT('Ctrl Pts',(-0.150159449777708,0.0406009636922113,
0.966320474541299));
#14509=CARTESIAN_POINT('Ctrl Pts',(-0.149865254441721,0.0416697901246329,
0.966239446105639));
#14510=CARTESIAN_POINT('Ctrl Pts',(-0.149756460307496,0.0420591072626695,
0.966209980399501));
#14511=CARTESIAN_POINT('Ctrl Pts',(-0.14954746175416,0.0427959105822705,
0.966154312981632));
#14512=CARTESIAN_POINT('Ctrl Pts',(-0.149447561013226,0.0431434791603147,
0.966128094706468));
#14513=CARTESIAN_POINT('Ctrl Pts',(-0.149273064956088,0.0437426961357795,
0.966082969047862));
#14514=CARTESIAN_POINT('Ctrl Pts',(-0.14919904359982,0.043994508520487,
0.966064028690258));
#14515=CARTESIAN_POINT('Ctrl Pts',(-0.149054123432694,0.0444829382910349,
0.966027336978042));
#14516=CARTESIAN_POINT('Ctrl Pts',(-0.148983298445989,0.0447195739892545,
0.966009581323496));
#14517=CARTESIAN_POINT('Ctrl Pts',(-0.148790385769705,0.0453585758574079,
0.96596168843626));
#14518=CARTESIAN_POINT('Ctrl Pts',(-0.148667228541293,0.0457606213929604,
0.965931613040074));
#14519=CARTESIAN_POINT('Ctrl Pts',(-0.148202364632928,0.0472564787402857,
0.965819911902308));
#14520=CARTESIAN_POINT('Ctrl Pts',(-0.147850193040741,0.0483470401309401,
0.965738870691897));
#14521=CARTESIAN_POINT('Ctrl Pts',(-0.143937089513277,0.0600218388052825,
0.964874540776392));
#14522=CARTESIAN_POINT('Ctrl Pts',(-0.139257682058014,0.0701989279265626,
0.964148331841343));
#14523=CARTESIAN_POINT('Ctrl Pts',(-0.130476418450045,0.0848945881474805,
0.963020807890539));
#14524=CARTESIAN_POINT('Ctrl Pts',(-0.127134947714255,0.0898214061625449,
0.962627603067687));
#14525=CARTESIAN_POINT('Ctrl Pts',(-0.121456318897918,0.0972403748156322,
0.961997027651078));
#14526=CARTESIAN_POINT('Ctrl Pts',(-0.11930529405679,0.099867773011555,
0.961765440021246));
#14527=CARTESIAN_POINT('Ctrl Pts',(-0.115625740977078,0.104073544230565,
0.961378831861088));
#14528=CARTESIAN_POINT('Ctrl Pts',(-0.114146629132364,0.105693712220032,
0.961225760216138));
#14529=CARTESIAN_POINT('Ctrl Pts',(-0.112128227808992,0.10781280260133,
0.961019606789338));
#14530=CARTESIAN_POINT('Ctrl Pts',(-0.111618902524712,0.108340022348401,
0.960967809708947));
#14531=CARTESIAN_POINT('Ctrl Pts',(-0.110803574142548,0.109172144043803,
0.96088523450927));
#14532=CARTESIAN_POINT('Ctrl Pts',(-0.110499989881001,0.109479410426454,
0.960854562077295));
#14533=CARTESIAN_POINT('Ctrl Pts',(-0.109869009262583,0.110112745909587,
0.960790961315572));
#14534=CARTESIAN_POINT('Ctrl Pts',(-0.109541432329764,0.110438628218438,
0.960758025198734));
#14535=CARTESIAN_POINT('Ctrl Pts',(-0.108795167077099,0.111174446102175,
0.960683175131711));
#14536=CARTESIAN_POINT('Ctrl Pts',(-0.108375606736996,0.111583483062982,
0.960641222543674));
#14537=CARTESIAN_POINT('Ctrl Pts',(-0.107287225097557,0.112632636905629,
0.960532717301163));
#14538=CARTESIAN_POINT('Ctrl Pts',(-0.106614990726881,0.113269162832774,
0.96046601116039));
#14539=CARTESIAN_POINT('Ctrl Pts',(-0.102321723565499,0.11726229574931,
0.960041885322198));
#14540=CARTESIAN_POINT('Ctrl Pts',(-0.0985486826696047,0.120450521752605,
0.959677465052248));
#14541=CARTESIAN_POINT('Ctrl Pts',(-0.0871678471949762,0.129174262363729,
0.958600134462228));
#14542=CARTESIAN_POINT('Ctrl Pts',(-0.0792023049743255,0.134205732013114,
0.957871163454998));
#14543=CARTESIAN_POINT('Ctrl Pts',(-0.0684802489422896,0.139689793109977,
0.956937584580619));
#14544=CARTESIAN_POINT('Ctrl Pts',(-0.066098187521275,0.140832551192719,
0.956733100905458));
#14545=CARTESIAN_POINT('Ctrl Pts',(-0.0636886228436577,0.14191392398309,
0.956529730343417));
#14546=CARTESIAN_POINT('Ctrl Pts',(-0.0636886279045123,0.141913921711862,
0.942835077379979));
#14547=CARTESIAN_POINT('Ctrl Pts',(-0.0651754685424693,0.141246652151541,
0.942961311460843));
#14548=CARTESIAN_POINT('Ctrl Pts',(-0.066652314796618,0.14055579521858,
0.943087417724883));
#14549=CARTESIAN_POINT('Ctrl Pts',(-0.072064565846341,0.137919418819438,
0.943551732415686));
#14550=CARTESIAN_POINT('Ctrl Pts',(-0.0759277422258973,0.135830968303831,
0.943887488150879));
#14551=CARTESIAN_POINT('Ctrl Pts',(-0.0815815806014431,0.132457769055618,
0.944380644775852));
#14552=CARTESIAN_POINT('Ctrl Pts',(-0.0834416230631961,0.131293989808811,
0.944543177869038));
#14553=CARTESIAN_POINT('Ctrl Pts',(-0.0857050585164088,0.129810276820697,
0.944740753488416));
#14554=CARTESIAN_POINT('Ctrl Pts',(-0.086132187189012,0.129527261121152,
0.944778028232698));
#14555=CARTESIAN_POINT('Ctrl Pts',(-0.0868027456224855,0.129078164997774,
0.944836522224598));
#14556=CARTESIAN_POINT('Ctrl Pts',(-0.0870471099441541,0.128913498056301,
0.944857833407518));
#14557=CARTESIAN_POINT('Ctrl Pts',(-0.0875049863599552,0.128603058658927,
0.94489775325352));
#14558=CARTESIAN_POINT('Ctrl Pts',(-0.087718600383088,0.128457450085994,
0.94491637198416));
#14559=CARTESIAN_POINT('Ctrl Pts',(-0.0882078249401503,0.128122184049715,
0.944959002633468));
#14560=CARTESIAN_POINT('Ctrl Pts',(-0.0884831870764194,0.127932169671416,
0.944982990055015));
#14561=CARTESIAN_POINT('Ctrl Pts',(-0.0893360607912009,0.127339570942061,
0.945057270049096));
#14562=CARTESIAN_POINT('Ctrl Pts',(-0.0899114650685197,0.126933945754263,
0.945107361632916));
#14563=CARTESIAN_POINT('Ctrl Pts',(-0.0962832704591434,0.122377140429815,
0.945662048960674));
#14564=CARTESIAN_POINT('Ctrl Pts',(-0.101791385661413,0.11783538614154,
0.946141636405166));
#14565=CARTESIAN_POINT('Ctrl Pts',(-0.11327216640534,0.106960701624341,
0.947190343089342));
#14566=CARTESIAN_POINT('Ctrl Pts',(-0.119064248156573,0.100473284690167,
0.947754939511273));
#14567=CARTESIAN_POINT('Ctrl Pts',(-0.128088442724773,0.0884825577143471,
0.948756471065218));
#14568=CARTESIAN_POINT('Ctrl Pts',(-0.131579780562707,0.0832019109009361,
0.94918528971279));
#14569=CARTESIAN_POINT('Ctrl Pts',(-0.135478504404585,0.0764432028338188,
0.949729402576262));
#14570=CARTESIAN_POINT('Ctrl Pts',(-0.136198940769557,0.0751520903527141,
0.949833123954001));
#14571=CARTESIAN_POINT('Ctrl Pts',(-0.137204603257862,0.0732878481805892,
0.949982670777034));
#14572=CARTESIAN_POINT('Ctrl Pts',(-0.137504882587856,0.072722892465042,
0.950027962413833));
#14573=CARTESIAN_POINT('Ctrl Pts',(-0.138019591791376,0.0717399155998343,
0.950106725343007));
#14574=CARTESIAN_POINT('Ctrl Pts',(-0.138235630771024,0.0713227424108879,
0.950140139493161));
#14575=CARTESIAN_POINT('Ctrl Pts',(-0.138647508029358,0.0705185024513608,
0.950204535318532));
#14576=CARTESIAN_POINT('Ctrl Pts',(-0.138843623797926,0.0701315820039001,
0.950235506885803));
#14577=CARTESIAN_POINT('Ctrl Pts',(-0.139353389066908,0.0691153375162837,
0.950316832390534));
#14578=CARTESIAN_POINT('Ctrl Pts',(-0.139664391166885,0.0684847043821068,
0.950367278017445));
#14579=CARTESIAN_POINT('Ctrl Pts',(-0.140729801554834,0.0662868814749985,
0.950543029360024));
#14580=CARTESIAN_POINT('Ctrl Pts',(-0.141462166834518,0.0647092157217563,
0.950669090923648));
#14581=CARTESIAN_POINT('Ctrl Pts',(-0.146953411502017,0.0523409818694037,
0.95165700755847));
#14582=CARTESIAN_POINT('Ctrl Pts',(-0.150496627030119,0.0410552769420669,
0.952560821658465));
#14583=CARTESIAN_POINT('Ctrl Pts',(-0.154606588493676,0.0197626040760926,
0.95424235999968));
#14584=CARTESIAN_POINT('Ctrl Pts',(-0.155550828322176,0.00988668057949216,
0.955011981534242));
#14585=CARTESIAN_POINT('Ctrl Pts',(-0.155549938049739,-0.000746640964265864,
0.955792014344006));
#14586=CARTESIAN_POINT('Ctrl Pts',(-0.155544686718657,-0.00148026240623606,
0.955845574819193));
#14587=CARTESIAN_POINT('Ctrl Pts',(-0.155529454776193,-0.00255038945730868,
0.955923303393528));
#14588=CARTESIAN_POINT('Ctrl Pts',(-0.155523571979401,-0.00288692811582805,
0.95594769018274));
#14589=CARTESIAN_POINT('Ctrl Pts',(-0.155511220153815,-0.0034828468616109,
0.955990767375515));
#14590=CARTESIAN_POINT('Ctrl Pts',(-0.155505194491466,-0.00374223280619009,
0.956009482205337));
#14591=CARTESIAN_POINT('Ctrl Pts',(-0.155491054726831,-0.004291689999359,
0.956049049889402));
#14592=CARTESIAN_POINT('Ctrl Pts',(-0.155482777959434,-0.00458175347388352,
0.956069893538374));
#14593=CARTESIAN_POINT('Ctrl Pts',(-0.155458275685357,-0.00536369497479437,
0.956125967191308));
#14594=CARTESIAN_POINT('Ctrl Pts',(-0.155440527265389,-0.0058555276371858,
0.956161113328801));
#14595=CARTESIAN_POINT('Ctrl Pts',(-0.155341367983861,-0.00828355785472875,
0.956334046009413));
#14596=CARTESIAN_POINT('Ctrl Pts',(-0.155226109101509,-0.0102183132283127,
0.956470045809172));
#14597=CARTESIAN_POINT('Ctrl Pts',(-0.154790182263663,-0.0157819589500135,
0.95685725921668));
#14598=CARTESIAN_POINT('Ctrl Pts',(-0.154378156275497,-0.0194025735734962,
0.95710449747206));
#14599=CARTESIAN_POINT('Ctrl Pts',(-0.15279598079913,-0.0299826185236076,
0.957821678177203));
#14600=CARTESIAN_POINT('Ctrl Pts',(-0.151279154900507,-0.0368808282153937,
0.958282782973249));
#14601=CARTESIAN_POINT('Ctrl Pts',(-0.146393928955871,-0.053589158847619,
0.959430151307216));
#14602=CARTESIAN_POINT('Ctrl Pts',(-0.142504435665996,-0.0632093065583088,
0.960119472663025));
#14603=CARTESIAN_POINT('Ctrl Pts',(-0.13715870772068,-0.0733797647467837,
0.960923981128279));
#14604=CARTESIAN_POINT('Ctrl Pts',(-0.136617486203173,-0.0743825471406965,
0.961004142971918));
#14605=CARTESIAN_POINT('Ctrl Pts',(-0.135782475356866,-0.0758898051601302,
0.961125953140414));
#14606=CARTESIAN_POINT('Ctrl Pts',(-0.13549677444249,-0.0763987384721141,
0.961167313439395));
#14607=CARTESIAN_POINT('Ctrl Pts',(-0.134979951949463,-0.0773073620862803,
0.961241576296655));
#14608=CARTESIAN_POINT('Ctrl Pts',(-0.134749900974497,-0.0777076562505997,
0.961274440111972));
#14609=CARTESIAN_POINT('Ctrl Pts',(-0.134258285270607,-0.0785543315578226,
0.961344267949642));
#14610=CARTESIAN_POINT('Ctrl Pts',(-0.133996269340237,-0.0790004427915584,
0.961381247987981));
#14611=CARTESIAN_POINT('Ctrl Pts',(-0.13328993072773,-0.0801894392379389,
0.961480318075936));
#14612=CARTESIAN_POINT('Ctrl Pts',(-0.132841629884341,-0.0809299271723088,
0.961542552231131));
#14613=CARTESIAN_POINT('Ctrl Pts',(-0.130641410828768,-0.0844966327945511,
0.961844957377596));
#14614=CARTESIAN_POINT('Ctrl Pts',(-0.128805481071348,-0.0872697202501926,
0.96208819702262));
#14615=CARTESIAN_POINT('Ctrl Pts',(-0.118224401331525,-0.102189993479413,
0.963443850940698));
#14616=CARTESIAN_POINT('Ctrl Pts',(-0.10785057381332,-0.11308354743713,
0.964621104832272));
#14617=CARTESIAN_POINT('Ctrl Pts',(-0.0953028372259867,-0.122939665508869,
0.965843841327429));
#14618=CARTESIAN_POINT('Ctrl Pts',(-0.0945146265885371,-0.123546661509761,
0.965919867220125));
#14619=CARTESIAN_POINT('Ctrl Pts',(-0.0930565935277422,-0.124647363189706,
0.966059004665618));
#14620=CARTESIAN_POINT('Ctrl Pts',(-0.0923885302816992,-0.125143334904367,
0.966122191268034));
#14621=CARTESIAN_POINT('Ctrl Pts',(-0.0891437560344951,-0.127512116654156,
0.96642626333075));
#14622=CARTESIAN_POINT('Ctrl Pts',(-0.0865136716872677,-0.129311010767833,
0.966664220660414));
#14623=CARTESIAN_POINT('Ctrl Pts',(-0.0833702842405818,-0.13132210781512,
0.966937240046204));
#14624=CARTESIAN_POINT('Ctrl Pts',(-0.0829090532376879,-0.131613788070727,
0.96697702066885));
#14625=CARTESIAN_POINT('Ctrl Pts',(-0.0821651622539671,-0.132078758777087,
0.967040720479944));
#14626=CARTESIAN_POINT('Ctrl Pts',(-0.0818834722534007,-0.132253579859319,
0.967064736522244));
#14627=CARTESIAN_POINT('Ctrl Pts',(-0.0813808878923997,-0.132563270049107,
0.9671073953741));
#14628=CARTESIAN_POINT('Ctrl Pts',(-0.0811602138422337,-0.132698489717835,
0.967126060948625));
#14629=CARTESIAN_POINT('Ctrl Pts',(-0.0806888852063093,-0.132985684282409,
0.967165788784842));
#14630=CARTESIAN_POINT('Ctrl Pts',(-0.0804381387799087,-0.133137501303722,
0.96718684072077));
#14631=CARTESIAN_POINT('Ctrl Pts',(-0.0797538940055538,-0.133549145700793,
0.967244065849));
#14632=CARTESIAN_POINT('Ctrl Pts',(-0.0793195508828488,-0.133807573751385,
0.967280149161536));
#14633=CARTESIAN_POINT('Ctrl Pts',(-0.0770726073458707,-0.135129688030806,
0.967465612986509));
#14634=CARTESIAN_POINT('Ctrl Pts',(-0.0752397313942165,-0.136158743334439,
0.967612881071657));
#14635=CARTESIAN_POINT('Ctrl Pts',(-0.069761205089701,-0.139090193404506,
0.968043050445934));
#14636=CARTESIAN_POINT('Ctrl Pts',(-0.0660601664104152,-0.140885654933273,
0.968320844720841));
#14637=CARTESIAN_POINT('Ctrl Pts',(-0.0527289265985237,-0.146711906241544,
0.969292022268375));
#14638=CARTESIAN_POINT('Ctrl Pts',(-0.0427694867708225,-0.149918324311593,
0.969966649056215));
#14639=CARTESIAN_POINT('Ctrl Pts',(-0.0296467473691113,-0.152727770702798,
0.9708646569596));
#14640=CARTESIAN_POINT('Ctrl Pts',(-0.0267124924318142,-0.153268205414237,
0.971065866025252));
#14641=CARTESIAN_POINT('Ctrl Pts',(-0.0201146065116749,-0.154288192067154,
0.971521255039313));
#14642=CARTESIAN_POINT('Ctrl Pts',(-0.0164459180903311,-0.154722240224255,
0.971776500787789));
#14643=CARTESIAN_POINT('Ctrl Pts',(-0.0118419564899607,-0.155101351632126,
0.972100947891838));
#14644=CARTESIAN_POINT('Ctrl Pts',(-0.0109177724930156,-0.155169144449239,
0.972166281098758));
#14645=CARTESIAN_POINT('Ctrl Pts',(-0.00945782179957791,-0.155263130746387,
0.972269836249907));
#14646=CARTESIAN_POINT('Ctrl Pts',(-0.00892241964447542,-0.155294818255313,
0.972307886201858));
#14647=CARTESIAN_POINT('Ctrl Pts',(-0.00793220838357111,-0.155348285765796,
0.972378399363978));
#14648=CARTESIAN_POINT('Ctrl Pts',(-0.00747744529648016,-0.155370839039889,
0.972410838026622));
#14649=CARTESIAN_POINT('Ctrl Pts',(-0.00646789566210372,-0.15541646355692,
0.972482975184194));
#14650=CARTESIAN_POINT('Ctrl Pts',(-0.00591307366941867,-0.155438561379853,
0.972522703668489));
#14651=CARTESIAN_POINT('Ctrl Pts',(-0.00431885141996092,-0.155493509353143,
0.97263710694313));
#14652=CARTESIAN_POINT('Ctrl Pts',(-0.003279242013222,-0.155518906897948,
0.972712013097095));
#14653=CARTESIAN_POINT('Ctrl Pts',(0.00417961038448302,-0.155626304365034,
0.973251706253133));
#14654=CARTESIAN_POINT('Ctrl Pts',(0.0105973077003786,-0.155321251546523,
0.97372849901456));
#14655=CARTESIAN_POINT('Ctrl Pts',(0.0289198148856911,-0.153309478670649,
0.975126461956969));
#14656=CARTESIAN_POINT('Ctrl Pts',(0.04066898390607,-0.150619192295392,
0.976071065891629));
#14657=CARTESIAN_POINT('Ctrl Pts',(0.0561918459608765,-0.145114255809288,
0.977329798968758));
#14658=CARTESIAN_POINT('Ctrl Pts',(0.0603274096331646,-0.143444357283329,
0.977665732262299));
#14659=CARTESIAN_POINT('Ctrl Pts',(0.0649877866080395,-0.141325253149211,
0.978040737765118));
#14660=CARTESIAN_POINT('Ctrl Pts',(0.0655878796580297,-0.141047756699409,
0.978088954821194));
#14661=CARTESIAN_POINT('Ctrl Pts',(0.0664813172160623,-0.140627676187754,
0.978160616839568));
#14662=CARTESIAN_POINT('Ctrl Pts',(0.0667760015370219,-0.140487986934058,
0.978184232828689));
#14663=CARTESIAN_POINT('Ctrl Pts',(0.0673027998977323,-0.140236236604451,
0.978226410944971));
#14664=CARTESIAN_POINT('Ctrl Pts',(0.0675350756757461,-0.140124524934311,
0.97824499413902));
#14665=CARTESIAN_POINT('Ctrl Pts',(0.0680374265608438,-0.139881382953603,
0.978285154038826));
#14666=CARTESIAN_POINT('Ctrl Pts',(0.0683073982668438,-0.139749747964746,
0.978306717777954));
#14667=CARTESIAN_POINT('Ctrl Pts',(0.0690601129544049,-0.13938003091338,
0.978366792196688));
#14668=CARTESIAN_POINT('Ctrl Pts',(0.0695420103728628,-0.139140220766205,
0.978405197345101));
#14669=CARTESIAN_POINT('Ctrl Pts',(0.0723242573724227,-0.137737605389497,
0.978626666634669));
#14670=CARTESIAN_POINT('Ctrl Pts',(0.074596839239336,-0.136520180964435,
0.978806519351657));
#14671=CARTESIAN_POINT('Ctrl Pts',(0.0896386722774296,-0.127974402577677,
0.979997024779159));
#14672=CARTESIAN_POINT('Ctrl Pts',(0.101343105035339,-0.118921083136701,
0.980930233407886));
#14673=CARTESIAN_POINT('Ctrl Pts',(0.112901056904835,-0.107016993056017,
0.982044901681032));
#14674=CARTESIAN_POINT('Ctrl Pts',(0.114176856439393,-0.105654770467335,
0.982170964815923));
#14675=CARTESIAN_POINT('Ctrl Pts',(0.118150500277885,-0.10125591023318,
0.98257408841126));
#14676=CARTESIAN_POINT('Ctrl Pts',(0.120753871774969,-0.0981366272187767,
0.982854192280061));
#14677=CARTESIAN_POINT('Ctrl Pts',(0.123763674068294,-0.0942290535155104,
0.983200453310723));
#14678=CARTESIAN_POINT('Ctrl Pts',(0.124289496702211,-0.0935343920696952,
0.983261836424757));
#14679=CARTESIAN_POINT('Ctrl Pts',(0.125149098781142,-0.0923787283553328,
0.983363692952847));
#14680=CARTESIAN_POINT('Ctrl Pts',(0.125486238194224,-0.0919202392649491,
0.983404035329012));
#14681=CARTESIAN_POINT('Ctrl Pts',(0.126091553489631,-0.0910875106948584,
0.983477191340299));
#14682=CARTESIAN_POINT('Ctrl Pts',(0.1263605996034,-0.0907139092175491,
0.983509970917649));
#14683=CARTESIAN_POINT('Ctrl Pts',(0.126934040150914,-0.0899101199345179,
0.983580409167302));
#14684=CARTESIAN_POINT('Ctrl Pts',(0.127237914153945,-0.0894795697620802,
0.983618087232992));
#14685=CARTESIAN_POINT('Ctrl Pts',(0.128060048929613,-0.0883020549922773,
0.983720997241086));
#14686=CARTESIAN_POINT('Ctrl Pts',(0.128573951065136,-0.0875520878678512,
0.983786393415878));
#14687=CARTESIAN_POINT('Ctrl Pts',(0.131245346144746,-0.0835793202351674,
0.98413208898729));
#14688=CARTESIAN_POINT('Ctrl Pts',(0.133288137551191,-0.0802814491528155,
0.984416618854767));
#14689=CARTESIAN_POINT('Ctrl Pts',(0.14252933799061,-0.064035904474919,
0.985808355921005));
#14690=CARTESIAN_POINT('Ctrl Pts',(0.147975937388227,-0.0501815091361336,
0.986975912152673));
#14691=CARTESIAN_POINT('Ctrl Pts',(0.152402707976014,-0.0314476080578434,
0.988446945003004));
#14692=CARTESIAN_POINT('Ctrl Pts',(0.153238747877481,-0.0270819629670539,
0.988781716040223));
#14693=CARTESIAN_POINT('Ctrl Pts',(0.15398314584966,-0.0220324700510599,
0.989155584208909));
#14694=CARTESIAN_POINT('Ctrl Pts',(0.154075333604147,-0.0213782730607475,
0.989203765396006));
#14695=CARTESIAN_POINT('Ctrl Pts',(0.154206786705354,-0.0204003852691087,
0.989275384691173));
#14696=CARTESIAN_POINT('Ctrl Pts',(0.154249205283681,-0.0200771377385511,
0.989298993531867));
#14697=CARTESIAN_POINT('Ctrl Pts',(0.154323338313836,-0.0194981070605036,
0.989341163950043));
#14698=CARTESIAN_POINT('Ctrl Pts',(0.154355433469979,-0.0192423774284857,
0.98935974656144));
#14699=CARTESIAN_POINT('Ctrl Pts',(0.154423563335354,-0.0186883878346796,
0.989399910974417));
#14700=CARTESIAN_POINT('Ctrl Pts',(0.154459369553669,-0.0183901037053667,
0.989421479783852));
#14701=CARTESIAN_POINT('Ctrl Pts',(0.154556953350991,-0.0175567862331444,
0.989481582609495));
#14702=CARTESIAN_POINT('Ctrl Pts',(0.154616817491248,-0.0170215258944013,
0.989520010932838));
#14703=CARTESIAN_POINT('Ctrl Pts',(0.15494764676042,-0.0139176320546861,
0.989741881549012));
#14704=CARTESIAN_POINT('Ctrl Pts',(0.155157401757367,-0.0113426849930247,
0.989922098789935));
#14705=CARTESIAN_POINT('Ctrl Pts',(0.156132117426485,0.0059307821592932,
0.991112598290918));
#14706=CARTESIAN_POINT('Ctrl Pts',(0.154871822917651,0.0206697883842667,
0.992045555031383));
#14707=CARTESIAN_POINT('Ctrl Pts',(0.151136687573145,0.0368376112444624,
0.993160347712217));
#14708=CARTESIAN_POINT('Ctrl Pts',(0.150682359059377,0.0386540323005574,
0.993286820563852));
#14709=CARTESIAN_POINT('Ctrl Pts',(0.149140586046172,0.0443771436301441,
0.993689915692079));
#14710=CARTESIAN_POINT('Ctrl Pts',(0.147933195110242,0.0482494576948214,
0.993969564796378));
#14711=CARTESIAN_POINT('Ctrl Pts',(0.146284517609919,0.0528904590626598,
0.994315322690666));
#14712=CARTESIAN_POINT('Ctrl Pts',(0.145986147965356,0.0537085216662338,
0.994376674074993));
#14713=CARTESIAN_POINT('Ctrl Pts',(0.145481495854097,0.0550568849639068,
0.994478488818316));
#14714=CARTESIAN_POINT('Ctrl Pts',(0.145279141257644,0.0555886437836925,
0.994518821328992));
#14715=CARTESIAN_POINT('Ctrl Pts',(0.144907777827163,0.0565486549957006,
0.994591966784752));
#14716=CARTESIAN_POINT('Ctrl Pts',(0.144739775587607,0.056977292065568,
0.994624745717515));
#14717=CARTESIAN_POINT('Ctrl Pts',(0.144375354026135,0.0578950556897465,
0.994695190708184));
#14718=CARTESIAN_POINT('Ctrl Pts',(0.144178346979375,0.0583839410553832,
0.994732876194692));
#14719=CARTESIAN_POINT('Ctrl Pts',(0.143634595916026,0.0597137567792696,
0.994835827161011));
#14720=CARTESIAN_POINT('Ctrl Pts',(0.143282959046863,0.060552650430303,
0.994901257093939));
#14721=CARTESIAN_POINT('Ctrl Pts',(0.141390865147565,0.0649578089395814,
0.995247454082914));
#14722=CARTESIAN_POINT('Ctrl Pts',(0.139724702220233,0.0684682137111977,
0.995532466245441));
#14723=CARTESIAN_POINT('Ctrl Pts',(0.131083263538171,0.0850426409293185,
0.996924413983738));
#14724=CARTESIAN_POINT('Ctrl Pts',(0.122397897917246,0.0971271347750815,
0.998091617682632));
#14725=CARTESIAN_POINT('Ctrl Pts',(0.109062425398387,0.110999558059501,
0.999562077214838));
#14726=CARTESIAN_POINT('Ctrl Pts',(0.105849553528857,0.11406750477441,0.999896648026993));
#14727=CARTESIAN_POINT('Ctrl Pts',(0.10201262818374,0.117429393773445,1.00027032021568));
#14728=CARTESIAN_POINT('Ctrl Pts',(0.101513025104336,0.117861548467192,
1.00031849519401));
#14729=CARTESIAN_POINT('Ctrl Pts',(0.100762762552196,0.118502212877876,
1.00039010709367));
#14730=CARTESIAN_POINT('Ctrl Pts',(0.1005141847983,0.118713130839588,1.00041371469671));
#14731=CARTESIAN_POINT('Ctrl Pts',(0.100067896593436,0.119089399183898,
1.00045588378237));
#14732=CARTESIAN_POINT('Ctrl Pts',(0.0998704374891159,0.119255040337439,
1.00047446629319));
#14733=CARTESIAN_POINT('Ctrl Pts',(0.0994419110524191,0.119612704537383,
1.0005146314889));
#14734=CARTESIAN_POINT('Ctrl Pts',(0.0992106994597293,0.119804548650624,
1.00053620117724));
#14735=CARTESIAN_POINT('Ctrl Pts',(0.0985634083727691,0.12033846917419,
1.00059630892742));
#14736=CARTESIAN_POINT('Ctrl Pts',(0.0981461002175099,0.120679060604004,
1.00063474126835));
#14737=CARTESIAN_POINT('Ctrl Pts',(0.0957168351372661,0.122640800646394,
1.00085668155352));
#14738=CARTESIAN_POINT('Ctrl Pts',(0.0936663525049465,0.12421390834673,
1.00103696207699));
#14739=CARTESIAN_POINT('Ctrl Pts',(0.0796813794627272,0.134399657797159,
1.00222746062012));
#14740=CARTESIAN_POINT('Ctrl Pts',(0.066614805334272,0.141332824680005,
1.00316037368355));
#14741=CARTESIAN_POINT('Ctrl Pts',(0.0510047975938716,0.146961976327272,
1.00427518840198));
#14742=CARTESIAN_POINT('Ctrl Pts',(0.0492312643835637,0.147565558590524,
1.00440173276362));
#14743=CARTESIAN_POINT('Ctrl Pts',(0.0435867099227604,0.149373473060959,
1.0048048229761));
#14744=CARTESIAN_POINT('Ctrl Pts',(0.0396795691273101,0.150458508016175,
1.00508439276004));
#14745=CARTESIAN_POINT('Ctrl Pts',(0.0348873772864512,0.15158968144272,
1.0054300628959));
#14746=CARTESIAN_POINT('Ctrl Pts',(0.0340383188044144,0.151782585996964,
1.00549140874169));
#14747=CARTESIAN_POINT('Ctrl Pts',(0.0326318634008249,0.15208973561969,
1.00559321619123));
#14748=CARTESIAN_POINT('Ctrl Pts',(0.0320753711090026,0.152208070556371,
1.00563354697973));
#14749=CARTESIAN_POINT('Ctrl Pts',(0.0310674131024543,0.152416633928575,
1.00570669059324));
#14750=CARTESIAN_POINT('Ctrl Pts',(0.0306161699791301,0.152507916458299,
1.00573946941385));
#14751=CARTESIAN_POINT('Ctrl Pts',(0.0301633266312624,0.152597431918257,
1.00577239994307));
#14752=CARTESIAN_POINT('Ctrl Pts',(0.0301621205796583,0.152597670308719,
1.00577248764676));
#14753=CARTESIAN_POINT('Ctrl Pts',(0.0301597155018312,0.152598145671376,
1.00577266254375));
#14754=CARTESIAN_POINT('Ctrl Pts',(0.0301585162608852,0.152598382686173,
1.00577274975267));
#14755=CARTESIAN_POINT('Ctrl Pts',(0.0301561244804412,0.152598855362015,
1.00577292368367));
#14756=CARTESIAN_POINT('Ctrl Pts',(0.0301549319303764,0.152599091025312,
1.00577301040653));
#14757=CARTESIAN_POINT('Ctrl Pts',(0.0301525534617249,0.15259956101247,
1.00577318337048));
#14758=CARTESIAN_POINT('Ctrl Pts',(0.0301513675411587,0.152599795336883,
1.00577326961171));
#14759=CARTESIAN_POINT('Ctrl Pts',(0.0301490022977461,0.152600262653427,
1.00577344161489));
#14760=CARTESIAN_POINT('Ctrl Pts',(0.0301478229596279,0.152600495648734,
1.00577352737793));
#14761=CARTESIAN_POINT('Ctrl Pts',(0.0301454708219992,0.152600960319221,
1.005773698429));
#14762=CARTESIAN_POINT('Ctrl Pts',(0.0301442980134178,0.15260119199635,
1.00577378371768));
#14763=CARTESIAN_POINT('Ctrl Pts',(0.0301419588697503,0.152601654043811,
1.00577395382475));
#14764=CARTESIAN_POINT('Ctrl Pts',(0.0301407925320586,0.152601884414814,
1.00577403864334));
#14765=CARTESIAN_POINT('Ctrl Pts',(0.0301384662985743,0.152602343856728,
1.0057742078125));
#14766=CARTESIAN_POINT('Ctrl Pts',(0.0301373063880749,0.152602572930696,
1.00577429216415));
#14767=CARTESIAN_POINT('Ctrl Pts',(0.0301349929385682,0.152603029792905,
1.00577446040456));
#14768=CARTESIAN_POINT('Ctrl Pts',(0.0301338393974747,0.152603257581708,
1.00577454429347));
#14769=CARTESIAN_POINT('Ctrl Pts',(0.0301315386429228,0.152603711882696,
1.0057747116116));
#14770=CARTESIAN_POINT('Ctrl Pts',(0.0301303914208618,0.152603938396728,
1.00577479504143));
#14771=CARTESIAN_POINT('Ctrl Pts',(0.0296182384711124,0.152705054780455,
1.00581204062154));
#14772=CARTESIAN_POINT('Ctrl Pts',(0.0291067350185148,0.152803376173466,
1.00584928425823));
#14773=CARTESIAN_POINT('Ctrl Pts',(0.0277248485209288,0.1530618125971,1.00595002994691));
#14774=CARTESIAN_POINT('Ctrl Pts',(0.0268535885034833,0.15321706962793,
1.00601368517867));
#14775=CARTESIAN_POINT('Ctrl Pts',(0.0249153348461428,0.153545423153314,
1.00615561810144));
#14776=CARTESIAN_POINT('Ctrl Pts',(0.0238477748976303,0.153714847703908,
1.00623400855744));
#14777=CARTESIAN_POINT('Ctrl Pts',(0.020598848896711,0.154195801449675,
1.00647326815107));
#14778=CARTESIAN_POINT('Ctrl Pts',(0.0184126347732405,0.15447210664942,
1.00663521659951));
#14779=CARTESIAN_POINT('Ctrl Pts',(0.00128168582482278,0.156268386009311,
1.00791204814532));
#14780=CARTESIAN_POINT('Ctrl Pts',(-0.0138047606114468,0.155662166319765,
1.00909405839476));
#14781=CARTESIAN_POINT('Ctrl Pts',(-0.0293488402462114,0.1527582513758,
1.01030532816512));
#14782=CARTESIAN_POINT('Ctrl Pts',(-0.0301312089151297,0.152605858579218,
1.01036624553402));
#14783=CARTESIAN_POINT('Ctrl Pts',(-0.0320990556092688,0.152206830408436,
1.01051929652536));
#14784=CARTESIAN_POINT('Ctrl Pts',(-0.0332829103453998,0.151952349857471,
1.01061121519526));
#14785=CARTESIAN_POINT('Ctrl Pts',(-0.0373399433792838,0.151030562971816,
1.0109254352568));
#14786=CARTESIAN_POINT('Ctrl Pts',(-0.0401972737794545,0.150295324446178,
1.01114539025543));
#14787=CARTESIAN_POINT('Ctrl Pts',(-0.0435447708229174,0.149331644117594,
1.01140017135279));
#14788=CARTESIAN_POINT('Ctrl Pts',(-0.0440565877785823,0.149181446890677,
1.01143904484155));
#14789=CARTESIAN_POINT('Ctrl Pts',(-0.0448851285912375,0.148933668291434,
1.01150183086639));
#14790=CARTESIAN_POINT('Ctrl Pts',(-0.0452023250601255,0.148837704007131,
1.01152583355143));
#14791=CARTESIAN_POINT('Ctrl Pts',(-0.0457661109998347,0.148665168246601,
1.01156843220941));
#14792=CARTESIAN_POINT('Ctrl Pts',(-0.0460128181847806,0.148588996000174,
1.01158705102834));
#14793=CARTESIAN_POINT('Ctrl Pts',(-0.0465426001212743,0.148423976818807,
1.01162698557786));
#14794=CARTESIAN_POINT('Ctrl Pts',(-0.0468256099792224,0.148334934438409,
1.01164828966424));
#14795=CARTESIAN_POINT('Ctrl Pts',(-0.0475954101592194,0.148090312299131,
1.01170616329803));
#14796=CARTESIAN_POINT('Ctrl Pts',(-0.0480816972259792,0.147933140562169,
1.01174264114639));
#14797=CARTESIAN_POINT('Ctrl Pts',(-0.0506542848038794,0.147087634838227,
1.01193523195263));
#14798=CARTESIAN_POINT('Ctrl Pts',(-0.052726738744623,0.146357511749173,
1.01208903112382));
#14799=CARTESIAN_POINT('Ctrl Pts',(-0.0577889011771071,0.144452618949119,
1.01246299068799));
#14800=CARTESIAN_POINT('Ctrl Pts',(-0.0607588120708827,0.14322877469962,
1.01268089937769));
#14801=CARTESIAN_POINT('Ctrl Pts',(-0.063688626060837,0.141913922539273,
1.01289638536134));
#14802=CARTESIAN_POINT('Origin',(0.,0.,-0.129405622560373));
#14803=CARTESIAN_POINT('',(-0.0636886243720526,0.141913923297172,1.09662690323003));
#14804=CARTESIAN_POINT('',(-0.0636886366175018,0.141913917801616,1.08266645291));
#14805=CARTESIAN_POINT('',(-0.0636886258329924,0.141913922641526,-0.129405622560373));
#14806=CARTESIAN_POINT('Ctrl Pts',(-0.0636886243721051,0.141913923297148,
1.09662690323004));
#14807=CARTESIAN_POINT('Ctrl Pts',(-0.0606910358173481,0.143259191520664,
1.09641019358287));
#14808=CARTESIAN_POINT('Ctrl Pts',(-0.0576487518881258,0.144510416255214,
1.09619253612461));
#14809=CARTESIAN_POINT('Ctrl Pts',(-0.0487306005434893,0.147851148303692,
1.09555661654928));
#14810=CARTESIAN_POINT('Ctrl Pts',(-0.0427697403818496,0.149684226985495,
1.09513391348564));
#14811=CARTESIAN_POINT('Ctrl Pts',(-0.0352901438448625,0.151501022618486,
1.09459708320992));
#14812=CARTESIAN_POINT('Ctrl Pts',(-0.0338599732463984,0.151827059712076,
1.09449416940812));
#14813=CARTESIAN_POINT('Ctrl Pts',(-0.0318015728751101,0.152265785270025,
1.09434557360214));
#14814=CARTESIAN_POINT('Ctrl Pts',(-0.031176894660229,0.152394916643116,
1.09430041584057));
#14815=CARTESIAN_POINT('Ctrl Pts',(-0.0300910129164921,0.15261243051825,
1.09422180185109));
#14816=CARTESIAN_POINT('Ctrl Pts',(-0.0296301670539519,0.152702574302262,
1.09418840209104));
#14817=CARTESIAN_POINT('Ctrl Pts',(-0.0287422018335271,0.152872093799484,
1.09412397412506));
#14818=CARTESIAN_POINT('Ctrl Pts',(-0.028315143627443,0.152951769728825,
1.09409295579902));
#14819=CARTESIAN_POINT('Ctrl Pts',(-0.0271931157132175,0.15315624543371,
1.09401137203812));
#14820=CARTESIAN_POINT('Ctrl Pts',(-0.0264976271319612,0.153278102752604,
1.09396071384157));
#14821=CARTESIAN_POINT('Ctrl Pts',(-0.0240698801550837,0.153686454030928,
1.09378355623299));
#14822=CARTESIAN_POINT('Ctrl Pts',(-0.0223336788795188,0.153948340690714,
1.0936562850526));
#14823=CARTESIAN_POINT('Ctrl Pts',(-0.00984123617193006,0.155616920212879,
1.09273602087342));
#14824=CARTESIAN_POINT('Ctrl Pts',(0.00102956083148582,0.155924103007786,
1.09190809851299));
#14825=CARTESIAN_POINT('Ctrl Pts',(0.0179309100360783,0.154633695595715,
1.09059497342993));
#14826=CARTESIAN_POINT('Ctrl Pts',(0.0239876154017345,0.153810583154407,
1.09011986125403));
#14827=CARTESIAN_POINT('Ctrl Pts',(0.0332290777608797,0.151995368933204,
1.08939855476949));
#14828=CARTESIAN_POINT('Ctrl Pts',(0.0364568356744049,0.151253648520396,
1.08914738422744));
#14829=CARTESIAN_POINT('Ctrl Pts',(0.0408257540884962,0.150101689040192,
1.08881044914836));
#14830=CARTESIAN_POINT('Ctrl Pts',(0.0419892496499482,0.14978038051122,
1.08872101926153));
#14831=CARTESIAN_POINT('Ctrl Pts',(0.0437178039215849,0.1492813006192,1.08858872034962));
#14832=CARTESIAN_POINT('Ctrl Pts',(0.0442857464431731,0.149113801458605,
1.08854534280673));
#14833=CARTESIAN_POINT('Ctrl Pts',(0.0453102739715165,0.148805275119575,
1.0884672748202));
#14834=CARTESIAN_POINT('Ctrl Pts',(0.0457671884065209,0.148665380342434,
1.08843252409074));
#14835=CARTESIAN_POINT('Ctrl Pts',(0.0464838097112746,0.148442353398558,
1.08837813240717));
#14836=CARTESIAN_POINT('Ctrl Pts',(0.0467439496842704,0.148360641744423,
1.08835841080417));
#14837=CARTESIAN_POINT('Ctrl Pts',(0.0472496306887385,0.148200341983529,
1.08832012108284));
#14838=CARTESIAN_POINT('Ctrl Pts',(0.0474951885219765,0.148121828348726,
1.08830154941273));
#14839=CARTESIAN_POINT('Ctrl Pts',(0.0480507510872503,0.147942671488438,
1.08825958021533));
#14840=CARTESIAN_POINT('Ctrl Pts',(0.0483606348011116,0.147841664405186,
1.08823620432213));
#14841=CARTESIAN_POINT('Ctrl Pts',(0.0492969520476,0.147533211393719,1.08816566965565));
#14842=CARTESIAN_POINT('Ctrl Pts',(0.0499223962295122,0.147322748893458,
1.08811868373729));
#14843=CARTESIAN_POINT('Ctrl Pts',(0.0547219064225555,0.145673634499721,
1.08775898813051));
#14844=CARTESIAN_POINT('Ctrl Pts',(0.0588348417975893,0.144061671967499,
1.08745576702389));
#14845=CARTESIAN_POINT('Ctrl Pts',(0.0763913558360544,0.136303202843618,
1.08616036458814));
#14846=CARTESIAN_POINT('Ctrl Pts',(0.0889885014990023,0.128434020690596,
1.08522070187036));
#14847=CARTESIAN_POINT('Ctrl Pts',(0.103291450140318,0.116370662134439,
1.08394619738253));
#14848=CARTESIAN_POINT('Ctrl Pts',(0.106198923090093,0.113723519562871,
1.08367473356972));
#14849=CARTESIAN_POINT('Ctrl Pts',(0.109654247928001,0.110329425742178,
1.08333443202295));
#14850=CARTESIAN_POINT('Ctrl Pts',(0.110300001892403,0.109683844718726,
1.08327003373154));
#14851=CARTESIAN_POINT('Ctrl Pts',(0.111310099622651,0.108656076544217,
1.08316800385142));
#14852=CARTESIAN_POINT('Ctrl Pts',(0.111678253091648,0.108277647840552,
1.08313053947914));
#14853=CARTESIAN_POINT('Ctrl Pts',(0.112363873283518,0.107565675344448,
1.08306024238957));
#14854=CARTESIAN_POINT('Ctrl Pts',(0.112681800248584,0.107232580944171,
1.08302743012615));
#14855=CARTESIAN_POINT('Ctrl Pts',(0.113388711572908,0.106485329604507,
1.08295398606815));
#14856=CARTESIAN_POINT('Ctrl Pts',(0.113776913415572,0.106070444945475,
1.08291332135019));
#14857=CARTESIAN_POINT('Ctrl Pts',(0.114752364388992,0.105016430667634,
1.0828102888986));
#14858=CARTESIAN_POINT('Ctrl Pts',(0.115336546583136,0.104374502674475,
1.08274779255658));
#14859=CARTESIAN_POINT('Ctrl Pts',(0.118589858393052,0.100738940043217,
1.08239521443387));
#14860=CARTESIAN_POINT('Ctrl Pts',(0.121147556661058,0.0976481059500292,
1.08210057196515));
#14861=CARTESIAN_POINT('Ctrl Pts',(0.124743587952362,0.092943496655078,
1.08165888842169));
#14862=CARTESIAN_POINT('Ctrl Pts',(0.125876260641376,0.0914036256625607,
1.08151534591618));
#14863=CARTESIAN_POINT('Ctrl Pts',(0.13548016295333,0.0778299329645663,
1.08025903975177));
#14864=CARTESIAN_POINT('Ctrl Pts',(0.142231095549923,0.0646731057569159,
1.07909202409414));
#14865=CARTESIAN_POINT('Ctrl Pts',(0.147880404653027,0.0483107645352777,
1.07778978239498));
#14866=CARTESIAN_POINT('Ctrl Pts',(0.148666263755362,0.0458354472663105,
1.07759679249956));
#14867=CARTESIAN_POINT('Ctrl Pts',(0.1495401688619,0.0428232587818683,1.07736767329061));
#14868=CARTESIAN_POINT('Ctrl Pts',(0.149687806861027,0.0423043035196591,
1.07732840285649));
#14869=CARTESIAN_POINT('Ctrl Pts',(0.149913516779106,0.0414949442716691,
1.07726748432112));
#14870=CARTESIAN_POINT('Ctrl Pts',(0.149993449921502,0.041205071265812,
1.07724573146733));
#14871=CARTESIAN_POINT('Ctrl Pts',(0.15014035435182,0.0406662385563369,
1.07720541930946));
#14872=CARTESIAN_POINT('Ctrl Pts',(0.150207546605777,0.0404173466191966,
1.07718684777061));
#14873=CARTESIAN_POINT('Ctrl Pts',(0.150358279277258,0.0398534385236162,
1.07714488065014));
#14874=CARTESIAN_POINT('Ctrl Pts',(0.150441448511972,0.0395383267763001,
1.07712150669359));
#14875=CARTESIAN_POINT('Ctrl Pts',(0.150689987245872,0.0385845242215516,
1.07705098364594));
#14876=CARTESIAN_POINT('Ctrl Pts',(0.150852287229712,0.0379450292475615,
1.07700400732597));
#14877=CARTESIAN_POINT('Ctrl Pts',(0.152068354326881,0.0330223284250973,
1.07664461155035));
#14878=CARTESIAN_POINT('Ctrl Pts',(0.152943695199273,0.0286965807532526,
1.07634166281779));
#14879=CARTESIAN_POINT('Ctrl Pts',(0.155520071892186,0.0124338223857224,
1.07523038589395));
#14880=CARTESIAN_POINT('Ctrl Pts',(0.156016042365109,0.00034937246958913,
1.07445655448604));
#14881=CARTESIAN_POINT('Ctrl Pts',(0.154791477433783,-0.0159244915900999,
1.07336407318295));
#14882=CARTESIAN_POINT('Ctrl Pts',(0.154296729050599,-0.0201619837809552,
1.07307529362274));
#14883=CARTESIAN_POINT('Ctrl Pts',(0.15321980489979,-0.0269499301488922,
1.07260168214296));
#14884=CARTESIAN_POINT('Ctrl Pts',(0.152746332292334,-0.0295154862350913,
1.07242011852912));
#14885=CARTESIAN_POINT('Ctrl Pts',(0.152044447913902,-0.0328469539985112,
1.07218046013581));
#14886=CARTESIAN_POINT('Ctrl Pts',(0.151874315636641,-0.0336248232116175,
1.072124223568));
#14887=CARTESIAN_POINT('Ctrl Pts',(0.151587175255337,-0.034891014769014,
1.07203221349378));
#14888=CARTESIAN_POINT('Ctrl Pts',(0.151473760009997,-0.0353801445893342,
1.07199655522128));
#14889=CARTESIAN_POINT('Ctrl Pts',(0.151250578989105,-0.0363219188264252,
1.07192767294409));
#14890=CARTESIAN_POINT('Ctrl Pts',(0.151141144320495,-0.0367746368654985,
1.07189445990069));
#14891=CARTESIAN_POINT('Ctrl Pts',(0.150885170755583,-0.0378131239575834,
1.0718180373986));
#14892=CARTESIAN_POINT('Ctrl Pts',(0.1507372517929,-0.0383985416424383,
1.07177478395101));
#14893=CARTESIAN_POINT('Ctrl Pts',(0.150333548822834,-0.0399579872764489,
1.07165909588471));
#14894=CARTESIAN_POINT('Ctrl Pts',(0.150071711740404,-0.0409304030697252,
1.07158646715413));
#14895=CARTESIAN_POINT('Ctrl Pts',(0.147918322892713,-0.0486291427657746,
1.07100746526774));
#14896=CARTESIAN_POINT('Ctrl Pts',(0.145585250760267,-0.0552225589933986,
1.07048676710374));
#14897=CARTESIAN_POINT('Ctrl Pts',(0.138752403217296,-0.0710550084938144,
1.06917379951877));
#14898=CARTESIAN_POINT('Ctrl Pts',(0.133765686062294,-0.0800484779595857,
1.06837052268306));
#14899=CARTESIAN_POINT('Ctrl Pts',(0.125770847161814,-0.0916073867786282,
1.06729026894513));
#14900=CARTESIAN_POINT('Ctrl Pts',(0.123497161338834,-0.0946502772148985,
1.06700107517324));
#14901=CARTESIAN_POINT('Ctrl Pts',(0.119863541997304,-0.0991589950937276,
1.06656832044312));
#14902=CARTESIAN_POINT('Ctrl Pts',(0.118583074845973,-0.100686793531841,
1.06642089617918));
#14903=CARTESIAN_POINT('Ctrl Pts',(0.116947108837644,-0.102564238848323,
1.06623917283221));
#14904=CARTESIAN_POINT('Ctrl Pts',(0.116618903470063,-0.102937265981192,
1.06620303824192));
#14905=CARTESIAN_POINT('Ctrl Pts',(0.11609545490084,-0.103526483069429,
1.06614592551476));
#14906=CARTESIAN_POINT('Ctrl Pts',(0.115901385961924,-0.103743703815122,
1.06612486247855));
#14907=CARTESIAN_POINT('Ctrl Pts',(0.1155334025084,-0.104153265159255,1.06608513617389));
#14908=CARTESIAN_POINT('Ctrl Pts',(0.115359619451581,-0.104345713566927,
1.06606646413134));
#14909=CARTESIAN_POINT('Ctrl Pts',(0.114960275617218,-0.104785732302075,
1.06602375862612));
#14910=CARTESIAN_POINT('Ctrl Pts',(0.114734396013438,-0.105033009293303,
1.06599974955649));
#14911=CARTESIAN_POINT('Ctrl Pts',(0.114130725738578,-0.10568959359255,
1.06593596655915));
#14912=CARTESIAN_POINT('Ctrl Pts',(0.113751527524001,-0.106097609597714,
1.06589629631628));
#14913=CARTESIAN_POINT('Ctrl Pts',(0.111032829077625,-0.108991589265561,
1.06561460110371));
#14914=CARTESIAN_POINT('Ctrl Pts',(0.108614020427173,-0.111402220634307,
1.06537824634035));
#14915=CARTESIAN_POINT('Ctrl Pts',(0.102257363715481,-0.11733332244437,
1.06478590157066));
#14916=CARTESIAN_POINT('Ctrl Pts',(0.0982159520673129,-0.120736539660136,
1.06443543904685));
#14917=CARTESIAN_POINT('Ctrl Pts',(0.0875729060468159,-0.128810126936401,
1.06355393235674));
#14918=CARTESIAN_POINT('Ctrl Pts',(0.0807665015236307,-0.133183442397176,
1.06302648001027));
#14919=CARTESIAN_POINT('Ctrl Pts',(0.0700365598773572,-0.138951523080993,
1.06220985634516));
#14920=CARTESIAN_POINT('Ctrl Pts',(0.0663465139486922,-0.140750777184016,
1.06193159544409));
#14921=CARTESIAN_POINT('Ctrl Pts',(0.0602671256429053,-0.143422848512658,
1.06147366750183));
#14922=CARTESIAN_POINT('Ctrl Pts',(0.0579198746834443,-0.144386726332588,
1.06129699407416));
#14923=CARTESIAN_POINT('Ctrl Pts',(0.0548138787475647,-0.145574251307052,
1.06106288825577));
#14924=CARTESIAN_POINT('Ctrl Pts',(0.0540754259205835,-0.145850170440064,
1.06100720668279));
#14925=CARTESIAN_POINT('Ctrl Pts',(0.052864892295059,-0.146292023098675,
1.06091587688621));
#14926=CARTESIAN_POINT('Ctrl Pts',(0.0523940448716134,-0.146461315407852,
1.06088034064395));
#14927=CARTESIAN_POINT('Ctrl Pts',(0.0514827469776956,-0.146784014082325,
1.06081153369587));
#14928=CARTESIAN_POINT('Ctrl Pts',(0.0510424066282559,-0.146937717225271,
1.06077827324443));
#14929=CARTESIAN_POINT('Ctrl Pts',(0.0500265810100475,-0.147287179332254,
1.0607015112467));
#14930=CARTESIAN_POINT('Ctrl Pts',(0.0494506294451958,-0.147481548782424,
1.06065796441789));
#14931=CARTESIAN_POINT('Ctrl Pts',(0.0479043451970216,-0.147993305538292,
1.06054097860186));
#14932=CARTESIAN_POINT('Ctrl Pts',(0.0469320170991188,-0.148304519322536,
1.06046733856679));
#14933=CARTESIAN_POINT('Ctrl Pts',(0.0387145581156659,-0.150845783481167,
1.05984422857643));
#14934=CARTESIAN_POINT('Ctrl Pts',(0.031319620478302,-0.152552659921158,
1.05927779558591));
#14935=CARTESIAN_POINT('Ctrl Pts',(0.0141675525319759,-0.155211810083501,
1.05795196677633));
#14936=CARTESIAN_POINT('Ctrl Pts',(0.00438468218431797,-0.155795321765404,
1.05718646470351));
#14937=CARTESIAN_POINT('Ctrl Pts',(-0.00908359376598436,-0.155328587943792,
1.05615132862355));
#14938=CARTESIAN_POINT('Ctrl Pts',(-0.0127744985669397,-0.155068689149605,
1.05586984441875));
#14939=CARTESIAN_POINT('Ctrl Pts',(-0.0184000582917418,-0.154470303649111,
1.05544723229978));
#14940=CARTESIAN_POINT('Ctrl Pts',(-0.0203432661095739,-0.154226422353404,
1.05530243735466));
#14941=CARTESIAN_POINT('Ctrl Pts',(-0.0227703244371664,-0.153875140326209,
1.05512349078963));
#14942=CARTESIAN_POINT('Ctrl Pts',(-0.023258848588846,-0.153802056116356,
1.05508756894396));
#14943=CARTESIAN_POINT('Ctrl Pts',(-0.0240342566423214,-0.153682274443948,
1.05503071492794));
#14944=CARTESIAN_POINT('Ctrl Pts',(-0.0243213663826324,-0.153637098747953,
1.05500969914258));
#14945=CARTESIAN_POINT('Ctrl Pts',(-0.0248645376653519,-0.153550071908389,
1.05497000959026));
#14946=CARTESIAN_POINT('Ctrl Pts',(-0.0251206178240656,-0.153508385366391,
1.05495132729294));
#14947=CARTESIAN_POINT('Ctrl Pts',(-0.0257081412498728,-0.153411234594297,
1.05490853065624));
#14948=CARTESIAN_POINT('Ctrl Pts',(-0.0260395099131109,-0.153355336899367,
1.0548844410755));
#14949=CARTESIAN_POINT('Ctrl Pts',(-0.0269234538962342,-0.153203279043141,
1.05482030293648));
#14950=CARTESIAN_POINT('Ctrl Pts',(-0.0274757016220419,-0.153105202149349,
1.05478035989851));
#14951=CARTESIAN_POINT('Ctrl Pts',(-0.0314650975034128,-0.152374421485862,
1.05449265718641));
#14952=CARTESIAN_POINT('Ctrl Pts',(-0.03488092383369,-0.151628963823294,
1.05425084321478));
#14953=CARTESIAN_POINT('Ctrl Pts',(-0.0433137369418515,-0.149488498295355,
1.05365857132373));
#14954=CARTESIAN_POINT('Ctrl Pts',(-0.0482913525893562,-0.147955547414858,
1.05331313684806));
#14955=CARTESIAN_POINT('Ctrl Pts',(-0.0607702538684128,-0.143415356197325,
1.0524369138624));
#14956=CARTESIAN_POINT('Ctrl Pts',(-0.0681307305130796,-0.140068504963997,
1.05190974114082));
#14957=CARTESIAN_POINT('Ctrl Pts',(-0.080612022054574,-0.133175654673393,
1.05095390104198));
#14958=CARTESIAN_POINT('Ctrl Pts',(-0.0858422056327382,-0.129865904897493,
1.05053207977654));
#14959=CARTESIAN_POINT('Ctrl Pts',(-0.091698278722626,-0.125651470789151,
1.05002604385517));
#14960=CARTESIAN_POINT('Ctrl Pts',(-0.0925294520410273,-0.125040660770912,
1.04995339073812));
#14961=CARTESIAN_POINT('Ctrl Pts',(-0.0937972728805838,-0.124089405488513,
1.04984125333863));
#14962=CARTESIAN_POINT('Ctrl Pts',(-0.0942382920711193,-0.123754811007321,
1.04980199703721));
#14963=CARTESIAN_POINT('Ctrl Pts',(-0.095038840145718,-0.123140686838785,
1.04973027781843));
#14964=CARTESIAN_POINT('Ctrl Pts',(-0.0953989470330005,-0.122861917567147,
1.04969784508377));
#14965=CARTESIAN_POINT('Ctrl Pts',(-0.0961819073568622,-0.122250287512484,
1.04962694949502));
#14966=CARTESIAN_POINT('Ctrl Pts',(-0.0966042666007759,-0.121916806719874,
1.04958846229534));
#14967=CARTESIAN_POINT('Ctrl Pts',(-0.09775496451879,-0.120998520172192,
1.04948293112828));
#14968=CARTESIAN_POINT('Ctrl Pts',(-0.0984797691577612,-0.12040934335774,
1.04941571275575));
#14969=CARTESIAN_POINT('Ctrl Pts',(-0.102109763473829,-0.11740390569505,
1.04907522485682));
#14970=CARTESIAN_POINT('Ctrl Pts',(-0.104931287377558,-0.114889082188782,
1.04879796829395));
#14971=CARTESIAN_POINT('Ctrl Pts',(-0.10919103813286,-0.110804464448972,
1.04835861563113));
#14972=CARTESIAN_POINT('Ctrl Pts',(-0.110693499877065,-0.10930352466307,
1.04819931522705));
#14973=CARTESIAN_POINT('Ctrl Pts',(-0.122272958236273,-0.0972521362867354,
1.04693699596424));
#14974=CARTESIAN_POINT('Ctrl Pts',(-0.130849422265921,-0.0853639515742955,
1.04578074713185));
#14975=CARTESIAN_POINT('Ctrl Pts',(-0.138929417834625,-0.070014527411993,
1.04447366457841));
#14976=CARTESIAN_POINT('Ctrl Pts',(-0.140149706544214,-0.0675387259033696,
1.04426830095686));
#14977=CARTESIAN_POINT('Ctrl Pts',(-0.141533135571074,-0.0645327479449565,
1.04402651454286));
#14978=CARTESIAN_POINT('Ctrl Pts',(-0.141760066509343,-0.0640327071862858,
1.04398654020616));
#14979=CARTESIAN_POINT('Ctrl Pts',(-0.142108010454061,-0.0632550988868648,
1.04392476972932));
#14980=CARTESIAN_POINT('Ctrl Pts',(-0.142230865920963,-0.0629783689376224,
1.04390286414137));
#14981=CARTESIAN_POINT('Ctrl Pts',(-0.142456758298112,-0.0624655175453418,
1.04386241192416));
#14982=CARTESIAN_POINT('Ctrl Pts',(-0.142560015706833,-0.0622295009676079,
1.0438438523141));
#14983=CARTESIAN_POINT('Ctrl Pts',(-0.1427914799433,-0.0616968409654128,
1.04380209238037));
#14984=CARTESIAN_POINT('Ctrl Pts',(-0.142919348705197,-0.0614000545629998,
1.04377891277425));
#14985=CARTESIAN_POINT('Ctrl Pts',(-0.14324511842001,-0.0606374037818408,
1.04371956859916));
#14986=CARTESIAN_POINT('Ctrl Pts',(-0.143441674222118,-0.060170963128615,
1.04368348379786));
#14987=CARTESIAN_POINT('Ctrl Pts',(-0.144593446739929,-0.0574000071597424,
1.04347031321858));
#14988=CARTESIAN_POINT('Ctrl Pts',(-0.145495460382989,-0.0550735741235107,
1.04329623015511));
#14989=CARTESIAN_POINT('Ctrl Pts',(-0.150654583141779,-0.0407544870207453,
1.04224836769704));
#14990=CARTESIAN_POINT('Ctrl Pts',(-0.153483136687386,-0.0282973266317507,
1.04143322562587));
#14991=CARTESIAN_POINT('Ctrl Pts',(-0.155285119331868,-0.0104587456189201,
1.04024137622979));
#14992=CARTESIAN_POINT('Ctrl Pts',(-0.155547943927636,-0.00526147652008941,
1.03989176974618));
#14993=CARTESIAN_POINT('Ctrl Pts',(-0.155550304046007,0.00074293371199677,
1.03947950815874));
#14994=CARTESIAN_POINT('Ctrl Pts',(-0.155544385392344,0.00154698563916683,
1.03942413272929));
#14995=CARTESIAN_POINT('Ctrl Pts',(-0.155519543941367,0.00319043249726224,
1.03931057288901));
#14996=CARTESIAN_POINT('Ctrl Pts',(-0.155500058275444,0.0040297938030437,
1.03925237420997));
#14997=CARTESIAN_POINT('Ctrl Pts',(-0.155421679500313,0.00653256384603913,
1.03907819969411));
#14998=CARTESIAN_POINT('Ctrl Pts',(-0.155342883500902,0.00819518279790847,
1.0389616482437));
#14999=CARTESIAN_POINT('Ctrl Pts',(-0.155193655213519,0.0105455716828021,
1.03879554745463));
#15000=CARTESIAN_POINT('Ctrl Pts',(-0.155145292663299,0.0112346712151309,
1.03874668659369));
#15001=CARTESIAN_POINT('Ctrl Pts',(-0.155059257330732,0.0123537650580931,
1.03866706293629));
#15002=CARTESIAN_POINT('Ctrl Pts',(-0.155024381570459,0.012783970701975,
1.03863638792337));
#15003=CARTESIAN_POINT('Ctrl Pts',(-0.154947636149121,0.0136841203952315,
1.03857206381552));
#15004=CARTESIAN_POINT('Ctrl Pts',(-0.154905418043876,0.0141540294905362,
1.03853840411779));
#15005=CARTESIAN_POINT('Ctrl Pts',(-0.154799912420558,0.0152713031239057,
1.03845817866608));
#15006=CARTESIAN_POINT('Ctrl Pts',(-0.154734701321405,0.0159184725298402,
1.03841155307539));
#15007=CARTESIAN_POINT('Ctrl Pts',(-0.154501464116133,0.0180961536281239,
1.03825412354951));
#15008=CARTESIAN_POINT('Ctrl Pts',(-0.154314777935465,0.0196245301591377,
1.03814273739566));
#15009=CARTESIAN_POINT('Ctrl Pts',(-0.153177925353005,0.027908054748001,
1.03753396069297));
#15010=CARTESIAN_POINT('Ctrl Pts',(-0.15180699820084,0.0345969160339381,
1.03702347618112));
#15011=CARTESIAN_POINT('Ctrl Pts',(-0.146992244641157,0.0521378965533142,
1.03563505623994));
#15012=CARTESIAN_POINT('Ctrl Pts',(-0.142789835132019,0.0627385163250416,
1.03474117253609));
#15013=CARTESIAN_POINT('Ctrl Pts',(-0.137084250266438,0.0735145576289548,
1.03381248727888));
#15014=CARTESIAN_POINT('Ctrl Pts',(-0.136692780018179,0.0742399204835402,
1.03374988908897));
#15015=CARTESIAN_POINT('Ctrl Pts',(-0.134756038515252,0.077761287729729,
1.03344568520926));
#15016=CARTESIAN_POINT('Ctrl Pts',(-0.133130508350137,0.0805126035024925,
1.03320702448004));
#15017=CARTESIAN_POINT('Ctrl Pts',(-0.131129005210508,0.0836736811500931,
1.03293328622031));
#15018=CARTESIAN_POINT('Ctrl Pts',(-0.130834333783726,0.0841336915384147,
1.03289346315085));
#15019=CARTESIAN_POINT('Ctrl Pts',(-0.130356825132937,0.0848705526022756,
1.03282970467976));
#15020=CARTESIAN_POINT('Ctrl Pts',(-0.130175518600981,0.0851483817831765,
1.03280567218244));
#15021=CARTESIAN_POINT('Ctrl Pts',(-0.129851136339618,0.0856419985902897,
1.03276298976655));
#15022=CARTESIAN_POINT('Ctrl Pts',(-0.129708409410495,0.0858580110617567,
1.03274431702986));
#15023=CARTESIAN_POINT('Ctrl Pts',(-0.129402926228979,0.0863178493697545,
1.03270457997533));
#15024=CARTESIAN_POINT('Ctrl Pts',(-0.129240020209961,0.0865615712452648,
1.03268352596436));
#15025=CARTESIAN_POINT('Ctrl Pts',(-0.128794463471499,0.0872241019831028,
1.03262630853718));
#15026=CARTESIAN_POINT('Ctrl Pts',(-0.12851045623412,0.0876420016041505,
1.0325902349196));
#15027=CARTESIAN_POINT('Ctrl Pts',(-0.127036443167708,0.0897883522852053,
1.03240500526207));
#15028=CARTESIAN_POINT('Ctrl Pts',(-0.125813511017835,0.0914940856854288,
1.03225795500926));
#15029=CARTESIAN_POINT('Ctrl Pts',(-0.122099379454723,0.0964591554942415,
1.03182866613633));
#15030=CARTESIAN_POINT('Ctrl Pts',(-0.119513235456922,0.0996454684090201,
1.03155150908419));
#15031=CARTESIAN_POINT('Ctrl Pts',(-0.10992207231965,0.110551032666018,
1.03058196476839));
#15032=CARTESIAN_POINT('Ctrl Pts',(-0.102271325088489,0.117664688174515,
1.02990834360504));
#15033=CARTESIAN_POINT('Ctrl Pts',(-0.0888470525279429,0.127840813923076,
1.02878131596413));
#15034=CARTESIAN_POINT('Ctrl Pts',(-0.0834926896625997,0.131400251833672,
1.02834409311594));
#15035=CARTESIAN_POINT('Ctrl Pts',(-0.0770749002046541,0.135115683781773,
1.02782449295394));
#15036=CARTESIAN_POINT('Ctrl Pts',(-0.0762109318635579,0.135604874650322,
1.02775464162569));
#15037=CARTESIAN_POINT('Ctrl Pts',(-0.0748177402280161,0.136376199647507,
1.02764212760664));
#15038=CARTESIAN_POINT('Ctrl Pts',(-0.0742914549166371,0.13666360814519,
1.02759965311995));
#15039=CARTESIAN_POINT('Ctrl Pts',(-0.0733540270983685,0.137168529731964,
1.02752404016595));
#15040=CARTESIAN_POINT('Ctrl Pts',(-0.0729435435536719,0.137387256634697,
1.02749094517889));
#15041=CARTESIAN_POINT('Ctrl Pts',(-0.0720862412349883,0.137839146596797,
1.02742185272222));
#15042=CARTESIAN_POINT('Ctrl Pts',(-0.0716392586049876,0.138071985302678,
1.02738584429824));
#15043=CARTESIAN_POINT('Ctrl Pts',(-0.0704755970230742,0.138670979012717,
1.02729213545477));
#15044=CARTESIAN_POINT('Ctrl Pts',(-0.0697572018836638,0.139033747472617,
1.02723431727667));
#15045=CARTESIAN_POINT('Ctrl Pts',(-0.0672695769006429,0.140265791643921,
1.02703419969377));
#15046=CARTESIAN_POINT('Ctrl Pts',(-0.0654867846816166,0.141106938634866,
1.02689093980976));
#15047=CARTESIAN_POINT('Ctrl Pts',(-0.0636886257384703,0.141913922683946,
1.02674653231234));
#15048=CARTESIAN_POINT('',(-0.155549929113474,0.000137046190443996,1.02555842627611));
#15049=CARTESIAN_POINT('Ctrl Pts',(-0.063688626060837,0.141913922539273,
1.01289638536134));
#15050=CARTESIAN_POINT('Ctrl Pts',(-0.0647860609483699,0.141421411875573,
1.01297710100986));
#15051=CARTESIAN_POINT('Ctrl Pts',(-0.0658778700550637,0.140916132225413,
1.01305747580239));
#15052=CARTESIAN_POINT('Ctrl Pts',(-0.0760690842855253,0.136055365930432,
1.01380936440437));
#15053=CARTESIAN_POINT('Ctrl Pts',(-0.0847302227510347,0.130837162779552,
1.01446245564984));
#15054=CARTESIAN_POINT('Ctrl Pts',(-0.0952273593882092,0.123030541893768,
1.01533815688697));
#15055=CARTESIAN_POINT('Ctrl Pts',(-0.0975773191783891,0.121175201413414,
1.01554017014227));
#15056=CARTESIAN_POINT('Ctrl Pts',(-0.102650124851414,0.116926830655957,
1.01599176444776));
#15057=CARTESIAN_POINT('Ctrl Pts',(-0.105345713945323,0.114504187027946,
1.01624227641435));
#15058=CARTESIAN_POINT('Ctrl Pts',(-0.108617462215164,0.111350340665435,
1.016561467905));
#15059=CARTESIAN_POINT('Ctrl Pts',(-0.109275120327414,0.110705011072708,
1.01662643313479));
#15060=CARTESIAN_POINT('Ctrl Pts',(-0.110305605145272,0.109675714431107,
1.01672953292112));
#15061=CARTESIAN_POINT('Ctrl Pts',(-0.110682257903037,0.109295592934538,
1.01676749802043));
#15062=CARTESIAN_POINT('Ctrl Pts',(-0.111378872258385,0.108585269341235,
1.01683824409808));
#15063=CARTESIAN_POINT('Ctrl Pts',(-0.111699346758633,0.108255576432907,
1.01687100214167));
#15064=CARTESIAN_POINT('Ctrl Pts',(-0.112323589949379,0.107607653929309,
1.01693522953592));
#15065=CARTESIAN_POINT('Ctrl Pts',(-0.112627479845196,0.107289546646727,
1.01696669319418));
#15066=CARTESIAN_POINT('Ctrl Pts',(-0.113517513823187,0.106349924313232,
1.01705942952358));
#15067=CARTESIAN_POINT('Ctrl Pts',(-0.114099883571762,0.105724873425555,
1.01712086294045));
#15068=CARTESIAN_POINT('Ctrl Pts',(-0.116964830475933,0.102598716268135,
1.01742689602063));
#15069=CARTESIAN_POINT('Ctrl Pts',(-0.119170294333364,0.100028524794018,
1.01767469167025));
#15070=CARTESIAN_POINT('Ctrl Pts',(-0.125196932601442,0.0925228114824073,
1.01838852799206));
#15071=CARTESIAN_POINT('Ctrl Pts',(-0.128807067184689,0.0874269130915619,
1.01886202898012));
#15072=CARTESIAN_POINT('Ctrl Pts',(-0.13395178446543,0.0791518038537113,
1.0196115992907));
#15073=CARTESIAN_POINT('Ctrl Pts',(-0.135701272316662,0.0761134159306673,
1.0198829829854));
#15074=CARTESIAN_POINT('Ctrl Pts',(-0.13980491859699,0.0683945368410447,
1.02056082806488));
#15075=CARTESIAN_POINT('Ctrl Pts',(-0.142028237974713,0.0636491242664318,
1.02096743996051));
#15076=CARTESIAN_POINT('Ctrl Pts',(-0.144383867333696,0.0578799616989279,
1.02144466275083));
#15077=CARTESIAN_POINT('Ctrl Pts',(-0.144750897720426,0.0569558495145081,
1.02152059276024));
#15078=CARTESIAN_POINT('Ctrl Pts',(-0.14649447471692,0.0524401144942479,
1.02188896295792));
#15079=CARTESIAN_POINT('Ctrl Pts',(-0.147746487837052,0.0488014171157882,
1.02217764892268));
#15080=CARTESIAN_POINT('Ctrl Pts',(-0.149045187578953,0.0445166442764345,
1.02250544703461));
#15081=CARTESIAN_POINT('Ctrl Pts',(-0.149224303425284,0.0439124909539369,
1.02255138919605));
#15082=CARTESIAN_POINT('Ctrl Pts',(-0.149489963520654,0.0429960266407157,
1.02262064426518));
#15083=CARTESIAN_POINT('Ctrl Pts',(-0.14957920839652,0.0426845161735899,
1.0226441083061));
#15084=CARTESIAN_POINT('Ctrl Pts',(-0.149737650714609,0.0421248716764276,
1.02268612343052));
#15085=CARTESIAN_POINT('Ctrl Pts',(-0.149807205442616,0.041876843913858,
1.0227046948792));
#15086=CARTESIAN_POINT('Ctrl Pts',(-0.149956941572525,0.041337746915761,
1.02274495363199));
#15087=CARTESIAN_POINT('Ctrl Pts',(-0.150036891607409,0.0410466174838701,
1.02276662741799));
#15088=CARTESIAN_POINT('Ctrl Pts',(-0.150199845258332,0.0404464016318723,
1.02281117704768));
#15089=CARTESIAN_POINT('Ctrl Pts',(-0.150282743698556,0.0401372877994007,
1.02283404684204));
#15090=CARTESIAN_POINT('Ctrl Pts',(-0.1504922043831,0.0393464984929881,
1.02289237105019));
#15091=CARTESIAN_POINT('Ctrl Pts',(-0.150617409745395,0.0388644622096398,
1.02292775074723));
#15092=CARTESIAN_POINT('Ctrl Pts',(-0.150974076895866,0.0374636920773357,
1.02303008434339));
#15093=CARTESIAN_POINT('Ctrl Pts',(-0.151199467838778,0.0365434146561254,
1.02309672042778));
#15094=CARTESIAN_POINT('Ctrl Pts',(-0.154152104867538,0.0239924909809659,
1.02399816488502));
#15095=CARTESIAN_POINT('Ctrl Pts',(-0.155539404807646,0.0120860470003205,
1.02476979575327));
#15096=CARTESIAN_POINT('Ctrl Pts',(-0.155549939545188,0.000137140396363124,
1.02555840182376));
#15097=CARTESIAN_POINT('Ctrl Pts',(-0.155549939629264,0.000137045001298319,
1.02555840811966));
#15098=CARTESIAN_POINT('Ctrl Pts',(-0.15555638673202,-0.00718059836358552,
1.02604135928988));
#15099=CARTESIAN_POINT('Ctrl Pts',(-0.155046468706238,-0.0144890321433455,
1.02652860014069));
#15100=CARTESIAN_POINT('Ctrl Pts',(-0.153657490307648,-0.0243323487880368,
1.02721131832332));
#15101=CARTESIAN_POINT('Ctrl Pts',(-0.153225198880862,-0.0269207088545793,
1.0273933055807));
#15102=CARTESIAN_POINT('Ctrl Pts',(-0.152589172553378,-0.0302139105113054,
1.02762857309124));
#15103=CARTESIAN_POINT('Ctrl Pts',(-0.152445622439239,-0.0309300523082306,
1.02767996051711));
#15104=CARTESIAN_POINT('Ctrl Pts',(-0.152193820717065,-0.0321418860646949,
1.02776731336339));
#15105=CARTESIAN_POINT('Ctrl Pts',(-0.152088176654594,-0.0326381129224696,
1.02780319605185));
#15106=CARTESIAN_POINT('Ctrl Pts',(-0.151888104592615,-0.0335558152533673,
1.02786976999309));
#15107=CARTESIAN_POINT('Ctrl Pts',(-0.151794344794366,-0.0339774327406821,
1.02790043971062));
#15108=CARTESIAN_POINT('Ctrl Pts',(-0.151596719587348,-0.0348489644006529,
1.02796401393735));
#15109=CARTESIAN_POINT('Ctrl Pts',(-0.151492604511346,-0.0352988169683653,
1.02799692615122));
#15110=CARTESIAN_POINT('Ctrl Pts',(-0.151252241920828,-0.0363167046911205,
1.02807162169078));
#15111=CARTESIAN_POINT('Ctrl Pts',(-0.151114795156655,-0.036884446494989,
1.02811344310804));
#15112=CARTESIAN_POINT('Ctrl Pts',(-0.150699234371018,-0.0385596562193391,
1.02823732199884));
#15113=CARTESIAN_POINT('Ctrl Pts',(-0.150412125425806,-0.0396648298038098,
1.02831966747295));
#15114=CARTESIAN_POINT('Ctrl Pts',(-0.147808877674448,-0.0492506161193129,
1.02903945206169));
#15115=CARTESIAN_POINT('Ctrl Pts',(-0.144790268005165,-0.0575222821753394,
1.02969993143085));
#15116=CARTESIAN_POINT('Ctrl Pts',(-0.138594862237303,-0.0708687962269089,
1.03083027615649));
#15117=CARTESIAN_POINT('Ctrl Pts',(-0.135794596768898,-0.0760969462009458,
1.03129090727525));
#15118=CARTESIAN_POINT('Ctrl Pts',(-0.128882948186217,-0.0873990998547369,
1.03231709409162));
#15119=CARTESIAN_POINT('Ctrl Pts',(-0.124626065847134,-0.0933690903900244,
1.03288068852961));
#15120=CARTESIAN_POINT('Ctrl Pts',(-0.119258877614252,-0.0998716635760938,
1.03350340387367));
#15121=CARTESIAN_POINT('Ctrl Pts',(-0.118544748090849,-0.100718280188701,
1.03358465558085));
#15122=CARTESIAN_POINT('Ctrl Pts',(-0.11761931029254,-0.10179192676455,
1.03368784540701));
#15123=CARTESIAN_POINT('Ctrl Pts',(-0.117416307608891,-0.102026022269235,
1.0337103539049));
#15124=CARTESIAN_POINT('Ctrl Pts',(-0.117018844857276,-0.102481604769332,
1.03375417397945));
#15125=CARTESIAN_POINT('Ctrl Pts',(-0.116824452234789,-0.102703148597403,
1.03377549026883));
#15126=CARTESIAN_POINT('Ctrl Pts',(-0.116458377500567,-0.103117969520258,
1.03381541438236));
#15127=CARTESIAN_POINT('Ctrl Pts',(-0.11628684535156,-0.10331136882119,
1.0338340322998));
#15128=CARTESIAN_POINT('Ctrl Pts',(-0.11589228745911,-0.103753997795884,
1.03387665413083));
#15129=CARTESIAN_POINT('Ctrl Pts',(-0.115668939709457,-0.104002936224478,
1.03390063358425));
#15130=CARTESIAN_POINT('Ctrl Pts',(-0.115080513889742,-0.104654542373605,
1.0339634294704));
#15131=CARTESIAN_POINT('Ctrl Pts',(-0.114714120861869,-0.105056025123374,
1.03400214971291));
#15132=CARTESIAN_POINT('Ctrl Pts',(-0.11221541397595,-0.107765376097631,
1.03426371397184));
#15133=CARTESIAN_POINT('Ctrl Pts',(-0.110015509031068,-0.110010303150013,
1.03448176231003));
#15134=CARTESIAN_POINT('Ctrl Pts',(-0.103903846574431,-0.115880177176948,
1.03506079674051));
#15135=CARTESIAN_POINT('Ctrl Pts',(-0.0998711563501876,-0.11937330497986,
1.03541523746203));
#15136=CARTESIAN_POINT('Ctrl Pts',(-0.0900258171908573,-0.127052481858011,
1.03623970143847));
#15137=CARTESIAN_POINT('Ctrl Pts',(-0.0840882067401964,-0.131057820393929,
1.03670708353823));
#15138=CARTESIAN_POINT('Ctrl Pts',(-0.0736789606190546,-0.137080086506898,
1.0375082964557));
#15139=CARTESIAN_POINT('Ctrl Pts',(-0.0693498745563778,-0.139320234349415,
1.03783661039076));
#15140=CARTESIAN_POINT('Ctrl Pts',(-0.0623248513823275,-0.142546800669475,
1.03836803899733));
#15141=CARTESIAN_POINT('Ctrl Pts',(-0.0596943554125757,-0.143668227518083,
1.03856671905054));
#15142=CARTESIAN_POINT('Ctrl Pts',(-0.0562665431508622,-0.145019171648208,
1.03882593928562));
#15143=CARTESIAN_POINT('Ctrl Pts',(-0.0554961110168068,-0.145315744634239,
1.0388842206676));
#15144=CARTESIAN_POINT('Ctrl Pts',(-0.0543164782900724,-0.14575908764223,
1.03897350248566));
#15145=CARTESIAN_POINT('Ctrl Pts',(-0.0539089534078625,-0.145910301828275,
1.03900435465503));
#15146=CARTESIAN_POINT('Ctrl Pts',(-0.0531124012079008,-0.146202073976774,
1.03906467729382));
#15147=CARTESIAN_POINT('Ctrl Pts',(-0.0527234361511966,-0.146342792345662,
1.0390941421451));
#15148=CARTESIAN_POINT('Ctrl Pts',(-0.0518256092848952,-0.146663560846093,
1.03916217674319));
#15149=CARTESIAN_POINT('Ctrl Pts',(-0.0513163648635911,-0.146842516123313,
1.03920078233914));
#15150=CARTESIAN_POINT('Ctrl Pts',(-0.0499162159752346,-0.147326374271991,
1.03930697869207));
#15151=CARTESIAN_POINT('Ctrl Pts',(-0.0490234709920573,-0.147625839177458,
1.03937474757955));
#15152=CARTESIAN_POINT('Ctrl Pts',(-0.044445477679734,-0.149115389190766,
1.03972261090321));
#15153=CARTESIAN_POINT('Ctrl Pts',(-0.0407197456305465,-0.150175554462964,
1.04000690180176));
#15154=CARTESIAN_POINT('Ctrl Pts',(-0.0239888927808989,-0.154267994572837,
1.04129016625844));
#15155=CARTESIAN_POINT('Ctrl Pts',(-0.0106659611612102,-0.155756875866865,
1.0423361013792));
#15156=CARTESIAN_POINT('Ctrl Pts',(0.00817651927052412,-0.155432200473962,
1.04378662559924));
#15157=CARTESIAN_POINT('Ctrl Pts',(0.0136649733281473,-0.155046147179955,
1.04420466206531));
#15158=CARTESIAN_POINT('Ctrl Pts',(0.0199782635207121,-0.154264110596041,
1.04467259664815));
#15159=CARTESIAN_POINT('Ctrl Pts',(0.0208335953327372,-0.154150926783172,
1.0447357133346));
#15160=CARTESIAN_POINT('Ctrl Pts',(0.0220571587866953,-0.153978645438524,
1.04482556035108));
#15161=CARTESIAN_POINT('Ctrl Pts',(0.0224261676963277,-0.153925334221279,
1.04485259916815));
#15162=CARTESIAN_POINT('Ctrl Pts',(0.0230565395317354,-0.153831948554754,
1.04489868636746));
#15163=CARTESIAN_POINT('Ctrl Pts',(0.0233179969262047,-0.153792533742621,
1.04491777153483));
#15164=CARTESIAN_POINT('Ctrl Pts',(0.0238205546847454,-0.153715461873917,
1.04495439617364));
#15165=CARTESIAN_POINT('Ctrl Pts',(0.024061667327688,-0.153677904112031,
1.04497194130618));
#15166=CARTESIAN_POINT('Ctrl Pts',(0.0247031289444782,-0.153576437911108,
1.04501855117061));
#15167=CARTESIAN_POINT('Ctrl Pts',(0.0251033219348603,-0.153511530833782,
1.04504755983632));
#15168=CARTESIAN_POINT('Ctrl Pts',(0.0265378143113057,-0.153273111714175,
1.04515130472308));
#15169=CARTESIAN_POINT('Ctrl Pts',(0.0275706380732488,-0.153090700039239,
1.04522555837581));
#15170=CARTESIAN_POINT('Ctrl Pts',(0.0289267396891793,-0.152837023207303,
1.04532256690412));
#15171=CARTESIAN_POINT('Ctrl Pts',(0.0292517129266021,-0.15277515906515,
1.0453457769324));
#15172=CARTESIAN_POINT('Ctrl Pts',(0.0306709667188219,-0.152500285615089,
1.04544699061635));
#15173=CARTESIAN_POINT('Ctrl Pts',(0.0317631688852504,-0.152276546373705,
1.0455244872103));
#15174=CARTESIAN_POINT('Ctrl Pts',(0.047402082307416,-0.148897303309184,
1.0466297226484));
#15175=CARTESIAN_POINT('Ctrl Pts',(0.0614263248973267,-0.14368122410808,
1.04757244456601));
#15176=CARTESIAN_POINT('Ctrl Pts',(0.0779899716290621,-0.134644721141109,
1.04883869988228));
#15177=CARTESIAN_POINT('Ctrl Pts',(0.0814084843795106,-0.132605774035906,
1.04910877983507));
#15178=CARTESIAN_POINT('Ctrl Pts',(0.0868251284683801,-0.129086612970358,
1.04955445353322));
#15179=CARTESIAN_POINT('Ctrl Pts',(0.0888726438301031,-0.127685584766996,
1.04972725785172));
#15180=CARTESIAN_POINT('Ctrl Pts',(0.0915201024552387,-0.125779507292003,
1.04995695163857));
#15181=CARTESIAN_POINT('Ctrl Pts',(0.092151054125934,-0.125317982713782,
1.05001217284377));
#15182=CARTESIAN_POINT('Ctrl Pts',(0.0931788548844407,-0.124554214339172,
1.05010293110671));
#15183=CARTESIAN_POINT('Ctrl Pts',(0.0935777821293927,-0.124254778533468,
1.05013835882304));
#15184=CARTESIAN_POINT('Ctrl Pts',(0.0943472287041001,-0.12367142284037,
1.0502070861079));
#15185=CARTESIAN_POINT('Ctrl Pts',(0.0947179242917529,-0.123387743316071,
1.05024037599956));
#15186=CARTESIAN_POINT('Ctrl Pts',(0.0955708971304279,-0.122728886044468,
1.05031739504716));
#15187=CARTESIAN_POINT('Ctrl Pts',(0.0960522490324654,-0.122352528719732,
1.05036117053008));
#15188=CARTESIAN_POINT('Ctrl Pts',(0.0973406894648549,-0.121332839474084,
1.05047919589814));
#15189=CARTESIAN_POINT('Ctrl Pts',(0.0981436005974994,-0.120684304392054,
1.05055365254962));
#15190=CARTESIAN_POINT('Ctrl Pts',(0.105252511557614,-0.114824368025818,
1.05122116184318));
#15191=CARTESIAN_POINT('Ctrl Pts',(0.111143566069588,-0.109131990173809,
1.05183409310911));
#15192=CARTESIAN_POINT('Ctrl Pts',(0.12137141947274,-0.0975581665313749,
1.05301740366399));
#15193=CARTESIAN_POINT('Ctrl Pts',(0.125796107690552,-0.0917820685073719,
1.05358329161818));
#15194=CARTESIAN_POINT('Ctrl Pts',(0.133652426975203,-0.0798854723415791,
1.05468597355418));
#15195=CARTESIAN_POINT('Ctrl Pts',(0.137107274774414,-0.0737989238872712,
1.05522173388818));
#15196=CARTESIAN_POINT('Ctrl Pts',(0.140506342900226,-0.0667418752230778,
1.05579751233231));
#15197=CARTESIAN_POINT('Ctrl Pts',(0.140865279488935,-0.0659809322687426,
1.05585902504274));
#15198=CARTESIAN_POINT('Ctrl Pts',(0.141368859449671,-0.0648905038175394,
1.05594632085494));
#15199=CARTESIAN_POINT('Ctrl Pts',(0.141518552544912,-0.0645633890100181,
1.05597239984413));
#15200=CARTESIAN_POINT('Ctrl Pts',(0.141775337618558,-0.0639970688885476,
1.05601735811322));
#15201=CARTESIAN_POINT('Ctrl Pts',(0.141882961727943,-0.0637581081819211,
1.0560362697451));
#15202=CARTESIAN_POINT('Ctrl Pts',(0.142091022322258,-0.0632930098663629,
1.0560729629802));
#15203=CARTESIAN_POINT('Ctrl Pts',(0.14219152308005,-0.0630669048634031,
1.05609074865594));
#15204=CARTESIAN_POINT('Ctrl Pts',(0.142462339179833,-0.0624536890412416,
1.05613884529386));
#15205=CARTESIAN_POINT('Ctrl Pts',(0.142631617724237,-0.0620661179397875,
1.05616909344945));
#15206=CARTESIAN_POINT('Ctrl Pts',(0.143260170546572,-0.060610864462488,
1.05628212449736));
#15207=CARTESIAN_POINT('Ctrl Pts',(0.143709070050202,-0.059538699647432,
1.0563643048027));
#15208=CARTESIAN_POINT('Ctrl Pts',(0.147448148468797,-0.0503194295806551,
1.05706246195061));
#15209=CARTESIAN_POINT('Ctrl Pts',(0.150055099039325,-0.0419108167251852,
1.05764330628785));
#15210=CARTESIAN_POINT('Ctrl Pts',(0.153916072896132,-0.0243080105455735,
1.05883034463277));
#15211=CARTESIAN_POINT('Ctrl Pts',(0.15508714616739,-0.0151326586777039,
1.05943450274364));
#15212=CARTESIAN_POINT('Ctrl Pts',(0.155601387929949,-0.00160304465676362,
1.06035399711173));
#15213=CARTESIAN_POINT('Ctrl Pts',(0.155586088778054,0.00270644086793452,
1.06065087361816));
#15214=CARTESIAN_POINT('Ctrl Pts',(0.155349709937214,0.00794672527266573,
1.06101928921471));
#15215=CARTESIAN_POINT('Ctrl Pts',(0.155298951399112,0.00888360544141311,
1.06108544202211));
#15216=CARTESIAN_POINT('Ctrl Pts',(0.155206049001805,0.010352262687595,
1.06118961680611));
#15217=CARTESIAN_POINT('Ctrl Pts',(0.155169639421713,0.0108843915012997,
1.06122745931737));
#15218=CARTESIAN_POINT('Ctrl Pts',(0.155100138035701,0.0118288103339126,
1.06129479981587));
#15219=CARTESIAN_POINT('Ctrl Pts',(0.155068137072414,0.0122411776981126,
1.06132426336619));
#15220=CARTESIAN_POINT('Ctrl Pts',(0.15499047865882,0.0131926788158454,
1.06139238958401));
#15221=CARTESIAN_POINT('Ctrl Pts',(0.154943652346649,0.0137317090357788,
1.06143108852619));
#15222=CARTESIAN_POINT('Ctrl Pts',(0.154807111791426,0.0152137417484865,
1.06153778451709));
#15223=CARTESIAN_POINT('Ctrl Pts',(0.154711595621551,0.0161561723702731,
1.06160596246047));
#15224=CARTESIAN_POINT('Ctrl Pts',(0.154174160474704,0.0210159911292765,
1.0619592908737));
#15225=CARTESIAN_POINT('Ctrl Pts',(0.153592081076033,0.02491608052403,1.06224879629655));
#15226=CARTESIAN_POINT('Ctrl Pts',(0.152497251361756,0.0307292486535779,
1.06268976956176));
#15227=CARTESIAN_POINT('Ctrl Pts',(0.152095063209109,0.0326617445901642,
1.06283794475441));
#15228=CARTESIAN_POINT('Ctrl Pts',(0.148397923695127,0.0488733426306351,
1.06409413651517));
#15229=CARTESIAN_POINT('Ctrl Pts',(0.143137722902858,0.0626263656406572,
1.06525590161234));
#15230=CARTESIAN_POINT('Ctrl Pts',(0.134738491699489,0.0777718093808967,
1.06655970121872));
#15231=CARTESIAN_POINT('Ctrl Pts',(0.133385148051825,0.0800707192484765,
1.06675804369127));
#15232=CARTESIAN_POINT('Ctrl Pts',(0.131685488591,0.0827951094216,1.06699264285331));
#15233=CARTESIAN_POINT('Ctrl Pts',(0.131395311181108,0.0832548513477145,
1.06703221547851));
#15234=CARTESIAN_POINT('Ctrl Pts',(0.130940450828424,0.0839672064189209,
1.06709349558014));
#15235=CARTESIAN_POINT('Ctrl Pts',(0.130777437561475,0.0842208717956763,
1.06711530983263));
#15236=CARTESIAN_POINT('Ctrl Pts',(0.130473775096756,0.0846903942935624,
1.06715567122704));
#15237=CARTESIAN_POINT('Ctrl Pts',(0.130333328578934,0.0849063739482967,
1.06717423093138));
#15238=CARTESIAN_POINT('Ctrl Pts',(0.130014746267877,0.0853936389680652,
1.06721608918345));
#15239=CARTESIAN_POINT('Ctrl Pts',(0.129836298049103,0.0856647158252774,
1.06723936653524));
#15240=CARTESIAN_POINT('Ctrl Pts',(0.129307602782967,0.086462398428511,
1.06730784215413));
#15241=CARTESIAN_POINT('Ctrl Pts',(0.128954985250558,0.0869874375709762,
1.06735288565789));
#15242=CARTESIAN_POINT('Ctrl Pts',(0.126402072990087,0.0907390222725643,
1.06767465291229));
#15243=CARTESIAN_POINT('Ctrl Pts',(0.124083924370035,0.0938841865071074,
1.06794396832215));
#15244=CARTESIAN_POINT('Ctrl Pts',(0.120883022390932,0.0979010234299841,
1.06829220904676));
#15245=CARTESIAN_POINT('Ctrl Pts',(0.120105060143235,0.0988538828532884,
1.06837514926172));
#15246=CARTESIAN_POINT('Ctrl Pts',(0.109794580690215,0.1111808903071,1.06945397985748));
#15247=CARTESIAN_POINT('Ctrl Pts',(0.0986936807561965,0.121142998892111,
1.07039962773869));
#15248=CARTESIAN_POINT('Ctrl Pts',(0.0836236490103462,0.13120070260349,
1.0716405631523));
#15249=CARTESIAN_POINT('Ctrl Pts',(0.0808416115047966,0.132932953776351,
1.07186770146406));
#15250=CARTESIAN_POINT('Ctrl Pts',(0.0772618433269091,0.135007970601706,
1.07215865035472));
#15251=CARTESIAN_POINT('Ctrl Pts',(0.0765130053908597,0.135433764301552,
1.07221944023647));
#15252=CARTESIAN_POINT('Ctrl Pts',(0.0753096377071011,0.136104840760534,
1.07231703206297));
#15253=CARTESIAN_POINT('Ctrl Pts',(0.0748573478585455,0.136354122306217,
1.07235369071308));
#15254=CARTESIAN_POINT('Ctrl Pts',(0.073998234657351,0.136822063573469,
1.07242328656145));
#15255=CARTESIAN_POINT('Ctrl Pts',(0.0735916615311184,0.137041173220109,
1.0724562073157));
#15256=CARTESIAN_POINT('Ctrl Pts',(0.0726677382375444,0.137533795039334,
1.07253098744599));
#15257=CARTESIAN_POINT('Ctrl Pts',(0.0721498108724101,0.137806203533238,
1.07257288525258));
#15258=CARTESIAN_POINT('Ctrl Pts',(0.0706123965769501,0.138603777354705,
1.07269719804892));
#15259=CARTESIAN_POINT('Ctrl Pts',(0.0695886451013722,0.139120587941932,
1.0727799040547));
#15260=CARTESIAN_POINT('Ctrl Pts',(0.0598130626881689,0.143920603518945,
1.07356912409087));
#15261=CARTESIAN_POINT('Ctrl Pts',(0.0506844926983515,0.147383018702806,
1.07430427059204));
#15262=CARTESIAN_POINT('Ctrl Pts',(0.0359713117426475,0.151434292157295,
1.0754807478648));
#15263=CARTESIAN_POINT('Ctrl Pts',(0.0305745581743558,0.152615446450166,
1.07591011801506));
#15264=CARTESIAN_POINT('Ctrl Pts',(0.022396772766402,0.153954014577287,
1.07655129702871));
#15265=CARTESIAN_POINT('Ctrl Pts',(0.0196554356018252,0.154327958805929,
1.07676462717102));
#15266=CARTESIAN_POINT('Ctrl Pts',(0.0126390444695441,0.155095058921444,
1.07730469236253));
#15267=CARTESIAN_POINT('Ctrl Pts',(0.00835463179472849,0.155384782872206,
1.07762890009589));
#15268=CARTESIAN_POINT('Ctrl Pts',(0.00315740721380089,0.155520591813789,
1.07801150601459));
#15269=CARTESIAN_POINT('Ctrl Pts',(0.00225129750139979,0.15553634772494,
1.07807781735803));
#15270=CARTESIAN_POINT('Ctrl Pts',(0.000974385890557175,0.155547389857333,
1.07817066262109));
#15271=CARTESIAN_POINT('Ctrl Pts',(0.000603683169115436,0.155549270308945,
1.07819754519448));
#15272=CARTESIAN_POINT('Ctrl Pts',(-3.10391346713135E-5,0.155550220953408,
1.07824344748054));
#15273=CARTESIAN_POINT('Ctrl Pts',(-0.000295054584715183,0.155549944227611,
1.07826250325319));
#15274=CARTESIAN_POINT('Ctrl Pts',(-0.000803595253981717,0.155548116435916,
1.07829913441133));
#15275=CARTESIAN_POINT('Ctrl Pts',(-0.00104811779847694,0.155546660984548,
1.07831671520905));
#15276=CARTESIAN_POINT('Ctrl Pts',(-0.00170066357540278,0.155541238067592,
1.07836354762745));
#15277=CARTESIAN_POINT('Ctrl Pts',(-0.00210868024925973,0.155536241673692,
1.07839274218876));
#15278=CARTESIAN_POINT('Ctrl Pts',(-0.00358170545025264,0.155512406144702,
1.07849783725151));
#15279=CARTESIAN_POINT('Ctrl Pts',(-0.00464656617794333,0.15548423286056,
1.07857323862844));
#15280=CARTESIAN_POINT('Ctrl Pts',(-0.0173853034967802,0.155016208496515,
1.07946930766489));
#15281=CARTESIAN_POINT('Ctrl Pts',(-0.0289761485197711,0.153273456008125,
1.08022670769006));
#15282=CARTESIAN_POINT('Ctrl Pts',(-0.0482860736035472,0.148098724003954,
1.08154419935884));
#15283=CARTESIAN_POINT('Ctrl Pts',(-0.0561189341247354,0.145311076014374,
1.08209531018966));
#15284=CARTESIAN_POINT('Ctrl Pts',(-0.0636886366174998,0.141913917801617,
1.08266645291));
#15285=CARTESIAN_POINT('Origin',(0.,0.,-0.129405622560373));
#15286=CARTESIAN_POINT('',(-0.063688625668895,0.14191392271517,1.16646420862114));
#15287=CARTESIAN_POINT('',(-0.0636886503124993,0.141913911655525,1.15273999320994));
#15288=CARTESIAN_POINT('',(-0.0636886258329924,0.141913922641526,-0.129405622560373));
#15289=CARTESIAN_POINT('',(-0.155549963960585,-0.000105886074850944,1.10930622288127));
#15290=CARTESIAN_POINT('Ctrl Pts',(-0.063688625668895,0.14191392271517,
1.16646420862114));
#15291=CARTESIAN_POINT('Ctrl Pts',(-0.0633562430797375,0.142063090533907,
1.16643737473818));
#15292=CARTESIAN_POINT('Ctrl Pts',(-0.0630233164927144,0.142211099570305,
1.16641059995971));
#15293=CARTESIAN_POINT('Ctrl Pts',(-0.0620459505366581,0.142641500039162,
1.16633230565896));
#15294=CARTESIAN_POINT('Ctrl Pts',(-0.061400116299543,0.142920688776291,
1.16628096054214));
#15295=CARTESIAN_POINT('Ctrl Pts',(-0.0604444253465264,0.143326152047841,
1.16620557966343));
#15296=CARTESIAN_POINT('Ctrl Pts',(-0.0601360323837594,0.143455819091346,
1.1661813463566));
#15297=CARTESIAN_POINT('Ctrl Pts',(-0.0595885203170512,0.143683950446014,
1.16613848815509));
#15298=CARTESIAN_POINT('Ctrl Pts',(-0.0593495720378749,0.143782814244999,
1.16611983937787));
#15299=CARTESIAN_POINT('Ctrl Pts',(-0.0588376497593383,0.143993126231899,
1.1660800058962));
#15300=CARTESIAN_POINT('Ctrl Pts',(-0.0585646057520897,0.144104394063067,
1.16605883213009));
#15301=CARTESIAN_POINT('Ctrl Pts',(-0.0578157134663128,0.144407094180099,
1.16600095093007));
#15302=CARTESIAN_POINT('Ctrl Pts',(-0.0573392262610129,0.144596952681633,
1.16596433684071));
#15303=CARTESIAN_POINT('Ctrl Pts',(-0.0548145519022079,0.145588478520955,
1.16577141674684));
#15304=CARTESIAN_POINT('Ctrl Pts',(-0.0527503385582262,0.146349046113564,
1.16561743048276));
#15305=CARTESIAN_POINT('Ctrl Pts',(-0.0374258082868009,0.15162901781501,
1.16449672842429));
#15306=CARTESIAN_POINT('Ctrl Pts',(-0.0236237399812131,0.154382896166755,
1.16360521488536));
#15307=CARTESIAN_POINT('Ctrl Pts',(-0.00283498022770765,0.155673451882592,
1.16221468753969));
#15308=CARTESIAN_POINT('Ctrl Pts',(0.003987463663544,0.155648132176121,
1.16175177476129));
#15309=CARTESIAN_POINT('Ctrl Pts',(0.0117858821283563,0.155106095329073,
1.16120412078219));
#15310=CARTESIAN_POINT('Ctrl Pts',(0.0127854113815099,0.155026904111061,
1.16113358687199));
#15311=CARTESIAN_POINT('Ctrl Pts',(0.0143842477566286,0.154884663420545,
1.16102018378491));
#15312=CARTESIAN_POINT('Ctrl Pts',(0.0149840876226635,0.154827783831081,
1.1609775076354));
#15313=CARTESIAN_POINT('Ctrl Pts',(0.0160467930153873,0.154720779732145,
1.16090166239918));
#15314=CARTESIAN_POINT('Ctrl Pts',(0.0165097953145605,0.154672059199608,
1.16086853771235));
#15315=CARTESIAN_POINT('Ctrl Pts',(0.0174722472861841,0.154566412144577,
1.16079951045634));
#15316=CARTESIAN_POINT('Ctrl Pts',(0.0179716529309728,0.154509141698687,
1.16076359745229));
#15317=CARTESIAN_POINT('Ctrl Pts',(0.0192639673169386,0.154354592508808,
1.16067041288259));
#15318=CARTESIAN_POINT('Ctrl Pts',(0.0200564112502258,0.154253625529255,
1.16061302601831));
#15319=CARTESIAN_POINT('Ctrl Pts',(0.0234566325922731,0.153793752068544,
1.16036570303146));
#15320=CARTESIAN_POINT('Ctrl Pts',(0.0260557021282155,0.153374804321913,
1.16017389184886));
#15321=CARTESIAN_POINT('Ctrl Pts',(0.0328878155923632,0.152094862297774,
1.15966197711718));
#15322=CARTESIAN_POINT('Ctrl Pts',(0.0370975267667694,0.151123203978766,
1.1593386086524));
#15323=CARTESIAN_POINT('Ctrl Pts',(0.0532192413900348,0.146687889726904,
1.15806980855491));
#15324=CARTESIAN_POINT('Ctrl Pts',(0.0647396495391824,0.14198013101031,
1.15709322072974));
#15325=CARTESIAN_POINT('Ctrl Pts',(0.0763174580160261,0.135543954120722,
1.1560839775288));
#15326=CARTESIAN_POINT('Ctrl Pts',(0.0770533692457254,0.135126963394234,
1.15601972133894));
#15327=CARTESIAN_POINT('Ctrl Pts',(0.0805744679824971,0.13309367773476,
1.15571187718268));
#15328=CARTESIAN_POINT('Ctrl Pts',(0.0833126727950094,0.131397010503638,
1.15547125955316));
#15329=CARTESIAN_POINT('Ctrl Pts',(0.086452731762303,0.129313678664958,
1.15519554652275));
#15330=CARTESIAN_POINT('Ctrl Pts',(0.0869074068190293,0.129008546162611,
1.15515562958001));
#15331=CARTESIAN_POINT('Ctrl Pts',(0.0876352692150949,0.128514483220765,
1.15509175020849));
#15332=CARTESIAN_POINT('Ctrl Pts',(0.0879094736650297,0.128327071397393,
1.15506769010618));
#15333=CARTESIAN_POINT('Ctrl Pts',(0.0883963962761222,0.127991978968315,
1.15502497672983));
#15334=CARTESIAN_POINT('Ctrl Pts',(0.0886093479428623,0.127844644064732,
1.15500630051377));
#15335=CARTESIAN_POINT('Ctrl Pts',(0.0890624049284862,0.127529511607132,
1.15496657625368));
#15336=CARTESIAN_POINT('Ctrl Pts',(0.0893024039862383,0.127361567784584,
1.15494553843046));
#15337=CARTESIAN_POINT('Ctrl Pts',(0.089954236164962,0.126902687685521,
1.15488841061848));
#15338=CARTESIAN_POINT('Ctrl Pts',(0.0903651363077546,0.126610421785932,
1.15485240995418));
#15339=CARTESIAN_POINT('Ctrl Pts',(0.0924679553092545,0.125099272379248,
1.15466819058106));
#15340=CARTESIAN_POINT('Ctrl Pts',(0.0941367669183605,0.123848378969873,
1.15452205037058));
#15341=CARTESIAN_POINT('Ctrl Pts',(0.0989812484015199,0.120062571378479,
1.15409630480898));
#15342=CARTESIAN_POINT('Ctrl Pts',(0.102083508069634,0.117436244459679,
1.15382168212832));
#15343=CARTESIAN_POINT('Ctrl Pts',(0.112762360953917,0.107652327060995,
1.1528544828009));
#15344=CARTESIAN_POINT('Ctrl Pts',(0.119718458835612,0.0998592747115928,
1.1521809658162));
#15345=CARTESIAN_POINT('Ctrl Pts',(0.129650173409336,0.0861892306737257,
1.1510508166205));
#15346=CARTESIAN_POINT('Ctrl Pts',(0.133125632428243,0.0807174054335912,
1.15061013908672));
#15347=CARTESIAN_POINT('Ctrl Pts',(0.136729381274919,0.0741745730719639,
1.15008676910077));
#15348=CARTESIAN_POINT('Ctrl Pts',(0.137200679315452,0.0732991439809676,
1.1500168215337));
#15349=CARTESIAN_POINT('Ctrl Pts',(0.137942912327108,0.071888215375048,
1.1499041821268));
#15350=CARTESIAN_POINT('Ctrl Pts',(0.138219202464033,0.0713555507513797,
1.14986167916771));
#15351=CARTESIAN_POINT('Ctrl Pts',(0.138704197110923,0.0704071345885378,
1.149786033466));
#15352=CARTESIAN_POINT('Ctrl Pts',(0.138914132934551,0.0699920178276809,
1.14975293433335));
#15353=CARTESIAN_POINT('Ctrl Pts',(0.139347548895304,0.0691253711555583,
1.14968385131716));
#15354=CARTESIAN_POINT('Ctrl Pts',(0.139570703379246,0.0686736854095561,
1.14964785655326));
#15355=CARTESIAN_POINT('Ctrl Pts',(0.140144250557256,0.0674984286022034,
1.14955422273499));
#15356=CARTESIAN_POINT('Ctrl Pts',(0.140491231068684,0.0667732190012126,
1.14949646627521));
#15357=CARTESIAN_POINT('Ctrl Pts',(0.141970290858724,0.0636193294008904,
1.1492453516703));
#15358=CARTESIAN_POINT('Ctrl Pts',(0.143045065787499,0.0611644509053154,
1.14905004635061));
#15359=CARTESIAN_POINT('Ctrl Pts',(0.145726137108539,0.0545829394362312,
1.14852643143988));
#15360=CARTESIAN_POINT('Ctrl Pts',(0.147220453331585,0.0504136460590183,
1.14819466807285));
#15361=CARTESIAN_POINT('Ctrl Pts',(0.15220152426085,0.0343946765982378,
1.14692049224163));
#15362=CARTESIAN_POINT('Ctrl Pts',(0.154450636942299,0.0222093985832487,
1.14594799416917));
#15363=CARTESIAN_POINT('Ctrl Pts',(0.155323824893923,0.00849969005322668,
1.14490215593787));
#15364=CARTESIAN_POINT('Ctrl Pts',(0.155393590976728,0.00711107859627856,
1.14479682981267));
#15365=CARTESIAN_POINT('Ctrl Pts',(0.155541279411767,0.00309872455081711,
1.1444945467261));
#15366=CARTESIAN_POINT('Ctrl Pts',(0.155571429467965,0.000473533873413159,
1.14429929940269));
#15367=CARTESIAN_POINT('Ctrl Pts',(0.155528005882422,-0.00266582157227178,
1.1440697725068));
#15368=CARTESIAN_POINT('Ctrl Pts',(0.155518337305567,-0.00318025158010444,
1.14403228854922));
#15369=CARTESIAN_POINT('Ctrl Pts',(0.155498379868171,-0.00402025461294613,
1.14397129989625));
#15370=CARTESIAN_POINT('Ctrl Pts',(0.155489620693745,-0.00434585441326615,
1.14394771318136));
#15371=CARTESIAN_POINT('Ctrl Pts',(0.155472096916919,-0.00492910086356511,
1.14390556109948));
#15372=CARTESIAN_POINT('Ctrl Pts',(0.155463714542212,-0.00518675421837981,
1.14388697482293));
#15373=CARTESIAN_POINT('Ctrl Pts',(0.155444162321329,-0.00574503226446389,
1.14384677799949));
#15374=CARTESIAN_POINT('Ctrl Pts',(0.155432760951465,-0.00604564493531247,
1.14382518056169));
#15375=CARTESIAN_POINT('Ctrl Pts',(0.155398449624585,-0.00688593695445099,
1.14376493692664));
#15376=CARTESIAN_POINT('Ctrl Pts',(0.155373600240654,-0.00742554003681481,
1.14372639718238));
#15377=CARTESIAN_POINT('Ctrl Pts',(0.155212459038221,-0.0105683635775332,
1.14350272447473));
#15378=CARTESIAN_POINT('Ctrl Pts',(0.155013546443811,-0.013168155818712,
1.14332087773324));
#15379=CARTESIAN_POINT('Ctrl Pts',(0.153259323998841,-0.0303909811588266,
1.14212996784765));
#15380=CARTESIAN_POINT('Ctrl Pts',(0.149702400890423,-0.0447362457528364,
1.14119776336399));
#15381=CARTESIAN_POINT('Ctrl Pts',(0.143461225765647,-0.0601529699931097,
1.14008029486486));
#15382=CARTESIAN_POINT('Ctrl Pts',(0.142706369311765,-0.061922490523329,
1.139950317881));
#15383=CARTESIAN_POINT('Ctrl Pts',(0.140282618866334,-0.0673243355060292,
1.13954747653858));
#15384=CARTESIAN_POINT('Ctrl Pts',(0.138506503880416,-0.0709064382457621,
1.13927172827274));
#15385=CARTESIAN_POINT('Ctrl Pts',(0.136179762983446,-0.0751772996682384,
1.13893027429809));
#15386=CARTESIAN_POINT('Ctrl Pts',(0.135758623082696,-0.0759351725890784,
1.13886918442797));
#15387=CARTESIAN_POINT('Ctrl Pts',(0.135051191831707,-0.0771835512987573,
1.13876770728354));
#15388=CARTESIAN_POINT('Ctrl Pts',(0.134768506581321,-0.077676087855746,
1.13872744926716));
#15389=CARTESIAN_POINT('Ctrl Pts',(0.134251748899673,-0.0785651476838894,
1.13865437359359));
#15390=CARTESIAN_POINT('Ctrl Pts',(0.13401859974567,-0.0789622025216168,
1.13862158956739));
#15391=CARTESIAN_POINT('Ctrl Pts',(0.133514228524791,-0.0798124818145884,
1.13855106098906));
#15392=CARTESIAN_POINT('Ctrl Pts',(0.133242454775471,-0.0802653705197622,
1.13851329668065));
#15393=CARTESIAN_POINT('Ctrl Pts',(0.132494057108027,-0.0814982384245717,
1.13840994454275));
#15394=CARTESIAN_POINT('Ctrl Pts',(0.132012862734086,-0.082275403625522,
1.13834419016624));
#15395=CARTESIAN_POINT('Ctrl Pts',(0.129418852359069,-0.0863835789277452,
1.13799332704225));
#15396=CARTESIAN_POINT('Ctrl Pts',(0.127186936864152,-0.0896372686180094,
1.1377038362538));
#15397=CARTESIAN_POINT('Ctrl Pts',(0.116021290579455,-0.104656841062771,
1.1363094611363));
#15398=CARTESIAN_POINT('Ctrl Pts',(0.105565367074166,-0.115194632027259,
1.13514499951444));
#15399=CARTESIAN_POINT('Ctrl Pts',(0.0902668802598648,-0.126756206626722,
1.1336799300187));
#15400=CARTESIAN_POINT('Ctrl Pts',(0.0866371621923835,-0.129264289969544,
1.13334771529968));
#15401=CARTESIAN_POINT('Ctrl Pts',(0.0823471793799926,-0.131966585728735,
1.13297633923749));
#15402=CARTESIAN_POINT('Ctrl Pts',(0.0817867472475284,-0.132314646646602,
1.13292822730454));
#15403=CARTESIAN_POINT('Ctrl Pts',(0.0809461743344661,-0.132829309881414,
1.13285668596281));
#15404=CARTESIAN_POINT('Ctrl Pts',(0.0806677067432171,-0.132998608252282,
1.13283308641053));
#15405=CARTESIAN_POINT('Ctrl Pts',(0.0801680005297435,-0.133300265013923,
1.13279092052415));
#15406=CARTESIAN_POINT('Ctrl Pts',(0.0799469640705385,-0.133432949083612,
1.13277233322123));
#15407=CARTESIAN_POINT('Ctrl Pts',(0.0794725849776099,-0.133716108071473,
1.13273257932045));
#15408=CARTESIAN_POINT('Ctrl Pts',(0.0792191451721574,-0.13386641237789,
1.13271142383295));
#15409=CARTESIAN_POINT('Ctrl Pts',(0.0785172623001348,-0.134279977746775,
1.13265306065199));
#15410=CARTESIAN_POINT('Ctrl Pts',(0.0780679181940378,-0.134541714989414,
1.13261595010682));
#15411=CARTESIAN_POINT('Ctrl Pts',(0.0770579626559391,-0.135123237881236,
1.13253308618868));
#15412=CARTESIAN_POINT('Ctrl Pts',(0.0764966526510069,-0.135441800026314,
1.13248740687318));
#15413=CARTESIAN_POINT('Ctrl Pts',(0.0747454207279084,-0.136421322714181,
1.13234599968118));
#15414=CARTESIAN_POINT('Ctrl Pts',(0.0735487578478895,-0.137070185442955,
1.13225095155387));
#15415=CARTESIAN_POINT('Ctrl Pts',(0.06883857314864,-0.139544724179392,
1.13188234282979));
#15416=CARTESIAN_POINT('Ctrl Pts',(0.06526413281883,-0.141251822571692,
1.13161444238228));
#15417=CARTESIAN_POINT('Ctrl Pts',(0.0519849262739079,-0.146981892733538,
1.13064773465753));
#15418=CARTESIAN_POINT('Ctrl Pts',(0.0419450048870137,-0.150155712891625,
1.12996913343594));
#15419=CARTESIAN_POINT('Ctrl Pts',(0.0252631104516602,-0.153623852135527,
1.12882988961763));
#15420=CARTESIAN_POINT('Ctrl Pts',(0.0187879596408262,-0.154549369007396,
1.12838536887849));
#15421=CARTESIAN_POINT('Ctrl Pts',(0.0112817900340348,-0.155143530793578,
1.12785780677971));
#15422=CARTESIAN_POINT('Ctrl Pts',(0.0102884767902182,-0.1552125674589,
1.12778775645848));
#15423=CARTESIAN_POINT('Ctrl Pts',(0.00869516897896647,-0.155307942902629,
1.12767498318806));
#15424=CARTESIAN_POINT('Ctrl Pts',(0.00809555361213224,-0.155340352406017,
1.12763244984327));
#15425=CARTESIAN_POINT('Ctrl Pts',(0.00703106321219006,-0.155391708620779,
1.12755676917574));
#15426=CARTESIAN_POINT('Ctrl Pts',(0.00656625970249629,-0.155412043236324,
1.12752366560146));
#15427=CARTESIAN_POINT('Ctrl Pts',(0.0055981576850239,-0.155450045834558,
1.12745459257405));
#15428=CARTESIAN_POINT('Ctrl Pts',(0.00509485138919411,-0.15546735540863,
1.12741861231931));
#15429=CARTESIAN_POINT('Ctrl Pts',(0.00378878336307197,-0.155505924314436,
1.1273250581996));
#15430=CARTESIAN_POINT('Ctrl Pts',(0.00298593414470183,-0.155523411513032,
1.12726736730399));
#15431=CARTESIAN_POINT('Ctrl Pts',(-0.000487867583251774,-0.15557216788484,
1.1270169295851));
#15432=CARTESIAN_POINT('Ctrl Pts',(-0.00315909247217263,-0.155540849702531,
1.12682224856852));
#15433=CARTESIAN_POINT('Ctrl Pts',(-0.0102328672689935,-0.155275628195431,
1.12630073125421));
#15434=CARTESIAN_POINT('Ctrl Pts',(-0.0146282716989421,-0.154923333642065,
1.12597047548947));
#15435=CARTESIAN_POINT('Ctrl Pts',(-0.0260239987464294,-0.153520693462305,
1.12509853558099));
#15436=CARTESIAN_POINT('Ctrl Pts',(-0.032977934394724,-0.152178491831197,
1.12455051349504));
#15437=CARTESIAN_POINT('Ctrl Pts',(-0.0486385558193611,-0.148031725065138,
1.12329418510298));
#15438=CARTESIAN_POINT('Ctrl Pts',(-0.057239789031957,-0.144923263589032,
1.12258754429739));
#15439=CARTESIAN_POINT('Ctrl Pts',(-0.0661404259855582,-0.140789612528867,
1.121868347043));
#15440=CARTESIAN_POINT('Ctrl Pts',(-0.0667592846064621,-0.140497220296242,
1.12181841273334));
#15441=CARTESIAN_POINT('Ctrl Pts',(-0.0676743675827402,-0.140057459287887,
1.12174470423906));
#15442=CARTESIAN_POINT('Ctrl Pts',(-0.0679720727886764,-0.139913220448408,
1.12172074469596));
#15443=CARTESIAN_POINT('Ctrl Pts',(-0.0685013363151543,-0.139654703100791,
1.12167818802388));
#15444=CARTESIAN_POINT('Ctrl Pts',(-0.0687330717253776,-0.139540797009703,
1.12165956826852));
#15445=CARTESIAN_POINT('Ctrl Pts',(-0.0692256081841168,-0.139297173377963,
1.12162002257628));
#15446=CARTESIAN_POINT('Ctrl Pts',(-0.0694863280482958,-0.139167300605119,
1.12159910655085));
#15447=CARTESIAN_POINT('Ctrl Pts',(-0.0701963730350758,-0.138811112019545,
1.12154218637856));
#15448=CARTESIAN_POINT('Ctrl Pts',(-0.0706449728533462,-0.138583344730476,
1.12150627137715));
#15449=CARTESIAN_POINT('Ctrl Pts',(-0.0716446162270851,-0.138069681067937,
1.12142632622767));
#15450=CARTESIAN_POINT('Ctrl Pts',(-0.0721950729448844,-0.137782652536816,
1.12138236329432));
#15451=CARTESIAN_POINT('Ctrl Pts',(-0.0738834156721675,-0.136889391948427,
1.12124765772941));
#15452=CARTESIAN_POINT('Ctrl Pts',(-0.0750155282569507,-0.136272284504057,
1.12115752268528));
#15453=CARTESIAN_POINT('Ctrl Pts',(-0.0793229668529194,-0.133854376152974,
1.12081480123757));
#15454=CARTESIAN_POINT('Ctrl Pts',(-0.0824424322483272,-0.13195596506273,
1.12056705880209));
#15455=CARTESIAN_POINT('Ctrl Pts',(-0.0934202578858593,-0.124733760884153,
1.11968617951262));
#15456=CARTESIAN_POINT('Ctrl Pts',(-0.100854403356595,-0.118803450949042,
1.11907118391773));
#15457=CARTESIAN_POINT('Ctrl Pts',(-0.113419725811636,-0.106745344595956,
1.11791478960237));
#15458=CARTESIAN_POINT('Ctrl Pts',(-0.118709038154767,-0.100830245741666,
1.11737985631687));
#15459=CARTESIAN_POINT('Ctrl Pts',(-0.124148939567688,-0.0937224601918963,
1.11675303801319));
#15460=CARTESIAN_POINT('Ctrl Pts',(-0.12476544876914,-0.0929001692356106,
1.11668076014295));
#15461=CARTESIAN_POINT('Ctrl Pts',(-0.125734729447746,-0.0915803048102074,
1.11656508825902));
#15462=CARTESIAN_POINT('Ctrl Pts',(-0.126092808844497,-0.0910866508165007,
1.11652189985285));
#15463=CARTESIAN_POINT('Ctrl Pts',(-0.126719783184938,-0.0902115118721126,
1.1164454612175));
#15464=CARTESIAN_POINT('Ctrl Pts',(-0.126989883235489,-0.0898308959759313,
1.11641225773307));
#15465=CARTESIAN_POINT('Ctrl Pts',(-0.12754551881558,-0.0890403990382476,
1.11634337949984));
#15466=CARTESIAN_POINT('Ctrl Pts',(-0.127830800625397,-0.0886303471253588,
1.11630769558946));
#15467=CARTESIAN_POINT('Ctrl Pts',(-0.128559050824582,-0.0875727610082243,
1.11621577209192));
#15468=CARTESIAN_POINT('Ctrl Pts',(-0.12899909959997,-0.086923243612193,
1.11615942304626));
#15469=CARTESIAN_POINT('Ctrl Pts',(-0.130822948536014,-0.0841868665323108,
1.11592244302159));
#15470=CARTESIAN_POINT('Ctrl Pts',(-0.132161095769767,-0.0820701880659587,
1.11574012628876));
#15471=CARTESIAN_POINT('Ctrl Pts',(-0.136111454279218,-0.0754742086738379,
1.11517459898141));
#15472=CARTESIAN_POINT('Ctrl Pts',(-0.138551054097449,-0.0708962541165567,
1.1147855490348));
#15473=CARTESIAN_POINT('Ctrl Pts',(-0.14506078784016,-0.0570561214165265,
1.11362037035487));
#15474=CARTESIAN_POINT('Ctrl Pts',(-0.148461737401086,-0.0475091711978216,
1.11282885262876));
#15475=CARTESIAN_POINT('Ctrl Pts',(-0.151408433680578,-0.0357139079813251,
1.11189417581377));
#15476=CARTESIAN_POINT('Ctrl Pts',(-0.151865550194059,-0.0337172400337054,
1.11173747911819));
#15477=CARTESIAN_POINT('Ctrl Pts',(-0.152298128320758,-0.0316399752128557,
1.11157636335709));
#15478=CARTESIAN_POINT('Ctrl Pts',(-0.152313088284246,-0.0315678801763142,
1.11157077392979));
#15479=CARTESIAN_POINT('Ctrl Pts',(-0.153035949009394,-0.0280717944816777,
1.11129984302843));
#15480=CARTESIAN_POINT('Ctrl Pts',(-0.153628327122837,-0.0246245666204027,
1.11103806087691));
#15481=CARTESIAN_POINT('Ctrl Pts',(-0.154180355191951,-0.0206042526620967,
1.11074105418904));
#15482=CARTESIAN_POINT('Ctrl Pts',(-0.154253656785587,-0.020048105866898,
1.11070015146496));
#15483=CARTESIAN_POINT('Ctrl Pts',(-0.154366061112768,-0.0191581475115949,
1.11063500393307));
#15484=CARTESIAN_POINT('Ctrl Pts',(-0.154407092428787,-0.0188245917093234,
1.11061065529324));
#15485=CARTESIAN_POINT('Ctrl Pts',(-0.154477885216618,-0.0182332880964603,
1.11056761638991));
#15486=CARTESIAN_POINT('Ctrl Pts',(-0.154508083188542,-0.0179755959403103,
1.11054890189106));
#15487=CARTESIAN_POINT('Ctrl Pts',(-0.15456518562475,-0.0174775395335369,
1.11051281326533));
#15488=CARTESIAN_POINT('Ctrl Pts',(-0.154592174130371,-0.0172371893065659,
1.11049543435578));
#15489=CARTESIAN_POINT('Ctrl Pts',(-0.154649991288702,-0.016711230218809,
1.11045748215791));
#15490=CARTESIAN_POINT('Ctrl Pts',(-0.154680589660553,-0.016425596087944,
1.11043692170671));
#15491=CARTESIAN_POINT('Ctrl Pts',(-0.154753828119392,-0.0157235614993409,
1.11038650804981));
#15492=CARTESIAN_POINT('Ctrl Pts',(-0.154795579406378,-0.0153070673436705,
1.11035670296449));
#15493=CARTESIAN_POINT('Ctrl Pts',(-0.154974907011376,-0.0134423558667297,
1.11022370399947));
#15494=CARTESIAN_POINT('Ctrl Pts',(-0.155093850599082,-0.0119923575481582,
1.11012147967001));
#15495=CARTESIAN_POINT('Ctrl Pts',(-0.155428335971539,-0.00706773879775331,
1.10977769098852));
#15496=CARTESIAN_POINT('Ctrl Pts',(-0.155547593982592,-0.00358745805535069,
1.10954044697179));
#15497=CARTESIAN_POINT('Ctrl Pts',(-0.155549963960585,-0.000105886074850944,
1.10930622288127));
#15498=CARTESIAN_POINT('Ctrl Pts',(-0.155549963809809,-0.00010610733808079,
1.10930623776684));
#15499=CARTESIAN_POINT('Ctrl Pts',(-0.155557297589873,0.0106449796676609,
1.10858295385663));
#15500=CARTESIAN_POINT('Ctrl Pts',(-0.154450027858621,0.0213687656586557,
1.1078892507296));
#15501=CARTESIAN_POINT('Ctrl Pts',(-0.150893360043952,0.038346658686023,
1.10673341008683));
#15502=CARTESIAN_POINT('Ctrl Pts',(-0.14913277537527,0.0447064921555321,
1.10628718600213));
#15503=CARTESIAN_POINT('Ctrl Pts',(-0.14647918261692,0.0523635131565579,
1.10572229128449));
#15504=CARTESIAN_POINT('Ctrl Pts',(-0.145963312060206,0.053784753421134,
1.10561625172379));
#15505=CARTESIAN_POINT('Ctrl Pts',(-0.145197686054202,0.0558018943052019,
1.10546394518654));
#15506=CARTESIAN_POINT('Ctrl Pts',(-0.144964796317964,0.0564041421290725,
1.1054182397703));
#15507=CARTESIAN_POINT('Ctrl Pts',(-0.144555575186568,0.0574431020995894,
1.10533898121703));
#15508=CARTESIAN_POINT('Ctrl Pts',(-0.144380996280835,0.057880499310008,
1.10530548718048));
#15509=CARTESIAN_POINT('Ctrl Pts',(-0.144042236611525,0.0587181721893201,
1.1052410952041));
#15510=CARTESIAN_POINT('Ctrl Pts',(-0.143878366682379,0.059118569562777,
1.10521020799942));
#15511=CARTESIAN_POINT('Ctrl Pts',(-0.143446377233992,0.0601616513187481,
1.10512945611869));
#15512=CARTESIAN_POINT('Ctrl Pts',(-0.143175611114379,0.0608032218204263,
1.10507950230247));
#15513=CARTESIAN_POINT('Ctrl Pts',(-0.142229802399612,0.0630029306735668,
1.10490722883331));
#15514=CARTESIAN_POINT('Ctrl Pts',(-0.141533580788642,0.0645517702961384,
1.10478419273612));
#15515=CARTESIAN_POINT('Ctrl Pts',(-0.135434836821106,0.0775460561328283,
1.10373676204873));
#15516=CARTESIAN_POINT('Ctrl Pts',(-0.12868040533795,0.0883017650519376,
1.10276325893813));
#15517=CARTESIAN_POINT('Ctrl Pts',(-0.117272301066173,0.102335456757039,
1.10136071046782));
#15518=CARTESIAN_POINT('Ctrl Pts',(-0.11362536184951,0.106370209338636,
1.1009396706719));
#15519=CARTESIAN_POINT('Ctrl Pts',(-0.107933257392616,0.112040031229894,
1.10032846571767));
#15520=CARTESIAN_POINT('Ctrl Pts',(-0.106046174224259,0.113827796977805,
1.10013259529038));
#15521=CARTESIAN_POINT('Ctrl Pts',(-0.103356146547034,0.116251248891357,
1.09986358740521));
#15522=CARTESIAN_POINT('Ctrl Pts',(-0.102590493756333,0.11692748448397,
1.09978812704633));
#15523=CARTESIAN_POINT('Ctrl Pts',(-0.101253718857317,0.118084903552562,
1.09965835845616));
#15524=CARTESIAN_POINT('Ctrl Pts',(-0.100685700719042,0.118569598802221,
1.09960382346366));
#15525=CARTESIAN_POINT('Ctrl Pts',(-0.0998511425306055,0.119271413047385,
1.09952460492108));
#15526=CARTESIAN_POINT('Ctrl Pts',(-0.0995873498925043,0.119491758638643,
1.09949969576395));
#15527=CARTESIAN_POINT('Ctrl Pts',(-0.0991328597054476,0.119868843138172,
1.0994570068369));
#15528=CARTESIAN_POINT('Ctrl Pts',(-0.0989425166166196,0.120026004840455,
1.09943919653723));
#15529=CARTESIAN_POINT('Ctrl Pts',(-0.0985607538428087,0.120339691876037,
1.09940361226414));
#15530=CARTESIAN_POINT('Ctrl Pts',(-0.0983693351604216,0.120496213804917,
1.09938583841196));
#15531=CARTESIAN_POINT('Ctrl Pts',(-0.0978503814734785,0.120918498385561,
1.09933783391876));
#15532=CARTESIAN_POINT('Ctrl Pts',(-0.0975221340960157,0.121183389038653,
1.09930766562779));
#15533=CARTESIAN_POINT('Ctrl Pts',(-0.0962914216806294,0.122168316204022,
1.0991952645309));
#15534=CARTESIAN_POINT('Ctrl Pts',(-0.0953819964486638,0.122879657947254,
1.099113625682));
#15535=CARTESIAN_POINT('Ctrl Pts',(-0.0943523951287159,0.123666681103683,
1.09902266898451));
#15536=CARTESIAN_POINT('Ctrl Pts',(-0.0942399730443125,0.123752373563864,
1.09901275689679));
#15537=CARTESIAN_POINT('Ctrl Pts',(-0.0846948556055197,0.131007481372158,
1.09817281245617));
#15538=CARTESIAN_POINT('Ctrl Pts',(-0.0744813799541116,0.137070312887174,
1.09740716183172));
#15539=CARTESIAN_POINT('Ctrl Pts',(-0.0636886243721053,0.141913923297148,
1.09662690323004));
#15540=CARTESIAN_POINT('Ctrl Pts',(-0.0636886366174998,0.141913917801617,
1.08266645291));
#15541=CARTESIAN_POINT('Ctrl Pts',(-0.0654970691897544,0.141102322950838,
1.08280290121822));
#15542=CARTESIAN_POINT('Ctrl Pts',(-0.0672904848875035,0.140255937755946,
1.08294043971035));
#15543=CARTESIAN_POINT('Ctrl Pts',(-0.0701743012142742,0.13882685165615,
1.08316555758902));
#15544=CARTESIAN_POINT('Ctrl Pts',(-0.071274125431853,0.138265419322431,
1.08325236506509));
#15545=CARTESIAN_POINT('Ctrl Pts',(-0.0728937038206069,0.137414207154768,
1.0833816715481));
#15546=CARTESIAN_POINT('Ctrl Pts',(-0.0734186874626417,0.137134432941225,
1.08342381851927));
#15547=CARTESIAN_POINT('Ctrl Pts',(-0.0743493718815002,0.136631576695086,
1.08349895736458));
#15548=CARTESIAN_POINT('Ctrl Pts',(-0.0747557082670035,0.136409680456959,
1.0835319068682));
#15549=CARTESIAN_POINT('Ctrl Pts',(-0.0756084554011755,0.135939049288522,
1.08360136231955));
#15550=CARTESIAN_POINT('Ctrl Pts',(-0.0760546422768576,0.135689922345981,
1.0836378819665));
#15551=CARTESIAN_POINT('Ctrl Pts',(-0.0772283949122343,0.135026953361931,
1.08373442801632));
#15552=CARTESIAN_POINT('Ctrl Pts',(-0.0779538531808934,0.134609434432828,
1.08379458589444));
#15553=CARTESIAN_POINT('Ctrl Pts',(-0.0809989196872986,0.132824053168718,
1.08404918492504));
#15554=CARTESIAN_POINT('Ctrl Pts',(-0.0832860409962447,0.13140200829151,
1.08424557731263));
#15555=CARTESIAN_POINT('Ctrl Pts',(-0.0858571109904579,0.129709320179458,
1.08447252063562));
#15556=CARTESIAN_POINT('Ctrl Pts',(-0.0861784533760765,0.129496044024315,
1.08450099723456));
#15557=CARTESIAN_POINT('Ctrl Pts',(-0.0865619328377933,0.129239467723725,
1.08453511521819));
#15558=CARTESIAN_POINT('Ctrl Pts',(-0.0866248381435066,0.129197312861768,
1.08454071623207));
#15559=CARTESIAN_POINT('Ctrl Pts',(-0.0995119509813744,0.120547602334531,
1.08568906360688));
#15560=CARTESIAN_POINT('Ctrl Pts',(-0.110981311560037,0.110078664137978,
1.08690544180326));
#15561=CARTESIAN_POINT('Ctrl Pts',(-0.122742773812635,0.0956050415601197,
1.08833260506456));
#15562=CARTESIAN_POINT('Ctrl Pts',(-0.124690236484937,0.0930508487712888,
1.08857598900644));
#15563=CARTESIAN_POINT('Ctrl Pts',(-0.1272445532835,0.0894763831246984,
1.08890345243883));
#15564=CARTESIAN_POINT('Ctrl Pts',(-0.12792078492832,0.0885069063442847,
1.08899099433548));
#15565=CARTESIAN_POINT('Ctrl Pts',(-0.129062753524451,0.0868292934410465,
1.08914018600276));
#15566=CARTESIAN_POINT('Ctrl Pts',(-0.129533864614918,0.0861249008798765,
1.08920214705632));
#15567=CARTESIAN_POINT('Ctrl Pts',(-0.130197325078922,0.0851151526237553,
1.08928996333155));
#15568=CARTESIAN_POINT('Ctrl Pts',(-0.130394393414508,0.0848129402689565,
1.08931611919851));
#15569=CARTESIAN_POINT('Ctrl Pts',(-0.130732892256682,0.0842898698441625,
1.0893611672181));
#15570=CARTESIAN_POINT('Ctrl Pts',(-0.130874818165653,0.0840693359715489,
1.08938009207611));
#15571=CARTESIAN_POINT('Ctrl Pts',(-0.131149402518108,0.0836402880933896,
1.08941677711718));
#15572=CARTESIAN_POINT('Ctrl Pts',(-0.131282121688672,0.0834318170751442,
1.08943454150564));
#15573=CARTESIAN_POINT('Ctrl Pts',(-0.131639795992465,0.0828670270762352,
1.08948250773189));
#15574=CARTESIAN_POINT('Ctrl Pts',(-0.131863803253786,0.0825101052478858,
1.08951264736445));
#15575=CARTESIAN_POINT('Ctrl Pts',(-0.132694979999661,0.0811737196676346,
1.08962486970617));
#15576=CARTESIAN_POINT('Ctrl Pts',(-0.133292730079633,0.0801883956627173,
1.08970636075761));
#15577=CARTESIAN_POINT('Ctrl Pts',(-0.138763553081534,0.070940118128965,
1.09046054936208));
#15578=CARTESIAN_POINT('Ctrl Pts',(-0.142874200578925,0.0622482607887882,
1.09109120771017));
#15579=CARTESIAN_POINT('Ctrl Pts',(-0.150265617844189,0.0419537071894152,
1.09251280278583));
#15580=CARTESIAN_POINT('Ctrl Pts',(-0.153053454945115,0.0302399418655237,
1.09330186117327));
#15581=CARTESIAN_POINT('Ctrl Pts',(-0.154632764489578,0.0169260068846493,
1.09423762266343));
#15582=CARTESIAN_POINT('Ctrl Pts',(-0.154779513253198,0.015526867417129,
1.09433637251524));
#15583=CARTESIAN_POINT('Ctrl Pts',(-0.154964209771534,0.0135014608116345,
1.09448000137529));
#15584=CARTESIAN_POINT('Ctrl Pts',(-0.155017380769496,0.0128766219444452,
1.09452440383715));
#15585=CARTESIAN_POINT('Ctrl Pts',(-0.155103604872675,0.0117852855643695,
1.09460212636834));
#15586=CARTESIAN_POINT('Ctrl Pts',(-0.155138335437228,0.0113189252740619,
1.0946353935317));
#15587=CARTESIAN_POINT('Ctrl Pts',(-0.155201448455145,0.0104165175495574,
1.09469987320782));
#15588=CARTESIAN_POINT('Ctrl Pts',(-0.155230097597034,0.00998049263660528,
1.09473107704891));
#15589=CARTESIAN_POINT('Ctrl Pts',(-0.155293853886368,0.00894337672181383,
1.09480541603011));
#15590=CARTESIAN_POINT('Ctrl Pts',(-0.155327308623873,0.00834219508496718,
1.09484860244059));
#15591=CARTESIAN_POINT('Ctrl Pts',(-0.155433880402022,0.00620331918078968,
1.09500259714848));
#15592=CARTESIAN_POINT('Ctrl Pts',(-0.155487657697881,0.00466479716371283,
1.09511400571974));
#15593=CARTESIAN_POINT('Ctrl Pts',(-0.155539991536784,0.00206100437931375,
1.0953036963907));
#15594=CARTESIAN_POINT('Ctrl Pts',(-0.155550456350694,0.000996061320335559,
1.09538160219944));
#15595=CARTESIAN_POINT('Ctrl Pts',(-0.155548320038231,-0.00382820720160956,
1.09573602022358));
#15596=CARTESIAN_POINT('Ctrl Pts',(-0.155410374330263,-0.00758592816398812,
1.0960162512148));
#15597=CARTESIAN_POINT('Ctrl Pts',(-0.1545687886761,-0.0191046024222937,
1.09688802402212));
#15598=CARTESIAN_POINT('Ctrl Pts',(-0.153418226475811,-0.0268201758129123,
1.09749050156596));
#15599=CARTESIAN_POINT('Ctrl Pts',(-0.149765464875519,-0.0429202412377183,
1.09877084722375));
#15600=CARTESIAN_POINT('Ctrl Pts',(-0.147124210951748,-0.0512478577203565,
1.09944698107082));
#15601=CARTESIAN_POINT('Ctrl Pts',(-0.143355590093591,-0.0603848213541838,
1.10017766026405));
#15602=CARTESIAN_POINT('Ctrl Pts',(-0.142900633083672,-0.0614537317166153,
1.10026294405026));
#15603=CARTESIAN_POINT('Ctrl Pts',(-0.142263790529776,-0.0629046514851802,
1.1003783419895));
#15604=CARTESIAN_POINT('Ctrl Pts',(-0.142092274432174,-0.0632911275963539,
1.10040904449476));
#15605=CARTESIAN_POINT('Ctrl Pts',(-0.141817899775513,-0.0639026370033217,
1.10045756213078));
#15606=CARTESIAN_POINT('Ctrl Pts',(-0.14171607827137,-0.0641281285743524,
1.1004754393913));
#15607=CARTESIAN_POINT('Ctrl Pts',(-0.141505287899192,-0.0645919862475548,
1.10051218553325));
#15608=CARTESIAN_POINT('Ctrl Pts',(-0.141396254598972,-0.0648303198927974,
1.10053104987745));
#15609=CARTESIAN_POINT('Ctrl Pts',(-0.141136109539516,-0.0653951874454223,
1.10057572372054));
#15610=CARTESIAN_POINT('Ctrl Pts',(-0.140984464961606,-0.0657214774902751,
1.10060150060297));
#15611=CARTESIAN_POINT('Ctrl Pts',(-0.140474295765508,-0.0668093047137703,
1.10068735327252));
#15612=CARTESIAN_POINT('Ctrl Pts',(-0.140110713797553,-0.0675684758645069,
1.10074712753213));
#15613=CARTESIAN_POINT('Ctrl Pts',(-0.136584216494592,-0.0747810405082375,
1.1013140307224));
#15614=CARTESIAN_POINT('Ctrl Pts',(-0.13298329564159,-0.0810118923922004,
1.10179637340532));
#15615=CARTESIAN_POINT('Ctrl Pts',(-0.126302044105769,-0.0909189660146076,
1.10258794454168));
#15616=CARTESIAN_POINT('Ctrl Pts',(-0.123460514987323,-0.0947415813628541,
1.10290014561543));
#15617=CARTESIAN_POINT('Ctrl Pts',(-0.113816903159399,-0.106542654680463,
1.10390441927588));
#15618=CARTESIAN_POINT('Ctrl Pts',(-0.106383781919192,-0.113965191530275,
1.10460166598278));
#15619=CARTESIAN_POINT('Ctrl Pts',(-0.0973779838983343,-0.121303876758094,
1.1054150942691));
#15620=CARTESIAN_POINT('Ctrl Pts',(-0.0964863206428485,-0.122014310926978,
1.10549529538561));
#15621=CARTESIAN_POINT('Ctrl Pts',(-0.0951264112834025,-0.123073592449157,
1.10561715360899));
#15622=CARTESIAN_POINT('Ctrl Pts',(-0.0946638632870458,-0.123429721917901,
1.10565852234625));
#15623=CARTESIAN_POINT('Ctrl Pts',(-0.0938319116942235,-0.124062838998831,
1.10573279451285));
#15624=CARTESIAN_POINT('Ctrl Pts',(-0.0934632567380556,-0.124340803054096,
1.10576565916038));
#15625=CARTESIAN_POINT('Ctrl Pts',(-0.0926789475219452,-0.124926709639521,
1.10583548258261));
#15626=CARTESIAN_POINT('Ctrl Pts',(-0.0922629846139647,-0.125234227563094,
1.10587245734721));
#15627=CARTESIAN_POINT('Ctrl Pts',(-0.0911471488572198,-0.126050579080165,
1.10597149849921));
#15628=CARTESIAN_POINT('Ctrl Pts',(-0.0904445599742132,-0.126555650787017,
1.10603370884472));
#15629=CARTESIAN_POINT('Ctrl Pts',(-0.0870249032633656,-0.128970926971719,
1.1063358131559));
#15630=CARTESIAN_POINT('Ctrl Pts',(-0.0842515360231853,-0.130799500496015,
1.10657876839933));
#15631=CARTESIAN_POINT('Ctrl Pts',(-0.0686782772003354,-0.14036662284719,
1.10793332792345));
#15632=CARTESIAN_POINT('Ctrl Pts',(-0.054873220017387,-0.146315602695528,
1.10910968644308));
#15633=CARTESIAN_POINT('Ctrl Pts',(-0.0394448751007813,-0.15046912965479,
1.11033419412863));
#15634=CARTESIAN_POINT('Ctrl Pts',(-0.0384505822440917,-0.15072627492771,
1.11041267761977));
#15635=CARTESIAN_POINT('Ctrl Pts',(-0.0365365399051327,-0.151201114067557,
1.11056285619434));
#15636=CARTESIAN_POINT('Ctrl Pts',(-0.035617208046781,-0.151420309760325,
1.11063459045438));
#15637=CARTESIAN_POINT('Ctrl Pts',(-0.0317070461640164,-0.152315024873353,
1.1109378676337));
#15638=CARTESIAN_POINT('Ctrl Pts',(-0.0286983292024785,-0.152910473376288,
1.11116671455371));
#15639=CARTESIAN_POINT('Ctrl Pts',(-0.0251415121431128,-0.153505693844402,
1.11143051998525));
#15640=CARTESIAN_POINT('Ctrl Pts',(-0.0246088356718649,-0.153591988415209,
1.11146985146595));
#15641=CARTESIAN_POINT('Ctrl Pts',(-0.0237464616207541,-0.15372709301235,
1.1115332300835));
#15642=CARTESIAN_POINT('Ctrl Pts',(-0.0234170436193986,-0.153777617484842,
1.11155737011441));
#15643=CARTESIAN_POINT('Ctrl Pts',(-0.022831939179184,-0.153865434116311,
1.11160011994497));
#15644=CARTESIAN_POINT('Ctrl Pts',(-0.0225763202332963,-0.153903148216975,
1.11161875322072));
#15645=CARTESIAN_POINT('Ctrl Pts',(-0.022028188874875,-0.153982624663333,
1.11165861600681));
#15646=CARTESIAN_POINT('Ctrl Pts',(-0.021735651804616,-0.154024190463421,
1.11167983431728));
#15647=CARTESIAN_POINT('Ctrl Pts',(-0.0209318936926681,-0.154136058763158,
1.11173798211519));
#15648=CARTESIAN_POINT('Ctrl Pts',(-0.0204204321123242,-0.154204652190425,
1.11177481677605));
#15649=CARTESIAN_POINT('Ctrl Pts',(-0.0176833070480242,-0.154557878092712,
1.11197109406447));
#15650=CARTESIAN_POINT('Ctrl Pts',(-0.0154518743723241,-0.154796892807306,
1.11212811977314));
#15651=CARTESIAN_POINT('Ctrl Pts',(-0.00868775871410813,-0.155373673695075,
1.11259723580076));
#15652=CARTESIAN_POINT('Ctrl Pts',(-0.00414446113626913,-0.155561198042398,
1.11290305958846));
#15653=CARTESIAN_POINT('Ctrl Pts',(0.0113174035813567,-0.155521348501438,
1.11393170312614));
#15654=CARTESIAN_POINT('Ctrl Pts',(0.0222003559781261,-0.154344161504432,
1.11463728493112));
#15655=CARTESIAN_POINT('Ctrl Pts',(0.0381502817294884,-0.150895784237119,
1.11573609851731));
#15656=CARTESIAN_POINT('Ctrl Pts',(0.0433664588106869,-0.149480169757907,
1.11610582392226));
#15657=CARTESIAN_POINT('Ctrl Pts',(0.0493998566978678,-0.147500364522822,
1.11655104744773));
#15658=CARTESIAN_POINT('Ctrl Pts',(0.0502989439486908,-0.147196194050595,
1.11661785749473));
#15659=CARTESIAN_POINT('Ctrl Pts',(0.0517550911289746,-0.146688665666304,
1.11672684465253));
#15660=CARTESIAN_POINT('Ctrl Pts',(0.052313880831915,-0.146490313493395,
1.11676885654466));
#15661=CARTESIAN_POINT('Ctrl Pts',(0.0533067076934562,-0.146131487181524,
1.11684384386904));
#15662=CARTESIAN_POINT('Ctrl Pts',(0.0537411911567228,-0.145972261048395,
1.11687677755471));
#15663=CARTESIAN_POINT('Ctrl Pts',(0.0546549514227546,-0.145632760696325,
1.11694629158622));
#15664=CARTESIAN_POINT('Ctrl Pts',(0.0551340605323534,-0.1454520541646,
1.1169828860135));
#15665=CARTESIAN_POINT('Ctrl Pts',(0.0563983032747887,-0.144968073366379,
1.11707984187247));
#15666=CARTESIAN_POINT('Ctrl Pts',(0.0571818731949512,-0.144660790244102,
1.11714033679843));
#15667=CARTESIAN_POINT('Ctrl Pts',(0.0608006923555885,-0.1432076461129,
1.11742162981614));
#15668=CARTESIAN_POINT('Ctrl Pts',(0.0636040664325067,-0.141984768098211,
1.11764500199353));
#15669=CARTESIAN_POINT('Ctrl Pts',(0.0794316034484524,-0.134517728496603,
1.11893895879046));
#15670=CARTESIAN_POINT('Ctrl Pts',(0.0915701824792191,-0.126566735119113,
1.1200704520659));
#15671=CARTESIAN_POINT('Ctrl Pts',(0.106731728029147,-0.113299339923834,
1.12162072573471));
#15672=CARTESIAN_POINT('Ctrl Pts',(0.110818815718578,-0.109305120442082,
1.12205446270915));
#15673=CARTESIAN_POINT('Ctrl Pts',(0.115144697854957,-0.104584795121255,
1.12252375486159));
#15674=CARTESIAN_POINT('Ctrl Pts',(0.115608573557686,-0.104071795327169,
1.12257421775728));
#15675=CARTESIAN_POINT('Ctrl Pts',(0.116290145892974,-0.103307864118604,
1.12264854876261));
#15676=CARTESIAN_POINT('Ctrl Pts',(0.116510476461629,-0.103059311567851,
1.12267260677771));
#15677=CARTESIAN_POINT('Ctrl Pts',(0.116900715102366,-0.102616236593141,
1.12271526622882));
#15678=CARTESIAN_POINT('Ctrl Pts',(0.117070936076066,-0.102421995362803,
1.12273389076476));
#15679=CARTESIAN_POINT('Ctrl Pts',(0.117435331978952,-0.102004083404415,
1.12277379591227));
#15680=CARTESIAN_POINT('Ctrl Pts',(0.117629351609803,-0.101780282334224,
1.12279506506013));
#15681=CARTESIAN_POINT('Ctrl Pts',(0.118161765155601,-0.101162588994287,
1.12285349540955));
#15682=CARTESIAN_POINT('Ctrl Pts',(0.118498831983934,-0.100767549318997,
1.12289056024653));
#15683=CARTESIAN_POINT('Ctrl Pts',(0.120311211755843,-0.0986217843385661,
1.12309029984792));
#15684=CARTESIAN_POINT('Ctrl Pts',(0.121749814844777,-0.0968402194555562,
1.12325045558052));
#15685=CARTESIAN_POINT('Ctrl Pts',(0.131871453724246,-0.0837233075298303,
1.12439468636902));
#15686=CARTESIAN_POINT('Ctrl Pts',(0.138997340849035,-0.0712707743269609,
1.12530193213362));
#15687=CARTESIAN_POINT('Ctrl Pts',(0.146734909735347,-0.052023356075842,
1.12668953372001));
#15688=CARTESIAN_POINT('Ctrl Pts',(0.148769016498788,-0.0458838287626516,
1.12712926028703));
#15689=CARTESIAN_POINT('Ctrl Pts',(0.150668539235068,-0.0386753296758805,
1.12765157865191));
#15690=CARTESIAN_POINT('Ctrl Pts',(0.150912516359792,-0.037712095746547,
1.12772148587669));
#15691=CARTESIAN_POINT('Ctrl Pts',(0.151288935602114,-0.036163796979812,
1.12783406573565));
#15692=CARTESIAN_POINT('Ctrl Pts',(0.151427253957926,-0.0355801768986072,
1.12787654973777));
#15693=CARTESIAN_POINT('Ctrl Pts',(0.151666812982498,-0.0345426777461856,
1.1279521649268));
#15694=CARTESIAN_POINT('Ctrl Pts',(0.151769400792548,-0.0340891144006268,
1.127985252556));
#15695=CARTESIAN_POINT('Ctrl Pts',(0.151978863791308,-0.033143342471659,
1.12805431477707));
#15696=CARTESIAN_POINT('Ctrl Pts',(0.152085385009902,-0.032651061925674,
1.12809030025567));
#15697=CARTESIAN_POINT('Ctrl Pts',(0.152355696446327,-0.0313718091724201,
1.12818391681753));
#15698=CARTESIAN_POINT('Ctrl Pts',(0.152515778791782,-0.0305840779639932,
1.12824166529263));
#15699=CARTESIAN_POINT('Ctrl Pts',(0.153183102045879,-0.0271647276782974,
1.12849280687957));
#15700=CARTESIAN_POINT('Ctrl Pts',(0.153628359806295,-0.0245216350459134,
1.12868814800275));
#15701=CARTESIAN_POINT('Ctrl Pts',(0.154627755927137,-0.0174835642627882,
1.12921191354052));
#15702=CARTESIAN_POINT('Ctrl Pts',(0.155062794237672,-0.0130744419771307,
1.12954379478179));
#15703=CARTESIAN_POINT('Ctrl Pts',(0.155995907612279,0.00367337566344355,
1.13081785208543));
#15704=CARTESIAN_POINT('Ctrl Pts',(0.155212788901227,0.0160363950270534,
1.13179008482513));
#15705=CARTESIAN_POINT('Ctrl Pts',(0.152729909648759,0.0295166937569477,
1.13283361576225));
#15706=CARTESIAN_POINT('Ctrl Pts',(0.152465383301336,0.0308539727840429,
1.13293689479962));
#15707=CARTESIAN_POINT('Ctrl Pts',(0.151634849969303,0.0347807378250339,
1.13323914784211));
#15708=CARTESIAN_POINT('Ctrl Pts',(0.151020162428184,0.0373596072769394,
1.13343634854853));
#15709=CARTESIAN_POINT('Ctrl Pts',(0.150207384422566,0.0404204208364463,
1.13366787515993));
#15710=CARTESIAN_POINT('Ctrl Pts',(0.150072470524546,0.0409184844107916,
1.13370546889491));
#15711=CARTESIAN_POINT('Ctrl Pts',(0.149848248961683,0.0417302184649313,
1.13376659609405));
#15712=CARTESIAN_POINT('Ctrl Pts',(0.149760430391615,0.0420442902691618,
1.13379021222501));
#15713=CARTESIAN_POINT('Ctrl Pts',(0.149601437383147,0.0426060895181119,
1.13383239049407));
#15714=CARTESIAN_POINT('Ctrl Pts',(0.149530634688674,0.0428539172570351,
1.13385097369971));
#15715=CARTESIAN_POINT('Ctrl Pts',(0.149375990598862,0.0433901618087672,
1.1338911335101));
#15716=CARTESIAN_POINT('Ctrl Pts',(0.149291929990211,0.0436785113430009,
1.13391269714872));
#15717=CARTESIAN_POINT('Ctrl Pts',(0.149054896327362,0.0444829191098029,
1.13397277100443));
#15718=CARTESIAN_POINT('Ctrl Pts',(0.148900077098037,0.0449984363591205,
1.13401117569352));
#15719=CARTESIAN_POINT('Ctrl Pts',(0.147988441625811,0.0479777734246798,
1.13423263703831));
#15720=CARTESIAN_POINT('Ctrl Pts',(0.147173100554912,0.0504234683713321,
1.1344124825393));
#15721=CARTESIAN_POINT('Ctrl Pts',(0.141295478657645,0.0666942989391085,
1.13560298809118));
#15722=CARTESIAN_POINT('Ctrl Pts',(0.134352915397266,0.0797618053906868,
1.13653620171133));
#15723=CARTESIAN_POINT('Ctrl Pts',(0.124575945899856,0.0931671546948407,
1.13765086756548));
#15724=CARTESIAN_POINT('Ctrl Pts',(0.123449287116668,0.0946549424866219,
1.1377769226277));
#15725=CARTESIAN_POINT('Ctrl Pts',(0.119786144102283,0.0993155618988308,
1.13818004678914));
#15726=CARTESIAN_POINT('Ctrl Pts',(0.1171522105003,0.102409256447219,1.13846015962333));
#15727=CARTESIAN_POINT('Ctrl Pts',(0.113810100500386,0.106036892565904,
1.13880643057292));
#15728=CARTESIAN_POINT('Ctrl Pts',(0.113214411024951,0.106672670549852,
1.13886781431207));
#15729=CARTESIAN_POINT('Ctrl Pts',(0.112220835139746,0.107715414597813,
1.13896967166337));
#15730=CARTESIAN_POINT('Ctrl Pts',(0.111825994234747,0.10812526707127,1.13901001423389));
#15731=CARTESIAN_POINT('Ctrl Pts',(0.111107681329752,0.108862746684649,
1.13908317045316));
#15732=CARTESIAN_POINT('Ctrl Pts',(0.110784985388753,0.109191123587312,
1.13911595004324));
#15733=CARTESIAN_POINT('Ctrl Pts',(0.110089805059015,0.109892288335531,
1.13918638816027));
#15734=CARTESIAN_POINT('Ctrl Pts',(0.109716875492065,0.11026462457738,1.1392240660799));
#15735=CARTESIAN_POINT('Ctrl Pts',(0.108695440519839,0.11127412206478,1.13932697528191));
#15736=CARTESIAN_POINT('Ctrl Pts',(0.108043238536512,0.111907495604359,
1.13939237079232));
#15737=CARTESIAN_POINT('Ctrl Pts',(0.104579814027607,0.115212434965544,
1.13973805650465));
#15738=CARTESIAN_POINT('Ctrl Pts',(0.101675203216065,0.117783660829944,
1.14002257688992));
#15739=CARTESIAN_POINT('Ctrl Pts',(0.0872274311655971,0.129640222111979,
1.14141430982126));
#15740=CARTESIAN_POINT('Ctrl Pts',(0.0744942070606635,0.137352385128099,
1.14258187299207));
#15741=CARTESIAN_POINT('Ctrl Pts',(0.0567792200499203,0.144884982216121,
1.1440529171158));
#15742=CARTESIAN_POINT('Ctrl Pts',(0.0526179139068107,0.146447608911285,
1.14438769208398));
#15743=CARTESIAN_POINT('Ctrl Pts',(0.0477671107435503,0.148035610836402,
1.14476156410014));
#15744=CARTESIAN_POINT('Ctrl Pts',(0.0471379405001526,0.148237153075328,
1.14480974540904));
#15745=CARTESIAN_POINT('Ctrl Pts',(0.0461963888526278,0.148532159623132,
1.1448813648493));
#15746=CARTESIAN_POINT('Ctrl Pts',(0.0458849778270189,0.148628656726924,
1.14490497371427));
#15747=CARTESIAN_POINT('Ctrl Pts',(0.0453268368369209,0.14879968679282,
1.14494714415859));
#15748=CARTESIAN_POINT('Ctrl Pts',(0.0450802240279438,0.148874585918513,
1.14496572677196));
#15749=CARTESIAN_POINT('Ctrl Pts',(0.0445724622848307,0.149027421552716,
1.14500388366486));
#15750=CARTESIAN_POINT('Ctrl Pts',(0.0443112957304139,0.149105284422075,
1.14502345362964));
#15751=CARTESIAN_POINT('Ctrl Pts',(0.0435911318489811,0.149317931159207,
1.14507726697012));
#15752=CARTESIAN_POINT('Ctrl Pts',(0.0431317099502381,0.149451286225563,
1.14511142839477));
#15753=CARTESIAN_POINT('Ctrl Pts',(0.0421022664970025,0.149744957390049,
1.145187614446));
#15754=CARTESIAN_POINT('Ctrl Pts',(0.0415319263577029,0.149904143471119,
1.14522957701373));
#15755=CARTESIAN_POINT('Ctrl Pts',(0.0397961477847074,0.150377944854073,
1.14535657780777));
#15756=CARTESIAN_POINT('Ctrl Pts',(0.0386279112955131,0.15068226294323,
1.14544108615236));
#15757=CARTESIAN_POINT('Ctrl Pts',(0.034241787156889,0.151770454972918,
1.14575517427765));
#15758=CARTESIAN_POINT('Ctrl Pts',(0.0310024672085833,0.152465148008552,
1.14598073843499));
#15759=CARTESIAN_POINT('Ctrl Pts',(0.0164935159925448,0.155095067480247,
1.14697269925986));
#15760=CARTESIAN_POINT('Ctrl Pts',(0.00505301496596258,0.155887808668048,
1.14770856466844));
#15761=CARTESIAN_POINT('Ctrl Pts',(-0.0128930684129306,0.155152097511481,
1.14890955191355));
#15762=CARTESIAN_POINT('Ctrl Pts',(-0.0193904999980737,0.154474578282769,
1.14935353084091));
#15763=CARTESIAN_POINT('Ctrl Pts',(-0.0268070803942238,0.153225890617847,
1.14988048785086));
#15764=CARTESIAN_POINT('Ctrl Pts',(-0.027786933810309,0.153051231105118,
1.1499505095955));
#15765=CARTESIAN_POINT('Ctrl Pts',(-0.0293549441356074,0.152756178542819,
1.15006323864751));
#15766=CARTESIAN_POINT('Ctrl Pts',(-0.0299442093835759,0.152641760780974,
1.15010575651673));
#15767=CARTESIAN_POINT('Ctrl Pts',(-0.0309888378146968,0.152432643304446,
1.1501814106755));
#15768=CARTESIAN_POINT('Ctrl Pts',(-0.0314444690969005,0.152339306052311,
1.15021450325304));
#15769=CARTESIAN_POINT('Ctrl Pts',(-0.0323924233716294,0.152140681191502,
1.15028355432998));
#15770=CARTESIAN_POINT('Ctrl Pts',(-0.0328846667390771,0.152035044143676,
1.15031952362833));
#15771=CARTESIAN_POINT('Ctrl Pts',(-0.0341605116953441,0.151754757660172,
1.15041305131401));
#15772=CARTESIAN_POINT('Ctrl Pts',(-0.0349432807678018,0.151576429949095,
1.15047072667533));
#15773=CARTESIAN_POINT('Ctrl Pts',(-0.0383238783407153,0.150778696094525,
1.15072111324251));
#15774=CARTESIAN_POINT('Ctrl Pts',(-0.0409067486221699,0.150098538038684,
1.15091575797927));
#15775=CARTESIAN_POINT('Ctrl Pts',(-0.0477022978524671,0.148120615611087,
1.15143718354508));
#15776=CARTESIAN_POINT('Ctrl Pts',(-0.0518792533930157,0.146709789773049,
1.1517673829189));
#15777=CARTESIAN_POINT('Ctrl Pts',(-0.0585866146441732,0.14412201433543,
1.15231334060707));
#15778=CARTESIAN_POINT('Ctrl Pts',(-0.0611535904857956,0.143051605183529,
1.15252616729451));
#15779=CARTESIAN_POINT('Ctrl Pts',(-0.0636886503124892,0.14191391165553,
1.15273999320994));
#15780=CARTESIAN_POINT('Origin',(0.,0.,-0.129405622560373));
#15781=CARTESIAN_POINT('',(-0.063688617770428,0.141913926259872,1.23669476364274));
#15782=CARTESIAN_POINT('',(-0.0636886258329928,0.141913922641526,1.22279509470766));
#15783=CARTESIAN_POINT('',(-0.0636886258329924,0.141913922641526,-0.129405622560373));
#15784=CARTESIAN_POINT('Ctrl Pts',(-0.063688617770428,0.141913926259872,
1.23669476364274));
#15785=CARTESIAN_POINT('Ctrl Pts',(-0.0619802210974833,0.14268062636867,
1.23655225137014));
#15786=CARTESIAN_POINT('Ctrl Pts',(-0.0602576689874724,0.143416616927621,
1.2364089803923));
#15787=CARTESIAN_POINT('Ctrl Pts',(-0.049519912432359,0.147776775471332,
1.23551896995172));
#15788=CARTESIAN_POINT('Ctrl Pts',(-0.0401957081937531,0.15058053366981,
1.23475765945508));
#15789=CARTESIAN_POINT('Ctrl Pts',(-0.0277979561050489,0.153074049098719,
1.23379236394043));
#15790=CARTESIAN_POINT('Ctrl Pts',(-0.0249089320833586,0.153570629986059,
1.23357078671092));
#15791=CARTESIAN_POINT('Ctrl Pts',(-0.0209083663318317,0.154142386404852,
1.23326999052332));
#15792=CARTESIAN_POINT('Ctrl Pts',(-0.0198076328172458,0.154287695320831,
1.23318785437603));
#15793=CARTESIAN_POINT('Ctrl Pts',(-0.0179041886797547,0.154518263921758,
1.23304700410495));
#15794=CARTESIAN_POINT('Ctrl Pts',(-0.01710221149343,0.154609082188135,
1.23298802146388));
#15795=CARTESIAN_POINT('Ctrl Pts',(-0.015947708175783,0.154730728248995,
1.2329036656448));
#15796=CARTESIAN_POINT('Ctrl Pts',(-0.0155957453002853,0.154766599742278,
1.23287802278838));
#15797=CARTESIAN_POINT('Ctrl Pts',(-0.0149837427781496,0.154826865122191,
1.23283356627658));
#15798=CARTESIAN_POINT('Ctrl Pts',(-0.0147237600480891,0.154851805303272,
1.2328147222889));
#15799=CARTESIAN_POINT('Ctrl Pts',(-0.0142154178984678,0.154899278825929,
1.23277795891429));
#15800=CARTESIAN_POINT('Ctrl Pts',(-0.0139670676371253,0.154921869698375,
1.23276003624387));
#15801=CARTESIAN_POINT('Ctrl Pts',(-0.0132878934394813,0.154982003484026,
1.23271112370259));
#15802=CARTESIAN_POINT('Ctrl Pts',(-0.0128569610276343,0.155018347563041,
1.2326802004149));
#15803=CARTESIAN_POINT('Ctrl Pts',(-0.0112083343221554,0.155150467834646,
1.23256230323861));
#15804=CARTESIAN_POINT('Ctrl Pts',(-0.00998963530012164,0.155233700792277,
1.23247599911868));
#15805=CARTESIAN_POINT('Ctrl Pts',(-0.00825669940367521,0.155331560752508,
1.23235431942471));
#15806=CARTESIAN_POINT('Ctrl Pts',(-0.00774321797879547,0.155358004115675,
1.23231839454185));
#15807=CARTESIAN_POINT('Ctrl Pts',(0.00891379943519178,0.156133021579668,
1.23115694221173));
#15808=CARTESIAN_POINT('Ctrl Pts',(0.0250778714235947,0.154364029266605,
1.23014056897496));
#15809=CARTESIAN_POINT('Ctrl Pts',(0.0441742869932295,0.149189576965858,
1.22880824125981));
#15810=CARTESIAN_POINT('Ctrl Pts',(0.0476327197820298,0.14812163384217,
1.22856187345984));
#15811=CARTESIAN_POINT('Ctrl Pts',(0.0532362918842732,0.146174737072919,
1.22815190921912));
#15812=CARTESIAN_POINT('Ctrl Pts',(0.0554046816553065,0.145366697700235,
1.22799055424427));
#15813=CARTESIAN_POINT('Ctrl Pts',(0.0580831598197573,0.144299942100431,
1.22778748592316));
#15814=CARTESIAN_POINT('Ctrl Pts',(0.0586110054833854,0.144086351767268,
1.22774728357157));
#15815=CARTESIAN_POINT('Ctrl Pts',(0.0596311942272293,0.143667003538852,
1.22766921930849));
#15816=CARTESIAN_POINT('Ctrl Pts',(0.0601236753954979,0.143461600698028,
1.22763136974784));
#15817=CARTESIAN_POINT('Ctrl Pts',(0.0610292022110306,0.143078444131952,
1.22756146581913));
#15818=CARTESIAN_POINT('Ctrl Pts',(0.0614425542000458,0.142901424847058,
1.22752943664127));
#15819=CARTESIAN_POINT('Ctrl Pts',(0.0623547264745322,0.142506094838405,
1.22745848745755));
#15820=CARTESIAN_POINT('Ctrl Pts',(0.0628531777807489,0.142286953051706,
1.22741953946881));
#15821=CARTESIAN_POINT('Ctrl Pts',(0.0642128445064391,0.141680643307619,
1.22731280313361));
#15822=CARTESIAN_POINT('Ctrl Pts',(0.0650716890100894,0.14128824899465,
1.2272448367346));
#15823=CARTESIAN_POINT('Ctrl Pts',(0.0695513385731975,0.139192050424392,
1.22688740760547));
#15824=CARTESIAN_POINT('Ctrl Pts',(0.0731086525740806,0.13735696225473,
1.22659344783234));
#15825=CARTESIAN_POINT('Ctrl Pts',(0.0782668027717617,0.134438897707471,
1.22615143937549));
#15826=CARTESIAN_POINT('Ctrl Pts',(0.0799248063603882,0.133459860711217,
1.22600685624823));
#15827=CARTESIAN_POINT('Ctrl Pts',(0.094103027330795,0.124728780074457,
1.22474876560777));
#15828=CARTESIAN_POINT('Ctrl Pts',(0.105480051346796,0.115267208218718,
1.2235809571384));
#15829=CARTESIAN_POINT('Ctrl Pts',(0.117090789467428,0.102431591022558,
1.22227904061027));
#15830=CARTESIAN_POINT('Ctrl Pts',(0.118776873488069,0.100471589366699,
1.22208693209259));
#15831=CARTESIAN_POINT('Ctrl Pts',(0.120754546619859,0.0980532115760005,
1.22185871814389));
#15832=CARTESIAN_POINT('Ctrl Pts',(0.121093483359897,0.0976343235784191,
1.22181949992813));
#15833=CARTESIAN_POINT('Ctrl Pts',(0.121618066498002,0.0969790633141017,
1.22175864463112));
#15834=CARTESIAN_POINT('Ctrl Pts',(0.121805211580056,0.0967439055243859,
1.22173690314216));
#15835=CARTESIAN_POINT('Ctrl Pts',(0.122151636086156,0.0963060059019595,
1.22169660127609));
#15836=CARTESIAN_POINT('Ctrl Pts',(0.122311091405146,0.0961034124911095,
1.22167802871997));
#15837=CARTESIAN_POINT('Ctrl Pts',(0.122671100029508,0.0956436619132668,
1.22163604559286));
#15838=CARTESIAN_POINT('Ctrl Pts',(0.122871348429918,0.0953862704320105,
1.22161265671647));
#15839=CARTESIAN_POINT('Ctrl Pts',(0.123474905406152,0.0946054273645897,
1.22154204413177));
#15840=CARTESIAN_POINT('Ctrl Pts',(0.123875696463312,0.0940800245497745,
1.22149499384077));
#15841=CARTESIAN_POINT('Ctrl Pts',(0.126945161957871,0.0900025936559428,
1.22113327094287));
#15842=CARTESIAN_POINT('Ctrl Pts',(0.129464211722795,0.08633984106592,1.22082820814525));
#15843=CARTESIAN_POINT('Ctrl Pts',(0.139694322214312,0.0700082002312593,
1.21952793523499));
#15844=CARTESIAN_POINT('Ctrl Pts',(0.145728490340589,0.0563817964781705,
1.21858522679993));
#15845=CARTESIAN_POINT('Ctrl Pts',(0.150788030555051,0.03838864017662,1.21731136853533));
#15846=CARTESIAN_POINT('Ctrl Pts',(0.151694555985656,0.034633441164891,
1.21704455748844));
#15847=CARTESIAN_POINT('Ctrl Pts',(0.152640472689856,0.0299585274104973,
1.2167094165039));
#15848=CARTESIAN_POINT('Ctrl Pts',(0.15281277791523,0.0290668558830159,
1.21664536334146));
#15849=CARTESIAN_POINT('Ctrl Pts',(0.153072691823266,0.0276555802289996,
1.21654375704728));
#15850=CARTESIAN_POINT('Ctrl Pts',(0.153165487275325,0.0271369415209088,
1.2165063687731));
#15851=CARTESIAN_POINT('Ctrl Pts',(0.153334459092464,0.0261640647630248,
1.21643613967267));
#15852=CARTESIAN_POINT('Ctrl Pts',(0.153411256601335,0.0257099391232977,
1.21640331892501));
#15853=CARTESIAN_POINT('Ctrl Pts',(0.153578529731744,0.0246933642653808,
1.21632975858325));
#15854=CARTESIAN_POINT('Ctrl Pts',(0.153667934237563,0.024130748113193,
1.21628898558493));
#15855=CARTESIAN_POINT('Ctrl Pts',(0.153886481342392,0.0227049576631806,
1.21618549570191));
#15856=CARTESIAN_POINT('Ctrl Pts',(0.154011451859404,0.0218411739809905,
1.21612264820548));
#15857=CARTESIAN_POINT('Ctrl Pts',(0.154679355500181,0.0169335914477857,
1.21576468219993));
#15858=CARTESIAN_POINT('Ctrl Pts',(0.155070238804793,0.0128710845264202,
1.21546483867438));
#15859=CARTESIAN_POINT('Ctrl Pts',(0.15601372391043,-0.00378271351719459,
1.21421995094));
#15860=CARTESIAN_POINT('Ctrl Pts',(0.155194907269087,-0.0164023279397902,
1.21323498107176));
#15861=CARTESIAN_POINT('Ctrl Pts',(0.152051684110817,-0.0330962051367237,
1.21192481969369));
#15862=CARTESIAN_POINT('Ctrl Pts',(0.151057076281337,-0.0373743146290311,
1.21158901203215));
#15863=CARTESIAN_POINT('Ctrl Pts',(0.149295878405311,-0.043719071150448,
1.21109577630508));
#15864=CARTESIAN_POINT('Ctrl Pts',(0.148664320762149,-0.0458207111110437,
1.21093321511738));
#15865=CARTESIAN_POINT('Ctrl Pts',(0.147830613952849,-0.0483960199098577,
1.21073560195031));
#15866=CARTESIAN_POINT('Ctrl Pts',(0.147670352748653,-0.0488828405868441,
1.21069831709535));
#15867=CARTESIAN_POINT('Ctrl Pts',(0.147414135819535,-0.0496483830546644,
1.21063980657225));
#15868=CARTESIAN_POINT('Ctrl Pts',(0.147319790961125,-0.049927633375557,
1.21061848892346));
#15869=CARTESIAN_POINT('Ctrl Pts',(0.147141180875861,-0.0504513852073031,
1.21057855641658));
#15870=CARTESIAN_POINT('Ctrl Pts',(0.147057100701039,-0.05069594178788,
1.21055993148729));
#15871=CARTESIAN_POINT('Ctrl Pts',(0.146862806008311,-0.0512565188318028,
1.21051728555815));
#15872=CARTESIAN_POINT('Ctrl Pts',(0.146752181294994,-0.0515723937999081,
1.21049328907719));
#15873=CARTESIAN_POINT('Ctrl Pts',(0.146405596872808,-0.0525518767356506,
1.21041897692424));
#15874=CARTESIAN_POINT('Ctrl Pts',(0.146166144504838,-0.0532142536816687,
1.21036886243302));
#15875=CARTESIAN_POINT('Ctrl Pts',(0.1434115636404,-0.0606751261007935,
1.20980571108014));
#15876=CARTESIAN_POINT('Ctrl Pts',(0.140428243654262,-0.0672925627789582,
1.20931853588003));
#15877=CARTESIAN_POINT('Ctrl Pts',(0.136093794934221,-0.07535177962701,
1.20871199222262));
#15878=CARTESIAN_POINT('Ctrl Pts',(0.135163340672948,-0.0770083322369855,
1.20858658693945));
#15879=CARTESIAN_POINT('Ctrl Pts',(0.129414885904463,-0.0868174051934478,
1.20783732797264));
#15880=CARTESIAN_POINT('Ctrl Pts',(0.123891349658511,-0.0945324911768807,
1.20721852541187));
#15881=CARTESIAN_POINT('Ctrl Pts',(0.114844748748526,-0.105002712583112,
1.20627924981462));
#15882=CARTESIAN_POINT('Ctrl Pts',(0.111850965231517,-0.1081861427167,1.20597831166449));
#15883=CARTESIAN_POINT('Ctrl Pts',(0.108053577769304,-0.111897786817798,
1.2056053941144));
#15884=CARTESIAN_POINT('Ctrl Pts',(0.10737377445929,-0.112550268112186,
1.20553896142489));
#15885=CARTESIAN_POINT('Ctrl Pts',(0.106299235923427,-0.113563024269175,
1.20543443593749));
#15886=CARTESIAN_POINT('Ctrl Pts',(0.105908492122233,-0.113927517845795,
1.20539652455456));
#15887=CARTESIAN_POINT('Ctrl Pts',(0.10521187139343,-0.114570658622869,
1.20532910452442));
#15888=CARTESIAN_POINT('Ctrl Pts',(0.10490674446966,-0.114850113879322,
1.20529963059205));
#15889=CARTESIAN_POINT('Ctrl Pts',(0.104200542576868,-0.115491737597227,
1.20523154231391));
#15890=CARTESIAN_POINT('Ctrl Pts',(0.103798690028157,-0.115853038205152,
1.20519289194903));
#15891=CARTESIAN_POINT('Ctrl Pts',(0.102689790031226,-0.116839635536465,
1.20508648855512));
#15892=CARTESIAN_POINT('Ctrl Pts',(0.101978931240855,-0.117460593046961,
1.20501855632836));
#15893=CARTESIAN_POINT('Ctrl Pts',(0.0983036401510497,-0.120612564199263,
1.20466869132767));
#15894=CARTESIAN_POINT('Ctrl Pts',(0.095250734055821,-0.123037754119059,
1.20438250495474));
#15895=CARTESIAN_POINT('Ctrl Pts',(0.0904873900737765,-0.126538098902295,
1.20394200573127));
#15896=CARTESIAN_POINT('Ctrl Pts',(0.0888416159541147,-0.127698961976856,
1.20379085199413));
#15897=CARTESIAN_POINT('Ctrl Pts',(0.0750395186498058,-0.137038440380648,
1.20253192966964));
#15898=CARTESIAN_POINT('Ctrl Pts',(0.0618080310699531,-0.14349269137093,
1.20137042903056));
#15899=CARTESIAN_POINT('Ctrl Pts',(0.0453215735089315,-0.148825176660276,
1.20006580648903));
#15900=CARTESIAN_POINT('Ctrl Pts',(0.0427517391774704,-0.14958365345524,
1.19986657262076));
#15901=CARTESIAN_POINT('Ctrl Pts',(0.0396373991530571,-0.150416008195807,
1.19963105173685));
#15902=CARTESIAN_POINT('Ctrl Pts',(0.0391106593704193,-0.150553828515318,
1.19959141943221));
#15903=CARTESIAN_POINT('Ctrl Pts',(0.0382908663155733,-0.150763732761255,
1.19953006280081));
#15904=CARTESIAN_POINT('Ctrl Pts',(0.0379983157392788,-0.150837732562223,
1.19950823131869));
#15905=CARTESIAN_POINT('Ctrl Pts',(0.0374555311002822,-0.150973348975197,
1.19946784745641));
#15906=CARTESIAN_POINT('Ctrl Pts',(0.0372053616262849,-0.151035194504373,
1.19944928245664));
#15907=CARTESIAN_POINT('Ctrl Pts',(0.0366398570429438,-0.15117350513304,
1.19940742380824));
#15908=CARTESIAN_POINT('Ctrl Pts',(0.0363244363437008,-0.151249605314718,
1.19938415131125));
#15909=CARTESIAN_POINT('Ctrl Pts',(0.0353941045564056,-0.151470984274584,
1.19931572357958));
#15910=CARTESIAN_POINT('Ctrl Pts',(0.0347785336515983,-0.151613506482938,
1.19927072273528));
#15911=CARTESIAN_POINT('Ctrl Pts',(0.0303707580449849,-0.152605774027785,
1.19895035011309));
#15912=CARTESIAN_POINT('Ctrl Pts',(0.0265483514580583,-0.153316981129975,
1.19868231307047));
#15913=CARTESIAN_POINT('Ctrl Pts',(0.0215548149647822,-0.154053689659205,
1.19834002032633));
#15914=CARTESIAN_POINT('Ctrl Pts',(0.0204048210574672,-0.15421022254997,
1.19826172911738));
#15915=CARTESIAN_POINT('Ctrl Pts',(0.00446546950208221,-0.156198399855704,
1.1971827054929));
#15916=CARTESIAN_POINT('Ctrl Pts',(-0.0105101323408154,-0.155908463312189,
1.19623359751688));
#15917=CARTESIAN_POINT('Ctrl Pts',(-0.0284731120979938,-0.152957436135887,
1.1949870518704));
#15918=CARTESIAN_POINT('Ctrl Pts',(-0.0317118146184209,-0.152318920204246,
1.19475829833807));
#15919=CARTESIAN_POINT('Ctrl Pts',(-0.035769185809653,-0.151383994455983,
1.19446553096438));
#15920=CARTESIAN_POINT('Ctrl Pts',(-0.0366091589639963,-0.151183060747679,
1.19440458436024));
#15921=CARTESIAN_POINT('Ctrl Pts',(-0.0379492361250728,-0.150850672224008,
1.19430679258056));
#15922=CARTESIAN_POINT('Ctrl Pts',(-0.0384504426153417,-0.150723698481175,
1.1942700916753));
#15923=CARTESIAN_POINT('Ctrl Pts',(-0.0393982147852614,-0.150478558444309,
1.19420044862472));
#15924=CARTESIAN_POINT('Ctrl Pts',(-0.0398449063300372,-0.150360896880929,
1.19416752309115));
#15925=CARTESIAN_POINT('Ctrl Pts',(-0.0408557687123586,-0.150089808081514,
1.19409277717798));
#15926=CARTESIAN_POINT('Ctrl Pts',(-0.0414196091152278,-0.149935186965903,
1.1940509185778));
#15927=CARTESIAN_POINT('Ctrl Pts',(-0.043083862066403,-0.14946869737273,
1.19392686526356));
#15928=CARTESIAN_POINT('Ctrl Pts',(-0.0441817003601429,-0.149147872556758,
1.19384438143269));
#15929=CARTESIAN_POINT('Ctrl Pts',(-0.053882677392569,-0.146196420891749,
1.19310957500982));
#15930=CARTESIAN_POINT('Ctrl Pts',(-0.062244394346004,-0.142836673773181,
1.19243306582289));
#15931=CARTESIAN_POINT('Ctrl Pts',(-0.0722167194573638,-0.137787229550308,
1.19157367999377));
#15932=CARTESIAN_POINT('Ctrl Pts',(-0.0741447109484442,-0.136759411591685,
1.1914050161732));
#15933=CARTESIAN_POINT('Ctrl Pts',(-0.0820255930790969,-0.132342445727668,
1.19070586767833));
#15934=CARTESIAN_POINT('Ctrl Pts',(-0.0877731821701352,-0.128602463025855,
1.19017221128851));
#15935=CARTESIAN_POINT('Ctrl Pts',(-0.0958176736424423,-0.122576600687255,
1.18940312245267));
#15936=CARTESIAN_POINT('Ctrl Pts',(-0.098320053272869,-0.120578686991808,
1.18916050196915));
#15937=CARTESIAN_POINT('Ctrl Pts',(-0.101657803967322,-0.117740752355734,
1.18883396093112));
#15938=CARTESIAN_POINT('Ctrl Pts',(-0.102547762045985,-0.116966450663619,
1.18874659791094));
#15939=CARTESIAN_POINT('Ctrl Pts',(-0.104060824349233,-0.115619475999487,
1.18859767749402));
#15940=CARTESIAN_POINT('Ctrl Pts',(-0.104688208673864,-0.115051716396478,
1.18853581032601));
#15941=CARTESIAN_POINT('Ctrl Pts',(-0.105576358938092,-0.114234692579732,
1.18844809796628));
#15942=CARTESIAN_POINT('Ctrl Pts',(-0.105840924016965,-0.113989610779967,
1.18842195315675));
#15943=CARTESIAN_POINT('Ctrl Pts',(-0.10629643498847,-0.113564691721451,
1.18837691335344));
#15944=CARTESIAN_POINT('Ctrl Pts',(-0.106487781665436,-0.113385288540765,
1.18835798572348));
#15945=CARTESIAN_POINT('Ctrl Pts',(-0.106858648442976,-0.113035803642193,
1.18832128653134));
#15946=CARTESIAN_POINT('Ctrl Pts',(-0.107038216592967,-0.11286577799774,
1.18830351079552));
#15947=CARTESIAN_POINT('Ctrl Pts',(-0.107523063210476,-0.112404499014242,
1.18825549475797));
#15948=CARTESIAN_POINT('Ctrl Pts',(-0.107827566462819,-0.112112427690842,
1.18822531685948));
#15949=CARTESIAN_POINT('Ctrl Pts',(-0.108961442778839,-0.111015951073513,
1.18811284382975));
#15950=CARTESIAN_POINT('Ctrl Pts',(-0.109783061779411,-0.110203525181222,
1.18803114362674));
#15951=CARTESIAN_POINT('Ctrl Pts',(-0.117246506674956,-0.102657273156656,
1.18728623390129));
#15952=CARTESIAN_POINT('Ctrl Pts',(-0.12327134052086,-0.0953388315933695,
1.18666385947147));
#15953=CARTESIAN_POINT('Ctrl Pts',(-0.135465683443261,-0.0774209234427562,
1.1852372146688));
#15954=CARTESIAN_POINT('Ctrl Pts',(-0.141122963392481,-0.0665522584193492,
1.18443499002265));
#15955=CARTESIAN_POINT('Ctrl Pts',(-0.145930685351747,-0.0538690057411872,
1.18348768209875));
#15956=CARTESIAN_POINT('Ctrl Pts',(-0.146393910136079,-0.0525971251904986,
1.18339262430345));
#15957=CARTESIAN_POINT('Ctrl Pts',(-0.147044198216264,-0.050736452392353,
1.18325339859662));
#15958=CARTESIAN_POINT('Ctrl Pts',(-0.147244455766494,-0.0501523085864997,
1.18320966673442));
#15959=CARTESIAN_POINT('Ctrl Pts',(-0.147589803111224,-0.0491250436512505,
1.18313271302091));
#15960=CARTESIAN_POINT('Ctrl Pts',(-0.147736389696134,-0.0486824305785562,
1.18309954088138));
#15961=CARTESIAN_POINT('Ctrl Pts',(-0.148017398269068,-0.0478209766126687,
1.18303494510264));
#15962=CARTESIAN_POINT('Ctrl Pts',(-0.148152038073715,-0.0474022109379951,
1.18300352897577));
#15963=CARTESIAN_POINT('Ctrl Pts',(-0.148470013382179,-0.0463986340477675,
1.182928200616));
#15964=CARTESIAN_POINT('Ctrl Pts',(-0.148651671152288,-0.0458133032961269,
1.18288423395795));
#15965=CARTESIAN_POINT('Ctrl Pts',(-0.149296628477842,-0.0436909189728369,
1.18272468669071));
#15966=CARTESIAN_POINT('Ctrl Pts',(-0.149739570847545,-0.042147837890083,
1.18260844787047));
#15967=CARTESIAN_POINT('Ctrl Pts',(-0.153749221781477,-0.027317553069109,
1.1814886068959));
#15968=CARTESIAN_POINT('Ctrl Pts',(-0.155561372408739,-0.0136219463444048,
1.180425675306));
#15969=CARTESIAN_POINT('Ctrl Pts',(-0.155546145707511,0.00470322754191661,
1.17900566089395));
#15970=CARTESIAN_POINT('Ctrl Pts',(-0.155340598153982,0.00927506209337149,
1.17865239274666));
#15971=CARTESIAN_POINT('Ctrl Pts',(-0.154604355622536,0.0175221551153412,
1.17802297719083));
#15972=CARTESIAN_POINT('Ctrl Pts',(-0.154143062027286,0.0212003486761419,
1.1777451365529));
#15973=CARTESIAN_POINT('Ctrl Pts',(-0.153459731382905,0.0254212079748754,
1.1774321256691));
#15974=CARTESIAN_POINT('Ctrl Pts',(-0.153365608226058,0.0259830177487437,
1.17739058327479));
#15975=CARTESIAN_POINT('Ctrl Pts',(-0.153210617183231,0.0268779451206424,
1.17732461425008));
#15976=CARTESIAN_POINT('Ctrl Pts',(-0.153151745350456,0.0272113956569777,
1.17730007970307));
#15977=CARTESIAN_POINT('Ctrl Pts',(-0.153045778928927,0.0278003515984167,
1.17725682932418));
#15978=CARTESIAN_POINT('Ctrl Pts',(-0.152999132509397,0.0280559343562187,
1.17723808842471));
#15979=CARTESIAN_POINT('Ctrl Pts',(-0.15289920112623,0.028595811821361,
1.17719856145606));
#15980=CARTESIAN_POINT('Ctrl Pts',(-0.152845763592181,0.0288800746954604,
1.17717778419618));
#15981=CARTESIAN_POINT('Ctrl Pts',(-0.152700101637927,0.0296431993785588,
1.17712209597818));
#15982=CARTESIAN_POINT('Ctrl Pts',(-0.152606416675189,0.0301217847467337,
1.17708726687379));
#15983=CARTESIAN_POINT('Ctrl Pts',(-0.152139775951923,0.0324475286485161,
1.1769184383847));
#15984=CARTESIAN_POINT('Ctrl Pts',(-0.151735504739387,0.0342883508820558,
1.17678612513213));
#15985=CARTESIAN_POINT('Ctrl Pts',(-0.150486139297179,0.0395214228458968,
1.17641255207618));
#15986=CARTESIAN_POINT('Ctrl Pts',(-0.149559983868727,0.0428933099273924,
1.17617493976527));
#15987=CARTESIAN_POINT('Ctrl Pts',(-0.147778643598194,0.0486159671845375,
1.17577253304438));
#15988=CARTESIAN_POINT('Ctrl Pts',(-0.146979024622191,0.0509824172356096,
1.17560638874482));
#15989=CARTESIAN_POINT('Ctrl Pts',(-0.146030370902248,0.0535817681064151,
1.17542318066258));
#15990=CARTESIAN_POINT('Ctrl Pts',(-0.145937337713217,0.0538346408989314,
1.17540535012595));
#15991=CARTESIAN_POINT('Ctrl Pts',(-0.140900274802583,0.0674168316221702,
1.17444718201298));
#15992=CARTESIAN_POINT('Ctrl Pts',(-0.134153700911123,0.0800041192216123,
1.17352759854769));
#15993=CARTESIAN_POINT('Ctrl Pts',(-0.124878851177497,0.0927549672484988,
1.17242943214729));
#15994=CARTESIAN_POINT('Ctrl Pts',(-0.123947166271319,0.0939963355126361,
1.17232065427079));
#15995=CARTESIAN_POINT('Ctrl Pts',(-0.122627142882841,0.0957013663978207,
1.17216851787292));
#15996=CARTESIAN_POINT('Ctrl Pts',(-0.12225441801618,0.0961770500637115,
1.17212577251591));
#15997=CARTESIAN_POINT('Ctrl Pts',(-0.121607013823502,0.0969934441650213,
1.1720518822928));
#15998=CARTESIAN_POINT('Ctrl Pts',(-0.121333648908475,0.0973351922866325,
1.17202078990518));
#15999=CARTESIAN_POINT('Ctrl Pts',(-0.120765291084357,0.0980396119909781,
1.17195636362376));
#16000=CARTESIAN_POINT('Ctrl Pts',(-0.120470098444528,0.0984021159428093,
1.17192302192006));
#16001=CARTESIAN_POINT('Ctrl Pts',(-0.119776209733078,0.0992464265177424,
1.17184492296877));
#16002=CARTESIAN_POINT('Ctrl Pts',(-0.119376235764783,0.099727167351963,
1.17180011426692));
#16003=CARTESIAN_POINT('Ctrl Pts',(-0.118073702044355,0.10127365805355,
1.17165485379448));
#16004=CARTESIAN_POINT('Ctrl Pts',(-0.117159708419134,0.102329640948196,
1.17155393568649));
#16005=CARTESIAN_POINT('Ctrl Pts',(-0.112450723012935,0.107624373374184,
1.17103889718331));
#16006=CARTESIAN_POINT('Ctrl Pts',(-0.108439905333702,0.111664420554101,
1.17061577500794));
#16007=CARTESIAN_POINT('Ctrl Pts',(-0.0970908770588136,0.121906999106413,
1.1694574942426));
#16008=CARTESIAN_POINT('Ctrl Pts',(-0.0893848155286102,0.127664710528775,
1.16870907607776));
#16009=CARTESIAN_POINT('Ctrl Pts',(-0.0755642935341161,0.13612300119827,
1.16745655961448));
#16010=CARTESIAN_POINT('Ctrl Pts',(-0.0697158911162234,0.139208985486056,
1.16695080130333));
#16011=CARTESIAN_POINT('Ctrl Pts',(-0.063688625668895,0.14191392271517,
1.16646420862114));
#16012=CARTESIAN_POINT('',(-0.155549962195241,-0.000108448416659708,1.16559437743963));
#16013=CARTESIAN_POINT('Ctrl Pts',(-0.063688650312489,0.14191391165553,
1.15273999320994));
#16014=CARTESIAN_POINT('Ctrl Pts',(-0.0739614464780745,0.137303648186015,
1.153606477709));
#16015=CARTESIAN_POINT('Ctrl Pts',(-0.0837099676320785,0.131588667287672,
1.15449238101734));
#16016=CARTESIAN_POINT('Ctrl Pts',(-0.0946672385213198,0.123448594247607,
1.15551736220776));
#16017=CARTESIAN_POINT('Ctrl Pts',(-0.0965409102401436,0.121988916665539,
1.1556936561989));
#16018=CARTESIAN_POINT('Ctrl Pts',(-0.0987661346232789,0.120171964062281,
1.15590358349414));
#16019=CARTESIAN_POINT('Ctrl Pts',(-0.09915020928153,0.11985527236038,1.15593983744304));
#16020=CARTESIAN_POINT('Ctrl Pts',(-0.0997790856266643,0.11933163583965,
1.15599922346576));
#16021=CARTESIAN_POINT('Ctrl Pts',(-0.100024775746547,0.119125771697638,
1.15602243067));
#16022=CARTESIAN_POINT('Ctrl Pts',(-0.100466609141012,0.118753228160401,
1.1560641735315));
#16023=CARTESIAN_POINT('Ctrl Pts',(-0.100662975252751,0.118586821220957,
1.15608272836353));
#16024=CARTESIAN_POINT('Ctrl Pts',(-0.101086236400222,0.1182263272587,1.15612272882583));
#16025=CARTESIAN_POINT('Ctrl Pts',(-0.101312985219345,0.118032074779148,
1.15614416196145));
#16026=CARTESIAN_POINT('Ctrl Pts',(-0.101936280623036,0.117494987012195,
1.15620309422219));
#16027=CARTESIAN_POINT('Ctrl Pts',(-0.102331660733526,0.117150793906415,
1.15624049523621));
#16028=CARTESIAN_POINT('Ctrl Pts',(-0.103221703022011,0.116368034834469,
1.15632475031685));
#16029=CARTESIAN_POINT('Ctrl Pts',(-0.10371532835213,0.115928297712132,
1.15637152234746));
#16030=CARTESIAN_POINT('Ctrl Pts',(-0.105251243783014,0.114542392614199,
1.15651724711886));
#16031=CARTESIAN_POINT('Ctrl Pts',(-0.10628353675908,0.113585184664541,
1.15661547129891));
#16032=CARTESIAN_POINT('Ctrl Pts',(-0.110319236855961,0.109739823934036,
1.15700129835694));
#16033=CARTESIAN_POINT('Ctrl Pts',(-0.113219299269509,0.106745300377919,
1.15728266262057));
#16034=CARTESIAN_POINT('Ctrl Pts',(-0.123121353296417,0.0956624886927571,
1.15827429258106));
#16035=CARTESIAN_POINT('Ctrl Pts',(-0.129405384377851,0.0869737594051406,
1.15896519757145));
#16036=CARTESIAN_POINT('Ctrl Pts',(-0.135856822194371,0.075786866241766,
1.15983094069939));
#16037=CARTESIAN_POINT('Ctrl Pts',(-0.136923953371235,0.0738414219364007,
1.15998060764377));
#16038=CARTESIAN_POINT('Ctrl Pts',(-0.139829350213905,0.0682650315463581,
1.16040818602853));
#16039=CARTESIAN_POINT('Ctrl Pts',(-0.141567128377214,0.064584091911264,
1.1606887999465));
#16040=CARTESIAN_POINT('Ctrl Pts',(-0.143499512851601,0.0600370926553177,
1.16103563514014));
#16041=CARTESIAN_POINT('Ctrl Pts',(-0.143833769983821,0.0592318262448007,
1.16109706374737));
#16042=CARTESIAN_POINT('Ctrl Pts',(-0.14437506188982,0.0578961839209958,
1.16119898018359));
#16043=CARTESIAN_POINT('Ctrl Pts',(-0.144585989219853,0.0573673976574312,
1.16123933670269));
#16044=CARTESIAN_POINT('Ctrl Pts',(-0.144962239669032,0.056408896015496,
1.16131250785242));
#16045=CARTESIAN_POINT('Ctrl Pts',(-0.145128567555238,0.0559795797640432,
1.16134528836012));
#16046=CARTESIAN_POINT('Ctrl Pts',(-0.145481129207378,0.0550574346118643,
1.16141571697613));
#16047=CARTESIAN_POINT('Ctrl Pts',(-0.145666769589473,0.0545643866111579,
1.16145338442744));
#16048=CARTESIAN_POINT('Ctrl Pts',(-0.146165695174164,0.0532185812879525,
1.16155623585675));
#16049=CARTESIAN_POINT('Ctrl Pts',(-0.146474015771233,0.0523640189332964,
1.16162158375167));
#16050=CARTESIAN_POINT('Ctrl Pts',(-0.148055989901746,0.0478559950834417,
1.16196656378922));
#16051=CARTESIAN_POINT('Ctrl Pts',(-0.149200378438692,0.04415896912224,
1.16225040556449));
#16052=CARTESIAN_POINT('Ctrl Pts',(-0.153762637149028,0.027206489070008,
1.16355757203731));
#16053=CARTESIAN_POINT('Ctrl Pts',(-0.1555589075521,0.013579755087206,1.16463088765355));
#16054=CARTESIAN_POINT('Ctrl Pts',(-0.155549966785486,-0.000101651532510474,
1.16568277993484));
#16055=CARTESIAN_POINT('Ctrl Pts',(-0.155549962195241,-0.000108448416659708,
1.16559437743963));
#16056=CARTESIAN_POINT('Ctrl Pts',(-0.155545273848805,-0.00683304738623575,
1.16607786915525));
#16057=CARTESIAN_POINT('Ctrl Pts',(-0.15510450926904,-0.0135425737898805,
1.16656136087087));
#16058=CARTESIAN_POINT('Ctrl Pts',(-0.154233530772585,-0.0201945657398758,
1.1670448525865));
#16059=CARTESIAN_POINT('Ctrl Pts',(-0.152905315892433,-0.0303386447574308,
1.16778216228327));
#16060=CARTESIAN_POINT('Ctrl Pts',(-0.150567052089225,-0.0403891467591377,
1.16851947198005));
#16061=CARTESIAN_POINT('Ctrl Pts',(-0.147250196665396,-0.0501316475093558,
1.16925678167683));
#16062=CARTESIAN_POINT('Ctrl Pts',(-0.143912697417014,-0.0599347847512155,
1.16999868032612));
#16063=CARTESIAN_POINT('Ctrl Pts',(-0.139584514653525,-0.0694251282585468,
1.1707405789754));
#16064=CARTESIAN_POINT('Ctrl Pts',(-0.134349708248288,-0.0783961631306013,
1.17148247762469));
#16065=CARTESIAN_POINT('Ctrl Pts',(-0.12915924963263,-0.0872911979491647,
1.17221809111983));
#16066=CARTESIAN_POINT('Ctrl Pts',(-0.123077963757599,-0.0956748891994967,
1.17295370461497));
#16067=CARTESIAN_POINT('Ctrl Pts',(-0.1162338432083,-0.103370673757252,
1.17368931811011));
#16068=CARTESIAN_POINT('Ctrl Pts',(-0.109302007399008,-0.111165088626745,
1.17443435933647));
#16069=CARTESIAN_POINT('Ctrl Pts',(-0.10158825165106,-0.118253078296368,
1.17517940056283));
#16070=CARTESIAN_POINT('Ctrl Pts',(-0.0932649572480594,-0.124488755514374,
1.17592444178919));
#16071=CARTESIAN_POINT('Ctrl Pts',(-0.0849416628450579,-0.130724432732381,
1.17666948301555));
#16072=CARTESIAN_POINT('Ctrl Pts',(-0.0760096876809342,-0.136107321535937,
1.17741452424191));
#16073=CARTESIAN_POINT('Ctrl Pts',(-0.0666694354545085,-0.140538211445063,
1.17815956546827));
#16074=CARTESIAN_POINT('Ctrl Pts',(-0.0574261099938138,-0.144923120601443,
1.17889687516504));
#16075=CARTESIAN_POINT('Ctrl Pts',(-0.0477136841253745,-0.148408640914046,
1.17963418486182));
#16076=CARTESIAN_POINT('Ctrl Pts',(-0.0377293758646995,-0.1509049260192,
1.1803714945586));
#16077=CARTESIAN_POINT('Ctrl Pts',(-0.0276829261230913,-0.15341674778941,
1.18111339320789));
#16078=CARTESIAN_POINT('Ctrl Pts',(-0.0173620635116654,-0.154926575884814,
1.18185529185717));
#16079=CARTESIAN_POINT('Ctrl Pts',(-0.00698588565388585,-0.155393049721121,
1.18259719050646));
#16080=CARTESIAN_POINT('Ctrl Pts',(0.00330238817903047,-0.155855571723885,
1.1833328040016));
#16081=CARTESIAN_POINT('Ctrl Pts',(0.013644103539955,-0.155292330862292,
1.18406841749674));
#16082=CARTESIAN_POINT('Ctrl Pts',(0.0238215047300092,-0.153715120962117,
1.18480403099188));
#16083=CARTESIAN_POINT('Ctrl Pts',(0.0341293409971891,-0.152117697306865,
1.18554907221824));
#16084=CARTESIAN_POINT('Ctrl Pts',(0.0442676532751995,-0.149480227032185,
1.1862941134446));
#16085=CARTESIAN_POINT('Ctrl Pts',(0.0540203889062351,-0.145868434153586,
1.18703915467097));
#16086=CARTESIAN_POINT('Ctrl Pts',(0.06377312453727,-0.142256641274988,
1.18778419589733));
#16087=CARTESIAN_POINT('Ctrl Pts',(0.0731394184026082,-0.137670988493469,
1.18852923712369));
#16088=CARTESIAN_POINT('Ctrl Pts',(0.081927239882205,-0.132226055924253,
1.18927427835005));
#16089=CARTESIAN_POINT('Ctrl Pts',(0.0906238673454805,-0.126837627150743,
1.19001158804683));
#16090=CARTESIAN_POINT('Ctrl Pts',(0.0988192084139562,-0.120567343834098,
1.19074889774361));
#16091=CARTESIAN_POINT('Ctrl Pts',(0.106330827725443,-0.113532187397328,
1.19148620744039));
#16092=CARTESIAN_POINT('Ctrl Pts',(0.113889198713248,-0.106453244748434,
1.19222810608967));
#16093=CARTESIAN_POINT('Ctrl Pts',(0.120754500477318,-0.0986003842753631,
1.19297000473896));
#16094=CARTESIAN_POINT('Ctrl Pts',(0.12677317071246,-0.0901352632852945,
1.19371190338825));
#16095=CARTESIAN_POINT('Ctrl Pts',(0.132740852486812,-0.0817418563903375,
1.19444751688339));
#16096=CARTESIAN_POINT('Ctrl Pts',(0.137875666974655,-0.0727473026465363,
1.19518313037852));
#16097=CARTESIAN_POINT('Ctrl Pts',(0.142069439965937,-0.0633409561639615,
1.19591874387366));
#16098=CARTESIAN_POINT('Ctrl Pts',(0.146316960971395,-0.0538140565553291,
1.19666378510002));
#16099=CARTESIAN_POINT('Ctrl Pts',(0.149598704911011,-0.0438656002926485,
1.19740882632638));
#16100=CARTESIAN_POINT('Ctrl Pts',(0.151852733305272,-0.0337127555639993,
1.19815386755274));
#16101=CARTESIAN_POINT('Ctrl Pts',(0.154106761699532,-0.0235599108353509,
1.1988989087791));
#16102=CARTESIAN_POINT('Ctrl Pts',(0.155332994178447,-0.0132036554256187,
1.19964395000546));
#16103=CARTESIAN_POINT('Ctrl Pts',(0.15552356776244,-0.0028674676008397,
1.20038899123183));
#16104=CARTESIAN_POINT('Ctrl Pts',(0.155712163703785,0.00736145831798887,
1.2011263009286));
#16105=CARTESIAN_POINT('Ctrl Pts',(0.154887989418757,0.0176474101381822,
1.20186361062538));
#16106=CARTESIAN_POINT('Ctrl Pts',(0.153050402774849,0.0277736693732832,
1.20260092032215));
#16107=CARTESIAN_POINT('Ctrl Pts',(0.151201379148786,0.037962953580048,
1.20334281897144));
#16108=CARTESIAN_POINT('Ctrl Pts',(0.148326274897554,0.0479895961619971,
1.20408471762073));
#16109=CARTESIAN_POINT('Ctrl Pts',(0.144477641750931,0.0576369112122566,
1.20482661627002));
#16110=CARTESIAN_POINT('Ctrl Pts',(0.140661613128677,0.0672024969558601,
1.20556222976516));
#16111=CARTESIAN_POINT('Ctrl Pts',(0.135888857329139,0.0763942932412717,
1.20629784326029));
#16112=CARTESIAN_POINT('Ctrl Pts',(0.130259809785238,0.0850187300229408,
1.20703345675543));
#16113=CARTESIAN_POINT('Ctrl Pts',(0.124558619536452,0.0937536988604648,
1.20777849798179));
#16114=CARTESIAN_POINT('Ctrl Pts',(0.117979520416751,0.101905820061075,
1.20852353920816));
#16115=CARTESIAN_POINT('Ctrl Pts',(0.110671389748095,0.10930528802956,1.20926858043452));
#16116=CARTESIAN_POINT('Ctrl Pts',(0.10336325907944,0.116704755998046,1.21001362166088));
#16117=CARTESIAN_POINT('Ctrl Pts',(0.095326874815334,0.123350972979471,
1.21075866288724));
#16118=CARTESIAN_POINT('Ctrl Pts',(0.0867457397866691,0.129116145887583,
1.2115037041136));
#16119=CARTESIAN_POINT('Ctrl Pts',(0.0782536539233378,0.134821491764217,
1.21224101381038));
#16120=CARTESIAN_POINT('Ctrl Pts',(0.0691644551944208,0.139706830500264,
1.21297832350716));
#16121=CARTESIAN_POINT('Ctrl Pts',(0.0596598825377341,0.143654101631606,
1.21371563320394));
#16122=CARTESIAN_POINT('Ctrl Pts',(0.0500961542335173,0.147625940240959,
1.21445753185322));
#16123=CARTESIAN_POINT('Ctrl Pts',(0.040112660108692,0.15064746816253,1.21519943050251));
#16124=CARTESIAN_POINT('Ctrl Pts',(0.0299199574112516,0.152645336150532,
1.2159413291518));
#16125=CARTESIAN_POINT('Ctrl Pts',(0.0198136043893243,0.154626278769709,
1.21667694264694));
#16126=CARTESIAN_POINT('Ctrl Pts',(0.00950250084430574,0.155600681437315,
1.21741255614208));
#16127=CARTESIAN_POINT('Ctrl Pts',(-0.000796251833269475,0.155547962002136,
1.21814816963721));
#16128=CARTESIAN_POINT('Ctrl Pts',(-0.0112269948465221,0.155494566906889,
1.21889321086358));
#16129=CARTESIAN_POINT('Ctrl Pts',(-0.0216440962629482,0.154387488149287,
1.21963825208994));
#16130=CARTESIAN_POINT('Ctrl Pts',(-0.0318241528047296,0.152259731374586,
1.2203832933163));
#16131=CARTESIAN_POINT('Ctrl Pts',(-0.0420042093465111,0.150131974599885,
1.22112833454266));
#16132=CARTESIAN_POINT('Ctrl Pts',(-0.0519462969147143,0.146983869298261,
1.22187337576902));
#16133=CARTESIAN_POINT('Ctrl Pts',(-0.0614435346592933,0.142900295830947,
1.22261841699538));
#16134=CARTESIAN_POINT('Ctrl Pts',(-0.0621942538492122,0.142577505452544,
1.22267730956614));
#16135=CARTESIAN_POINT('Ctrl Pts',(-0.0629426524443354,0.142248703184176,
1.2227362021369));
#16136=CARTESIAN_POINT('Ctrl Pts',(-0.0636886258329928,0.141913922641526,
1.22279509470766));
#16137=CARTESIAN_POINT('Origin',(0.,0.,-0.129405622560373));
#16138=CARTESIAN_POINT('',(-0.0636118382027688,0.141739365081128,1.30659839996889));
#16139=CARTESIAN_POINT('',(-0.0636380227784817,0.141804318283712,1.29280313411188));
#16140=CARTESIAN_POINT('',(-0.0636886258329924,0.141913922641526,-0.129405622560373));
#16141=CARTESIAN_POINT('',(-0.155313773579517,1.76826588726336E-5,1.24941564258899));
#16142=CARTESIAN_POINT('Ctrl Pts',(-0.155296357294745,1.6960594703571E-5,
1.24940562256037));
#16143=CARTESIAN_POINT('Ctrl Pts',(-0.155270088652903,-0.0269814387089377,
1.2513319394326));
#16144=CARTESIAN_POINT('Ctrl Pts',(-0.135721405315835,-0.105941739255518,
1.25696316059875));
#16145=CARTESIAN_POINT('Ctrl Pts',(-0.0100014200241654,-0.183584930129994,
1.26629928605883));
#16146=CARTESIAN_POINT('Ctrl Pts',(0.148824776878697,-0.107956661491269,
1.2774139989406));
#16147=CARTESIAN_POINT('Ctrl Pts',(0.171409230594902,0.0665006063145147,
1.28852871182238));
#16148=CARTESIAN_POINT('Ctrl Pts',(0.0538351618240076,0.165910646501256,
1.29825684549848));
#16149=CARTESIAN_POINT('Ctrl Pts',(-0.0339132747862035,0.154841375238312,
1.30428007488065));
#16150=CARTESIAN_POINT('Ctrl Pts',(-0.0636118382027626,0.141739365081131,
1.30659839996889));
#16151=CARTESIAN_POINT('Ctrl Pts',(-0.155549997573297,2.74763022365475E-5,
1.24955154822045));
#16152=CARTESIAN_POINT('Ctrl Pts',(-0.155549897792255,0.00059236093511806,
1.2495109550988));
#16153=CARTESIAN_POINT('Ctrl Pts',(-0.155546720919687,0.00115723502798456,
1.24947026588767));
#16154=CARTESIAN_POINT('Ctrl Pts',(-0.155528391633386,0.00281276570515671,
1.24935072391838));
#16155=CARTESIAN_POINT('Ctrl Pts',(-0.15550484427919,0.00390327401653914,
1.24927161143684));
#16156=CARTESIAN_POINT('Ctrl Pts',(-0.155311207207001,0.009932153623866,
1.24883212517115));
#16157=CARTESIAN_POINT('Ctrl Pts',(-0.154917365575576,0.0148599720765029,
1.24846492479375));
#16158=CARTESIAN_POINT('Ctrl Pts',(-0.152420345190767,0.0343569442760507,
1.2469797991768));
#16159=CARTESIAN_POINT('Ctrl Pts',(-0.148489503867105,0.0486122476048482,
1.24581281742909));
#16160=CARTESIAN_POINT('Ctrl Pts',(-0.141578533564202,0.0644830634541898,
1.24451056172612));
#16161=CARTESIAN_POINT('Ctrl Pts',(-0.140482173517817,0.0668379212591646,
1.24431753404194));
#16162=CARTESIAN_POINT('Ctrl Pts',(-0.139087357506472,0.0696476891977804,
1.24408837602936));
#16163=CARTESIAN_POINT('Ctrl Pts',(-0.138844925967983,0.0701297382347594,
1.24404910336281));
#16164=CARTESIAN_POINT('Ctrl Pts',(-0.138463488660094,0.0708784538858501,
1.24398818212399));
#16165=CARTESIAN_POINT('Ctrl Pts',(-0.138326212901935,0.0711459889633148,
1.24396642878445));
#16166=CARTESIAN_POINT('Ctrl Pts',(-0.13806980264326,0.0716421563112034,
1.24392611618626));
#16167=CARTESIAN_POINT('Ctrl Pts',(-0.137950876737586,0.0718708882097017,
1.24390754469048));
#16168=CARTESIAN_POINT('Ctrl Pts',(-0.137680326337336,0.0723880960045699,
1.2438655782523));
#16169=CARTESIAN_POINT('Ctrl Pts',(-0.137528363896171,0.0726763911654976,
1.24384220493201));
#16170=CARTESIAN_POINT('Ctrl Pts',(-0.137066046733504,0.073546832286427,
1.24377168570132));
#16171=CARTESIAN_POINT('Ctrl Pts',(-0.136752888145346,0.0741274937650393,
1.24372471253454));
#16172=CARTESIAN_POINT('Ctrl Pts',(-0.134318256015227,0.078573868258185,
1.24336541512064));
#16173=CARTESIAN_POINT('Ctrl Pts',(-0.132036714779972,0.0823502380113913,
1.2430625557419));
#16174=CARTESIAN_POINT('Ctrl Pts',(-0.123133412475427,0.0957631579702634,
1.24197601185141));
#16175=CARTESIAN_POINT('Ctrl Pts',(-0.115592095511441,0.10474216075819,
1.24122458869673));
#16176=CARTESIAN_POINT('Ctrl Pts',(-0.103849755793823,0.115893556086649,
1.24014268286757));
#16177=CARTESIAN_POINT('Ctrl Pts',(-0.100450942899601,0.118851549300029,
1.23983829631164));
#16178=CARTESIAN_POINT('Ctrl Pts',(-0.094807264280304,0.123348057235167,
1.23934153179967));
#16179=CARTESIAN_POINT('Ctrl Pts',(-0.0926419890821297,0.124982482307883,
1.23915285454269));
#16180=CARTESIAN_POINT('Ctrl Pts',(-0.0899495996815603,0.126906375847685,
1.23891996101002));
#16181=CARTESIAN_POINT('Ctrl Pts',(-0.0894620117077727,0.127250568395987,
1.23887785168188));
#16182=CARTESIAN_POINT('Ctrl Pts',(-0.0885186639883457,0.127908383982087,
1.23879650332115));
#16183=CARTESIAN_POINT('Ctrl Pts',(-0.0880631874172144,0.128222398880844,
1.23875727987107));
#16184=CARTESIAN_POINT('Ctrl Pts',(-0.0876020550427119,0.128536697000022,
1.23871762066113));
#16185=CARTESIAN_POINT('Ctrl Pts',(-0.0875980592786067,0.128539420155855,
1.23871727701347));
#16186=CARTESIAN_POINT('Ctrl Pts',(-0.0875899532725982,0.128544943931847,
1.23871657988056));
#16187=CARTESIAN_POINT('Ctrl Pts',(-0.0875858430233142,0.128547744541213,
1.23871622639491));
#16188=CARTESIAN_POINT('Ctrl Pts',(-0.0875774993152979,0.128553429125475,
1.23871550883577));
#16189=CARTESIAN_POINT('Ctrl Pts',(-0.0875732658480037,0.128556313088679,
1.2387151447618));
#16190=CARTESIAN_POINT('Ctrl Pts',(-0.0875646661091541,0.128562170863362,
1.23871440520163));
#16191=CARTESIAN_POINT('Ctrl Pts',(-0.0875602998290239,0.128565144661216,
1.23871402971497));
#16192=CARTESIAN_POINT('Ctrl Pts',(-0.0875514238927936,0.128571189245924,
1.23871326642114));
#16193=CARTESIAN_POINT('Ctrl Pts',(-0.087546914226689,0.128574260017904,
1.23871287861341));
#16194=CARTESIAN_POINT('Ctrl Pts',(-0.087537739829984,0.128580506443638,
1.23871208967321));
#16195=CARTESIAN_POINT('Ctrl Pts',(-0.0875330750879808,0.128583682080917,
1.23871168854011));
#16196=CARTESIAN_POINT('Ctrl Pts',(-0.0875235775708511,0.128590146991806,
1.238710871835));
#16197=CARTESIAN_POINT('Ctrl Pts',(-0.0875187447831786,0.128593436246769,
1.23871045626231));
#16198=CARTESIAN_POINT('Ctrl Pts',(-0.0875088967333875,0.128600138138745,
1.23870960943737));
#16199=CARTESIAN_POINT('Ctrl Pts',(-0.0875038814573037,0.128603550754655,
1.23870917818436));
#16200=CARTESIAN_POINT('Ctrl Pts',(-0.0874936522875372,0.128610510259281,
1.23870829861201));
#16201=CARTESIAN_POINT('Ctrl Pts',(-0.0874884383775677,0.128614057124482,
1.23870785029175));
#16202=CARTESIAN_POINT('Ctrl Pts',(-0.0874777938169087,0.128621297350242,
1.23870693502806));
#16203=CARTESIAN_POINT('Ctrl Pts',(-0.0874723631478317,0.12862499068403,
1.23870646808361));
#16204=CARTESIAN_POINT('Ctrl Pts',(-0.0874612646317786,0.128632537625535,
1.23870551381596));
#16205=CARTESIAN_POINT('Ctrl Pts',(-0.0874555967642515,0.128636391202425,
1.23870502649164));
#16206=CARTESIAN_POINT('Ctrl Pts',(-0.0874440006928635,0.128644274237941,
1.23870402947504));
#16207=CARTESIAN_POINT('Ctrl Pts',(-0.0874380724658325,0.12864830366095,
1.23870351978149));
#16208=CARTESIAN_POINT('Ctrl Pts',(-0.0874259292990253,0.128656556158875,
1.23870247576086));
#16209=CARTESIAN_POINT('Ctrl Pts',(-0.0874197143313886,0.128660779193499,
1.23870194143222));
#16210=CARTESIAN_POINT('Ctrl Pts',(-0.0874069674644387,0.128669439265987,
1.23870084554592));
#16211=CARTESIAN_POINT('Ctrl Pts',(-0.0874004355336225,0.128673876256551,
1.23870028398651));
#16212=CARTESIAN_POINT('Ctrl Pts',(-0.0873870199099423,0.128682987688719,
1.23869913064722));
#16213=CARTESIAN_POINT('Ctrl Pts',(-0.0873801361795286,0.128687662075595,
1.23869853886523));
#16214=CARTESIAN_POINT('Ctrl Pts',(-0.0873659765319695,0.128697275503207,
1.23869732160901));
#16215=CARTESIAN_POINT('Ctrl Pts',(-0.0873587005713848,0.128702214479053,
1.23869669613236));
#16216=CARTESIAN_POINT('Ctrl Pts',(-0.0873437091146058,0.128712388933786,
1.23869540742055));
#16217=CARTESIAN_POINT('Ctrl Pts',(-0.0873359935669576,0.1287176243356,
1.23869474418252));
#16218=CARTESIAN_POINT('Ctrl Pts',(-0.0873200676345597,0.128728428820993,
1.23869337519903));
#16219=CARTESIAN_POINT('Ctrl Pts',(-0.0873118569454363,0.128733997977103,
1.23869266942927));
#16220=CARTESIAN_POINT('Ctrl Pts',(-0.0872948739885516,0.128745514825353,
1.23869120965114));
#16221=CARTESIAN_POINT('Ctrl Pts',(-0.0872861017185357,0.128751462357163,
1.23869045564486));
#16222=CARTESIAN_POINT('Ctrl Pts',(-0.0872699482499101,0.128762411875348,
1.23868906723332));
#16223=CARTESIAN_POINT('Ctrl Pts',(-0.0872625673151107,0.128767414065362,
1.2386884328454));
#16224=CARTESIAN_POINT('Ctrl Pts',(-0.0872447148154183,0.128779510780091,
1.23868689846265));
#16225=CARTESIAN_POINT('Ctrl Pts',(-0.087234242954536,0.128786604567902,
1.23868599845552));
#16226=CARTESIAN_POINT('Ctrl Pts',(-0.0868547250213077,0.129043627898895,
1.23865338161986));
#16227=CARTESIAN_POINT('Ctrl Pts',(-0.0864846108112903,0.129291968989012,
1.23862160529118));
#16228=CARTESIAN_POINT('Ctrl Pts',(-0.0856340603875407,0.129857389310533,
1.23854865160341));
#16229=CARTESIAN_POINT('Ctrl Pts',(-0.0851529236762294,0.130173397550784,
1.23850743470721));
#16230=CARTESIAN_POINT('Ctrl Pts',(-0.0837195808040299,0.131103463145408,
1.2383847902612));
#16231=CARTESIAN_POINT('Ctrl Pts',(-0.0827624256149272,0.131709783382766,
1.23830307772827));
#16232=CARTESIAN_POINT('Ctrl Pts',(-0.0759773452888538,0.135904701928224,
1.23772502082442));
#16233=CARTESIAN_POINT('Ctrl Pts',(-0.0699273504175132,0.139114086459763,
1.23721519076703));
#16234=CARTESIAN_POINT('Ctrl Pts',(-0.063688617770428,0.141913926259872,
1.23669476364274));
#16235=CARTESIAN_POINT('',(-0.155549948070468,0.000127103401447693,1.23559437743963));
#16236=CARTESIAN_POINT('Ctrl Pts',(-0.0636886258329928,0.141913922641526,
1.22279509470766));
#16237=CARTESIAN_POINT('Ctrl Pts',(-0.0730258425131839,0.137723533929853,
1.22353224257703));
#16238=CARTESIAN_POINT('Ctrl Pts',(-0.0819815705725974,0.132592492564984,
1.22426939044639));
#16239=CARTESIAN_POINT('Ctrl Pts',(-0.0903597265864884,0.126613278573833,
1.22500653831575));
#16240=CARTESIAN_POINT('Ctrl Pts',(-0.0987278568671842,0.120641219618241,
1.225742804076));
#16241=CARTESIAN_POINT('Ctrl Pts',(-0.106518983643229,0.113823461665015,
1.22647906983624));
#16242=CARTESIAN_POINT('Ctrl Pts',(-0.113563657596095,0.106297216207184,
1.22721533559648));
#16243=CARTESIAN_POINT('Ctrl Pts',(-0.120601882914084,0.0987778602107073,
1.22795092738528));
#16244=CARTESIAN_POINT('Ctrl Pts',(-0.126894366670152,0.0905519706795469,
1.22868651917408));
#16245=CARTESIAN_POINT('Ctrl Pts',(-0.132309082683801,0.0817930873568847,
1.22942211096287));
#16246=CARTESIAN_POINT('Ctrl Pts',(-0.137737399775053,0.0730122028338862,
1.23015955046464));
#16247=CARTESIAN_POINT('Ctrl Pts',(-0.14228306495749,0.0636964517140005,
1.23089698996641));
#16248=CARTESIAN_POINT('Ctrl Pts',(-0.145858742363638,0.0540465519353256,
1.23163442946818));
#16249=CARTESIAN_POINT('Ctrl Pts',(-0.149250783616596,0.0448922422988105,
1.23233399627117));
#16250=CARTESIAN_POINT('Ctrl Pts',(-0.151770122251847,0.03543807975696,
1.23303356307417));
#16251=CARTESIAN_POINT('Ctrl Pts',(-0.153384283523106,0.0258662727910986,
1.23373312987716));
#16252=CARTESIAN_POINT('Ctrl Pts',(-0.154815814063959,0.0173774468932388,
1.23435354573131));
#16253=CARTESIAN_POINT('Ctrl Pts',(-0.155542888541652,0.00876659949918076,
1.23497396158547));
#16254=CARTESIAN_POINT('Ctrl Pts',(-0.155549948070468,0.000127103401447693,
1.23559437743963));
#16255=CARTESIAN_POINT('Ctrl Pts',(-0.155651476811241,0.000126240882040021,
1.23559444529176));
#16256=CARTESIAN_POINT('Ctrl Pts',(-0.155271154691676,-0.0428543475497745,
1.23867891111416));
#16257=CARTESIAN_POINT('Ctrl Pts',(-0.114465767332605,-0.138094367465394,
1.24546828123047));
#16258=CARTESIAN_POINT('Ctrl Pts',(0.0468123474454561,-0.177797800804905,
1.25596255564071));
#16259=CARTESIAN_POINT('Ctrl Pts',(0.174771089844121,-0.0570834476806803,
1.26707726852248));
#16260=CARTESIAN_POINT('Ctrl Pts',(0.142735519209796,0.115887986436578,
1.27819198140426));
#16261=CARTESIAN_POINT('Ctrl Pts',(0.0172060236451339,0.167488946801519,
1.28676726993406));
#16262=CARTESIAN_POINT('Ctrl Pts',(-0.0488244285946477,0.148605630511624,
1.29163765416994));
#16263=CARTESIAN_POINT('Ctrl Pts',(-0.0636380227784998,0.141804318283704,
1.29280313411188));
#16264=CARTESIAN_POINT('Origin',(0.,0.,-0.129405622560373));
#16265=CARTESIAN_POINT('',(-0.0636886258329916,0.141913922641527,1.37660119646451));
#16266=CARTESIAN_POINT('',(-0.0636886474661844,0.141913912932905,1.36266955208845));
#16267=CARTESIAN_POINT('',(-0.0636886258329924,0.141913922641526,-0.129405622560373));
#16268=CARTESIAN_POINT('',(-0.155549935849213,-0.000141270329049539,1.31940562256037));
#16269=CARTESIAN_POINT('Ctrl Pts',(-0.155549935849213,-0.000141270329049539,
1.31940562256037));
#16270=CARTESIAN_POINT('Ctrl Pts',(-0.155539514661892,-0.0116158314067744,
1.32022803186282));
#16271=CARTESIAN_POINT('Ctrl Pts',(-0.154257754311619,-0.0230340958254805,
1.32105044116527));
#16272=CARTESIAN_POINT('Ctrl Pts',(-0.151751199017876,-0.0341668859663438,
1.32187285046771));
#16273=CARTESIAN_POINT('Ctrl Pts',(-0.149504011980853,-0.044147699775993,
1.32261016016449));
#16274=CARTESIAN_POINT('Ctrl Pts',(-0.146259507782471,-0.0539432732970475,
1.32334746986127));
#16275=CARTESIAN_POINT('Ctrl Pts',(-0.142068554767014,-0.0633429415674076,
1.32408477955805));
#16276=CARTESIAN_POINT('Ctrl Pts',(-0.137851517618334,-0.0728011125693691,
1.32482667820733));
#16277=CARTESIAN_POINT('Ctrl Pts',(-0.132676426851961,-0.0818575037646038,
1.32556857685662));
#16278=CARTESIAN_POINT('Ctrl Pts',(-0.126645813638856,-0.0903141206442943,
1.32631047550591));
#16279=CARTESIAN_POINT('Ctrl Pts',(-0.12066629006405,-0.0986990954732759,
1.32704608900104));
#16280=CARTESIAN_POINT('Ctrl Pts',(-0.113846248774929,-0.106493667539107,
1.32778170249618));
#16281=CARTESIAN_POINT('Ctrl Pts',(-0.106329241111352,-0.113533673351495,
1.32851731599132));
#16282=CARTESIAN_POINT('Ctrl Pts',(-0.0987158943671244,-0.120663904918345,
1.32926235721768));
#16283=CARTESIAN_POINT('Ctrl Pts',(-0.0903882631286982,-0.127019389420133,
1.33000739844404));
#16284=CARTESIAN_POINT('Ctrl Pts',(-0.0815313070020709,-0.132470557025077,
1.3307524396704));
#16285=CARTESIAN_POINT('Ctrl Pts',(-0.0726743508754436,-0.13792172463002,
1.33149748089676));
#16286=CARTESIAN_POINT('Ctrl Pts',(-0.0632889675620807,-0.14246817954184,
1.33224252212312));
#16287=CARTESIAN_POINT('Ctrl Pts',(-0.0535837684891806,-0.146029388324741,
1.33298756334948));
#16288=CARTESIAN_POINT('Ctrl Pts',(-0.0439792833514192,-0.149553641312332,
1.33372487304626));
#16289=CARTESIAN_POINT('Ctrl Pts',(-0.0339896175168683,-0.15213949602857,
1.33446218274304));
#16290=CARTESIAN_POINT('Ctrl Pts',(-0.0238193565707109,-0.1537154538508,
1.33519949243981));
#16291=CARTESIAN_POINT('Ctrl Pts',(-0.0135857967900037,-0.155301220299767,
1.3359413910891));
#16292=CARTESIAN_POINT('Ctrl Pts',(-0.00317028471788524,-0.155864153863497,
1.33668328973839));
#16293=CARTESIAN_POINT('Ctrl Pts',(0.00720522434977123,-0.155383033958246,
1.33742518838768));
#16294=CARTESIAN_POINT('Ctrl Pts',(0.017492835058364,-0.154905989963865,
1.33816080188282));
#16295=CARTESIAN_POINT('Ctrl Pts',(0.0277401800666532,-0.153402581451298,
1.33889641537795));
#16296=CARTESIAN_POINT('Ctrl Pts',(0.0377314847457342,-0.150904398739342,
1.33963202887309));
#16297=CARTESIAN_POINT('Ctrl Pts',(0.0478508394615628,-0.148374198948702,
1.34037707009945));
#16298=CARTESIAN_POINT('Ctrl Pts',(0.0577065890818968,-0.144823730709507,
1.34112211132582));
#16299=CARTESIAN_POINT('Ctrl Pts',(0.0670895699605935,-0.140338134883226,
1.34186715255218));
#16300=CARTESIAN_POINT('Ctrl Pts',(0.0764725508392916,-0.135852539056945,
1.34261219377854));
#16301=CARTESIAN_POINT('Ctrl Pts',(0.085381943627054,-0.130432355263206,
1.3433572350049));
#16302=CARTESIAN_POINT('Ctrl Pts',(0.0936369593371753,-0.12420918784892,
1.34410227623126));
#16303=CARTESIAN_POINT('Ctrl Pts',(0.101806310125775,-0.118050600220654,
1.34483958592804));
#16304=CARTESIAN_POINT('Ctrl Pts',(0.109396091215815,-0.111059513673848,
1.34557689562482));
#16305=CARTESIAN_POINT('Ctrl Pts',(0.116235287794278,-0.103369049388013,
1.3463142053216));
#16306=CARTESIAN_POINT('Ctrl Pts',(0.123117050947461,-0.0956307203100334,
1.34705610397088));
#16307=CARTESIAN_POINT('Ctrl Pts',(0.129238096716883,-0.0871848583285731,
1.34779800262017));
#16308=CARTESIAN_POINT('Ctrl Pts',(0.134460234808284,-0.0782064431827791,
1.34853990126946));
#16309=CARTESIAN_POINT('Ctrl Pts',(0.139638132432452,-0.0693040906140549,
1.3492755147646));
#16310=CARTESIAN_POINT('Ctrl Pts',(0.14393184220442,-0.059878997868156,
1.35001112825974));
#16311=CARTESIAN_POINT('Ctrl Pts',(0.147250897236983,-0.050129589694145,
1.35074674175487));
#16312=CARTESIAN_POINT('Ctrl Pts',(0.150612489769146,-0.0402552316647622,
1.35149178298124));
#16313=CARTESIAN_POINT('Ctrl Pts',(0.15297390508003,-0.030049089248297,
1.3522368242076));
#16314=CARTESIAN_POINT('Ctrl Pts',(0.154293254485432,-0.0197330717399448,
1.35298186543396));
#16315=CARTESIAN_POINT('Ctrl Pts',(0.155612603890834,-0.00941705423159124,
1.35372690666032));
#16316=CARTESIAN_POINT('Ctrl Pts',(0.155889896467494,0.00100785732826855,
1.35447194788668));
#16317=CARTESIAN_POINT('Ctrl Pts',(0.155137669070008,0.0113183980988834,
1.35521698911304));
#16318=CARTESIAN_POINT('Ctrl Pts',(0.154393247775287,0.0215219431111804,
1.35595429880981));
#16319=CARTESIAN_POINT('Ctrl Pts',(0.152635073861283,0.0316899759881723,
1.35669160850659));
#16320=CARTESIAN_POINT('Ctrl Pts',(0.149882258914002,0.041606621622478,
1.35742891820337));
#16321=CARTESIAN_POINT('Ctrl Pts',(0.14711231068186,0.0515849876113171,
1.35817081685266));
#16322=CARTESIAN_POINT('Ctrl Pts',(0.143335374636995,0.0613078750443079,
1.35891271550194));
#16323=CARTESIAN_POINT('Ctrl Pts',(0.1386235318856,0.0705642891805904,1.35965461415123));
#16324=CARTESIAN_POINT('Ctrl Pts',(0.133951606524602,0.0797422856114763,
1.36039022764637));
#16325=CARTESIAN_POINT('Ctrl Pts',(0.128361001530006,0.0884608550278958,
1.36112584114151));
#16326=CARTESIAN_POINT('Ctrl Pts',(0.121969375729713,0.0965363863219678,
1.36186145463665));
#16327=CARTESIAN_POINT('Ctrl Pts',(0.115495833908948,0.104715414818077,
1.36260649586301));
#16328=CARTESIAN_POINT('Ctrl Pts',(0.108201155658404,0.112234011397048,
1.36335153708937));
#16329=CARTESIAN_POINT('Ctrl Pts',(0.100249074280249,0.118936645345129,
1.36409657831573));
#16330=CARTESIAN_POINT('Ctrl Pts',(0.0922969929020949,0.125639279293211,
1.3648416195421));
#16331=CARTESIAN_POINT('Ctrl Pts',(0.0836883375898021,0.131525426243354,
1.36558666076846));
#16332=CARTESIAN_POINT('Ctrl Pts',(0.0746174941672043,0.136484548811238,
1.36633170199482));
#16333=CARTESIAN_POINT('Ctrl Pts',(0.065640543858759,0.141392339056463,
1.3670690312326));
#16334=CARTESIAN_POINT('Ctrl Pts',(0.0561436708638565,0.145429069350255,
1.36780636047038));
#16335=CARTESIAN_POINT('Ctrl Pts',(0.0463186330379303,0.148493726242887,
1.36854368970816));
#16336=CARTESIAN_POINT('Ctrl Pts',(0.0365092861973104,0.151553488753724,
1.36927984140113));
#16337=CARTESIAN_POINT('Ctrl Pts',(0.0263736652944203,0.153643898568171,
1.37001599309411));
#16338=CARTESIAN_POINT('Ctrl Pts',(0.0161230977477578,0.154712146320243,
1.37075214478708));
#16339=CARTESIAN_POINT('Ctrl Pts',(0.00588296731361892,0.155779306384054,
1.37148754693151));
#16340=CARTESIAN_POINT('Ctrl Pts',(-0.00447095844475691,0.155826254591357,
1.37222294907593));
#16341=CARTESIAN_POINT('Ctrl Pts',(-0.0147207954195999,0.154851866899351,
1.37295835122036));
#16342=CARTESIAN_POINT('Ctrl Pts',(-0.0249885283044939,0.153875777955458,
1.37369503735502));
#16343=CARTESIAN_POINT('Ctrl Pts',(-0.0351508846718456,0.151874897306929,
1.37443172348968));
#16344=CARTESIAN_POINT('Ctrl Pts',(-0.0449955051149119,0.14889998999145,
1.37516840962434));
#16345=CARTESIAN_POINT('Ctrl Pts',(-0.0513777991718371,0.146971349533518,
1.37564600523773));
#16346=CARTESIAN_POINT('Ctrl Pts',(-0.0576267276381069,0.144634402484416,
1.37612360085112));
#16347=CARTESIAN_POINT('Ctrl Pts',(-0.0636886258329916,0.141913922641527,
1.37660119646451));
#16348=CARTESIAN_POINT('Ctrl Pts',(-0.0636118382027626,0.141739365081131,
1.30659839996889));
#16349=CARTESIAN_POINT('Ctrl Pts',(-0.0813744076891851,0.133903115139863,
1.30798497917457));
#16350=CARTESIAN_POINT('Ctrl Pts',(-0.131574028003387,0.100038822065039,
1.31225404952175));
#16351=CARTESIAN_POINT('Ctrl Pts',(-0.155195691316953,0.0400812519945282,
1.31652311986892));
#16352=CARTESIAN_POINT('Ctrl Pts',(-0.15556701015029,-0.00014112466882523,
1.31940561101042));
#16353=CARTESIAN_POINT('',(-0.155315966858501,2.90168067545608E-5,1.30558500287933));
#16354=CARTESIAN_POINT('Ctrl Pts',(-0.0636380227784998,0.141804318283704,
1.29280313411188));
#16355=CARTESIAN_POINT('Ctrl Pts',(-0.0959148560870726,0.126985171874289,
1.29534255846386));
#16356=CARTESIAN_POINT('Ctrl Pts',(-0.142237182102223,0.0839092470420679,
1.29960629650446));
#16357=CARTESIAN_POINT('Ctrl Pts',(-0.155340312234673,0.0241955981471813,
1.30387003454505));
#16358=CARTESIAN_POINT('Ctrl Pts',(-0.155299723662096,2.96937538047808E-5,
1.30559434823368));
#16359=CARTESIAN_POINT('Ctrl Pts',(-0.15554999880721,1.92633547010141E-5,
1.30545035502838));
#16360=CARTESIAN_POINT('Ctrl Pts',(-0.15555005883387,-0.000465446963086064,
1.30548436162153));
#16361=CARTESIAN_POINT('Ctrl Pts',(-0.155547853246853,-0.000950150915595704,
1.30551843661611));
#16362=CARTESIAN_POINT('Ctrl Pts',(-0.155538567071807,-0.00195682091136872,
1.30558935389894));
#16363=CARTESIAN_POINT('Ctrl Pts',(-0.15553112438902,-0.00247877574768627,
1.30562620677271));
#16364=CARTESIAN_POINT('Ctrl Pts',(-0.155512361475722,-0.00345123213072981,
1.30569502622914));
#16365=CARTESIAN_POINT('Ctrl Pts',(-0.155501710515548,-0.00390174242615508,
1.30572697172978));
#16366=CARTESIAN_POINT('Ctrl Pts',(-0.155476661418278,-0.00479666117861854,
1.30579055932844));
#16367=CARTESIAN_POINT('Ctrl Pts',(-0.155462315094703,-0.00524106688709894,
1.30582219951222));
#16368=CARTESIAN_POINT('Ctrl Pts',(-0.155429905388864,-0.00612718932417162,
1.30588541762037));
#16369=CARTESIAN_POINT('Ctrl Pts',(-0.155411863922397,-0.00656890271905855,
1.30591699456666));
#16370=CARTESIAN_POINT('Ctrl Pts',(-0.155358282789037,-0.00775655577892897,
1.30600207252022));
#16371=CARTESIAN_POINT('Ctrl Pts',(-0.15531925424223,-0.00850231817017692,
1.30605568201404));
#16372=CARTESIAN_POINT('Ctrl Pts',(-0.15515504957497,-0.0112594031225942,
1.30625458678395));
#16373=CARTESIAN_POINT('Ctrl Pts',(-0.154996165888035,-0.0132684369198708,
1.30640092747855));
#16374=CARTESIAN_POINT('Ctrl Pts',(-0.153260185157275,-0.0308624912253183,
1.30769548410314));
#16375=CARTESIAN_POINT('Ctrl Pts',(-0.149376168893746,-0.0461270517189211,
1.30892174380606));
#16376=CARTESIAN_POINT('Ctrl Pts',(-0.141728961477359,-0.064223146296122,
1.31043358225343));
#16377=CARTESIAN_POINT('Ctrl Pts',(-0.140035518656591,-0.0678363444038684,
1.31073781150859));
#16378=CARTESIAN_POINT('Ctrl Pts',(-0.137259729596023,-0.0732107335590161,
1.31119021751654));
#16379=CARTESIAN_POINT('Ctrl Pts',(-0.136278228544455,-0.0750219329616712,
1.31134265236187));
#16380=CARTESIAN_POINT('Ctrl Pts',(-0.135013027115561,-0.0772498357529264,
1.31152964529558));
#16381=CARTESIAN_POINT('Ctrl Pts',(-0.134762959291308,-0.077685258811472,
1.31156616647412));
#16382=CARTESIAN_POINT('Ctrl Pts',(-0.134363939127277,-0.0783723156188709,
1.31162374493637));
#16383=CARTESIAN_POINT('Ctrl Pts',(-0.134216381170416,-0.0786247481562847,
1.31164488949119));
#16384=CARTESIAN_POINT('Ctrl Pts',(-0.133936798336288,-0.0790999596065081,
1.3116846728616));
#16385=CARTESIAN_POINT('Ctrl Pts',(-0.133804930607092,-0.0793228220937374,
1.31170332089917));
#16386=CARTESIAN_POINT('Ctrl Pts',(-0.13350235111456,-0.0798312937217863,
1.31174584735586));
#16387=CARTESIAN_POINT('Ctrl Pts',(-0.133331279168809,-0.080116684973965,
1.31176970206304));
#16388=CARTESIAN_POINT('Ctrl Pts',(-0.132875110235385,-0.0808721821959808,
1.31183281936455));
#16389=CARTESIAN_POINT('Ctrl Pts',(-0.132588430881952,-0.0813413350858101,
1.31187198163374));
#16390=CARTESIAN_POINT('Ctrl Pts',(-0.13058056559458,-0.0845884008884337,
1.3121428737138));
#16391=CARTESIAN_POINT('Ctrl Pts',(-0.12877454096456,-0.0873132481072574,
1.31236941160099));
#16392=CARTESIAN_POINT('Ctrl Pts',(-0.126441556042374,-0.0906030904096808,
1.31264462278728));
#16393=CARTESIAN_POINT('Ctrl Pts',(-0.125994676248581,-0.0912235094782895,
1.31269660069886));
#16394=CARTESIAN_POINT('Ctrl Pts',(-0.120080788991894,-0.0993076071044975,
1.31337524693761));
#16395=CARTESIAN_POINT('Ctrl Pts',(-0.113962685211251,-0.106272896949726,
1.31397633387423));
#16396=CARTESIAN_POINT('Ctrl Pts',(-0.101008947711542,-0.118606607006691,
1.31515751033723));
#16397=CARTESIAN_POINT('Ctrl Pts',(-0.0942726902580923,-0.124028075670657,
1.31573434681392));
#16398=CARTESIAN_POINT('Ctrl Pts',(-0.0861447681039709,-0.129523254266446,
1.31641646258377));
#16399=CARTESIAN_POINT('Ctrl Pts',(-0.0851599086974459,-0.130172901505695,
1.3164988776663));
#16400=CARTESIAN_POINT('Ctrl Pts',(-0.0835846070952162,-0.131186496412597,
1.31663038691622));
#16401=CARTESIAN_POINT('Ctrl Pts',(-0.0829989426063408,-0.131557815742141,
1.31667921113129));
#16402=CARTESIAN_POINT('Ctrl Pts',(-0.0818829618520441,-0.132254944809996,
1.31677212897925));
#16403=CARTESIAN_POINT('Ctrl Pts',(-0.081353133296262,-0.132581512854851,
1.31681619387815));
#16404=CARTESIAN_POINT('Ctrl Pts',(-0.0804277669819127,-0.133144241364318,
1.31689307703956));
#16405=CARTESIAN_POINT('Ctrl Pts',(-0.0800331105227539,-0.133381842549422,
1.31692584224083));
#16406=CARTESIAN_POINT('Ctrl Pts',(-0.079265107552474,-0.133839579608717,
1.31698955920957));
#16407=CARTESIAN_POINT('Ctrl Pts',(-0.0788918845356574,-0.134059915308606,
1.3170205033396));
#16408=CARTESIAN_POINT('Ctrl Pts',(-0.0779125034064613,-0.13463259593132,
1.31710165502572));
#16409=CARTESIAN_POINT('Ctrl Pts',(-0.0773048812742063,-0.1349824039481,
1.31715195351385));
#16410=CARTESIAN_POINT('Ctrl Pts',(-0.0751970672615263,-0.136176972196828,
1.31732628336913));
#16411=CARTESIAN_POINT('Ctrl Pts',(-0.0736852784998245,-0.137000897701598,
1.31745105324089));
#16412=CARTESIAN_POINT('Ctrl Pts',(-0.0613577688476295,-0.143456328404703,
1.31846674779829));
#16413=CARTESIAN_POINT('Ctrl Pts',(-0.0499299084519012,-0.147822103442598,
1.31940286221832));
#16414=CARTESIAN_POINT('Ctrl Pts',(-0.0290676287696828,-0.153094455870004,
1.32107164474723));
#16415=CARTESIAN_POINT('Ctrl Pts',(-0.0198341904778545,-0.154562244827643,
1.32179569083012));
#16416=CARTESIAN_POINT('Ctrl Pts',(-0.00966275032589286,-0.155251984663078,
1.32254537530335));
#16417=CARTESIAN_POINT('Ctrl Pts',(-0.00880110463397546,-0.155303213535837,
1.32260850064286));
#16418=CARTESIAN_POINT('Ctrl Pts',(-0.00757604145128999,-0.155365820617116,
1.32269766656506));
#16419=CARTESIAN_POINT('Ctrl Pts',(-0.00721296296253917,-0.155383100087144,
1.32272402031452));
#16420=CARTESIAN_POINT('Ctrl Pts',(-0.00658736044452346,-0.155410675960243,
1.32276929993152));
#16421=CARTESIAN_POINT('Ctrl Pts',(-0.00632486624407131,-0.155421580198741,
1.32278825941527));
#16422=CARTESIAN_POINT('Ctrl Pts',(-0.00581615089105437,-0.155441421733273,
1.32282492567624));
#16423=CARTESIAN_POINT('Ctrl Pts',(-0.00556993621752219,-0.155450439093941,
1.32284263699608));
#16424=CARTESIAN_POINT('Ctrl Pts',(-0.00490639121594114,-0.15547316223416,
1.32289027725792));
#16425=CARTESIAN_POINT('Ctrl Pts',(-0.004489021260279,-0.155485772818166,
1.32292014548915));
#16426=CARTESIAN_POINT('Ctrl Pts',(-0.00294478699710083,-0.155526207777226,
1.3230303117388));
#16427=CARTESIAN_POINT('Ctrl Pts',(-0.00181764390367268,-0.155543464803141,
1.32311004557123));
#16428=CARTESIAN_POINT('Ctrl Pts',(0.0100791143516344,-0.155596266098236,
1.32394542711257));
#16429=CARTESIAN_POINT('Ctrl Pts',(0.020826330625677,-0.154525495108031,
1.32464781194362));
#16430=CARTESIAN_POINT('Ctrl Pts',(0.0413458636283426,-0.15029934596446,
1.32602701958209));
#16431=CARTESIAN_POINT('Ctrl Pts',(0.0510867040265423,-0.14727349485332,
1.32670030768066));
#16432=CARTESIAN_POINT('Ctrl Pts',(0.0616369916589631,-0.142822656146584,
1.32749508757108));
#16433=CARTESIAN_POINT('Ctrl Pts',(0.0628061813464088,-0.142312379183446,
1.32758408225122));
#16434=CARTESIAN_POINT('Ctrl Pts',(0.0646363280112985,-0.141486690818027,
1.32772491077386));
#16435=CARTESIAN_POINT('Ctrl Pts',(0.0653015779032153,-0.141180885633662,
1.32777642193344));
#16436=CARTESIAN_POINT('Ctrl Pts',(0.0664247643782563,-0.140654937067164,
1.32786394975641));
#16437=CARTESIAN_POINT('Ctrl Pts',(0.0668838312467152,-0.140437223522803,
1.32789988313271));
#16438=CARTESIAN_POINT('Ctrl Pts',(0.0677835033993699,-0.140005140085795,
1.32797062282043));
#16439=CARTESIAN_POINT('Ctrl Pts',(0.0682241789873927,-0.139790929516246,
1.32800542331237));
#16440=CARTESIAN_POINT('Ctrl Pts',(0.0690699570036463,-0.139374848505379,
1.32807250982114));
#16441=CARTESIAN_POINT('Ctrl Pts',(0.0694752054871472,-0.139173284688337,
1.32810478489198));
#16442=CARTESIAN_POINT('Ctrl Pts',(0.0704149447012462,-0.138700746821056,
1.32817993675351));
#16443=CARTESIAN_POINT('Ctrl Pts',(0.0709487576107526,-0.138428448596697,
1.32822285953901));
#16444=CARTESIAN_POINT('Ctrl Pts',(0.0723618802064355,-0.137697293080737,
1.32833711480769));
#16445=CARTESIAN_POINT('Ctrl Pts',(0.0732383845764503,-0.137233105221232,
1.3284086339555));
#16446=CARTESIAN_POINT('Ctrl Pts',(0.0798282499757151,-0.133662066086512,
1.3289513703526));
#16447=CARTESIAN_POINT('Ctrl Pts',(0.0853453253919051,-0.130208488382998,
1.32943493838304));
#16448=CARTESIAN_POINT('Ctrl Pts',(0.099136254374105,-0.120321907435234,
1.33072326380972));
#16449=CARTESIAN_POINT('Ctrl Pts',(0.107005381870996,-0.113380657644936,
1.33154241044867));
#16450=CARTESIAN_POINT('Ctrl Pts',(0.116844662783263,-0.102758158034655,
1.33265684251503));
#16451=CARTESIAN_POINT('Ctrl Pts',(0.119457532452934,-0.0997086623250283,
1.33296306665312));
#16452=CARTESIAN_POINT('Ctrl Pts',(0.123233696633104,-0.0949396484958213,
1.33341807005433));
#16453=CARTESIAN_POINT('Ctrl Pts',(0.124485327771254,-0.0932924710202543,
1.33357116085352));
#16454=CARTESIAN_POINT('Ctrl Pts',(0.125999964122596,-0.0912143867383204,
1.33375884333785));
#16455=CARTESIAN_POINT('Ctrl Pts',(0.126294152199212,-0.0908066211577997,
1.3337954151008));
#16456=CARTESIAN_POINT('Ctrl Pts',(0.126756375052597,-0.090159355954568,
1.33385305504411));
#16457=CARTESIAN_POINT('Ctrl Pts',(0.126925716731405,-0.0899208013682111,
1.33387421080554));
#16458=CARTESIAN_POINT('Ctrl Pts',(0.127243668331612,-0.0894702096314062,
1.33391400317947));
#16459=CARTESIAN_POINT('Ctrl Pts',(0.127392419967987,-0.0892582818456491,
1.33393264907115));
#16460=CARTESIAN_POINT('Ctrl Pts',(0.127730974153045,-0.0887733703446588,
1.33397515519039));
#16461=CARTESIAN_POINT('Ctrl Pts',(0.127920431011737,-0.0885001490156586,
1.33399899178819));
#16462=CARTESIAN_POINT('Ctrl Pts',(0.128420358944783,-0.0877742287373203,
1.3340620295583));
#16463=CARTESIAN_POINT('Ctrl Pts',(0.128729316011371,-0.0873204846822686,
1.33410113080797));
#16464=CARTESIAN_POINT('Ctrl Pts',(0.130850942601287,-0.084168863182679,
1.33437071590776));
#16465=CARTESIAN_POINT('Ctrl Pts',(0.132581232917176,-0.0814161368992058,
1.33459606433394));
#16466=CARTESIAN_POINT('Ctrl Pts',(0.13696432431337,-0.0739322353633311,
1.33518800319543));
#16467=CARTESIAN_POINT('Ctrl Pts',(0.139458223087769,-0.0691130577450456,
1.33554804777151));
#16468=CARTESIAN_POINT('Ctrl Pts',(0.145033402583886,-0.0568029557448982,
1.33643986197597));
#16469=CARTESIAN_POINT('Ctrl Pts',(0.147791086080892,-0.0491838700494526,
1.33696806779057));
#16470=CARTESIAN_POINT('Ctrl Pts',(0.15103958279508,-0.0374141153602024,
1.33778644477238));
#16471=CARTESIAN_POINT('Ctrl Pts',(0.151977313754222,-0.0334015473762989,
1.33806571094217));
#16472=CARTESIAN_POINT('Ctrl Pts',(0.153234762328562,-0.0268585472664584,
1.33852512939468));
#16473=CARTESIAN_POINT('Ctrl Pts',(0.153653488114263,-0.0243490912198524,
1.33870226212154));
#16474=CARTESIAN_POINT('Ctrl Pts',(0.15412119574545,-0.0210495108636617,
1.33893687882431));
#16475=CARTESIAN_POINT('Ctrl Pts',(0.154225969808342,-0.0202675869584319,
1.33899260196162));
#16476=CARTESIAN_POINT('Ctrl Pts',(0.154387470077688,-0.0189884693381101,
1.33908397517323));
#16477=CARTESIAN_POINT('Ctrl Pts',(0.154447754039681,-0.0184917318341367,
1.33911951299218));
#16478=CARTESIAN_POINT('Ctrl Pts',(0.154559568710073,-0.017531672455502,
1.33918830549427));
#16479=CARTESIAN_POINT('Ctrl Pts',(0.154611415488617,-0.0170683921573794,
1.33922154985337));
#16480=CARTESIAN_POINT('Ctrl Pts',(0.154725999460209,-0.0160011347620351,
1.33929824946366));
#16481=CARTESIAN_POINT('Ctrl Pts',(0.154787283717015,-0.015397012787732,
1.33934174982579));
#16482=CARTESIAN_POINT('Ctrl Pts',(0.154941938873326,-0.0137781185837842,
1.3394585542182));
#16483=CARTESIAN_POINT('Ctrl Pts',(0.155028876030377,-0.0127627770634818,
1.33953205839517));
#16484=CARTESIAN_POINT('Ctrl Pts',(0.155672488145298,-0.00426437425598765,
1.34014945013254));
#16485=CARTESIAN_POINT('Ctrl Pts',(0.155696904999734,0.00324784418413023,
1.34070994580911));
#16486=CARTESIAN_POINT('Ctrl Pts',(0.154988708613029,0.0134885344485974,
1.34149374337532));
#16487=CARTESIAN_POINT('Ctrl Pts',(0.154724604865072,0.0162399507037654,
1.3417062056487));
#16488=CARTESIAN_POINT('Ctrl Pts',(0.15377534342252,0.0239603143191982,
1.34230675811499));
#16489=CARTESIAN_POINT('Ctrl Pts',(0.152922971557529,0.0289053037301482,
1.34269666516858));
#16490=CARTESIAN_POINT('Ctrl Pts',(0.15027405816035,0.0408043732246399,
1.34363994944597));
#16491=CARTESIAN_POINT('Ctrl Pts',(0.148231874503444,0.0476930636696109,
1.34419049859115));
#16492=CARTESIAN_POINT('Ctrl Pts',(0.145426531424755,0.0552053881976066,
1.34477995745877));
#16493=CARTESIAN_POINT('Ctrl Pts',(0.145125677442254,0.0559915061449438,
1.34484149760727));
#16494=CARTESIAN_POINT('Ctrl Pts',(0.14468712359748,0.0571101411239511,
1.3449288252831));
#16495=CARTESIAN_POINT('Ctrl Pts',(0.144554635294281,0.0574446636000431,
1.34495490898803));
#16496=CARTESIAN_POINT('Ctrl Pts',(0.144323634515648,0.0580220622612454,
1.34499987275872));
#16497=CARTESIAN_POINT('Ctrl Pts',(0.1442256672785,0.0582651533197557,1.34501878519815));
#16498=CARTESIAN_POINT('Ctrl Pts',(0.144034023106087,0.0587372445826408,
1.34505547791575));
#16499=CARTESIAN_POINT('Ctrl Pts',(0.143940414324524,0.0589662686602731,
1.34507326227463));
#16500=CARTESIAN_POINT('Ctrl Pts',(0.143685351890981,0.0595860800127816,
1.34512135085048));
#16501=CARTESIAN_POINT('Ctrl Pts',(0.143522849014139,0.0599764378858923,
1.34515159229808));
#16502=CARTESIAN_POINT('Ctrl Pts',(0.14290793553236,0.0614367472350435,
1.34526457374595));
#16503=CARTESIAN_POINT('Ctrl Pts',(0.142445120306893,0.0625023188678151,
1.345346711831));
#16504=CARTESIAN_POINT('Ctrl Pts',(0.138410328545972,0.0715142306325301,
1.3460396312365));
#16505=CARTESIAN_POINT('Ctrl Pts',(0.134187936901027,0.0791539555950223,
1.34661587583481));
#16506=CARTESIAN_POINT('Ctrl Pts',(0.124186779995331,0.094126300335312,
1.34780200127658));
#16507=CARTESIAN_POINT('Ctrl Pts',(0.118344985324206,0.101373392360171,
1.34840976117854));
#16508=CARTESIAN_POINT('Ctrl Pts',(0.108888713581815,0.111165366422583,
1.34933412339123));
#16509=CARTESIAN_POINT('Ctrl Pts',(0.105757617295196,0.114148198103218,
1.34963200466565));
#16510=CARTESIAN_POINT('Ctrl Pts',(0.101800194209621,0.117615496673495,
1.35000153061319));
#16511=CARTESIAN_POINT('Ctrl Pts',(0.101088199322572,0.118228002129573,
1.35006774952524));
#16512=CARTESIAN_POINT('Ctrl Pts',(0.0999630790796138,0.119178311917358,
1.35017200536985));
#16513=CARTESIAN_POINT('Ctrl Pts',(0.0995536788903767,0.119520509608348,
1.3502098623695));
#16514=CARTESIAN_POINT('Ctrl Pts',(0.0988238165589627,0.120124214282875,
1.35027721760755));
#16515=CARTESIAN_POINT('Ctrl Pts',(0.0985040550157329,0.120386563684455,
1.35030668134367));
#16516=CARTESIAN_POINT('Ctrl Pts',(0.097763763223876,0.12098901443662,1.35037479205684));
#16517=CARTESIAN_POINT('Ctrl Pts',(0.0973425000535687,0.121328202342699,
1.35041347523676));
#16518=CARTESIAN_POINT('Ctrl Pts',(0.0961793157355435,0.122254804502689,
1.35052008681497));
#16519=CARTESIAN_POINT('Ctrl Pts',(0.0954338005050662,0.122837647514763,
1.35058819563956));
#16520=CARTESIAN_POINT('Ctrl Pts',(0.0915646607598882,0.125806054160361,
1.35094059411344));
#16521=CARTESIAN_POINT('Ctrl Pts',(0.0883570238875594,0.128079200246822,
1.35122921152411));
#16522=CARTESIAN_POINT('Ctrl Pts',(0.0834054779091896,0.131313622394636,
1.35167006418441));
#16523=CARTESIAN_POINT('Ctrl Pts',(0.0817233868053524,0.132367022431365,
1.35181904253327));
#16524=CARTESIAN_POINT('Ctrl Pts',(0.0674609817423309,0.140923280334954,
1.3530755329944));
#16525=CARTESIAN_POINT('Ctrl Pts',(0.0539009984077992,0.1466456932042,1.35423674111801));
#16526=CARTESIAN_POINT('Ctrl Pts',(0.0371554732459155,0.15107094770266,
1.35554078946067));
#16527=CARTESIAN_POINT('Ctrl Pts',(0.0345514152839025,0.151687713662543,
1.35573977052441));
#16528=CARTESIAN_POINT('Ctrl Pts',(0.031399987164342,0.152348742674966,
1.35597502356239));
#16529=CARTESIAN_POINT('Ctrl Pts',(0.030866843031779,0.152457655149237,
1.35601463260471));
#16530=CARTESIAN_POINT('Ctrl Pts',(0.0300372862465848,0.152622589798859,
1.35607595678393));
#16531=CARTESIAN_POINT('Ctrl Pts',(0.0297412708606671,0.152680549821474,
1.35609777893962));
#16532=CARTESIAN_POINT('Ctrl Pts',(0.0291921220957172,0.152786415875712,
1.35613814757794));
#16533=CARTESIAN_POINT('Ctrl Pts',(0.0289390406972177,0.152834553665209,
1.35615670666161));
#16534=CARTESIAN_POINT('Ctrl Pts',(0.0283670050348196,0.152941886860572,
1.35619855417727));
#16535=CARTESIAN_POINT('Ctrl Pts',(0.0280479851518578,0.153000713283449,
1.35622182146033));
#16536=CARTESIAN_POINT('Ctrl Pts',(0.0271071200016452,0.153171164681162,
1.35629024007954));
#16537=CARTESIAN_POINT('Ctrl Pts',(0.0264847657914144,0.1532800015073,1.35633523703655));
#16538=CARTESIAN_POINT('Ctrl Pts',(0.0220274985685555,0.154031526773631,
1.35665575873807));
#16539=CARTESIAN_POINT('Ctrl Pts',(0.0181699346864958,0.154534079975703,
1.35692394025054));
#16540=CARTESIAN_POINT('Ctrl Pts',(0.0130954031246185,0.155002482321503,
1.35726951667139));
#16541=CARTESIAN_POINT('Ctrl Pts',(0.0118923341248151,0.155099424973858,
1.35735091721061));
#16542=CARTESIAN_POINT('Ctrl Pts',(-0.00414495506203996,0.156203998204142,
1.35843039170935));
#16543=CARTESIAN_POINT('Ctrl Pts',(-0.0190475710698942,0.155093808718543,
1.35937759843878));
#16544=CARTESIAN_POINT('Ctrl Pts',(-0.036777252879314,0.151175554073212,
1.3606211109334));
#16545=CARTESIAN_POINT('Ctrl Pts',(-0.0399644119627392,0.150364415807139,
1.36084903042339));
#16546=CARTESIAN_POINT('Ctrl Pts',(-0.0439519122134506,0.149213858928201,
1.3611408528136));
#16547=CARTESIAN_POINT('Ctrl Pts',(-0.0447785186189123,0.148967884123198,
1.36120171250906));
#16548=CARTESIAN_POINT('Ctrl Pts',(-0.0460969811192774,0.148563581575791,
1.36129939007872));
#16549=CARTESIAN_POINT('Ctrl Pts',(-0.0465901768561539,0.148409652138006,
1.36133606420958));
#16550=CARTESIAN_POINT('Ctrl Pts',(-0.0475227458362642,0.148113484883069,
1.36140567257607));
#16551=CARTESIAN_POINT('Ctrl Pts',(-0.0479622713609593,0.147971741536933,
1.3614385902877));
#16552=CARTESIAN_POINT('Ctrl Pts',(-0.0489569483565189,0.147646069128338,
1.36151334042957));
#16553=CARTESIAN_POINT('Ctrl Pts',(-0.0495117040588307,0.147460963191428,
1.36155521117024));
#16554=CARTESIAN_POINT('Ctrl Pts',(-0.0511495097849859,0.14690419080879,
1.361679370144));
#16555=CARTESIAN_POINT('Ctrl Pts',(-0.0522294935433872,0.146523696043513,
1.36176194832233));
#16556=CARTESIAN_POINT('Ctrl Pts',(-0.0568178536563893,0.144849973880894,
1.36211588511072));
#16557=CARTESIAN_POINT('Ctrl Pts',(-0.0602812047219647,0.143443117612085,
1.36239086377559));
#16558=CARTESIAN_POINT('Ctrl Pts',(-0.0636886474661844,0.141913912932905,
1.36266955208845));
#16559=CARTESIAN_POINT('Origin',(0.,0.,-0.129405622560373));
#16560=CARTESIAN_POINT('',(-0.0636885593981422,0.141913952456372,1.4466066640002));
#16561=CARTESIAN_POINT('',(-0.0636886279094242,0.141913921709658,1.43290478746296));
#16562=CARTESIAN_POINT('',(-0.0636886258329924,0.141913922641526,-0.129405622560373));
#16563=CARTESIAN_POINT('',(-0.15554998452487,6.93852476632616E-5,1.38940562256037));
#16564=CARTESIAN_POINT('Ctrl Pts',(-0.0636885593981421,0.141913952456372,
1.4466066640002));
#16565=CARTESIAN_POINT('Ctrl Pts',(-0.0577818439632503,0.144564785516205,
1.44610477136062));
#16566=CARTESIAN_POINT('Ctrl Pts',(-0.0517103760784334,0.14684652708226,
1.44560109607175));
#16567=CARTESIAN_POINT('Ctrl Pts',(-0.0451514202499666,0.148853254011476,
1.44507888033969));
#16568=CARTESIAN_POINT('Ctrl Pts',(-0.0447938953865853,0.148961232946105,
1.44505048298667));
#16569=CARTESIAN_POINT('Ctrl Pts',(-0.0410245876328218,0.150084834109221,
1.44475183615552));
#16570=CARTESIAN_POINT('Ctrl Pts',(-0.0375789354819654,0.150984445917234,
1.44448519240408));
#16571=CARTESIAN_POINT('Ctrl Pts',(-0.0335551471759432,0.151888684052997,
1.44418332779639));
#16572=CARTESIAN_POINT('Ctrl Pts',(-0.0330044949665369,0.152009287819579,
1.44414222263205));
#16573=CARTESIAN_POINT('Ctrl Pts',(-0.0321237319672833,0.152197180740983,
1.44407681499684));
#16574=CARTESIAN_POINT('Ctrl Pts',(-0.0317940441530217,0.152266394004828,
1.44405240740881));
#16575=CARTESIAN_POINT('Ctrl Pts',(-0.0312099338906359,0.152387039799096,
1.44400930159064));
#16576=CARTESIAN_POINT('Ctrl Pts',(-0.0309556046506675,0.152438907163245,
1.44399057886119));
#16577=CARTESIAN_POINT('Ctrl Pts',(-0.0304166696462392,0.152547412012865,
1.44395100309523));
#16578=CARTESIAN_POINT('Ctrl Pts',(-0.0301320353664039,0.152603889703489,
1.44393015923382));
#16579=CARTESIAN_POINT('Ctrl Pts',(-0.0293644953355584,0.152753955320119,
1.44387410349152));
#16580=CARTESIAN_POINT('Ctrl Pts',(-0.0288812953941729,0.152846050803369,
1.44383897534555));
#16581=CARTESIAN_POINT('Ctrl Pts',(-0.0264964975459197,0.153288868309562,
1.44366636114341));
#16582=CARTESIAN_POINT('Ctrl Pts',(-0.0245888012720797,0.153606423401509,
1.44353065367778));
#16583=CARTESIAN_POINT('Ctrl Pts',(-0.019083902879906,0.154417574327649,
1.44314455357656));
#16584=CARTESIAN_POINT('Ctrl Pts',(-0.0154745213177866,0.154820948220268,
1.44289810843775));
#16585=CARTESIAN_POINT('Ctrl Pts',(-0.00480911613752549,0.155636101335685,
1.4421809223941));
#16586=CARTESIAN_POINT('Ctrl Pts',(0.0022646345665849,0.155693943986604,
1.44171910471083));
#16587=CARTESIAN_POINT('Ctrl Pts',(0.0196580776261543,0.154650131224994,
1.44057063673603));
#16588=CARTESIAN_POINT('Ctrl Pts',(0.0299085088302777,0.152998478405293,
1.43988094496833));
#16589=CARTESIAN_POINT('Ctrl Pts',(0.0410192172414078,0.150048408023844,
1.43907602317761));
#16590=CARTESIAN_POINT('Ctrl Pts',(0.0421172723481944,0.149743901983534,
1.43899586272236));
#16591=CARTESIAN_POINT('Ctrl Pts',(0.043772630674002,0.149265200459738,
1.43887404651391));
#16592=CARTESIAN_POINT('Ctrl Pts',(0.0443324795148297,0.149099880977938,
1.43883267873659));
#16593=CARTESIAN_POINT('Ctrl Pts',(0.0453335617574274,0.148798131607573,
1.4387583983069));
#16594=CARTESIAN_POINT('Ctrl Pts',(0.0457751456257382,0.148662879785215,
1.43872552439566));
#16595=CARTESIAN_POINT('Ctrl Pts',(0.0467103315226779,0.148371881860805,
1.43865567067506));
#16596=CARTESIAN_POINT('Ctrl Pts',(0.0472037705228454,0.148215634918689,
1.43861867482091));
#16597=CARTESIAN_POINT('Ctrl Pts',(0.048520829108425,0.147791345606467,
1.43851955160848));
#16598=CARTESIAN_POINT('Ctrl Pts',(0.0493429946909558,0.14751888527274,
1.43845727994517));
#16599=CARTESIAN_POINT('Ctrl Pts',(0.0533140432296101,0.146165994816054,
1.43815455242023));
#16600=CARTESIAN_POINT('Ctrl Pts',(0.0564297389229465,0.14499160889433,
1.43791102043126));
#16601=CARTESIAN_POINT('Ctrl Pts',(0.0733461776969764,0.13798752141679,
1.43655400187372));
#16602=CARTESIAN_POINT('Ctrl Pts',(0.0862853316404953,0.130287721145884,
1.4353755561742));
#16603=CARTESIAN_POINT('Ctrl Pts',(0.0986594096163809,0.120262327467369,
1.43415525818263));
#16604=CARTESIAN_POINT('Ctrl Pts',(0.0993926787389034,0.119657018132877,
1.43408259507869));
#16605=CARTESIAN_POINT('Ctrl Pts',(0.100708129737373,0.118550685084848,
1.43395166214375));
#16606=CARTESIAN_POINT('Ctrl Pts',(0.101292236237424,0.118052002294806,
1.43389331290064));
#16607=CARTESIAN_POINT('Ctrl Pts',(0.104341615944375,0.115409288792641,
1.43358767713623));
#16608=CARTESIAN_POINT('Ctrl Pts',(0.106742811670848,0.113192106366835,
1.43334346488798));
#16609=CARTESIAN_POINT('Ctrl Pts',(0.109464630392999,0.110515155313681,
1.43306412769316));
#16610=CARTESIAN_POINT('Ctrl Pts',(0.109854628265314,0.110127496721022,
1.433024040159));
#16611=CARTESIAN_POINT('Ctrl Pts',(0.110477361758976,0.109501898620392,
1.4329599411417));
#16612=CARTESIAN_POINT('Ctrl Pts',(0.11071139891844,0.109265270867928,1.43293583093112));
#16613=CARTESIAN_POINT('Ctrl Pts',(0.111126239104583,0.108843137499665,
1.43289306127123));
#16614=CARTESIAN_POINT('Ctrl Pts',(0.111307339987436,0.108657929610833,
1.43287437865513));
#16615=CARTESIAN_POINT('Ctrl Pts',(0.111691962123727,0.108262614317263,
1.43283467723013));
#16616=CARTESIAN_POINT('Ctrl Pts',(0.111895353211077,0.108052385422434,
1.43281366848699));
#16617=CARTESIAN_POINT('Ctrl Pts',(0.11244644483601,0.107479541886851,1.43275670160171));
#16618=CARTESIAN_POINT('Ctrl Pts',(0.112792987822206,0.10711581021167,1.43272083193522));
#16619=CARTESIAN_POINT('Ctrl Pts',(0.114552659033195,0.105250849741183,
1.43253841066223));
#16620=CARTESIAN_POINT('Ctrl Pts',(0.115937689565636,0.103723219748211,
1.43239388945438));
#16621=CARTESIAN_POINT('Ctrl Pts',(0.119915291224847,0.0991568280322926,
1.43197441299661));
#16622=CARTESIAN_POINT('Ctrl Pts',(0.122421820668732,0.0960450767290035,
1.43170426801206));
#16623=CARTESIAN_POINT('Ctrl Pts',(0.131061486307808,0.0844306712315355,
1.43073700761423));
#16624=CARTESIAN_POINT('Ctrl Pts',(0.136451120246247,0.075410575303356,
1.43005973580173));
#16625=CARTESIAN_POINT('Ctrl Pts',(0.14365154759957,0.060020134466745,1.428923478612));
#16626=CARTESIAN_POINT('Ctrl Pts',(0.146037060753417,0.0539568617032269,
1.42848061335713));
#16627=CARTESIAN_POINT('Ctrl Pts',(0.148341149207721,0.0468155543687475,
1.42795485694693));
#16628=CARTESIAN_POINT('Ctrl Pts',(0.148637593005238,0.0458656575583375,
1.42788485045811));
#16629=CARTESIAN_POINT('Ctrl Pts',(0.149098227640117,0.0443382609546246,
1.42777213428897));
#16630=CARTESIAN_POINT('Ctrl Pts',(0.149268227875022,0.043762529619126,
1.42772961390418));
#16631=CARTESIAN_POINT('Ctrl Pts',(0.149564050288794,0.0427389025738611,
1.42765394815234));
#16632=CARTESIAN_POINT('Ctrl Pts',(0.149691204487337,0.0422913965544929,
1.42762084647468));
#16633=CARTESIAN_POINT('Ctrl Pts',(0.149951842233852,0.0413582061475625,
1.42755176919773));
#16634=CARTESIAN_POINT('Ctrl Pts',(0.150084977829886,0.0408724310980645,
1.42751578276327));
#16635=CARTESIAN_POINT('Ctrl Pts',(0.150424346916312,0.0396101483110438,
1.42742219469715));
#16636=CARTESIAN_POINT('Ctrl Pts',(0.15062692555304,0.0388326827286617,
1.42736447587529));
#16637=CARTESIAN_POINT('Ctrl Pts',(0.151477811000626,0.0354602509278637,
1.42711375007225));
#16638=CARTESIAN_POINT('Ctrl Pts',(0.152065112086073,0.0328505198945307,
1.42691880337861));
#16639=CARTESIAN_POINT('Ctrl Pts',(0.153442988303091,0.0258950709319782,
1.42639639379569));
#16640=CARTESIAN_POINT('Ctrl Pts',(0.154116209862769,0.0215288768052759,
1.42606549686928));
#16641=CARTESIAN_POINT('Ctrl Pts',(0.155968623241073,0.00482042250075044,
1.42478876453381));
#16642=CARTESIAN_POINT('Ctrl Pts',(0.155856938857634,-0.0076171419174825,
1.42381248347944));
#16643=CARTESIAN_POINT('Ctrl Pts',(0.153774950567523,-0.0237501082456536,
1.42257434509827));
#16644=CARTESIAN_POINT('Ctrl Pts',(0.153135890237625,-0.0275718797082024,
1.42228359891032));
#16645=CARTESIAN_POINT('Ctrl Pts',(0.152227431146282,-0.0319845317289718,
1.42195374719682));
#16646=CARTESIAN_POINT('Ctrl Pts',(0.152096361422313,-0.032602115607345,
1.42190771714814));
#16647=CARTESIAN_POINT('Ctrl Pts',(0.151892263690029,-0.033535771013551,
1.42183835162374));
#16648=CARTESIAN_POINT('Ctrl Pts',(0.15182200330985,-0.0338524300835437,
1.42181486435631));
#16649=CARTESIAN_POINT('Ctrl Pts',(0.151694145876041,-0.0344202703774804,
1.42177281888703));
#16650=CARTESIAN_POINT('Ctrl Pts',(0.151636914980676,-0.0346715290188518,
1.42175424023509));
#16651=CARTESIAN_POINT('Ctrl Pts',(0.15151129111076,-0.0352167896924782,
1.42171397842817));
#16652=CARTESIAN_POINT('Ctrl Pts',(0.151442666891154,-0.0355107344251004,
1.42169230874421));
#16653=CARTESIAN_POINT('Ctrl Pts',(0.151247774270836,-0.0363346960137935,
1.42163165965066));
#16654=CARTESIAN_POINT('Ctrl Pts',(0.151119574449685,-0.036864259088572,
1.42159278902156));
#16655=CARTESIAN_POINT('Ctrl Pts',(0.150343044405966,-0.039999784816153,
1.42136322255749));
#16656=CARTESIAN_POINT('Ctrl Pts',(0.149630051075436,-0.0425894816651851,
1.42117601860419));
#16657=CARTESIAN_POINT('Ctrl Pts',(0.144599141794687,-0.059171824955237,
1.41998507268791));
#16658=CARTESIAN_POINT('Ctrl Pts',(0.138390443961365,-0.0725148705404471,
1.41905647960248));
#16659=CARTESIAN_POINT('Ctrl Pts',(0.129303777530507,-0.0864894582732642,
1.41793636271821));
#16660=CARTESIAN_POINT('Ctrl Pts',(0.128168299171389,-0.088163370337069,
1.41779964322606));
#16661=CARTESIAN_POINT('Ctrl Pts',(0.124755382241895,-0.0929893363178283,
1.41739711657431));
#16662=CARTESIAN_POINT('Ctrl Pts',(0.122392155314658,-0.0960784993154756,
1.41712869992373));
#16663=CARTESIAN_POINT('Ctrl Pts',(0.119315148389064,-0.0998027420388395,
1.41678949072232));
#16664=CARTESIAN_POINT('Ctrl Pts',(0.118707859136016,-0.100524305832315,
1.41672301058473));
#16665=CARTESIAN_POINT('Ctrl Pts',(0.117742454555519,-0.101650424155894,
1.4166180292465));
#16666=CARTESIAN_POINT('Ctrl Pts',(0.117388721380442,-0.102058720426598,
1.41657970801144));
#16667=CARTESIAN_POINT('Ctrl Pts',(0.116760312732254,-0.102776471400776,
1.41651187971548));
#16668=CARTESIAN_POINT('Ctrl Pts',(0.116486514317401,-0.103086690115851,
1.41648240926242));
#16669=CARTESIAN_POINT('Ctrl Pts',(0.115856176468814,-0.103795156897169,
1.41641474794436));
#16670=CARTESIAN_POINT('Ctrl Pts',(0.115498817148986,-0.104192665026349,
1.41637652295596));
#16671=CARTESIAN_POINT('Ctrl Pts',(0.11450533741787,-0.105286369194166,
1.41627061864795));
#16672=CARTESIAN_POINT('Ctrl Pts',(0.113864933044019,-0.1059786241908,1.41620275869379));
#16673=CARTESIAN_POINT('Ctrl Pts',(0.110214094329664,-0.10985376323717,
1.41581811535255));
#16674=CARTESIAN_POINT('Ctrl Pts',(0.107076836824166,-0.112913860054328,
1.41549588364254));
#16675=CARTESIAN_POINT('Ctrl Pts',(0.0967251249128689,-0.12219120561543,
1.4144565926546));
#16676=CARTESIAN_POINT('Ctrl Pts',(0.0890678488002784,-0.127880071317682,
1.4137206249058));
#16677=CARTESIAN_POINT('Ctrl Pts',(0.0731533824215551,-0.137577348903586,
1.41227540112032));
#16678=CARTESIAN_POINT('Ctrl Pts',(0.0649636405681001,-0.141628791817655,
1.41156945595844));
#16679=CARTESIAN_POINT('Ctrl Pts',(0.0558273440849809,-0.145188080151334,
1.41085088590449));
#16680=CARTESIAN_POINT('Ctrl Pts',(0.0551879371257263,-0.145432329995708,
1.41080095051627));
#16681=CARTESIAN_POINT('Ctrl Pts',(0.0542371248206536,-0.14578836106835,
1.41072724074169));
#16682=CARTESIAN_POINT('Ctrl Pts',(0.0539269534087554,-0.145903377731254,
1.41070328098766));
#16683=CARTESIAN_POINT('Ctrl Pts',(0.0533810890189833,-0.146103814732317,
1.41066126798602));
#16684=CARTESIAN_POINT('Ctrl Pts',(0.0531455547277884,-0.146189655449437,
1.41064318999886));
#16685=CARTESIAN_POINT('Ctrl Pts',(0.052637320018521,-0.14637349147278,
1.41060429000276));
#16686=CARTESIAN_POINT('Ctrl Pts',(0.0523645536149028,-0.146471294092463,
1.41058347951496));
#16687=CARTESIAN_POINT('Ctrl Pts',(0.051801645183462,-0.146671356074279,
1.41054066751045));
#16688=CARTESIAN_POINT('Ctrl Pts',(0.0515114696000755,-0.146773518184855,
1.41051867172985));
#16689=CARTESIAN_POINT('Ctrl Pts',(0.0507790716106046,-0.147028933985619,
1.41046333534763));
#16690=CARTESIAN_POINT('Ctrl Pts',(0.0503364530170813,-0.147181055353175,
1.41043005885366));
#16691=CARTESIAN_POINT('Ctrl Pts',(0.0490711059691243,-0.147609560350339,
1.41033538234264));
#16692=CARTESIAN_POINT('Ctrl Pts',(0.0482467256730211,-0.14788106469746,
1.41027424557166));
#16693=CARTESIAN_POINT('Ctrl Pts',(0.0391794327031243,-0.15078342353184,
1.40960732321446));
#16694=CARTESIAN_POINT('Ctrl Pts',(0.0307317468248462,-0.15272941271282,
1.40903534193767));
#16695=CARTESIAN_POINT('Ctrl Pts',(0.00998667550152534,-0.155715935731724,
1.40765481029465));
#16696=CARTESIAN_POINT('Ctrl Pts',(-0.00235482521677464,-0.15601792333516,
1.4068500850827));
#16697=CARTESIAN_POINT('Ctrl Pts',(-0.0163125766955438,-0.154701820547001,
1.40587548298647));
#16698=CARTESIAN_POINT('Ctrl Pts',(-0.0180199694970762,-0.154512244590398,
1.40575524130209));
#16699=CARTESIAN_POINT('Ctrl Pts',(-0.020417841358966,-0.154205719083121,
1.40558477863521));
#16700=CARTESIAN_POINT('Ctrl Pts',(-0.0211112508531559,-0.154112319761558,
1.40553529663746));
#16701=CARTESIAN_POINT('Ctrl Pts',(-0.0222329614871399,-0.153953517733336,
1.40545493600479));
#16702=CARTESIAN_POINT('Ctrl Pts',(-0.0226616668443592,-0.153890997293083,
1.40542414843897));
#16703=CARTESIAN_POINT('Ctrl Pts',(-0.0235553598542659,-0.153756849814088,
1.40535980913494));
#16704=CARTESIAN_POINT('Ctrl Pts',(-0.0240202942240823,-0.15368490263867,
1.40532624759488));
#16705=CARTESIAN_POINT('Ctrl Pts',(-0.0251198653098533,-0.153509635866561,
1.40524665827793));
#16706=CARTESIAN_POINT('Ctrl Pts',(-0.0257541975902381,-0.15340448891919,
1.40520057318147));
#16707=CARTESIAN_POINT('Ctrl Pts',(-0.0278623127734888,-0.1530416037679,
1.40504683501376));
#16708=CARTESIAN_POINT('Ctrl Pts',(-0.0293329861536879,-0.152766542768491,
1.40493863630077));
#16709=CARTESIAN_POINT('Ctrl Pts',(-0.0371368685561892,-0.151190137438781,
1.40435925555681));
#16710=CARTESIAN_POINT('Ctrl Pts',(-0.0433874191859156,-0.149516270007874,
1.4038763527493));
#16711=CARTESIAN_POINT('Ctrl Pts',(-0.0582212203167935,-0.14453524535105,
1.40268457695414));
#16712=CARTESIAN_POINT('Ctrl Pts',(-0.0666510649336296,-0.140846590084201,
1.40196765960564));
#16713=CARTESIAN_POINT('Ctrl Pts',(-0.0803791378116622,-0.133329807803446,
1.4007597024399));
#16714=CARTESIAN_POINT('Ctrl Pts',(-0.0858542800401925,-0.129871894198812,
1.40026609142151));
#16715=CARTESIAN_POINT('Ctrl Pts',(-0.0916664649086831,-0.125672400356744,
1.39974042420532));
#16716=CARTESIAN_POINT('Ctrl Pts',(-0.0922313841861929,-0.12525839221855,
1.39968931597493));
#16717=CARTESIAN_POINT('Ctrl Pts',(-0.0930614944153107,-0.124641374578354,
1.3996142155801));
#16718=CARTESIAN_POINT('Ctrl Pts',(-0.0933288480639727,-0.124441311968053,
1.39959002794176));
#16719=CARTESIAN_POINT('Ctrl Pts',(-0.0937939489664914,-0.124090931711175,
1.39954795286849));
#16720=CARTESIAN_POINT('Ctrl Pts',(-0.0939919822351667,-0.123940999974898,
1.39953003893238));
#16721=CARTESIAN_POINT('Ctrl Pts',(-0.094417058220138,-0.123617568589008,
1.39949158978689));
#16722=CARTESIAN_POINT('Ctrl Pts',(-0.0946439818366814,-0.123443917843267,
1.3994710654618));
#16723=CARTESIAN_POINT('Ctrl Pts',(-0.0952439703452555,-0.122982156404739,
1.39941679891469));
#16724=CARTESIAN_POINT('Ctrl Pts',(-0.0956162103718621,-0.122692970502384,
1.39938313129306));
#16725=CARTESIAN_POINT('Ctrl Pts',(-0.0964419594738644,-0.12204542199597,
1.3993084308861));
#16726=CARTESIAN_POINT('Ctrl Pts',(-0.0968948000376298,-0.121686212571192,
1.39926745523872));
#16727=CARTESIAN_POINT('Ctrl Pts',(-0.0982558445771977,-0.120594167936516,
1.39914423307526));
#16728=CARTESIAN_POINT('Ctrl Pts',(-0.0991578384285692,-0.119853609089712,
1.39906248024986));
#16729=CARTESIAN_POINT('Ctrl Pts',(-0.102464323851287,-0.117076023258314,
1.39876208604954));
#16730=CARTESIAN_POINT('Ctrl Pts',(-0.104815233622259,-0.11497609589624,
1.39854709117054));
#16731=CARTESIAN_POINT('Ctrl Pts',(-0.115228207152847,-0.105089757898351,
1.39757939922236));
#16732=CARTESIAN_POINT('Ctrl Pts',(-0.122498157472708,-0.0965174939919779,
1.39685756992712));
#16733=CARTESIAN_POINT('Ctrl Pts',(-0.132690416520789,-0.0814712820860795,
1.39564527760622));
#16734=CARTESIAN_POINT('Ctrl Pts',(-0.136204499238017,-0.0754495189133748,
1.39517261860127));
#16735=CARTESIAN_POINT('Ctrl Pts',(-0.139750888521818,-0.0683118193043369,
1.39461428236302));
#16736=CARTESIAN_POINT('Ctrl Pts',(-0.140189960618132,-0.0674061596364181,
1.39454348279125));
#16737=CARTESIAN_POINT('Ctrl Pts',(-0.140878260102637,-0.06595060823246,
1.3944297338395));
#16738=CARTESIAN_POINT('Ctrl Pts',(-0.141133134085882,-0.0654034046535807,
1.39438697937938));
#16739=CARTESIAN_POINT('Ctrl Pts',(-0.141578995342617,-0.0644314169132236,
1.39431104373391));
#16740=CARTESIAN_POINT('Ctrl Pts',(-0.141771273283171,-0.0640072298315101,
1.39427790730606));
#16741=CARTESIAN_POINT('Ctrl Pts',(-0.142166912323166,-0.0631238760545666,
1.39420890434326));
#16742=CARTESIAN_POINT('Ctrl Pts',(-0.142369960313065,-0.0626645759357227,
1.39417302757229));
#16743=CARTESIAN_POINT('Ctrl Pts',(-0.142889335642401,-0.0614741801206648,
1.39408004221332));
#16744=CARTESIAN_POINT('Ctrl Pts',(-0.143202273898766,-0.0607416312609533,
1.39402281925644));
#16745=CARTESIAN_POINT('Ctrl Pts',(-0.144517074735001,-0.0575972086573725,
1.39377715921711));
#16746=CARTESIAN_POINT('Ctrl Pts',(-0.14546367967645,-0.0551628470339443,
1.39358687824211));
#16747=CARTESIAN_POINT('Ctrl Pts',(-0.147795945942313,-0.0486868470246648,
1.39308005716341));
#16748=CARTESIAN_POINT('Ctrl Pts',(-0.149077076666379,-0.0446101987501447,
1.39276033245939));
#16749=CARTESIAN_POINT('Ctrl Pts',(-0.15375309343562,-0.0272639702260042,
1.39139765354976));
#16750=CARTESIAN_POINT('Ctrl Pts',(-0.15555526912902,-0.0136311345579096,
1.39031463336019));
#16751=CARTESIAN_POINT('Ctrl Pts',(-0.15554998842971,5.99959743726453E-5,
1.38928122911086));
#16752=CARTESIAN_POINT('Ctrl Pts',(-0.0636886258329916,0.141913922641527,
1.37660119646451));
#16753=CARTESIAN_POINT('Ctrl Pts',(-0.0672646134278248,0.140309078439693,
1.3768829359352));
#16754=CARTESIAN_POINT('Ctrl Pts',(-0.0707755899134079,0.138570924731718,
1.3771646754059));
#16755=CARTESIAN_POINT('Ctrl Pts',(-0.0742113165068752,0.136705826511954,
1.37744641487659));
#16756=CARTESIAN_POINT('Ctrl Pts',(-0.0832025825392944,0.131824881007623,
1.37818372457337));
#16757=CARTESIAN_POINT('Ctrl Pts',(-0.0917439477378679,0.12603479045185,
1.37892103427014));
#16758=CARTESIAN_POINT('Ctrl Pts',(-0.0996465697393686,0.11944188394017,
1.37965834396692));
#16759=CARTESIAN_POINT('Ctrl Pts',(-0.107598376984517,0.112807943742069,
1.38040024261621));
#16760=CARTESIAN_POINT('Ctrl Pts',(-0.114902627518598,0.105361621827393,
1.38114214126549));
#16761=CARTESIAN_POINT('Ctrl Pts',(-0.121396743056803,0.0972555051151373,
1.38188403991478));
#16762=CARTESIAN_POINT('Ctrl Pts',(-0.127835842296946,0.0892180611159775,
1.38261965340992));
#16763=CARTESIAN_POINT('Ctrl Pts',(-0.133477910941686,0.080532706875503,
1.38335526690506));
#16764=CARTESIAN_POINT('Ctrl Pts',(-0.138204096147797,0.0713822828716657,
1.3840908804002));
#16765=CARTESIAN_POINT('Ctrl Pts',(-0.142990852841695,0.0621145856820285,
1.38483592162656));
#16766=CARTESIAN_POINT('Ctrl Pts',(-0.14683759102957,0.052370652666543,
1.38558096285292));
#16767=CARTESIAN_POINT('Ctrl Pts',(-0.14967002282687,0.0423637435433198,
1.38632600407929));
#16768=CARTESIAN_POINT('Ctrl Pts',(-0.152502454624171,0.0323568344200951,
1.38707104530565));
#16769=CARTESIAN_POINT('Ctrl Pts',(-0.154320443732021,0.0220879207575721,
1.38781608653201));
#16770=CARTESIAN_POINT('Ctrl Pts',(-0.155103327025007,0.0117796623794456,
1.38856112775838));
#16771=CARTESIAN_POINT('Ctrl Pts',(-0.155399123126889,0.0078849022373452,
1.38884262602571));
#16772=CARTESIAN_POINT('Ctrl Pts',(-0.155548240648023,0.00397886205704992,
1.38912412429304));
#16773=CARTESIAN_POINT('Ctrl Pts',(-0.15554998452487,6.93852476632616E-5,
1.38940562256037));
#16774=CARTESIAN_POINT('Ctrl Pts',(-0.0636886474661844,0.141913912932905,
1.36266955208845));
#16775=CARTESIAN_POINT('Ctrl Pts',(-0.0688639616191303,0.139591316424911,
1.3630928312682));
#16776=CARTESIAN_POINT('Ctrl Pts',(-0.0739102973562643,0.1369864912641,
1.36352480444837));
#16777=CARTESIAN_POINT('Ctrl Pts',(-0.0856921396542741,0.130063343831725,
1.36457710306135));
#16778=CARTESIAN_POINT('Ctrl Pts',(-0.0922573124579418,0.125491841598355,
1.36520095550586));
#16779=CARTESIAN_POINT('Ctrl Pts',(-0.101258002258513,0.118134858423088,
1.36609348767914));
#16780=CARTESIAN_POINT('Ctrl Pts',(-0.103992376674986,0.11573511776738,
1.36637012355003));
#16781=CARTESIAN_POINT('Ctrl Pts',(-0.108049550126467,0.111914451201318,
1.36678632492678));
#16782=CARTESIAN_POINT('Ctrl Pts',(-0.109433993044875,0.110561077140873,
1.36692943653171));
#16783=CARTESIAN_POINT('Ctrl Pts',(-0.111138206297609,0.108831721599176,
1.36710659491168));
#16784=CARTESIAN_POINT('Ctrl Pts',(-0.111481860535304,0.108479672356529,
1.36714237079528));
#16785=CARTESIAN_POINT('Ctrl Pts',(-0.11202552556295,0.107917414267432,
1.36719904304916));
#16786=CARTESIAN_POINT('Ctrl Pts',(-0.112226624449519,0.107708270101527,
1.36722002217535));
#16787=CARTESIAN_POINT('Ctrl Pts',(-0.11260645338804,0.107311026825936,
1.36725967580905));
#16788=CARTESIAN_POINT('Ctrl Pts',(-0.112785295681815,0.107123045617149,
1.36727835868759));
#16789=CARTESIAN_POINT('Ctrl Pts',(-0.113195109737595,0.106690125923971,
1.36732119946899));
#16790=CARTESIAN_POINT('Ctrl Pts',(-0.113425757291714,0.106444884455639,
1.36734533239698));
#16791=CARTESIAN_POINT('Ctrl Pts',(-0.114040092506407,0.105787413916382,
1.36740967563519));
#16792=CARTESIAN_POINT('Ctrl Pts',(-0.11442234565153,0.105373841552063,
1.36744977931787));
#16793=CARTESIAN_POINT('Ctrl Pts',(-0.117197768009641,0.102338108916556,
1.36774154067777));
#16794=CARTESIAN_POINT('Ctrl Pts',(-0.119503030045236,0.0996365205062875,
1.36798706129001));
#16795=CARTESIAN_POINT('Ctrl Pts',(-0.123008176081925,0.0952318784020268,
1.36837005112417));
#16796=CARTESIAN_POINT('Ctrl Pts',(-0.124269654302658,0.0935797826475085,
1.36851006608177));
#16797=CARTESIAN_POINT('Ctrl Pts',(-0.131659610814762,0.0834884465253215,
1.36934701413561));
#16798=CARTESIAN_POINT('Ctrl Pts',(-0.136959759196717,0.0744755810458954,
1.37002091294087));
#16799=CARTESIAN_POINT('Ctrl Pts',(-0.143918970474773,0.0593453450142004,
1.37113303291619));
#16800=CARTESIAN_POINT('Ctrl Pts',(-0.146177765129095,0.0535405087759689,
1.37155524821357));
#16801=CARTESIAN_POINT('Ctrl Pts',(-0.148531329392937,0.0462211527850203,
1.37209148393496));
#16802=CARTESIAN_POINT('Ctrl Pts',(-0.148960246835224,0.0448195870285426,
1.37219431909291));
#16803=CARTESIAN_POINT('Ctrl Pts',(-0.149547219814545,0.0427999770713411,
1.37234281282051));
#16804=CARTESIAN_POINT('Ctrl Pts',(-0.149721389143636,0.0421866638001736,
1.37238794802417));
#16805=CARTESIAN_POINT('Ctrl Pts',(-0.150017235197604,0.041119970684242,
1.37246652720118));
#16806=CARTESIAN_POINT('Ctrl Pts',(-0.150140640195161,0.040667075114373,
1.37249991478166));
#16807=CARTESIAN_POINT('Ctrl Pts',(-0.150374273564743,0.0397940822154385,
1.3725643224015));
#16808=CARTESIAN_POINT('Ctrl Pts',(-0.150484796326114,0.03937406757158,
1.37259533258));
#16809=CARTESIAN_POINT('Ctrl Pts',(-0.150770357516921,0.0382700957634074,
1.37267690199069));
#16810=CARTESIAN_POINT('Ctrl Pts',(-0.150942499280473,0.0375854069555614,
1.37272755397808));
#16811=CARTESIAN_POINT('Ctrl Pts',(-0.151526536980619,0.0351936746013996,
1.37290472285196));
#16812=CARTESIAN_POINT('Ctrl Pts',(-0.151914168737528,0.0334809051298725,
1.37303201180024));
#16813=CARTESIAN_POINT('Ctrl Pts',(-0.154461931925954,0.021266474322541,
1.37394307218985));
#16814=CARTESIAN_POINT('Ctrl Pts',(-0.155559753193871,0.0105748508364614,
1.37476089397571));
#16815=CARTESIAN_POINT('Ctrl Pts',(-0.15554787850174,-0.00238697431566608,
1.37576482688623));
#16816=CARTESIAN_POINT('Ctrl Pts',(-0.155497243431645,-0.00463113013496754,
1.37593896517501));
#16817=CARTESIAN_POINT('Ctrl Pts',(-0.155371172290793,-0.00748142693314287,
1.37616018003544));
#16818=CARTESIAN_POINT('Ctrl Pts',(-0.155340709994526,-0.00808929843285904,
1.37620735973367));
#16819=CARTESIAN_POINT('Ctrl Pts',(-0.155068274409692,-0.012954330088632,
1.37658492140736));
#16820=CARTESIAN_POINT('Ctrl Pts',(-0.15465489931931,-0.0172002902653275,
1.37691427835633));
#16821=CARTESIAN_POINT('Ctrl Pts',(-0.153955734643448,-0.0222282118735399,
1.37730091160018));
#16822=CARTESIAN_POINT('Ctrl Pts',(-0.153837619047051,-0.0230314707409262,
1.37736257448975));
#16823=CARTESIAN_POINT('Ctrl Pts',(-0.153221742392761,-0.0270034959724454,
1.37766686266045));
#16824=CARTESIAN_POINT('Ctrl Pts',(-0.152632292925795,-0.0301575550367337,
1.37790651831394));
#16825=CARTESIAN_POINT('Ctrl Pts',(-0.151828632635557,-0.0338255498098905,
1.37818125199822));
#16826=CARTESIAN_POINT('Ctrl Pts',(-0.151708782838084,-0.034359085284491,
1.37822111435406));
#16827=CARTESIAN_POINT('Ctrl Pts',(-0.151511680585906,-0.0352153840253586,
1.37828491943834));
#16828=CARTESIAN_POINT('Ctrl Pts',(-0.151436205901583,-0.0355385449017062,
1.3783089595231));
#16829=CARTESIAN_POINT('Ctrl Pts',(-0.151300020903333,-0.0361133379153534,
1.37835164532919));
#16830=CARTESIAN_POINT('Ctrl Pts',(-0.151239716149397,-0.0363650624067039,
1.37837031392336));
#16831=CARTESIAN_POINT('Ctrl Pts',(-0.151109827927862,-0.0369013306867755,
1.37841003056709));
#16832=CARTESIAN_POINT('Ctrl Pts',(-0.151040069148171,-0.0371858281933781,
1.37843106836598));
#16833=CARTESIAN_POINT('Ctrl Pts',(-0.150847979326769,-0.0379597701411314,
1.37848821522442));
#16834=CARTESIAN_POINT('Ctrl Pts',(-0.150724068690257,-0.0384488251123607,
1.37852423481855));
#16835=CARTESIAN_POINT('Ctrl Pts',(-0.150074597528192,-0.0409607858908205,
1.37870881429158));
#16836=CARTESIAN_POINT('Ctrl Pts',(-0.149510651397193,-0.0429736789304506,
1.37885528568167));
#16837=CARTESIAN_POINT('Ctrl Pts',(-0.147727364648117,-0.048877941345908,
1.37928234904023));
#16838=CARTESIAN_POINT('Ctrl Pts',(-0.14639534406895,-0.0527336349159576,
1.37955792098303));
#16839=CARTESIAN_POINT('Ctrl Pts',(-0.141127032686453,-0.0662381431887435,
1.38052583986846));
#16840=CARTESIAN_POINT('Ctrl Pts',(-0.136375449259961,-0.0755385871689743,
1.38119924533695));
#16841=CARTESIAN_POINT('Ctrl Pts',(-0.127228917362253,-0.0897236731873988,
1.38232824946926));
#16842=CARTESIAN_POINT('Ctrl Pts',(-0.123393759470827,-0.0949289090939788,
1.38276783184552));
#16843=CARTESIAN_POINT('Ctrl Pts',(-0.118608548226377,-0.100641949577517,
1.38328999288634));
#16844=CARTESIAN_POINT('Ctrl Pts',(-0.117963281886143,-0.101397503779286,
1.38335989613302));
#16845=CARTESIAN_POINT('Ctrl Pts',(-0.116916974779799,-0.102599138572368,
1.38347247080913));
#16846=CARTESIAN_POINT('Ctrl Pts',(-0.11652050726507,-0.103049180471761,
1.38351495363448));
#16847=CARTESIAN_POINT('Ctrl Pts',(-0.115812045556906,-0.103844060242853,
1.38359056746984));
#16848=CARTESIAN_POINT('Ctrl Pts',(-0.115501087177952,-0.104189815221598,
1.3836236549275));
#16849=CARTESIAN_POINT('Ctrl Pts',(-0.114850095895701,-0.104907157382385,
1.38369271753777));
#16850=CARTESIAN_POINT('Ctrl Pts',(-0.11450979969522,-0.105278497140006,
1.38372870358017));
#16851=CARTESIAN_POINT('Ctrl Pts',(-0.11362172833703,-0.106238183138333,
1.38382232323869));
#16852=CARTESIAN_POINT('Ctrl Pts',(-0.113071191298008,-0.106823940950737,
1.38388007426121));
#16853=CARTESIAN_POINT('Ctrl Pts',(-0.110665377499298,-0.10934423242774,
1.38413124219618));
#16854=CARTESIAN_POINT('Ctrl Pts',(-0.108764916641453,-0.111234788575827,
1.38432660762635));
#16855=CARTESIAN_POINT('Ctrl Pts',(-0.103596561826311,-0.116117083257788,
1.38485045490948));
#16856=CARTESIAN_POINT('Ctrl Pts',(-0.100248288453831,-0.119019740265329,
1.38518239493091));
#16857=CARTESIAN_POINT('Ctrl Pts',(-0.087118820782712,-0.129454390059997,
1.3864562449401));
#16858=CARTESIAN_POINT('Ctrl Pts',(-0.076578204865397,-0.13595538070058,
1.38742818457375));
#16859=CARTESIAN_POINT('Ctrl Pts',(-0.0618381345820382,-0.142783373288334,
1.38866493250698));
#16860=CARTESIAN_POINT('Ctrl Pts',(-0.0582344820537444,-0.144290672531536,
1.38895809129996));
#16861=CARTESIAN_POINT('Ctrl Pts',(-0.0539853604612679,-0.145882772414045,
1.38929032318999));
#16862=CARTESIAN_POINT('Ctrl Pts',(-0.0533918028628148,-0.146101053573369,
1.38933643295144));
#16863=CARTESIAN_POINT('Ctrl Pts',(-0.0524916553017162,-0.146425865002342,
1.38940589021137));
#16864=CARTESIAN_POINT('Ctrl Pts',(-0.0521860458781278,-0.146535062148398,
1.38942939013984));
#16865=CARTESIAN_POINT('Ctrl Pts',(-0.0516372166121848,-0.146729229306329,
1.389471443637));
#16866=CARTESIAN_POINT('Ctrl Pts',(-0.0513941266457318,-0.146814551806214,
1.38949001773675));
#16867=CARTESIAN_POINT('Ctrl Pts',(-0.0508660585021629,-0.146998426907031,
1.38953025258091));
#16868=CARTESIAN_POINT('Ctrl Pts',(-0.0505810061857008,-0.147096754682547,
1.3895518999392));
#16869=CARTESIAN_POINT('Ctrl Pts',(-0.0497811979379651,-0.147370045845346,
1.38961244336106));
#16870=CARTESIAN_POINT('Ctrl Pts',(-0.0492658010752367,-0.14754314266875,
1.38965123120975));
#16871=CARTESIAN_POINT('Ctrl Pts',(-0.0462163811985503,-0.148549534419033,
1.38987945017749));
#16872=CARTESIAN_POINT('Ctrl Pts',(-0.0436619728792823,-0.149320301683406,
1.39006543660367));
#16873=CARTESIAN_POINT('Ctrl Pts',(-0.0269586552924137,-0.153894999942996,
1.39125593265297));
#16874=CARTESIAN_POINT('Ctrl Pts',(-0.0123513654010456,-0.155749765170369,
1.39218496841677));
#16875=CARTESIAN_POINT('Ctrl Pts',(0.00427533182359346,-0.155503769413597,
1.39330228050662));
#16876=CARTESIAN_POINT('Ctrl Pts',(0.00624872162983864,-0.155436976886721,
1.39343571467272));
#16877=CARTESIAN_POINT('Ctrl Pts',(0.0121562485200483,-0.155124348832398,
1.39383840526435));
#16878=CARTESIAN_POINT('Ctrl Pts',(0.016082589362646,-0.15476654604438,
1.39411040583891));
#16879=CARTESIAN_POINT('Ctrl Pts',(0.0209301905851279,-0.15413833662402,
1.39445361014386));
#16880=CARTESIAN_POINT('Ctrl Pts',(0.0218683890596436,-0.15400802960993,
1.39452037592705));
#16881=CARTESIAN_POINT('Ctrl Pts',(0.0233405248334821,-0.153789840809534,
1.39462570306025));
#16882=CARTESIAN_POINT('Ctrl Pts',(0.0238753052025794,-0.153707725972915,
1.39466408239205));
#16883=CARTESIAN_POINT('Ctrl Pts',(0.0248181253091664,-0.153557918157794,
1.39473195725703));
#16884=CARTESIAN_POINT('Ctrl Pts',(0.0252263462605754,-0.153491384191743,
1.39476141587294));
#16885=CARTESIAN_POINT('Ctrl Pts',(0.0261603880445246,-0.153335322413091,
1.39482898301296));
#16886=CARTESIAN_POINT('Ctrl Pts',(0.0266860209431342,-0.153244716957228,
1.39486712533358));
#16887=CARTESIAN_POINT('Ctrl Pts',(0.028135011055712,-0.152987267690811,
1.39497260490883));
#16888=CARTESIAN_POINT('Ctrl Pts',(0.0290573272660953,-0.15281477213631,
1.3950401204951));
#16889=CARTESIAN_POINT('Ctrl Pts',(0.0342061668073188,-0.151803516406592,
1.39541918648165));
#16890=CARTESIAN_POINT('Ctrl Pts',(0.0383975681508075,-0.150797842921769,
1.39573600115996));
#16891=CARTESIAN_POINT('Ctrl Pts',(0.0514255078870773,-0.147093597668828,
1.39674807775293));
#16892=CARTESIAN_POINT('Ctrl Pts',(0.0600657864033322,-0.143781665621738,
1.39746102473362));
#16893=CARTESIAN_POINT('Ctrl Pts',(0.0762490817109134,-0.135863950107734,
1.3988582510672));
#16894=CARTESIAN_POINT('Ctrl Pts',(0.0837979015692544,-0.131342613888997,
1.39953943577331));
#16895=CARTESIAN_POINT('Ctrl Pts',(0.0918683127884089,-0.125528348512753,
1.40027478385204));
#16896=CARTESIAN_POINT('Ctrl Pts',(0.0928036634911799,-0.124838429317268,
1.40036010968599));
#16897=CARTESIAN_POINT('Ctrl Pts',(0.0940687339961342,-0.123883229831781,
1.40047555555102));
#16898=CARTESIAN_POINT('Ctrl Pts',(0.0944052023409424,-0.123627016187872,
1.40050626454325));
#16899=CARTESIAN_POINT('Ctrl Pts',(0.0949368675241207,-0.12321872790308,
1.40055478991603));
#16900=CARTESIAN_POINT('Ctrl Pts',(0.0951327502078574,-0.12306755690102,
1.40057266846064));
#16901=CARTESIAN_POINT('Ctrl Pts',(0.0955353687750359,-0.122755303341884,
1.40060941517653));
#16902=CARTESIAN_POINT('Ctrl Pts',(0.095742058273858,-0.122594165702152,
1.40062827881778));
#16903=CARTESIAN_POINT('Ctrl Pts',(0.0962314913249354,-0.122210605068048,
1.40067294767757));
#16904=CARTESIAN_POINT('Ctrl Pts',(0.0965138747426703,-0.12198772029559,
1.40069872029979));
#16905=CARTESIAN_POINT('Ctrl Pts',(0.0974540977165782,-0.121240295371979,
1.40078454409008));
#16906=CARTESIAN_POINT('Ctrl Pts',(0.0981084701426475,-0.120711385354342,
1.40084429400798));
#16907=CARTESIAN_POINT('Ctrl Pts',(0.104176922246356,-0.115724486195703,
1.40139892205179));
#16908=CARTESIAN_POINT('Ctrl Pts',(0.109288818738309,-0.110909744696904,
1.40187021526625));
#16909=CARTESIAN_POINT('Ctrl Pts',(0.119108621941048,-0.100319960387341,
1.40282760177878));
#16910=CARTESIAN_POINT('Ctrl Pts',(0.12376188341211,-0.0945196069906272,
1.40331190100052));
#16911=CARTESIAN_POINT('Ctrl Pts',(0.13253147237701,-0.0818245379964986,
1.40433611051396));
#16912=CARTESIAN_POINT('Ctrl Pts',(0.136564372787938,-0.0748998598947808,
1.40487608075201));
#16913=CARTESIAN_POINT('Ctrl Pts',(0.14049422660366,-0.0667700047747948,
1.40550843858125));
#16914=CARTESIAN_POINT('Ctrl Pts',(0.140932821439027,-0.0658392056291265,
1.4055808012198));
#16915=CARTESIAN_POINT('Ctrl Pts',(0.141616710180522,-0.0643496862914652,
1.4056965762208));
#16916=CARTESIAN_POINT('Ctrl Pts',(0.141868012452856,-0.0637937438284535,
1.40573978231875));
#16917=CARTESIAN_POINT('Ctrl Pts',(0.142305738899494,-0.0628100065914654,
1.40581623300461));
#16918=CARTESIAN_POINT('Ctrl Pts',(0.142493522022308,-0.0623828215516508,
1.40584943073304));
#16919=CARTESIAN_POINT('Ctrl Pts',(0.142878199657009,-0.0614969246758663,
1.40591827805429));
#16920=CARTESIAN_POINT('Ctrl Pts',(0.143074813656206,-0.0610380976796266,
1.40595393672606));
#16921=CARTESIAN_POINT('Ctrl Pts',(0.14357432231333,-0.0598567477798282,
1.40604575505881));
#16922=CARTESIAN_POINT('Ctrl Pts',(0.14387396983893,-0.0591328761656403,
1.40610202376271));
#16923=CARTESIAN_POINT('Ctrl Pts',(0.145105210971574,-0.0560937474687334,
1.4063383199317));
#16924=CARTESIAN_POINT('Ctrl Pts',(0.145986435800257,-0.0537586269911329,
1.40652002130098));
#16925=CARTESIAN_POINT('Ctrl Pts',(0.14813692276093,-0.0476167175418052,
1.40699864410027));
#16926=CARTESIAN_POINT('Ctrl Pts',(0.149315663517163,-0.0437804430263291,
1.4072983266247));
#16927=CARTESIAN_POINT('Ctrl Pts',(0.15239855114542,-0.0321649330990623,
1.40820768137138));
#16928=CARTESIAN_POINT('Ctrl Pts',(0.153851703617052,-0.0242802937348053,
1.40882823696877));
#16929=CARTESIAN_POINT('Ctrl Pts',(0.155614324890464,-0.00757268786725114,
1.41013088802435));
#16930=CARTESIAN_POINT('Ctrl Pts',(0.15579368843639,0.00123804627988295,
1.41081073047552));
#16931=CARTESIAN_POINT('Ctrl Pts',(0.155182541497356,0.0107079265542668,
1.41150627780658));
#16932=CARTESIAN_POINT('Ctrl Pts',(0.1551333939331,0.0113978511779808,1.4115567440063));
#16933=CARTESIAN_POINT('Ctrl Pts',(0.155053833879795,0.0124185919313914,
1.4116310789295));
#16934=CARTESIAN_POINT('Ctrl Pts',(0.155026961979705,0.0127496624003516,
1.41165513758687));
#16935=CARTESIAN_POINT('Ctrl Pts',(0.154977310630607,0.0133380056281854,
1.41169779774452));
#16936=CARTESIAN_POINT('Ctrl Pts',(0.154954950762529,0.0135953095755898,
1.41171642234768));
#16937=CARTESIAN_POINT('Ctrl Pts',(0.154905572837179,0.0141475697135342,
1.41175632715783));
#16938=CARTESIAN_POINT('Ctrl Pts',(0.15487835325053,0.0144425040492692,
1.4117775959032));
#16939=CARTESIAN_POINT('Ctrl Pts',(0.154801094654367,0.0152542854216299,
1.41183602401434));
#16940=CARTESIAN_POINT('Ctrl Pts',(0.154749309172403,0.0157709689358164,
1.41187308702776));
#16941=CARTESIAN_POINT('Ctrl Pts',(0.154455251342063,0.0185638810093464,
1.41207279890991));
#16942=CARTESIAN_POINT('Ctrl Pts',(0.154165327161617,0.020834964468423,
1.41223292957326));
#16943=CARTESIAN_POINT('Ctrl Pts',(0.151705237384277,0.037217687789671,
1.41337705047185));
#16944=CARTESIAN_POINT('Ctrl Pts',(0.147651269347817,0.0509789121898426,
1.41428422010012));
#16945=CARTESIAN_POINT('Ctrl Pts',(0.139116595903316,0.0698867453134283,
1.41567183097907));
#16946=CARTESIAN_POINT('Ctrl Pts',(0.13609296513136,0.0756060312159878,
1.41611166482707));
#16947=CARTESIAN_POINT('Ctrl Pts',(0.132204490486604,0.0819680585372037,
1.41663410024237));
#16948=CARTESIAN_POINT('Ctrl Pts',(0.13167817246175,0.0828109216298087,
1.41670401042212));
#16949=CARTESIAN_POINT('Ctrl Pts',(0.130821275621213,0.0841543588142361,
1.41681659413094));
#16950=CARTESIAN_POINT('Ctrl Pts',(0.130495807571174,0.0846581741517003,
1.41685907900717));
#16951=CARTESIAN_POINT('Ctrl Pts',(0.129912847467376,0.0855492303343974,
1.41693469520173));
#16952=CARTESIAN_POINT('Ctrl Pts',(0.129656515867659,0.0859372249514269,
1.41696778295836));
#16953=CARTESIAN_POINT('Ctrl Pts',(0.129118933912947,0.086743052107196,
1.41703684489041));
#16954=CARTESIAN_POINT('Ctrl Pts',(0.128837386665819,0.0871606790347807,
1.41707282995029));
#16955=CARTESIAN_POINT('Ctrl Pts',(0.128101263028642,0.0882412319664316,
1.41716644421233));
#16956=CARTESIAN_POINT('Ctrl Pts',(0.127643572574545,0.0889020075356767,
1.41722419079551));
#16957=CARTESIAN_POINT('Ctrl Pts',(0.125637867168078,0.0917502599931941,
1.41747531281612));
#16958=CARTESIAN_POINT('Ctrl Pts',(0.124038677058333,0.0939009521213358,
1.4176706358889));
#16959=CARTESIAN_POINT('Ctrl Pts',(0.119651533789701,0.0994933334042916,
1.4181943407255));
#16960=CARTESIAN_POINT('Ctrl Pts',(0.11677095914559,0.102858880511751,1.41852617831983));
#16961=CARTESIAN_POINT('Ctrl Pts',(0.105328564155101,0.115126780803263,
1.41980038714684));
#16962=CARTESIAN_POINT('Ctrl Pts',(0.0958618624554302,0.123120852445625,
1.4207728349456));
#16963=CARTESIAN_POINT('Ctrl Pts',(0.0843944804491291,0.13067245096559,
1.42181814082777));
#16964=CARTESIAN_POINT('Ctrl Pts',(0.0832285118141076,0.131418160214536,
1.42192299000539));
#16965=CARTESIAN_POINT('Ctrl Pts',(0.0798181917657878,0.133535676281692,
1.42222522710932));
#16966=CARTESIAN_POINT('Ctrl Pts',(0.0775486571921883,0.13486633591645,
1.42242089121785));
#16967=CARTESIAN_POINT('Ctrl Pts',(0.0747957817238612,0.136387897179991,
1.42265083862931));
#16968=CARTESIAN_POINT('Ctrl Pts',(0.0743440313754666,0.136634667927714,
1.42268833992154));
#16969=CARTESIAN_POINT('Ctrl Pts',(0.0736044233517935,0.137033928146401,
1.42274934712946));
#16970=CARTESIAN_POINT('Ctrl Pts',(0.073317301908686,0.137187761284676,
1.42277293518221));
#16971=CARTESIAN_POINT('Ctrl Pts',(0.0728076029199767,0.137458789202218,
1.42281463717451));
#16972=CARTESIAN_POINT('Ctrl Pts',(0.072585223292913,0.137576346567206,
1.42283277379023));
#16973=CARTESIAN_POINT('Ctrl Pts',(0.0721044479318759,0.137829010395008,
1.42287185937288));
#16974=CARTESIAN_POINT('Ctrl Pts',(0.0718459579075506,0.137963929540243,
1.42289279647424));
#16975=CARTESIAN_POINT('Ctrl Pts',(0.0713099135085865,0.138241803391027,
1.4229360581229));
#16976=CARTESIAN_POINT('Ctrl Pts',(0.0710323047159421,0.138384651102189,
1.42295837599763));
#16977=CARTESIAN_POINT('Ctrl Pts',(0.0703275649086268,0.138744605968689,
1.42301481791084));
#16978=CARTESIAN_POINT('Ctrl Pts',(0.069899853326939,0.138960579273107,
1.42304887398363));
#16979=CARTESIAN_POINT('Ctrl Pts',(0.0686683520551014,0.139575302188463,
1.42314638071538));
#16980=CARTESIAN_POINT('Ctrl Pts',(0.0678620848486968,0.139969086193708,
1.42320954854869));
#16981=CARTESIAN_POINT('Ctrl Pts',(0.058643275810757,0.144373202007019,
1.42392472497687));
#16982=CARTESIAN_POINT('Ctrl Pts',(0.0498887458046868,0.147627306158739,
1.4245377567599));
#16983=CARTESIAN_POINT('Ctrl Pts',(0.0297618703397016,0.153111617344858,
1.42591082694151));
#16984=CARTESIAN_POINT('Ctrl Pts',(0.0183280937428587,0.154896642435418,
1.42666886063419));
#16985=CARTESIAN_POINT('Ctrl Pts',(0.00505766118145182,0.155477567507879,
1.42759196224716));
#16986=CARTESIAN_POINT('Ctrl Pts',(0.0033113983290382,0.155524558013418,
1.4277142075388));
#16987=CARTESIAN_POINT('Ctrl Pts',(0.000860382596904026,0.155549215554783,
1.42788703450928));
#16988=CARTESIAN_POINT('Ctrl Pts',(0.000155961494741628,0.155551516754159,
1.42793684903535));
#16989=CARTESIAN_POINT('Ctrl Pts',(-0.000982460733778573,0.155547502862334,
1.42801759793379));
#16990=CARTESIAN_POINT('Ctrl Pts',(-0.00141646848126894,0.155544156064679,
1.4280484394362));
#16991=CARTESIAN_POINT('Ctrl Pts',(-0.00232004107025522,0.155533406231651,
1.42811277090245));
#16992=CARTESIAN_POINT('Ctrl Pts',(-0.00278959708450549,0.15552569300214,
1.4281462702244));
#16993=CARTESIAN_POINT('Ctrl Pts',(-0.00389776182029502,0.155502469475048,
1.42822549479645));
#16994=CARTESIAN_POINT('Ctrl Pts',(-0.00453631989229349,0.155485151507581,
1.42827127599278));
#16995=CARTESIAN_POINT('Ctrl Pts',(-0.00664665160358494,0.155414907372182,
1.4284230157242));
#16996=CARTESIAN_POINT('Ctrl Pts',(-0.0081177398432963,0.155345014189401,
1.42852950075198));
#16997=CARTESIAN_POINT('Ctrl Pts',(-0.0158553046780688,0.154867188745633,
1.42909349985657));
#16998=CARTESIAN_POINT('Ctrl Pts',(-0.0220929626075653,0.154100999410571,
1.42956205014491));
#16999=CARTESIAN_POINT('Ctrl Pts',(-0.0380932836478177,0.151144192606857,
1.43079982974944));
#17000=CARTESIAN_POINT('Ctrl Pts',(-0.0477217951951853,0.14838554072075,
1.43158139264115));
#17001=CARTESIAN_POINT('Ctrl Pts',(-0.0592634140963715,0.143838361237585,
1.43253669426715));
#17002=CARTESIAN_POINT('Ctrl Pts',(-0.0614875180861261,0.142901743502157,
1.43272156478415));
#17003=CARTESIAN_POINT('Ctrl Pts',(-0.0636886279094242,0.141913921709658,
1.43290478746296));
#17004=CARTESIAN_POINT('Origin',(0.,0.,-0.129405622560373));
#17005=CARTESIAN_POINT('',(-0.063688625831373,0.141913922642253,1.51675072916146));
#17006=CARTESIAN_POINT('',(-0.0636886280167372,0.141913921661498,1.50282608545586));
#17007=CARTESIAN_POINT('',(-0.0636886258329924,0.141913922641526,-0.129405622560373));
#17008=CARTESIAN_POINT('Ctrl Pts',(-0.063688625831373,0.141913922642253,
1.51675072916146));
#17009=CARTESIAN_POINT('Ctrl Pts',(-0.0634115737974058,0.142038259021649,
1.5167292894899));
#17010=CARTESIAN_POINT('Ctrl Pts',(-0.0631341587634355,0.142161783591578,
1.51670782241692));
#17011=CARTESIAN_POINT('Ctrl Pts',(-0.0623721692403226,0.142498404291874,
1.51664885823609));
#17012=CARTESIAN_POINT('Ctrl Pts',(-0.0618868709325375,0.142709838185951,
1.51661130546527));
#17013=CARTESIAN_POINT('Ctrl Pts',(-0.0613978711293336,0.142919921386151,
1.51657346424412));
#17014=CARTESIAN_POINT('Ctrl Pts',(-0.0613952339921468,0.142921054261741,
1.51657326016936));
#17015=CARTESIAN_POINT('Ctrl Pts',(-0.0613898650871311,0.142923360488841,
1.51657284469672));
#17016=CARTESIAN_POINT('Ctrl Pts',(-0.0613871333164061,0.142924533835284,
1.51657263329862));
#17017=CARTESIAN_POINT('Ctrl Pts',(-0.0613815715135784,0.142926922544389,
1.51657220289832));
#17018=CARTESIAN_POINT('Ctrl Pts',(-0.0613787414796765,0.142928137901035,
1.51657198389599));
#17019=CARTESIAN_POINT('Ctrl Pts',(-0.0613729789905258,0.142930612396411,
1.5165715379653));
#17020=CARTESIAN_POINT('Ctrl Pts',(-0.0613700465316182,0.142931871529327,
1.51657131103664));
#17021=CARTESIAN_POINT('Ctrl Pts',(-0.0613640771852345,0.142934434417069,
1.51657084909799));
#17022=CARTESIAN_POINT('Ctrl Pts',(-0.0613610391530454,0.142935738655462,
1.51657061399939));
#17023=CARTESIAN_POINT('Ctrl Pts',(-0.0613548529131532,0.142938394197412,
1.51657013527607));
#17024=CARTESIAN_POINT('Ctrl Pts',(-0.0613517047882596,0.142939745456975,
1.51656989165776));
#17025=CARTESIAN_POINT('Ctrl Pts',(-0.0613452940898259,0.142942496849713,
1.51656939556433));
#17026=CARTESIAN_POINT('Ctrl Pts',(-0.0613420315920367,0.142943896941283,
1.51656914309507));
#17027=CARTESIAN_POINT('Ctrl Pts',(-0.0613353876915296,0.142946747882776,
1.51656862895485));
#17028=CARTESIAN_POINT('Ctrl Pts',(-0.0613320063588894,0.142948198692836,
1.51656836728932));
#17029=CARTESIAN_POINT('Ctrl Pts',(-0.0613251201388662,0.142951153036596,
1.51656783439673));
#17030=CARTESIAN_POINT('Ctrl Pts',(-0.0613216153178053,0.142952656531297,
1.51656756317479));
#17031=CARTESIAN_POINT('Ctrl Pts',(-0.0613144772768866,0.142955718290263,
1.5165670107945));
#17032=CARTESIAN_POINT('Ctrl Pts',(-0.0613108441172547,0.142957276517335,
1.5165667296408));
#17033=CARTESIAN_POINT('Ctrl Pts',(-0.0613034444908888,0.142960449811625,
1.51656615701712));
#17034=CARTESIAN_POINT('Ctrl Pts',(-0.0612996780825213,0.142962064841614,
1.51656586555166));
#17035=CARTESIAN_POINT('Ctrl Pts',(-0.060872511151842,0.143145213360316,
1.5165328090021));
#17036=CARTESIAN_POINT('Ctrl Pts',(-0.0604483110807719,0.143324863164073,
1.51649998039455));
#17037=CARTESIAN_POINT('Ctrl Pts',(-0.0594965426649963,0.143722962528017,
1.51642631646053));
#17038=CARTESIAN_POINT('Ctrl Pts',(-0.0589685592715691,0.143940395818116,
1.51638544730296));
#17039=CARTESIAN_POINT('Ctrl Pts',(-0.057626579403494,0.144484425098828,
1.51628155080268));
#17040=CARTESIAN_POINT('Ctrl Pts',(-0.0568110051460953,0.144807048811859,
1.5162183910559));
#17041=CARTESIAN_POINT('Ctrl Pts',(-0.0521255864926039,0.146614825505493,
1.51585539465859));
#17042=CARTESIAN_POINT('Ctrl Pts',(-0.0482006912242076,0.147951583835434,
1.51555067628713));
#17043=CARTESIAN_POINT('Ctrl Pts',(-0.042509196919865,0.149639509079444,
1.51510739441969));
#17044=CARTESIAN_POINT('Ctrl Pts',(-0.0407823437156287,0.150119334225748,
1.51497272744455));
#17045=CARTESIAN_POINT('Ctrl Pts',(-0.0247139380899117,0.154286410622172,
1.5137182616087));
#17046=CARTESIAN_POINT('Ctrl Pts',(-0.00992516384667007,0.155937452321803,
1.51254348940641));
#17047=CARTESIAN_POINT('Ctrl Pts',(0.00734259446272711,0.155396250235547,
1.51124529336215));
#17048=CARTESIAN_POINT('Ctrl Pts',(0.00981036872442895,0.155259997484279,
1.51106177617048));
#17049=CARTESIAN_POINT('Ctrl Pts',(0.012812769854591,0.15502234512544,1.51084175491769));
#17050=CARTESIAN_POINT('Ctrl Pts',(0.0133512950299314,0.154976893451499,
1.51080241890958));
#17051=CARTESIAN_POINT('Ctrl Pts',(0.0141892635572375,0.154901768324114,
1.51074142096896));
#17052=CARTESIAN_POINT('Ctrl Pts',(0.0144888689648992,0.154874031750151,
1.51071965385025));
#17053=CARTESIAN_POINT('Ctrl Pts',(0.0150450130498069,0.15482091762925,
1.51067932874813));
#17054=CARTESIAN_POINT('Ctrl Pts',(0.0153015665954479,0.154795771953959,
1.51066075846002));
#17055=CARTESIAN_POINT('Ctrl Pts',(0.0158820647205028,0.154737418093621,
1.51061881131201));
#17056=CARTESIAN_POINT('Ctrl Pts',(0.0162059676230002,0.154703830452683,
1.51059545599026));
#17057=CARTESIAN_POINT('Ctrl Pts',(0.0170411077525711,0.154614577587804,
1.51053536108826));
#17058=CARTESIAN_POINT('Ctrl Pts',(0.0175521842537917,0.154557393235694,
1.51049870471842));
#17059=CARTESIAN_POINT('Ctrl Pts',(0.0206659005822639,0.154193355475082,
1.51027605435428));
#17060=CARTESIAN_POINT('Ctrl Pts',(0.0232609259647238,0.153823281139247,
1.51009337955431));
#17061=CARTESIAN_POINT('Ctrl Pts',(0.0272206377575225,0.153156076940302,
1.5098173466242));
#17062=CARTESIAN_POINT('Ctrl Pts',(0.0285925822364789,0.152905891033015,
1.50972221037129));
#17063=CARTESIAN_POINT('Ctrl Pts',(0.0311635770627496,0.15240123302773,
1.50954455974723));
#17064=CARTESIAN_POINT('Ctrl Pts',(0.0323633303686801,0.152150975501402,
1.50946191991524));
#17065=CARTESIAN_POINT('Ctrl Pts',(0.0480581833920141,0.148683126255555,
1.50838281827206));
#17066=CARTESIAN_POINT('Ctrl Pts',(0.0620226148497372,0.143420657705692,
1.50743675080658));
#17067=CARTESIAN_POINT('Ctrl Pts',(0.0769223327153423,0.135216214616027,
1.50627177882863));
#17068=CARTESIAN_POINT('Ctrl Pts',(0.078792825861938,0.134134856789172,
1.50612262793406));
#17069=CARTESIAN_POINT('Ctrl Pts',(0.0815514984620614,0.132462415389452,
1.50589787941424));
#17070=CARTESIAN_POINT('Ctrl Pts',(0.0824571545102543,0.131900553313644,
1.50582330859723));
#17071=CARTESIAN_POINT('Ctrl Pts',(0.0841002150065367,0.130857675917978,
1.50568652643191));
#17072=CARTESIAN_POINT('Ctrl Pts',(0.0848394515442751,0.130379618481977,
1.505624424245));
#17073=CARTESIAN_POINT('Ctrl Pts',(0.086006519932023,0.129610757963195,
1.5055254631358));
#17074=CARTESIAN_POINT('Ctrl Pts',(0.0864370360673013,0.129324045848996,
1.50548875710056));
#17075=CARTESIAN_POINT('Ctrl Pts',(0.0872481022272445,0.128778038522164,
1.50541922032438));
#17076=CARTESIAN_POINT('Ctrl Pts',(0.0876289473621483,0.128519189709944,
1.50538640665426));
#17077=CARTESIAN_POINT('Ctrl Pts',(0.0884773378952887,0.127937040372345,
1.50531294296411));
#17078=CARTESIAN_POINT('Ctrl Pts',(0.0889442697050343,0.127612861777527,
1.5052722599394));
#17079=CARTESIAN_POINT('Ctrl Pts',(0.0901203194974467,0.12678677089015,
1.50516915018316));
#17080=CARTESIAN_POINT('Ctrl Pts',(0.0908270208172611,0.12628146931204,
1.50510659450564));
#17081=CARTESIAN_POINT('Ctrl Pts',(0.0947820210169453,0.123403214296666,
1.50475308683724));
#17082=CARTESIAN_POINT('Ctrl Pts',(0.0979412515675018,0.120911085206228,
1.50445754595618));
#17083=CARTESIAN_POINT('Ctrl Pts',(0.102756938693512,0.116799615877514,
1.50398519670993));
#17084=CARTESIAN_POINT('Ctrl Pts',(0.104480059052111,0.115260813196359,
1.50381146899885));
#17085=CARTESIAN_POINT('Ctrl Pts',(0.116815377746958,0.103741026462546,
1.50253303966394));
#17086=CARTESIAN_POINT('Ctrl Pts',(0.126011599839395,0.0923528403500003,
1.50137757784007));
#17087=CARTESIAN_POINT('Ctrl Pts',(0.134700107778986,0.0778283231196782,
1.50010748544427));
#17088=CARTESIAN_POINT('Ctrl Pts',(0.135864952580801,0.0757765347766056,
1.4999324793348));
#17089=CARTESIAN_POINT('Ctrl Pts',(0.137231126208496,0.0732372535132789,
1.49972191510898));
#17090=CARTESIAN_POINT('Ctrl Pts',(0.137477167097544,0.0727743488516348,
1.4996837701762));
#17091=CARTESIAN_POINT('Ctrl Pts',(0.137859088665095,0.0720469470532173,
1.49962421576684));
#17092=CARTESIAN_POINT('Ctrl Pts',(0.137996555991879,0.071783295032284,
1.49960270886281));
#17093=CARTESIAN_POINT('Ctrl Pts',(0.13825198666125,0.0712899526891006,
1.49956261508574));
#17094=CARTESIAN_POINT('Ctrl Pts',(0.138370132754727,0.0710603654174914,
1.49954401719314));
#17095=CARTESIAN_POINT('Ctrl Pts',(0.138638281864521,0.0705360804446323,
1.49950168389232));
#17096=CARTESIAN_POINT('Ctrl Pts',(0.138787917007515,0.0702411983173544,
1.4994779716832));
#17097=CARTESIAN_POINT('Ctrl Pts',(0.139244078401547,0.0693351041010873,
1.49940540356294));
#17098=CARTESIAN_POINT('Ctrl Pts',(0.139547521508513,0.0687223349244418,
1.49935673548462));
#17099=CARTESIAN_POINT('Ctrl Pts',(0.143851463827285,0.0598849459786123,
1.49866039822767));
#17100=CARTESIAN_POINT('Ctrl Pts',(0.147123742185742,0.0513236201721397,
1.49805421826056));
#17101=CARTESIAN_POINT('Ctrl Pts',(0.152221494482901,0.0333862455787411,
1.49682522297701));
#17102=CARTESIAN_POINT('Ctrl Pts',(0.153975621809865,0.0240315752144556,
1.49620463236699));
#17103=CARTESIAN_POINT('Ctrl Pts',(0.155275615618776,0.0102192199852124,
1.4952629482169));
#17104=CARTESIAN_POINT('Ctrl Pts',(0.155501596065599,0.00584780215777957,
1.4949615235644));
#17105=CARTESIAN_POINT('Ctrl Pts',(0.155551952662081,0.00053031875706886,
1.49458806859122));
#17106=CARTESIAN_POINT('Ctrl Pts',(0.155552309763188,-0.000412398471685439,
1.49452160438454));
#17107=CARTESIAN_POINT('Ctrl Pts',(0.155539441981686,-0.00188947944462984,
1.49441704025413));
#17108=CARTESIAN_POINT('Ctrl Pts',(0.155532031826787,-0.00242388271454619,
1.49437912196931));
#17109=CARTESIAN_POINT('Ctrl Pts',(0.155513998882076,-0.00337192128196993,
1.49431169489536));
#17110=CARTESIAN_POINT('Ctrl Pts',(0.155504479421026,-0.00378557463955963,
1.4942822208522));
#17111=CARTESIAN_POINT('Ctrl Pts',(0.155478724166731,-0.00473927711242047,
1.49421413984222));
#17112=CARTESIAN_POINT('Ctrl Pts',(0.155461324882002,-0.00527928673103993,
1.49417549689011));
#17113=CARTESIAN_POINT('Ctrl Pts',(0.155405818573014,-0.00676196123561041,
1.49406913316351));
#17114=CARTESIAN_POINT('Ctrl Pts',(0.155361948755169,-0.00770437357741231,
1.49400123341052));
#17115=CARTESIAN_POINT('Ctrl Pts',(0.155093148164175,-0.0125327096170083,
1.49365180088238));
#17116=CARTESIAN_POINT('Ctrl Pts',(0.154731006502274,-0.016409266671623,
1.49336602700572));
#17117=CARTESIAN_POINT('Ctrl Pts',(0.153960853381503,-0.0222695801432221,
1.49292558228463));
#17118=CARTESIAN_POINT('Ctrl Pts',(0.153658855175888,-0.0242659055892493,
1.49277405386945));
#17119=CARTESIAN_POINT('Ctrl Pts',(0.150845569777699,-0.0406938567296243,
1.49151498647515));
#17120=CARTESIAN_POINT('Ctrl Pts',(0.146346575403846,-0.0547081111284029,
1.49035373953866));
#17121=CARTESIAN_POINT('Ctrl Pts',(0.13878414728827,-0.0702990705423108,
1.48904900247372));
#17122=CARTESIAN_POINT('Ctrl Pts',(0.137551059375049,-0.0726822349840366,
1.4888494766122));
#17123=CARTESIAN_POINT('Ctrl Pts',(0.13599410496507,-0.0755096192129182,
1.48861365684526));
#17124=CARTESIAN_POINT('Ctrl Pts',(0.135728857481408,-0.0759853699706729,
1.48857400795639));
#17125=CARTESIAN_POINT('Ctrl Pts',(0.135312758419945,-0.0767225585972718,
1.48851263125344));
#17126=CARTESIAN_POINT('Ctrl Pts',(0.135163639337301,-0.0769849608316749,
1.48849079617333));
#17127=CARTESIAN_POINT('Ctrl Pts',(0.134885781319639,-0.0774706067249488,
1.48845040900936));
#17128=CARTESIAN_POINT('Ctrl Pts',(0.134757252569568,-0.0776939623804312,
1.48843184428833));
#17129=CARTESIAN_POINT('Ctrl Pts',(0.134465669142637,-0.0781977720815382,
1.48838999051033));
#17130=CARTESIAN_POINT('Ctrl Pts',(0.134302292186977,-0.0784780354941646,
1.48836672258367));
#17131=CARTESIAN_POINT('Ctrl Pts',(0.133818280215661,-0.0793023909855428,
1.4882983207155));
#17132=CARTESIAN_POINT('Ctrl Pts',(0.133495201828687,-0.0798450528280568,
1.4882533409902));
#17133=CARTESIAN_POINT('Ctrl Pts',(0.13116444263278,-0.0837062405859229,
1.48793353066938));
#17134=CARTESIAN_POINT('Ctrl Pts',(0.129036355577877,-0.0869509694362822,
1.48766600553238));
#17135=CARTESIAN_POINT('Ctrl Pts',(0.119613596422089,-0.100208778496501,
1.48656292868547));
#17136=CARTESIAN_POINT('Ctrl Pts',(0.111257771295966,-0.109411914234389,
1.48576902397183));
#17137=CARTESIAN_POINT('Ctrl Pts',(0.0985606166172678,-0.120420595091738,
1.48464549146989));
#17138=CARTESIAN_POINT('Ctrl Pts',(0.0951016149729839,-0.123170583067822,
1.48434675531116));
#17139=CARTESIAN_POINT('Ctrl Pts',(0.0893674766942415,-0.127343681998074,
1.4838583572797));
#17140=CARTESIAN_POINT('Ctrl Pts',(0.0871643172428911,-0.128861707025169,
1.48367223611274));
#17141=CARTESIAN_POINT('Ctrl Pts',(0.0842500556813007,-0.130760759396556,
1.48342741238877));
#17142=CARTESIAN_POINT('Ctrl Pts',(0.083573511007153,-0.131194193067917,
1.48337067111942));
#17143=CARTESIAN_POINT('Ctrl Pts',(0.0824674293604693,-0.131890785544996,
1.4832780421304));
#17144=CARTESIAN_POINT('Ctrl Pts',(0.0820399120696445,-0.132157137657141,
1.48324227263292));
#17145=CARTESIAN_POINT('Ctrl Pts',(0.081215067482475,-0.132665488135432,
1.48317331874972));
#17146=CARTESIAN_POINT('Ctrl Pts',(0.0808179327809818,-0.132907790068002,
1.48314014595945));
#17147=CARTESIAN_POINT('Ctrl Pts',(0.0799058888868548,-0.133458651874716,
1.48306401884765));
#17148=CARTESIAN_POINT('Ctrl Pts',(0.079390271329594,-0.13376601825027,
1.48302102166397));
#17149=CARTESIAN_POINT('Ctrl Pts',(0.0780153002244631,-0.134574906415282,
1.48290646315729));
#17150=CARTESIAN_POINT('Ctrl Pts',(0.0771529042156,-0.135071173058272,1.48283471366319));
#17151=CARTESIAN_POINT('Ctrl Pts',(0.0706168988435978,-0.138749306670897,
1.4822916159683));
#17152=CARTESIAN_POINT('Ctrl Pts',(0.0647542977002466,-0.141580277692862,
1.48180791387295));
#17153=CARTESIAN_POINT('Ctrl Pts',(0.0490378072537463,-0.147988884587285,
1.48051921234261));
#17154=CARTESIAN_POINT('Ctrl Pts',(0.038969174287163,-0.150952929635953,
1.47969982599384));
#17155=CARTESIAN_POINT('Ctrl Pts',(0.0247427598898267,-0.153621776764717,
1.47858580191837));
#17156=CARTESIAN_POINT('Ctrl Pts',(0.0207775636243955,-0.154208146445459,
1.47828016280414));
#17157=CARTESIAN_POINT('Ctrl Pts',(0.014739926060913,-0.154863828791347,
1.47782590921319));
#17158=CARTESIAN_POINT('Ctrl Pts',(0.0126816152154906,-0.155045956596636,
1.47767299937988));
#17159=CARTESIAN_POINT('Ctrl Pts',(0.0101186113198169,-0.15522135461602,
1.47748549914493));
#17160=CARTESIAN_POINT('Ctrl Pts',(0.00961689504560676,-0.155253246576093,
1.47744893346168));
#17161=CARTESIAN_POINT('Ctrl Pts',(0.00882294108970852,-0.155299851309404,
1.47739129666488));
#17162=CARTESIAN_POINT('Ctrl Pts',(0.00853080739872957,-0.155316172484348,
1.47737013802526));
#17163=CARTESIAN_POINT('Ctrl Pts',(0.00797996845085937,-0.155345388394753,
1.47733033585618));
#17164=CARTESIAN_POINT('Ctrl Pts',(0.00772128030091277,-0.155358461063024,
1.47731168306248));
#17165=CARTESIAN_POINT('Ctrl Pts',(0.00713025432043404,-0.155386848386901,
1.47726915525496));
#17166=CARTESIAN_POINT('Ctrl Pts',(0.00679789938511911,-0.155401743065625,
1.47724530391799));
#17167=CARTESIAN_POINT('Ctrl Pts',(0.00591652592644753,-0.155438409376836,
1.47718221483092));
#17168=CARTESIAN_POINT('Ctrl Pts',(0.00536742875672291,-0.155458338860321,
1.47714307722409));
#17169=CARTESIAN_POINT('Ctrl Pts',(0.00156140291275468,-0.155576288708972,
1.47687288263785));
#17170=CARTESIAN_POINT('Ctrl Pts',(-0.00169809842502759,-0.155574869554208,
1.47664698689106));
#17171=CARTESIAN_POINT('Ctrl Pts',(-0.016995090789953,-0.155087297234471,
1.47560251408687));
#17172=CARTESIAN_POINT('Ctrl Pts',(-0.0289503915960709,-0.153306339930389,
1.47482903575262));
#17173=CARTESIAN_POINT('Ctrl Pts',(-0.0454927493567403,-0.148835805218277,
1.47368908609705));
#17174=CARTESIAN_POINT('Ctrl Pts',(-0.0503357744107182,-0.147268427433021,
1.47334680726373));
#17175=CARTESIAN_POINT('Ctrl Pts',(-0.0578569305323005,-0.144419919534064,
1.47279438291488));
#17176=CARTESIAN_POINT('Ctrl Pts',(-0.0605902921229622,-0.143294633785485,
1.47258911397594));
#17177=CARTESIAN_POINT('Ctrl Pts',(-0.0640498721877315,-0.141753690268276,
1.47232268022847));
#17178=CARTESIAN_POINT('Ctrl Pts',(-0.0648072068765667,-0.141409054591942,
1.47226394151801));
#17179=CARTESIAN_POINT('Ctrl Pts',(-0.0660242433682394,-0.140843395021498,
1.4721688611638));
#17180=CARTESIAN_POINT('Ctrl Pts',(-0.0664856944397882,-0.140626153531635,
1.47213264985675));
#17181=CARTESIAN_POINT('Ctrl Pts',(-0.06736435848372,-0.140207205428986,
1.47206338710323));
#17182=CARTESIAN_POINT('Ctrl Pts',(-0.0677817556138718,-0.140005895752607,
1.47203034968942));
#17183=CARTESIAN_POINT('Ctrl Pts',(-0.0687350800936344,-0.139540847206908,
1.47195457964884));
#17184=CARTESIAN_POINT('Ctrl Pts',(-0.0692703974540884,-0.139275881949594,
1.47191180472571));
#17185=CARTESIAN_POINT('Ctrl Pts',(-0.070664977048832,-0.138575579961187,
1.47179976469628));
#17186=CARTESIAN_POINT('Ctrl Pts',(-0.0715217332533905,-0.138135339206531,
1.47173032896428));
#17187=CARTESIAN_POINT('Ctrl Pts',(-0.0774278834447004,-0.135030811581515,
1.47124738770725));
#17188=CARTESIAN_POINT('Ctrl Pts',(-0.0823306923332227,-0.132098595536396,
1.47082444168715));
#17189=CARTESIAN_POINT('Ctrl Pts',(-0.0991899908242285,-0.120711951329825,
1.46928763740646));
#17190=CARTESIAN_POINT('Ctrl Pts',(-0.11010048399853,-0.11085050504113,
1.4681273943134));
#17191=CARTESIAN_POINT('Ctrl Pts',(-0.121199325080069,-0.0975387340276034,
1.46682219980044));
#17192=CARTESIAN_POINT('Ctrl Pts',(-0.122872931636337,-0.0954218324286447,
1.46662151448217));
#17193=CARTESIAN_POINT('Ctrl Pts',(-0.124817856587308,-0.0928256582437247,
1.46638450832105));
#17194=CARTESIAN_POINT('Ctrl Pts',(-0.125142670933285,-0.0923872939699318,
1.46634479387056));
#17195=CARTESIAN_POINT('Ctrl Pts',(-0.125643695949999,-0.0917036279220294,
1.46628333782497));
#17196=CARTESIAN_POINT('Ctrl Pts',(-0.125821505572221,-0.091459512604308,
1.46626148852585));
#17197=CARTESIAN_POINT('Ctrl Pts',(-0.126149710211356,-0.0910061509644667,
1.46622108829661));
#17198=CARTESIAN_POINT('Ctrl Pts',(-0.126300294845668,-0.0907970507429409,
1.46620252465993));
#17199=CARTESIAN_POINT('Ctrl Pts',(-0.12663913666572,-0.0903240645472233,
1.46616069005108));
#17200=CARTESIAN_POINT('Ctrl Pts',(-0.126827088619721,-0.0900599642971817,
1.46613744012514));
#17201=CARTESIAN_POINT('Ctrl Pts',(-0.127378104741062,-0.0892805593620771,
1.46606914007957));
#17202=CARTESIAN_POINT('Ctrl Pts',(-0.127738869693975,-0.0887636246050923,
1.46602424349131));
#17203=CARTESIAN_POINT('Ctrl Pts',(-0.130279831990909,-0.085075141410753,
1.46570663186922));
#17204=CARTESIAN_POINT('Ctrl Pts',(-0.132345033404127,-0.0818255017189523,
1.46544110840641));
#17205=CARTESIAN_POINT('Ctrl Pts',(-0.140580248884761,-0.0677381545590202,
1.4643341473842));
#17206=CARTESIAN_POINT('Ctrl Pts',(-0.145556096661793,-0.0562559756689722,
1.46353523306249));
#17207=CARTESIAN_POINT('Ctrl Pts',(-0.15081424120074,-0.038558615019287,
1.4623005878519));
#17208=CARTESIAN_POINT('Ctrl Pts',(-0.152187254146884,-0.032721983969422,
1.46189353868082));
#17209=CARTESIAN_POINT('Ctrl Pts',(-0.153467820857172,-0.0254065550269558,
1.46137537860276));
#17210=CARTESIAN_POINT('Ctrl Pts',(-0.153695845333057,-0.0239885798235002,
1.46127459126849));
#17211=CARTESIAN_POINT('Ctrl Pts',(-0.153995958444428,-0.021941907579324,
1.46112852548002));
#17212=CARTESIAN_POINT('Ctrl Pts',(-0.154083901223177,-0.0213155785265165,
1.46108374660701));
#17213=CARTESIAN_POINT('Ctrl Pts',(-0.154230354402046,-0.0202242410176655,
1.46100557647946));
#17214=CARTESIAN_POINT('Ctrl Pts',(-0.154290587972173,-0.0197594685689641,
1.46097223988432));
#17215=CARTESIAN_POINT('Ctrl Pts',(-0.154402771545967,-0.0188620393145703,
1.46090777839004));
#17216=CARTESIAN_POINT('Ctrl Pts',(-0.154455005714666,-0.0184294218775842,
1.46087666276279));
#17217=CARTESIAN_POINT('Ctrl Pts',(-0.154587937220006,-0.0172881705170024,
1.46079446762885));
#17218=CARTESIAN_POINT('Ctrl Pts',(-0.154665578990884,-0.0165791983449027,
1.46074329267338));
#17219=CARTESIAN_POINT('Ctrl Pts',(-0.154921716261145,-0.0140817228979077,
1.46056260428469));
#17220=CARTESIAN_POINT('Ctrl Pts',(-0.155074079500373,-0.0122907466228192,
1.46043227807444));
#17221=CARTESIAN_POINT('Ctrl Pts',(-0.155223278801377,-0.010085000523286,
1.46027077696939));
#17222=CARTESIAN_POINT('Ctrl Pts',(-0.155249541780747,-0.00967229487752725,
1.46024051678374));
#17223=CARTESIAN_POINT('Ctrl Pts',(-0.155361757049497,-0.00779053619728491,
1.46010234740602));
#17224=CARTESIAN_POINT('Ctrl Pts',(-0.155428503039985,-0.00632045743794215,
1.45999386036422));
#17225=CARTESIAN_POINT('Ctrl Pts',(-0.155525890911946,-0.00319834126535703,
1.45976227499357));
#17226=CARTESIAN_POINT('Ctrl Pts',(-0.155551086954946,-0.00154632552727123,
1.4596390326755));
#17227=CARTESIAN_POINT('Ctrl Pts',(-0.155542083644713,0.0116999912811569,
1.45864523099621));
#17228=CARTESIAN_POINT('Ctrl Pts',(-0.154237875836441,0.0232559469567256,
1.45773979922087));
#17229=CARTESIAN_POINT('Ctrl Pts',(-0.150213724972465,0.040916709570916,
1.45634155928028));
#17230=CARTESIAN_POINT('Ctrl Pts',(-0.148366021733034,0.0471793087978687,
1.45584369951952));
#17231=CARTESIAN_POINT('Ctrl Pts',(-0.145890113147153,0.0539663629180312,
1.45531407205644));
#17232=CARTESIAN_POINT('Ctrl Pts',(-0.145645536924261,0.0546229902568069,
1.45526294065231));
#17233=CARTESIAN_POINT('Ctrl Pts',(-0.145277840313227,0.0555901354045607,
1.455187812813));
#17234=CARTESIAN_POINT('Ctrl Pts',(-0.145158148106829,0.0559019327416983,
1.45516362070176));
#17235=CARTESIAN_POINT('Ctrl Pts',(-0.144944021864038,0.0564544051812521,
1.45512080809518));
#17236=CARTESIAN_POINT('Ctrl Pts',(-0.144849991295519,0.0566952322871937,
1.45510216390611));
#17237=CARTESIAN_POINT('Ctrl Pts',(-0.144647309738644,0.0572105359484672,
1.45506231005985));
#17238=CARTESIAN_POINT('Ctrl Pts',(-0.144538477997265,0.0574849373343044,
1.45504111147077));
#17239=CARTESIAN_POINT('Ctrl Pts',(-0.144237821837179,0.0582367406029928,
1.4549830924919));
#17240=CARTESIAN_POINT('Ctrl Pts',(-0.144044406595513,0.0587135091183309,
1.45494636619012));
#17241=CARTESIAN_POINT('Ctrl Pts',(-0.143003457963293,0.0612433411001956,
1.45475180234469));
#17242=CARTESIAN_POINT('Ctrl Pts',(-0.142114333570494,0.0632791702539503,
1.45459633170291));
#17243=CARTESIAN_POINT('Ctrl Pts',(-0.135277085610954,0.0780626828194668,
1.45347045437207));
#17244=CARTESIAN_POINT('Ctrl Pts',(-0.127667147193817,0.0899715609165035,
1.45257557106974));
#17245=CARTESIAN_POINT('Ctrl Pts',(-0.11419699211101,0.105831201253436,
1.45118584178815));
#17246=CARTESIAN_POINT('Ctrl Pts',(-0.109506996859866,0.110676982970521,
1.45072806844399));
#17247=CARTESIAN_POINT('Ctrl Pts',(-0.103777032265685,0.115875499728354,
1.4501860377342));
#17248=CARTESIAN_POINT('Ctrl Pts',(-0.103029454382375,0.116540702374766,
1.45011564141425));
#17249=CARTESIAN_POINT('Ctrl Pts',(-0.101821985733292,0.117594421930672,
1.45000241749149));
#17250=CARTESIAN_POINT('Ctrl Pts',(-0.101366158168923,0.117987570563655,
1.44995978193925));
#17251=CARTESIAN_POINT('Ctrl Pts',(-0.100553828062199,0.118680018648249,
1.4498839835271));
#17252=CARTESIAN_POINT('Ctrl Pts',(-0.100198240235437,0.118980384137098,
1.44985086488177));
#17253=CARTESIAN_POINT('Ctrl Pts',(-0.0994556460677442,0.119601964515796,
1.44978182480859));
#17254=CARTESIAN_POINT('Ctrl Pts',(-0.0990684198671205,0.119922907006395,
1.44974589284215));
#17255=CARTESIAN_POINT('Ctrl Pts',(-0.0980612124555313,0.120749497582212,
1.4496526040471));
#17256=CARTESIAN_POINT('Ctrl Pts',(-0.0974388813301696,0.121252244990941,
1.44959513143233));
#17257=CARTESIAN_POINT('Ctrl Pts',(-0.0947438296693985,0.123395283276602,
1.44934693393863));
#17258=CARTESIAN_POINT('Ctrl Pts',(-0.0926334784519948,0.124987304443538,
1.44915431749672));
#17259=CARTESIAN_POINT('Ctrl Pts',(-0.0869504457183114,0.12905150589219,
1.44863971489913));
#17260=CARTESIAN_POINT('Ctrl Pts',(-0.0833132171826555,0.131428964260243,
1.44831442098161));
#17261=CARTESIAN_POINT('Ctrl Pts',(-0.0744421641491966,0.136711174792291,
1.44753079664743));
#17262=CARTESIAN_POINT('Ctrl Pts',(-0.0691354132859616,0.13946949740905,
1.44706948227971));
#17263=CARTESIAN_POINT('Ctrl Pts',(-0.0636885593981421,0.141913952456372,
1.4466066640002));
#17264=CARTESIAN_POINT('',(-0.155550023928855,6.62725240224652E-5,1.44572602062627));
#17265=CARTESIAN_POINT('Ctrl Pts',(-0.0636886279094242,0.141913921709658,
1.43290478746296));
#17266=CARTESIAN_POINT('Ctrl Pts',(-0.0668602430864753,0.140490553117982,
1.43316879602027));
#17267=CARTESIAN_POINT('Ctrl Pts',(-0.0699841163588671,0.138960872955427,
1.43342939107116));
#17268=CARTESIAN_POINT('Ctrl Pts',(-0.0736672353627304,0.137001540179662,
1.43373518284804));
#17269=CARTESIAN_POINT('Ctrl Pts',(-0.0742774077252028,0.136671688098216,
1.43378579276417));
#17270=CARTESIAN_POINT('Ctrl Pts',(-0.0751768316905237,0.136177667246265,
1.43386029807908));
#17271=CARTESIAN_POINT('Ctrl Pts',(-0.0754677845091119,0.136016640844285,
1.43388438465061));
#17272=CARTESIAN_POINT('Ctrl Pts',(-0.0759774083613463,0.13573245338047,
1.43392654462472));
#17273=CARTESIAN_POINT('Ctrl Pts',(-0.0761962995396099,0.135609695162602,
1.43394464331935));
#17274=CARTESIAN_POINT('Ctrl Pts',(-0.0764155917042016,0.135486013466821,
1.43396276517435));
#17275=CARTESIAN_POINT('Ctrl Pts',(-0.0764162857534264,0.13548562201319,
1.43396282252904));
#17276=CARTESIAN_POINT('Ctrl Pts',(-0.0764176762548998,0.135484837736335,
1.43396293743684));
#17277=CARTESIAN_POINT('Ctrl Pts',(-0.0764183686206453,0.135484447218061,
1.43396299465224));
#17278=CARTESIAN_POINT('Ctrl Pts',(-0.0764197434379997,0.135483671759706,
1.43396310826356));
#17279=CARTESIAN_POINT('Ctrl Pts',(-0.0764204300266164,0.135483284486199,
1.43396316500135));
#17280=CARTESIAN_POINT('Ctrl Pts',(-0.0764217988286091,0.135482512393346,
1.43396327811519));
#17281=CARTESIAN_POINT('Ctrl Pts',(-0.0764224810472205,0.135482127571133,
1.43396333449167));
#17282=CARTESIAN_POINT('Ctrl Pts',(-0.076423841161059,0.135481360351876,
1.43396344688716));
#17283=CARTESIAN_POINT('Ctrl Pts',(-0.0764245190480729,0.135480977959552,
1.4339635029055));
#17284=CARTESIAN_POINT('Ctrl Pts',(-0.0764258705221563,0.135480215587106,
1.43396361458666));
#17285=CARTESIAN_POINT('Ctrl Pts',(-0.0764265441094105,0.135479835606966,
1.4339636702495));
#17286=CARTESIAN_POINT('Ctrl Pts',(-0.0764278869939382,0.135479078053522,
1.43396378122048));
#17287=CARTESIAN_POINT('Ctrl Pts',(-0.0764285563026247,0.135478700473864,
1.43396383652957));
#17288=CARTESIAN_POINT('Ctrl Pts',(-0.076429890685956,0.13547794769008,
1.43396394679769));
#17289=CARTESIAN_POINT('Ctrl Pts',(-0.0764305557548401,0.135477572489285,
1.43396400175623));
#17290=CARTESIAN_POINT('Ctrl Pts',(-0.0764318816780812,0.135476824452463,
1.43396411132488));
#17291=CARTESIAN_POINT('Ctrl Pts',(-0.0764325425344626,0.135476451615376,
1.43396416593515));
#17292=CARTESIAN_POINT('Ctrl Pts',(-0.0764338600625909,0.135475708289349,
1.4339642748097));
#17293=CARTESIAN_POINT('Ctrl Pts',(-0.0764345167354105,0.135475337799884,
1.43396432907408));
#17294=CARTESIAN_POINT('Ctrl Pts',(-0.076686958807072,0.135332909616235,
1.43398518967622));
#17295=CARTESIAN_POINT('Ctrl Pts',(-0.0769383504848944,0.135190148696767,
1.43400595061829));
#17296=CARTESIAN_POINT('Ctrl Pts',(-0.077622914201455,0.134798869008774,
1.43406245367472));
#17297=CARTESIAN_POINT('Ctrl Pts',(-0.0780552949481778,0.134548960769233,
1.43409810790209));
#17298=CARTESIAN_POINT('Ctrl Pts',(-0.0790162257184926,0.133987369047628,
1.43417728809716));
#17299=CARTESIAN_POINT('Ctrl Pts',(-0.0795441536008456,0.133674629795657,
1.43422074941251));
#17300=CARTESIAN_POINT('Ctrl Pts',(-0.0811578847840455,0.13270572594395,
1.43435352128418));
#17301=CARTESIAN_POINT('Ctrl Pts',(-0.0822375542790302,0.132039376247014,
1.43444224421883));
#17302=CARTESIAN_POINT('Ctrl Pts',(-0.0863188856540324,0.129450978327353,
1.43477770445624));
#17303=CARTESIAN_POINT('Ctrl Pts',(-0.0892625256301097,0.127439049537694,
1.43501981488321));
#17304=CARTESIAN_POINT('Ctrl Pts',(-0.103965632118176,0.116630052961153,
1.43624418362759));
#17305=CARTESIAN_POINT('Ctrl Pts',(-0.114505203178463,0.106301487881652,
1.43718053136615));
#17306=CARTESIAN_POINT('Ctrl Pts',(-0.124394528177384,0.0934037576710502,
1.43829306053358));
#17307=CARTESIAN_POINT('Ctrl Pts',(-0.12532961566483,0.0921452535014083,
1.43840100210623));
#17308=CARTESIAN_POINT('Ctrl Pts',(-0.126512023532436,0.0905025886058208,
1.43854124387494));
#17309=CARTESIAN_POINT('Ctrl Pts',(-0.126776919984283,0.0901311444205592,
1.43857291352931));
#17310=CARTESIAN_POINT('Ctrl Pts',(-0.128009439705179,0.0883866918441236,
1.43872146083014));
#17311=CARTESIAN_POINT('Ctrl Pts',(-0.128956384159158,0.0869992790175068,
1.43883906885174));
#17312=CARTESIAN_POINT('Ctrl Pts',(-0.130262094986369,0.0850180546590946,
1.43900640773484));
#17313=CARTESIAN_POINT('Ctrl Pts',(-0.130639666580749,0.0844367248055172,
1.43905543577075));
#17314=CARTESIAN_POINT('Ctrl Pts',(-0.131246189784394,0.0834890816321818,
1.4391352505341));
#17315=CARTESIAN_POINT('Ctrl Pts',(-0.131477526430731,0.083124299224057,
1.43916594857187));
#17316=CARTESIAN_POINT('Ctrl Pts',(-0.131958058826364,0.0823595488234174,
1.43923025511968));
#17317=CARTESIAN_POINT('Ctrl Pts',(-0.132206961996207,0.0819594031357007,
1.43926387398682));
#17318=CARTESIAN_POINT('Ctrl Pts',(-0.132793794704565,0.0810063607224184,
1.43934388116802));
#17319=CARTESIAN_POINT('Ctrl Pts',(-0.133130092845252,0.0804524750707311,
1.43939032851898));
#17320=CARTESIAN_POINT('Ctrl Pts',(-0.13424671203123,0.0785872215250863,
1.43954658591223));
#17321=CARTESIAN_POINT('Ctrl Pts',(-0.135011172449007,0.0772665133395266,
1.43965696656311));
#17322=CARTESIAN_POINT('Ctrl Pts',(-0.139031529309008,0.0700789303461437,
1.44025650117011));
#17323=CARTESIAN_POINT('Ctrl Pts',(-0.141924196325721,0.0640181319700254,
1.44075830936803));
#17324=CARTESIAN_POINT('Ctrl Pts',(-0.149173224157554,0.0459030258503039,
1.44224662345396));
#17325=CARTESIAN_POINT('Ctrl Pts',(-0.152443922324118,0.0334748473956542,
1.44325749513671));
#17326=CARTESIAN_POINT('Ctrl Pts',(-0.154402401088823,0.0189508145755707,
1.44436240359479));
#17327=CARTESIAN_POINT('Ctrl Pts',(-0.154617171674818,0.0171103998377668,
1.44450093548808));
#17328=CARTESIAN_POINT('Ctrl Pts',(-0.154916380755177,0.014076482955724,
1.44472643444083));
#17329=CARTESIAN_POINT('Ctrl Pts',(-0.155020019995029,0.0128851090380782,
1.4448142589062));
#17330=CARTESIAN_POINT('Ctrl Pts',(-0.155142071079203,0.0112660237619248,
1.44493252516681));
#17331=CARTESIAN_POINT('Ctrl Pts',(-0.155172468910344,0.0108392995238594,
1.44496359283506));
#17332=CARTESIAN_POINT('Ctrl Pts',(-0.155217733881369,0.0101646096483685,
1.4450125461272));
#17333=CARTESIAN_POINT('Ctrl Pts',(-0.155233767880125,0.00991672893084847,
1.44503049582247));
#17334=CARTESIAN_POINT('Ctrl Pts',(-0.155264598648404,0.00942168837145768,
1.44506627029735));
#17335=CARTESIAN_POINT('Ctrl Pts',(-0.155279398888671,0.00917453470046273,
1.44508409464911));
#17336=CARTESIAN_POINT('Ctrl Pts',(-0.15530832920788,0.00867128370831169,
1.44512031583044));
#17337=CARTESIAN_POINT('Ctrl Pts',(-0.155322416004253,0.00841518696559419,
1.44513871007935));
#17338=CARTESIAN_POINT('Ctrl Pts',(-0.155353676275033,0.00782003937749486,
1.44518137060307));
#17339=CARTESIAN_POINT('Ctrl Pts',(-0.155370373447767,0.00748096307339606,
1.4452056108182));
#17340=CARTESIAN_POINT('Ctrl Pts',(-0.155426861121103,0.00625195164849051,
1.44529324507949));
#17341=CARTESIAN_POINT('Ctrl Pts',(-0.155460117764408,0.00536171048518981,
1.44535629318325));
#17342=CARTESIAN_POINT('Ctrl Pts',(-0.155527938024698,0.00300326776435513,
1.44552230000122));
#17343=CARTESIAN_POINT('Ctrl Pts',(-0.155549361931428,0.00153474931081583,
1.44562461906036));
#17344=CARTESIAN_POINT('Ctrl Pts',(-0.155549985958724,6.60926688657478E-5,
1.44572609898142));
#17345=CARTESIAN_POINT('Ctrl Pts',(-0.155549985880275,6.62770408882546E-5,
1.44572608624184));
#17346=CARTESIAN_POINT('Ctrl Pts',(-0.155555884261965,-0.0137770264064439,
1.44668261909254));
#17347=CARTESIAN_POINT('Ctrl Pts',(-0.153713842315672,-0.0275617844757425,
1.44756441268068));
#17348=CARTESIAN_POINT('Ctrl Pts',(-0.148397421963137,-0.0470578811843007,
1.44891276289187));
#17349=CARTESIAN_POINT('Ctrl Pts',(-0.146350050898578,-0.0530837628227759,
1.44934377173934));
#17350=CARTESIAN_POINT('Ctrl Pts',(-0.143377844087416,-0.060338998466371,
1.44989049754077));
#17351=CARTESIAN_POINT('Ctrl Pts',(-0.142796199559207,-0.0617028851532562,
1.44999451141723));
#17352=CARTESIAN_POINT('Ctrl Pts',(-0.141935498362046,-0.0636437513946578,
1.45014440564446));
#17353=CARTESIAN_POINT('Ctrl Pts',(-0.141672221417332,-0.0642276766150209,
1.45018974871774));
#17354=CARTESIAN_POINT('Ctrl Pts',(-0.141209554897716,-0.0652371438245133,
1.45026857212844));
#17355=CARTESIAN_POINT('Ctrl Pts',(-0.141011827971094,-0.0656634425854908,
1.45030199507685));
#17356=CARTESIAN_POINT('Ctrl Pts',(-0.140627943276303,-0.0664813665042139,
1.45036638728402));
#17357=CARTESIAN_POINT('Ctrl Pts',(-0.140442073405624,-0.0668731226495726,
1.45039734635409));
#17358=CARTESIAN_POINT('Ctrl Pts',(-0.139950906342907,-0.0678972712266717,
1.45047859273995));
#17359=CARTESIAN_POINT('Ctrl Pts',(-0.139642963495729,-0.0685283761837179,
1.45052897140022));
#17360=CARTESIAN_POINT('Ctrl Pts',(-0.138559903887194,-0.0707104072854445,
1.45070425874791));
#17361=CARTESIAN_POINT('Ctrl Pts',(-0.137763163170063,-0.0722503915897387,
1.45082991799839));
#17362=CARTESIAN_POINT('Ctrl Pts',(-0.131276622364889,-0.0842904099810718,
1.45182826473611));
#17363=CARTESIAN_POINT('Ctrl Pts',(-0.12442160425429,-0.0941146757048641,
1.45274409610553));
#17364=CARTESIAN_POINT('Ctrl Pts',(-0.113115782874773,-0.106896722346074,
1.45406740405386));
#17365=CARTESIAN_POINT('Ctrl Pts',(-0.109531027348519,-0.110566935091132,
1.45446532660342));
#17366=CARTESIAN_POINT('Ctrl Pts',(-0.103385019780831,-0.116266647129765,
1.4551069970546));
#17367=CARTESIAN_POINT('Ctrl Pts',(-0.100929530532689,-0.118404512394445,
1.45535379310498));
#17368=CARTESIAN_POINT('Ctrl Pts',(-0.097484762347844,-0.121218590306139,
1.45568540759061));
#17369=CARTESIAN_POINT('Ctrl Pts',(-0.0965522433164416,-0.121962658432099,
1.4557737769378));
#17370=CARTESIAN_POINT('Ctrl Pts',(-0.0951481141398284,-0.123056830682451,
1.45590465629463));
#17371=CARTESIAN_POINT('Ctrl Pts',(-0.0946829572533972,-0.123415091606327,
1.45594766276057));
#17372=CARTESIAN_POINT('Ctrl Pts',(-0.0938365513568218,-0.124059386055306,
1.45602526836916));
#17373=CARTESIAN_POINT('Ctrl Pts',(-0.0934559977689739,-0.124346315329659,
1.45605992551397));
#17374=CARTESIAN_POINT('Ctrl Pts',(-0.0928439463858557,-0.124803391980281,
1.45611528167249));
#17375=CARTESIAN_POINT('Ctrl Pts',(-0.0926132897209681,-0.124974651833897,
1.45613605645235));
#17376=CARTESIAN_POINT('Ctrl Pts',(-0.0921805918670213,-0.125294069100675,
1.45617486475617));
#17377=CARTESIAN_POINT('Ctrl Pts',(-0.0919786696687933,-0.125442375599448,
1.45619290828136));
#17378=CARTESIAN_POINT('Ctrl Pts',(-0.0915079832365281,-0.125786334765552,
1.45623481462039));
#17379=CARTESIAN_POINT('Ctrl Pts',(-0.0912389495831145,-0.125981614112253,
1.45625865150709));
#17380=CARTESIAN_POINT('Ctrl Pts',(-0.0904071059761214,-0.126581349418227,
1.45633200507005));
#17381=CARTESIAN_POINT('Ctrl Pts',(-0.0898422067906105,-0.12698291522245,
1.45638132790259));
#17382=CARTESIAN_POINT('Ctrl Pts',(-0.0844731044489688,-0.130745844846642,
1.45684569309584));
#17383=CARTESIAN_POINT('Ctrl Pts',(-0.0794844516205588,-0.133837298701754,
1.45724389397698));
#17384=CARTESIAN_POINT('Ctrl Pts',(-0.0654955047627734,-0.141447317290972,
1.45830716768045));
#17385=CARTESIAN_POINT('Ctrl Pts',(-0.0562129904523487,-0.145386087761141,
1.45895811863497));
#17386=CARTESIAN_POINT('Ctrl Pts',(-0.0406558060572818,-0.150272828303824,
1.46004689625182));
#17387=CARTESIAN_POINT('Ctrl Pts',(-0.0345900401560761,-0.151783831623902,
1.46047056160612));
#17388=CARTESIAN_POINT('Ctrl Pts',(-0.0270066512672671,-0.153194646851783,
1.46100852701119));
#17389=CARTESIAN_POINT('Ctrl Pts',(-0.0255592221090781,-0.153442774163672,
1.46111155734078));
#17390=CARTESIAN_POINT('Ctrl Pts',(-0.0234781893404814,-0.153769256504804,
1.46126028305847));
#17391=CARTESIAN_POINT('Ctrl Pts',(-0.0228472455114183,-0.153864268013597,
1.46130545278962));
#17392=CARTESIAN_POINT('Ctrl Pts',(-0.0217510617368836,-0.154022447190428,
1.46138407249907));
#17393=CARTESIAN_POINT('Ctrl Pts',(-0.0212860836033319,-0.154087395854437,
1.46141746591925));
#17394=CARTESIAN_POINT('Ctrl Pts',(-0.0203905331982704,-0.154208356398516,
1.46148187083243));
#17395=CARTESIAN_POINT('Ctrl Pts',(-0.0199600058174525,-0.154264672520849,
1.46151287240982));
#17396=CARTESIAN_POINT('Ctrl Pts',(-0.018829467076732,-0.154407743366576,
1.46159438755667));
#17397=CARTESIAN_POINT('Ctrl Pts',(-0.0181290984750088,-0.154491539574334,
1.46164499364392));
#17398=CARTESIAN_POINT('Ctrl Pts',(-0.0156868821653269,-0.15476690520148,
1.46182184974499));
#17399=CARTESIAN_POINT('Ctrl Pts',(-0.0139424454136736,-0.154933795431414,
1.46194886823718));
#17400=CARTESIAN_POINT('Ctrl Pts',(-0.000967069848389774,-0.155954248321953,
1.46289918150943));
#17401=CARTESIAN_POINT('Ctrl Pts',(0.0103218826449606,-0.155614979710487,
1.46376039466813));
#17402=CARTESIAN_POINT('Ctrl Pts',(0.0309491545747352,-0.15273996312124,
1.46537464278981));
#17403=CARTESIAN_POINT('Ctrl Pts',(0.0402842533858207,-0.150547538675237,
1.46612008562082));
#17404=CARTESIAN_POINT('Ctrl Pts',(0.0502202307510351,-0.147222807003356,
1.46689662719046));
#17405=CARTESIAN_POINT('Ctrl Pts',(0.0510785382727514,-0.146927225203477,
1.46696355276793));
#17406=CARTESIAN_POINT('Ctrl Pts',(0.0523896146094526,-0.146462842278603,
1.46706549354239));
#17407=CARTESIAN_POINT('Ctrl Pts',(0.0528442487279792,-0.146299423374875,
1.46710078934916));
#17408=CARTESIAN_POINT('Ctrl Pts',(0.0535929688179008,-0.146026349307755,
1.46715881978337));
#17409=CARTESIAN_POINT('Ctrl Pts',(0.0538874930350643,-0.145917919043164,
1.46718162239263));
#17410=CARTESIAN_POINT('Ctrl Pts',(0.0544604445138456,-0.145705013354702,
1.46722593019383));
#17411=CARTESIAN_POINT('Ctrl Pts',(0.0547389041125046,-0.145600629510848,
1.46724744057498));
#17412=CARTESIAN_POINT('Ctrl Pts',(0.0552514994867895,-0.145406798747639,
1.46728699164855));
#17413=CARTESIAN_POINT('Ctrl Pts',(0.0554857159518271,-0.145317585461868,
1.46730504551919));
#17414=CARTESIAN_POINT('Ctrl Pts',(0.0560241661246784,-0.145110997655194,
1.46734651011147));
#17415=CARTESIAN_POINT('Ctrl Pts',(0.0563282466725011,-0.144993232471512,
1.46736989717426));
#17416=CARTESIAN_POINT('Ctrl Pts',(0.0572475793965496,-0.144633862058948,
1.46744052137001));
#17417=CARTESIAN_POINT('Ctrl Pts',(0.0578616749148832,-0.144389286370534,
1.4674875849479));
#17418=CARTESIAN_POINT('Ctrl Pts',(0.062588994771145,-0.142471534521782,
1.46784915550281));
#17419=CARTESIAN_POINT('Ctrl Pts',(0.0666309110330868,-0.140626638159003,
1.46815406336401));
#17420=CARTESIAN_POINT('Ctrl Pts',(0.0837838346528959,-0.131891377797621,
1.46945286882374));
#17421=CARTESIAN_POINT('Ctrl Pts',(0.0959518789394761,-0.123322145138005,
1.47039437582479));
#17422=CARTESIAN_POINT('Ctrl Pts',(0.109549190329018,-0.110498160018304,
1.47166801489904));
#17423=CARTESIAN_POINT('Ctrl Pts',(0.112272044791458,-0.107730460295084,
1.47193614076816));
#17424=CARTESIAN_POINT('Ctrl Pts',(0.115501431708237,-0.104192364136783,
1.47227272693303));
#17425=CARTESIAN_POINT('Ctrl Pts',(0.116108576133004,-0.103515351309303,
1.47233686470461));
#17426=CARTESIAN_POINT('Ctrl Pts',(0.117058159788745,-0.102437627347766,
1.4724385673571));
#17427=CARTESIAN_POINT('Ctrl Pts',(0.117404565578478,-0.10204042453194,
1.47247596677038));
#17428=CARTESIAN_POINT('Ctrl Pts',(0.118049777825564,-0.10129296331252,
1.47254619378121));
#17429=CARTESIAN_POINT('Ctrl Pts',(0.118349061666832,-0.100943122873771,
1.47257900119857));
#17430=CARTESIAN_POINT('Ctrl Pts',(0.119014770133553,-0.100157929230913,
1.47265250167308));
#17431=CARTESIAN_POINT('Ctrl Pts',(0.119380366170484,-0.0997218855360148,
1.47269322796467));
#17432=CARTESIAN_POINT('Ctrl Pts',(0.120299497932282,-0.0986133456734842,
1.47279654268661));
#17433=CARTESIAN_POINT('Ctrl Pts',(0.120849786575204,-0.097938195690126,
1.47285926102369));
#17434=CARTESIAN_POINT('Ctrl Pts',(0.123931884101641,-0.0940912375239001,
1.47321551952547));
#17435=CARTESIAN_POINT('Ctrl Pts',(0.12634423975266,-0.0908262092641361,
1.47351373311157));
#17436=CARTESIAN_POINT('Ctrl Pts',(0.129677174229151,-0.0859251260479744,
1.47395599148305));
#17437=CARTESIAN_POINT('Ctrl Pts',(0.130700358120536,-0.0843606110481342,
1.47409639616372));
#17438=CARTESIAN_POINT('Ctrl Pts',(0.139530188385669,-0.0703128715222547,
1.47535011854989));
#17439=CARTESIAN_POINT('Ctrl Pts',(0.145554817728985,-0.0568004479896118,
1.47651773171049));
#17440=CARTESIAN_POINT('Ctrl Pts',(0.150297799419483,-0.0401625635120625,
1.47781904721061));
#17441=CARTESIAN_POINT('Ctrl Pts',(0.150943372028449,-0.037663783351134,
1.47801080598762));
#17442=CARTESIAN_POINT('Ctrl Pts',(0.151648188697762,-0.0346254135198081,
1.4782386517208));
#17443=CARTESIAN_POINT('Ctrl Pts',(0.151767134934008,-0.0341002811383624,
1.47827784040259));
#17444=CARTESIAN_POINT('Ctrl Pts',(0.151948190899554,-0.0332812261503539,
1.4783386556423));
#17445=CARTESIAN_POINT('Ctrl Pts',(0.152012178402532,-0.0329877303434083,
1.47836038643159));
#17446=CARTESIAN_POINT('Ctrl Pts',(0.152129488893868,-0.0324420643481126,
1.47840067185755));
#17447=CARTESIAN_POINT('Ctrl Pts',(0.152183034803574,-0.0321899495197964,
1.47841923864801));
#17448=CARTESIAN_POINT('Ctrl Pts',(0.152302902619557,-0.0316185810926165,
1.47846121270219));
#17449=CARTESIAN_POINT('Ctrl Pts',(0.152368847373672,-0.0312992519392227,
1.47848459826537));
#17450=CARTESIAN_POINT('Ctrl Pts',(0.152565410643715,-0.0303320743832381,
1.47855521345657));
#17451=CARTESIAN_POINT('Ctrl Pts',(0.152692907338625,-0.0296835872399399,
1.4786022695946));
#17452=CARTESIAN_POINT('Ctrl Pts',(0.153646851598111,-0.0246626897207158,
1.47896449404554));
#17453=CARTESIAN_POINT('Ctrl Pts',(0.154289562871379,-0.0202569336694151,
1.4792700215471));
#17454=CARTESIAN_POINT('Ctrl Pts',(0.156250945074814,-0.00108291402047901,
1.48057041607453));
#17455=CARTESIAN_POINT('Ctrl Pts',(0.155643980696658,0.0138032492495018,
1.48151289734109));
#17456=CARTESIAN_POINT('Ctrl Pts',(0.152235093389752,0.032174147735988,
1.48278634181575));
#17457=CARTESIAN_POINT('Ctrl Pts',(0.151389978387864,0.0359411964516643,
1.48305299247909));
#17458=CARTESIAN_POINT('Ctrl Pts',(0.15017419118367,0.0405504488736418,
1.4833879420295));
#17459=CARTESIAN_POINT('Ctrl Pts',(0.149934983553131,0.0414261661999468,
1.48345196957891));
#17460=CARTESIAN_POINT('Ctrl Pts',(0.149544902348627,0.0428065659085886,
1.4835535369468));
#17461=CARTESIAN_POINT('Ctrl Pts',(0.149399104157245,0.0433126721404501,
1.48359091204912));
#17462=CARTESIAN_POINT('Ctrl Pts',(0.149121038802963,0.0442598043363893,
1.48366111740284));
#17463=CARTESIAN_POINT('Ctrl Pts',(0.148989377996394,0.0447010036738334,
1.48369392759408));
#17464=CARTESIAN_POINT('Ctrl Pts',(0.148690485271175,0.045686611111643,
1.48376746552164));
#17465=CARTESIAN_POINT('Ctrl Pts',(0.148522219139039,0.0462306959833868,
1.48380822664702));
#17466=CARTESIAN_POINT('Ctrl Pts',(0.148088593398823,0.0476060118109163,
1.48391168857637));
#17467=CARTESIAN_POINT('Ctrl Pts',(0.147819223451407,0.0484359471460012,
1.48397451993311));
#17468=CARTESIAN_POINT('Ctrl Pts',(0.146250907906993,0.0531330056507727,
1.48433242268847));
#17469=CARTESIAN_POINT('Ctrl Pts',(0.14480733046948,0.0569497641838245,
1.48463221769303));
#17470=CARTESIAN_POINT('Ctrl Pts',(0.142493434724198,0.0624087125628709,
1.4850747108299));
#17471=CARTESIAN_POINT('Ctrl Pts',(0.141740995629489,0.064099266948442,
1.4852137061978));
#17472=CARTESIAN_POINT('Ctrl Pts',(0.134726915753676,0.0791305219141532,
1.48646708409862));
#17473=CARTESIAN_POINT('Ctrl Pts',(0.126630198981664,0.0915297580205269,
1.48763587098451));
#17474=CARTESIAN_POINT('Ctrl Pts',(0.115220403714577,0.104530525350124,
1.48893671597374));
#17475=CARTESIAN_POINT('Ctrl Pts',(0.113482210491339,0.106415046599015,
1.48912718000755));
#17476=CARTESIAN_POINT('Ctrl Pts',(0.111324116088501,0.108641761957279,
1.4893536949623));
#17477=CARTESIAN_POINT('Ctrl Pts',(0.110948127501568,0.109025704725514,
1.48939280626932));
#17478=CARTESIAN_POINT('Ctrl Pts',(0.110359031453347,0.109621059885288,
1.48945352779327));
#17479=CARTESIAN_POINT('Ctrl Pts',(0.110147293978273,0.109833811857386,
1.4894752417319));
#17480=CARTESIAN_POINT('Ctrl Pts',(0.109752580500884,0.110228127154517,
1.48951551194084));
#17481=CARTESIAN_POINT('Ctrl Pts',(0.10956977088265,0.110409846721838,1.48953408028221));
#17482=CARTESIAN_POINT('Ctrl Pts',(0.109154462501349,0.110820631372166,
1.48957607826367));
#17483=CARTESIAN_POINT('Ctrl Pts',(0.108921694425129,0.111049419226494,
1.48959948609944));
#17484=CARTESIAN_POINT('Ctrl Pts',(0.108229627143164,0.111725383075129,
1.48966870239664));
#17485=CARTESIAN_POINT('Ctrl Pts',(0.107768274202797,0.11217046192405,1.48971435105897));
#17486=CARTESIAN_POINT('Ctrl Pts',(0.104320196925757,0.115455998311285,
1.49005200372553));
#17487=CARTESIAN_POINT('Ctrl Pts',(0.101224048397197,0.118179907897032,
1.4903357453819));
#17488=CARTESIAN_POINT('Ctrl Pts',(0.0944537116180991,0.123674695446542,
1.49092574789563));
#17489=CARTESIAN_POINT('Ctrl Pts',(0.0907575486910384,0.126412049213838,
1.49123056583958));
#17490=CARTESIAN_POINT('Ctrl Pts',(0.0802684797198167,0.133482627971982,
1.4920651201986));
#17491=CARTESIAN_POINT('Ctrl Pts',(0.0732524561281435,0.137458039535143,
1.4925909880447));
#17492=CARTESIAN_POINT('Ctrl Pts',(0.0622720201376527,0.142599384165511,
1.49340398158541));
#17493=CARTESIAN_POINT('Ctrl Pts',(0.0585175391296592,0.144180727764252,
1.49368018723737));
#17494=CARTESIAN_POINT('Ctrl Pts',(0.0523437859084846,0.146500156571934,
1.49413503204976));
#17495=CARTESIAN_POINT('Ctrl Pts',(0.0499608954449104,0.147329818643918,
1.4943107294488));
#17496=CARTESIAN_POINT('Ctrl Pts',(0.0468101115165871,0.14834161460208,
1.49454371466506));
#17497=CARTESIAN_POINT('Ctrl Pts',(0.0460594253692922,0.148576412854791,
1.49459927262882));
#17498=CARTESIAN_POINT('Ctrl Pts',(0.0448288119657272,0.148951099299118,
1.49469044343985));
#17499=CARTESIAN_POINT('Ctrl Pts',(0.0443499270738089,0.149094387294051,
1.4947259449938));
#17500=CARTESIAN_POINT('Ctrl Pts',(0.0434229252378279,0.149366895820032,
1.49479471568083));
#17501=CARTESIAN_POINT('Ctrl Pts',(0.0429749008280187,0.149496414315641,
1.49482797470186));
#17502=CARTESIAN_POINT('Ctrl Pts',(0.0419410275847551,0.149790263124095,
1.49490477792963));
#17503=CARTESIAN_POINT('Ctrl Pts',(0.0413547867953527,0.149953173728624,
1.49494836764182));
#17504=CARTESIAN_POINT('Ctrl Pts',(0.0397800928699485,0.150380829341477,
1.49506556808322));
#17505=CARTESIAN_POINT('Ctrl Pts',(0.0387899729541331,0.150639262900873,
1.49513938109479));
#17506=CARTESIAN_POINT('Ctrl Pts',(0.0303222044629162,0.152760437628917,
1.49577178373413));
#17507=CARTESIAN_POINT('Ctrl Pts',(0.0227195059877597,0.154074576238643,
1.49634792594783));
#17508=CARTESIAN_POINT('Ctrl Pts',(0.00542278598953225,0.155756192039893,
1.49767623381201));
#17509=CARTESIAN_POINT('Ctrl Pts',(-0.00427251752851013,0.155791935864253,
1.49843351483685));
#17510=CARTESIAN_POINT('Ctrl Pts',(-0.0175733425171971,0.154597954370988,
1.49945914687245));
#17511=CARTESIAN_POINT('Ctrl Pts',(-0.0212267375298337,0.154138832514533,
1.49973922890827));
#17512=CARTESIAN_POINT('Ctrl Pts',(-0.0267871768189891,0.153238566954269,
1.50015998097054));
#17513=CARTESIAN_POINT('Ctrl Pts',(-0.0287077740239233,0.152890404927404,
1.50030428317809));
#17514=CARTESIAN_POINT('Ctrl Pts',(-0.0311050698127636,0.152409056398671,
1.50048270106527));
#17515=CARTESIAN_POINT('Ctrl Pts',(-0.0315882565704743,0.152309644819597,
1.50051857495411));
#17516=CARTESIAN_POINT('Ctrl Pts',(-0.0323551653793269,0.152148053308166,
1.50057536640989));
#17517=CARTESIAN_POINT('Ctrl Pts',(-0.0326391946659658,0.152087375634961,
1.50059636732096));
#17518=CARTESIAN_POINT('Ctrl Pts',(-0.0331765734398989,0.151970999734814,
1.50063603768734));
#17519=CARTESIAN_POINT('Ctrl Pts',(-0.0334299502935069,0.151915464026069,
1.50065471562645));
#17520=CARTESIAN_POINT('Ctrl Pts',(-0.0340113409566138,0.151786508508554,
1.50069751344723));
#17521=CARTESIAN_POINT('Ctrl Pts',(-0.0343392565427413,0.151712659144659,
1.50072160852585));
#17522=CARTESIAN_POINT('Ctrl Pts',(-0.0352141459113909,0.151512644748447,
1.50078578453248));
#17523=CARTESIAN_POINT('Ctrl Pts',(-0.0357606873851245,0.15138457931469,
1.50082575970356));
#17524=CARTESIAN_POINT('Ctrl Pts',(-0.0397181838498521,0.150434631511984,
1.50111446185025));
#17525=CARTESIAN_POINT('Ctrl Pts',(-0.0431014933384724,0.14950043024761,
1.50135719576532));
#17526=CARTESIAN_POINT('Ctrl Pts',(-0.0510483094276349,0.147013879926685,
1.50192396544413));
#17527=CARTESIAN_POINT('Ctrl Pts',(-0.0555770073255496,0.145362352243247,
1.50224429122203));
#17528=CARTESIAN_POINT('Ctrl Pts',(-0.0612512216731276,0.142989040176923,
1.50265055624028));
#17529=CARTESIAN_POINT('Ctrl Pts',(-0.0624735223751187,0.142459241037525,
1.50273836689477));
#17530=CARTESIAN_POINT('Ctrl Pts',(-0.0636886280167373,0.141913921661498,
1.50282608545586));
#17531=CARTESIAN_POINT('Origin',(0.,0.,-0.129405622560373));
#17532=CARTESIAN_POINT('',(-0.0636885910816305,0.141913938237359,1.58655050058549));
#17533=CARTESIAN_POINT('',(-0.0636886258330468,0.141913922641502,1.57264613271722));
#17534=CARTESIAN_POINT('',(-0.0636886258329924,0.141913922641526,-0.129405622560373));
#17535=CARTESIAN_POINT('',(-0.155549955824825,-0.000117230094128791,1.52948519617329));
#17536=CARTESIAN_POINT('Ctrl Pts',(-0.0636885910816225,0.141913938237362,
1.58655050058549));
#17537=CARTESIAN_POINT('Ctrl Pts',(-0.0556566821640682,0.145518524009616,
1.58596898071156));
#17538=CARTESIAN_POINT('Ctrl Pts',(-0.0473230433865961,0.148439344786728,
1.58539453072637));
#17539=CARTESIAN_POINT('Ctrl Pts',(-0.0369753918880226,0.15110286815688,
1.58467671135735));
#17540=CARTESIAN_POINT('Ctrl Pts',(-0.0351674945549438,0.15153383555548,
1.58455118008554));
#17541=CARTESIAN_POINT('Ctrl Pts',(-0.029377214912228,0.152804924617277,
1.58414806595958));
#17542=CARTESIAN_POINT('Ctrl Pts',(-0.0253696890077411,0.1535211375448,
1.5838674194839));
#17543=CARTESIAN_POINT('Ctrl Pts',(-0.020475120461954,0.154199002900961,
1.58352053583815));
#17544=CARTESIAN_POINT('Ctrl Pts',(-0.0196102935714569,0.154311371533294,
1.58345909242817));
#17545=CARTESIAN_POINT('Ctrl Pts',(-0.0181792653722453,0.154485083758022,
1.58335714966645));
#17546=CARTESIAN_POINT('Ctrl Pts',(-0.0176135821246357,0.154550601753242,
1.58331678168058));
#17547=CARTESIAN_POINT('Ctrl Pts',(-0.0165897724954009,0.154663486526208,
1.5832435885002));
#17548=CARTESIAN_POINT('Ctrl Pts',(-0.0161317690197289,0.154711927904163,
1.58321079744361));
#17549=CARTESIAN_POINT('Ctrl Pts',(-0.0151492142706765,0.154811438748106,
1.58314034474764));
#17550=CARTESIAN_POINT('Ctrl Pts',(-0.0146246064298436,0.154861877602033,
1.58310266374686));
#17551=CARTESIAN_POINT('Ctrl Pts',(-0.0131946410138899,0.15499203196548,
1.58299977156646));
#17552=CARTESIAN_POINT('Ctrl Pts',(-0.012288837353915,0.155066479084393,
1.58293439632498));
#17553=CARTESIAN_POINT('Ctrl Pts',(-0.0075212108637616,0.1554162904106,
1.58258920501048));
#17554=CARTESIAN_POINT('Ctrl Pts',(-0.00365108860593273,0.155555316686229,
1.58230517371162));
#17555=CARTESIAN_POINT('Ctrl Pts',(0.0150428509126474,0.155528890487122,
1.58091321801508));
#17556=CARTESIAN_POINT('Ctrl Pts',(0.0297856744671923,0.153389011804456,
1.5797448052151));
#17557=CARTESIAN_POINT('Ctrl Pts',(0.0482562558965439,0.147942019332466,
1.57827325319499));
#17558=CARTESIAN_POINT('Ctrl Pts',(0.0524588000232345,0.146504575755587,
1.57793874454224));
#17559=CARTESIAN_POINT('Ctrl Pts',(0.0572099228700218,0.144648759804374,
1.57756512209116));
#17560=CARTESIAN_POINT('Ctrl Pts',(0.0578237920587437,0.144404460116962,
1.5775169383558));
#17561=CARTESIAN_POINT('Ctrl Pts',(0.058738299094188,0.144033749690548,
1.57744531147985));
#17562=CARTESIAN_POINT('Ctrl Pts',(0.0590401153383496,0.143910297117811,
1.5774216976075));
#17563=CARTESIAN_POINT('Ctrl Pts',(0.0595798627299743,0.143687539217213,
1.57737951631109));
#17564=CARTESIAN_POINT('Ctrl Pts',(0.0598179361593073,0.143588591073243,
1.57736092785211));
#17565=CARTESIAN_POINT('Ctrl Pts',(0.0603330154932123,0.143373010265121,
1.57732074831686));
#17566=CARTESIAN_POINT('Ctrl Pts',(0.0606099289638933,0.143256166869518,
1.57729917025226));
#17567=CARTESIAN_POINT('Ctrl Pts',(0.0613824117816885,0.142927577618771,
1.57723903520187));
#17568=CARTESIAN_POINT('Ctrl Pts',(0.0618772285626696,0.142714055118859,
1.57720058404964));
#17569=CARTESIAN_POINT('Ctrl Pts',(0.0647401251846981,0.141460973749207,
1.57697845592858));
#17570=CARTESIAN_POINT('Ctrl Pts',(0.0670832736254019,0.140364979302545,
1.57679801237641));
#17571=CARTESIAN_POINT('Ctrl Pts',(0.0825731030057564,0.132643131517349,
1.57560708805293));
#17572=CARTESIAN_POINT('Ctrl Pts',(0.094750267783738,0.124237730949311,
1.57467392033339));
#17573=CARTESIAN_POINT('Ctrl Pts',(0.106960209445948,0.112955408353615,
1.57355700766039));
#17574=CARTESIAN_POINT('Ctrl Pts',(0.108331551213944,0.111640876414733,
1.57342867826927));
#17575=CARTESIAN_POINT('Ctrl Pts',(0.11253190951898,0.107464248395496,1.57302573598501));
#17576=CARTESIAN_POINT('Ctrl Pts',(0.115273968044647,0.104517476238519,
1.57274817229802));
#17577=CARTESIAN_POINT('Ctrl Pts',(0.118465297370982,0.100809378217501,
1.57240470942564));
#17578=CARTESIAN_POINT('Ctrl Pts',(0.119026531521166,0.100146104054536,
1.57234349162891));
#17579=CARTESIAN_POINT('Ctrl Pts',(0.119945717366291,0.0990411557789255,
1.57224184598916));
#17580=CARTESIAN_POINT('Ctrl Pts',(0.120306862379425,0.0986021526204787,
1.57220154816511));
#17581=CARTESIAN_POINT('Ctrl Pts',(0.120956183908531,0.0978039678336131,
1.57212843000783));
#17582=CARTESIAN_POINT('Ctrl Pts',(0.121245188648127,0.0974454656258248,
1.57209564348913));
#17583=CARTESIAN_POINT('Ctrl Pts',(0.121861992679752,0.0966733457073927,
1.57202514263034));
#17584=CARTESIAN_POINT('Ctrl Pts',(0.122189286471885,0.0962593335160649,
1.57198740867769));
#17585=CARTESIAN_POINT('Ctrl Pts',(0.12307650856888,0.0951252206334363,
1.5718842241905));
#17586=CARTESIAN_POINT('Ctrl Pts',(0.123632211881265,0.0944018574052578,
1.57181860801666));
#17587=CARTESIAN_POINT('Ctrl Pts',(0.126540837546597,0.0905459440414115,
1.5714698258673));
#17588=CARTESIAN_POINT('Ctrl Pts',(0.128780943135694,0.0873304936325884,
1.57118233946005));
#17589=CARTESIAN_POINT('Ctrl Pts',(0.138887336311401,0.0715881151431334,
1.56978886304873));
#17590=CARTESIAN_POINT('Ctrl Pts',(0.145060854949176,0.0580667996396583,
1.56862296286742));
#17591=CARTESIAN_POINT('Ctrl Pts',(0.150478939492959,0.0396412815761459,
1.56715551576624));
#17592=CARTESIAN_POINT('Ctrl Pts',(0.151544784499264,0.0353486877907396,
1.56682245053035));
#17593=CARTESIAN_POINT('Ctrl Pts',(0.15255801130537,0.0303692503469366,
1.56645024136146));
#17594=CARTESIAN_POINT('Ctrl Pts',(0.152685509662734,0.0297215975510851,
1.56640210267336));
#17595=CARTESIAN_POINT('Ctrl Pts',(0.152869808344361,0.0287529206726211,
1.56633052945828));
#17596=CARTESIAN_POINT('Ctrl Pts',(0.152929726256561,0.0284325092603508,
1.56630692456872));
#17597=CARTESIAN_POINT('Ctrl Pts',(0.153035229685331,0.0278583459606465,
1.56626475294019));
#17598=CARTESIAN_POINT('Ctrl Pts',(0.153081191748813,0.0276046680979614,
1.56624616520777));
#17599=CARTESIAN_POINT('Ctrl Pts',(0.1531793867987,0.0270549135134226,1.56620597997554));
#17600=CARTESIAN_POINT('Ctrl Pts',(0.15323139204343,0.0267588000823964,
1.56618439551956));
#17601=CARTESIAN_POINT('Ctrl Pts',(0.153374289456989,0.025931075945803,
1.5661242246527));
#17602=CARTESIAN_POINT('Ctrl Pts',(0.153463277064963,0.0253991334819934,
1.56608574427951));
#17603=CARTESIAN_POINT('Ctrl Pts',(0.153964016877278,0.0223071164953629,
1.56586310822235));
#17604=CARTESIAN_POINT('Ctrl Pts',(0.154314502410786,0.0197373354956073,
1.56568220327));
#17605=CARTESIAN_POINT('Ctrl Pts',(0.156223997462395,0.00253380361185688,
1.5644912848206));
#17606=CARTESIAN_POINT('Ctrl Pts',(0.155763942122512,-0.0122499353637323,
1.56355843465293));
#17607=CARTESIAN_POINT('Ctrl Pts',(0.1529045904742,-0.0286291255538685,
1.56244134592911));
#17608=CARTESIAN_POINT('Ctrl Pts',(0.152542051866071,-0.0305018461616655,
1.56231248056851));
#17609=CARTESIAN_POINT('Ctrl Pts',(0.151309670152531,-0.0362947451860791,
1.56190957189021));
#17610=CARTESIAN_POINT('Ctrl Pts',(0.150322477734291,-0.0401879675000319,
1.56163259952195));
#17611=CARTESIAN_POINT('Ctrl Pts',(0.14894005216354,-0.0448711181363862,
1.56128979096042));
#17612=CARTESIAN_POINT('Ctrl Pts',(0.148687271128286,-0.0457017694546805,
1.56122861475013));
#17613=CARTESIAN_POINT('Ctrl Pts',(0.148257561911159,-0.0470725055479746,
1.56112702388317));
#17614=CARTESIAN_POINT('Ctrl Pts',(0.148084601901424,-0.047613822641663,
1.56108673899788));
#17615=CARTESIAN_POINT('Ctrl Pts',(0.147766130500411,-0.0485920283040405,
1.56101363465571));
#17616=CARTESIAN_POINT('Ctrl Pts',(0.147621637264206,-0.0490292437310833,
1.56098084895372));
#17617=CARTESIAN_POINT('Ctrl Pts',(0.147307332476802,-0.0499662983611577,
1.56091033911669));
#17618=CARTESIAN_POINT('Ctrl Pts',(0.147136913947535,-0.0504659262736511,
1.56087259532246));
#17619=CARTESIAN_POINT('Ctrl Pts',(0.146664889008093,-0.0518270780518389,
1.56076935648805));
#17620=CARTESIAN_POINT('Ctrl Pts',(0.14635824139556,-0.05268681805503,1.56070369551455));
#17621=CARTESIAN_POINT('Ctrl Pts',(0.144692481630524,-0.0572302822320028,
1.56035424050756));
#17622=CARTESIAN_POINT('Ctrl Pts',(0.143201939211302,-0.060863937608011,
1.56006610617318));
#17623=CARTESIAN_POINT('Ctrl Pts',(0.135451344610029,-0.0778928958688598,
1.55867234057212));
#17624=CARTESIAN_POINT('Ctrl Pts',(0.127440169506251,-0.0904059070917594,
1.55750690693877));
#17625=CARTESIAN_POINT('Ctrl Pts',(0.114902357022042,-0.104941696078521,
1.55604022870995));
#17626=CARTESIAN_POINT('Ctrl Pts',(0.111875995914586,-0.108162293550515,
1.55570743735417));
#17627=CARTESIAN_POINT('Ctrl Pts',(0.108244311040234,-0.111711266904603,
1.55533549643098));
#17628=CARTESIAN_POINT('Ctrl Pts',(0.107769374344055,-0.112169514670204,
1.55528736634133));
#17629=CARTESIAN_POINT('Ctrl Pts',(0.107055531867526,-0.112849553972302,
1.55521580336939));
#17630=CARTESIAN_POINT('Ctrl Pts',(0.106818830509863,-0.113073631713981,
1.55519220019493));
#17631=CARTESIAN_POINT('Ctrl Pts',(0.106393647576462,-0.113473612434715,
1.55515003041178));
#17632=CARTESIAN_POINT('Ctrl Pts',(0.106205432294646,-0.113649791545102,
1.55513144281756));
#17633=CARTESIAN_POINT('Ctrl Pts',(0.105796764802373,-0.114030423365754,
1.5550912564952));
#17634=CARTESIAN_POINT('Ctrl Pts',(0.105576158176472,-0.114234704553788,
1.55506967081703));
#17635=CARTESIAN_POINT('Ctrl Pts',(0.104958121374668,-0.114803685520051,
1.55500949310048));
#17636=CARTESIAN_POINT('Ctrl Pts',(0.104559379171323,-0.11516696445515,
1.55497100713885));
#17637=CARTESIAN_POINT('Ctrl Pts',(0.102231973945652,-0.117265323800681,
1.55474827376936));
#17638=CARTESIAN_POINT('Ctrl Pts',(0.100261889740756,-0.118954143513077,
1.55456728041599));
#17639=CARTESIAN_POINT('Ctrl Pts',(0.0868424298189114,-0.129887333099358,
1.55337636296554));
#17640=CARTESIAN_POINT('Ctrl Pts',(0.0741724075246528,-0.137516871166556,
1.55244357354668));
#17641=CARTESIAN_POINT('Ctrl Pts',(0.0588595508066705,-0.143996526635533,
1.55132645033646));
#17642=CARTESIAN_POINT('Ctrl Pts',(0.0570880699550032,-0.144707975802186,
1.55119748163509));
#17643=CARTESIAN_POINT('Ctrl Pts',(0.051552664492229,-0.146813602988849,
1.55079457934938));
#17644=CARTESIAN_POINT('Ctrl Pts',(0.0477478216708934,-0.148094739961655,
1.55051772090849));
#17645=CARTESIAN_POINT('Ctrl Pts',(0.0430651036888921,-0.149472248346351,
1.55017503841363));
#17646=CARTESIAN_POINT('Ctrl Pts',(0.0422302225422405,-0.149710268288718,
1.55011387022457));
#17647=CARTESIAN_POINT('Ctrl Pts',(0.040845652384426,-0.150092498424037,
1.55001228992244));
#17648=CARTESIAN_POINT('Ctrl Pts',(0.04029707939573,-0.150240709458207,
1.54997200753299));
#17649=CARTESIAN_POINT('Ctrl Pts',(0.0393025272743941,-0.150503574327373,
1.549898905855));
#17650=CARTESIAN_POINT('Ctrl Pts',(0.038856825538882,-0.150619260508583,
1.54986612030983));
#17651=CARTESIAN_POINT('Ctrl Pts',(0.0384094511441652,-0.150733262965616,
1.54983318460491));
#17652=CARTESIAN_POINT('Ctrl Pts',(0.0384082812240369,-0.150733561076728,
1.5498330984752));
#17653=CARTESIAN_POINT('Ctrl Pts',(0.0384059482241151,-0.150734155527031,
1.54983292671899));
#17654=CARTESIAN_POINT('Ctrl Pts',(0.0384047849173861,-0.150734451924203,
1.5498328410758));
#17655=CARTESIAN_POINT('Ctrl Pts',(0.0384024648054546,-0.150735043033431,
1.54983267026768));
#17656=CARTESIAN_POINT('Ctrl Pts',(0.0384013079879752,-0.150735337748775,
1.54983258510185));
#17657=CARTESIAN_POINT('Ctrl Pts',(0.038399000799677,-0.150735925508802,
1.54983241524446));
#17658=CARTESIAN_POINT('Ctrl Pts',(0.0383978504192419,-0.150736218556093,
1.54983233055217));
#17659=CARTESIAN_POINT('Ctrl Pts',(0.0383955560448425,-0.150736802995819,
1.54983216163743));
#17660=CARTESIAN_POINT('Ctrl Pts',(0.0383944120462634,-0.150737094389585,
1.54983207741463));
#17661=CARTESIAN_POINT('Ctrl Pts',(0.0383921303896934,-0.150737675534414,
1.54983190943548));
#17662=CARTESIAN_POINT('Ctrl Pts',(0.0383909927238457,-0.150737965287632,
1.54983182567856));
#17663=CARTESIAN_POINT('Ctrl Pts',(0.0383887236718577,-0.150738543167327,
1.54983165862668));
#17664=CARTESIAN_POINT('Ctrl Pts',(0.0383875922829476,-0.150738831294662,
1.54983157533152));
#17665=CARTESIAN_POINT('Ctrl Pts',(0.0383853357452364,-0.15073940593313,
1.54983140920027));
#17666=CARTESIAN_POINT('Ctrl Pts',(0.0383842105854601,-0.150739692447207,
1.54983132636337));
#17667=CARTESIAN_POINT('Ctrl Pts',(0.0378784145714043,-0.150868483838546,
1.54979408839843));
#17668=CARTESIAN_POINT('Ctrl Pts',(0.0373731072941603,-0.150994452034455,
1.54975685181441));
#17669=CARTESIAN_POINT('Ctrl Pts',(0.0360039248769304,-0.151328481988625,
1.54965585637752));
#17670=CARTESIAN_POINT('Ctrl Pts',(0.0351388954336563,-0.151531679969435,
1.54959194240574));
#17671=CARTESIAN_POINT('Ctrl Pts',(0.033215670583364,-0.151966097899554,
1.54944958677945));
#17672=CARTESIAN_POINT('Ctrl Pts',(0.0321567139432671,-0.152193696719653,
1.54937103286091));
#17673=CARTESIAN_POINT('Ctrl Pts',(0.0289305899631102,-0.152851906613502,
1.54913116213137));
#17674=CARTESIAN_POINT('Ctrl Pts',(0.0267566307217201,-0.153247401894846,
1.54896875973545));
#17675=CARTESIAN_POINT('Ctrl Pts',(0.00971253633883327,-0.155974418521599,
1.54768915225262));
#17676=CARTESIAN_POINT('Ctrl Pts',(-0.00541511996463198,-0.156182133455611,
1.54650455329011));
#17677=CARTESIAN_POINT('Ctrl Pts',(-0.0213156022871069,-0.154085794186762,
1.54527632582219));
#17678=CARTESIAN_POINT('Ctrl Pts',(-0.0222979999171409,-0.153946699031075,
1.54520055812721));
#17679=CARTESIAN_POINT('Ctrl Pts',(-0.027084322626774,-0.153222237503554,
1.54483216666574));
#17680=CARTESIAN_POINT('Ctrl Pts',(-0.0308673593586107,-0.152505170350796,
1.54454330112266));
#17681=CARTESIAN_POINT('Ctrl Pts',(-0.0352348124117305,-0.151508111477618,
1.54421531433216));
#17682=CARTESIAN_POINT('Ctrl Pts',(-0.035848513556617,-0.151364077513409,
1.54416935515123));
#17683=CARTESIAN_POINT('Ctrl Pts',(-0.0367764532943639,-0.151140332324158,
1.54410007512831));
#17684=CARTESIAN_POINT('Ctrl Pts',(-0.0370913361095948,-0.151063365389453,
1.54407660304249));
#17685=CARTESIAN_POINT('Ctrl Pts',(-0.0376560979925255,-0.150923448088007,
1.54403457379678));
#17686=CARTESIAN_POINT('Ctrl Pts',(-0.037906061975162,-0.150860860953929,
1.54401599625702));
#17687=CARTESIAN_POINT('Ctrl Pts',(-0.0384486518283259,-0.150723571077916,
1.54397572429345));
#17688=CARTESIAN_POINT('Ctrl Pts',(-0.0387412152232905,-0.150648637408858,
1.54395404339664));
#17689=CARTESIAN_POINT('Ctrl Pts',(-0.0395616785001038,-0.150435945653083,
1.54389333129864));
#17690=CARTESIAN_POINT('Ctrl Pts',(-0.0400890817171997,-0.150296259771007,
1.54385440924167));
#17691=CARTESIAN_POINT('Ctrl Pts',(-0.0431834631573669,-0.149459247171671,
1.54362659971488));
#17692=CARTESIAN_POINT('Ctrl Pts',(-0.0457331476969293,-0.148698888836349,
1.54344113449963));
#17693=CARTESIAN_POINT('Ctrl Pts',(-0.0621986944461384,-0.143324937242515,
1.5422504559959));
#17694=CARTESIAN_POINT('Ctrl Pts',(-0.0754234495681357,-0.136828813611224,
1.54132086961655));
#17695=CARTESIAN_POINT('Ctrl Pts',(-0.0891924794692178,-0.127453837113262,
1.54020156738352));
#17696=CARTESIAN_POINT('Ctrl Pts',(-0.0908190090555407,-0.12629998460038,
1.54006678877674));
#17697=CARTESIAN_POINT('Ctrl Pts',(-0.0955754575545617,-0.122786386575669,
1.53966418471888));
#17698=CARTESIAN_POINT('Ctrl Pts',(-0.0986386532251725,-0.12033942185457,
1.53939367059065));
#17699=CARTESIAN_POINT('Ctrl Pts',(-0.102321989093311,-0.117161884816545,
1.5390521152515));
#17700=CARTESIAN_POINT('Ctrl Pts',(-0.103032336512979,-0.116537694623025,
1.5389854596192));
#17701=CARTESIAN_POINT('Ctrl Pts',(-0.104139904084976,-0.115546420695352,
1.53888026126525));
#17702=CARTESIAN_POINT('Ctrl Pts',(-0.104540985114314,-0.115183668010008,
1.53884189974842));
#17703=CARTESIAN_POINT('Ctrl Pts',(-0.105245572700112,-0.114539701059432,
1.53877403230619));
#17704=CARTESIAN_POINT('Ctrl Pts',(-0.105549865940272,-0.114259351852185,
1.53874456317922));
#17705=CARTESIAN_POINT('Ctrl Pts',(-0.106171531832482,-0.113682000611127,
1.53868402889633));
#17706=CARTESIAN_POINT('Ctrl Pts',(-0.106488785044677,-0.113384875919292,
1.53865295865482));
#17707=CARTESIAN_POINT('Ctrl Pts',(-0.107374542791091,-0.112548319597805,
1.53856570780345));
#17708=CARTESIAN_POINT('Ctrl Pts',(-0.107940215108548,-0.112005922184834,
1.53850939976295));
#17709=CARTESIAN_POINT('Ctrl Pts',(-0.110396007242005,-0.109615293510668,
1.53826233353636));
#17710=CARTESIAN_POINT('Ctrl Pts',(-0.112242828511042,-0.107723427538483,
1.53806967550875));
#17711=CARTESIAN_POINT('Ctrl Pts',(-0.117008391145977,-0.102585986612004,
1.53755350668103));
#17712=CARTESIAN_POINT('Ctrl Pts',(-0.119840092423245,-0.0992632562063584,
1.53722663949761));
#17713=CARTESIAN_POINT('Ctrl Pts',(-0.125319458678206,-0.0922570627906749,
1.53655144489211));
#17714=CARTESIAN_POINT('Ctrl Pts',(-0.127953316081791,-0.0885679207499895,
1.53620308667115));
#17715=CARTESIAN_POINT('Ctrl Pts',(-0.136444596427738,-0.0755036163819786,
1.53499794868475));
#17716=CARTESIAN_POINT('Ctrl Pts',(-0.141462839237484,-0.0656218689355162,
1.53413205024323));
#17717=CARTESIAN_POINT('Ctrl Pts',(-0.145801859913025,-0.0542121062604883,
1.53322971772738));
#17718=CARTESIAN_POINT('Ctrl Pts',(-0.14620014266447,-0.0531286487386191,
1.53314498102163));
#17719=CARTESIAN_POINT('Ctrl Pts',(-0.146727444750919,-0.0516433667767692,
1.5330302003167));
#17720=CARTESIAN_POINT('Ctrl Pts',(-0.146866931506856,-0.0512453394583839,
1.53299957590929));
#17721=CARTESIAN_POINT('Ctrl Pts',(-0.147085623620473,-0.0506130710337204,
1.5329511475679));
#17722=CARTESIAN_POINT('Ctrl Pts',(-0.147165890900045,-0.0503792039757457,
1.53293328192992));
#17723=CARTESIAN_POINT('Ctrl Pts',(-0.147330164328206,-0.0498968334491959,
1.5328965314027));
#17724=CARTESIAN_POINT('Ctrl Pts',(-0.147414099533037,-0.0496483088260831,
1.53287765115235));
#17725=CARTESIAN_POINT('Ctrl Pts',(-0.147611973517906,-0.0490574960146327,
1.53283289377293));
#17726=CARTESIAN_POINT('Ctrl Pts',(-0.147725351940766,-0.0487150186508342,
1.53280704956052));
#17727=CARTESIAN_POINT('Ctrl Pts',(-0.148100870838974,-0.0475673376954453,
1.53272076832629));
#17728=CARTESIAN_POINT('Ctrl Pts',(-0.148357633861336,-0.0467603691133015,
1.53266063688858));
#17729=CARTESIAN_POINT('Ctrl Pts',(-0.148956623168405,-0.0448232216206301,
1.53251747722622));
#17730=CARTESIAN_POINT('Ctrl Pts',(-0.149292601094478,-0.0436911460954515,
1.53243477581042));
#17731=CARTESIAN_POINT('Ctrl Pts',(-0.15354171451918,-0.0287521432711609,
1.53135468308444));
#17732=CARTESIAN_POINT('Ctrl Pts',(-0.155539138206286,-0.0144708830394118,
1.53044271801542));
#17733=CARTESIAN_POINT('Ctrl Pts',(-0.155549955824825,-0.000117230094128791,
1.52948519617329));
#17734=CARTESIAN_POINT('Ctrl Pts',(-0.155549955959819,-0.000117050836907798,
1.52948518421517));
#17735=CARTESIAN_POINT('Ctrl Pts',(-0.15555361652718,0.00474751149236398,
1.52916067267151));
#17736=CARTESIAN_POINT('Ctrl Pts',(-0.155329081858837,0.00960927334777459,
1.52883228170288));
#17737=CARTESIAN_POINT('Ctrl Pts',(-0.154667493090214,0.0166991392445401,
1.52834182545603));
#17738=CARTESIAN_POINT('Ctrl Pts',(-0.154408973841275,0.0189410288731022,
1.52818505108391));
#17739=CARTESIAN_POINT('Ctrl Pts',(-0.154002792797181,0.0218968289681659,
1.52797575505208));
#17740=CARTESIAN_POINT('Ctrl Pts',(-0.153898744482907,0.0226165364934278,
1.52792458944346));
#17741=CARTESIAN_POINT('Ctrl Pts',(-0.153713728409857,0.023835862659298,
1.52783754538967));
#17742=CARTESIAN_POINT('Ctrl Pts',(-0.153635360888999,0.0243358690817255,
1.5278017486645));
#17743=CARTESIAN_POINT('Ctrl Pts',(-0.153485598628029,0.0252618297821512,
1.52773526186373));
#17744=CARTESIAN_POINT('Ctrl Pts',(-0.153414867105046,0.0256878876989072,
1.52770459295538));
#17745=CARTESIAN_POINT('Ctrl Pts',(-0.153264775614349,0.0265692425148711,
1.52764098885568));
#17746=CARTESIAN_POINT('Ctrl Pts',(-0.153185159142653,0.0270244907796942,
1.52760804583765));
#17747=CARTESIAN_POINT('Ctrl Pts',(-0.152999854071414,0.0280569327466712,
1.52753312886163));
#17748=CARTESIAN_POINT('Ctrl Pts',(-0.152892926342534,0.0286338938670022,
1.52749111599814));
#17749=CARTESIAN_POINT('Ctrl Pts',(-0.152608376227765,0.0301222199511238,
1.52738235278711));
#17750=CARTESIAN_POINT('Ctrl Pts',(-0.152425855783712,0.0310326126635933,
1.52731544773114));
#17751=CARTESIAN_POINT('Ctrl Pts',(-0.151211072439986,0.0368223830296505,
1.52688749663444));
#17752=CARTESIAN_POINT('Ctrl Pts',(-0.149952909476299,0.0416508209832279,
1.52651930361146));
#17753=CARTESIAN_POINT('Ctrl Pts',(-0.147577486777783,0.0492497716186313,
1.52592093659929));
#17754=CARTESIAN_POINT('Ctrl Pts',(-0.14660854425104,0.0520633037270451,
1.5256951460568));
#17755=CARTESIAN_POINT('Ctrl Pts',(-0.141862381581549,0.0646591989635105,
1.52466587351159));
#17756=CARTESIAN_POINT('Ctrl Pts',(-0.137182830609302,0.0740716023997038,
1.52384325656873));
#17757=CARTESIAN_POINT('Ctrl Pts',(-0.129429928590226,0.0863721085416373,
1.52273207343837));
#17758=CARTESIAN_POINT('Ctrl Pts',(-0.127134049424308,0.0897172657392608,
1.52242607129844));
#17759=CARTESIAN_POINT('Ctrl Pts',(-0.124153766175856,0.0937150487894601,
1.52205895510559));
#17760=CARTESIAN_POINT('Ctrl Pts',(-0.123591023726735,0.0944559526629043,
1.52199085743058));
#17761=CARTESIAN_POINT('Ctrl Pts',(-0.122792336945533,0.0954881400845872,
1.52189595261002));
#17762=CARTESIAN_POINT('Ctrl Pts',(-0.122561951204366,0.095783667889189,
1.52186877616365));
#17763=CARTESIAN_POINT('Ctrl Pts',(-0.122166923059399,0.096286632207899,
1.52182252122679));
#17764=CARTESIAN_POINT('Ctrl Pts',(-0.122002815713996,0.0964944847846486,
1.52180340532849));
#17765=CARTESIAN_POINT('Ctrl Pts',(-0.121686676101729,0.096892800281814,
1.52176677277924));
#17766=CARTESIAN_POINT('Ctrl Pts',(-0.121534726782528,0.0970833254234786,
1.52174925026152));
#17767=CARTESIAN_POINT('Ctrl Pts',(-0.121130027613349,0.097588327612628,
1.5217028025437));
#17768=CARTESIAN_POINT('Ctrl Pts',(-0.120876498573878,0.0979021827039805,
1.52167393265855));
#17769=CARTESIAN_POINT('Ctrl Pts',(-0.119967470267349,0.0990185959212297,
1.52157121424968));
#17770=CARTESIAN_POINT('Ctrl Pts',(-0.119305156555559,0.0998156101702898,
1.52149783582755));
#17771=CARTESIAN_POINT('Ctrl Pts',(-0.11083595244985,0.109802524168907,
1.52057688839368));
#17772=CARTESIAN_POINT('Ctrl Pts',(-0.1019926628234,0.118062709094982,1.51979700344774));
#17773=CARTESIAN_POINT('Ctrl Pts',(-0.0867237757790628,0.129315376007072,
1.51854618159232));
#17774=CARTESIAN_POINT('Ctrl Pts',(-0.0808992164164632,0.133036773350022,
1.518087620436));
#17775=CARTESIAN_POINT('Ctrl Pts',(-0.0727567280229446,0.137506171537307,
1.5174533249823));
#17776=CARTESIAN_POINT('Ctrl Pts',(-0.070640345994748,0.138605300070893,
1.51728908493507));
#17777=CARTESIAN_POINT('Ctrl Pts',(-0.0674723434137778,0.140159175835041,
1.51704361012463));
#17778=CARTESIAN_POINT('Ctrl Pts',(-0.0664395570622591,0.140651686209092,
1.51696364300846));
#17779=CARTESIAN_POINT('Ctrl Pts',(-0.0648320825538602,0.141396596043321,
1.51683921847546));
#17780=CARTESIAN_POINT('Ctrl Pts',(-0.0642611292064625,0.141656992578138,
1.51679503233496));
#17781=CARTESIAN_POINT('Ctrl Pts',(-0.063688625831373,0.141913922642253,
1.51675072916146));
#17782=CARTESIAN_POINT('Ctrl Pts',(-0.0636886280167373,0.141913921661498,
1.50282608545586));
#17783=CARTESIAN_POINT('Ctrl Pts',(-0.069444972190622,0.139330569312872,
1.50324163634357));
#17784=CARTESIAN_POINT('Ctrl Pts',(-0.0750398294545228,0.136398920592801,
1.50365538729071));
#17785=CARTESIAN_POINT('Ctrl Pts',(-0.0858316222556287,0.129878352651127,
1.50449700233988));
#17786=CARTESIAN_POINT('Ctrl Pts',(-0.0910178110036122,0.126298046577962,
1.50492397268563));
#17787=CARTESIAN_POINT('Ctrl Pts',(-0.0971330857956377,0.121503668744037,
1.50546588059912));
#17788=CARTESIAN_POINT('Ctrl Pts',(-0.0982807663767021,0.120577230738902,
1.50556935458113));
#17789=CARTESIAN_POINT('Ctrl Pts',(-0.0999066632205765,0.11922612840304,
1.50571860750275));
#17790=CARTESIAN_POINT('Ctrl Pts',(-0.100395731115997,0.118814595910981,
1.50576385555925));
#17791=CARTESIAN_POINT('Ctrl Pts',(-0.101239754958756,0.118095449204696,
1.50584256726852));
#17792=CARTESIAN_POINT('Ctrl Pts',(-0.101595882549911,0.117789217448042,
1.50587597398802));
#17793=CARTESIAN_POINT('Ctrl Pts',(-0.102278347938201,0.11719697240293,
1.50594037297893));
#17794=CARTESIAN_POINT('Ctrl Pts',(-0.102604887052154,0.116911196826329,
1.50597135521098));
#17795=CARTESIAN_POINT('Ctrl Pts',(-0.10345800454188,0.116158251228628,
1.50605274816537));
#17796=CARTESIAN_POINT('Ctrl Pts',(-0.103982609688192,0.115688871048648,
1.50610325087151));
#17797=CARTESIAN_POINT('Ctrl Pts',(-0.105795760814115,0.114044293669446,
1.50627939666306));
#17798=CARTESIAN_POINT('Ctrl Pts',(-0.107067672047422,0.112851039281774,
1.50640580009945));
#17799=CARTESIAN_POINT('Ctrl Pts',(-0.116677511358743,0.103526774118044,
1.50738336605908));
#17800=CARTESIAN_POINT('Ctrl Pts',(-0.124096874798023,0.0945055082776629,
1.50827533962111));
#17801=CARTESIAN_POINT('Ctrl Pts',(-0.135465062304186,0.0770073141830383,
1.50989323292198));
#17802=CARTESIAN_POINT('Ctrl Pts',(-0.139793357834833,0.068838665034212,
1.51061081365883));
#17803=CARTESIAN_POINT('Ctrl Pts',(-0.143889194726233,0.0591056476709399,
1.5113931951411));
#17804=CARTESIAN_POINT('Ctrl Pts',(-0.144390242499144,0.0578708574297155,
1.51149115765783));
#17805=CARTESIAN_POINT('Ctrl Pts',(-0.145032258433162,0.0562283931100693,
1.51161961860247));
#17806=CARTESIAN_POINT('Ctrl Pts',(-0.145187467966838,0.0558264035680713,
1.51165091411164));
#17807=CARTESIAN_POINT('Ctrl Pts',(-0.145439545192993,0.0551653666251637,
1.51170213316269));
#17808=CARTESIAN_POINT('Ctrl Pts',(-0.145537394643253,0.0549067003613529,
1.51172211433182));
#17809=CARTESIAN_POINT('Ctrl Pts',(-0.145726583888102,0.0544025171063036,
1.51176094030336));
#17810=CARTESIAN_POINT('Ctrl Pts',(-0.145817993731529,0.0541570293206293,
1.51177978905553));
#17811=CARTESIAN_POINT('Ctrl Pts',(-0.146018138485127,0.0536153456280201,
1.51182125968183));
#17812=CARTESIAN_POINT('Ctrl Pts',(-0.146126593882742,0.0533190455508414,
1.51184386498518));
#17813=CARTESIAN_POINT('Ctrl Pts',(-0.146502906194542,0.0522811880439779,
1.51192277572943));
#17814=CARTESIAN_POINT('Ctrl Pts',(-0.146766032147455,0.0515379086126578,
1.51197880876514));
#17815=CARTESIAN_POINT('Ctrl Pts',(-0.147283986004412,0.050038648279442,
1.51209093085876));
#17816=CARTESIAN_POINT('Ctrl Pts',(-0.147538672438769,0.0492826445702359,
1.51214701110478));
#17817=CARTESIAN_POINT('Ctrl Pts',(-0.152918541545005,0.0328976348044611,
1.51335327493306));
#17818=CARTESIAN_POINT('Ctrl Pts',(-0.155539453720288,0.0165532974770953,
1.51438598880801));
#17819=CARTESIAN_POINT('Ctrl Pts',(-0.155553444498373,-0.00534049677197997,
1.51585984431451));
#17820=CARTESIAN_POINT('Ctrl Pts',(-0.155271557712048,-0.0107762398997825,
1.51623210021386));
#17821=CARTESIAN_POINT('Ctrl Pts',(-0.154606664813331,-0.0171314357059268,
1.51668011258868));
#17822=CARTESIAN_POINT('Ctrl Pts',(-0.15449903999975,-0.0180763232433023,
1.51674705151692));
#17823=CARTESIAN_POINT('Ctrl Pts',(-0.154310187101259,-0.0196092048191349,
1.51685620759762));
#17824=CARTESIAN_POINT('Ctrl Pts',(-0.154234244480277,-0.0201978357447761,
1.51689825867686));
#17825=CARTESIAN_POINT('Ctrl Pts',(-0.154093090948979,-0.0212446702859214,
1.51697328991365));
#17826=CARTESIAN_POINT('Ctrl Pts',(-0.154029199895858,-0.021703047360469,
1.51700622814368));
#17827=CARTESIAN_POINT('Ctrl Pts',(-0.153890355103112,-0.0226676642162984,
1.51707572496404));
#17828=CARTESIAN_POINT('Ctrl Pts',(-0.153814946926987,-0.0231738319033319,
1.51711229752432));
#17829=CARTESIAN_POINT('Ctrl Pts',(-0.153609121163664,-0.0245101309648115,
1.51720913354702));
#17830=CARTESIAN_POINT('Ctrl Pts',(-0.153474473709909,-0.0253395835127291,
1.51726952991206));
#17831=CARTESIAN_POINT('Ctrl Pts',(-0.152821097537498,-0.0291681002791789,
1.51754967649849));
#17832=CARTESIAN_POINT('Ctrl Pts',(-0.15222117140047,-0.0321524257371666,
1.51777197528291));
#17833=CARTESIAN_POINT('Ctrl Pts',(-0.148277860043631,-0.0491682716583368,
1.51906327028534));
#17834=CARTESIAN_POINT('Ctrl Pts',(-0.143083300910731,-0.0626964888878243,
1.52019305239524));
#17835=CARTESIAN_POINT('Ctrl Pts',(-0.135880080004464,-0.0757140516487397,
1.52133804497986));
#17836=CARTESIAN_POINT('Ctrl Pts',(-0.135655760700474,-0.0761152307567261,
1.52137338324612));
#17837=CARTESIAN_POINT('Ctrl Pts',(-0.134692032277317,-0.0778209971365417,
1.52152384288372));
#17838=CARTESIAN_POINT('Ctrl Pts',(-0.133935539062451,-0.0791158818654948,
1.52163857524532));
#17839=CARTESIAN_POINT('Ctrl Pts',(-0.131160395055023,-0.0837121619605214,
1.52204723064755));
#17840=CARTESIAN_POINT('Ctrl Pts',(-0.129037241460994,-0.08694924932166,
1.52233769971124));
#17841=CARTESIAN_POINT('Ctrl Pts',(-0.126429796501199,-0.0906184708903705,
1.5226672661327));
#17842=CARTESIAN_POINT('Ctrl Pts',(-0.126061125027223,-0.0911306397614478,
1.52271327554927));
#17843=CARTESIAN_POINT('Ctrl Pts',(-0.125498319491155,-0.0919025540052432,
1.5227826117621));
#17844=CARTESIAN_POINT('Ctrl Pts',(-0.125306479454328,-0.0921639508689246,
1.52280609021135));
#17845=CARTESIAN_POINT('Ctrl Pts',(-0.124960755326893,-0.0926319517778517,
1.52284812073254));
#17846=CARTESIAN_POINT('Ctrl Pts',(-0.124807174878304,-0.0928387740352898,
1.52286669323626));
#17847=CARTESIAN_POINT('Ctrl Pts',(-0.124472577915545,-0.093287035016655,
1.52290694234757));
#17848=CARTESIAN_POINT('Ctrl Pts',(-0.124291372940341,-0.0935283281790202,
1.52292860549018));
#17849=CARTESIAN_POINT('Ctrl Pts',(-0.123781108591073,-0.0942036960613757,
1.52298923756913));
#17850=CARTESIAN_POINT('Ctrl Pts',(-0.123450465241844,-0.0946365777641985,
1.52302809777984));
#17851=CARTESIAN_POINT('Ctrl Pts',(-0.121476589716869,-0.0971928472241987,
1.52325762300377));
#17852=CARTESIAN_POINT('Ctrl Pts',(-0.119780748903356,-0.0992753037702003,
1.52344479717875));
#17853=CARTESIAN_POINT('Ctrl Pts',(-0.10849835884994,-0.112419521216316,
1.52463531288907));
#17854=CARTESIAN_POINT('Ctrl Pts',(-0.0974443086764656,-0.122125975980344,
1.52556355617038));
#17855=CARTESIAN_POINT('Ctrl Pts',(-0.0835241903286924,-0.131238332286373,
1.52668150667753));
#17856=CARTESIAN_POINT('Ctrl Pts',(-0.081832556840949,-0.132299744509495,
1.52681647728102));
#17857=CARTESIAN_POINT('Ctrl Pts',(-0.0767637363690003,-0.135345752809189,
1.52721910217065));
#17858=CARTESIAN_POINT('Ctrl Pts',(-0.0733317325616018,-0.137235551443579,
1.52748943807872));
#17859=CARTESIAN_POINT('Ctrl Pts',(-0.0689876956504054,-0.139418054031481,
1.52783078086008));
#17860=CARTESIAN_POINT('Ctrl Pts',(-0.0681392487230121,-0.139834683302201,
1.52789740828192));
#17861=CARTESIAN_POINT('Ctrl Pts',(-0.066799672897471,-0.140477394785457,
1.52800256433278));
#17862=CARTESIAN_POINT('Ctrl Pts',(-0.0663110618788404,-0.140708698394978,
1.5280409119228));
#17863=CARTESIAN_POINT('Ctrl Pts',(-0.0654464972878158,-0.141112471360968,
1.52810875587328));
#17864=CARTESIAN_POINT('Ctrl Pts',(-0.0650710407117796,-0.141285998016322,
1.52813821546646));
#17865=CARTESIAN_POINT('Ctrl Pts',(-0.0642094402273372,-0.141680045349909,
1.52820581487852));
#17866=CARTESIAN_POINT('Ctrl Pts',(-0.0637228466240425,-0.141899564022123,
1.52824398863043));
#17867=CARTESIAN_POINT('Ctrl Pts',(-0.0623760520317323,-0.142498823781674,
1.52834964274461));
#17868=CARTESIAN_POINT('Ctrl Pts',(-0.0615135353915239,-0.142873270900201,
1.52841730241486));
#17869=CARTESIAN_POINT('Ctrl Pts',(-0.0566509017817775,-0.144932107739253,
1.52879878717056));
#17870=CARTESIAN_POINT('Ctrl Pts',(-0.0525854398684352,-0.146456154268644,
1.52911795621707));
#17871=CARTESIAN_POINT('Ctrl Pts',(-0.0395687427654616,-0.150723946323055,
1.53014180490559));
#17872=CARTESIAN_POINT('Ctrl Pts',(-0.0304316585136157,-0.152830831413686,
1.53086469320528));
#17873=CARTESIAN_POINT('Ctrl Pts',(-0.020797883252986,-0.154153772759252,
1.53161883178106));
#17874=CARTESIAN_POINT('Ctrl Pts',(-0.0204335598364272,-0.154202487776322,
1.53164733682165));
#17875=CARTESIAN_POINT('Ctrl Pts',(-0.0111912446707548,-0.155404982102844,
1.5323700644299));
#17876=CARTESIAN_POINT('Ctrl Pts',(-0.00222902233224552,-0.1557916158411,
1.53306260286976));
#17877=CARTESIAN_POINT('Ctrl Pts',(0.00740435802095051,-0.155375192187848,
1.53376928677472));
#17878=CARTESIAN_POINT('Ctrl Pts',(0.00809081799741246,-0.155340959107295,
1.53381943165361));
#17879=CARTESIAN_POINT('Ctrl Pts',(0.00910781764832401,-0.155283482435782,
1.53389338544108));
#17880=CARTESIAN_POINT('Ctrl Pts',(0.00943853346218654,-0.155263731603161,
1.53391738152706));
#17881=CARTESIAN_POINT('Ctrl Pts',(0.0100268667346512,-0.155226708735474,
1.53395997294424));
#17882=CARTESIAN_POINT('Ctrl Pts',(0.0102845060329824,-0.155209851816248,
1.53397859109114));
#17883=CARTESIAN_POINT('Ctrl Pts',(0.010838168354797,-0.15517224192069,
1.53401852919249));
#17884=CARTESIAN_POINT('Ctrl Pts',(0.0111341735715102,-0.15515128339423,
1.53403983748106));
#17885=CARTESIAN_POINT('Ctrl Pts',(0.0119505053287088,-0.155091135120756,
1.53409848558904));
#17886=CARTESIAN_POINT('Ctrl Pts',(0.0124707040401007,-0.155050173596458,
1.53413572785112));
#17887=CARTESIAN_POINT('Ctrl Pts',(0.0153079241649146,-0.154812393608124,
1.53433818697536));
#17888=CARTESIAN_POINT('Ctrl Pts',(0.0176206745639658,-0.154566241950804,
1.53450080302301));
#17889=CARTESIAN_POINT('Ctrl Pts',(0.0342238390238381,-0.152421572197943,
1.53565645592005));
#17890=CARTESIAN_POINT('Ctrl Pts',(0.0481959687578782,-0.148596326319939,
1.53657171804269));
#17891=CARTESIAN_POINT('Ctrl Pts',(0.0641985574908062,-0.141715723954383,
1.53773801530244));
#17892=CARTESIAN_POINT('Ctrl Pts',(0.0669194130766444,-0.140451385815345,
1.53794050088983));
#17893=CARTESIAN_POINT('Ctrl Pts',(0.069708249892309,-0.13905601942523,
1.53815340403113));
#17894=CARTESIAN_POINT('Ctrl Pts',(0.069814537463293,-0.139002687024802,
1.53816152634118));
#17895=CARTESIAN_POINT('Ctrl Pts',(0.0702831661230713,-0.138766867991926,
1.53819737449482));
#17896=CARTESIAN_POINT('Ctrl Pts',(0.0706448512547139,-0.138583087276658,
1.538225137932));
#17897=CARTESIAN_POINT('Ctrl Pts',(0.0737972682836353,-0.136965722164754,
1.53846797897592));
#17898=CARTESIAN_POINT('Ctrl Pts',(0.0765445746188577,-0.135449516746621,
1.5386855169345));
#17899=CARTESIAN_POINT('Ctrl Pts',(0.0800068983158047,-0.133399717839762,
1.53896833123945));
#17900=CARTESIAN_POINT('Ctrl Pts',(0.0807659013304027,-0.132941557166834,
1.53903087636554));
#17901=CARTESIAN_POINT('Ctrl Pts',(0.0819655073193224,-0.132203368334583,
1.53913062378229));
#17902=CARTESIAN_POINT('Ctrl Pts',(0.082408697213326,-0.131927561944565,
1.539167671321));
#17903=CARTESIAN_POINT('Ctrl Pts',(0.0832016193457557,-0.131428555361072,
1.53923431160548));
#17904=CARTESIAN_POINT('Ctrl Pts',(0.0835518644830371,-0.131206175774389,
1.53926387384011));
#17905=CARTESIAN_POINT('Ctrl Pts',(0.0843684200379183,-0.130683128391871,
1.53933309319188));
#17906=CARTESIAN_POINT('Ctrl Pts',(0.0848340171459703,-0.130381363185524,
1.53937279080153));
#17907=CARTESIAN_POINT('Ctrl Pts',(0.0861659216132569,-0.129507967703471,
1.53948701781686));
#17908=CARTESIAN_POINT('Ctrl Pts',(0.0870281206490416,-0.128930158866643,
1.53956177747625));
#17909=CARTESIAN_POINT('Ctrl Pts',(0.0931353516324097,-0.124748182397607,
1.54009727450012));
#17910=CARTESIAN_POINT('Ctrl Pts',(0.0981598706743632,-0.120834272545009,
1.54056980284225));
#17911=CARTESIAN_POINT('Ctrl Pts',(0.111562080883876,-0.109005767817966,
1.5419250403268));
#17912=CARTESIAN_POINT('Ctrl Pts',(0.119321292594309,-0.100452684296784,
1.54282864467559));
#17913=CARTESIAN_POINT('Ctrl Pts',(0.126743056985038,-0.0901850353215221,
1.54380000538621));
#17914=CARTESIAN_POINT('Ctrl Pts',(0.127410851236553,-0.0892391068311109,
1.54388850193799));
#17915=CARTESIAN_POINT('Ctrl Pts',(0.130277074632733,-0.0850813415508628,
1.54427293294728));
#17916=CARTESIAN_POINT('Ctrl Pts',(0.132365310144968,-0.0817947551773177,
1.54456514531427));
#17917=CARTESIAN_POINT('Ctrl Pts',(0.13464686993893,-0.0778872405679721,
1.54489643957362));
#17918=CARTESIAN_POINT('Ctrl Pts',(0.134962183732542,-0.0773395812411422,
1.54494251417033));
#17919=CARTESIAN_POINT('Ctrl Pts',(0.135434316361647,-0.0765078669353528,
1.54501192901333));
#17920=CARTESIAN_POINT('Ctrl Pts',(0.135593593250301,-0.0762252269661567,
1.54503542141711));
#17921=CARTESIAN_POINT('Ctrl Pts',(0.13587776159334,-0.0757172554511573,
1.54507746686208));
#17922=CARTESIAN_POINT('Ctrl Pts',(0.13600297794591,-0.0754921112565072,
1.54509604039955));
#17923=CARTESIAN_POINT('Ctrl Pts',(0.136273578065135,-0.0750027025446985,
1.54513628022747));
#17924=CARTESIAN_POINT('Ctrl Pts',(0.136418752363205,-0.0747383266842448,
1.54515793310422));
#17925=CARTESIAN_POINT('Ctrl Pts',(0.136823627343831,-0.0739959017149442,
1.54521850751742));
#17926=CARTESIAN_POINT('Ctrl Pts',(0.137081593907283,-0.0735169035363521,
1.54525732066058));
#17927=CARTESIAN_POINT('Ctrl Pts',(0.138592393976546,-0.0706760134066091,
1.54548599512565));
#17928=CARTESIAN_POINT('Ctrl Pts',(0.13978677568173,-0.0682833083686396,
1.54567239570051));
#17929=CARTESIAN_POINT('Ctrl Pts',(0.147120079079251,-0.0525926184865806,
1.54686289783887));
#17930=CARTESIAN_POINT('Ctrl Pts',(0.151416910879703,-0.0385139647951244,
1.54779165672244));
#17931=CARTESIAN_POINT('Ctrl Pts',(0.153987358873573,-0.0220822312958419,
1.54890918710999));
#17932=CARTESIAN_POINT('Ctrl Pts',(0.154256241516254,-0.0201182285771598,
1.54904315331504));
#17933=CARTESIAN_POINT('Ctrl Pts',(0.15494641234157,-0.0142435921607052,
1.54944582064566));
#17934=CARTESIAN_POINT('Ctrl Pts',(0.155256968029684,-0.0103218214161604,
1.54971724428619));
#17935=CARTESIAN_POINT('Ctrl Pts',(0.155457480032245,-0.0054470448734784,
1.55005980348155));
#17936=CARTESIAN_POINT('Ctrl Pts',(0.155487746234464,-0.00450101057047012,
1.55012652140976));
#17937=CARTESIAN_POINT('Ctrl Pts',(0.155521737129451,-0.00301402491509948,
1.55023178937231));
#17938=CARTESIAN_POINT('Ctrl Pts',(0.155531277385485,-0.00247321801681153,
1.55027015772737));
#17939=CARTESIAN_POINT('Ctrl Pts',(0.155543134947022,-0.00151879767110524,
1.55033802189473));
#17940=CARTESIAN_POINT('Ctrl Pts',(0.155546623552833,-0.00110520168523168,
1.55036748084161));
#17941=CARTESIAN_POINT('Ctrl Pts',(0.155550834700325,-0.000158068670969605,
1.55043505910856));
#17942=CARTESIAN_POINT('Ctrl Pts',(0.155550461825959,0.000375465450121448,
1.55047321227224));
#17943=CARTESIAN_POINT('Ctrl Pts',(0.155541856941821,0.00184795701881281,
1.55057875205052));
#17944=CARTESIAN_POINT('Ctrl Pts',(0.155527867702242,0.00278684448913933,
1.55064631733326));
#17945=CARTESIAN_POINT('Ctrl Pts',(0.155401918969186,0.0080440055154591,
1.55102621526338));
#17946=CARTESIAN_POINT('Ctrl Pts',(0.155118626540416,0.0123558618895632,
1.55134383952312));
#17947=CARTESIAN_POINT('Ctrl Pts',(0.153663197767928,0.0258748777886286,
1.55235994877738));
#17948=CARTESIAN_POINT('Ctrl Pts',(0.151846816500051,0.0349912598644559,
1.55307629706358));
#17949=CARTESIAN_POINT('Ctrl Pts',(0.146766439254243,0.0522648696525828,
1.55447266127039));
#17950=CARTESIAN_POINT('Ctrl Pts',(0.143602462384224,0.060418307932727,
1.55514954786331));
#17951=CARTESIAN_POINT('Ctrl Pts',(0.139260916542254,0.0693076386202358,
1.55588090862892));
#17952=CARTESIAN_POINT('Ctrl Pts',(0.138739478815335,0.070345638683965,
1.55596618557241));
#17953=CARTESIAN_POINT('Ctrl Pts',(0.138012428955761,0.0717534021209866,
1.55608157571296));
#17954=CARTESIAN_POINT('Ctrl Pts',(0.137816882122592,0.0721282765326171,
1.55611227716316));
#17955=CARTESIAN_POINT('Ctrl Pts',(0.137504487899386,0.0727212453058917,
1.55616079354087));
#17956=CARTESIAN_POINT('Ctrl Pts',(0.137388646498821,0.0729398623996804,
1.55617867059255));
#17957=CARTESIAN_POINT('Ctrl Pts',(0.137149016359225,0.0733894985907175,
1.55621541664127));
#17958=CARTESIAN_POINT('Ctrl Pts',(0.137025165344152,0.0736204812215321,
1.5562342810999));
#17959=CARTESIAN_POINT('Ctrl Pts',(0.136729901106469,0.0741678239361704,
1.55627895575397));
#17960=CARTESIAN_POINT('Ctrl Pts',(0.136557971456493,0.0744839070050875,
1.55630473332968));
#17961=CARTESIAN_POINT('Ctrl Pts',(0.135980166110081,0.0755374442698578,
1.55639059069942));
#17962=CARTESIAN_POINT('Ctrl Pts',(0.135569391641532,0.0762722177235443,
1.5564503689208));
#17963=CARTESIAN_POINT('Ctrl Pts',(0.131580832986118,0.0832727218406192,
1.55701928367226));
#17964=CARTESIAN_POINT('Ctrl Pts',(0.127576570210791,0.0892866858644213,
1.5575034343084));
#17965=CARTESIAN_POINT('Ctrl Pts',(0.119931106816773,0.0991989453113594,
1.55833258742462));
#17966=CARTESIAN_POINT('Ctrl Pts',(0.116481183418192,0.103228079688648,
1.55867982116881));
#17967=CARTESIAN_POINT('Ctrl Pts',(0.106013084429045,0.114259212070549,
1.55968306451265));
#17968=CARTESIAN_POINT('Ctrl Pts',(0.0985241911643273,0.120776154013316,
1.56034437423262));
#17969=CARTESIAN_POINT('Ctrl Pts',(0.089538363528991,0.127200582193882,
1.56111779693658));
#17970=CARTESIAN_POINT('Ctrl Pts',(0.0886021124757208,0.127854496188725,
1.56119813186994));
#17971=CARTESIAN_POINT('Ctrl Pts',(0.0871761870278595,0.128827233831791,
1.56132015382112));
#17972=CARTESIAN_POINT('Ctrl Pts',(0.0866917615519426,0.129153715485122,
1.56136155129668));
#17973=CARTESIAN_POINT('Ctrl Pts',(0.085821161334806,0.129733357235402,
1.5614358551832));
#17974=CARTESIAN_POINT('Ctrl Pts',(0.0854356745157989,0.129987542572472,
1.56146872268003));
#17975=CARTESIAN_POINT('Ctrl Pts',(0.0850481166150463,0.130240624850765,
1.56150173537069));
#17976=CARTESIAN_POINT('Ctrl Pts',(0.0850471677999097,0.130241244429319,
1.56150181619182));
#17977=CARTESIAN_POINT('Ctrl Pts',(0.0850452782299925,0.130242478293549,
1.56150197714712));
#17978=CARTESIAN_POINT('Ctrl Pts',(0.0850443373587732,0.130243092655502,
1.5615020572912));
#17979=CARTESIAN_POINT('Ctrl Pts',(0.0850424634429056,0.130244316239917,
1.56150221691234));
#17980=CARTESIAN_POINT('Ctrl Pts',(0.0850415304015873,0.130244925460447,
1.5615022963891));
#17981=CARTESIAN_POINT('Ctrl Pts',(0.0850396720898532,0.130246138799087,
1.56150245468034));
#17982=CARTESIAN_POINT('Ctrl Pts',(0.0850387468118492,0.130246742922389,
1.56150253349547));
#17983=CARTESIAN_POINT('Ctrl Pts',(0.0850369039616087,0.130247946109813,
1.56150269046898));
#17984=CARTESIAN_POINT('Ctrl Pts',(0.085035986380576,0.13024854517991,1.56150276862813));
#17985=CARTESIAN_POINT('Ctrl Pts',(0.0850341588439292,0.130249738314079,
1.56150292429654));
#17986=CARTESIAN_POINT('Ctrl Pts',(0.0850332488867652,0.130250332379392,
1.56150300180593));
#17987=CARTESIAN_POINT('Ctrl Pts',(0.0850314365403697,0.130251515542208,
1.56150315617976));
#17988=CARTESIAN_POINT('Ctrl Pts',(0.0850305341430547,0.130252104645214,
1.56150323304487));
#17989=CARTESIAN_POINT('Ctrl Pts',(0.0850289355560498,0.130253148211074,
1.56150336921029));
#17990=CARTESIAN_POINT('Ctrl Pts',(0.0850282393656419,0.130253602679813,
1.56150342851071));
#17991=CARTESIAN_POINT('Ctrl Pts',(0.0850268481085561,0.130254510867813,
1.56150354701565));
#17992=CARTESIAN_POINT('Ctrl Pts',(0.0850261532053007,0.130254964480427,
1.56150360620624));
#17993=CARTESIAN_POINT('Ctrl Pts',(0.0850247647277499,0.130255870822304,
1.56150372447402));
#17994=CARTESIAN_POINT('Ctrl Pts',(0.0850240711573939,0.130256323549025,
1.56150378355087));
#17995=CARTESIAN_POINT('Ctrl Pts',(0.0850226853581879,0.130257228111018,
1.56150390159011));
#17996=CARTESIAN_POINT('Ctrl Pts',(0.085021993122497,0.130257679950786,
1.56150396055308));
#17997=CARTESIAN_POINT('Ctrl Pts',(0.0850206099815398,0.130258582746196,
1.56150407836549));
#17998=CARTESIAN_POINT('Ctrl Pts',(0.0850199190752802,0.130259033702517,
1.56150413721503));
#17999=CARTESIAN_POINT('Ctrl Pts',(0.0850185385898779,0.130259934733284,
1.56150425480085));
#18000=CARTESIAN_POINT('Ctrl Pts',(0.0850178490111873,0.130260384807466,
1.56150431353711));
#18001=CARTESIAN_POINT('Ctrl Pts',(0.0850164711629671,0.130261284085763,
1.56150443089791));
#18002=CARTESIAN_POINT('Ctrl Pts',(0.0850157829010244,0.130261733284957,
1.56150448952181));
#18003=CARTESIAN_POINT('Ctrl Pts',(0.0850144077030382,0.130262630802446,
1.56150460665647));
#18004=CARTESIAN_POINT('Ctrl Pts',(0.0850137207604828,0.130263079125021,
1.5615046651678));
#18005=CARTESIAN_POINT('Ctrl Pts',(0.0850123481892908,0.13026397489718,
1.56150478207833));
#18006=CARTESIAN_POINT('Ctrl Pts',(0.0850116625591765,0.130264422347757,
1.56150484047767));
#18007=CARTESIAN_POINT('Ctrl Pts',(0.0850102926156679,0.130265316374184,
1.56150495716399));
#18008=CARTESIAN_POINT('Ctrl Pts',(0.0850096082961706,0.130265762954044,
1.5615050154515));
#18009=CARTESIAN_POINT('Ctrl Pts',(0.0850082409734261,0.130266655239432,
1.56150513191421));
#18010=CARTESIAN_POINT('Ctrl Pts',(0.0850075579651311,0.130267100948282,
1.56150519008984));
#18011=CARTESIAN_POINT('Ctrl Pts',(0.085006193239945,0.130267991507951,
1.56150530633091));
#18012=CARTESIAN_POINT('Ctrl Pts',(0.0850055115319338,0.130268436353005,
1.56150536439559));
#18013=CARTESIAN_POINT('Ctrl Pts',(0.0850041494113009,0.130269325182566,
1.56150548041443));
#18014=CARTESIAN_POINT('Ctrl Pts',(0.0850034689998191,0.13026976916636,
1.56150553836849));
#18015=CARTESIAN_POINT('Ctrl Pts',(0.0850021094819115,0.130270656267183,
1.56150565416526));
#18016=CARTESIAN_POINT('Ctrl Pts',(0.0850014303686737,0.130271099388686,
1.56150571200855));
#18017=CARTESIAN_POINT('Ctrl Pts',(0.0850000734329893,0.130271984774323,
1.56150582758499));
#18018=CARTESIAN_POINT('Ctrl Pts',(0.0849993956119666,0.130272427037556,
1.56150588531802));
#18019=CARTESIAN_POINT('Ctrl Pts',(0.0849980412531082,0.130273310711701,
1.5615060006746));
#18020=CARTESIAN_POINT('Ctrl Pts',(0.0849973647178349,0.13027375212097,
1.56150605829793));
#18021=CARTESIAN_POINT('Ctrl Pts',(0.0849960129377777,0.130274634082507,
1.56150617343448));
#18022=CARTESIAN_POINT('Ctrl Pts',(0.0849953376882651,0.13027507463789,
1.5615062309481));
#18023=CARTESIAN_POINT('Ctrl Pts',(0.0849939884714945,0.130275954897114,
1.56150634586595));
#18024=CARTESIAN_POINT('Ctrl Pts',(0.0849933145031967,0.130276394601663,
1.56150640327026));
#18025=CARTESIAN_POINT('Ctrl Pts',(0.0849919678425465,0.130277273163421,
1.56150651797001));
#18026=CARTESIAN_POINT('Ctrl Pts',(0.0849912951501145,0.13027771202071,
1.56150657526546));
#18027=CARTESIAN_POINT('Ctrl Pts',(0.0849899510453231,0.130278588885343,
1.56150668974715));
#18028=CARTESIAN_POINT('Ctrl Pts',(0.0849892796286742,0.130279026895512,
1.56150674693375));
#18029=CARTESIAN_POINT('Ctrl Pts',(0.0849879380621388,0.130279902074672,
1.56150686119886));
#18030=CARTESIAN_POINT('Ctrl Pts',(0.0849872679143556,0.130280339242319,
1.5615069182772));
#18031=CARTESIAN_POINT('Ctrl Pts',(0.0849859288870869,0.130281212735516,
1.56150703232567));
#18032=CARTESIAN_POINT('Ctrl Pts',(0.0849852600061635,0.130281649062032,
1.56150708929592));
#18033=CARTESIAN_POINT('Ctrl Pts',(0.0849839235058335,0.130282520877476,
1.56150720312879));
#18034=CARTESIAN_POINT('Ctrl Pts',(0.0849832558862233,0.130282956366564,
1.56150725999143));
#18035=CARTESIAN_POINT('Ctrl Pts',(0.084981921914536,0.13028382650331,1.56150737360856));
#18036=CARTESIAN_POINT('Ctrl Pts',(0.0849812555576062,0.130284261154161,
1.56150743036346));
#18037=CARTESIAN_POINT('Ctrl Pts',(0.0849799240902541,0.130285129628232,
1.56150754376692));
#18038=CARTESIAN_POINT('Ctrl Pts',(0.0849792589851656,0.130285563447999,
1.56150760041502));
#18039=CARTESIAN_POINT('Ctrl Pts',(0.0849779300375986,0.130286430249482,
1.5615077136035));
#18040=CARTESIAN_POINT('Ctrl Pts',(0.0849772661888218,0.130286863235332,
1.56150777014441));
#18041=CARTESIAN_POINT('Ctrl Pts',(0.0849759397301668,0.130287728384529,
1.56150788312054));
#18042=CARTESIAN_POINT('Ctrl Pts',(0.0849752771264454,0.130288160543886,
1.56150793955522));
#18043=CARTESIAN_POINT('Ctrl Pts',(0.0849739531671769,0.130289024034129,
1.56150805231811));
#18044=CARTESIAN_POINT('Ctrl Pts',(0.0849732918071016,0.130289455367994,
1.56150810864669));
#18045=CARTESIAN_POINT('Ctrl Pts',(0.0845396412154296,0.130572274183848,
1.56154504296552));
#18046=CARTESIAN_POINT('Ctrl Pts',(0.0841052518826073,0.130852498318634,
1.56158200121162));
#18047=CARTESIAN_POINT('Ctrl Pts',(0.082927807262822,0.131603781511331,
1.56168207970147));
#18048=CARTESIAN_POINT('Ctrl Pts',(0.0821821488629356,0.132070704074363,
1.56174535160851));
#18049=CARTESIAN_POINT('Ctrl Pts',(0.0805253933788353,0.13308868181175,
1.5618857186583));
#18050=CARTESIAN_POINT('Ctrl Pts',(0.0796125251914252,0.133636753675993,
1.56196291900752));
#18051=CARTESIAN_POINT('Ctrl Pts',(0.0768328353601118,0.135267046982856,
1.5621976046397));
#18052=CARTESIAN_POINT('Ctrl Pts',(0.0749491242085214,0.136319795022483,
1.56235612186252));
#18053=CARTESIAN_POINT('Ctrl Pts',(0.0599444478031621,0.144300432763399,
1.56361513618728));
#18054=CARTESIAN_POINT('Ctrl Pts',(0.0459164366917163,0.149356840055325,
1.56478118003828));
#18055=CARTESIAN_POINT('Ctrl Pts',(0.0301810729871011,0.152598913166574,
1.5660135910902));
#18056=CARTESIAN_POINT('Ctrl Pts',(0.0289694288724993,0.15283356238019,
1.5661079505423));
#18057=CARTESIAN_POINT('Ctrl Pts',(0.0239086094199343,0.153751302093287,
1.56649954020732));
#18058=CARTESIAN_POINT('Ctrl Pts',(0.0200367682716553,0.154303658225789,
1.56679307317728));
#18059=CARTESIAN_POINT('Ctrl Pts',(0.0155186683575466,0.154775235751206,
1.56712567569115));
#18060=CARTESIAN_POINT('Ctrl Pts',(0.0148890874526731,0.15483706849828,
1.567171799314));
#18061=CARTESIAN_POINT('Ctrl Pts',(0.0139359312257882,0.154924812942091,
1.56724127329328));
#18062=CARTESIAN_POINT('Ctrl Pts',(0.0136126336331707,0.154953554509322,
1.56726477618714));
#18063=CARTESIAN_POINT('Ctrl Pts',(0.0130325554285475,0.155003294715676,
1.56730683285849));
#18064=CARTESIAN_POINT('Ctrl Pts',(0.0127758117812956,0.155024667425858,
1.56732540718076));
#18065=CARTESIAN_POINT('Ctrl Pts',(0.0122184880154698,0.155069668061854,
1.56736564006512));
#18066=CARTESIAN_POINT('Ctrl Pts',(0.0119178927641437,0.155093059930054,
1.56738728525196));
#18067=CARTESIAN_POINT('Ctrl Pts',(0.0110752135637488,0.155156171556046,
1.56744781648038));
#18068=CARTESIAN_POINT('Ctrl Pts',(0.0105329793624024,0.155193924806041,
1.56748659437724));
#18069=CARTESIAN_POINT('Ctrl Pts',(0.00733093561575968,0.155400008749324,
1.56771463446037));
#18070=CARTESIAN_POINT('Ctrl Pts',(0.00466714645000089,0.155502814694375,
1.5679004582478));
#18071=CARTESIAN_POINT('Ctrl Pts',(-0.0126493454488499,0.15572568448945,
1.56909095213178));
#18072=CARTESIAN_POINT('Ctrl Pts',(-0.0272550133597357,0.153843311786539,
1.57002009679163));
#18073=CARTESIAN_POINT('Ctrl Pts',(-0.0432831259387198,0.149419743499892,
1.57113732443984));
#18074=CARTESIAN_POINT('Ctrl Pts',(-0.0451732350353517,0.148859219126361,
1.57127055077436));
#18075=CARTESIAN_POINT('Ctrl Pts',(-0.0508121737982156,0.147069668340408,
1.57167325060518));
#18076=CARTESIAN_POINT('Ctrl Pts',(-0.0545251612263234,0.145733889712186,
1.57194547669648));
#18077=CARTESIAN_POINT('Ctrl Pts',(-0.0590618147930818,0.143904142525083,
1.57228893315267));
#18078=CARTESIAN_POINT('Ctrl Pts',(-0.0599372348335434,0.143541729166917,
1.57235571761362));
#18079=CARTESIAN_POINT('Ctrl Pts',(-0.0613073225914843,0.142959810781406,
1.57246106784065));
#18080=CARTESIAN_POINT('Ctrl Pts',(-0.0618042597800819,0.142745678609127,
1.57249945145615));
#18081=CARTESIAN_POINT('Ctrl Pts',(-0.0626790491542835,0.142363304151395,
1.5725673304979));
#18082=CARTESIAN_POINT('Ctrl Pts',(-0.0630573687742955,0.142196138516448,
1.57259678898663));
#18083=CARTESIAN_POINT('Ctrl Pts',(-0.0634381286191023,0.14202607629919,
1.57262654252104));
#18084=CARTESIAN_POINT('Ctrl Pts',(-0.0634412433382933,0.142024685020998,
1.57262678592017));
#18085=CARTESIAN_POINT('Ctrl Pts',(-0.0634473630981949,0.142021951214305,
1.57262726416154));
#18086=CARTESIAN_POINT('Ctrl Pts',(-0.0634503691532165,0.142020608241029,
1.57262749908257));
#18087=CARTESIAN_POINT('Ctrl Pts',(-0.0634562764064302,0.142017968914926,
1.57262796074315));
#18088=CARTESIAN_POINT('Ctrl Pts',(-0.0634591776953348,0.142016672529454,
1.57262818748932));
#18089=CARTESIAN_POINT('Ctrl Pts',(-0.0634648813406012,0.142014123754777,
1.57262863326187));
#18090=CARTESIAN_POINT('Ctrl Pts',(-0.0634676825240292,0.142012871897032,
1.57262885219614));
#18091=CARTESIAN_POINT('Ctrl Pts',(-0.0634731880889014,0.142010411247224,
1.57262928251015));
#18092=CARTESIAN_POINT('Ctrl Pts',(-0.0634758924728102,0.142009202460809,
1.57262949388969));
#18093=CARTESIAN_POINT('Ctrl Pts',(-0.0635486298516659,0.141976688328124,
1.57263517931892));
#18094=CARTESIAN_POINT('Ctrl Pts',(-0.0636186395413799,0.141945331333901,
1.5726406551333));
#18095=CARTESIAN_POINT('Ctrl Pts',(-0.0636886258330468,0.141913922641502,
1.57264613271722));
#18096=CARTESIAN_POINT('Origin',(0.,0.,-0.129405622560373));
#18097=CARTESIAN_POINT('',(-0.0636886255459746,0.141913922770335,1.65651328069486));
#18098=CARTESIAN_POINT('',(-0.0636886598674488,0.141913907367419,1.64281642759095));
#18099=CARTESIAN_POINT('',(-0.0636886258329924,0.141913922641526,-0.129405622560373));
#18100=CARTESIAN_POINT('Ctrl Pts',(-0.0636886255459746,0.141913922770335,
1.65651328069486));
#18101=CARTESIAN_POINT('Ctrl Pts',(-0.0608990448660293,0.143165840523626,
1.65627904268153));
#18102=CARTESIAN_POINT('Ctrl Pts',(-0.0580727927935074,0.144335398020984,
1.65604680844661));
#18103=CARTESIAN_POINT('Ctrl Pts',(-0.0532792558894189,0.146155411082134,
1.65566325401286));
#18104=CARTESIAN_POINT('Ctrl Pts',(-0.0513303839785977,0.146851203993629,
1.65551010689714));
#18105=CARTESIAN_POINT('Ctrl Pts',(-0.048892337343171,0.147667171491005,
1.6553224457726));
#18106=CARTESIAN_POINT('Ctrl Pts',(-0.0484158141915759,0.147824095268433,
1.65528595146716));
#18107=CARTESIAN_POINT('Ctrl Pts',(-0.0476582378689306,0.14806951635225,
1.65522823447466));
#18108=CARTESIAN_POINT('Ctrl Pts',(-0.0473776837606538,0.148159523470421,
1.65520692551255));
#18109=CARTESIAN_POINT('Ctrl Pts',(-0.0468503818960722,0.148327041047081,
1.65516700025293));
#18110=CARTESIAN_POINT('Ctrl Pts',(-0.046603699570519,0.14840473232819,
1.65514837392804));
#18111=CARTESIAN_POINT('Ctrl Pts',(-0.0460371625309225,0.148581608235836,
1.65510571294197));
#18112=CARTESIAN_POINT('Ctrl Pts',(-0.045717180761911,0.14868037539884,
1.65508170286278));
#18113=CARTESIAN_POINT('Ctrl Pts',(-0.0448758194306769,0.148937101191185,
1.65501878744189));
#18114=CARTESIAN_POINT('Ctrl Pts',(-0.0443539184682187,0.149093357399847,
1.65497997884451));
#18115=CARTESIAN_POINT('Ctrl Pts',(-0.0407948483387557,0.150138594078206,
1.65471674004791));
#18116=CARTESIAN_POINT('Ctrl Pts',(-0.0377317114262756,0.150937532491612,
1.65449717498095));
#18117=CARTESIAN_POINT('Ctrl Pts',(-0.0331615458721655,0.151981687012985,
1.65417692292831));
#18118=CARTESIAN_POINT('Ctrl Pts',(-0.031672086360532,0.152299049725731,
1.65407368844555));
#18119=CARTESIAN_POINT('Ctrl Pts',(-0.0289650801959153,0.152834406306263,
1.65388773220125));
#18120=CARTESIAN_POINT('Ctrl Pts',(-0.0277491570929766,0.153059844579423,
1.6538048096822));
#18121=CARTESIAN_POINT('Ctrl Pts',(-0.0123393781655351,0.155727225291964,
1.65276011155914));
#18122=CARTESIAN_POINT('Ctrl Pts',(0.00212350071491233,0.156200920876923,
1.65183866873016));
#18123=CARTESIAN_POINT('Ctrl Pts',(0.0184314283601973,0.154467064384953,
1.65071291298783));
#18124=CARTESIAN_POINT('Ctrl Pts',(0.0204131604714797,0.154217683190534,
1.65057478364117));
#18125=CARTESIAN_POINT('Ctrl Pts',(0.0238302356705591,0.153720662540302,
1.6503339576218));
#18126=CARTESIAN_POINT('Ctrl Pts',(0.0252679441965128,0.153490888875607,
1.65023181555931));
#18127=CARTESIAN_POINT('Ctrl Pts',(0.0273279953237563,0.153131925854066,
1.65008419239853));
#18128=CARTESIAN_POINT('Ctrl Pts',(0.0279531343480862,0.153019045555367,
1.65003922680355));
#18129=CARTESIAN_POINT('Ctrl Pts',(0.0290409301239692,0.152815735752017,
1.64996068157849));
#18130=CARTESIAN_POINT('Ctrl Pts',(0.0295039033391887,0.152727025750853,
1.64992715688427));
#18131=CARTESIAN_POINT('Ctrl Pts',(0.0303904628814731,0.152552971037272,
1.64986277346434));
#18132=CARTESIAN_POINT('Ctrl Pts',(0.0308141115406093,0.152467962960981,
1.64983192574029));
#18133=CARTESIAN_POINT('Ctrl Pts',(0.0318081470859526,0.152264190551568,
1.64975935087931));
#18134=CARTESIAN_POINT('Ctrl Pts',(0.0323782284159838,0.152143985266898,
1.64971757813069));
#18135=CARTESIAN_POINT('Ctrl Pts',(0.0343395720239793,0.151718900773944,
1.64957333084143));
#18136=CARTESIAN_POINT('Ctrl Pts',(0.0357272764128497,0.151398125906685,
1.64947035097586));
#18137=CARTESIAN_POINT('Ctrl Pts',(0.0383481723473096,0.15075425329151,
1.64927404850625));
#18138=CARTESIAN_POINT('Ctrl Pts',(0.0395821865771257,0.150434961147849,
1.64918085502293));
#18139=CARTESIAN_POINT('Ctrl Pts',(0.0419622201260025,0.149787833747246,
1.64899959722581));
#18140=CARTESIAN_POINT('Ctrl Pts',(0.0431086740996831,0.149461918668807,
1.64891159858675));
#18141=CARTESIAN_POINT('Ctrl Pts',(0.0444682074201275,0.149058485998785,
1.64880641742109));
#18142=CARTESIAN_POINT('Ctrl Pts',(0.0446850315587759,0.148993629639146,
1.6487896175478));
#18143=CARTESIAN_POINT('Ctrl Pts',(0.0477825914626118,0.148059718869342,
1.64854925400293));
#18144=CARTESIAN_POINT('Ctrl Pts',(0.0506374859098835,0.147107781428493,
1.64832324982666));
#18145=CARTESIAN_POINT('Ctrl Pts',(0.0670354821435085,0.14110613213863,
1.64699946975092));
#18146=CARTESIAN_POINT('Ctrl Pts',(0.0798478749821994,0.134271947911623,
1.6458533670116));
#18147=CARTESIAN_POINT('Ctrl Pts',(0.0934185158888525,0.124395442551841,
1.64459418947251));
#18148=CARTESIAN_POINT('Ctrl Pts',(0.0952738298962443,0.122980259278891,
1.64442114330223));
#18149=CARTESIAN_POINT('Ctrl Pts',(0.0975048878654918,0.121197657906949,
1.644212612415));
#18150=CARTESIAN_POINT('Ctrl Pts',(0.0979114048193897,0.120869484433413,
1.64417459824159));
#18151=CARTESIAN_POINT('Ctrl Pts',(0.0985463757246321,0.120351578744076,
1.64411520245888));
#18152=CARTESIAN_POINT('Ctrl Pts',(0.0987759477626466,0.12016323407049,
1.64409372425862));
#18153=CARTESIAN_POINT('Ctrl Pts',(0.0992041761750668,0.119809851966965,
1.64405365534143));
#18154=CARTESIAN_POINT('Ctrl Pts',(0.099402958605543,0.119644979088099,
1.644035053748));
#18155=CARTESIAN_POINT('Ctrl Pts',(0.0998557774768346,0.119267497402749,
1.64399267485924));
#18156=CARTESIAN_POINT('Ctrl Pts',(0.100109545671274,0.119054571954386,
1.64396892095671));
#18157=CARTESIAN_POINT('Ctrl Pts',(0.100887317786163,0.118397733259442,
1.64389609851998));
#18158=CARTESIAN_POINT('Ctrl Pts',(0.101409073416943,0.117951150932913,
1.64384721973603));
#18159=CARTESIAN_POINT('Ctrl Pts',(0.10872128947443,0.111608074310811,1.64316153026293));
#18160=CARTESIAN_POINT('Ctrl Pts',(0.114992101339153,0.105135885224328,
1.64256480800013));
#18161=CARTESIAN_POINT('Ctrl Pts',(0.126736238818706,0.0906982327804394,
1.64133787331371));
#18162=CARTESIAN_POINT('Ctrl Pts',(0.13209835676458,0.0826937244621174,
1.64071013236468));
#18163=CARTESIAN_POINT('Ctrl Pts',(0.1387894139837,0.0703754215808663,1.63975882676826));
#18164=CARTESIAN_POINT('Ctrl Pts',(0.140726172301134,0.0664179164084416,
1.63945547254118));
#18165=CARTESIAN_POINT('Ctrl Pts',(0.142871091869294,0.0615186612949306,
1.63907988628775));
#18166=CARTESIAN_POINT('Ctrl Pts',(0.143241990890116,0.0606500334301699,
1.63901329769885));
#18167=CARTESIAN_POINT('Ctrl Pts',(0.14381049156699,0.0592843240338944,
1.63890858107055));
#18168=CARTESIAN_POINT('Ctrl Pts',(0.144013483480364,0.05878949841387,1.63887063555498));
#18169=CARTESIAN_POINT('Ctrl Pts',(0.14436898269628,0.057910021110664,1.63880318066238));
#18170=CARTESIAN_POINT('Ctrl Pts',(0.14452251560409,0.0575257871496899,
1.63877370615406));
#18171=CARTESIAN_POINT('Ctrl Pts',(0.144872839991548,0.0566388048512115,
1.63870565367149));
#18172=CARTESIAN_POINT('Ctrl Pts',(0.1450685497369,0.0561356379303422,1.63866703984484));
#18173=CARTESIAN_POINT('Ctrl Pts',(0.145598419287832,0.0547520735697982,
1.63856083193652));
#18174=CARTESIAN_POINT('Ctrl Pts',(0.14592720518945,0.0538696572518743,
1.63849305973633));
#18175=CARTESIAN_POINT('Ctrl Pts',(0.147566469274839,0.0493449416341665,
1.63814532036692));
#18176=CARTESIAN_POINT('Ctrl Pts',(0.148748560080375,0.0456579353734974,
1.63786116083493));
#18177=CARTESIAN_POINT('Ctrl Pts',(0.150341403995638,0.0399677495943722,
1.63742092773571));
#18178=CARTESIAN_POINT('Ctrl Pts',(0.150852294287511,0.0379939919776107,
1.63726793120321));
#18179=CARTESIAN_POINT('Ctrl Pts',(0.154712733765083,0.0217717087940917,
1.63600828353048));
#18180=CARTESIAN_POINT('Ctrl Pts',(0.156074187606125,0.00712789092104505,
1.6348480177686));
#18181=CARTESIAN_POINT('Ctrl Pts',(0.155239727571641,-0.0101836218114814,
1.63354283366155));
#18182=CARTESIAN_POINT('Ctrl Pts',(0.155039772122432,-0.0128744175193736,
1.63334217459848));
#18183=CARTESIAN_POINT('Ctrl Pts',(0.154715338728085,-0.0161016797795056,
1.63310519529515));
#18184=CARTESIAN_POINT('Ctrl Pts',(0.154657913323084,-0.0166442182149594,
1.63306548232412));
#18185=CARTESIAN_POINT('Ctrl Pts',(0.154564266180585,-0.0174866041143586,
1.6330040280689));
#18186=CARTESIAN_POINT('Ctrl Pts',(0.154530024400451,-0.0177866597884741,
1.63298217909055));
#18187=CARTESIAN_POINT('Ctrl Pts',(0.154464946537715,-0.0183425513784935,
1.63294177915638));
#18188=CARTESIAN_POINT('Ctrl Pts',(0.15443434890426,-0.018598408007981,
1.63292321549553));
#18189=CARTESIAN_POINT('Ctrl Pts',(0.154363824260655,-0.0191759572147144,
1.63288138045559));
#18190=CARTESIAN_POINT('Ctrl Pts',(0.154323527480886,-0.0194976010454009,
1.63285813012462));
#18191=CARTESIAN_POINT('Ctrl Pts',(0.154201906116936,-0.0204443642792246,
1.63278982778873));
#18192=CARTESIAN_POINT('Ctrl Pts',(0.154117785318179,-0.0210691282638834,
1.63274492933054));
#18193=CARTESIAN_POINT('Ctrl Pts',(0.153493036751052,-0.0255050413541026,
1.63242726852459));
#18194=CARTESIAN_POINT('Ctrl Pts',(0.152814846553349,-0.029295877355782,
1.63216170028516));
#18195=CARTESIAN_POINT('Ctrl Pts',(0.149346229066439,-0.0452441415977786,
1.6310545253876));
#18196=CARTESIAN_POINT('Ctrl Pts',(0.145239883189182,-0.0570679676901702,
1.63025545384045));
#18197=CARTESIAN_POINT('Ctrl Pts',(0.137841738755214,-0.0722126059881266,
1.6291282522567));
#18198=CARTESIAN_POINT('Ctrl Pts',(0.13575292830234,-0.0760666996721423,
1.6288318105809));
#18199=CARTESIAN_POINT('Ctrl Pts',(0.132139286810853,-0.0821102106241265,
1.62834681508476));
#18200=CARTESIAN_POINT('Ctrl Pts',(0.130715962735821,-0.0843576518202812,
1.62816173812118));
#18201=CARTESIAN_POINT('Ctrl Pts',(0.128789548325315,-0.0872335812082629,
1.62791809706117));
#18202=CARTESIAN_POINT('Ctrl Pts',(0.128338167522774,-0.0878963034601271,
1.62786147038103));
#18203=CARTESIAN_POINT('Ctrl Pts',(0.12759513557189,-0.0889693049913206,
1.62776898193407));
#18204=CARTESIAN_POINT('Ctrl Pts',(0.127306576884649,-0.0893817169409214,
1.62773323770841));
#18205=CARTESIAN_POINT('Ctrl Pts',(0.126747403762903,-0.090172693644091,
1.62766430033181));
#18206=CARTESIAN_POINT('Ctrl Pts',(0.126477081824213,-0.0905514594263828,
1.62763111863301));
#18207=CARTESIAN_POINT('Ctrl Pts',(0.125853700756244,-0.0914166822604713,
1.62755492553131));
#18208=CARTESIAN_POINT('Ctrl Pts',(0.12549951531312,-0.091902314589759,
1.6275118710144));
#18209=CARTESIAN_POINT('Ctrl Pts',(0.124549973800148,-0.0931885287988769,
1.62739706011512));
#18210=CARTESIAN_POINT('Ctrl Pts',(0.123949723620422,-0.0939854446256672,
1.62732511424198));
#18211=CARTESIAN_POINT('Ctrl Pts',(0.119311853432945,-0.100021154511619,
1.62677388799046));
#18212=CARTESIAN_POINT('Ctrl Pts',(0.114952059642142,-0.105002619974225,
1.62628182057047));
#18213=CARTESIAN_POINT('Ctrl Pts',(0.100301786128063,-0.119732780894116,
1.62470339456722));
#18214=CARTESIAN_POINT('Ctrl Pts',(0.0889910152439483,-0.128362542830679,
1.62358093978354));
#18215=CARTESIAN_POINT('Ctrl Pts',(0.0747092684357749,-0.136452933630983,
1.62235060537937));
#18216=CARTESIAN_POINT('Ctrl Pts',(0.0727250401928938,-0.137520717940809,
1.62218360900416));
#18217=CARTESIAN_POINT('Ctrl Pts',(0.0702578804341241,-0.138780041118213,
1.62198136918977));
#18218=CARTESIAN_POINT('Ctrl Pts',(0.0697964062257403,-0.139012701845162,
1.62194376953812));
#18219=CARTESIAN_POINT('Ctrl Pts',(0.0690690724596102,-0.139374865623461,
1.62188487680579));
#18220=CARTESIAN_POINT('Ctrl Pts',(0.0688039943269213,-0.139505914952153,
1.62186348976599));
#18221=CARTESIAN_POINT('Ctrl Pts',(0.0683065312387699,-0.13975008796814,
1.62182349886584));
#18222=CARTESIAN_POINT('Ctrl Pts',(0.0680742408054287,-0.139863387050623,
1.62180488458511));
#18223=CARTESIAN_POINT('Ctrl Pts',(0.0675418477765219,-0.140121419859923,
1.62176235664602));
#18224=CARTESIAN_POINT('Ctrl Pts',(0.0672415621391036,-0.140265768565776,
1.6217384670107));
#18225=CARTESIAN_POINT('Ctrl Pts',(0.0664541678305077,-0.140641162994019,
1.62167607329915));
#18226=CARTESIAN_POINT('Ctrl Pts',(0.0659663120283192,-0.140870645808377,
1.6216376633919));
#18227=CARTESIAN_POINT('Ctrl Pts',(0.0627064436900205,-0.142383409102036,
1.62138259153232));
#18228=CARTESIAN_POINT('Ctrl Pts',(0.0598980985505228,-0.143587445112446,
1.62117045865516));
#18229=CARTESIAN_POINT('Ctrl Pts',(0.0561656990506188,-0.145059065001976,
1.62089604740292));
#18230=CARTESIAN_POINT('Ctrl Pts',(0.0552722903491997,-0.145401829718346,
1.62083091813414));
#18231=CARTESIAN_POINT('Ctrl Pts',(0.0427160679497486,-0.150086688148569,
1.61992257091531));
#18232=CARTESIAN_POINT('Ctrl Pts',(0.0305758766177735,-0.153022345700376,
1.61912506603374));
#18233=CARTESIAN_POINT('Ctrl Pts',(0.0139089090212142,-0.154987558843089,
1.61800229009047));
#18234=CARTESIAN_POINT('Ctrl Pts',(0.00958397355394749,-0.155314982099894,
1.61770887540659));
#18235=CARTESIAN_POINT('Ctrl Pts',(0.00261304499458369,-0.155550450607335,
1.6172283732642));
#18236=CARTESIAN_POINT('Ctrl Pts',(-2.6877447953494E-5,-0.155572389983154,
1.61704467941598));
#18237=CARTESIAN_POINT('Ctrl Pts',(-0.00346548728426643,-0.155513447477885,
1.6168026055892));
#18238=CARTESIAN_POINT('Ctrl Pts',(-0.00426489386183244,-0.155493577314534,
1.61674613164135));
#18239=CARTESIAN_POINT('Ctrl Pts',(-0.00556669045004523,-0.155451173440848,
1.6166538304993));
#18240=CARTESIAN_POINT('Ctrl Pts',(-0.00606919463109662,-0.15543236545974,
1.61661811994087));
#18241=CARTESIAN_POINT('Ctrl Pts',(-0.00703667833054223,-0.155391455198736,
1.61654920434037));
#18242=CARTESIAN_POINT('Ctrl Pts',(-0.00750166788576647,-0.155369701554002,
1.61651601055884));
#18243=CARTESIAN_POINT('Ctrl Pts',(-0.00856789683317475,-0.155315022502935,
1.61643972852662));
#18244=CARTESIAN_POINT('Ctrl Pts',(-0.00916905339990963,-0.15528069265723,
1.61639659682268));
#18245=CARTESIAN_POINT('Ctrl Pts',(-0.0107693250207461,-0.155179981856469,
1.61628144583911));
#18246=CARTESIAN_POINT('Ctrl Pts',(-0.0117680094202036,-0.155107443397999,
1.61620923528349));
#18247=CARTESIAN_POINT('Ctrl Pts',(-0.0195048804513893,-0.154470333450239,
1.61564702504305));
#18248=CARTESIAN_POINT('Ctrl Pts',(-0.0261994534767621,-0.153476668823616,
1.61514364061818));
#18249=CARTESIAN_POINT('Ctrl Pts',(-0.0465427341251147,-0.149087292981438,
1.61356109177057));
#18250=CARTESIAN_POINT('Ctrl Pts',(-0.0598118587421958,-0.144276643097595,
1.61244770586571));
#18251=CARTESIAN_POINT('Ctrl Pts',(-0.0742153613327783,-0.136721567354128,
1.61122909042333));
#18252=CARTESIAN_POINT('Ctrl Pts',(-0.0761544684454786,-0.135651041840217,
1.61106498337927));
#18253=CARTESIAN_POINT('Ctrl Pts',(-0.0785147694634054,-0.134281412300164,
1.61086575619115));
#18254=CARTESIAN_POINT('Ctrl Pts',(-0.0789580834437356,-0.134021221424974,
1.61082836053673));
#18255=CARTESIAN_POINT('Ctrl Pts',(-0.079653855175316,-0.133608206827305,
1.61076971546948));
#18256=CARTESIAN_POINT('Ctrl Pts',(-0.0799071762423404,-0.133456857316653,
1.61074837338163));
#18257=CARTESIAN_POINT('Ctrl Pts',(-0.0803816446792122,-0.133171545564208,
1.61070842040982));
#18258=CARTESIAN_POINT('Ctrl Pts',(-0.0806028860838241,-0.133037754437413,
1.61068979933147));
#18259=CARTESIAN_POINT('Ctrl Pts',(-0.0811092948571913,-0.132729787315012,
1.61064719541816));
#18260=CARTESIAN_POINT('Ctrl Pts',(-0.0813942350286625,-0.132555243814392,
1.61062323692579));
#18261=CARTESIAN_POINT('Ctrl Pts',(-0.082275654491854,-0.132011406080598,
1.61054915921582));
#18262=CARTESIAN_POINT('Ctrl Pts',(-0.0828702109502639,-0.131638986793843,
1.61049923935756));
#18263=CARTESIAN_POINT('Ctrl Pts',(-0.0889730323680434,-0.127758556568765,
1.60998711866178));
#18264=CARTESIAN_POINT('Ctrl Pts',(-0.0942585466354453,-0.123910455787155,
1.60954585498792));
#18265=CARTESIAN_POINT('Ctrl Pts',(-0.106475918302234,-0.113780014484492,
1.60849026713087));
#18266=CARTESIAN_POINT('Ctrl Pts',(-0.113113290732006,-0.107183956619845,
1.60788436084267));
#18267=CARTESIAN_POINT('Ctrl Pts',(-0.123157428193711,-0.0952233449593448,
1.60684173613532));
#18268=CARTESIAN_POINT('Ctrl Pts',(-0.126900462689203,-0.0901748015851321,
1.60641588726636));
#18269=CARTESIAN_POINT('Ctrl Pts',(-0.131131959578575,-0.0836802319201613,
1.60587530442445));
#18270=CARTESIAN_POINT('Ctrl Pts',(-0.131918436185703,-0.0824348104279719,
1.60577196781285));
#18271=CARTESIAN_POINT('Ctrl Pts',(-0.133020543422085,-0.0806334036975268,
1.60562286950216));
#18272=CARTESIAN_POINT('Ctrl Pts',(-0.133350635522648,-0.0800863206037155,
1.60557763701917));
#18273=CARTESIAN_POINT('Ctrl Pts',(-0.133917548202222,-0.0791335166894393,
1.60549893528809));
#18274=CARTESIAN_POINT('Ctrl Pts',(-0.134155920706063,-0.0787287248136627,
1.60546552286574));
#18275=CARTESIAN_POINT('Ctrl Pts',(-0.13461107059375,-0.0779477432779104,
1.60540110065436));
#18276=CARTESIAN_POINT('Ctrl Pts',(-0.134828114049524,-0.0775717130358765,
1.60537010086352));
#18277=CARTESIAN_POINT('Ctrl Pts',(-0.135393310042289,-0.0765829662989665,
1.60528863410829));
#18278=CARTESIAN_POINT('Ctrl Pts',(-0.135738874513178,-0.0759687899531634,
1.60523807489396));
#18279=CARTESIAN_POINT('Ctrl Pts',(-0.136926926855174,-0.0738232619916477,
1.60506159470033));
#18280=CARTESIAN_POINT('Ctrl Pts',(-0.137747740716487,-0.072280127098607,
1.60493490971184));
#18281=CARTESIAN_POINT('Ctrl Pts',(-0.143773936652353,-0.0604752419742803,
1.6039672214554));
#18282=CARTESIAN_POINT('Ctrl Pts',(-0.147851177544411,-0.0496802116189772,
1.6030864788912));
#18283=CARTESIAN_POINT('Ctrl Pts',(-0.152010189535636,-0.0334161921619007,
1.60178501563297));
#18284=CARTESIAN_POINT('Ctrl Pts',(-0.153057848066806,-0.0282318594119336,
1.60137443230578));
#18285=CARTESIAN_POINT('Ctrl Pts',(-0.154347217967444,-0.0196092291115015,
1.60070605620649));
#18286=CARTESIAN_POINT('Ctrl Pts',(-0.154742391955338,-0.0161981870267941,
1.60044537289847));
#18287=CARTESIAN_POINT('Ctrl Pts',(-0.155125986029771,-0.0115438708860894,
1.60009691644077));
#18288=CARTESIAN_POINT('Ctrl Pts',(-0.155212881636932,-0.0103099034523768,
1.60000522377524));
#18289=CARTESIAN_POINT('Ctrl Pts',(-0.155336268681461,-0.00819858687494373,
1.59984965990898));
#18290=CARTESIAN_POINT('Ctrl Pts',(-0.155380067408009,-0.00732174454646084,
1.59978544256913));
#18291=CARTESIAN_POINT('Ctrl Pts',(-0.155431607352676,-0.00607881011711824,
1.59969500816238));
#18292=CARTESIAN_POINT('Ctrl Pts',(-0.15544548242148,-0.00571301136625637,
1.59966846599659));
#18293=CARTESIAN_POINT('Ctrl Pts',(-0.155467115126977,-0.0050840836155134,
1.59962296049571));
#18294=CARTESIAN_POINT('Ctrl Pts',(-0.155475496322718,-0.004820979126039,
1.59960396269339));
#18295=CARTESIAN_POINT('Ctrl Pts',(-0.155490412169377,-0.00431215066376854,
1.59956729864621));
#18296=CARTESIAN_POINT('Ctrl Pts',(-0.155497032284993,-0.00406643244278431,
1.59954962755572));
#18297=CARTESIAN_POINT('Ctrl Pts',(-0.155511551798444,-0.00347548561179453,
1.59950720929809));
#18298=CARTESIAN_POINT('Ctrl Pts',(-0.155518884167485,-0.00313024224005751,
1.59948249358364));
#18299=CARTESIAN_POINT('Ctrl Pts',(-0.155541455586974,-0.00186975543433769,
1.59939248742674));
#18300=CARTESIAN_POINT('Ctrl Pts',(-0.155549765843993,-0.000954381856539534,
1.59932756922752));
#18301=CARTESIAN_POINT('Ctrl Pts',(-0.155551134068566,0.00450845599433179,
1.59894251175487));
#18302=CARTESIAN_POINT('Ctrl Pts',(-0.155352860170298,0.00905426146478352,
1.5986318572618));
#18303=CARTESIAN_POINT('Ctrl Pts',(-0.154448678088801,0.0193674575730714,
1.59793608506419));
#18304=CARTESIAN_POINT('Ctrl Pts',(-0.153618477239644,0.0251169824458964,
1.59755456985286));
#18305=CARTESIAN_POINT('Ctrl Pts',(-0.150286555365268,0.0416072564119696,
1.59644737583076));
#18306=CARTESIAN_POINT('Ctrl Pts',(-0.146963300510667,0.0521436018595768,
1.59572128706499));
#18307=CARTESIAN_POINT('Ctrl Pts',(-0.141853017373797,0.0638482912150727,
1.59483381564902));
#18308=CARTESIAN_POINT('Ctrl Pts',(-0.141123612738972,0.0654446966530539,
1.59471100082097));
#18309=CARTESIAN_POINT('Ctrl Pts',(-0.140063169080135,0.0676654236340094,
1.59453748856884));
#18310=CARTESIAN_POINT('Ctrl Pts',(-0.139754630913405,0.0683003952916319,
1.59448756631896));
#18311=CARTESIAN_POINT('Ctrl Pts',(-0.139249274571283,0.0693226567645971,
1.59440668226401));
#18312=CARTESIAN_POINT('Ctrl Pts',(-0.139055134896915,0.0697112663874624,
1.59437581388086));
#18313=CARTESIAN_POINT('Ctrl Pts',(-0.138647746111038,0.0705182637366695,
1.59431145754517));
#18314=CARTESIAN_POINT('Ctrl Pts',(-0.1384342253951,0.070936508600774,1.59427796034206));
#18315=CARTESIAN_POINT('Ctrl Pts',(-0.137926161880283,0.0719206742820159,
1.59419879667209));
#18316=CARTESIAN_POINT('Ctrl Pts',(-0.1376300267808,0.0724857587810418,
1.59415307456456));
#18317=CARTESIAN_POINT('Ctrl Pts',(-0.136641325530374,0.0743444942841696,
1.59400178093749));
#18318=CARTESIAN_POINT('Ctrl Pts',(-0.13593394908114,0.0756301321293891,
1.59389568731288));
#18319=CARTESIAN_POINT('Ctrl Pts',(-0.132125460839137,0.0823258798620948,
1.59333530373664));
#18320=CARTESIAN_POINT('Ctrl Pts',(-0.128719697480759,0.0875551708774029,
1.59287013634606));
#18321=CARTESIAN_POINT('Ctrl Pts',(-0.118992645195992,0.100691575591468,
1.59162704895687));
#18322=CARTESIAN_POINT('Ctrl Pts',(-0.112197685779111,0.108211341500411,
1.59083604402017));
#18323=CARTESIAN_POINT('Ctrl Pts',(-0.103439407548259,0.116185629617623,
1.58992415061848));
#18324=CARTESIAN_POINT('Ctrl Pts',(-0.102137268875093,0.117331965792144,
1.58979109670331));
#18325=CARTESIAN_POINT('Ctrl Pts',(-0.0976508970352144,0.121150242182378,
1.58934176515385));
#18326=CARTESIAN_POINT('Ctrl Pts',(-0.0943785271117786,0.123716531480324,
1.58902913788554));
#18327=CARTESIAN_POINT('Ctrl Pts',(-0.0904858430417309,0.12652481003959,
1.58867762143987));
#18328=CARTESIAN_POINT('Ctrl Pts',(-0.0899624225478717,0.126897509488944,
1.58863076554809));
#18329=CARTESIAN_POINT('Ctrl Pts',(-0.0891693495499287,0.127454840521981,
1.58856040451098));
#18330=CARTESIAN_POINT('Ctrl Pts',(-0.0889014089021963,0.127641877031725,
1.58853674112355));
#18331=CARTESIAN_POINT('Ctrl Pts',(-0.0884209665925671,0.127975004054119,
1.58849450645339));
#18332=CARTESIAN_POINT('Ctrl Pts',(-0.0882086901163782,0.128121411119852,
1.58847591390732));
#18333=CARTESIAN_POINT('Ctrl Pts',(-0.0877486162166966,0.12843703860928,
1.58843576539972));
#18334=CARTESIAN_POINT('Ctrl Pts',(-0.0875006936127996,0.128606069670505,
1.58841422227375));
#18335=CARTESIAN_POINT('Ctrl Pts',(-0.0868080096992661,0.129075404092504,
1.58835428290342));
#18336=CARTESIAN_POINT('Ctrl Pts',(-0.0863621752602171,0.12937412877617,
1.58831599138052));
#18337=CARTESIAN_POINT('Ctrl Pts',(-0.0837893738352354,0.131078769604917,
1.58809661187422));
#18338=CARTESIAN_POINT('Ctrl Pts',(-0.081629483383893,0.132434634746554,
1.58791866445991));
#18339=CARTESIAN_POINT('Ctrl Pts',(-0.0743414998873913,0.136763553021572,
1.58733513929074));
#18340=CARTESIAN_POINT('Ctrl Pts',(-0.0690831115522936,0.139492968087388,
1.58694107036115));
#18341=CARTESIAN_POINT('Ctrl Pts',(-0.0636885910816225,0.141913938237362,
1.58655050058549));
#18342=CARTESIAN_POINT('',(-0.155549951835907,-0.000122408525016587,1.5855045602941));
#18343=CARTESIAN_POINT('Ctrl Pts',(-0.0636886258330468,0.141913922641502,
1.57264613271722));
#18344=CARTESIAN_POINT('Ctrl Pts',(-0.0641009893096017,0.141728860720327,
1.57267840697396));
#18345=CARTESIAN_POINT('Ctrl Pts',(-0.0645125404901902,0.141542004026234,
1.572710742672));
#18346=CARTESIAN_POINT('Ctrl Pts',(-0.0657682771443213,0.140965247108265,
1.57280979326616));
#18347=CARTESIAN_POINT('Ctrl Pts',(-0.066609771862077,0.140569574921234,
1.57287670606264));
#18348=CARTESIAN_POINT('Ctrl Pts',(-0.0684762451562442,0.139671433497722,
1.57302634481513));
#18349=CARTESIAN_POINT('Ctrl Pts',(-0.0694993329444581,0.139165182704767,
1.57310919892679));
#18350=CARTESIAN_POINT('Ctrl Pts',(-0.0726354278548155,0.137570153615389,
1.57336579223499));
#18351=CARTESIAN_POINT('Ctrl Pts',(-0.0747290332704821,0.136444212032398,
1.57354080031439));
#18352=CARTESIAN_POINT('Ctrl Pts',(-0.0827711363756286,0.13187855044631,
1.57422788854089));
#18353=CARTESIAN_POINT('Ctrl Pts',(-0.088514280696203,0.128094549558014,
1.57475129930091));
#18354=CARTESIAN_POINT('Ctrl Pts',(-0.103637280342916,0.116626620711548,
1.57621574777035));
#18355=CARTESIAN_POINT('Ctrl Pts',(-0.112399649295948,0.108207267080965,
1.57716846422573));
#18356=CARTESIAN_POINT('Ctrl Pts',(-0.120754353733163,0.0980574257201111,
1.57813834724618));
#18357=CARTESIAN_POINT('Ctrl Pts',(-0.121403843831507,0.0972521441515603,
1.57821418932147));
#18358=CARTESIAN_POINT('Ctrl Pts',(-0.122295194171986,0.0961241409372753,
1.57831882957718));
#18359=CARTESIAN_POINT('Ctrl Pts',(-0.122543887254475,0.0958068927318171,
1.57834808641387));
#18360=CARTESIAN_POINT('Ctrl Pts',(-0.122940871744623,0.0952964001535855,
1.57839488291515));
#18361=CARTESIAN_POINT('Ctrl Pts',(-0.123089945057767,0.095103770984556,
1.57841247723702));
#18362=CARTESIAN_POINT('Ctrl Pts',(-0.123400122205798,0.0947010160723929,
1.57844912955671));
#18363=CARTESIAN_POINT('Ctrl Pts',(-0.123561142518773,0.0944908284784867,
1.57846818133122));
#18364=CARTESIAN_POINT('Ctrl Pts',(-0.123948777951951,0.0939821440320722,
1.57851410848399));
#18365=CARTESIAN_POINT('Ctrl Pts',(-0.124174854625687,0.0936832345687884,
1.57854094615465));
#18366=CARTESIAN_POINT('Ctrl Pts',(-0.124958856351856,0.0926388349516308,
1.57863420915078));
#18367=CARTESIAN_POINT('Ctrl Pts',(-0.125511181178498,0.0918891344735284,
1.57870025732461));
#18368=CARTESIAN_POINT('Ctrl Pts',(-0.128439987064137,0.0878380254440191,
1.57905263748089));
#18369=CARTESIAN_POINT('Ctrl Pts',(-0.130693245446137,0.0844489874748747,
1.57933147835119));
#18370=CARTESIAN_POINT('Ctrl Pts',(-0.138703349340222,0.0713112319659295,
1.58036948929031));
#18371=CARTESIAN_POINT('Ctrl Pts',(-0.143523343782884,0.061032705977832,
1.58109818109095));
#18372=CARTESIAN_POINT('Ctrl Pts',(-0.148132973116123,0.0475500180583476,
1.58204864027409));
#18373=CARTESIAN_POINT('Ctrl Pts',(-0.149002034925602,0.0447523651002227,
1.58224542028539));
#18374=CARTESIAN_POINT('Ctrl Pts',(-0.150942859024143,0.0378192491131736,
1.58273422236917));
#18375=CARTESIAN_POINT('Ctrl Pts',(-0.151924184315183,0.0336612365864171,
1.58302839554287));
#18376=CARTESIAN_POINT('Ctrl Pts',(-0.15290082213847,0.0285993782884959,
1.58339022061924));
#18377=CARTESIAN_POINT('Ctrl Pts',(-0.153061072270756,0.0277289369942959,
1.58345256806181));
#18378=CARTESIAN_POINT('Ctrl Pts',(-0.153312881779592,0.0262924236948839,
1.58355569402839));
#18379=CARTESIAN_POINT('Ctrl Pts',(-0.153408756414912,0.0257271199821655,
1.58359633569648));
#18380=CARTESIAN_POINT('Ctrl Pts',(-0.153576028521563,0.0247066435513975,
1.5836698136023));
#18381=CARTESIAN_POINT('Ctrl Pts',(-0.153648533684215,0.0242516568578654,
1.58370261440413));
#18382=CARTESIAN_POINT('Ctrl Pts',(-0.153785235291465,0.0233685958684075,
1.58376635668532));
#18383=CARTESIAN_POINT('Ctrl Pts',(-0.153849668423592,0.0229405620130406,
1.58379729035895));
#18384=CARTESIAN_POINT('Ctrl Pts',(-0.153986700382066,0.0220036992745516,
1.58386507966919));
#18385=CARTESIAN_POINT('Ctrl Pts',(-0.154058565256427,0.021494769961388,
1.58390195811923));
#18386=CARTESIAN_POINT('Ctrl Pts',(-0.154228627503786,0.0202457485549701,
1.58399260116161));
#18387=CARTESIAN_POINT('Ctrl Pts',(-0.154324020593649,0.0195052943559023,
1.58404645332476));
#18388=CARTESIAN_POINT('Ctrl Pts',(-0.155175713289649,0.0124965551309151,
1.5845573346251));
#18389=CARTESIAN_POINT('Ctrl Pts',(-0.155554918866201,0.00618941757411276,
1.58502610640015));
#18390=CARTESIAN_POINT('Ctrl Pts',(-0.155549951835907,-0.000122408525016587,
1.5855045602941));
#18391=CARTESIAN_POINT('Ctrl Pts',(-0.155549951984829,-0.000122219136381302,
1.58550454593792));
#18392=CARTESIAN_POINT('Ctrl Pts',(-0.155538491446423,-0.0147082017546809,
1.58661020339111));
#18393=CARTESIAN_POINT('Ctrl Pts',(-0.153475709607054,-0.0292190019038337,
1.58776745108562));
#18394=CARTESIAN_POINT('Ctrl Pts',(-0.148802379594176,-0.0453720922747867,
1.58902755176202));
#18395=CARTESIAN_POINT('Ctrl Pts',(-0.148136618725812,-0.0475007213513245,
1.58919281443146));
#18396=CARTESIAN_POINT('Ctrl Pts',(-0.147260995464319,-0.0501025644401173,
1.58939323892886));
#18397=CARTESIAN_POINT('Ctrl Pts',(-0.147094296660472,-0.0505898770390524,
1.5894307085037));
#18398=CARTESIAN_POINT('Ctrl Pts',(-0.146828229298458,-0.0513552407590471,
1.58948943906636));
#18399=CARTESIAN_POINT('Ctrl Pts',(-0.146730486280146,-0.0516338461893166,
1.58951079321163));
#18400=CARTESIAN_POINT('Ctrl Pts',(-0.146545704910844,-0.0521557825658739,
1.58955074911237));
#18401=CARTESIAN_POINT('Ctrl Pts',(-0.14645885448696,-0.0523991720044517,
1.58956936115171));
#18402=CARTESIAN_POINT('Ctrl Pts',(-0.14625849122999,-0.0529562795384037,
1.58961191829856));
#18403=CARTESIAN_POINT('Ctrl Pts',(-0.146144575521072,-0.0532698493600022,
1.58963583921745));
#18404=CARTESIAN_POINT('Ctrl Pts',(-0.14578881330739,-0.0542394064791313,
1.58970970910822));
#18405=CARTESIAN_POINT('Ctrl Pts',(-0.145543547778571,-0.0548941440404258,
1.5897594602705));
#18406=CARTESIAN_POINT('Ctrl Pts',(-0.143021884688049,-0.0614900128456147,
1.5902595289591));
#18407=CARTESIAN_POINT('Ctrl Pts',(-0.140387082166975,-0.0672887219819591,
1.59068998170838));
#18408=CARTESIAN_POINT('Ctrl Pts',(-0.134297636723575,-0.0787646396975859,
1.59155484140726));
#18409=CARTESIAN_POINT('Ctrl Pts',(-0.130820217965645,-0.0844144462868939,
1.59198789187369));
#18410=CARTESIAN_POINT('Ctrl Pts',(-0.123490325215985,-0.094777276869097,
1.59282579115613));
#18411=CARTESIAN_POINT('Ctrl Pts',(-0.119701331001564,-0.0995197194283522,
1.59322917291949));
#18412=CARTESIAN_POINT('Ctrl Pts',(-0.113893444138414,-0.105976168084892,
1.59382046568316));
#18413=CARTESIAN_POINT('Ctrl Pts',(-0.112092678362978,-0.107879075754502,
1.59400046833136));
#18414=CARTESIAN_POINT('Ctrl Pts',(-0.109381273124607,-0.110603064638166,
1.5942674716509));
#18415=CARTESIAN_POINT('Ctrl Pts',(-0.108507551249869,-0.111460360634871,
1.59435292497363));
#18416=CARTESIAN_POINT('Ctrl Pts',(-0.106915725200688,-0.112985804704476,
1.59450764301884));
#18417=CARTESIAN_POINT('Ctrl Pts',(-0.106201239844089,-0.113657647947922,
1.59457674620904));
#18418=CARTESIAN_POINT('Ctrl Pts',(-0.105082341619254,-0.114690005718117,
1.5946844662465));
#18419=CARTESIAN_POINT('Ctrl Pts',(-0.104682308369287,-0.115055248610404,
1.59472288191528));
#18420=CARTESIAN_POINT('Ctrl Pts',(-0.104276848401272,-0.115421581214919,
1.59476172424332));
#18421=CARTESIAN_POINT('Ctrl Pts',(-0.104273316613153,-0.115424771886918,
1.594762062575));
#18422=CARTESIAN_POINT('Ctrl Pts',(-0.104266188632333,-0.115431210820863,
1.59476274539356));
#18423=CARTESIAN_POINT('Ctrl Pts',(-0.104262592433992,-0.115434459077119,
1.59476308988071));
#18424=CARTESIAN_POINT('Ctrl Pts',(-0.10425533355106,-0.115441015027213,
1.59476378520881));
#18425=CARTESIAN_POINT('Ctrl Pts',(-0.104251670860391,-0.115444322715207,
1.59476413605006));
#18426=CARTESIAN_POINT('Ctrl Pts',(-0.104244276822995,-0.115450999453986,
1.59476484429339));
#18427=CARTESIAN_POINT('Ctrl Pts',(-0.104240545471063,-0.115454368497553,
1.59476520169566));
#18428=CARTESIAN_POINT('Ctrl Pts',(-0.104233011856434,-0.115461169947195,
1.5947659232761));
#18429=CARTESIAN_POINT('Ctrl Pts',(-0.104229209586497,-0.115464602347268,
1.59476628745466));
#18430=CARTESIAN_POINT('Ctrl Pts',(-0.104221531629341,-0.115471532734658,
1.59476702282681));
#18431=CARTESIAN_POINT('Ctrl Pts',(-0.104217655935357,-0.115475030714798,
1.59476739402075));
#18432=CARTESIAN_POINT('Ctrl Pts',(-0.104209829464429,-0.11548209372588,
1.59476814358221));
#18433=CARTESIAN_POINT('Ctrl Pts',(-0.104205878220374,-0.115485659164419,
1.59476852199414));
#18434=CARTESIAN_POINT('Ctrl Pts',(-0.104197897533482,-0.115492859861755,
1.59476928628899));
#18435=CARTESIAN_POINT('Ctrl Pts',(-0.104193868131432,-0.115496495069185,
1.59476967216763));
#18436=CARTESIAN_POINT('Ctrl Pts',(-0.104187081761086,-0.115502616887622,
1.59477032205367));
#18437=CARTESIAN_POINT('Ctrl Pts',(-0.10418432528971,-0.11550510325396,
1.59477058601844));
#18438=CARTESIAN_POINT('Ctrl Pts',(-0.104178555092443,-0.115510307658326,
1.59477113857399));
#18439=CARTESIAN_POINT('Ctrl Pts',(-0.104175541349362,-0.115513025676923,
1.59477142716557));
#18440=CARTESIAN_POINT('Ctrl Pts',(-0.104169230240371,-0.115518717058501,
1.59477203149712));
#18441=CARTESIAN_POINT('Ctrl Pts',(-0.104165932852789,-0.115521690398911,
1.59477234723813));
#18442=CARTESIAN_POINT('Ctrl Pts',(-0.104159024941802,-0.115527918906233,
1.59477300869137));
#18443=CARTESIAN_POINT('Ctrl Pts',(-0.104155414394165,-0.115531174044115,
1.59477335440467));
#18444=CARTESIAN_POINT('Ctrl Pts',(-0.104147847062779,-0.115537995830658,
1.59477407896804));
#18445=CARTESIAN_POINT('Ctrl Pts',(-0.104143890247432,-0.115541562446195,
1.59477445781963));
#18446=CARTESIAN_POINT('Ctrl Pts',(-0.103798001153679,-0.115853309617982,
1.59480757473686));
#18447=CARTESIAN_POINT('Ctrl Pts',(-0.103454706161338,-0.116159967965073,
1.59484037625974));
#18448=CARTESIAN_POINT('Ctrl Pts',(-0.102684789330843,-0.116841598537461,
1.59491379539122));
#18449=CARTESIAN_POINT('Ctrl Pts',(-0.102257466540345,-0.117215765277699,
1.59495444589779));
#18450=CARTESIAN_POINT('Ctrl Pts',(-0.10117222881644,-0.118155555915076,
1.59505744051841));
#18451=CARTESIAN_POINT('Ctrl Pts',(-0.100511620385407,-0.118718024697535,
1.59511991313928));
#18452=CARTESIAN_POINT('Ctrl Pts',(-0.0967726047640296,-0.121847995796988,
1.5954723086324));
#18453=CARTESIAN_POINT('Ctrl Pts',(-0.0936008302561725,-0.124301046747286,
1.59576678718968));
#18454=CARTESIAN_POINT('Ctrl Pts',(-0.0887801218319639,-0.127740186614871,
1.59620847516393));
#18455=CARTESIAN_POINT('Ctrl Pts',(-0.0872017938363406,-0.128822792743492,
1.59635219285179));
#18456=CARTESIAN_POINT('Ctrl Pts',(-0.0733365962841737,-0.137961632791901,
1.59760686314945));
#18457=CARTESIAN_POINT('Ctrl Pts',(-0.0599875829553543,-0.14426739288354,
1.59877186826312));
#18458=CARTESIAN_POINT('Ctrl Pts',(-0.0434518173529107,-0.149380718370231,
1.60007426281184));
#18459=CARTESIAN_POINT('Ctrl Pts',(-0.0409307752605421,-0.150091083329582,
1.60026893035934));
#18460=CARTESIAN_POINT('Ctrl Pts',(-0.0378687789950389,-0.150870972998337,
1.60049976261099));
#18461=CARTESIAN_POINT('Ctrl Pts',(-0.0373440511814109,-0.151001711184865,
1.60053912285829));
#18462=CARTESIAN_POINT('Ctrl Pts',(-0.0365262973534834,-0.151200934651514,
1.60060014585674));
#18463=CARTESIAN_POINT('Ctrl Pts',(-0.0362337434210195,-0.151271308845205,
1.60062191397313));
#18464=CARTESIAN_POINT('Ctrl Pts',(-0.0356902669833577,-0.151400375649145,
1.60066223325285));
#18465=CARTESIAN_POINT('Ctrl Pts',(-0.0354394052980914,-0.151459293072542,
1.60068079675295));
#18466=CARTESIAN_POINT('Ctrl Pts',(-0.0348714535585298,-0.151591193987663,
1.60072271846523));
#18467=CARTESIAN_POINT('Ctrl Pts',(-0.0345542808419705,-0.151663805994165,
1.60074605520443));
#18468=CARTESIAN_POINT('Ctrl Pts',(-0.0337358981894035,-0.151848462068656,
1.60080608342902));
#18469=CARTESIAN_POINT('Ctrl Pts',(-0.0332343515683297,-0.151959021301206,
1.60084269197597));
#18470=CARTESIAN_POINT('Ctrl Pts',(-0.0301791796583233,-0.152616643331872,
1.601064651903));
#18471=CARTESIAN_POINT('Ctrl Pts',(-0.0276124635346965,-0.15310185080803,
1.60124670734571));
#18472=CARTESIAN_POINT('Ctrl Pts',(-0.013087507785053,-0.155470404943941,
1.60225847370539));
#18473=CARTESIAN_POINT('Ctrl Pts',(-0.000952604160578558,-0.156017600948628,
1.60303630552406));
#18474=CARTESIAN_POINT('Ctrl Pts',(0.0185569001430925,-0.154618803304722,
1.60433387041633));
#18475=CARTESIAN_POINT('Ctrl Pts',(0.0259408193680818,-0.153552544362755,
1.60483550064718));
#18476=CARTESIAN_POINT('Ctrl Pts',(0.0342923725770274,-0.151726867270332,
1.60543071201355));
#18477=CARTESIAN_POINT('Ctrl Pts',(0.0353629313006877,-0.151480929663042,
1.60550753120635));
#18478=CARTESIAN_POINT('Ctrl Pts',(0.037304855217024,-0.151013107507209,
1.60564787829376));
#18479=CARTESIAN_POINT('Ctrl Pts',(0.0381770793018721,-0.150794964826758,
1.60571128590364));
#18480=CARTESIAN_POINT('Ctrl Pts',(0.0395534839803293,-0.150438019821967,
1.60581195401872));
#18481=CARTESIAN_POINT('Ctrl Pts',(0.0400589500622079,-0.1503042128841,
1.60584905339225));
#18482=CARTESIAN_POINT('Ctrl Pts',(0.0409630275035369,-0.150060001176227,
1.60591564753866));
#18483=CARTESIAN_POINT('Ctrl Pts',(0.0413618933100495,-0.149950549685586,
1.60594511122004));
#18484=CARTESIAN_POINT('Ctrl Pts',(0.0422813648041068,-0.149694292716365,
1.60601322638313));
#18485=CARTESIAN_POINT('Ctrl Pts',(0.042801648105003,-0.14954636066248,
1.60605191408833));
#18486=CARTESIAN_POINT('Ctrl Pts',(0.0442302732157723,-0.149132093953987,
1.6061585498992));
#18487=CARTESIAN_POINT('Ctrl Pts',(0.045136958731249,-0.148860180702317,
1.60622667856557));
#18488=CARTESIAN_POINT('Ctrl Pts',(0.0497985951275568,-0.147415660652176,
1.60657934372105));
#18489=CARTESIAN_POINT('Ctrl Pts',(0.0535102374539595,-0.146109296074309,
1.60686821576001));
#18490=CARTESIAN_POINT('Ctrl Pts',(0.0590109264500262,-0.143935539167679,
1.60730910289901));
#18491=CARTESIAN_POINT('Ctrl Pts',(0.0608396022899218,-0.143172172850268,
1.6074578508425));
#18492=CARTESIAN_POINT('Ctrl Pts',(0.0760617286545473,-0.136473526198417,
1.60871425493073));
#18493=CARTESIAN_POINT('Ctrl Pts',(0.0885675115807059,-0.128709470481681,
1.60987562209073));
#18494=CARTESIAN_POINT('Ctrl Pts',(0.101852403437895,-0.117596919525811,
1.61117959919475));
#18495=CARTESIAN_POINT('Ctrl Pts',(0.103858326047605,-0.115829176009994,
1.61137839771205));
#18496=CARTESIAN_POINT('Ctrl Pts',(0.106216566638279,-0.1136403951341,1.61161346385528));
#18497=CARTESIAN_POINT('Ctrl Pts',(0.106613354810553,-0.113268226058625,
1.61165306250203));
#18498=CARTESIAN_POINT('Ctrl Pts',(0.10722708436266,-0.112686493611665,
1.6117143740992));
#18499=CARTESIAN_POINT('Ctrl Pts',(0.107445377135773,-0.11247837303137,
1.61173619399909));
#18500=CARTESIAN_POINT('Ctrl Pts',(0.107849008024455,-0.112091303579534,
1.61177656056892));
#18501=CARTESIAN_POINT('Ctrl Pts',(0.108034505150202,-0.111912530884119,
1.61179511982888));
#18502=CARTESIAN_POINT('Ctrl Pts',(0.108452606383653,-0.111507577885951,
1.61183697040504));
#18503=CARTESIAN_POINT('Ctrl Pts',(0.108684947048038,-0.11128113069057,
1.61186024055892));
#18504=CARTESIAN_POINT('Ctrl Pts',(0.109367769416864,-0.110611450109255,
1.61192867542775));
#18505=CARTESIAN_POINT('Ctrl Pts',(0.109816267856839,-0.110166189155547,
1.61197368565408));
#18506=CARTESIAN_POINT('Ctrl Pts',(0.113008144300139,-0.106958491154229,
1.61229456172564));
#18507=CARTESIAN_POINT('Ctrl Pts',(0.115649962477262,-0.104096360051836,
1.61256306584535));
#18508=CARTESIAN_POINT('Ctrl Pts',(0.118973248598713,-0.100213023861677,
1.61290965119603));
#18509=CARTESIAN_POINT('Ctrl Pts',(0.119753790463617,-0.0992789697551679,
1.61299173799172));
#18510=CARTESIAN_POINT('Ctrl Pts',(0.129916160190895,-0.0868236684504053,
1.61407107780314));
#18511=CARTESIAN_POINT('Ctrl Pts',(0.137611047442096,-0.0740255833049523,
1.61501769906086));
#18512=CARTESIAN_POINT('Ctrl Pts',(0.144647674180816,-0.0573030255549669,
1.61626024620509));
#18513=CARTESIAN_POINT('Ctrl Pts',(0.1458250664502,-0.0542368295019263,
1.61648787510743));
#18514=CARTESIAN_POINT('Ctrl Pts',(0.147187876624879,-0.0503217111952048,
1.61677937258711));
#18515=CARTESIAN_POINT('Ctrl Pts',(0.147464493213308,-0.0495052404372288,
1.61684020634253));
#18516=CARTESIAN_POINT('Ctrl Pts',(0.147895991165963,-0.0481959038810381,
1.6169378520534));
#18517=CARTESIAN_POINT('Ctrl Pts',(0.148055231497199,-0.0477044837354233,
1.6169745204323));
#18518=CARTESIAN_POINT('Ctrl Pts',(0.148352194074432,-0.0467722385928116,
1.61704412414389));
#18519=CARTESIAN_POINT('Ctrl Pts',(0.148490407000467,-0.0463315746555803,
1.61707704298228));
#18520=CARTESIAN_POINT('Ctrl Pts',(0.148799230140329,-0.045331377578911,
1.61715180424851));
#18521=CARTESIAN_POINT('Ctrl Pts',(0.148968649719736,-0.0447714872094166,
1.61719368503133));
#18522=CARTESIAN_POINT('Ctrl Pts',(0.149460536441214,-0.0431122159625067,
1.61731790106654));
#18523=CARTESIAN_POINT('Ctrl Pts',(0.149774013737616,-0.0420102344294362,
1.61740052666116));
#18524=CARTESIAN_POINT('Ctrl Pts',(0.15260073891637,-0.0316393156406922,
1.61817950146115));
#18525=CARTESIAN_POINT('Ctrl Pts',(0.154262194263629,-0.0221616663302259,
1.61890361821304));
#18526=CARTESIAN_POINT('Ctrl Pts',(0.155498454352139,-0.0069415028431265,
1.62008027058633));
#18527=CARTESIAN_POINT('Ctrl Pts',(0.155648131324104,-0.00126910782265343,
1.62052131682621));
#18528=CARTESIAN_POINT('Ctrl Pts',(0.155285799835476,0.0115390096794103,
1.62151272711295));
#18529=CARTESIAN_POINT('Ctrl Pts',(0.154592155718011,0.0186580014901159,
1.62206070911721));
#18530=CARTESIAN_POINT('Ctrl Pts',(0.153272328652688,0.0265349597668693,
1.62264779499802));
#18531=CARTESIAN_POINT('Ctrl Pts',(0.153126511334706,0.02736388919834,1.62270933041169));
#18532=CARTESIAN_POINT('Ctrl Pts',(0.15290876174406,0.0285454467125072,
1.62279665258911));
#18533=CARTESIAN_POINT('Ctrl Pts',(0.15284232639969,0.0288990521284464,
1.62282273548038));
#18534=CARTESIAN_POINT('Ctrl Pts',(0.152725376908729,0.0295098362577918,
1.62286769830176));
#18535=CARTESIAN_POINT('Ctrl Pts',(0.15267543885169,0.0297671221949332,
1.62288661060182));
#18536=CARTESIAN_POINT('Ctrl Pts',(0.152577093417965,0.030267049393774,
1.62292330340858));
#18537=CARTESIAN_POINT('Ctrl Pts',(0.152528757467485,0.0305097011235796,
1.62294108799456));
#18538=CARTESIAN_POINT('Ctrl Pts',(0.152396246944083,0.0311667324322055,
1.62298917796088));
#18539=CARTESIAN_POINT('Ctrl Pts',(0.152310960507785,0.0315808900069481,
1.62301942056542));
#18540=CARTESIAN_POINT('Ctrl Pts',(0.151985024893486,0.0331316223537152,
1.62313241057119));
#18541=CARTESIAN_POINT('Ctrl Pts',(0.151733325781553,0.0342658759284377,
1.62321455594131));
#18542=CARTESIAN_POINT('Ctrl Pts',(0.149489407706759,0.0438678618898174,
1.62390654670031));
#18543=CARTESIAN_POINT('Ctrl Pts',(0.146802490387278,0.0521588710615691,
1.62448196320056));
#18544=CARTESIAN_POINT('Ctrl Pts',(0.139837337937942,0.0687591919449881,
1.62566791106308));
#18545=CARTESIAN_POINT('Ctrl Pts',(0.135477172078487,0.0769949797846055,
1.62627630484703));
#18546=CARTESIAN_POINT('Ctrl Pts',(0.128049777669527,0.0884181414269208,
1.62720152331419));
#18547=CARTESIAN_POINT('Ctrl Pts',(0.125541825453071,0.0919443171454096,
1.62749958074425));
#18548=CARTESIAN_POINT('Ctrl Pts',(0.122314515324278,0.0961032998971747,
1.62786930134601));
#18549=CARTESIAN_POINT('Ctrl Pts',(0.121731929724715,0.096840188592139,
1.62793553181913));
#18550=CARTESIAN_POINT('Ctrl Pts',(0.120807993965982,0.0979873249105489,
1.62803980184016));
#18551=CARTESIAN_POINT('Ctrl Pts',(0.120471138713455,0.0984011787195175,
1.62807766137335));
#18552=CARTESIAN_POINT('Ctrl Pts',(0.119869415365946,0.0991327233402488,
1.62814501919019));
#18553=CARTESIAN_POINT('Ctrl Pts',(0.119605395605289,0.0994511081540412,
1.62817448296013));
#18554=CARTESIAN_POINT('Ctrl Pts',(0.118993242028814,0.100183348538964,
1.62824259096909));
#18555=CARTESIAN_POINT('Ctrl Pts',(0.118644215225826,0.100596447018815,
1.62828127139845));
#18556=CARTESIAN_POINT('Ctrl Pts',(0.117678659710625,0.101727236933942,
1.62838786824827));
#18557=CARTESIAN_POINT('Ctrl Pts',(0.11705773498536,0.10244112598021,1.62845596501337));
#18558=CARTESIAN_POINT('Ctrl Pts',(0.113825380935251,0.106089663973962,
1.62880820151027));
#18559=CARTESIAN_POINT('Ctrl Pts',(0.111110201860496,0.108930032774784,
1.62909666427657));
#18560=CARTESIAN_POINT('Ctrl Pts',(0.106864621967582,0.113047340626661,
1.62953749603657));
#18561=CARTESIAN_POINT('Ctrl Pts',(0.10541227774224,0.114402796107027,1.62968661436019));
#18562=CARTESIAN_POINT('Ctrl Pts',(0.0930373740300897,0.125516408366512,
1.63094315755684));
#18563=CARTESIAN_POINT('Ctrl Pts',(0.0808145956572658,0.133713293366128,
1.63210426934996));
#18564=CARTESIAN_POINT('Ctrl Pts',(0.0652165164700719,0.141243669643269,
1.63340836092647));
#18565=CARTESIAN_POINT('Ctrl Pts',(0.0627760123512031,0.142345153953356,
1.63360745264081));
#18566=CARTESIAN_POINT('Ctrl Pts',(0.0598064430301666,0.143594178342537,
1.63384281895697));
#18567=CARTESIAN_POINT('Ctrl Pts',(0.0593036714474582,0.143802549554729,
1.6338824342949));
#18568=CARTESIAN_POINT('Ctrl Pts',(0.0585205380821814,0.144122309569973,
1.63394376609378));
#18569=CARTESIAN_POINT('Ctrl Pts',(0.0582409352313616,0.144235526001098,
1.63396558961549));
#18570=CARTESIAN_POINT('Ctrl Pts',(0.0577219348874819,0.144443923723307,
1.63400595950676));
#18571=CARTESIAN_POINT('Ctrl Pts',(0.0574826325525906,0.14453932276196,
1.63402451848401));
#18572=CARTESIAN_POINT('Ctrl Pts',(0.0569414823546903,0.144753498411835,
1.63406636414789));
#18573=CARTESIAN_POINT('Ctrl Pts',(0.0566394999374847,0.144871925393607,
1.63408962969368));
#18574=CARTESIAN_POINT('Ctrl Pts',(0.0557483655392799,0.145218184950564,
1.63415803848032));
#18575=CARTESIAN_POINT('Ctrl Pts',(0.0551581839969529,0.145443378244983,
1.63420302740827));
#18576=CARTESIAN_POINT('Ctrl Pts',(0.050928096019057,0.147027984704399,
1.6345233349603));
#18577=CARTESIAN_POINT('Ctrl Pts',(0.0472393694787453,0.1482543344237,1.63479132151644));
#18578=CARTESIAN_POINT('Ctrl Pts',(0.0382617588238942,0.150869817069479,
1.63542543736143));
#18579=CARTESIAN_POINT('Ctrl Pts',(0.0329380507054243,0.15212086218133,
1.63578683279977));
#18580=CARTESIAN_POINT('Ctrl Pts',(0.0183162213266262,0.154753094581853,
1.63676575034025));
#18581=CARTESIAN_POINT('Ctrl Pts',(0.00894222820702628,0.15557642651765,
1.63737974698278));
#18582=CARTESIAN_POINT('Ctrl Pts',(-0.00479705107421926,0.155536816711758,
1.63831252813579));
#18583=CARTESIAN_POINT('Ctrl Pts',(-0.00914283221186623,0.155341931498338,
1.63861213383822));
#18584=CARTESIAN_POINT('Ctrl Pts',(-0.0144117077594486,0.154883796176454,
1.63898356514615));
#18585=CARTESIAN_POINT('Ctrl Pts',(-0.0153482117848556,0.154793798209709,
1.63904989686948));
#18586=CARTESIAN_POINT('Ctrl Pts',(-0.0168148261158964,0.154639416742765,
1.63915429104215));
#18587=CARTESIAN_POINT('Ctrl Pts',(-0.017345531104498,0.154580788345859,
1.63919217275941));
#18588=CARTESIAN_POINT('Ctrl Pts',(-0.0182867992969613,0.15447189567868,
1.63925955317337));
#18589=CARTESIAN_POINT('Ctrl Pts',(-0.0186974859233309,0.154422723707281,
1.6392890172563));
#18590=CARTESIAN_POINT('Ctrl Pts',(-0.0196443511186888,0.154305521884548,
1.6393571016759));
#18591=CARTESIAN_POINT('Ctrl Pts',(-0.0201803782875225,0.154236334673412,
1.63939575809348));
#18592=CARTESIAN_POINT('Ctrl Pts',(-0.0216523074370992,0.154038542356466,
1.63950222639143));
#18593=CARTESIAN_POINT('Ctrl Pts',(-0.0225874018261968,0.153904204472222,
1.6395702179044));
#18594=CARTESIAN_POINT('Ctrl Pts',(-0.0273865823106737,0.153170063832257,
1.63992104413842));
#18595=CARTESIAN_POINT('Ctrl Pts',(-0.0312279455946206,0.152433276152811,
1.64020816085631));
#18596=CARTESIAN_POINT('Ctrl Pts',(-0.0369886077255515,0.151101479231752,
1.64064881192362));
#18597=CARTESIAN_POINT('Ctrl Pts',(-0.0389310677558046,0.150612700262753,
1.64079914989949));
#18598=CARTESIAN_POINT('Ctrl Pts',(-0.0486830380937218,0.147957569881437,
1.64156267073385));
#18599=CARTESIAN_POINT('Ctrl Pts',(-0.0563140102735931,0.145223530492718,
1.6421896099303));
#18600=CARTESIAN_POINT('Ctrl Pts',(-0.0636886598674488,0.141913907367419,
1.64281642759095));
#18601=CARTESIAN_POINT('Origin',(0.,0.,-0.129405622560373));
#18602=CARTESIAN_POINT('',(-0.0636886248462869,0.141913923084343,1.72674034350975));
#18603=CARTESIAN_POINT('',(-0.0636886260955797,0.141913922523681,1.71290984779881));
#18604=CARTESIAN_POINT('',(-0.0636886258329924,0.141913922641526,-0.129405622560373));
#18605=CARTESIAN_POINT('',(-0.155549925504284,0.000142733485857199,1.66943656442265));
#18606=CARTESIAN_POINT('Ctrl Pts',(-0.0636886248462869,0.141913923084343,
1.72674034350975));
#18607=CARTESIAN_POINT('Ctrl Pts',(-0.0621902796711602,0.142586355652444,
1.72661900977629));
#18608=CARTESIAN_POINT('Ctrl Pts',(-0.0606812720557253,0.143235064542905,
1.72649690634238));
#18609=CARTESIAN_POINT('Ctrl Pts',(-0.0502628428185461,0.147519630401365,
1.72565450019174));
#18610=CARTESIAN_POINT('Ctrl Pts',(-0.0410442217624049,0.150345333593974,
1.72491025279256));
#18611=CARTESIAN_POINT('Ctrl Pts',(-0.0228284591095591,0.154127809374507,
1.72346757472166));
#18612=CARTESIAN_POINT('Ctrl Pts',(-0.0138888489024449,0.155189123259374,
1.72277247368547));
#18613=CARTESIAN_POINT('Ctrl Pts',(-0.00422002387772398,0.155494262660439,
1.72206350403877));
#18614=CARTESIAN_POINT('Ctrl Pts',(-0.0035333195842798,0.15551138228955,
1.7220133882769));
#18615=CARTESIAN_POINT('Ctrl Pts',(-0.0025152771248716,0.155530015210193,
1.72193946442735));
#18616=CARTESIAN_POINT('Ctrl Pts',(-0.00218402404886312,0.155535019512673,
1.72191546943375));
#18617=CARTESIAN_POINT('Ctrl Pts',(-0.00159451054005605,0.155542041695949,
1.72187287391598));
#18618=CARTESIAN_POINT('Ctrl Pts',(-0.00133625934049361,0.15554447471248,
1.7218542506026));
#18619=CARTESIAN_POINT('Ctrl Pts',(-0.000781080073054311,0.155548322324139,
1.72181429434771));
#18620=CARTESIAN_POINT('Ctrl Pts',(-0.000484154410688755,0.155549529933284,
1.72179297311045));
#18621=CARTESIAN_POINT('Ctrl Pts',(0.000335130299288034,0.155550516044807,
1.72173427231057));
#18622=CARTESIAN_POINT('Ctrl Pts',(0.000857494205561969,0.155548513585851,
1.7216969905533));
#18623=CARTESIAN_POINT('Ctrl Pts',(0.00371153867656535,0.155523195020484,
1.72149403721382));
#18624=CARTESIAN_POINT('Ctrl Pts',(0.00604263981905059,0.155450081347442,
1.72133098112));
#18625=CARTESIAN_POINT('Ctrl Pts',(0.0227955254658225,0.154547167001268,
1.72017293357849));
#18626=CARTESIAN_POINT('Ctrl Pts',(0.0370426749005134,0.151764344056263,
1.71925593674634));
#18627=CARTESIAN_POINT('Ctrl Pts',(0.0535441078097416,0.146074862506836,
1.71808701521844));
#18628=CARTESIAN_POINT('Ctrl Pts',(0.0563565522332939,0.145013014471313,
1.71788407502271));
#18629=CARTESIAN_POINT('Ctrl Pts',(0.0593257138165678,0.143792573158951,
1.71766483809867));
#18630=CARTESIAN_POINT('Ctrl Pts',(0.0595149195771825,0.143714365192403,
1.71765084568062));
#18631=CARTESIAN_POINT('Ctrl Pts',(0.060628188029096,0.143251621550014,
1.71756838539903));
#18632=CARTESIAN_POINT('Ctrl Pts',(0.0615486600053697,0.142858554662465,
1.71749967638848));
#18633=CARTESIAN_POINT('Ctrl Pts',(0.0645049474021633,0.141562263683949,
1.71727719848676));
#18634=CARTESIAN_POINT('Ctrl Pts',(0.0665250987980878,0.140624226602029,
1.71712238342063));
#18635=CARTESIAN_POINT('Ctrl Pts',(0.0693242904106561,0.139250634783446,
1.71690356064034));
#18636=CARTESIAN_POINT('Ctrl Pts',(0.070120846455336,0.138851227442003,
1.71684079425987));
#18637=CARTESIAN_POINT('Ctrl Pts',(0.0714259751798809,0.13818271806797,
1.71673711024488));
#18638=CARTESIAN_POINT('Ctrl Pts',(0.0719365725886382,0.137917595001939,
1.71669633199495));
#18639=CARTESIAN_POINT('Ctrl Pts',(0.072853656223835,0.13743492941285,1.71662269659871));
#18640=CARTESIAN_POINT('Ctrl Pts',(0.0732606704849775,0.137218399639411,
1.7165898754797));
#18641=CARTESIAN_POINT('Ctrl Pts',(0.0741272961890235,0.136752403758898,
1.71651968749743));
#18642=CARTESIAN_POINT('Ctrl Pts',(0.0745866231069483,0.13650242347777,
1.71648230269036));
#18643=CARTESIAN_POINT('Ctrl Pts',(0.0758245583202079,0.135820586011575,
1.71638104257065));
#18644=CARTESIAN_POINT('Ctrl Pts',(0.0766007232022802,0.135384357931939,
1.71631701188344));
#18645=CARTESIAN_POINT('Ctrl Pts',(0.0805180282808756,0.133138243997113,
1.71599104083602));
#18646=CARTESIAN_POINT('Ctrl Pts',(0.0835987048773317,0.13122574963496,
1.7157254247197));
#18647=CARTESIAN_POINT('Ctrl Pts',(0.0990752212562384,0.120851633452506,
1.71434095445131));
#18648=CARTESIAN_POINT('Ctrl Pts',(0.110264933582334,0.110736177202784,
1.71315843172312));
#18649=CARTESIAN_POINT('Ctrl Pts',(0.122719629522112,0.0956882025727495,
1.71166485677054));
#18650=CARTESIAN_POINT('Ctrl Pts',(0.125455521444773,0.0920720441788441,
1.71132314837159));
#18651=CARTESIAN_POINT('Ctrl Pts',(0.128406743986182,0.0877949372396135,
1.71094248750993));
#18652=CARTESIAN_POINT('Ctrl Pts',(0.128780148148875,0.0872462972929728,
1.71089408581105));
#18653=CARTESIAN_POINT('Ctrl Pts',(0.129332110189271,0.0864240388497398,
1.71082219936142));
#18654=CARTESIAN_POINT('Ctrl Pts',(0.129513329272134,0.0861522301701557,
1.71079854208761));
#18655=CARTESIAN_POINT('Ctrl Pts',(0.129836059376996,0.0856648508895601,
1.71075631401498));
#18656=CARTESIAN_POINT('Ctrl Pts',(0.129977891278066,0.0854494983891286,
1.71073772198102));
#18657=CARTESIAN_POINT('Ctrl Pts',(0.130283640625665,0.0849827368135727,
1.71069756967657));
#18658=CARTESIAN_POINT('Ctrl Pts',(0.130447365756298,0.0847312064259459,
1.71067602226329));
#18659=CARTESIAN_POINT('Ctrl Pts',(0.130901967046047,0.0840283631318044,
1.71061605889121));
#18660=CARTESIAN_POINT('Ctrl Pts',(0.131191239832641,0.0835760097218225,
1.71057774778998));
#18661=CARTESIAN_POINT('Ctrl Pts',(0.132842999884799,0.080963344304532,
1.71035803352663));
#18662=CARTESIAN_POINT('Ctrl Pts',(0.134154559932035,0.0787710722785302,
1.71017978216496));
#18663=CARTESIAN_POINT('Ctrl Pts',(0.142668881122267,0.0637093034277671,
1.70898881459483));
#18664=CARTESIAN_POINT('Ctrl Pts',(0.148064372925472,0.0499032798740733,
1.70805412698548));
#18665=CARTESIAN_POINT('Ctrl Pts',(0.151860681372334,0.0337284438750968,
1.7069379584023));
#18666=CARTESIAN_POINT('Ctrl Pts',(0.152253800459681,0.0319069637616406,
1.70681209572631));
#18667=CARTESIAN_POINT('Ctrl Pts',(0.153400017014601,0.0260913009158145,
1.7064090056545));
#18668=CARTESIAN_POINT('Ctrl Pts',(0.154029287767484,0.0220747544083784,
1.70612872805264));
#18669=CARTESIAN_POINT('Ctrl Pts',(0.154601630055619,0.0171726061421569,
1.70578225223314));
#18670=CARTESIAN_POINT('Ctrl Pts',(0.154695438831028,0.016305936568474,
1.70572083424175));
#18671=CARTESIAN_POINT('Ctrl Pts',(0.154838465462932,0.0148719964267047,
1.70561892495261));
#18672=CARTESIAN_POINT('Ctrl Pts',(0.15489186297775,0.0143051540458542,
1.70557856486868));
#18673=CARTESIAN_POINT('Ctrl Pts',(0.154982822217146,0.01327928559562,1.70550538014689));
#18674=CARTESIAN_POINT('Ctrl Pts',(0.155021459761912,0.012820359325902,
1.70547258961052));
#18675=CARTESIAN_POINT('Ctrl Pts',(0.15509994685119,0.0118358283690187,
1.70540213153404));
#18676=CARTESIAN_POINT('Ctrl Pts',(0.155139163817248,0.0113101805414122,
1.70536444460437));
#18677=CARTESIAN_POINT('Ctrl Pts',(0.155238745155906,0.0098773073973731,
1.70526151970379));
#18678=CARTESIAN_POINT('Ctrl Pts',(0.155293827139638,0.00896974838637173,
1.70519611749477));
#18679=CARTESIAN_POINT('Ctrl Pts',(0.155541871189152,0.00419023123780119,
1.70485052656883));
#18680=CARTESIAN_POINT('Ctrl Pts',(0.155597971960112,0.000312878410750554,
1.70456611098715));
#18681=CARTESIAN_POINT('Ctrl Pts',(0.155169831926513,-0.0183776312293385,
1.70317398794097));
#18682=CARTESIAN_POINT('Ctrl Pts',(0.152714794916144,-0.0330674755562086,
1.7020058566634));
#18683=CARTESIAN_POINT('Ctrl Pts',(0.146875203436004,-0.05141170805286,
1.70053476160677));
#18684=CARTESIAN_POINT('Ctrl Pts',(0.145348872480629,-0.0555806033333861,
1.70020041206912));
#18685=CARTESIAN_POINT('Ctrl Pts',(0.143392726748624,-0.0602890107288308,
1.69982694537498));
#18686=CARTESIAN_POINT('Ctrl Pts',(0.143135386460692,-0.0608974554787733,
1.69977876658327));
#18687=CARTESIAN_POINT('Ctrl Pts',(0.142745243939314,-0.0618037551798422,
1.69970714559602));
#18688=CARTESIAN_POINT('Ctrl Pts',(0.142615373296841,-0.0621028511932481,
1.69968353270926));
#18689=CARTESIAN_POINT('Ctrl Pts',(0.142381134503401,-0.0626377003586985,
1.69964135247382));
#18690=CARTESIAN_POINT('Ctrl Pts',(0.142277120340909,-0.0628736033621158,
1.69962276409479));
#18691=CARTESIAN_POINT('Ctrl Pts',(0.142050574907161,-0.0633839648923704,
1.6995825839355));
#18692=CARTESIAN_POINT('Ctrl Pts',(0.141927834871523,-0.0636583264764555,
1.69956100517044));
#18693=CARTESIAN_POINT('Ctrl Pts',(0.141582785348254,-0.0644236591788939,
1.69950086619507));
#18694=CARTESIAN_POINT('Ctrl Pts',(0.14135871533123,-0.0649138397557635,
1.6994624118407));
#18695=CARTESIAN_POINT('Ctrl Pts',(0.140044389966331,-0.0677500079083123,
1.69924022813088));
#18696=CARTESIAN_POINT('Ctrl Pts',(0.138898211917177,-0.0700698478122041,
1.69905973408469));
#18697=CARTESIAN_POINT('Ctrl Pts',(0.130846717308816,-0.0853910809206949,
1.69786881045817));
#18698=CARTESIAN_POINT('Ctrl Pts',(0.122183178584942,-0.0973852161518665,
1.69693567752971));
#18699=CARTESIAN_POINT('Ctrl Pts',(0.110642208770475,-0.109351340065427,
1.69581874591437));
#18700=CARTESIAN_POINT('Ctrl Pts',(0.109298041309343,-0.110694858485372,
1.69569035814836));
#18701=CARTESIAN_POINT('Ctrl Pts',(0.105032569139117,-0.114804821627704,
1.69528741956143));
#18702=CARTESIAN_POINT('Ctrl Pts',(0.102028540804921,-0.117482593256126,
1.69500992031412));
#18703=CARTESIAN_POINT('Ctrl Pts',(0.0982538541989605,-0.120593272780645,
1.69466652874491));
#18704=CARTESIAN_POINT('Ctrl Pts',(0.0975787844512952,-0.121140158805345,
1.69460531547638));
#18705=CARTESIAN_POINT('Ctrl Pts',(0.096454506142932,-0.122035461544504,
1.69450367580057));
#18706=CARTESIAN_POINT('Ctrl Pts',(0.0960078991214324,-0.122387127265827,
1.69446337938529));
#18707=CARTESIAN_POINT('Ctrl Pts',(0.0951960336694066,-0.123019225009838,
1.6943902627325));
#18708=CARTESIAN_POINT('Ctrl Pts',(0.0948314366721004,-0.123300499426217,
1.69435747630302));
#18709=CARTESIAN_POINT('Ctrl Pts',(0.0940462976561442,-0.123900665627293,
1.69428697446816));
#18710=CARTESIAN_POINT('Ctrl Pts',(0.0936253719542922,-0.124219043465397,
1.69424923944512));
#18711=CARTESIAN_POINT('Ctrl Pts',(0.0924724870374513,-0.12508186849218,
1.69414604904736));
#18712=CARTESIAN_POINT('Ctrl Pts',(0.091737355735077,-0.12562202108412,
1.69408042800136));
#18713=CARTESIAN_POINT('Ctrl Pts',(0.087819326678101,-0.128448140427465,
1.69373157275498));
#18714=CARTESIAN_POINT('Ctrl Pts',(0.0845559194517856,-0.130619486613579,
1.69344401596673));
#18715=CARTESIAN_POINT('Ctrl Pts',(0.0686006736491443,-0.140386888143415,
1.69205050820341));
#18716=CARTESIAN_POINT('Ctrl Pts',(0.0549510210868276,-0.146269513419567,
1.69088465877147));
#18717=CARTESIAN_POINT('Ctrl Pts',(0.0364148689997084,-0.151292089567808,
1.68941729520283));
#18718=CARTESIAN_POINT('Ctrl Pts',(0.0321008433189015,-0.152265833028252,
1.68908425966835));
#18719=CARTESIAN_POINT('Ctrl Pts',(0.0271012745242674,-0.153172318264588,
1.68871207958855));
#18720=CARTESIAN_POINT('Ctrl Pts',(0.0264510568042694,-0.153285941296637,
1.68866394183213));
#18721=CARTESIAN_POINT('Ctrl Pts',(0.0254786767409904,-0.153449489345264,
1.68859236972694));
#18722=CARTESIAN_POINT('Ctrl Pts',(0.0251570602629359,-0.153502544190706,
1.68856876502321));
#18723=CARTESIAN_POINT('Ctrl Pts',(0.0245807756505278,-0.15359575004806,
1.68852659359464));
#18724=CARTESIAN_POINT('Ctrl Pts',(0.0243261734729441,-0.153636279088315,
1.6885080058772));
#18725=CARTESIAN_POINT('Ctrl Pts',(0.0237744438685795,-0.153722700682457,
1.68846782052689));
#18726=CARTESIAN_POINT('Ctrl Pts',(0.0234772846073057,-0.153768364750389,
1.68844623593852));
#18727=CARTESIAN_POINT('Ctrl Pts',(0.0226825125674879,-0.153888138690049,
1.68838865982359));
#18728=CARTESIAN_POINT('Ctrl Pts',(0.022184663753379,-0.15396069731827,
1.68835275437093));
#18729=CARTESIAN_POINT('Ctrl Pts',(0.0207276994924552,-0.15416582767185,
1.68824812194769));
#18730=CARTESIAN_POINT('Ctrl Pts',(0.0197676656421202,-0.154291864548211,
1.68817974064249));
#18731=CARTESIAN_POINT('Ctrl Pts',(0.0117002595409241,-0.155274447353317,
1.6876093631198));
#18732=CARTESIAN_POINT('Ctrl Pts',(0.00454170618044673,-0.155648488354195,
1.68713068333181));
#18733=CARTESIAN_POINT('Ctrl Pts',(-0.0151857048727512,-0.155316411781556,
1.68582582001257));
#18734=CARTESIAN_POINT('Ctrl Pts',(-0.0276801780676523,-0.153582471245924,
1.68501150631254));
#18735=CARTESIAN_POINT('Ctrl Pts',(-0.0418752221184455,-0.149822383142834,
1.68400173179385));
#18736=CARTESIAN_POINT('Ctrl Pts',(-0.0439094940949159,-0.149238856601813,
1.68385504424759));
#18737=CARTESIAN_POINT('Ctrl Pts',(-0.0471129417140584,-0.148248788398493,
1.68362052776947));
#18738=CARTESIAN_POINT('Ctrl Pts',(-0.0482903037082227,-0.147869465916276,
1.68353357278228));
#18739=CARTESIAN_POINT('Ctrl Pts',(-0.0500274918601302,-0.147286819065948,
1.68340408039277));
#18740=CARTESIAN_POINT('Ctrl Pts',(-0.0505908975013504,-0.147094248985235,
1.68336189641236));
#18741=CARTESIAN_POINT('Ctrl Pts',(-0.0515905862066681,-0.146746136037554,
1.68328670693969));
#18742=CARTESIAN_POINT('Ctrl Pts',(-0.0520273089034335,-0.146591869306822,
1.68325374395372));
#18743=CARTESIAN_POINT('Ctrl Pts',(-0.0529444080338,-0.146263301270018,
1.68318427577034));
#18744=CARTESIAN_POINT('Ctrl Pts',(-0.0534246266353773,-0.146088578943822,
1.68314775693024));
#18745=CARTESIAN_POINT('Ctrl Pts',(-0.0546787698962851,-0.145625261773817,
1.68305200312311));
#18746=CARTESIAN_POINT('Ctrl Pts',(-0.0554512631295895,-0.145332866594336,
1.68299264218823));
#18747=CARTESIAN_POINT('Ctrl Pts',(-0.0589214847480966,-0.14398766350857,
1.68272422422411));
#18748=CARTESIAN_POINT('Ctrl Pts',(-0.0615916560628935,-0.142865861636052,
1.68251287238652));
#18749=CARTESIAN_POINT('Ctrl Pts',(-0.0687469479031943,-0.1396218791372,
1.68193280630791));
#18750=CARTESIAN_POINT('Ctrl Pts',(-0.07316405003253,-0.137358744072712,
1.68155961454382));
#18751=CARTESIAN_POINT('Ctrl Pts',(-0.0837218573212822,-0.131295509928521,
1.6806308223803));
#18752=CARTESIAN_POINT('Ctrl Pts',(-0.0897206945410314,-0.127271541947837,
1.68007022374981));
#18753=CARTESIAN_POINT('Ctrl Pts',(-0.0987082351388976,-0.120290654484318,
1.67918843258652));
#18754=CARTESIAN_POINT('Ctrl Pts',(-0.101894438825308,-0.11760392757248,
1.67886664288369));
#18755=CARTESIAN_POINT('Ctrl Pts',(-0.105730888838739,-0.114095781323018,
1.67847045657023));
#18756=CARTESIAN_POINT('Ctrl Pts',(-0.106485776219649,-0.113391568151434,
1.6783920583149));
#18757=CARTESIAN_POINT('Ctrl Pts',(-0.109469377391134,-0.110552176207903,
1.67808059380407));
#18758=CARTESIAN_POINT('Ctrl Pts',(-0.111641529068101,-0.108358205449172,
1.67785019934036));
#18759=CARTESIAN_POINT('Ctrl Pts',(-0.114115999024375,-0.105705410009279,
1.67758481793004));
#18760=CARTESIAN_POINT('Ctrl Pts',(-0.114482805595466,-0.105308034758351,
1.67754540036274));
#18761=CARTESIAN_POINT('Ctrl Pts',(-0.115072580211439,-0.10466238636816,
1.67748190641606));
#18762=CARTESIAN_POINT('Ctrl Pts',(-0.115296830485323,-0.104415299274141,
1.67745773664183));
#18763=CARTESIAN_POINT('Ctrl Pts',(-0.115693396686145,-0.103975512911542,
1.67741494872579));
#18764=CARTESIAN_POINT('Ctrl Pts',(-0.115866028711086,-0.103783104196319,
1.67739630699268));
#18765=CARTESIAN_POINT('Ctrl Pts',(-0.116234898285699,-0.103369909412223,
1.6773564419577));
#18766=CARTESIAN_POINT('Ctrl Pts',(-0.116430986365507,-0.103148994998968,
1.67733522979475));
#18767=CARTESIAN_POINT('Ctrl Pts',(-0.116832064831628,-0.102694535824578,
1.67729179746501));
#18768=CARTESIAN_POINT('Ctrl Pts',(-0.117036987233973,-0.102460932480184,
1.67726958231469));
#18769=CARTESIAN_POINT('Ctrl Pts',(-0.117975589053052,-0.101384473995773,
1.67716770979881));
#18770=CARTESIAN_POINT('Ctrl Pts',(-0.118700898655694,-0.100534312698694,
1.67708864586632));
#18771=CARTESIAN_POINT('Ctrl Pts',(-0.124017663084639,-0.0941645775738576,
1.67650586116718));
#18772=CARTESIAN_POINT('Ctrl Pts',(-0.12823187938772,-0.0883400418125101,
1.67602561287012));
#18773=CARTESIAN_POINT('Ctrl Pts',(-0.135105043945632,-0.0773063737489884,
1.67516577306635));
#18774=CARTESIAN_POINT('Ctrl Pts',(-0.137901615269926,-0.0721996784829089,
1.67478508094758));
#18775=CARTESIAN_POINT('Ctrl Pts',(-0.14429005042737,-0.0588017038235194,
1.67380353963478));
#18776=CARTESIAN_POINT('Ctrl Pts',(-0.14745756184697,-0.0503337688795338,
1.67319805828984));
#18777=CARTESIAN_POINT('Ctrl Pts',(-0.150179245924141,-0.0405377002749772,
1.67248620391373));
#18778=CARTESIAN_POINT('Ctrl Pts',(-0.150473291748599,-0.0394322126766379,
1.67240573522298));
#18779=CARTESIAN_POINT('Ctrl Pts',(-0.1508991655586,-0.0377569358248633,
1.67228354188828));
#18780=CARTESIAN_POINT('Ctrl Pts',(-0.151040021851116,-0.0371894629089671,
1.67224210792303));
#18781=CARTESIAN_POINT('Ctrl Pts',(-0.151286427096358,-0.0361722664439251,
1.67216775443045));
#18782=CARTESIAN_POINT('Ctrl Pts',(-0.15139317903366,-0.0357228388698459,
1.67213487394908));
#18783=CARTESIAN_POINT('Ctrl Pts',(-0.151615167547079,-0.0347693943048376,
1.6720650546568));
#18784=CARTESIAN_POINT('Ctrl Pts',(-0.151729896008312,-0.0342652660291548,
1.67202810000512));
#18785=CARTESIAN_POINT('Ctrl Pts',(-0.151958238584241,-0.0332382689430707,
1.67195273538521));
#18786=CARTESIAN_POINT('Ctrl Pts',(-0.152071672269328,-0.0327153675799722,
1.67191432018145));
#18787=CARTESIAN_POINT('Ctrl Pts',(-0.152347430496839,-0.0314117615938241,
1.67181843846283));
#18788=CARTESIAN_POINT('Ctrl Pts',(-0.152506452286314,-0.0306303821785156,
1.67176086756998));
#18789=CARTESIAN_POINT('Ctrl Pts',(-0.154591595367232,-0.0199657264572257,
1.67097367949842));
#18790=CARTESIAN_POINT('Ctrl Pts',(-0.155559175245397,-0.00992182041362863,
1.67021316201263));
#18791=CARTESIAN_POINT('Ctrl Pts',(-0.155549934436305,0.000142817580648246,
1.66943657356483));
#18792=CARTESIAN_POINT('Ctrl Pts',(-0.155549934512386,0.000142734692933504,
1.66943657996045));
#18793=CARTESIAN_POINT('Ctrl Pts',(-0.155539137165992,0.0119095062458819,
1.6685286547989));
#18794=CARTESIAN_POINT('Ctrl Pts',(-0.154193252094498,0.0236380265554001,
1.6676035159115));
#18795=CARTESIAN_POINT('Ctrl Pts',(-0.151337655230667,0.0359652464455898,
1.66666617482456));
#18796=CARTESIAN_POINT('Ctrl Pts',(-0.151130694450945,0.0368252376739049,
1.66660098940656));
#18797=CARTESIAN_POINT('Ctrl Pts',(-0.150801489054699,0.0381436547827868,
1.66650142185785));
#18798=CARTESIAN_POINT('Ctrl Pts',(-0.150684468554527,0.0386033476928826,
1.66646677418678));
#18799=CARTESIAN_POINT('Ctrl Pts',(-0.150487433397983,0.0393628142365004,
1.66640965369194));
#18800=CARTESIAN_POINT('Ctrl Pts',(-0.150408622536469,0.0396628923111269,
1.66638711588306));
#18801=CARTESIAN_POINT('Ctrl Pts',(-0.150253114584839,0.040247870811502,
1.66634324428768));
#18802=CARTESIAN_POINT('Ctrl Pts',(-0.150176503741395,0.0405327925916355,
1.66632190575373));
#18803=CARTESIAN_POINT('Ctrl Pts',(-0.150031233585902,0.041066997726144,
1.66628195576479));
#18804=CARTESIAN_POINT('Ctrl Pts',(-0.149962764227588,0.0413163248639212,
1.66626333413331));
#18805=CARTESIAN_POINT('Ctrl Pts',(-0.149804362163746,0.0418875552102819,
1.66622072414155));
#18806=CARTESIAN_POINT('Ctrl Pts',(-0.149714013519591,0.0422093397995702,
1.66619676014939));
#18807=CARTESIAN_POINT('Ctrl Pts',(-0.149430701463523,0.0432060259544392,
1.66612264852466));
#18808=CARTESIAN_POINT('Ctrl Pts',(-0.14923420267766,0.0438799272961263,
1.66607270051438));
#18809=CARTESIAN_POINT('Ctrl Pts',(-0.147171696164676,0.0507792456934329,
1.66556278043678));
#18810=CARTESIAN_POINT('Ctrl Pts',(-0.144921546684449,0.0568841835550285,
1.66512353976677));
#18811=CARTESIAN_POINT('Ctrl Pts',(-0.14050220428334,0.0668927945026448,
1.66439574086609));
#18812=CARTESIAN_POINT('Ctrl Pts',(-0.138535671451816,0.0708758427997087,
1.66410392300456));
#18813=CARTESIAN_POINT('Ctrl Pts',(-0.133991836450683,0.0791651363283613,
1.66348177255836));
#18814=CARTESIAN_POINT('Ctrl Pts',(-0.131371266710808,0.0834417067831042,
1.66315166620737));
#18815=CARTESIAN_POINT('Ctrl Pts',(-0.12517581927803,0.0925348804722615,
1.66241681467428));
#18816=CARTESIAN_POINT('Ctrl Pts',(-0.121519943266147,0.0972860727935802,
1.66201061047322));
#18817=CARTESIAN_POINT('Ctrl Pts',(-0.116553790789091,0.103022177224845,
1.66148235382466));
#18818=CARTESIAN_POINT('Ctrl Pts',(-0.115489513312837,0.104213852873291,
1.66137039643182));
#18819=CARTESIAN_POINT('Ctrl Pts',(-0.114058271967494,0.105767566756887,
1.66122134764429));
#18820=CARTESIAN_POINT('Ctrl Pts',(-0.113707567033721,0.106144508900237,
1.66118494228352));
#18821=CARTESIAN_POINT('Ctrl Pts',(-0.113010548470682,0.106886254705663,
1.66111281232678));
#18822=CARTESIAN_POINT('Ctrl Pts',(-0.112664323758821,0.107251133568759,
1.66107709178419));
#18823=CARTESIAN_POINT('Ctrl Pts',(-0.111994324880774,0.107950406854623,
1.66100816975163));
#18824=CARTESIAN_POINT('Ctrl Pts',(-0.111670807098616,0.108285040420481,
1.66097497957913));
#18825=CARTESIAN_POINT('Ctrl Pts',(-0.110925552528462,0.109049009557853,
1.66089872404221));
#18826=CARTESIAN_POINT('Ctrl Pts',(-0.110502818544229,0.109477357312976,
1.66085561532559));
#18827=CARTESIAN_POINT('Ctrl Pts',(-0.109370904472022,0.110611067350389,
1.6607405656587));
#18828=CARTESIAN_POINT('Ctrl Pts',(-0.108657398884225,0.111312050318993,
1.66066843396511));
#18829=CARTESIAN_POINT('Ctrl Pts',(-0.103099606565561,0.116667942460483,
1.66010946271525));
#18830=CARTESIAN_POINT('Ctrl Pts',(-0.0979658329955401,0.121010779089143,
1.6596094160886));
#18831=CARTESIAN_POINT('Ctrl Pts',(-0.0843613742516448,0.131084872809554,
1.65832247287911));
#18832=CARTESIAN_POINT('Ctrl Pts',(-0.0755763720173321,0.136338799584819,
1.65752347763966));
#18833=CARTESIAN_POINT('Ctrl Pts',(-0.0654607327810812,0.141108618882644,
1.65666259874332));
#18834=CARTESIAN_POINT('Ctrl Pts',(-0.0645765368292703,0.141515442845773,
1.65658783762612));
#18835=CARTESIAN_POINT('Ctrl Pts',(-0.0636886255459746,0.141913922770335,
1.65651328069486));
#18836=CARTESIAN_POINT('Ctrl Pts',(-0.0636886598674488,0.141913907367419,
1.64281642759095));
#18837=CARTESIAN_POINT('Ctrl Pts',(-0.0696330708281112,0.139246152143079,
1.64332168031176));
#18838=CARTESIAN_POINT('Ctrl Pts',(-0.0754109669663114,0.136204428267244,
1.64382658077215));
#18839=CARTESIAN_POINT('Ctrl Pts',(-0.0832833891595775,0.131403626069983,
1.64452090893243));
#18840=CARTESIAN_POINT('Ctrl Pts',(-0.0855430853569352,0.129943906277431,
1.64472095711442));
#18841=CARTESIAN_POINT('Ctrl Pts',(-0.0882139005972584,0.12811872317121,
1.64495730235532));
#18842=CARTESIAN_POINT('Ctrl Pts',(-0.0886622273260183,0.12780887666781,
1.64499697193528));
#18843=CARTESIAN_POINT('Ctrl Pts',(-0.0893563051957705,0.127323777480203,
1.64505836938074));
#18844=CARTESIAN_POINT('Ctrl Pts',(-0.08960318421742,0.12715015915208,1.64508020466903));
#18845=CARTESIAN_POINT('Ctrl Pts',(-0.0900598428983295,0.126827022189883,
1.64512058536336));
#18846=CARTESIAN_POINT('Ctrl Pts',(-0.0902697544971528,0.126677702400157,
1.64513914343452));
#18847=CARTESIAN_POINT('Ctrl Pts',(-0.0907429770297453,0.126339303854352,
1.64518097319549));
#18848=CARTESIAN_POINT('Ctrl Pts',(-0.0910060678913912,0.12614992346714,
1.64520422381417));
#18849=CARTESIAN_POINT('Ctrl Pts',(-0.0917792790783532,0.125589665965622,
1.64527254814335));
#18850=CARTESIAN_POINT('Ctrl Pts',(-0.0922877464173775,0.125216501161205,
1.64531746810929));
#18851=CARTESIAN_POINT('Ctrl Pts',(-0.0958922898108027,0.122537238655754,
1.64563594524948));
#18852=CARTESIAN_POINT('Ctrl Pts',(-0.0989041643992458,0.120119435183958,
1.64590226541571));
#18853=CARTESIAN_POINT('Ctrl Pts',(-0.111212056617696,0.109461978895362,
1.64700659241976));
#18854=CARTESIAN_POINT('Ctrl Pts',(-0.119593975365025,0.100236594805785,
1.64780253800066));
#18855=CARTESIAN_POINT('Ctrl Pts',(-0.129343642028543,0.0865185434543424,
1.648927809384));
#18856=CARTESIAN_POINT('Ctrl Pts',(-0.131743353118494,0.0828185961175443,
1.64922596428644));
#18857=CARTESIAN_POINT('Ctrl Pts',(-0.135339569960334,0.0767211732355931,
1.64971348892717));
#18858=CARTESIAN_POINT('Ctrl Pts',(-0.136636999311302,0.0743859297701268,
1.64989933389391));
#18859=CARTESIAN_POINT('Ctrl Pts',(-0.13824533020108,0.0713069127118367,
1.65014383348089));
#18860=CARTESIAN_POINT('Ctrl Pts',(-0.138611538128635,0.0705924116116407,
1.65020053306397));
#18861=CARTESIAN_POINT('Ctrl Pts',(-0.139198355740396,0.0694253104936047,
1.65029310342311));
#18862=CARTESIAN_POINT('Ctrl Pts',(-0.139422331690481,0.0689744111471147,
1.65032885619316));
#18863=CARTESIAN_POINT('Ctrl Pts',(-0.139848993042136,0.068104904046188,
1.65039778430641));
#18864=CARTESIAN_POINT('Ctrl Pts',(-0.140051998053364,0.0676864583403743,
1.65043094809085));
#18865=CARTESIAN_POINT('Ctrl Pts',(-0.140512695921535,0.0667258951248426,
1.65050706362396));
#18866=CARTESIAN_POINT('Ctrl Pts',(-0.140769132144931,0.0661831867759373,
1.65055005825754));
#18867=CARTESIAN_POINT('Ctrl Pts',(-0.141442373725473,0.0647367580688794,
1.65066462960091));
#18868=CARTESIAN_POINT('Ctrl Pts',(-0.141853652048706,0.0638305118669644,
1.65073639462226));
#18869=CARTESIAN_POINT('Ctrl Pts',(-0.144894198105596,0.0569561672351944,
1.65128071634126));
#18870=CARTESIAN_POINT('Ctrl Pts',(-0.147154115014761,0.0508328387688611,
1.65176569269126));
#18871=CARTESIAN_POINT('Ctrl Pts',(-0.152609498950707,0.0325991504708884,
1.65321090196849));
#18872=CARTESIAN_POINT('Ctrl Pts',(-0.154736235093912,0.0202242079391262,
1.65419674266683));
#18873=CARTESIAN_POINT('Ctrl Pts',(-0.155486463517174,0.00514398693103164,
1.65534527268703));
#18874=CARTESIAN_POINT('Ctrl Pts',(-0.155550535912096,0.00255606724769628,
1.65554031219657));
#18875=CARTESIAN_POINT('Ctrl Pts',(-0.155549684800338,-0.00152922855669905,
1.65584381983182));
#18876=CARTESIAN_POINT('Ctrl Pts',(-0.155527767599779,-0.00302604029328143,
1.65595409233396));
#18877=CARTESIAN_POINT('Ctrl Pts',(-0.155470640415711,-0.00499013556192593,
1.65609737461512));
#18878=CARTESIAN_POINT('Ctrl Pts',(-0.15545492428974,-0.00545783964186859,
1.65613138851678));
#18879=CARTESIAN_POINT('Ctrl Pts',(-0.15542624885748,-0.00621005391579775,
1.65618591631687));
#18880=CARTESIAN_POINT('Ctrl Pts',(-0.155414618645756,-0.00649460686367938,
1.6562065026805));
#18881=CARTESIAN_POINT('Ctrl Pts',(-0.155390829282578,-0.00703994525832174,
1.65624587568077));
#18882=CARTESIAN_POINT('Ctrl Pts',(-0.155378795250698,-0.00730072886467567,
1.6562646686136));
#18883=CARTESIAN_POINT('Ctrl Pts',(-0.155348921076262,-0.00791455449382164,
1.6563088215818));
#18884=CARTESIAN_POINT('Ctrl Pts',(-0.155330533965986,-0.00826756777560345,
1.65633415087878));
#18885=CARTESIAN_POINT('Ctrl Pts',(-0.155266286447439,-0.00942507830682467,
1.65641700591314));
#18886=CARTESIAN_POINT('Ctrl Pts',(-0.155215377120556,-0.010229300459691,
1.65647425819608));
#18887=CARTESIAN_POINT('Ctrl Pts',(-0.155079624390963,-0.0121383854708783,
1.65660949677501));
#18888=CARTESIAN_POINT('Ctrl Pts',(-0.154989219180336,-0.0132428249859943,
1.65668720227188));
#18889=CARTESIAN_POINT('Ctrl Pts',(-0.154617457942235,-0.0172564884077534,
1.65696796573091));
#18890=CARTESIAN_POINT('Ctrl Pts',(-0.154265910475499,-0.0201587693636289,
1.65716787423104));
#18891=CARTESIAN_POINT('Ctrl Pts',(-0.152660455799996,-0.0308735473163772,
1.6579000569243));
#18892=CARTESIAN_POINT('Ctrl Pts',(-0.150892899133274,-0.0385971554754417,
1.65841670732667));
#18893=CARTESIAN_POINT('Ctrl Pts',(-0.145417038713349,-0.0562213604750931,
1.65963272517138));
#18894=CARTESIAN_POINT('Ctrl Pts',(-0.14127393965906,-0.0659437576669107,
1.66033395098969));
#18895=CARTESIAN_POINT('Ctrl Pts',(-0.135630689927324,-0.0761669931610973,
1.66115162361125));
#18896=CARTESIAN_POINT('Ctrl Pts',(-0.135070416611611,-0.0771561879066619,
1.66123159960294));
#18897=CARTESIAN_POINT('Ctrl Pts',(-0.13420646198002,-0.0786432962058877,
1.66135318233756));
#18898=CARTESIAN_POINT('Ctrl Pts',(-0.133910731248095,-0.0791458054172151,
1.66139450267861));
#18899=CARTESIAN_POINT('Ctrl Pts',(-0.133375814087743,-0.0800431622486336,
1.66146872148062));
#18900=CARTESIAN_POINT('Ctrl Pts',(-0.133137680665298,-0.0804386324161293,
1.66150158138257));
#18901=CARTESIAN_POINT('Ctrl Pts',(-0.132628757659542,-0.0812753540107831,
1.66157143026112));
#18902=CARTESIAN_POINT('Ctrl Pts',(-0.132357519081919,-0.081716324308003,
1.6616084353776));
#18903=CARTESIAN_POINT('Ctrl Pts',(-0.131626074080158,-0.0828922862668488,
1.66170764307559));
#18904=CARTESIAN_POINT('Ctrl Pts',(-0.131161920090704,-0.0836247879630223,
1.66176999046477));
#18905=CARTESIAN_POINT('Ctrl Pts',(-0.128878585763506,-0.087162439543451,
1.66207383103529));
#18906=CARTESIAN_POINT('Ctrl Pts',(-0.126975542748679,-0.0899121186349089,
1.66231842819615));
#18907=CARTESIAN_POINT('Ctrl Pts',(-0.116045692141403,-0.104664819909547,
1.66367941556095));
#18908=CARTESIAN_POINT('Ctrl Pts',(-0.105406201266564,-0.115371964736592,
1.66486106855164));
#18909=CARTESIAN_POINT('Ctrl Pts',(-0.0927583720169072,-0.124869270264632,
1.6660726566817));
#18910=CARTESIAN_POINT('Ctrl Pts',(-0.0921110448530989,-0.12534753962072,
1.66613416883196));
#18911=CARTESIAN_POINT('Ctrl Pts',(-0.0904911099740408,-0.126525081974917,
1.66628682152846));
#18912=CARTESIAN_POINT('Ctrl Pts',(-0.0895140652474005,-0.1272181969108,
1.66637775821602));
#18913=CARTESIAN_POINT('Ctrl Pts',(-0.0860956409361392,-0.129584342684377,
1.66669178116432));
#18914=CARTESIAN_POINT('Ctrl Pts',(-0.0836143996295749,-0.131199072049607,
1.66691249641876));
#18915=CARTESIAN_POINT('Ctrl Pts',(-0.0806327420107087,-0.133020481491082,
1.66716805035641));
#18916=CARTESIAN_POINT('Ctrl Pts',(-0.0801756623993111,-0.133296476927886,
1.66720696381084));
#18917=CARTESIAN_POINT('Ctrl Pts',(-0.0794324578715335,-0.133740035384074,
1.66726980156947));
#18918=CARTESIAN_POINT('Ctrl Pts',(-0.0791472077299594,-0.133909043541375,
1.66729381626074));
#18919=CARTESIAN_POINT('Ctrl Pts',(-0.0786388476163664,-0.134208050502176,
1.66733642809792));
#18920=CARTESIAN_POINT('Ctrl Pts',(-0.0784159528092604,-0.134338406730369,
1.66735504814494));
#18921=CARTESIAN_POINT('Ctrl Pts',(-0.0779363488900173,-0.134617294500187,
1.66739497625711));
#18922=CARTESIAN_POINT('Ctrl Pts',(-0.0776795399353789,-0.134765646721615,
1.66741627271742));
#18923=CARTESIAN_POINT('Ctrl Pts',(-0.0769703944147217,-0.135172602115724,
1.66747485499864));
#18924=CARTESIAN_POINT('Ctrl Pts',(-0.0765171746668741,-0.135429671715231,
1.66751204362349));
#18925=CARTESIAN_POINT('Ctrl Pts',(-0.0740438155234889,-0.136816199528646,
1.66771367587367));
#18926=CARTESIAN_POINT('Ctrl Pts',(-0.0719998140710258,-0.137902818643324,
1.66787554369753));
#18927=CARTESIAN_POINT('Ctrl Pts',(-0.0570948028164132,-0.145404716711965,
1.66902758374665));
#18928=CARTESIAN_POINT('Ctrl Pts',(-0.0434225200963941,-0.150056473541935,
1.6699402891408));
#18929=CARTESIAN_POINT('Ctrl Pts',(-0.0263668142056738,-0.153328210403919,
1.67110271705952));
#18930=CARTESIAN_POINT('Ctrl Pts',(-0.023413799724451,-0.153806831536226,
1.67130453543832));
#18931=CARTESIAN_POINT('Ctrl Pts',(-0.0168406777585501,-0.15467851383071,
1.67175701362771));
#18932=CARTESIAN_POINT('Ctrl Pts',(-0.0132169975193409,-0.155030185554693,
1.67200863604789));
#18933=CARTESIAN_POINT('Ctrl Pts',(-0.00866347803873654,-0.155311294684052,
1.6723290736954));
#18934=CARTESIAN_POINT('Ctrl Pts',(-0.00774193572927483,-0.155359957755644,
1.67239413894371));
#18935=CARTESIAN_POINT('Ctrl Pts',(-0.00628508900860785,-0.155423894146872,
1.67249736250885));
#18936=CARTESIAN_POINT('Ctrl Pts',(-0.00575003410384543,-0.155444608495739,
1.67253535068103));
#18937=CARTESIAN_POINT('Ctrl Pts',(-0.00475537792328659,-0.155477973580735,
1.67260611849973));
#18938=CARTESIAN_POINT('Ctrl Pts',(-0.00429580540813051,-0.155491350034431,
1.67263887510052));
#18939=CARTESIAN_POINT('Ctrl Pts',(-0.00327810358583532,-0.155516456303218,
1.6727115468847));
#18940=CARTESIAN_POINT('Ctrl Pts',(-0.00271995908620184,-0.15552721932762,
1.6727514918256));
#18941=CARTESIAN_POINT('Ctrl Pts',(-0.00110780371142387,-0.155549626620776,
1.67286713403311));
#18942=CARTESIAN_POINT('Ctrl Pts',(-5.37351301366745E-5,-0.155553561777881,
1.67294307053711));
#18943=CARTESIAN_POINT('Ctrl Pts',(0.0078371315832451,-0.155502818304252,
1.67351408898011));
#18944=CARTESIAN_POINT('Ctrl Pts',(0.0146625772559204,-0.155008161139295,
1.67402284845758));
#18945=CARTESIAN_POINT('Ctrl Pts',(0.0322087304461537,-0.152567279615475,
1.67536978566281));
#18946=CARTESIAN_POINT('Ctrl Pts',(0.0427976767973349,-0.149941669114859,
1.67622289292575));
#18947=CARTESIAN_POINT('Ctrl Pts',(0.0542038428614482,-0.145805758563602,
1.6771537820205));
#18948=CARTESIAN_POINT('Ctrl Pts',(0.0553778441067607,-0.14536392376341,
1.67724970476158));
#18949=CARTESIAN_POINT('Ctrl Pts',(0.0602028331178171,-0.143481102364144,
1.67764407956139));
#18950=CARTESIAN_POINT('Ctrl Pts',(0.0638043615254592,-0.141916235491553,
1.67793882653811));
#18951=CARTESIAN_POINT('Ctrl Pts',(0.067913959592622,-0.139942479369938,
1.67827263124267));
#18952=CARTESIAN_POINT('Ctrl Pts',(0.068483073974055,-0.139664856194405,
1.67831879968475));
#18953=CARTESIAN_POINT('Ctrl Pts',(0.0693414430730594,-0.139239621522635,
1.67838832772092));
#18954=CARTESIAN_POINT('Ctrl Pts',(0.0696319475470539,-0.139094571480213,
1.67841184020019));
#18955=CARTESIAN_POINT('Ctrl Pts',(0.0701521421251393,-0.138832798119229,
1.67845390713552));
#18956=CARTESIAN_POINT('Ctrl Pts',(0.0703819971923152,-0.138716413423375,
1.67847248218063));
#18957=CARTESIAN_POINT('Ctrl Pts',(0.0708801245158005,-0.138462635000128,
1.67851270874644));
#18958=CARTESIAN_POINT('Ctrl Pts',(0.0711482862031795,-0.138325032865015,
1.67853434692692));
#18959=CARTESIAN_POINT('Ctrl Pts',(0.0718985058007074,-0.137937312925557,
1.6785948388176));
#18960=CARTESIAN_POINT('Ctrl Pts',(0.0723796627695605,-0.137685445397633,
1.67863358460929));
#18961=CARTESIAN_POINT('Ctrl Pts',(0.0752073851927819,-0.13618631961288,
1.67886104884831));
#18962=CARTESIAN_POINT('Ctrl Pts',(0.0775231779717367,-0.134881516871162,
1.6790463491165));
#18963=CARTESIAN_POINT('Ctrl Pts',(0.0923867584467787,-0.125997451889897,
1.68023683690014));
#18964=CARTESIAN_POINT('Ctrl Pts',(0.103843963428959,-0.116735633874203,
1.68116633271599));
#18965=CARTESIAN_POINT('Ctrl Pts',(0.115172767310384,-0.104569996036062,
1.68228329354739));
#18966=CARTESIAN_POINT('Ctrl Pts',(0.116482263970444,-0.103109321267012,
1.68241585518357));
#18967=CARTESIAN_POINT('Ctrl Pts',(0.120348004786674,-0.0986296439602964,
1.68281858515854));
#18968=CARTESIAN_POINT('Ctrl Pts',(0.12281687951383,-0.0955377331799848,
1.68309153308614));
#18969=CARTESIAN_POINT('Ctrl Pts',(0.125678045156998,-0.0916601215768736,
1.6834298729078));
#18970=CARTESIAN_POINT('Ctrl Pts',(0.126185195648886,-0.0909606797874612,
1.68349074897831));
#18971=CARTESIAN_POINT('Ctrl Pts',(0.127015395210541,-0.0897953963022938,
1.68359193766495));
#18972=CARTESIAN_POINT('Ctrl Pts',(0.127341776185319,-0.089331941880324,
1.68363212225834));
#18973=CARTESIAN_POINT('Ctrl Pts',(0.127928551282849,-0.0884889828633044,
1.68370510988962));
#18974=CARTESIAN_POINT('Ctrl Pts',(0.128189809387703,-0.0881100850204399,
1.68373787959695));
#18975=CARTESIAN_POINT('Ctrl Pts',(0.128747535538402,-0.0872934937996512,
1.68380842776158));
#18976=CARTESIAN_POINT('Ctrl Pts',(0.129043460713491,-0.0868554385246392,
1.68384622618183));
#18977=CARTESIAN_POINT('Ctrl Pts',(0.129846409855484,-0.0856536786309938,
1.68394980090174));
#18978=CARTESIAN_POINT('Ctrl Pts',(0.130348917824022,-0.0848869976536648,
1.68401574503198));
#18979=CARTESIAN_POINT('Ctrl Pts',(0.132999277386099,-0.080764291726573,
1.68436969391954));
#18980=CARTESIAN_POINT('Ctrl Pts',(0.13502416931733,-0.0773314096988657,
1.68466217351912));
#18981=CARTESIAN_POINT('Ctrl Pts',(0.143909515226997,-0.0608527305361322,
1.68605747249563));
#18982=CARTESIAN_POINT('Ctrl Pts',(0.14902438131944,-0.046953113821582,
1.6872193210833));
#18983=CARTESIAN_POINT('Ctrl Pts',(0.153027406998455,-0.0282447476203451,
1.68868092412717));
#18984=CARTESIAN_POINT('Ctrl Pts',(0.153765034917613,-0.0239055639275688,
1.68901232356463));
#18985=CARTESIAN_POINT('Ctrl Pts',(0.154400573580371,-0.0188865011680879,
1.68938288971926));
#18986=CARTESIAN_POINT('Ctrl Pts',(0.154479227788622,-0.0182319848580721,
1.68943096519793));
#18987=CARTESIAN_POINT('Ctrl Pts',(0.154590527217519,-0.017253332784338,
1.68950245856718));
#18988=CARTESIAN_POINT('Ctrl Pts',(0.154626317708848,-0.0169295739653336,
1.68952604632471));
#18989=CARTESIAN_POINT('Ctrl Pts',(0.154688603530453,-0.0163494603590062,
1.68956819405555));
#18990=CARTESIAN_POINT('Ctrl Pts',(0.154715478881031,-0.0160931511633394,
1.6895867749655));
#18991=CARTESIAN_POINT('Ctrl Pts',(0.154772325683636,-0.0155376987664653,
1.68962695276701));
#18992=CARTESIAN_POINT('Ctrl Pts',(0.154802066870917,-0.0152385359251876,
1.68964853659093));
#18993=CARTESIAN_POINT('Ctrl Pts',(0.15488276067512,-0.0144022243222315,
1.68970872356026));
#18994=CARTESIAN_POINT('Ctrl Pts',(0.154931786791348,-0.0138648867450967,
1.68974722053324));
#18995=CARTESIAN_POINT('Ctrl Pts',(0.155200676341018,-0.0107380728470826,
1.6899702854882));
#18996=CARTESIAN_POINT('Ctrl Pts',(0.155358431275879,-0.00814347085545896,
1.69015158768149));
#18997=CARTESIAN_POINT('Ctrl Pts',(0.155975385435482,0.00914959567733008,
1.69134207364734));
#18998=CARTESIAN_POINT('Ctrl Pts',(0.154413352523018,0.0238466180257112,
1.69227428366037));
#18999=CARTESIAN_POINT('Ctrl Pts',(0.15034687495937,0.0399398757435825,
1.6933894720056));
#19000=CARTESIAN_POINT('Ctrl Pts',(0.149850374205536,0.0417641165950445,
1.69351718634346));
#19001=CARTESIAN_POINT('Ctrl Pts',(0.148190441517036,0.0474517992128966,
1.69392019827623));
#19002=CARTESIAN_POINT('Ctrl Pts',(0.146909960643382,0.0512790292291801,
1.69419847241471));
#19003=CARTESIAN_POINT('Ctrl Pts',(0.145174573974553,0.0558650286124685,
1.69454270902867));
#19004=CARTESIAN_POINT('Ctrl Pts',(0.144860073122485,0.0566755459689623,
1.69460396422499));
#19005=CARTESIAN_POINT('Ctrl Pts',(0.144328698412257,0.0580116587106637,
1.69470565229256));
#19006=CARTESIAN_POINT('Ctrl Pts',(0.144115704695172,0.0585387852315177,
1.69474595488943));
#19007=CARTESIAN_POINT('Ctrl Pts',(0.143725023936878,0.0594906036513178,
1.6948190683612));
#19008=CARTESIAN_POINT('Ctrl Pts',(0.143548331354511,0.0599156989898146,
1.69485184536161));
#19009=CARTESIAN_POINT('Ctrl Pts',(0.143165169928412,0.0608261027120477,
1.69492231089825));
#19010=CARTESIAN_POINT('Ctrl Pts',(0.142958115235106,0.0613111566319243,
1.69496001897018));
#19011=CARTESIAN_POINT('Ctrl Pts',(0.142386678232713,0.0626311929415151,
1.6950630946148));
#19012=CARTESIAN_POINT('Ctrl Pts',(0.142017425788805,0.0634640305538876,
1.69512862731331));
#19013=CARTESIAN_POINT('Ctrl Pts',(0.1400270637585,0.0678488653660929,1.69547635632691));
#19014=CARTESIAN_POINT('Ctrl Pts',(0.138280100457666,0.0713418241189861,
1.69576284263471));
#19015=CARTESIAN_POINT('Ctrl Pts',(0.12929312704414,0.0877379337101477,
1.69715543865748));
#19016=CARTESIAN_POINT('Ctrl Pts',(0.120368473044545,0.0996290235350693,
1.69832156987168));
#19017=CARTESIAN_POINT('Ctrl Pts',(0.106766568743113,0.113209292569439,
1.69979027804044));
#19018=CARTESIAN_POINT('Ctrl Pts',(0.103497486430046,0.116205522633102,
1.70012423338428));
#19019=CARTESIAN_POINT('Ctrl Pts',(0.0995991367852806,0.119483264264915,
1.70049730306448));
#19020=CARTESIAN_POINT('Ctrl Pts',(0.0990910336566504,0.119904985628396,
1.70054545890344));
#19021=CARTESIAN_POINT('Ctrl Pts',(0.0983281183143945,0.120530037289042,
1.70061704800486));
#19022=CARTESIAN_POINT('Ctrl Pts',(0.098075336429289,0.120735815439028,
1.70064065179217));
#19023=CARTESIAN_POINT('Ctrl Pts',(0.0976215204798244,0.121102880493464,
1.70068281677014));
#19024=CARTESIAN_POINT('Ctrl Pts',(0.0974207315975459,0.121264462985403,
1.70070139897141));
#19025=CARTESIAN_POINT('Ctrl Pts',(0.096984982316196,0.121613346260353,
1.70074156658287));
#19026=CARTESIAN_POINT('Ctrl Pts',(0.0967498811808077,0.121800465020371,
1.70076313898286));
#19027=CARTESIAN_POINT('Ctrl Pts',(0.0960916814512226,0.122321222926369,
1.70082326192739));
#19028=CARTESIAN_POINT('Ctrl Pts',(0.0956673837028532,0.122653351119015,
1.70086170666449));
#19029=CARTESIAN_POINT('Ctrl Pts',(0.0931962540677215,0.124567056451588,
1.70108386208888));
#19030=CARTESIAN_POINT('Ctrl Pts',(0.0911117975507876,0.126099705730657,
1.70126433803457));
#19031=CARTESIAN_POINT('Ctrl Pts',(0.0769212176750395,0.135997972692268,
1.70245483375188));
#19032=CARTESIAN_POINT('Ctrl Pts',(0.0637179849680319,0.142662012931959,
1.70338761203266));
#19033=CARTESIAN_POINT('Ctrl Pts',(0.0479955919389848,0.147972116324583,
1.70450249562277));
#19034=CARTESIAN_POINT('Ctrl Pts',(0.0462070074747395,0.148540351839447,
1.70462926152316));
#19035=CARTESIAN_POINT('Ctrl Pts',(0.0405270475174182,0.150232368714803,
1.70503233660449));
#19036=CARTESIAN_POINT('Ctrl Pts',(0.0366021100722138,0.15123652616071,
1.70531166074971));
#19037=CARTESIAN_POINT('Ctrl Pts',(0.0317916694146205,0.152269005188088,
1.70565705911394));
#19038=CARTESIAN_POINT('Ctrl Pts',(0.0309390982600143,0.152444522135648,
1.70571838780001));
#19039=CARTESIAN_POINT('Ctrl Pts',(0.0295269941928091,0.152722895196094,
1.70582017265145));
#19040=CARTESIAN_POINT('Ctrl Pts',(0.0289682817630957,0.152829855523179,
1.70586049810404));
#19041=CARTESIAN_POINT('Ctrl Pts',(0.0279563649510032,0.153017829381643,
1.70593363601026));
#19042=CARTESIAN_POINT('Ctrl Pts',(0.0275033614987932,0.153099900548161,
1.70596641448408));
#19043=CARTESIAN_POINT('Ctrl Pts',(0.0265308740041513,0.153271631834918,
1.70603686430812));
#19044=CARTESIAN_POINT('Ctrl Pts',(0.0260112865099643,0.15336066432507,
1.70607455511215));
#19045=CARTESIAN_POINT('Ctrl Pts',(0.0246403235618893,0.153588414389331,
1.70617414285442));
#19046=CARTESIAN_POINT('Ctrl Pts',(0.0237882399181991,0.153722692422995,
1.70623617923938));
#19047=CARTESIAN_POINT('Ctrl Pts',(0.0194753583731613,0.154365633256455,
1.70655093027577));
#19048=CARTESIAN_POINT('Ctrl Pts',(0.0159994862901673,0.15476450204419,
1.70680706561581));
#19049=CARTESIAN_POINT('Ctrl Pts',(-0.00253453420130531,0.156260337500092,
1.70818732570391));
#19050=CARTESIAN_POINT('Ctrl Pts',(-0.017677856791741,0.155277312488693,
1.70937668862919));
#19051=CARTESIAN_POINT('Ctrl Pts',(-0.0339945702669225,0.151798243479703,
1.71065271643613));
#19052=CARTESIAN_POINT('Ctrl Pts',(-0.0355466066846262,0.151442321075664,
1.71077391313104));
#19053=CARTESIAN_POINT('Ctrl Pts',(-0.0400948938486527,0.150325503416693,
1.71112809218911));
#19054=CARTESIAN_POINT('Ctrl Pts',(-0.043074476475213,0.149498998094757,
1.71135884752414));
#19055=CARTESIAN_POINT('Ctrl Pts',(-0.0465443836294818,0.14842410664082,
1.71162458566063));
#19056=CARTESIAN_POINT('Ctrl Pts',(-0.0470602389120831,0.14826135375155,
1.71166401282278));
#19057=CARTESIAN_POINT('Ctrl Pts',(-0.0478929114937225,0.147993860868635,
1.71172751517046));
#19058=CARTESIAN_POINT('Ctrl Pts',(-0.0482102530516723,0.147890788531662,
1.71175168382805));
#19059=CARTESIAN_POINT('Ctrl Pts',(-0.0487727917824953,0.147706073216984,
1.71179446527758));
#19060=CARTESIAN_POINT('Ctrl Pts',(-0.0490181190927283,0.147624839671233,
1.71181310167686));
#19061=CARTESIAN_POINT('Ctrl Pts',(-0.0495432762298786,0.147449494532381,
1.7118529500133));
#19062=CARTESIAN_POINT('Ctrl Pts',(-0.0498230402452061,0.147355197811706,
1.71187415084166));
#19063=CARTESIAN_POINT('Ctrl Pts',(-0.0505802082159241,0.147097585359871,
1.71193146008684));
#19064=CARTESIAN_POINT('Ctrl Pts',(-0.0510570944556044,0.146932740417311,
1.71196747978987));
#19065=CARTESIAN_POINT('Ctrl Pts',(-0.0535251601482233,0.146066138891908,
1.71215354612816));
#19066=CARTESIAN_POINT('Ctrl Pts',(-0.0555028290526461,0.145326174028104,
1.71230146085976));
#19067=CARTESIAN_POINT('Ctrl Pts',(-0.0595584335563164,0.143713850590068,
1.71260355222163));
#19068=CARTESIAN_POINT('Ctrl Pts',(-0.0616334814827387,0.142836237505129,
1.71275743129292));
#19069=CARTESIAN_POINT('Ctrl Pts',(-0.0636886260955797,0.141913922523681,
1.71290984779881));
#19070=CARTESIAN_POINT('Origin',(0.,0.,-0.129405622560373));
#19071=CARTESIAN_POINT('',(-0.0636886042805274,0.141913932313915,1.79664456958818));
#19072=CARTESIAN_POINT('',(-0.0636886300450479,0.141913920751225,1.78267615293977));
#19073=CARTESIAN_POINT('',(-0.0636886258329924,0.141913922641526,-0.129405622560373));
#19074=CARTESIAN_POINT('Ctrl Pts',(-0.0636886042805435,0.141913932313908,
1.79664456958818));
#19075=CARTESIAN_POINT('Ctrl Pts',(-0.0614297561867433,0.142927665638256,
1.79648079782229));
#19076=CARTESIAN_POINT('Ctrl Pts',(-0.059145515988598,0.143888001777509,
1.79631627691133));
#19077=CARTESIAN_POINT('Ctrl Pts',(-0.0527327728000258,0.146405273857401,
1.7958556637672));
#19078=CARTESIAN_POINT('Ctrl Pts',(-0.0485614736293651,0.147841224542857,
1.79555741037763));
#19079=CARTESIAN_POINT('Ctrl Pts',(-0.0417739006076907,0.149859545289724,
1.79506972800745));
#19080=CARTESIAN_POINT('Ctrl Pts',(-0.0391936775312136,0.150554960846653,
1.79488382624486));
#19081=CARTESIAN_POINT('Ctrl Pts',(-0.0358163629284328,0.151372506336316,
1.79463925097973));
#19082=CARTESIAN_POINT('Ctrl Pts',(-0.0350343331617838,0.15155541225724,
1.79458253373647));
#19083=CARTESIAN_POINT('Ctrl Pts',(-0.0337596684824227,0.151843145793434,
1.79448993421611));
#19084=CARTESIAN_POINT('Ctrl Pts',(-0.0332678716153356,0.151951652994638,
1.79445417001827));
#19085=CARTESIAN_POINT('Ctrl Pts',(-0.0323207632470261,0.152155799149134,
1.79438521960791));
#19086=CARTESIAN_POINT('Ctrl Pts',(-0.031865531871939,0.15225178758049,
1.79435204496081));
#19087=CARTESIAN_POINT('Ctrl Pts',(-0.0308218024391521,0.15246697849679,
1.79427590406428));
#19088=CARTESIAN_POINT('Ctrl Pts',(-0.0302330342769231,0.152584817911995,
1.7942328949001));
#19089=CARTESIAN_POINT('Ctrl Pts',(-0.0286662985969709,0.152888969355366,
1.79411828366799));
#19090=CARTESIAN_POINT('Ctrl Pts',(-0.0276872138123964,0.153069303687585,
1.79404649315364));
#19091=CARTESIAN_POINT('Ctrl Pts',(-0.0202760461716728,0.154360911349842,
1.7935017247999));
#19092=CARTESIAN_POINT('Ctrl Pts',(-0.0137824124696716,0.155075567007255,
1.79301630472144));
#19093=CARTESIAN_POINT('Ctrl Pts',(0.00413527026421228,0.155913203716126,
1.79165419749622));
#19094=CARTESIAN_POINT('Ctrl Pts',(0.0155582255594549,0.155189985203871,
1.79075829529241));
#19095=CARTESIAN_POINT('Ctrl Pts',(0.0300745935375249,0.15265119873261,
1.78962949936132));
#19096=CARTESIAN_POINT('Ctrl Pts',(0.0333326124151484,0.151973056529895,
1.78937708450784));
#19097=CARTESIAN_POINT('Ctrl Pts',(0.0377435759024,0.150906233401039,1.78903863983636));
#19098=CARTESIAN_POINT('Ctrl Pts',(0.0389172324148559,0.150607828637981,
1.78894891178945));
#19099=CARTESIAN_POINT('Ctrl Pts',(0.0406607787106198,0.150142784755903,
1.78881621507753));
#19100=CARTESIAN_POINT('Ctrl Pts',(0.0412333609081846,0.149986548454196,
1.78877273446958));
#19101=CARTESIAN_POINT('Ctrl Pts',(0.0422668048210996,0.149698194814547,
1.78869444982059));
#19102=CARTESIAN_POINT('Ctrl Pts',(0.0427279731440021,0.149567217824945,
1.78865958543256));
#19103=CARTESIAN_POINT('Ctrl Pts',(0.0434506720264532,0.149358347791677,
1.78860506662737));
#19104=CARTESIAN_POINT('Ctrl Pts',(0.0437126102944892,0.149281896621743,
1.7885853308385));
#19105=CARTESIAN_POINT('Ctrl Pts',(0.0442216398803071,0.149131872955087,
1.78854702692104));
#19106=CARTESIAN_POINT('Ctrl Pts',(0.0444687467635335,0.149058376242083,
1.78852845518331));
#19107=CARTESIAN_POINT('Ctrl Pts',(0.0450278572064945,0.148890566563971,
1.78848648491731));
#19108=CARTESIAN_POINT('Ctrl Pts',(0.0453397471599194,0.148795887272133,
1.78846310802776));
#19109=CARTESIAN_POINT('Ctrl Pts',(0.0462822324077931,0.148506541947426,
1.78839256738333));
#19110=CARTESIAN_POINT('Ctrl Pts',(0.0469118997549415,0.14830883905122,
1.7883455765265));
#19111=CARTESIAN_POINT('Ctrl Pts',(0.0517460803809523,0.146757135091929,
1.78798572640871));
#19112=CARTESIAN_POINT('Ctrl Pts',(0.0558929478068463,0.145228444324451,
1.78768236493972));
#19113=CARTESIAN_POINT('Ctrl Pts',(0.0736088245304174,0.137826161752135,
1.78638659755108));
#19114=CARTESIAN_POINT('Ctrl Pts',(0.0863661990675227,0.130212281457774,
1.78544670842502));
#19115=CARTESIAN_POINT('Ctrl Pts',(0.100909341190346,0.118442048586702,
1.78417225536528));
#19116=CARTESIAN_POINT('Ctrl Pts',(0.103866059720712,0.115857892080291,
1.78390114102821));
#19117=CARTESIAN_POINT('Ctrl Pts',(0.107385717028277,0.112538630610634,
1.78356122697175));
#19118=CARTESIAN_POINT('Ctrl Pts',(0.108044213586633,0.111906583579372,
1.78349685436312));
#19119=CARTESIAN_POINT('Ctrl Pts',(0.109074706407254,0.110899907956114,
1.7833948560023));
#19120=CARTESIAN_POINT('Ctrl Pts',(0.109450431117544,0.110529110546453,
1.78335739729049));
#19121=CARTESIAN_POINT('Ctrl Pts',(0.110150354307671,0.109831297836998,
1.78328710527739));
#19122=CARTESIAN_POINT('Ctrl Pts',(0.110475003153329,0.109504740575762,
1.78325429240209));
#19123=CARTESIAN_POINT('Ctrl Pts',(0.111197065875754,0.108771954100905,
1.78318083978658));
#19124=CARTESIAN_POINT('Ctrl Pts',(0.111593711400995,0.108364980589715,
1.78314016708753));
#19125=CARTESIAN_POINT('Ctrl Pts',(0.112590742517728,0.107330709302985,
1.7830371009355));
#19126=CARTESIAN_POINT('Ctrl Pts',(0.113188115343678,0.106700548022423,
1.782974578727));
#19127=CARTESIAN_POINT('Ctrl Pts',(0.116518547812333,0.103127874327755,
1.782621595668));
#19128=CARTESIAN_POINT('Ctrl Pts',(0.119141881637525,0.100085648283759,
1.7823265618551));
#19129=CARTESIAN_POINT('Ctrl Pts',(0.122832787030665,0.0954544124569725,
1.78188481960353));
#19130=CARTESIAN_POINT('Ctrl Pts',(0.123993630577599,0.0939415641716582,
1.78174162531866));
#19131=CARTESIAN_POINT('Ctrl Pts',(0.133870792564449,0.0805672292569739,
1.78048542063198));
#19132=CARTESIAN_POINT('Ctrl Pts',(0.140889114517399,0.0675473692591731,
1.77931813274184));
#19133=CARTESIAN_POINT('Ctrl Pts',(0.146868830591789,0.0513037026695924,
1.77801600318244));
#19134=CARTESIAN_POINT('Ctrl Pts',(0.147703536442457,0.0488486517205632,
1.7778233163896));
#19135=CARTESIAN_POINT('Ctrl Pts',(0.148637317158402,0.0458589280376593,
1.77759450845042));
#19136=CARTESIAN_POINT('Ctrl Pts',(0.148795419061345,0.0453433194896637,
1.77755525594162));
#19137=CARTESIAN_POINT('Ctrl Pts',(0.149037477146129,0.0445390086004645,
1.77749435911389));
#19138=CARTESIAN_POINT('Ctrl Pts',(0.149123281222634,0.0442508743729996,
1.77747261016086));
#19139=CARTESIAN_POINT('Ctrl Pts',(0.149281114213581,0.043715190782248,
1.77743230153753));
#19140=CARTESIAN_POINT('Ctrl Pts',(0.149353362345588,0.0434677135802262,
1.7774137296516));
#19141=CARTESIAN_POINT('Ctrl Pts',(0.149515568406769,0.0429069173957601,
1.77737175704667));
#19142=CARTESIAN_POINT('Ctrl Pts',(0.149605156767253,0.0425934951645332,
1.77734837797657));
#19143=CARTESIAN_POINT('Ctrl Pts',(0.149873182732766,0.041644535510489,
1.77727782424821));
#19144=CARTESIAN_POINT('Ctrl Pts',(0.1500485638648,0.0410081304618911,1.77723082258238));
#19145=CARTESIAN_POINT('Ctrl Pts',(0.151367495790153,0.0361003572884876,
1.77687063369835));
#19146=CARTESIAN_POINT('Ctrl Pts',(0.152332630229546,0.031782597305135,
1.77656696448232));
#19147=CARTESIAN_POINT('Ctrl Pts',(0.155720548205868,0.0128708290260328,
1.77527039341198));
#19148=CARTESIAN_POINT('Ctrl Pts',(0.156239098195963,-0.001984978289228,
1.77433000466234));
#19149=CARTESIAN_POINT('Ctrl Pts',(0.154231853951435,-0.0205830012752516,
1.77305566313613));
#19150=CARTESIAN_POINT('Ctrl Pts',(0.153665108098895,-0.0244572036581431,
1.77278531792012));
#19151=CARTESIAN_POINT('Ctrl Pts',(0.152786964628181,-0.0292023553823572,
1.77244625671808));
#19152=CARTESIAN_POINT('Ctrl Pts',(0.152613139939519,-0.0300975675878516,
1.7723819407683));
#19153=CARTESIAN_POINT('Ctrl Pts',(0.152326318839247,-0.0315083094250501,
1.77228001194332));
#19154=CARTESIAN_POINT('Ctrl Pts',(0.152218551002129,-0.0320248917604507,
1.77224256572046));
#19155=CARTESIAN_POINT('Ctrl Pts',(0.152011822993217,-0.0329912143564052,
1.77217228489697));
#19156=CARTESIAN_POINT('Ctrl Pts',(0.151913489960272,-0.0334410842250751,
1.77213947066084));
#19157=CARTESIAN_POINT('Ctrl Pts',(0.151689291382762,-0.0344453859752673,
1.77206599911256));
#19158=CARTESIAN_POINT('Ctrl Pts',(0.151562381368257,-0.034999575330341,
1.77202530876318));
#19159=CARTESIAN_POINT('Ctrl Pts',(0.15123379420906,-0.0363991389352862,
1.77192216807315));
#19160=CARTESIAN_POINT('Ctrl Pts',(0.151028067204055,-0.0372435321326472,
1.77185958865131));
#19161=CARTESIAN_POINT('Ctrl Pts',(0.149829145972329,-0.0419910763485591,
1.77150570836117));
#19162=CARTESIAN_POINT('Ctrl Pts',(0.148691818572973,-0.0458558722880187,
1.77120980727176));
#19163=CARTESIAN_POINT('Ctrl Pts',(0.146800331638623,-0.0514690357844124,
1.77076793398806));
#19164=CARTESIAN_POINT('Ctrl Pts',(0.146161945132119,-0.0532548992426505,
1.77062551044896));
#19165=CARTESIAN_POINT('Ctrl Pts',(0.140281243814903,-0.068802994596929,
1.76936952347799));
#19166=CARTESIAN_POINT('Ctrl Pts',(0.133142695530272,-0.0817656667338998,
1.76820162548707));
#19167=CARTESIAN_POINT('Ctrl Pts',(0.122735797628334,-0.0955949843381436,
1.76689974540649));
#19168=CARTESIAN_POINT('Ctrl Pts',(0.121131040660769,-0.0976204392709824,
1.76670773615539));
#19169=CARTESIAN_POINT('Ctrl Pts',(0.119131466240921,-0.10001893068078,
1.76647962418861));
#19170=CARTESIAN_POINT('Ctrl Pts',(0.118784332818932,-0.100430946640481,
1.76644041187204));
#19171=CARTESIAN_POINT('Ctrl Pts',(0.118240238495962,-0.101069969871784,
1.76637956371951));
#19172=CARTESIAN_POINT('Ctrl Pts',(0.118044753159109,-0.101298218470267,
1.76635782351474));
#19173=CARTESIAN_POINT('Ctrl Pts',(0.117680327458635,-0.101721234270261,
1.76631752281045));
#19174=CARTESIAN_POINT('Ctrl Pts',(0.117511566036504,-0.101916146030575,
1.76629895013822));
#19175=CARTESIAN_POINT('Ctrl Pts',(0.117128227505168,-0.102356666532666,
1.76625696519708));
#19176=CARTESIAN_POINT('Ctrl Pts',(0.116913362512068,-0.102602020124317,
1.76623357463067));
#19177=CARTESIAN_POINT('Ctrl Pts',(0.116260740110817,-0.103342535376414,
1.76616295189995));
#19178=CARTESIAN_POINT('Ctrl Pts',(0.115820589321804,-0.103835593319316,
1.76611589322625));
#19179=CARTESIAN_POINT('Ctrl Pts',(0.112395106378392,-0.107623944885169,
1.76575390418718));
#19180=CARTESIAN_POINT('Ctrl Pts',(0.109272509583499,-0.110793056565655,
1.76544859960747));
#19181=CARTESIAN_POINT('Ctrl Pts',(0.0951632378153099,-0.123934686704193,
1.76414767363625));
#19182=CARTESIAN_POINT('Ctrl Pts',(0.0829181456910517,-0.132440467940152,
1.76320455285298));
#19183=CARTESIAN_POINT('Ctrl Pts',(0.0662080847190203,-0.140808864601828,
1.76193077465562));
#19184=CARTESIAN_POINT('Ctrl Pts',(0.0627004738156415,-0.14240538316404,
1.7616645856437));
#19185=CARTESIAN_POINT('Ctrl Pts',(0.058298099649379,-0.144214970203719,
1.76133013486416));
#19186=CARTESIAN_POINT('Ctrl Pts',(0.0574557570431828,-0.144552627004233,
1.76126612837196));
#19187=CARTESIAN_POINT('Ctrl Pts',(0.0561199150854454,-0.145074584526248,
1.76116457936147));
#19188=CARTESIAN_POINT('Ctrl Pts',(0.0556283413968665,-0.145263786146715,
1.76112720138286));
#19189=CARTESIAN_POINT('Ctrl Pts',(0.0547051359064052,-0.145613745056728,
1.76105698143769));
#19190=CARTESIAN_POINT('Ctrl Pts',(0.0542737314389346,-0.145775089474504,
1.76102415949882));
#19191=CARTESIAN_POINT('Ctrl Pts',(0.0533069661870855,-0.146131771433182,
1.76095058321685));
#19192=CARTESIAN_POINT('Ctrl Pts',(0.052771238087427,-0.146326086809594,
1.76090979540374));
#19193=CARTESIAN_POINT('Ctrl Pts',(0.0514117408556365,-0.146810756752664,
1.76080624289936));
#19194=CARTESIAN_POINT('Ctrl Pts',(0.0505865810045376,-0.147097121523561,
1.76074334732105));
#19195=CARTESIAN_POINT('Ctrl Pts',(0.0458839497237457,-0.148684881624701,
1.76038461023037));
#19196=CARTESIAN_POINT('Ctrl Pts',(0.041959105488379,-0.14983977620702,
1.76008401985359));
#19197=CARTESIAN_POINT('Ctrl Pts',(0.0257902264300201,-0.153912437759099,
1.75883952410253));
#19198=CARTESIAN_POINT('Ctrl Pts',(0.0132601626775284,-0.155493560898368,
1.75785586721246));
#19199=CARTESIAN_POINT('Ctrl Pts',(-0.00371418171453799,-0.155567708351024,
1.75654666089774));
#19200=CARTESIAN_POINT('Ctrl Pts',(-0.00810704462424373,-0.155400737191817,
1.75621055179108));
#19201=CARTESIAN_POINT('Ctrl Pts',(-0.0146755064276768,-0.154871725841464,
1.75571692940235));
#19202=CARTESIAN_POINT('Ctrl Pts',(-0.01685992661398,-0.154649171268608,
1.75555427434402));
#19203=CARTESIAN_POINT('Ctrl Pts',(-0.0195477958919771,-0.154317688341038,
1.75535656312287));
#19204=CARTESIAN_POINT('Ctrl Pts',(-0.0200562385351817,-0.154252431342088,
1.75531927150631));
#19205=CARTESIAN_POINT('Ctrl Pts',(-0.0208565449046498,-0.154145690585219,
1.75526075277204));
#19206=CARTESIAN_POINT('Ctrl Pts',(-0.0211486228915669,-0.154105889391339,
1.75523943363137));
#19207=CARTESIAN_POINT('Ctrl Pts',(-0.0216967268285729,-0.154029612159401,
1.7551994998784));
#19208=CARTESIAN_POINT('Ctrl Pts',(-0.0219527718555892,-0.153993328382706,
1.75518087518737));
#19209=CARTESIAN_POINT('Ctrl Pts',(-0.0225399509756017,-0.153908625812204,
1.75513823183764));
#19210=CARTESIAN_POINT('Ctrl Pts',(-0.0228710198485558,-0.153859776894972,
1.75511423768703));
#19211=CARTESIAN_POINT('Ctrl Pts',(-0.0238981897699672,-0.153704830212752,
1.755039939928));
#19212=CARTESIAN_POINT('Ctrl Pts',(-0.024593743258209,-0.153595072016359,
1.75498983738828));
#19213=CARTESIAN_POINT('Ctrl Pts',(-0.03261523520254,-0.152273394418483,
1.75441418523699));
#19214=CARTESIAN_POINT('Ctrl Pts',(-0.0398473069998486,-0.1505429092258,
1.75391579057767));
#19215=CARTESIAN_POINT('Ctrl Pts',(-0.0486997482833774,-0.147741620341379,
1.75330080075456));
#19216=CARTESIAN_POINT('Ctrl Pts',(-0.0504602974047382,-0.147149619128453,
1.75317825574012));
#19217=CARTESIAN_POINT('Ctrl Pts',(-0.0610314623959728,-0.143382929269549,
1.75243886850096));
#19218=CARTESIAN_POINT('Ctrl Pts',(-0.0695505348139731,-0.139449670314694,
1.75182651991915));
#19219=CARTESIAN_POINT('Ctrl Pts',(-0.0814260692977656,-0.13260637965032,
1.75089594662155));
#19220=CARTESIAN_POINT('Ctrl Pts',(-0.0850955006778522,-0.130282026716384,
1.75059677779658));
#19221=CARTESIAN_POINT('Ctrl Pts',(-0.0894355041149582,-0.12727127664727,
1.75022581498615));
#19222=CARTESIAN_POINT('Ctrl Pts',(-0.0902034640843575,-0.126728143099933,
1.75015949745554));
#19223=CARTESIAN_POINT('Ctrl Pts',(-0.091399601169933,-0.125865803774084,
1.75005511316914));
#19224=CARTESIAN_POINT('Ctrl Pts',(-0.0918311503139302,-0.125551294190099,
1.75001722701113));
#19225=CARTESIAN_POINT('Ctrl Pts',(-0.0925941831546651,-0.124989163282781,
1.74994983269994));
#19226=CARTESIAN_POINT('Ctrl Pts',(-0.0929263162411565,-0.124742428371377,
1.74992035914783));
#19227=CARTESIAN_POINT('Ctrl Pts',(-0.093690262986942,-0.124170163700927,
1.74985224417579));
#19228=CARTESIAN_POINT('Ctrl Pts',(-0.0941213691942,-0.123843703027014,
1.74981356661273));
#19229=CARTESIAN_POINT('Ctrl Pts',(-0.0953015517344583,-0.122940273070961,
1.74970701764101));
#19230=CARTESIAN_POINT('Ctrl Pts',(-0.0960470724287772,-0.122358719796578,
1.74963896622906));
#19231=CARTESIAN_POINT('Ctrl Pts',(-0.0998545441082448,-0.119332413049575,
1.74928750901641));
#19232=CARTESIAN_POINT('Ctrl Pts',(-0.102828366574918,-0.116779607382737,
1.74899980343514));
#19233=CARTESIAN_POINT('Ctrl Pts',(-0.107166286715345,-0.112761566433556,
1.74855910185614));
#19234=CARTESIAN_POINT('Ctrl Pts',(-0.108603860203675,-0.111377667502997,
1.74840932632836));
#19235=CARTESIAN_POINT('Ctrl Pts',(-0.120380034043979,-0.0995963734766138,
1.74715092626957));
#19236=CARTESIAN_POINT('Ctrl Pts',(-0.129225898037721,-0.0878144591943174,
1.74598848002336));
#19237=CARTESIAN_POINT('Ctrl Pts',(-0.137575586934046,-0.0726351137692201,
1.74468428046566));
#19238=CARTESIAN_POINT('Ctrl Pts',(-0.138799677234858,-0.0702677293479703,
1.74448613123363));
#19239=CARTESIAN_POINT('Ctrl Pts',(-0.140199622447735,-0.0673807382183866,
1.74425172095393));
#19240=CARTESIAN_POINT('Ctrl Pts',(-0.140434252619785,-0.0668903485727644,
1.74421215051362));
#19241=CARTESIAN_POINT('Ctrl Pts',(-0.140795044273981,-0.0661260081715274,
1.74415086876003));
#19242=CARTESIAN_POINT('Ctrl Pts',(-0.140922984900632,-0.0658529101842299,
1.74412905070382));
#19243=CARTESIAN_POINT('Ctrl Pts',(-0.141158785723988,-0.0653457430306535,
1.7440886791461));
#19244=CARTESIAN_POINT('Ctrl Pts',(-0.141266857434217,-0.0651117801313446,
1.74407011309058));
#19245=CARTESIAN_POINT('Ctrl Pts',(-0.141509780469074,-0.0645824276924301,
1.74402823619718));
#19246=CARTESIAN_POINT('Ctrl Pts',(-0.141644288367612,-0.0642868844563697,
1.74400494659083));
#19247=CARTESIAN_POINT('Ctrl Pts',(-0.14203826023097,-0.0634140029055581,
1.74393642199687));
#19248=CARTESIAN_POINT('Ctrl Pts',(-0.142295131171779,-0.0628354900950748,
1.7438913420529));
#19249=CARTESIAN_POINT('Ctrl Pts',(-0.144115399130699,-0.0586675566993679,
1.74356885058617));
#19250=CARTESIAN_POINT('Ctrl Pts',(-0.145546485575233,-0.0550214285575594,
1.7432988846673));
#19251=CARTESIAN_POINT('Ctrl Pts',(-0.147503303763815,-0.0494230355989775,
1.74289682713822));
#19252=CARTESIAN_POINT('Ctrl Pts',(-0.148131046112163,-0.0475084708582904,
1.7427614784464));
#19253=CARTESIAN_POINT('Ctrl Pts',(-0.152286772020839,-0.0339495446450549,
1.741814519695));
#19254=CARTESIAN_POINT('Ctrl Pts',(-0.154474985958918,-0.0219390321530172,
1.74103177607834));
#19255=CARTESIAN_POINT('Ctrl Pts',(-0.15544609479793,-0.00654950058985834,
1.7399894607761));
#19256=CARTESIAN_POINT('Ctrl Pts',(-0.155549053882137,-0.00329755167798682,
1.73976727166252));
#19257=CARTESIAN_POINT('Ctrl Pts',(-0.155550109736665,0.000357396774194728,
1.73951423103283));
#19258=CARTESIAN_POINT('Ctrl Pts',(-0.155548665002922,0.000759725169547559,
1.73948633212019));
#19259=CARTESIAN_POINT('Ctrl Pts',(-0.155532254608223,0.00295634915230469,
1.73933375698741));
#19260=CARTESIAN_POINT('Ctrl Pts',(-0.155487803810492,0.00475022358437416,
1.7392082315102));
#19261=CARTESIAN_POINT('Ctrl Pts',(-0.155382355293907,0.00725493685538521,
1.73903149831066));
#19262=CARTESIAN_POINT('Ctrl Pts',(-0.15534748395943,0.00796678369735155,
1.73898110474304));
#19263=CARTESIAN_POINT('Ctrl Pts',(-0.155283416033973,0.00911334238682362,
1.73889965944689));
#19264=CARTESIAN_POINT('Ctrl Pts',(-0.155257282486212,0.00954822143587498,
1.73886870368154));
#19265=CARTESIAN_POINT('Ctrl Pts',(-0.155199240457862,0.0104507399107341,
1.73880432378887));
#19266=CARTESIAN_POINT('Ctrl Pts',(-0.15516704451143,0.0109183557425694,
1.73877089098723));
#19267=CARTESIAN_POINT('Ctrl Pts',(-0.155086412699842,0.0120169713761962,
1.73869216148284));
#19268=CARTESIAN_POINT('Ctrl Pts',(-0.155036238829405,0.0126478311529641,
1.73864681084841));
#19269=CARTESIAN_POINT('Ctrl Pts',(-0.154859438128438,0.0147114118553243,
1.73849799092978));
#19270=CARTESIAN_POINT('Ctrl Pts',(-0.154716792603448,0.016142646757619,
1.73839402280467));
#19271=CARTESIAN_POINT('Ctrl Pts',(-0.15387559904101,0.0235415007387464,
1.73785249273175));
#19272=CARTESIAN_POINT('Ctrl Pts',(-0.152851654066885,0.029466194238073,
1.73740485654255));
#19273=CARTESIAN_POINT('Ctrl Pts',(-0.14866079573209,0.0474427755649512,
1.73600321158561));
#19274=CARTESIAN_POINT('Ctrl Pts',(-0.144388304701991,0.0591846610049198,
1.73502235396061));
#19275=CARTESIAN_POINT('Ctrl Pts',(-0.137023622434677,0.0737233545624012,
1.73378210400021));
#19276=CARTESIAN_POINT('Ctrl Pts',(-0.135158024795964,0.0770903411674165,
1.73349332339123));
#19277=CARTESIAN_POINT('Ctrl Pts',(-0.13284354065872,0.080924616152256,
1.73316542085292));
#19278=CARTESIAN_POINT('Ctrl Pts',(-0.132514523738763,0.0814622662888544,
1.73311946488892));
#19279=CARTESIAN_POINT('Ctrl Pts',(-0.132011371080237,0.0822733582114227,
1.73305018874747));
#19280=CARTESIAN_POINT('Ctrl Pts',(-0.131839639273269,0.0825482712561308,
1.73302671735105));
#19281=CARTESIAN_POINT('Ctrl Pts',(-0.131529845980388,0.0830407641754954,
1.73298468884172));
#19282=CARTESIAN_POINT('Ctrl Pts',(-0.131392102794995,0.0832585384511001,
1.73296611135214));
#19283=CARTESIAN_POINT('Ctrl Pts',(-0.131091741687671,0.0837308125575096,
1.73292583892584));
#19284=CARTESIAN_POINT('Ctrl Pts',(-0.130928923996588,0.0839851806902346,
1.73290415751868));
#19285=CARTESIAN_POINT('Ctrl Pts',(-0.130469887999167,0.0846977479744231,
1.73284344255255));
#19286=CARTESIAN_POINT('Ctrl Pts',(-0.130171994269653,0.0851548713704573,
1.73280451815436));
#19287=CARTESIAN_POINT('Ctrl Pts',(-0.12838655454332,0.0878633975707241,
1.7325739748399));
#19288=CARTESIAN_POINT('Ctrl Pts',(-0.126842916780531,0.0900775269508181,
1.732385882531));
#19289=CARTESIAN_POINT('Ctrl Pts',(-0.116564191198058,0.10403225749559,
1.73119491717937));
#19290=CARTESIAN_POINT('Ctrl Pts',(-0.106266314764755,0.114531636572013,
1.73026691320409));
#19291=CARTESIAN_POINT('Ctrl Pts',(-0.0930327779010258,0.124679051186721,
1.72914628381507));
#19292=CARTESIAN_POINT('Ctrl Pts',(-0.0913898172430544,0.125888301145483,
1.72900838379073));
#19293=CARTESIAN_POINT('Ctrl Pts',(-0.0865626836008204,0.129296858176909,
1.72860590125256));
#19294=CARTESIAN_POINT('Ctrl Pts',(-0.0833198339825612,0.13140995661346,
1.72833875754766));
#19295=CARTESIAN_POINT('Ctrl Pts',(-0.0791943083075496,0.133884093862236,
1.7280009725506));
#19296=CARTESIAN_POINT('Ctrl Pts',(-0.0783824512172755,0.134361007473451,
1.7279345995908));
#19297=CARTESIAN_POINT('Ctrl Pts',(-0.0770983746296638,0.135099720892583,
1.72782975079831));
#19298=CARTESIAN_POINT('Ctrl Pts',(-0.0766290262744205,0.135366488743217,
1.72779145417624));
#19299=CARTESIAN_POINT('Ctrl Pts',(-0.0757975150310976,0.135833392159041,
1.72772364974976));
#19300=CARTESIAN_POINT('Ctrl Pts',(-0.0754359223462922,0.13603453724704,
1.72769417843668));
#19301=CARTESIAN_POINT('Ctrl Pts',(-0.0746050829093937,0.136492381437273,
1.72762649160836));
#19302=CARTESIAN_POINT('Ctrl Pts',(-0.0741353083437456,0.136748106494806,
1.72758824186227));
#19303=CARTESIAN_POINT('Ctrl Pts',(-0.0728322608673699,0.137448741583128,
1.72748219994082));
#19304=CARTESIAN_POINT('Ctrl Pts',(-0.071996252046468,0.137888485392943,
1.72741422635685));
#19305=CARTESIAN_POINT('Ctrl Pts',(-0.0686990227952293,0.139584680263499,
1.72714633417309));
#19306=CARTESIAN_POINT('Ctrl Pts',(-0.0662089069558742,0.140782862098249,
1.72694443215555));
#19307=CARTESIAN_POINT('Ctrl Pts',(-0.0636886248462869,0.141913923084343,
1.72674034350975));
#19308=CARTESIAN_POINT('',(-0.155549931058622,0.000140704823091921,1.72557622542367));
#19309=CARTESIAN_POINT('Ctrl Pts',(-0.0636886260955797,0.141913922523681,
1.71290984779881));
#19310=CARTESIAN_POINT('Ctrl Pts',(-0.0654236273732955,0.141135282586974,
1.71303852138742));
#19311=CARTESIAN_POINT('Ctrl Pts',(-0.0671444433123963,0.140324783043432,
1.71316615252523));
#19312=CARTESIAN_POINT('Ctrl Pts',(-0.0772688368385502,0.135327275048561,
1.71391956536969));
#19313=CARTESIAN_POINT('Ctrl Pts',(-0.0852940727414064,0.130418076052826,
1.71452828255038));
#19314=CARTESIAN_POINT('Ctrl Pts',(-0.0987184873531856,0.120434032958858,
1.71564217942489));
#19315=CARTESIAN_POINT('Ctrl Pts',(-0.104290828069218,0.115642100442611,
1.71613933078241));
#19316=CARTESIAN_POINT('Ctrl Pts',(-0.110224802971553,0.109760313978326,
1.71672455251474));
#19317=CARTESIAN_POINT('Ctrl Pts',(-0.110938992223859,0.109038404393045,
1.71679597868351));
#19318=CARTESIAN_POINT('Ctrl Pts',(-0.112068134301731,0.107874479070005,
1.71691053600853));
#19319=CARTESIAN_POINT('Ctrl Pts',(-0.112487669015793,0.107436931550854,
1.71695346771157));
#19320=CARTESIAN_POINT('Ctrl Pts',(-0.113225180465223,0.106658699474202,
1.71702959980754));
#19321=CARTESIAN_POINT('Ctrl Pts',(-0.113544205895162,0.106319015062676,
1.71706275459873));
#19322=CARTESIAN_POINT('Ctrl Pts',(-0.114202917058564,0.105611301785401,
1.71713167813114));
#19323=CARTESIAN_POINT('Ctrl Pts',(-0.114542360901767,0.10524305619718,
1.7171674566231));
#19324=CARTESIAN_POINT('Ctrl Pts',(-0.115225048223495,0.104495227917897,
1.7172399485924));
#19325=CARTESIAN_POINT('Ctrl Pts',(-0.115568208460668,0.104115577976137,
1.7172766649682));
#19326=CARTESIAN_POINT('Ctrl Pts',(-0.116953931359989,0.10256721343367,
1.71742607025569));
#19327=CARTESIAN_POINT('Ctrl Pts',(-0.117980655635431,0.101384515062276,
1.71753941478281));
#19328=CARTESIAN_POINT('Ctrl Pts',(-0.123146891222748,0.0952486934955429,
1.71812372408852));
#19329=CARTESIAN_POINT('Ctrl Pts',(-0.126992474937705,0.0900575395294839,
1.71860627911308));
#19330=CARTESIAN_POINT('Ctrl Pts',(-0.133269256976991,0.0803799065816245,
1.71948534075563));
#19331=CARTESIAN_POINT('Ctrl Pts',(-0.135823658657544,0.0759838961843065,
1.71987771314208));
#19332=CARTESIAN_POINT('Ctrl Pts',(-0.142660297122646,0.0627682207319928,
1.72103098931182));
#19333=CARTESIAN_POINT('Ctrl Pts',(-0.146330456601708,0.0536586167239064,
1.72179451302398));
#19334=CARTESIAN_POINT('Ctrl Pts',(-0.1494467083144,0.0431602601280605,
1.72260396684577));
#19335=CARTESIAN_POINT('Ctrl Pts',(-0.149761922609095,0.0420534591620181,
1.72268844091508));
#19336=CARTESIAN_POINT('Ctrl Pts',(-0.150175685682622,0.0405369372520968,
1.72280291723953));
#19337=CARTESIAN_POINT('Ctrl Pts',(-0.150284885609153,0.0401302008553649,
1.72283349616439));
#19338=CARTESIAN_POINT('Ctrl Pts',(-0.15045553121994,0.0394841319253197,
1.72288186642966));
#19339=CARTESIAN_POINT('Ctrl Pts',(-0.150518059737978,0.0392450919686247,
1.72289971924773));
#19340=CARTESIAN_POINT('Ctrl Pts',(-0.150645789894482,0.0387519971155168,
1.72293645469024));
#19341=CARTESIAN_POINT('Ctrl Pts',(-0.150710918551079,0.0384979262306401,
1.72295533263976));
#19342=CARTESIAN_POINT('Ctrl Pts',(-0.150864150120947,0.0378938121398273,
1.72300010240695));
#19343=CARTESIAN_POINT('Ctrl Pts',(-0.150951678573044,0.0375436217391715,
1.72302596122048));
#19344=CARTESIAN_POINT('Ctrl Pts',(-0.151134419985444,0.03680152504019,
1.72308056845939));
#19345=CARTESIAN_POINT('Ctrl Pts',(-0.151229329620691,0.0364095457484073,
1.72310929990258));
#19346=CARTESIAN_POINT('Ctrl Pts',(-0.151485282034299,0.0353341867975488,
1.7231878255408));
#19347=CARTESIAN_POINT('Ctrl Pts',(-0.151643226805986,0.0346500684072558,
1.72323745429586));
#19348=CARTESIAN_POINT('Ctrl Pts',(-0.154280640908645,0.0228628859446989,
1.72408729525527));
#19349=CARTESIAN_POINT('Ctrl Pts',(-0.155539639183238,0.0115203149781142,
1.7248266954542));
#19350=CARTESIAN_POINT('Ctrl Pts',(-0.1555499363173,0.000140753984132637,
1.72557621298977));
#19351=CARTESIAN_POINT('Ctrl Pts',(-0.155549936362318,0.000140704224764531,
1.72557621626718));
#19352=CARTESIAN_POINT('Ctrl Pts',(-0.155557231474537,-0.00792411574282843,
1.72610740759547));
#19353=CARTESIAN_POINT('Ctrl Pts',(-0.154937332086665,-0.0159767149073688,
1.72664147358767));
#19354=CARTESIAN_POINT('Ctrl Pts',(-0.153271235507139,-0.0266710360606433,
1.72738304732705));
#19355=CARTESIAN_POINT('Ctrl Pts',(-0.152774050896218,-0.0293854314049922,
1.72757403013639));
#19356=CARTESIAN_POINT('Ctrl Pts',(-0.152040759071231,-0.0328640208606756,
1.72782302989824));
#19357=CARTESIAN_POINT('Ctrl Pts',(-0.151870572343261,-0.0336417226174832,
1.72787897336641));
#19358=CARTESIAN_POINT('Ctrl Pts',(-0.151576166862013,-0.0349392872115377,
1.72797279031911));
#19359=CARTESIAN_POINT('Ctrl Pts',(-0.151455223537571,-0.0354598844018647,
1.72801055968426));
#19360=CARTESIAN_POINT('Ctrl Pts',(-0.15121211856038,-0.0364823865362186,
1.72808500171594));
#19361=CARTESIAN_POINT('Ctrl Pts',(-0.151090134917705,-0.0369843270281836,
1.72812166827056));
#19362=CARTESIAN_POINT('Ctrl Pts',(-0.150854357508204,-0.0379338716032327,
1.72819127050672));
#19363=CARTESIAN_POINT('Ctrl Pts',(-0.150741065737695,-0.0383815956655832,
1.72822418970341));
#19364=CARTESIAN_POINT('Ctrl Pts',(-0.150479751482428,-0.039395293231898,
1.72829895450225));
#19365=CARTESIAN_POINT('Ctrl Pts',(-0.150330527356654,-0.0399609467156958,
1.72834083847357));
#19366=CARTESIAN_POINT('Ctrl Pts',(-0.149879573722586,-0.0416320666385901,
1.72846507262903));
#19367=CARTESIAN_POINT('Ctrl Pts',(-0.149568821301318,-0.0427350342895152,
1.72854771328153));
#19368=CARTESIAN_POINT('Ctrl Pts',(-0.146529633706473,-0.0530827502500465,
1.72932926656177));
#19369=CARTESIAN_POINT('Ctrl Pts',(-0.142960188045411,-0.0620566522011234,
1.73005616359697));
#19370=CARTESIAN_POINT('Ctrl Pts',(-0.136058948306859,-0.0755955641029131,
1.73122726110572));
#19371=CARTESIAN_POINT('Ctrl Pts',(-0.133269673865166,-0.0804109353330466,
1.73165974624265));
#19372=CARTESIAN_POINT('Ctrl Pts',(-0.12649044660889,-0.0907892833558381,
1.7326190552481));
#19373=CARTESIAN_POINT('Ctrl Pts',(-0.122378613694646,-0.0962601935947096,
1.73314386905609));
#19374=CARTESIAN_POINT('Ctrl Pts',(-0.117198038191796,-0.102282191626779,
1.73373054988717));
#19375=CARTESIAN_POINT('Ctrl Pts',(-0.116467454786522,-0.103113331067661,
1.7338117278688));
#19376=CARTESIAN_POINT('Ctrl Pts',(-0.115521071871376,-0.104167079217518,
1.73391483679874));
#19377=CARTESIAN_POINT('Ctrl Pts',(-0.115313416915625,-0.104396907630037,
1.73393733708179));
#19378=CARTESIAN_POINT('Ctrl Pts',(-0.114906883315595,-0.104844158103298,
1.73398114321194));
#19379=CARTESIAN_POINT('Ctrl Pts',(-0.114708070779714,-0.10506163821127,
1.73400245375995));
#19380=CARTESIAN_POINT('Ctrl Pts',(-0.114333665793,-0.105468868399165,1.73404237307569));
#19381=CARTESIAN_POINT('Ctrl Pts',(-0.114158220408911,-0.105658743365668,
1.73406099190778));
#19382=CARTESIAN_POINT('Ctrl Pts',(-0.113754632556436,-0.106093345727504,
1.73410362365506));
#19383=CARTESIAN_POINT('Ctrl Pts',(-0.113526173529466,-0.106337774874026,
1.73412761206854));
#19384=CARTESIAN_POINT('Ctrl Pts',(-0.112814515616789,-0.107094272738072,
1.73420189818956));
#19385=CARTESIAN_POINT('Ctrl Pts',(-0.112328618271171,-0.107603809201015,
1.73425199486069));
#19386=CARTESIAN_POINT('Ctrl Pts',(-0.106707450824626,-0.113418877160757,
1.73482468526606));
#19387=CARTESIAN_POINT('Ctrl Pts',(-0.101203284594116,-0.118356460023565,
1.73532043183209));
#19388=CARTESIAN_POINT('Ctrl Pts',(-0.0897364859266798,-0.127255592215326,
1.73628197636209));
#19389=CARTESIAN_POINT('Ctrl Pts',(-0.0838109111111542,-0.131233970511423,
1.73674719417848));
#19390=CARTESIAN_POINT('Ctrl Pts',(-0.0728495457315214,-0.137547163850056,
1.73758641401376));
#19391=CARTESIAN_POINT('Ctrl Pts',(-0.0679228654962218,-0.140045543363424,
1.73795661394668));
#19392=CARTESIAN_POINT('Ctrl Pts',(-0.0600219163241034,-0.143537089284572,
1.73854903602219));
#19393=CARTESIAN_POINT('Ctrl Pts',(-0.0571326140867982,-0.144711397329763,
1.73876538497644));
#19394=CARTESIAN_POINT('Ctrl Pts',(-0.0534350880930995,-0.146086199251163,
1.73904281585321));
#19395=CARTESIAN_POINT('Ctrl Pts',(-0.0526577645394653,-0.146368186562579,
1.73910116911291));
#19396=CARTESIAN_POINT('Ctrl Pts',(-0.0513875174733978,-0.146817561952489,
1.73919659117301));
#19397=CARTESIAN_POINT('Ctrl Pts',(-0.0508959292532899,-0.146988699644592,
1.73923353551572));
#19398=CARTESIAN_POINT('Ctrl Pts',(-0.0499671905651373,-0.147306805894034,
1.73930336730971));
#19399=CARTESIAN_POINT('Ctrl Pts',(-0.049530226343338,-0.147454304330661,
1.73933623685491));
#19400=CARTESIAN_POINT('Ctrl Pts',(-0.0485436195289985,-0.147782455805455,
1.73941048738589));
#19401=CARTESIAN_POINT('Ctrl Pts',(-0.047993614597459,-0.147961988976933,
1.73945190467083));
#19402=CARTESIAN_POINT('Ctrl Pts',(-0.046583665922037,-0.148413537317381,
1.73955814890924));
#19403=CARTESIAN_POINT('Ctrl Pts',(-0.0457223450234555,-0.148681145716725,
1.73962311889532));
#19404=CARTESIAN_POINT('Ctrl Pts',(-0.0405150468451091,-0.150249502106093,
1.74001636252311));
#19405=CARTESIAN_POINT('Ctrl Pts',(-0.0361166406666132,-0.151366978928621,
1.74035051644414));
#19406=CARTESIAN_POINT('Ctrl Pts',(-0.0193356853182221,-0.154857378831999,
1.74163433119736));
#19407=CARTESIAN_POINT('Ctrl Pts',(-0.00673007942645939,-0.155914386861695,
1.74262168519795));
#19408=CARTESIAN_POINT('Ctrl Pts',(0.00987534283940077,-0.155288149733739,
1.74390068800435));
#19409=CARTESIAN_POINT('Ctrl Pts',(0.0138815922782705,-0.154981413030162,
1.74420708414451));
#19410=CARTESIAN_POINT('Ctrl Pts',(0.0198985994718691,-0.154285486156554,
1.74466015548634));
#19411=CARTESIAN_POINT('Ctrl Pts',(0.0219207576787233,-0.15401119106018,
1.74481119196353));
#19412=CARTESIAN_POINT('Ctrl Pts',(0.0244339350925388,-0.153619784494405,
1.74499690292667));
#19413=CARTESIAN_POINT('Ctrl Pts',(0.024930440361999,-0.153539990016912,
1.7450334942952));
#19414=CARTESIAN_POINT('Ctrl Pts',(0.025722947577856,-0.153408678782246,
1.74509173475559));
#19415=CARTESIAN_POINT('Ctrl Pts',(0.0260191965912659,-0.153358710775517,
1.74511346872854));
#19416=CARTESIAN_POINT('Ctrl Pts',(0.0265693236146171,-0.153264281457372,
1.74515375703412));
#19417=CARTESIAN_POINT('Ctrl Pts',(0.0268232333488723,-0.153220047913235,
1.74517232353617));
#19418=CARTESIAN_POINT('Ctrl Pts',(0.0273980642454144,-0.153118434075364,
1.74521429309068));
#19419=CARTESIAN_POINT('Ctrl Pts',(0.0277189150736658,-0.153060675976906,
1.74523767446213));
#19420=CARTESIAN_POINT('Ctrl Pts',(0.0286893488580272,-0.15288283138867,
1.74530826448711));
#19421=CARTESIAN_POINT('Ctrl Pts',(0.0293383621485162,-0.15275961318156,
1.74535529983243));
#19422=CARTESIAN_POINT('Ctrl Pts',(0.0343440365276796,-0.151776183564272,
1.7457168637528));
#19423=CARTESIAN_POINT('Ctrl Pts',(0.0386633523977352,-0.15073379573123,
1.74602179117571));
#19424=CARTESIAN_POINT('Ctrl Pts',(0.0571643788942634,-0.14542104904157,
1.74732057551452));
#19425=CARTESIAN_POINT('Ctrl Pts',(0.0707397721978309,-0.139323294616565,
1.74826204308894));
#19426=CARTESIAN_POINT('Ctrl Pts',(0.0865285793673756,-0.129320069239485,
1.74953569024452));
#19427=CARTESIAN_POINT('Ctrl Pts',(0.0897289405352208,-0.127120369063847,
1.74980387603136));
#19428=CARTESIAN_POINT('Ctrl Pts',(0.093573142699395,-0.12426059935753,
1.75014052866187));
#19429=CARTESIAN_POINT('Ctrl Pts',(0.0942980334991059,-0.123711399647648,
1.75020467089541));
#19430=CARTESIAN_POINT('Ctrl Pts',(0.0954353443859444,-0.122833933937407,
1.75030637902431));
#19431=CARTESIAN_POINT('Ctrl Pts',(0.0958509918576321,-0.122509867488594,
1.75034377942158));
#19432=CARTESIAN_POINT('Ctrl Pts',(0.0966266145223844,-0.121898776966581,
1.75041400731021));
#19433=CARTESIAN_POINT('Ctrl Pts',(0.0969869789748826,-0.121612254156248,
1.75044681461652));
#19434=CARTESIAN_POINT('Ctrl Pts',(0.0977898748815137,-0.120968039772314,
1.75052031358092));
#19435=CARTESIAN_POINT('Ctrl Pts',(0.0982317243458602,-0.120609512857936,
1.75056103846722));
#19436=CARTESIAN_POINT('Ctrl Pts',(0.0993448760503353,-0.119696101194275,
1.75066434725146));
#19437=CARTESIAN_POINT('Ctrl Pts',(0.100013495837147,-0.119137994072607,
1.75072706103009));
#19438=CARTESIAN_POINT('Ctrl Pts',(0.103770331522889,-0.115948193752939,
1.75108324752233));
#19439=CARTESIAN_POINT('Ctrl Pts',(0.106759054856323,-0.113202313939023,
1.75138139144821));
#19440=CARTESIAN_POINT('Ctrl Pts',(0.11096342196824,-0.109024854418954,
1.75182363894561));
#19441=CARTESIAN_POINT('Ctrl Pts',(0.112266115707445,-0.107682954389712,
1.75196410517105));
#19442=CARTESIAN_POINT('Ctrl Pts',(0.123607070491539,-0.0955711673085891,
1.75321784346555));
#19443=CARTESIAN_POINT('Ctrl Pts',(0.132091779129171,-0.0834520237155355,
1.75438540631624));
#19444=CARTESIAN_POINT('Ctrl Pts',(0.139913288702606,-0.0680201106625926,
1.75568674219346));
#19445=CARTESIAN_POINT('Ctrl Pts',(0.141022722549392,-0.0656890984411436,
1.75587855666601));
#19446=CARTESIAN_POINT('Ctrl Pts',(0.142292944183374,-0.0628395614316616,
1.75610645962497));
#19447=CARTESIAN_POINT('Ctrl Pts',(0.142509626835847,-0.0623466015711575,
1.7561456516211));
#19448=CARTESIAN_POINT('Ctrl Pts',(0.142843198153651,-0.0615768907859745,
1.75620647087489));
#19449=CARTESIAN_POINT('Ctrl Pts',(0.142961849499286,-0.0613009162211243,
1.75622820238575));
#19450=CARTESIAN_POINT('Ctrl Pts',(0.143180817146159,-0.0607875195341439,
1.75626848846425));
#19451=CARTESIAN_POINT('Ctrl Pts',(0.143281341825506,-0.0605501941885859,
1.75628705518921));
#19452=CARTESIAN_POINT('Ctrl Pts',(0.143507700127799,-0.0600120722183201,
1.75632902822296));
#19453=CARTESIAN_POINT('Ctrl Pts',(0.143633177929451,-0.0597111297085974,
1.75635241283563));
#19454=CARTESIAN_POINT('Ctrl Pts',(0.144010096591986,-0.0587990752681772,
1.7564230223198));
#19455=CARTESIAN_POINT('Ctrl Pts',(0.144258594841011,-0.0581867427253662,
1.75647007374252));
#19456=CARTESIAN_POINT('Ctrl Pts',(0.146149408554309,-0.0534409518917513,
1.75683214812904));
#19457=CARTESIAN_POINT('Ctrl Pts',(0.147617849606137,-0.0492398692978504,
1.75713753929933));
#19458=CARTESIAN_POINT('Ctrl Pts',(0.153189754390315,-0.0307947914952604,
1.75843756626187));
#19459=CARTESIAN_POINT('Ctrl Pts',(0.155426056734633,-0.016068878104595,
1.75937981562853));
#19460=CARTESIAN_POINT('Ctrl Pts',(0.155576005672513,0.00261647402569874,
1.76065330553863));
#19461=CARTESIAN_POINT('Ctrl Pts',(0.155462972470131,0.00648069197999925,
1.76092030639963));
#19462=CARTESIAN_POINT('Ctrl Pts',(0.155145838445867,0.0112426018721626,
1.76125564449856));
#19463=CARTESIAN_POINT('Ctrl Pts',(0.155077555704418,0.0121482071999812,
1.7613196982774));
#19464=CARTESIAN_POINT('Ctrl Pts',(0.154957143229427,0.0135780614487544,
1.76142129783928));
#19465=CARTESIAN_POINT('Ctrl Pts',(0.154910272775595,0.0141027432332509,
1.76145867872746));
#19466=CARTESIAN_POINT('Ctrl Pts',(0.154817443031725,0.0150855500045843,
1.7615288892302));
#19467=CARTESIAN_POINT('Ctrl Pts',(0.154772112917346,0.0155437299433997,
1.76156169875603));
#19468=CARTESIAN_POINT('Ctrl Pts',(0.154666174746554,0.0165680748340622,
1.7616352277448));
#19469=CARTESIAN_POINT('Ctrl Pts',(0.154604491052928,0.0171341193168057,
1.76167598055993));
#19470=CARTESIAN_POINT('Ctrl Pts',(0.15444045686002,0.0185663268778815,
1.76177940736583));
#19471=CARTESIAN_POINT('Ctrl Pts',(0.154333927727908,0.0194319814569409,
1.76184221175509));
#19472=CARTESIAN_POINT('Ctrl Pts',(0.153688554556271,0.0243357164885009,
1.76219968263018));
#19473=CARTESIAN_POINT('Ctrl Pts',(0.152998566227657,0.0283519293732846,
1.76249905939415));
#19474=CARTESIAN_POINT('Ctrl Pts',(0.151766141399666,0.0341508855888993,
1.76294148558436));
#19475=CARTESIAN_POINT('Ctrl Pts',(0.151348032537155,0.035958548735151,
1.76308084876283));
#19476=CARTESIAN_POINT('Ctrl Pts',(0.147321336088201,0.052050910791138,
1.76433431280582));
#19477=CARTESIAN_POINT('Ctrl Pts',(0.141733246908828,0.0657607987281602,
1.76550278924448));
#19478=CARTESIAN_POINT('Ctrl Pts',(0.133005762830483,0.0806961110609668,
1.76680375777164));
#19479=CARTESIAN_POINT('Ctrl Pts',(0.13165551943514,0.0828807672353076,
1.76699456339878));
#19480=CARTESIAN_POINT('Ctrl Pts',(0.129957796177516,0.0854813592326551,
1.76722142954024));
#19481=CARTESIAN_POINT('Ctrl Pts',(0.129661554647012,0.0859300461600298,
1.76726056132213));
#19482=CARTESIAN_POINT('Ctrl Pts',(0.129196275788744,0.0866268720001769,
1.76732130764618));
#19483=CARTESIAN_POINT('Ctrl Pts',(0.129028840368,0.0868760668289772,1.76734302604481));
#19484=CARTESIAN_POINT('Ctrl Pts',(0.128716310194509,0.0873383102035789,
1.76738330027735));
#19485=CARTESIAN_POINT('Ctrl Pts',(0.128571408823881,0.0875514807080559,
1.76740186820422));
#19486=CARTESIAN_POINT('Ctrl Pts',(0.128241873787442,0.0880336911344328,
1.76744385983441));
#19487=CARTESIAN_POINT('Ctrl Pts',(0.128056923399997,0.0883025103940371,
1.76746726176095));
#19488=CARTESIAN_POINT('Ctrl Pts',(0.12749416283232,0.0891149775839778,
1.76753797524011));
#19489=CARTESIAN_POINT('Ctrl Pts',(0.127113719881456,0.0896568070248737,
1.76758511259187));
#19490=CARTESIAN_POINT('Ctrl Pts',(0.124128822420835,0.0938507254158757,
1.76794994727309));
#19491=CARTESIAN_POINT('Ctrl Pts',(0.121370647486039,0.0973914711342306,
1.76825784620435));
#19492=CARTESIAN_POINT('Ctrl Pts',(0.108812642963751,0.112148753435143,
1.76956480867118));
#19493=CARTESIAN_POINT('Ctrl Pts',(0.0975841401833062,0.122044732983213,
1.77051148329402));
#19494=CARTESIAN_POINT('Ctrl Pts',(0.0819661568475446,0.132255605476125,
1.77178419864028));
#19495=CARTESIAN_POINT('Ctrl Pts',(0.0787392383769247,0.134201804712946,
1.77204461483336));
#19496=CARTESIAN_POINT('Ctrl Pts',(0.0746571354149566,0.136465843557174,
1.77237264348729));
#19497=CARTESIAN_POINT('Ctrl Pts',(0.0738654296511796,0.136895991787701,
1.77243619732048));
#19498=CARTESIAN_POINT('Ctrl Pts',(0.0726064048948479,0.137565941636466,
1.77253718319987));
#19499=CARTESIAN_POINT('Ctrl Pts',(0.0721415222795669,0.13781030106984,
1.77257445374281));
#19500=CARTESIAN_POINT('Ctrl Pts',(0.0712666397819486,0.138264531587501,
1.77264456661951));
#19501=CARTESIAN_POINT('Ctrl Pts',(0.0708569268086231,0.138474945588649,
1.77267738941107));
#19502=CARTESIAN_POINT('Ctrl Pts',(0.0699366546778662,0.138942411008693,
1.77275109163477));
#19503=CARTESIAN_POINT('Ctrl Pts',(0.0694256032566575,0.139198472839179,
1.77279200513208));
#19504=CARTESIAN_POINT('Ctrl Pts',(0.0681248077724416,0.139841289810439,
1.77289611155742));
#19505=CARTESIAN_POINT('Ctrl Pts',(0.0673331832232085,0.140224171054325,
1.77295943788348));
#19506=CARTESIAN_POINT('Ctrl Pts',(0.0627576298089193,0.14238952801178,
1.77332533835482));
#19507=CARTESIAN_POINT('Ctrl Pts',(0.0589066301748565,0.144025346776159,
1.77363288645451));
#19508=CARTESIAN_POINT('Ctrl Pts',(0.0533485686906487,0.14612607454763,
1.77407669683773));
#19509=CARTESIAN_POINT('Ctrl Pts',(0.0516920282657672,0.14672025507256,
1.77420895249216));
#19510=CARTESIAN_POINT('Ctrl Pts',(0.036000900263383,0.152049753605084,
1.77546134552491));
#19511=CARTESIAN_POINT('Ctrl Pts',(0.0213697357688163,0.154785173011199,
1.77663647192841));
#19512=CARTESIAN_POINT('Ctrl Pts',(0.00410313479575672,0.155515535062561,
1.77793493690867));
#19513=CARTESIAN_POINT('Ctrl Pts',(0.00163018392792171,0.155561118990352,
1.77811856032015));
#19514=CARTESIAN_POINT('Ctrl Pts',(-0.00137463617365801,0.155544834492541,
1.77833802929362));
#19515=CARTESIAN_POINT('Ctrl Pts',(-0.00190628019363298,0.155539227463588,
1.7783767211403));
#19516=CARTESIAN_POINT('Ctrl Pts',(-0.00273676651825873,0.155526209864854,
1.77843693442425));
#19517=CARTESIAN_POINT('Ctrl Pts',(-0.00303562697926189,0.155520663639465,
1.77845855683875));
#19518=CARTESIAN_POINT('Ctrl Pts',(-0.00359231848293808,0.155508727288098,
1.77849874513097));
#19519=CARTESIAN_POINT('Ctrl Pts',(-0.00385014687188625,0.155502557489095,
1.77851732262894));
#19520=CARTESIAN_POINT('Ctrl Pts',(-0.00443597061740971,0.155487080902078,
1.77855945390996));
#19521=CARTESIAN_POINT('Ctrl Pts',(-0.00476395208235854,0.155477377546403,
1.7785829853135));
#19522=CARTESIAN_POINT('Ctrl Pts',(-0.00561421528973363,0.155449529391081,
1.77864384800574));
#19523=CARTESIAN_POINT('Ctrl Pts',(-0.00613644649395696,0.155429790086746,
1.77868109245691));
#19524=CARTESIAN_POINT('Ctrl Pts',(-0.00941449492455507,0.155289338994041,
1.77891406980479));
#19525=CARTESIAN_POINT('Ctrl Pts',(-0.0121670130950097,0.155097962027391,
1.77910611946731));
#19526=CARTESIAN_POINT('Ctrl Pts',(-0.0163642092862801,0.15469369767609,
1.77939550118484));
#19527=CARTESIAN_POINT('Ctrl Pts',(-0.0178132250117427,0.154533545665462,
1.77949477075443));
#19528=CARTESIAN_POINT('Ctrl Pts',(-0.0210375272090124,0.154131224583442,
1.77971466890965));
#19529=CARTESIAN_POINT('Ctrl Pts',(-0.0228113228616239,0.153878705077222,
1.77983496857021));
#19530=CARTESIAN_POINT('Ctrl Pts',(-0.0342514347887873,0.15204790607571,
1.78060870008363));
#19531=CARTESIAN_POINT('Ctrl Pts',(-0.0437547698812458,0.149590296956172,
1.7812429162474));
#19532=CARTESIAN_POINT('Ctrl Pts',(-0.0565926488913294,0.144941255437753,
1.78215317429878));
#19533=CARTESIAN_POINT('Ctrl Pts',(-0.0601699153776717,0.143493061934122,
1.78241277129182));
#19534=CARTESIAN_POINT('Ctrl Pts',(-0.0636886300450479,0.141913920751225,
1.78267615293977));
#19535=CARTESIAN_POINT('Origin',(0.,0.,-0.129405622560373));
#19536=CARTESIAN_POINT('',(-0.0636886258329835,0.14191392264153,1.86645936880636));
#19537=CARTESIAN_POINT('',(-0.0636886270478348,0.141913922096325,1.85272361624831));
#19538=CARTESIAN_POINT('',(-0.0636886258329924,0.141913922641526,-0.129405622560373));
#19539=CARTESIAN_POINT('',(-0.155549955676549,-0.000117426673429394,1.80932156858097));
#19540=CARTESIAN_POINT('Ctrl Pts',(-0.0636886258329876,0.141913922641528,
1.86645936880636));
#19541=CARTESIAN_POINT('Ctrl Pts',(-0.0636564620419431,0.141928357220004,
1.86645680851686));
#19542=CARTESIAN_POINT('Ctrl Pts',(-0.0636242932870201,0.141942780889352,
1.86645424886815));
#19543=CARTESIAN_POINT('Ctrl Pts',(-0.0632942811561062,0.142090615390378,
1.86642800064363));
#19544=CARTESIAN_POINT('Ctrl Pts',(-0.0629960198527353,0.142223101137319,
1.86640436670713));
#19545=CARTESIAN_POINT('Ctrl Pts',(-0.0624613755478455,0.142458574836849,
1.8663621637997));
#19546=CARTESIAN_POINT('Ctrl Pts',(-0.0622251524764948,0.142561914208194,
1.86634357370127));
#19547=CARTESIAN_POINT('Ctrl Pts',(-0.0617131975510311,0.142784361743086,
1.86630340681509));
#19548=CARTESIAN_POINT('Ctrl Pts',(-0.0614373780922462,0.142903258492115,
1.86628184296741));
#19549=CARTESIAN_POINT('Ctrl Pts',(-0.0606665579334369,0.143232889651892,
1.86622178756415));
#19550=CARTESIAN_POINT('Ctrl Pts',(-0.0601707992166112,0.143441858862749,
1.86618340138882));
#19551=CARTESIAN_POINT('Ctrl Pts',(-0.0572994636863012,0.144634661035102,
1.86596239739613));
#19552=CARTESIAN_POINT('Ctrl Pts',(-0.0549006897583775,0.14556211750769,
1.86578297484937));
#19553=CARTESIAN_POINT('Ctrl Pts',(-0.0386103521660974,0.151400509948218,
1.86459203355857));
#19554=CARTESIAN_POINT('Ctrl Pts',(-0.0241036913399888,0.154376150486204,
1.86365816026321));
#19555=CARTESIAN_POINT('Ctrl Pts',(-0.00751453163996468,0.155379785751169,
1.86254161332361));
#19556=CARTESIAN_POINT('Ctrl Pts',(-0.00563369337086947,0.155459342306031,
1.8624144493627));
#19557=CARTESIAN_POINT('Ctrl Pts',(0.000290051260673029,0.15560226687935,
1.86201143129366));
#19558=CARTESIAN_POINT('Ctrl Pts',(0.00433395751572635,0.155542153580607,
1.86173257915957));
#19559=CARTESIAN_POINT('Ctrl Pts',(0.00923954774031282,0.155277784727314,
1.86138769066159));
#19560=CARTESIAN_POINT('Ctrl Pts',(0.0101080190607186,0.155223669484268,
1.86132638251121));
#19561=CARTESIAN_POINT('Ctrl Pts',(0.0115434237840658,0.155122130840707,
1.861224617874));
#19562=CARTESIAN_POINT('Ctrl Pts',(0.0121106410099563,0.155078878213475,
1.86118429194483));
#19563=CARTESIAN_POINT('Ctrl Pts',(0.0131365864351479,0.154994982734194,
1.86111114375714));
#19564=CARTESIAN_POINT('Ctrl Pts',(0.0135953979016833,0.154955412049647,
1.8610783554427));
#19565=CARTESIAN_POINT('Ctrl Pts',(0.0145793310951522,0.154866148093182,
1.86100787398236));
#19566=CARTESIAN_POINT('Ctrl Pts',(0.0151043879339209,0.154815820163473,
1.8609701613248));
#19567=CARTESIAN_POINT('Ctrl Pts',(0.0165354040004468,0.154671304854158,
1.86086709441261));
#19568=CARTESIAN_POINT('Ctrl Pts',(0.0174407956175257,0.154571830271281,
1.86080157515396));
#19569=CARTESIAN_POINT('Ctrl Pts',(0.022217170088745,0.154004555563906,
1.86045424302941));
#19570=CARTESIAN_POINT('Ctrl Pts',(0.0260700845105509,0.153399320174467,
1.86016815238346));
#19571=CARTESIAN_POINT('Ctrl Pts',(0.0444232491006836,0.149804927033222,
1.85877529464241));
#19572=CARTESIAN_POINT('Ctrl Pts',(0.0584690221189989,0.144900545957311,
1.85760838445969));
#19573=CARTESIAN_POINT('Ctrl Pts',(0.0755370563172391,0.13604985293001,
1.85613928008289));
#19574=CARTESIAN_POINT('Ctrl Pts',(0.0793795865855532,0.133844311176416,
1.85580562828475));
#19575=CARTESIAN_POINT('Ctrl Pts',(0.0836812765253949,0.131124682910041,
1.85543284471027));
#19576=CARTESIAN_POINT('Ctrl Pts',(0.0842371598384742,0.130768266232467,
1.85538468766181));
#19577=CARTESIAN_POINT('Ctrl Pts',(0.0850640872380474,0.130230602568646,
1.85531309257506));
#19578=CARTESIAN_POINT('Ctrl Pts',(0.085336848668374,0.130052032078268,
1.85528948402377));
#19579=CARTESIAN_POINT('Ctrl Pts',(0.0858243027934332,0.129730713466181,
1.85524730845479));
#19580=CARTESIAN_POINT('Ctrl Pts',(0.0860392028736441,0.129588288586679,
1.85522872042675));
#19581=CARTESIAN_POINT('Ctrl Pts',(0.0865039097251108,0.12927863885955,
1.85518853751938));
#19582=CARTESIAN_POINT('Ctrl Pts',(0.0867535854775034,0.129111224431017,
1.85516695567075));
#19583=CARTESIAN_POINT('Ctrl Pts',(0.0874497063912889,0.128641525318255,
1.85510679941594));
#19584=CARTESIAN_POINT('Ctrl Pts',(0.0878950735235377,0.128337637727252,
1.85506833096416));
#19585=CARTESIAN_POINT('Ctrl Pts',(0.0904708221408475,0.126560428105555,
1.85484590231258));
#19586=CARTESIAN_POINT('Ctrl Pts',(0.092565878869125,0.125036281979947,
1.85466518576827));
#19587=CARTESIAN_POINT('Ctrl Pts',(0.106303783438006,0.114507329475116,
1.8534742650543));
#19588=CARTESIAN_POINT('Ctrl Pts',(0.116656893927821,0.103940854068111,
1.85254128531495));
#19589=CARTESIAN_POINT('Ctrl Pts',(0.126498330036356,0.090540603257222,
1.85142426928196));
#19590=CARTESIAN_POINT('Ctrl Pts',(0.127597159841334,0.088985351218547,
1.85129562347155));
#19591=CARTESIAN_POINT('Ctrl Pts',(0.130925501772152,0.0840860669673104,
1.85089270111927));
#19592=CARTESIAN_POINT('Ctrl Pts',(0.133054005605272,0.0806757738536333,
1.85061548661836));
#19593=CARTESIAN_POINT('Ctrl Pts',(0.135478920018413,0.0764331017066894,
1.85027241012731));
#19594=CARTESIAN_POINT('Ctrl Pts',(0.135903560914175,0.0756754840238233,
1.85021121687891));
#19595=CARTESIAN_POINT('Ctrl Pts',(0.136595553117784,0.0744162643307243,
1.85010960357116));
#19596=CARTESIAN_POINT('Ctrl Pts',(0.136866543398813,0.0739166747831478,
1.85006931338459));
#19597=CARTESIAN_POINT('Ctrl Pts',(0.137352121588842,0.0730096516749289,
1.84999620338284));
#19598=CARTESIAN_POINT('Ctrl Pts',(0.137567650845395,0.0726027270505144,
1.84996341734699));
#19599=CARTESIAN_POINT('Ctrl Pts',(0.138026352217636,0.0717273114519083,
1.84989291119219));
#19600=CARTESIAN_POINT('Ctrl Pts',(0.138268952240869,0.0712585289502712,
1.84985517143316));
#19601=CARTESIAN_POINT('Ctrl Pts',(0.138924441542764,0.0699759584983784,
1.84975195488272));
#19602=CARTESIAN_POINT('Ctrl Pts',(0.139332557373286,0.0691597687649968,
1.84968631227857));
#19603=CARTESIAN_POINT('Ctrl Pts',(0.141456960674764,0.0648160461813629,
1.84933713336321));
#19604=CARTESIAN_POINT('Ctrl Pts',(0.143046377612563,0.0612284270731534,
1.8490492649099));
#19605=CARTESIAN_POINT('Ctrl Pts',(0.149972392480942,0.0438488933048152,
1.84765561813267));
#19606=CARTESIAN_POINT('Ctrl Pts',(0.153459237289211,0.0294034203451148,
1.84648999322492));
#19607=CARTESIAN_POINT('Ctrl Pts',(0.155272196199702,0.010289272616759,
1.84502299951898));
#19608=CARTESIAN_POINT('Ctrl Pts',(0.15550184761795,0.00587438691557986,
1.84469009565279));
#19609=CARTESIAN_POINT('Ctrl Pts',(0.155549367139988,0.000795280883174198,
1.84431804453059));
#19610=CARTESIAN_POINT('Ctrl Pts',(0.155551341470964,0.000135269279772496,
1.84426991090671));
#19611=CARTESIAN_POINT('Ctrl Pts',(0.155548015282042,-0.000850695760490853,
1.8441983437245));
#19612=CARTESIAN_POINT('Ctrl Pts',(0.155545891181125,-0.00117664073826175,
1.84417473984506));
#19613=CARTESIAN_POINT('Ctrl Pts',(0.155540252168953,-0.00176037473149842,
1.84413256930341));
#19614=CARTESIAN_POINT('Ctrl Pts',(0.155537120928838,-0.00201816269779856,
1.84411398165239));
#19615=CARTESIAN_POINT('Ctrl Pts',(0.155528949690423,-0.0025765673966196,
1.84407379577822));
#19616=CARTESIAN_POINT('Ctrl Pts',(0.155523679061816,-0.00287717684641305,
1.8440522106025));
#19617=CARTESIAN_POINT('Ctrl Pts',(0.155506517963022,-0.0037170266902462,
1.84399203570189));
#19618=CARTESIAN_POINT('Ctrl Pts',(0.155492694173688,-0.00425623049467691,
1.8439535520377));
#19619=CARTESIAN_POINT('Ctrl Pts',(0.155396105290372,-0.00738785208885911,
1.84373085868057));
#19620=CARTESIAN_POINT('Ctrl Pts',(0.155251308132826,-0.009978143621746,
1.84354990167561));
#19621=CARTESIAN_POINT('Ctrl Pts',(0.153853230496537,-0.0272309194385228,
1.84235898381934));
#19622=CARTESIAN_POINT('Ctrl Pts',(0.150589433582856,-0.0416565841488789,
1.84142616942558));
#19623=CARTESIAN_POINT('Ctrl Pts',(0.144666507281365,-0.0571930563456218,
1.84030906042476));
#19624=CARTESIAN_POINT('Ctrl Pts',(0.143954006901864,-0.0589634421328646,
1.84018013424006));
#19625=CARTESIAN_POINT('Ctrl Pts',(0.141642135899606,-0.0644160085607246,
1.83977722932767));
#19626=CARTESIAN_POINT('Ctrl Pts',(0.139932787840494,-0.0680494448601561,
1.83950032401785));
#19627=CARTESIAN_POINT('Ctrl Pts',(0.137685262712994,-0.0723831796436164,
1.83915758965993));
#19628=CARTESIAN_POINT('Ctrl Pts',(0.137279122640218,-0.0731505208210331,
1.83909641817064));
#19629=CARTESIAN_POINT('Ctrl Pts',(0.136596561435496,-0.0744144127340373,
1.83899483352174));
#19630=CARTESIAN_POINT('Ctrl Pts',(0.136323800816748,-0.0749129276819405,
1.83895455010541));
#19631=CARTESIAN_POINT('Ctrl Pts',(0.135825082211533,-0.0758126742612604,
1.8388814473313));
#19632=CARTESIAN_POINT('Ctrl Pts',(0.135600061426161,-0.0762144203499371,
1.83884866172163));
#19633=CARTESIAN_POINT('Ctrl Pts',(0.135113243312695,-0.0770745916055004,
1.83877815086338));
#19634=CARTESIAN_POINT('Ctrl Pts',(0.13485089013256,-0.077532693796875,
1.83874040595029));
#19635=CARTESIAN_POINT('Ctrl Pts',(0.134128524073201,-0.0787792792874892,
1.83863716093697));
#19636=CARTESIAN_POINT('Ctrl Pts',(0.133663900431018,-0.079565051817242,
1.83857149486996));
#19637=CARTESIAN_POINT('Ctrl Pts',(0.131163751583623,-0.0837096019302213,
1.8382219632588));
#19638=CARTESIAN_POINT('Ctrl Pts',(0.129008657715937,-0.0869941852401678,
1.83793375514853));
#19639=CARTESIAN_POINT('Ctrl Pts',(0.118159868929774,-0.102237932551405,
1.83653995653891));
#19640=CARTESIAN_POINT('Ctrl Pts',(0.107915092313449,-0.112997952342107,
1.83537457593628));
#19641=CARTESIAN_POINT('Ctrl Pts',(0.0928419949743466,-0.124882631437129,
1.83390798523657));
#19642=CARTESIAN_POINT('Ctrl Pts',(0.0892585910117333,-0.127468508177072,
1.83357522512988));
#19643=CARTESIAN_POINT('Ctrl Pts',(0.0850184828871368,-0.130261642765548,
1.83320331481461));
#19644=CARTESIAN_POINT('Ctrl Pts',(0.0844650618765273,-0.130621175053868,
1.83315518570705));
#19645=CARTESIAN_POINT('Ctrl Pts',(0.0836349106926757,-0.131153003956719,
1.83308362390508));
#19646=CARTESIAN_POINT('Ctrl Pts',(0.083359909733341,-0.13132796422693,
1.83306002092652));
#19647=CARTESIAN_POINT('Ctrl Pts',(0.0828664088163777,-0.131639763192521,
1.83301785135415));
#19648=CARTESIAN_POINT('Ctrl Pts',(0.082648117757366,-0.131776923617908,
1.8329992637757));
#19649=CARTESIAN_POINT('Ctrl Pts',(0.0821796301652738,-0.132069669821476,
1.83295951200915));
#19650=CARTESIAN_POINT('Ctrl Pts',(0.0819293331163704,-0.132225087180495,
1.83293835891954));
#19651=CARTESIAN_POINT('Ctrl Pts',(0.0812366087046629,-0.132652499503837,
1.83288004523023));
#19652=CARTESIAN_POINT('Ctrl Pts',(0.0807932528251867,-0.132922994763733,
1.83284298142844));
#19653=CARTESIAN_POINT('Ctrl Pts',(0.0797964936795299,-0.133524296518719,
1.83276021080323));
#19654=CARTESIAN_POINT('Ctrl Pts',(0.0792423678983951,-0.133853895464776,
1.83271457795244));
#19655=CARTESIAN_POINT('Ctrl Pts',(0.0775137429805142,-0.13486759998589,
1.83257335318037));
#19656=CARTESIAN_POINT('Ctrl Pts',(0.0763322792542339,-0.135539785033318,
1.83247843898825));
#19657=CARTESIAN_POINT('Ctrl Pts',(0.0716828811839098,-0.138104944678126,
1.83211054704997));
#19658=CARTESIAN_POINT('Ctrl Pts',(0.068151902602447,-0.139881144391765,
1.8318432060018));
#19659=CARTESIAN_POINT('Ctrl Pts',(0.0517969745066226,-0.147341675565304,
1.83064156364857));
#19660=CARTESIAN_POINT('Ctrl Pts',(0.0383091525225917,-0.151409762360861,
1.82974390620955));
#19661=CARTESIAN_POINT('Ctrl Pts',(0.0234906498389948,-0.15376915258353,
1.8287176225249));
#19662=CARTESIAN_POINT('Ctrl Pts',(0.0225214150315662,-0.153914095240971,
1.82865035313605));
#19663=CARTESIAN_POINT('Ctrl Pts',(0.0192895791703714,-0.154366214720551,
1.82842548450659));
#19664=CARTESIAN_POINT('Ctrl Pts',(0.0170216819466096,-0.154632718166361,
1.82826676225427));
#19665=CARTESIAN_POINT('Ctrl Pts',(0.0138781364727169,-0.15493212974269,
1.82804509243061));
#19666=CARTESIAN_POINT('Ctrl Pts',(0.0130067672610395,-0.15500771415759,
1.82798347167475));
#19667=CARTESIAN_POINT('Ctrl Pts',(0.0115663056362418,-0.155120431486351,
1.82788129539222));
#19668=CARTESIAN_POINT('Ctrl Pts',(0.010997555341956,-0.155161791209602,
1.8278408722943));
#19669=CARTESIAN_POINT('Ctrl Pts',(0.00996901504006827,-0.155230903523213,
1.82776762005582));
#19670=CARTESIAN_POINT('Ctrl Pts',(0.00950930247782793,-0.155259743100141,
1.82773482530713));
#19671=CARTESIAN_POINT('Ctrl Pts',(0.00852390171567526,-0.15531716828125,
1.82766440983169));
#19672=CARTESIAN_POINT('Ctrl Pts',(0.00799818427422717,-0.155345127696682,
1.82762676993899));
#19673=CARTESIAN_POINT('Ctrl Pts',(0.00656710084386395,-0.155413953818681,
1.82752410456597));
#19674=CARTESIAN_POINT('Ctrl Pts',(0.00566151576986955,-0.155449577129231,
1.82745891624326));
#19675=CARTESIAN_POINT('Ctrl Pts',(0.00112065133212638,-0.155588471614936,
1.827130884288));
#19676=CARTESIAN_POINT('Ctrl Pts',(-0.00251685938817576,-0.155572136556827,
1.82686434952662));
#19677=CARTESIAN_POINT('Ctrl Pts',(-0.0211178836382268,-0.15483610736433,
1.82548066633444));
#19678=CARTESIAN_POINT('Ctrl Pts',(-0.0359203693870522,-0.152084692956403,
1.82430027079617));
#19679=CARTESIAN_POINT('Ctrl Pts',(-0.0543748581382912,-0.145806716336831,
1.8228099120028));
#19680=CARTESIAN_POINT('Ctrl Pts',(-0.0585881334893525,-0.144165404552133,
1.82246919741571));
#19681=CARTESIAN_POINT('Ctrl Pts',(-0.0633313089393348,-0.142075288787899,
1.82208950700556));
#19682=CARTESIAN_POINT('Ctrl Pts',(-0.0639365256379832,-0.141803960127855,
1.82204113472764));
#19683=CARTESIAN_POINT('Ctrl Pts',(-0.0648371595087773,-0.141393252709448,
1.82196928330904));
#19684=CARTESIAN_POINT('Ctrl Pts',(-0.0651338924031497,-0.141256805962291,
1.82194563188759));
#19685=CARTESIAN_POINT('Ctrl Pts',(-0.0656641306598325,-0.141010960332821,
1.82190341012858));
#19686=CARTESIAN_POINT('Ctrl Pts',(-0.065897794752191,-0.140901914960937,
1.82188481858288));
#19687=CARTESIAN_POINT('Ctrl Pts',(-0.0663974298853807,-0.140667232593432,
1.82184509669582));
#19688=CARTESIAN_POINT('Ctrl Pts',(-0.0666633151911642,-0.140541422479324,
1.821823977286));
#19689=CARTESIAN_POINT('Ctrl Pts',(-0.0673932488709636,-0.140193499054368,
1.82176604602531));
#19690=CARTESIAN_POINT('Ctrl Pts',(-0.0678565604684636,-0.139969833863938,
1.82172932846458));
#19691=CARTESIAN_POINT('Ctrl Pts',(-0.0688929303610933,-0.139463167570136,
1.82164729626669));
#19692=CARTESIAN_POINT('Ctrl Pts',(-0.0694653753341122,-0.139178923074163,
1.82160205454881));
#19693=CARTESIAN_POINT('Ctrl Pts',(-0.0712349755614895,-0.138286599596392,
1.82146236315737));
#19694=CARTESIAN_POINT('Ctrl Pts',(-0.0724260578789047,-0.137666523916598,
1.82136857435658));
#19695=CARTESIAN_POINT('Ctrl Pts',(-0.0770261396153564,-0.135195497144179,
1.82100668035147));
#19696=CARTESIAN_POINT('Ctrl Pts',(-0.0803737028351996,-0.133232584158757,
1.82074401750884));
#19697=CARTESIAN_POINT('Ctrl Pts',(-0.0889778440617732,-0.12774489896864,
1.82006139434388));
#19698=CARTESIAN_POINT('Ctrl Pts',(-0.0940988123137882,-0.124021110263872,
1.81964717418066));
#19699=CARTESIAN_POINT('Ctrl Pts',(-0.107274675415437,-0.11315294392232,
1.81852213990994));
#19700=CARTESIAN_POINT('Ctrl Pts',(-0.11483708847046,-0.105469592136939,
1.81780778981687));
#19701=CARTESIAN_POINT('Ctrl Pts',(-0.12225534010549,-0.0961806920995499,
1.81697539317036));
#19702=CARTESIAN_POINT('Ctrl Pts',(-0.122954673636267,-0.0952850556319218,
1.81689545334115));
#19703=CARTESIAN_POINT('Ctrl Pts',(-0.123997902005043,-0.0939183835674643,
1.81677390713177));
#19704=CARTESIAN_POINT('Ctrl Pts',(-0.124349075167464,-0.0934529291236586,
1.81673258680023));
#19705=CARTESIAN_POINT('Ctrl Pts',(-0.124973655052058,-0.0926153403581597,
1.81665835866833));
#19706=CARTESIAN_POINT('Ctrl Pts',(-0.125248038816172,-0.0922439401316245,
1.8166254893906));
#19707=CARTESIAN_POINT('Ctrl Pts',(-0.125826704208121,-0.0914533287066598,
1.81655561062264));
#19708=CARTESIAN_POINT('Ctrl Pts',(-0.126130552970582,-0.0910338092071362,
1.81651858494027));
#19709=CARTESIAN_POINT('Ctrl Pts',(-0.126937929762812,-0.0899072738824901,
1.81641929804675));
#19710=CARTESIAN_POINT('Ctrl Pts',(-0.127437638408971,-0.0891975569703274,
1.81635689169476));
#19711=CARTESIAN_POINT('Ctrl Pts',(-0.129837449838406,-0.0857278654928895,
1.81605245436584));
#19712=CARTESIAN_POINT('Ctrl Pts',(-0.131653834759047,-0.0829113675733186,
1.81580730510471));
#19713=CARTESIAN_POINT('Ctrl Pts',(-0.139956286019524,-0.0690760177112689,
1.81461117564694));
#19714=CARTESIAN_POINT('Ctrl Pts',(-0.145157214274883,-0.0573456832257681,
1.81361539428185));
#19715=CARTESIAN_POINT('Ctrl Pts',(-0.149542666292154,-0.0428750426454134,
1.81244648344936));
#19716=CARTESIAN_POINT('Ctrl Pts',(-0.150170754217539,-0.0406204816221885,
1.81226617356169));
#19717=CARTESIAN_POINT('Ctrl Pts',(-0.151009461864669,-0.0373238742499031,
1.81200578953618));
#19718=CARTESIAN_POINT('Ctrl Pts',(-0.1512606415017,-0.0362925279388187,
1.81192478832263));
#19719=CARTESIAN_POINT('Ctrl Pts',(-0.152341911866877,-0.0316464705246524,
1.81156215943024));
#19720=CARTESIAN_POINT('Ctrl Pts',(-0.153053207698486,-0.0280049726370916,
1.81128406451051));
#19721=CARTESIAN_POINT('Ctrl Pts',(-0.153722844379017,-0.0237784405222317,
1.81097080115317));
#19722=CARTESIAN_POINT('Ctrl Pts',(-0.15380891120363,-0.0232152100761871,
1.81092924927667));
#19723=CARTESIAN_POINT('Ctrl Pts',(-0.15394119655569,-0.0223164777682235,
1.81086326808289));
#19724=CARTESIAN_POINT('Ctrl Pts',(-0.153989416428217,-0.0219812831971472,
1.81083873078794));
#19725=CARTESIAN_POINT('Ctrl Pts',(-0.154072695950437,-0.0213886503143945,
1.8107954772736));
#19726=CARTESIAN_POINT('Ctrl Pts',(-0.154108205726354,-0.0211312785174762,
1.81077673597431));
#19727=CARTESIAN_POINT('Ctrl Pts',(-0.154175500040681,-0.0206343423719801,
1.81074063407907));
#19728=CARTESIAN_POINT('Ctrl Pts',(-0.15420737101874,-0.0203947940315143,
1.81072326854061));
#19729=CARTESIAN_POINT('Ctrl Pts',(-0.154275728181463,-0.0198716866236958,
1.81068542668589));
#19730=CARTESIAN_POINT('Ctrl Pts',(-0.154311991230341,-0.0195880984587095,
1.8106649628452));
#19731=CARTESIAN_POINT('Ctrl Pts',(-0.15439900183165,-0.0188924093816475,
1.81061488322392));
#19732=CARTESIAN_POINT('Ctrl Pts',(-0.154448882006616,-0.0184801990277524,
1.81058531454102));
#19733=CARTESIAN_POINT('Ctrl Pts',(-0.15468090489266,-0.0164961782766216,
1.81044347774166));
#19734=CARTESIAN_POINT('Ctrl Pts',(-0.154840716091074,-0.0149217755762949,
1.81033237560722));
#19735=CARTESIAN_POINT('Ctrl Pts',(-0.155355261515561,-0.00894637900416368,
1.80991525300518));
#19736=CARTESIAN_POINT('Ctrl Pts',(-0.15554662219701,-0.004533140577823,
1.80961648263341));
#19737=CARTESIAN_POINT('Ctrl Pts',(-0.155549955676549,-0.000117426673429394,
1.80932156858097));
#19738=CARTESIAN_POINT('Ctrl Pts',(-0.155549955521704,-0.000117631611270232,
1.80932158226823));
#19739=CARTESIAN_POINT('Ctrl Pts',(-0.155560738863627,0.0141417017295138,
1.80836923805862));
#19740=CARTESIAN_POINT('Ctrl Pts',(-0.153610934688343,0.0283350059680006,
1.80745647397623));
#19741=CARTESIAN_POINT('Ctrl Pts',(-0.149198092134331,0.0440449895399718,
1.80633725968971));
#19742=CARTESIAN_POINT('Ctrl Pts',(-0.148602762839775,0.0460135851926938,
1.80619512336027));
#19743=CARTESIAN_POINT('Ctrl Pts',(-0.14750525529041,0.0493989841121755,
1.80594701719294));
#19744=CARTESIAN_POINT('Ctrl Pts',(-0.147021237269486,0.0508214077378316,
1.80584163231634));
#19745=CARTESIAN_POINT('Ctrl Pts',(-0.146300409230229,0.052843236139914,
1.8056901021855));
#19746=CARTESIAN_POINT('Ctrl Pts',(-0.146080350264335,0.0534485602310435,
1.80564451057016));
#19747=CARTESIAN_POINT('Ctrl Pts',(-0.145692988874763,0.0544938254972557,
1.80556538623048));
#19748=CARTESIAN_POINT('Ctrl Pts',(-0.145527435991347,0.0549344098854867,
1.8055319120577));
#19749=CARTESIAN_POINT('Ctrl Pts',(-0.145205745548454,0.0557788619924441,
1.80546751375657));
#19750=CARTESIAN_POINT('Ctrl Pts',(-0.145049915975545,0.0561828430569072,
1.80543660018784));
#19751=CARTESIAN_POINT('Ctrl Pts',(-0.14463836210943,0.0572366523974596,
1.80535568023318));
#19752=CARTESIAN_POINT('Ctrl Pts',(-0.144379947365159,0.0578854121581196,
1.80530558397854));
#19753=CARTESIAN_POINT('Ctrl Pts',(-0.143473777047417,0.0601165646048386,
1.80513231648243));
#19754=CARTESIAN_POINT('Ctrl Pts',(-0.142804325916678,0.0616899514174252,
1.80500841767145));
#19755=CARTESIAN_POINT('Ctrl Pts',(-0.13704350715295,0.0746328736371978,
1.80397451163622));
#19756=CARTESIAN_POINT('Ctrl Pts',(-0.130630140419206,0.0853617221118853,
1.80301710881141));
#19757=CARTESIAN_POINT('Ctrl Pts',(-0.11974069723175,0.0994307349326424,
1.80163736795009));
#19758=CARTESIAN_POINT('Ctrl Pts',(-0.116257570484368,0.103481825035288,
1.80122351873294));
#19759=CARTESIAN_POINT('Ctrl Pts',(-0.110651771172711,0.109360584763755,
1.80060435374106));
#19760=CARTESIAN_POINT('Ctrl Pts',(-0.108676792236485,0.1113234428085,1.80039416712177));
#19761=CARTESIAN_POINT('Ctrl Pts',(-0.105484411770058,0.114330247428091,
1.8000680034392));
#19762=CARTESIAN_POINT('Ctrl Pts',(-0.104301814567342,0.115410132263105,
1.79994996008178));
#19763=CARTESIAN_POINT('Ctrl Pts',(-0.102757966688457,0.116776773101693,
1.79979962313376));
#19764=CARTESIAN_POINT('Ctrl Pts',(-0.10241188418018,0.117080401635869,
1.79976616070373));
#19765=CARTESIAN_POINT('Ctrl Pts',(-0.101880673211268,0.117542291265832,
1.79971516827065));
#19766=CARTESIAN_POINT('Ctrl Pts',(-0.101696516859723,0.117701657893309,
1.79969755801851));
#19767=CARTESIAN_POINT('Ctrl Pts',(-0.101316590455687,0.118028884174733,
1.79966136685421));
#19768=CARTESIAN_POINT('Ctrl Pts',(-0.101120779604156,0.118196687496519,
1.7996427905456));
#19769=CARTESIAN_POINT('Ctrl Pts',(-0.100675826185169,0.118576082580841,
1.79960075005223));
#19770=CARTESIAN_POINT('Ctrl Pts',(-0.100426433879831,0.118787376104477,
1.79957730781075));
#19771=CARTESIAN_POINT('Ctrl Pts',(-0.0997798874355749,0.119331660390181,
1.79951684062115));
#19772=CARTESIAN_POINT('Ctrl Pts',(-0.0993817274198907,0.119663458847844,
1.79947990061539));
#19773=CARTESIAN_POINT('Ctrl Pts',(-0.0969100736687121,0.121702314961719,
1.79925236440348));
#19774=CARTESIAN_POINT('Ctrl Pts',(-0.0947941533135505,0.123357556214743,
1.79906525705705));
#19775=CARTESIAN_POINT('Ctrl Pts',(-0.0836215375643028,0.131640300423681,
1.79810995077965));
#19776=CARTESIAN_POINT('Ctrl Pts',(-0.0739152376547061,0.13732438993798,
1.79738602440817));
#19777=CARTESIAN_POINT('Ctrl Pts',(-0.0636886042805433,0.141913932313908,
1.79664456958818));
#19778=CARTESIAN_POINT('Ctrl Pts',(-0.0636886300450479,0.141913920751225,
1.78267615293977));
#19779=CARTESIAN_POINT('Ctrl Pts',(-0.0660993195437263,0.14083204301279,
1.7828565970601));
#19780=CARTESIAN_POINT('Ctrl Pts',(-0.0684825273057478,0.139688702071741,
1.78303880607663));
#19781=CARTESIAN_POINT('Ctrl Pts',(-0.0721719261371492,0.137801551123463,
1.78332771456659));
#19782=CARTESIAN_POINT('Ctrl Pts',(-0.0734979305663783,0.137098899853142,
1.78343297136628));
#19783=CARTESIAN_POINT('Ctrl Pts',(-0.0753778312888652,0.136067627770644,
1.78358434088179));
#19784=CARTESIAN_POINT('Ctrl Pts',(-0.075940205827141,0.135754564908042,
1.78362990145506));
#19785=CARTESIAN_POINT('Ctrl Pts',(-0.0769102537213168,0.135206644490763,
1.7837089809439));
#19786=CARTESIAN_POINT('Ctrl Pts',(-0.0773188377909223,0.134973409068957,
1.78374244142472));
#19787=CARTESIAN_POINT('Ctrl Pts',(-0.0781013399649563,0.134522007880192,
1.78380681971748));
#19788=CARTESIAN_POINT('Ctrl Pts',(-0.0784754183176416,0.134304127342873,
1.78383772700189));
#19789=CARTESIAN_POINT('Ctrl Pts',(-0.0794505923334774,0.133730675704304,
1.78391864458196));
#19790=CARTESIAN_POINT('Ctrl Pts',(-0.0800502055771495,0.133372616394951,
1.78396874479226));
#19791=CARTESIAN_POINT('Ctrl Pts',(-0.0821104010587525,0.132123472014965,
1.78414209602427));
#19792=CARTESIAN_POINT('Ctrl Pts',(-0.0835586318831108,0.131212363832694,
1.78426607572063));
#19793=CARTESIAN_POINT('Ctrl Pts',(-0.0853677588334433,0.130032111762796,
1.78442371875312));
#19794=CARTESIAN_POINT('Ctrl Pts',(-0.0857429610185856,0.129785010558621,
1.78445656564615));
#19795=CARTESIAN_POINT('Ctrl Pts',(-0.0873986339145944,0.128684301854563,
1.78460219098865));
#19796=CARTESIAN_POINT('Ctrl Pts',(-0.0886674266789305,0.1278133713383,
1.78471559824639));
#19797=CARTESIAN_POINT('Ctrl Pts',(-0.0901471572161616,0.126765010868033,
1.78485003112098));
#19798=CARTESIAN_POINT('Ctrl Pts',(-0.090370843407186,0.126605642033457,
1.78487041218998));
#19799=CARTESIAN_POINT('Ctrl Pts',(-0.0906681003255401,0.126392667387216,
1.78489757573141));
#19800=CARTESIAN_POINT('Ctrl Pts',(-0.0907420488753485,0.126339587429039,
1.78490433973949));
#19801=CARTESIAN_POINT('Ctrl Pts',(-0.102437483933876,0.117929088007935,
1.78597514634011));
#19802=CARTESIAN_POINT('Ctrl Pts',(-0.112848559638326,0.10800818693888,
1.78709972280912));
#19803=CARTESIAN_POINT('Ctrl Pts',(-0.123971048553361,0.0940195166007185,
1.7884711231809));
#19804=CARTESIAN_POINT('Ctrl Pts',(-0.126091641044852,0.0911558683767185,
1.78874191736275));
#19805=CARTESIAN_POINT('Ctrl Pts',(-0.129194697338093,0.0866497298841924,
1.78915038510548));
#19806=CARTESIAN_POINT('Ctrl Pts',(-0.130248259928525,0.0850578461985455,
1.78929146074993));
#19807=CARTESIAN_POINT('Ctrl Pts',(-0.131534996704143,0.0830336492029423,
1.78946646280861));
#19808=CARTESIAN_POINT('Ctrl Pts',(-0.131795728586652,0.0826191757504856,
1.78950206909926));
#19809=CARTESIAN_POINT('Ctrl Pts',(-0.132207560964326,0.0819575939476739,
1.78955853505648));
#19810=CARTESIAN_POINT('Ctrl Pts',(-0.132359932985498,0.0817112876269627,
1.78957947646506));
#19811=CARTESIAN_POINT('Ctrl Pts',(-0.132647573136666,0.0812434073068773,
1.7896191013932));
#19812=CARTESIAN_POINT('Ctrl Pts',(-0.132782972792836,0.081021923128343,
1.78963779308804));
#19813=CARTESIAN_POINT('Ctrl Pts',(-0.133093183275362,0.0805116205024207,
1.78968070943139));
#19814=CARTESIAN_POINT('Ctrl Pts',(-0.133267608817349,0.0802225711146323,
1.78970490880335));
#19815=CARTESIAN_POINT('Ctrl Pts',(-0.133732131629205,0.0794470907854553,
1.78976954596523));
#19816=CARTESIAN_POINT('Ctrl Pts',(-0.134020519326323,0.0789596332954653,
1.7898098755891));
#19817=CARTESIAN_POINT('Ctrl Pts',(-0.136135832341254,0.0753391723804295,
1.79010728011749));
#19818=CARTESIAN_POINT('Ctrl Pts',(-0.137855533453968,0.0721443898547238,
1.79035794716405));
#19819=CARTESIAN_POINT('Ctrl Pts',(-0.140324060946091,0.0671472110759991,
1.79073686992327));
#19820=CARTESIAN_POINT('Ctrl Pts',(-0.141153210864882,0.0653862495728781,
1.79086797575452));
#19821=CARTESIAN_POINT('Ctrl Pts',(-0.146464826947219,0.0535331182565205,
1.79173739516868));
#19822=CARTESIAN_POINT('Ctrl Pts',(-0.149894712614579,0.0430038453052157,
1.79244953890622));
#19823=CARTESIAN_POINT('Ctrl Pts',(-0.15337120981272,0.0265734408528152,
1.79357441874203));
#19824=CARTESIAN_POINT('Ctrl Pts',(-0.154248625780776,0.0208859992640989,
1.79396571069371));
#19825=CARTESIAN_POINT('Ctrl Pts',(-0.154946063020434,0.0137656402587616,
1.79446506825141));
#19826=CARTESIAN_POINT('Ctrl Pts',(-0.155064040519323,0.012366018279522,
1.79456366349082));
#19827=CARTESIAN_POINT('Ctrl Pts',(-0.155207222483695,0.0103398906956653,
1.7947071078982));
#19828=CARTESIAN_POINT('Ctrl Pts',(-0.155247620745165,0.00971449859113958,
1.79475148224923));
#19829=CARTESIAN_POINT('Ctrl Pts',(-0.15531155967217,0.00862209785140042,
1.79482917205834));
#19830=CARTESIAN_POINT('Ctrl Pts',(-0.155336775987848,0.00815519197361416,
1.79486243474348));
#19831=CARTESIAN_POINT('Ctrl Pts',(-0.155381489267641,0.00725164310437124,
1.79492691776882));
#19832=CARTESIAN_POINT('Ctrl Pts',(-0.155401251826188,0.00681501712472446,
1.79495812948408));
#19833=CARTESIAN_POINT('Ctrl Pts',(-0.155443880419716,0.00577629483704786,
1.7950325063112));
#19834=CARTESIAN_POINT('Ctrl Pts',(-0.155465088631871,0.0051741414487422,
1.7950757228151));
#19835=CARTESIAN_POINT('Ctrl Pts',(-0.1555281175846,0.00303062474474945,
1.79522992849819));
#19836=CARTESIAN_POINT('Ctrl Pts',(-0.155550516320546,0.00148882645850541,
1.79534152011039));
#19837=CARTESIAN_POINT('Ctrl Pts',(-0.155547567385575,-0.00716617543588156,
1.7959719428411));
#19838=CARTESIAN_POINT('Ctrl Pts',(-0.155057239775376,-0.0142696878047434,
1.7965050829819));
#19839=CARTESIAN_POINT('Ctrl Pts',(-0.152542314054278,-0.0324507130486709,
1.79790842307936));
#19840=CARTESIAN_POINT('Ctrl Pts',(-0.149799043234581,-0.0433870598182914,
1.79879230599892));
#19841=CARTESIAN_POINT('Ctrl Pts',(-0.144597648413662,-0.0574583069646395,
1.7999331806907));
#19842=CARTESIAN_POINT('Ctrl Pts',(-0.143166574684856,-0.0609366453009342,
1.80021518730951));
#19843=CARTESIAN_POINT('Ctrl Pts',(-0.141351425281628,-0.0649304991732725,
1.80053635122305));
#19844=CARTESIAN_POINT('Ctrl Pts',(-0.141088705842597,-0.0654994066505062,
1.80058203520829));
#19845=CARTESIAN_POINT('Ctrl Pts',(-0.140685242475547,-0.0663593969260929,
1.80065097868876));
#19846=CARTESIAN_POINT('Ctrl Pts',(-0.140547021498559,-0.0666516448698306,
1.80067438732942));
#19847=CARTESIAN_POINT('Ctrl Pts',(-0.140297049425733,-0.0671759387921151,
1.80071634337122));
#19848=CARTESIAN_POINT('Ctrl Pts',(-0.140185632876428,-0.0674081387414485,
1.80073491088125));
#19849=CARTESIAN_POINT('Ctrl Pts',(-0.139942102350116,-0.067912458271536,
1.80077520724378));
#19850=CARTESIAN_POINT('Ctrl Pts',(-0.13980977154196,-0.0681844687908162,
1.80079692237223));
#19851=CARTESIAN_POINT('Ctrl Pts',(-0.139435443380284,-0.0689482415791615,
1.80085784673591));
#19852=CARTESIAN_POINT('Ctrl Pts',(-0.13919163593693,-0.0694391200753304,
1.80089694555382));
#19853=CARTESIAN_POINT('Ctrl Pts',(-0.137711901960155,-0.0723792856437115,
1.80113084839836));
#19854=CARTESIAN_POINT('Ctrl Pts',(-0.136413851222573,-0.074797009417925,
1.80132200456924));
#19855=CARTESIAN_POINT('Ctrl Pts',(-0.127812274866051,-0.0898484976299198,
1.80251263430261));
#19856=CARTESIAN_POINT('Ctrl Pts',(-0.118824899933258,-0.101437051090246,
1.8034382554979));
#19857=CARTESIAN_POINT('Ctrl Pts',(-0.106863679347039,-0.113049832999375,
1.80455860297636));
#19858=CARTESIAN_POINT('Ctrl Pts',(-0.105345721639859,-0.114465667781599,
1.80469894264839));
#19859=CARTESIAN_POINT('Ctrl Pts',(-0.100946634805867,-0.118407163799,1.80510136841206));
#19860=CARTESIAN_POINT('Ctrl Pts',(-0.0980000889938683,-0.120857179759862,
1.80536591627675));
#19861=CARTESIAN_POINT('Ctrl Pts',(-0.094223240516612,-0.123768589372263,
1.80570078304102));
#19862=CARTESIAN_POINT('Ctrl Pts',(-0.0934750117855153,-0.124334648716937,
1.8057669226331));
#19863=CARTESIAN_POINT('Ctrl Pts',(-0.0922889535057659,-0.125215183091308,
1.80587147538308));
#19864=CARTESIAN_POINT('Ctrl Pts',(-0.0918545225953824,-0.125534217173092,
1.80590971093589));
#19865=CARTESIAN_POINT('Ctrl Pts',(-0.0910837666838125,-0.12609409606157,
1.80597744626916));
#19866=CARTESIAN_POINT('Ctrl Pts',(-0.0907481206592936,-0.126335870621284,
1.80600690981264));
#19867=CARTESIAN_POINT('Ctrl Pts',(-0.0899758631602345,-0.126887482348012,
1.80607462551528));
#19868=CARTESIAN_POINT('Ctrl Pts',(-0.0895386105955854,-0.127196408469037,
1.806112912097));
#19869=CARTESIAN_POINT('Ctrl Pts',(-0.0883231888106177,-0.1280457512492,
1.80621919341197));
#19870=CARTESIAN_POINT('Ctrl Pts',(-0.0875416752411319,-0.128581317137559,
1.80628737098144));
#19871=CARTESIAN_POINT('Ctrl Pts',(-0.0830573240377973,-0.131594579400806,
1.80667772327069));
#19872=CARTESIAN_POINT('Ctrl Pts',(-0.0792546492225045,-0.133919175292075,
1.80700553961995));
#19873=CARTESIAN_POINT('Ctrl Pts',(-0.0667617630725284,-0.140837575497677,
1.80807385880212));
#19874=CARTESIAN_POINT('Ctrl Pts',(-0.0577350301942027,-0.144772140236993,
1.80883464127416));
#19875=CARTESIAN_POINT('Ctrl Pts',(-0.0454155540406945,-0.148805527999693,
1.80983969709433));
#19876=CARTESIAN_POINT('Ctrl Pts',(-0.0424031260308537,-0.149691795115015,
1.81008277682033));
#19877=CARTESIAN_POINT('Ctrl Pts',(-0.0339685556882593,-0.151898203642045,
1.8107532468151));
#19878=CARTESIAN_POINT('Ctrl Pts',(-0.0284984445059328,-0.153018893773931,
1.81117672278218));
#19879=CARTESIAN_POINT('Ctrl Pts',(-0.0222966298226149,-0.153945247472467,
1.81163632006117));
#19880=CARTESIAN_POINT('Ctrl Pts',(-0.0216132823917812,-0.154042672635799,
1.81168668193879));
#19881=CARTESIAN_POINT('Ctrl Pts',(-0.0206004328109134,-0.154180202394673,
1.81176089314641));
#19882=CARTESIAN_POINT('Ctrl Pts',(-0.0202714272233383,-0.154223804538641,
1.81178493151334));
#19883=CARTESIAN_POINT('Ctrl Pts',(-0.0196861668887895,-0.154299462162193,
1.81182756935953));
#19884=CARTESIAN_POINT('Ctrl Pts',(-0.019429970062829,-0.15433193272133,
1.81184619184856));
#19885=CARTESIAN_POINT('Ctrl Pts',(-0.0188795836738217,-0.154400296799664,
1.81188610735996));
#19886=CARTESIAN_POINT('Ctrl Pts',(-0.0185853727809231,-0.154435987561571,
1.81190738885477));
#19887=CARTESIAN_POINT('Ctrl Pts',(-0.017774589932738,-0.154531993232262,
1.81196588787537));
#19888=CARTESIAN_POINT('Ctrl Pts',(-0.0172578081988455,-0.154590559402815,
1.81200300866115));
#19889=CARTESIAN_POINT('Ctrl Pts',(-0.0144534021128516,-0.154894140810337,
1.81220360099765));
#19890=CARTESIAN_POINT('Ctrl Pts',(-0.0121606943537004,-0.155090988527376,
1.81236452802214));
#19891=CARTESIAN_POINT('Ctrl Pts',(0.00442615334605453,-0.156144975493712,
1.81351220119229));
#19892=CARTESIAN_POINT('Ctrl Pts',(0.0187751646110651,-0.155075624351142,
1.81442184189406));
#19893=CARTESIAN_POINT('Ctrl Pts',(0.0356907355888509,-0.151429388518624,
1.8155796519892));
#19894=CARTESIAN_POINT('Ctrl Pts',(0.0385859211185941,-0.15071766147605,
1.81578069014362));
#19895=CARTESIAN_POINT('Ctrl Pts',(0.0450329377410033,-0.148934847196117,
1.81623688953109));
#19896=CARTESIAN_POINT('Ctrl Pts',(0.0485703607026916,-0.147819046283623,
1.81649314541671));
#19897=CARTESIAN_POINT('Ctrl Pts',(0.0529387295115218,-0.146267407488952,
1.81681872475852));
#19898=CARTESIAN_POINT('Ctrl Pts',(0.0538103341798763,-0.145949002890421,
1.81688414689994));
#19899=CARTESIAN_POINT('Ctrl Pts',(0.0551814079429259,-0.145434186813767,
1.81698781209391));
#19900=CARTESIAN_POINT('Ctrl Pts',(0.0556828093102768,-0.145242952362378,
1.81702588253904));
#19901=CARTESIAN_POINT('Ctrl Pts',(0.0566077790248279,-0.144884675386082,
1.81709641511479));
#19902=CARTESIAN_POINT('Ctrl Pts',(0.0570316243283967,-0.144718359672256,
1.81712885259955));
#19903=CARTESIAN_POINT('Ctrl Pts',(0.0579704130695654,-0.144345216931998,
1.81720096412459));
#19904=CARTESIAN_POINT('Ctrl Pts',(0.0584849901120479,-0.144137491165365,
1.81724066804496));
#19905=CARTESIAN_POINT('Ctrl Pts',(0.0599591696251532,-0.143533196780265,
1.81735493107821));
#19906=CARTESIAN_POINT('Ctrl Pts',(0.0609159111996078,-0.143129774210828,
1.8174297206714));
#19907=CARTESIAN_POINT('Ctrl Pts',(0.0677178553124872,-0.140181094127348,
1.81796607029896));
#19908=CARTESIAN_POINT('Ctrl Pts',(0.0734049020781071,-0.137288550936618,
1.81843946477828));
#19909=CARTESIAN_POINT('Ctrl Pts',(0.0889259439808886,-0.128153719506339,
1.81980497193102));
#19910=CARTESIAN_POINT('Ctrl Pts',(0.0982598328355665,-0.12114520778316,
1.82071862790115));
#19911=CARTESIAN_POINT('Ctrl Pts',(0.107372640040885,-0.112550941083126,
1.82167832073806));
#19912=CARTESIAN_POINT('Ctrl Pts',(0.108016307700081,-0.111933352892162,
1.82174649227641));
#19913=CARTESIAN_POINT('Ctrl Pts',(0.109290533549153,-0.110689527238917,
1.82188216856525));
#19914=CARTESIAN_POINT('Ctrl Pts',(0.109921111213798,-0.110063352362464,
1.82194967260876));
#19915=CARTESIAN_POINT('Ctrl Pts',(0.112790446884848,-0.107164794065537,
1.82225838512181));
#19916=CARTESIAN_POINT('Ctrl Pts',(0.114964542771656,-0.10482907839211,
1.82249668855405));
#19917=CARTESIAN_POINT('Ctrl Pts',(0.117424940355258,-0.102017076636863,
1.82277005737856));
#19918=CARTESIAN_POINT('Ctrl Pts',(0.117782272923036,-0.101604314631881,
1.8228098547045));
#19919=CARTESIAN_POINT('Ctrl Pts',(0.118353141528868,-0.100937834051706,
1.82287357603107));
#19920=CARTESIAN_POINT('Ctrl Pts',(0.118568047962958,-0.100685304094595,
1.82289759698814));
#19921=CARTESIAN_POINT('Ctrl Pts',(0.118949252924753,-0.100234448734355,
1.82294026134793));
#19922=CARTESIAN_POINT('Ctrl Pts',(0.119115865551268,-0.100036393689773,
1.82295892753767));
#19923=CARTESIAN_POINT('Ctrl Pts',(0.11947009688091,-0.0996131735623726,
1.82299865307639));
#19924=CARTESIAN_POINT('Ctrl Pts',(0.119657573375082,-0.0993878943018883,
1.82301970211499));
#19925=CARTESIAN_POINT('Ctrl Pts',(0.120166483775259,-0.0987728399755167,
1.8230769112006));
#19926=CARTESIAN_POINT('Ctrl Pts',(0.120486661144623,-0.0983820219601504,
1.82311298145283));
#19927=CARTESIAN_POINT('Ctrl Pts',(0.122127374922265,-0.0963592947283289,
1.82329826361165));
#19928=CARTESIAN_POINT('Ctrl Pts',(0.12341676408973,-0.0947022328146605,
1.82344536802031));
#19929=CARTESIAN_POINT('Ctrl Pts',(0.127126826336368,-0.0897297040578735,
1.82387489839765));
#19930=CARTESIAN_POINT('Ctrl Pts',(0.129450397223665,-0.0863437902506564,
1.82415223531415));
#19931=CARTESIAN_POINT('Ctrl Pts',(0.137192624616017,-0.0740453521775083,
1.8251223837964));
#19932=CARTESIAN_POINT('Ctrl Pts',(0.141846434226912,-0.064684847224075,
1.82579642226397));
#19933=CARTESIAN_POINT('Ctrl Pts',(0.146581187528148,-0.0521405823635516,
1.82669353215479));
#19934=CARTESIAN_POINT('Ctrl Pts',(0.147553220218096,-0.049322718362778,
1.82689452583116));
#19935=CARTESIAN_POINT('Ctrl Pts',(0.149552901486416,-0.0429361484432803,
1.82735093735407));
#19936=CARTESIAN_POINT('Ctrl Pts',(0.150534869711399,-0.0393552076327877,
1.82760745739826));
#19937=CARTESIAN_POINT('Ctrl Pts',(0.151601063376423,-0.034839371066159,
1.82793333279798));
#19938=CARTESIAN_POINT('Ctrl Pts',(0.151806269759443,-0.033934062359601,
1.82799877814057));
#19939=CARTESIAN_POINT('Ctrl Pts',(0.152117313596115,-0.0325025147192592,
1.82810247204166));
#19940=CARTESIAN_POINT('Ctrl Pts',(0.152228553651633,-0.031977460793193,
1.82814054783209));
#19941=CARTESIAN_POINT('Ctrl Pts',(0.152429134973468,-0.0310059448483054,
1.82821108547675));
#19942=CARTESIAN_POINT('Ctrl Pts',(0.152519237897706,-0.0305596444303453,
1.82824352265947));
#19943=CARTESIAN_POINT('Ctrl Pts',(0.152714790353047,-0.0295686176922568,
1.82831562752342));
#19944=CARTESIAN_POINT('Ctrl Pts',(0.152819286971521,-0.0290237120227464,
1.82835532505633));
#19945=CARTESIAN_POINT('Ctrl Pts',(0.153110884644325,-0.0274579085000242,
1.8284695516337));
#19946=CARTESIAN_POINT('Ctrl Pts',(0.153290682892403,-0.0264356989142027,
1.82854431092911));
#19947=CARTESIAN_POINT('Ctrl Pts',(0.154499878070304,-0.0191334435096642,
1.82907979760083));
#19948=CARTESIAN_POINT('Ctrl Pts',(0.155153109478316,-0.0127981444706719,
1.82955231542756));
#19949=CARTESIAN_POINT('Ctrl Pts',(0.15589327309689,0.0050602976572865,
1.8309074224547));
#19950=CARTESIAN_POINT('Ctrl Pts',(0.155091624561486,0.0165790394049576,
1.83181089860493));
#19951=CARTESIAN_POINT('Ctrl Pts',(0.152818973036498,0.0290432345926528,
1.83278231029944));
#19952=CARTESIAN_POINT('Ctrl Pts',(0.152598141460801,0.0301820365419172,
1.83287096904561));
#19953=CARTESIAN_POINT('Ctrl Pts',(0.151581035387582,0.0351302943827947,
1.83325553092566));
#19954=CARTESIAN_POINT('Ctrl Pts',(0.150654612573212,0.0389119779843826,
1.8335477137593));
#19955=CARTESIAN_POINT('Ctrl Pts',(0.149413908964097,0.0432629820613394,
1.83387897875532));
#19956=CARTESIAN_POINT('Ctrl Pts',(0.149236919992898,0.0438696199729306,
1.83392505225227));
#19957=CARTESIAN_POINT('Ctrl Pts',(0.148963475759938,0.0447860540657251,
1.83399446576866));
#19958=CARTESIAN_POINT('Ctrl Pts',(0.148869743022015,0.0450966447426477,
1.83401795793707));
#19959=CARTESIAN_POINT('Ctrl Pts',(0.148699835394235,0.0456533440427679,
1.83406000313021));
#19960=CARTESIAN_POINT('Ctrl Pts',(0.148624020592433,0.045899557459171,
1.83407857665016));
#19961=CARTESIAN_POINT('Ctrl Pts',(0.148458116425995,0.0464336207548007,
1.83411881663422));
#19962=CARTESIAN_POINT('Ctrl Pts',(0.148367801696054,0.0467213965250036,
1.83414046968378));
#19963=CARTESIAN_POINT('Ctrl Pts',(0.148112233844685,0.0475275148505829,
1.83420104506756));
#19964=CARTESIAN_POINT('Ctrl Pts',(0.147945095322541,0.0480452627835881,
1.8342398590029));
#19965=CARTESIAN_POINT('Ctrl Pts',(0.146940498640245,0.0511022643155373,
1.83446854775261));
#19966=CARTESIAN_POINT('Ctrl Pts',(0.146040333109687,0.053620658169714,
1.83465496131582));
#19967=CARTESIAN_POINT('Ctrl Pts',(0.139792189951052,0.0697742106026303,
1.83584546365845));
#19968=CARTESIAN_POINT('Ctrl Pts',(0.132605760892131,0.0826203013978173,
1.83677421386824));
#19969=CARTESIAN_POINT('Ctrl Pts',(0.122525980638904,0.095849447959219,
1.83789175117716));
#19970=CARTESIAN_POINT('Ctrl Pts',(0.121294500062462,0.0974031641989691,
1.8380257341323));
#19971=CARTESIAN_POINT('Ctrl Pts',(0.117532433172077,0.101967620598429,
1.83842840073955));
#19972=CARTESIAN_POINT('Ctrl Pts',(0.114917183916687,0.104906171616982,
1.83869980622522));
#19973=CARTESIAN_POINT('Ctrl Pts',(0.111537998011291,0.108424966472421,
1.83904234511952));
#19974=CARTESIAN_POINT('Ctrl Pts',(0.110876199861009,0.109101634216439,
1.83910906154016));
#19975=CARTESIAN_POINT('Ctrl Pts',(0.10982657322855,0.110155430521953,1.83921432763862));
#19976=CARTESIAN_POINT('Ctrl Pts',(0.10944287425874,0.110536656006763,1.83925269564785));
#19977=CARTESIAN_POINT('Ctrl Pts',(0.108762269989605,0.11120585507206,1.83932055947829));
#19978=CARTESIAN_POINT('Ctrl Pts',(0.108466188023637,0.111494661868445,
1.83935001843572));
#19979=CARTESIAN_POINT('Ctrl Pts',(0.107785543376571,0.112153304925547,
1.8394175970538));
#19980=CARTESIAN_POINT('Ctrl Pts',(0.10740022451946,0.112522348565853,1.83945575055955));
#19981=CARTESIAN_POINT('Ctrl Pts',(0.106331536040258,0.113535407207977,
1.83956129223723));
#19982=CARTESIAN_POINT('Ctrl Pts',(0.105644231564068,0.114175218466854,
1.83962885908791));
#19983=CARTESIAN_POINT('Ctrl Pts',(0.101762631557791,0.117723541423356,
1.84000878330593));
#19984=CARTESIAN_POINT('Ctrl Pts',(0.0984543531845678,0.120503937292651,
1.84032643315056));
#19985=CARTESIAN_POINT('Ctrl Pts',(0.0876887107061473,0.128812275736433,
1.84134267010741));
#19986=CARTESIAN_POINT('Ctrl Pts',(0.0798508008916404,0.133812249993449,
1.84205912617447));
#19987=CARTESIAN_POINT('Ctrl Pts',(0.063869432813875,0.142100795277643,
1.84345531006633));
#19988=CARTESIAN_POINT('Ctrl Pts',(0.0557983230588078,0.145459693439072,
1.84413190748522));
#19989=CARTESIAN_POINT('Ctrl Pts',(0.0463798087230875,0.148479185020984,
1.84486312267671));
#19990=CARTESIAN_POINT('Ctrl Pts',(0.0452683488239298,0.14882181242591,
1.84494850821844));
#19991=CARTESIAN_POINT('Ctrl Pts',(0.0437474753535629,0.149272033066379,
1.84506402214846));
#19992=CARTESIAN_POINT('Ctrl Pts',(0.0433413493375018,0.149390457876521,
1.84509474036294));
#19993=CARTESIAN_POINT('Ctrl Pts',(0.042696897616408,0.149575528304435,
1.8451432767349));
#19994=CARTESIAN_POINT('Ctrl Pts',(0.0424588914603739,0.14964326336967,
1.84516115710521));
#19995=CARTESIAN_POINT('Ctrl Pts',(0.0419830460689904,0.149777459337608,
1.84519681432051));
#19996=CARTESIAN_POINT('Ctrl Pts',(0.0417452103449352,0.149843921788952,
1.84521459088366));
#19997=CARTESIAN_POINT('Ctrl Pts',(0.0412001750947033,0.149994831822142,
1.84525522607425));
#19998=CARTESIAN_POINT('Ctrl Pts',(0.0408928704552919,0.150078903087757,
1.8452780629343));
#19999=CARTESIAN_POINT('Ctrl Pts',(0.0399183311950965,0.150342298394119,
1.8453502555376));
#20000=CARTESIAN_POINT('Ctrl Pts',(0.0392501462326343,0.15051812488837,
1.84539941460077));
#20001=CARTESIAN_POINT('Ctrl Pts',(0.0376800354154955,0.150920117894542,
1.84551418364878));
#20002=CARTESIAN_POINT('Ctrl Pts',(0.0367771982865184,0.151142663882436,
1.84557960291966));
#20003=CARTESIAN_POINT('Ctrl Pts',(0.0260358983979863,0.15368840576173,
1.84635170687233));
#20004=CARTESIAN_POINT('Ctrl Pts',(0.0159939699430354,0.155055637559006,
1.84701287198638));
#20005=CARTESIAN_POINT('Ctrl Pts',(-0.00477519838170218,0.155842517043863,
1.84838083111003));
#20006=CARTESIAN_POINT('Ctrl Pts',(-0.0154511770288652,0.155148025289232,
1.84908550015695));
#20007=CARTESIAN_POINT('Ctrl Pts',(-0.0277029342446309,0.153073298042157,
1.8499489559353));
#20008=CARTESIAN_POINT('Ctrl Pts',(-0.0294294398859672,0.15275076029185,
1.8500718556735));
#20009=CARTESIAN_POINT('Ctrl Pts',(-0.0318418007782946,0.152257678713395,
1.85024545977228));
#20010=CARTESIAN_POINT('Ctrl Pts',(-0.0325325655679186,0.152111581255175,
1.85029538769803));
#20011=CARTESIAN_POINT('Ctrl Pts',(-0.0336466039222151,0.151868025541415,
1.85037627150864));
#20012=CARTESIAN_POINT('Ctrl Pts',(-0.0340705118489478,0.151773486988713,
1.85040713391551));
#20013=CARTESIAN_POINT('Ctrl Pts',(-0.0349517304995187,0.151573082618227,
1.85047147030397));
#20014=CARTESIAN_POINT('Ctrl Pts',(-0.0354089684165464,0.151466919774893,
1.85050495350313));
#20015=CARTESIAN_POINT('Ctrl Pts',(-0.0364860651375931,0.151211692650571,
1.85058407059821));
#20016=CARTESIAN_POINT('Ctrl Pts',(-0.0371054977746631,0.151060884930411,
1.85062976001696));
#20017=CARTESIAN_POINT('Ctrl Pts',(-0.0391457136313872,0.150550866002977,
1.8507808845945));
#20018=CARTESIAN_POINT('Ctrl Pts',(-0.0405623092609289,0.150175393936783,
1.85088684038298));
#20019=CARTESIAN_POINT('Ctrl Pts',(-0.0438918500549089,0.149242345557987,
1.85113838253134));
#20020=CARTESIAN_POINT('Ctrl Pts',(-0.0457997631904259,0.148667929376365,
1.85128449512738));
#20021=CARTESIAN_POINT('Ctrl Pts',(-0.0526889163383386,0.146448613827277,
1.8518194535888));
#20022=CARTESIAN_POINT('Ctrl Pts',(-0.0575967032354593,0.144588822137862,
1.85221485904219));
#20023=CARTESIAN_POINT('Ctrl Pts',(-0.06283094935431,0.142296503403254,
1.85265170021791));
#20024=CARTESIAN_POINT('Ctrl Pts',(-0.063260249095217,0.142106171054403,
1.85268764120887));
#20025=CARTESIAN_POINT('Ctrl Pts',(-0.0636886270478348,0.141913922096325,
1.85272361624831));
#20026=CARTESIAN_POINT('Origin',(0.,0.,-0.129405622560373));
#20027=CARTESIAN_POINT('',(-0.0636886188644129,0.141913925768909,1.93667989110148));
#20028=CARTESIAN_POINT('',(-0.0637929161402304,0.142146585575849,1.92279372449516));
#20029=CARTESIAN_POINT('',(-0.0636886258329924,0.141913922641526,-0.129405622560373));
#20030=CARTESIAN_POINT('Ctrl Pts',(-0.0636886188644129,0.141913925768909,
1.93667989110148));
#20031=CARTESIAN_POINT('Ctrl Pts',(-0.0623139118484019,0.142530871503576,
1.93656459384097));
#20032=CARTESIAN_POINT('Ctrl Pts',(-0.0609299693695357,0.143127963941791,
1.93644886047932));
#20033=CARTESIAN_POINT('Ctrl Pts',(-0.0517943039187702,0.14691288511572,
1.93568741913531));
#20034=CARTESIAN_POINT('Ctrl Pts',(-0.0438049553579604,0.14948969874181,
1.93503240351246));
#20035=CARTESIAN_POINT('Ctrl Pts',(-0.0312589033511584,0.152443451415049,
1.93404478225449));
#20036=CARTESIAN_POINT('Ctrl Pts',(-0.026827496764667,0.153285417555423,
1.93370371892127));
#20037=CARTESIAN_POINT('Ctrl Pts',(-0.0214448949121712,0.154067465911734,
1.93330327514698));
#20038=CARTESIAN_POINT('Ctrl Pts',(-0.0205232561249677,0.154192942906666,
1.93323519557578));
#20039=CARTESIAN_POINT('Ctrl Pts',(-0.0192288309749084,0.154357361143084,
1.93314031154491));
#20040=CARTESIAN_POINT('Ctrl Pts',(-0.0188569699294528,0.154403230447954,
1.93311313799678));
#20041=CARTESIAN_POINT('Ctrl Pts',(-0.0182220015482922,0.154479226070539,
1.93306688649942));
#20042=CARTESIAN_POINT('Ctrl Pts',(-0.0179589779841986,0.154510024729143,
1.93304777115586));
#20043=CARTESIAN_POINT('Ctrl Pts',(-0.0174537511212499,0.154567876556912,
1.93301113852488));
#20044=CARTESIAN_POINT('Ctrl Pts',(-0.0172115624190806,0.154595032303292,
1.93299361537522));
#20045=CARTESIAN_POINT('Ctrl Pts',(-0.0165682151779505,0.154665637940117,
1.93294716369307));
#20046=CARTESIAN_POINT('Ctrl Pts',(-0.0161669459236324,0.154708096694891,
1.93291829049311));
#20047=CARTESIAN_POINT('Ctrl Pts',(-0.0147343356668726,0.154854048087741,
1.93281554837794));
#20048=CARTESIAN_POINT('Ctrl Pts',(-0.0137021001236858,0.154948796261485,
1.93274214984823));
#20049=CARTESIAN_POINT('Ctrl Pts',(-0.000670994318541644,0.156013668215569,
1.93182261060386));
#20050=CARTESIAN_POINT('Ctrl Pts',(0.0114024185719397,0.155598210855758,
1.93104392642662));
#20051=CARTESIAN_POINT('Ctrl Pts',(0.0332150902691036,0.152292320637181,
1.92958910232593));
#20052=CARTESIAN_POINT('Ctrl Pts',(0.0429516234219893,0.149837594639623,
1.92892106207387));
#20053=CARTESIAN_POINT('Ctrl Pts',(0.0531768037239526,0.146180503189244,
1.92816119596865));
#20054=CARTESIAN_POINT('Ctrl Pts',(0.0539675716987259,0.145890414773736,
1.92810205404783));
#20055=CARTESIAN_POINT('Ctrl Pts',(0.0552742669836312,0.14539898411847,
1.92800367805756));
#20056=CARTESIAN_POINT('Ctrl Pts',(0.0557915519445576,0.145201280609501,
1.92796456429893));
#20057=CARTESIAN_POINT('Ctrl Pts',(0.0567947883230385,0.144811696626983,
1.92788837004811));
#20058=CARTESIAN_POINT('Ctrl Pts',(0.0572808510281883,0.144620121539214,
1.92785130014233));
#20059=CARTESIAN_POINT('Ctrl Pts',(0.0577670814972464,0.144425644526231,
1.9278140601499));
#20060=CARTESIAN_POINT('Ctrl Pts',(0.0577682289553095,0.144425185562954,
1.92781397226615));
#20061=CARTESIAN_POINT('Ctrl Pts',(0.0577705286696384,0.14442426568541,
1.92781379612939));
#20062=CARTESIAN_POINT('Ctrl Pts',(0.0577716809171636,0.144423804774507,
1.92781370787704));
#20063=CARTESIAN_POINT('Ctrl Pts',(0.0577739902531458,0.144422880984219,
1.9278135309998));
#20064=CARTESIAN_POINT('Ctrl Pts',(0.0577751473352169,0.144422418107254,
1.92781344237538));
#20065=CARTESIAN_POINT('Ctrl Pts',(0.0577774663928809,0.144421490363398,
1.92781326474995));
#20066=CARTESIAN_POINT('Ctrl Pts',(0.0577786283594959,0.144421025499963,
1.92781317574961));
#20067=CARTESIAN_POINT('Ctrl Pts',(0.0577809572255915,0.144420093767015,
1.92781299736929));
#20068=CARTESIAN_POINT('Ctrl Pts',(0.057782124121597,0.144419626898754,
1.92781290798957));
#20069=CARTESIAN_POINT('Ctrl Pts',(0.0577844628997235,0.144418691134434,
1.92781272884639));
#20070=CARTESIAN_POINT('Ctrl Pts',(0.0577856347748191,0.144418222241045,
1.92781263908345));
#20071=CARTESIAN_POINT('Ctrl Pts',(0.0577879835587649,0.144417282406983,
1.92781245917018));
#20072=CARTESIAN_POINT('Ctrl Pts',(0.0577891604607995,0.144416811468895,
1.92781236902035));
#20073=CARTESIAN_POINT('Ctrl Pts',(0.0577915193551739,0.144415867522377,
1.92781218832892));
#20074=CARTESIAN_POINT('Ctrl Pts',(0.0577927013373603,0.144415394517866,
1.92781209778809));
#20075=CARTESIAN_POINT('Ctrl Pts',(0.057795070432269,0.144414446421968,
1.92781191631155));
#20076=CARTESIAN_POINT('Ctrl Pts',(0.0577962575422328,0.144413971331538,
1.92781182537605));
#20077=CARTESIAN_POINT('Ctrl Pts',(0.0577986369423441,0.144413019043491,
1.92781164310634));
#20078=CARTESIAN_POINT('Ctrl Pts',(0.0577998292292903,0.144412541847007,
1.92781155177237));
#20079=CARTESIAN_POINT('Ctrl Pts',(0.0578022190430724,0.144411585322508,
1.92781136870113));
#20080=CARTESIAN_POINT('Ctrl Pts',(0.0578034165613076,0.144411105997784,
1.92781127696451));
#20081=CARTESIAN_POINT('Ctrl Pts',(0.0578058168844282,0.144410145197635,
1.92781109308437));
#20082=CARTESIAN_POINT('Ctrl Pts',(0.0578070196837962,0.144409663724265,
1.92781100094125));
#20083=CARTESIAN_POINT('Ctrl Pts',(0.0578094306291128,0.144408698602372,
1.9278108162435));
#20084=CARTESIAN_POINT('Ctrl Pts',(0.0578106387657814,0.144408214957409,
1.92781072368956));
#20085=CARTESIAN_POINT('Ctrl Pts',(0.0578130604282165,0.144407245474843,
1.92781053816687));
#20086=CARTESIAN_POINT('Ctrl Pts',(0.057814273951153,0.144406759638215,
1.92781044519834));
#20087=CARTESIAN_POINT('Ctrl Pts',(0.0578167064520139,0.144405785745466,
1.92781025884137));
#20088=CARTESIAN_POINT('Ctrl Pts',(0.0578179254201832,0.144405297693089,
1.92781016545369));
#20089=CARTESIAN_POINT('Ctrl Pts',(0.0578203688550495,0.14440431935093,
1.92780997825508));
#20090=CARTESIAN_POINT('Ctrl Pts',(0.057821593319676,0.144403829061813,
1.9278098844443));
#20091=CARTESIAN_POINT('Ctrl Pts',(0.0578240478057935,0.144402846222325,
1.927809696395));
#20092=CARTESIAN_POINT('Ctrl Pts',(0.0578252778222605,0.144402353673801,
1.92780960215685));
#20093=CARTESIAN_POINT('Ctrl Pts',(0.0578277434745848,0.144401366289966,
1.927809413248));
#20094=CARTESIAN_POINT('Ctrl Pts',(0.0578289791022361,0.144400871457773,
1.92780931857791));
#20095=CARTESIAN_POINT('Ctrl Pts',(0.0578314560243601,0.144399879487104,
1.92780912880152));
#20096=CARTESIAN_POINT('Ctrl Pts',(0.0578326973169664,0.144399382349204,
1.92780903369534));
#20097=CARTESIAN_POINT('Ctrl Pts',(0.0578351856314596,0.144398385741596,
1.92780884304196));
#20098=CARTESIAN_POINT('Ctrl Pts',(0.0578364326485176,0.144397886273649,
1.9278087474951));
#20099=CARTESIAN_POINT('Ctrl Pts',(0.057838932463049,0.144396884984946,
1.92780855595642));
#20100=CARTESIAN_POINT('Ctrl Pts',(0.0578401852584092,0.144396383164863,
1.92780845996474));
#20101=CARTESIAN_POINT('Ctrl Pts',(0.0578426966671834,0.144395377156286,
1.92780826753348));
#20102=CARTESIAN_POINT('Ctrl Pts',(0.057843955267745,0.144394872972768,
1.92780817109488));
#20103=CARTESIAN_POINT('Ctrl Pts',(0.058263349400423,0.144226861272854,
1.92777603522118));
#20104=CARTESIAN_POINT('Ctrl Pts',(0.0586807511613323,0.144057540001483,
1.92774393501312));
#20105=CARTESIAN_POINT('Ctrl Pts',(0.0596249573297357,0.143669733141378,
1.92767105218755));
#20106=CARTESIAN_POINT('Ctrl Pts',(0.0601513048402488,0.143450159524081,
1.92763023315416));
#20107=CARTESIAN_POINT('Ctrl Pts',(0.0616491619313125,0.142815613159336,
1.9275135199763));
#20108=CARTESIAN_POINT('Ctrl Pts',(0.0626176511231864,0.142393638180758,
1.9274373892381));
#20109=CARTESIAN_POINT('Ctrl Pts',(0.0689594296508403,0.139553287951784,
1.92693438521286));
#20110=CARTESIAN_POINT('Ctrl Pts',(0.0741951774994299,0.136841448071204,
1.9264974890208));
#20111=CARTESIAN_POINT('Ctrl Pts',(0.0886274701633403,0.12829419562457,
1.92522888995344));
#20112=CARTESIAN_POINT('Ctrl Pts',(0.0973826318216243,0.121781805653149,
1.92437757624002));
#20113=CARTESIAN_POINT('Ctrl Pts',(0.108462282707068,0.111576142891768,
1.9232170303326));
#20114=CARTESIAN_POINT('Ctrl Pts',(0.111423856662008,0.108618747148631,
1.92289749086033));
#20115=CARTESIAN_POINT('Ctrl Pts',(0.115705287199864,0.103983693219156,
1.92242520471983));
#20116=CARTESIAN_POINT('Ctrl Pts',(0.117115706861975,0.102392550395139,
1.92226778376168));
#20117=CARTESIAN_POINT('Ctrl Pts',(0.118821857108639,0.100386384550469,
1.92207554879086));
#20118=CARTESIAN_POINT('Ctrl Pts',(0.11914867290999,0.0999982684501449,
1.92203864094211));
#20119=CARTESIAN_POINT('Ctrl Pts',(0.119661612000995,0.099383033384467,
1.92198058835522));
#20120=CARTESIAN_POINT('Ctrl Pts',(0.119848997320651,0.0991569793636126,
1.92195935398295));
#20121=CARTESIAN_POINT('Ctrl Pts',(0.120200351758247,0.0987306686046086,
1.92191949035984));
#20122=CARTESIAN_POINT('Ctrl Pts',(0.120364459124811,0.0985305357081057,
1.92190085145918));
#20123=CARTESIAN_POINT('Ctrl Pts',(0.120737300986166,0.0980735244724467,
1.92185845837926));
#20124=CARTESIAN_POINT('Ctrl Pts',(0.120945715434853,0.097816389093736,
1.92183472733057));
#20125=CARTESIAN_POINT('Ctrl Pts',(0.121594618114691,0.097010548112544,
1.92176072704574));
#20126=CARTESIAN_POINT('Ctrl Pts',(0.122032213544002,0.0964595070853536,
1.92171065978423));
#20127=CARTESIAN_POINT('Ctrl Pts',(0.12721840456848,0.0898370255894188,
1.92111504142826));
#20128=CARTESIAN_POINT('Ctrl Pts',(0.131513918716525,0.0834226674214282,
1.92059877771323));
#20129=CARTESIAN_POINT('Ctrl Pts',(0.136027103254726,0.0754619459107344,
1.91999332196306));
#20130=CARTESIAN_POINT('Ctrl Pts',(0.136720195103678,0.0741988303345223,
1.91989825731979));
#20131=CARTESIAN_POINT('Ctrl Pts',(0.141835793118025,0.0645608630874822,
1.91917917413033));
#20132=CARTESIAN_POINT('Ctrl Pts',(0.145502367260375,0.055808084062282,
1.91856029763987));
#20133=CARTESIAN_POINT('Ctrl Pts',(0.14966388251135,0.0426099853983275,
1.91762092243679));
#20134=CARTESIAN_POINT('Ctrl Pts',(0.150801413108891,0.0383903154641012,
1.91731996413983));
#20135=CARTESIAN_POINT('Ctrl Pts',(0.151966538816563,0.0332093583025964,
1.91694702433368));
#20136=CARTESIAN_POINT('Ctrl Pts',(0.152164920032293,0.0322881935172756,
1.91688059033774));
#20137=CARTESIAN_POINT('Ctrl Pts',(0.152462665451181,0.030841914450291,
1.91677606324851));
#20138=CARTESIAN_POINT('Ctrl Pts',(0.152567716070872,0.0303179821788781,
1.91673815157947));
#20139=CARTESIAN_POINT('Ctrl Pts',(0.152749314471582,0.0293874229549187,
1.91667073125739));
#20140=CARTESIAN_POINT('Ctrl Pts',(0.152826943796132,0.0289810100468157,
1.91664125732049));
#20141=CARTESIAN_POINT('Ctrl Pts',(0.153002218912614,0.0280431012866468,
1.91657316934394));
#20142=CARTESIAN_POINT('Ctrl Pts',(0.153098717875223,0.0275113993338287,
1.9165345192866));
#20143=CARTESIAN_POINT('Ctrl Pts',(0.153356150227412,0.026049655686807,
1.91642811753844));
#20144=CARTESIAN_POINT('Ctrl Pts',(0.153511389780534,0.0251186486230227,
1.91636018665901));
#20145=CARTESIAN_POINT('Ctrl Pts',(0.15426419225691,0.0203360152192596,
1.91601033961286));
#20146=CARTESIAN_POINT('Ctrl Pts',(0.154725255158399,0.0164646564458348,
1.91572417036638));
#20147=CARTESIAN_POINT('Ctrl Pts',(0.155203329134184,0.0105728759093058,
1.91528367340942));
#20148=CARTESIAN_POINT('Ctrl Pts',(0.1553272104684,0.00856248482435424,
1.91513250411983));
#20149=CARTESIAN_POINT('Ctrl Pts',(0.156028991951178,-0.00808786285475393,
1.91387357579896));
#20150=CARTESIAN_POINT('Ctrl Pts',(0.154574863219057,-0.022737484364409,
1.91271208571841));
#20151=CARTESIAN_POINT('Ctrl Pts',(0.150457012439278,-0.0395685038675411,
1.91140745841941));
#20152=CARTESIAN_POINT('Ctrl Pts',(0.149753199934081,-0.0421540099016685,
1.91120821240737));
#20153=CARTESIAN_POINT('Ctrl Pts',(0.14882635930982,-0.0452417254090879,
1.9109726790923));
#20154=CARTESIAN_POINT('Ctrl Pts',(0.148667086556234,-0.0457623900394041,
1.91093304609735));
#20155=CARTESIAN_POINT('Ctrl Pts',(0.148415293903251,-0.0465703134641446,
1.91087168863046));
#20156=CARTESIAN_POINT('Ctrl Pts',(0.148324668573028,-0.0468581503846347,
1.91084985699857));
#20157=CARTESIAN_POINT('Ctrl Pts',(0.148155097894984,-0.0473913059371092,
1.91080947299888));
#20158=CARTESIAN_POINT('Ctrl Pts',(0.148076381296406,-0.0476366897966697,
1.91079090801075));
#20159=CARTESIAN_POINT('Ctrl Pts',(0.147897175919077,-0.0481905917348518,
1.91074904956525));
#20160=CARTESIAN_POINT('Ctrl Pts',(0.147796331645468,-0.0484989910611065,
1.91072577725864));
#20161=CARTESIAN_POINT('Ctrl Pts',(0.147496274558364,-0.0494069902958142,
1.91065735060439));
#20162=CARTESIAN_POINT('Ctrl Pts',(0.147294369399312,-0.0500057044594937,
1.91061235063989));
#20163=CARTESIAN_POINT('Ctrl Pts',(0.145824664325777,-0.0542777118261522,
1.91029200147478));
#20164=CARTESIAN_POINT('Ctrl Pts',(0.144423123413583,-0.057903977461674,
1.91002398578684));
#20165=CARTESIAN_POINT('Ctrl Pts',(0.137997202822195,-0.0728399901529379,
1.90892136321839));
#20166=CARTESIAN_POINT('Ctrl Pts',(0.13176851512132,-0.0835822783268564,
1.90812824162826));
#20167=CARTESIAN_POINT('Ctrl Pts',(0.121675761418994,-0.097006975209353,
1.90700538139795));
#20168=CARTESIAN_POINT('Ctrl Pts',(0.118870109722951,-0.10042527567558,
1.90670642910167));
#20169=CARTESIAN_POINT('Ctrl Pts',(0.114138129585178,-0.105714021259405,
1.90621771070855));
#20170=CARTESIAN_POINT('Ctrl Pts',(0.11230228023296,-0.107662264840207,
1.90603149136525));
#20171=CARTESIAN_POINT('Ctrl Pts',(0.109851135057086,-0.110132540395431,
1.90578655647061));
#20172=CARTESIAN_POINT('Ctrl Pts',(0.10928069072764,-0.110698594922814,
1.90572980445913));
#20173=CARTESIAN_POINT('Ctrl Pts',(0.108345587247929,-0.111612230401133,
1.90563716229442));
#20174=CARTESIAN_POINT('Ctrl Pts',(0.107983575257947,-0.111962510309686,
1.9056013904273));
#20175=CARTESIAN_POINT('Ctrl Pts',(0.107283980489765,-0.112632883512432,
1.90553243498937));
#20176=CARTESIAN_POINT('Ctrl Pts',(0.106946650103483,-0.112953233424516,
1.90549926302742));
#20177=CARTESIAN_POINT('Ctrl Pts',(0.106170817040806,-0.11368342165538,
1.90542314207001));
#20178=CARTESIAN_POINT('Ctrl Pts',(0.105731371493073,-0.114092242566667,
1.9053801502359));
#20179=CARTESIAN_POINT('Ctrl Pts',(0.104557360878036,-0.115171829421012,
1.90526561526976));
#20180=CARTESIAN_POINT('Ctrl Pts',(0.103818719463163,-0.115838099990894,
1.90519388408949));
#20181=CARTESIAN_POINT('Ctrl Pts',(0.0982094045153399,-0.120801077818922,
1.90465152504069));
#20182=CARTESIAN_POINT('Ctrl Pts',(0.0930810058893311,-0.1247953988602,
1.90416858222044));
#20183=CARTESIAN_POINT('Ctrl Pts',(0.0790913646547553,-0.134348414460681,
1.90288243823438));
#20184=CARTESIAN_POINT('Ctrl Pts',(0.0698928320481996,-0.139355299402337,
1.90206491437551));
#20185=CARTESIAN_POINT('Ctrl Pts',(0.0565477471750089,-0.144963435782579,
1.90095065518525));
#20186=CARTESIAN_POINT('Ctrl Pts',(0.0527726565901035,-0.14637997583789,
1.90064314923597));
#20187=CARTESIAN_POINT('Ctrl Pts',(0.0469777448818165,-0.148301031846785,
1.90018646657215));
#20188=CARTESIAN_POINT('Ctrl Pts',(0.044995974897906,-0.148914297332099,
1.90003294433012));
#20189=CARTESIAN_POINT('Ctrl Pts',(0.0425186630961812,-0.149626933262349,
1.89984480049977));
#20190=CARTESIAN_POINT('Ctrl Pts',(0.0420342409723471,-0.149763742186795,
1.89980818772617));
#20191=CARTESIAN_POINT('Ctrl Pts',(0.041267062793292,-0.149976390534752,
1.89975049369711));
#20192=CARTESIAN_POINT('Ctrl Pts',(0.0409847479424406,-0.150053785788246,
1.89972932462665));
#20193=CARTESIAN_POINT('Ctrl Pts',(0.0404522447870206,-0.150198154011838,
1.89968951406292));
#20194=CARTESIAN_POINT('Ctrl Pts',(0.0402021108516058,-0.150265298260502,
1.89967086325216));
#20195=CARTESIAN_POINT('Ctrl Pts',(0.0396305107052771,-0.15041720527188,
1.89962835431003));
#20196=CARTESIAN_POINT('Ctrl Pts',(0.0393089398654413,-0.150501562360012,
1.89960451977919));
#20197=CARTESIAN_POINT('Ctrl Pts',(0.0384559687603771,-0.15072240037002,
1.89954150448339));
#20198=CARTESIAN_POINT('Ctrl Pts',(0.0379241061700692,-0.150857103583914,
1.89950242348854));
#20199=CARTESIAN_POINT('Ctrl Pts',(0.0342445308266668,-0.151768328666505,
1.89923343862731));
#20200=CARTESIAN_POINT('Ctrl Pts',(0.0310736355660963,-0.152449160651027,
1.89900864384737));
#20201=CARTESIAN_POINT('Ctrl Pts',(0.027113845374644,-0.153170669212571,
1.89873391068488));
#20202=CARTESIAN_POINT('Ctrl Pts',(0.0263431413328027,-0.153305099275667,
1.89868071803145));
#20203=CARTESIAN_POINT('Ctrl Pts',(0.0133147919287953,-0.155476419337986,
1.89778573908806));
#20204=CARTESIAN_POINT('Ctrl Pts',(0.000856941605050558,-0.156043300709219,
1.89698938853222));
#20205=CARTESIAN_POINT('Ctrl Pts',(-0.0158528065020981,-0.154800599955869,
1.89586831877824));
#20206=CARTESIAN_POINT('Ctrl Pts',(-0.0201536477079932,-0.154299587793208,
1.89557538589128));
#20207=CARTESIAN_POINT('Ctrl Pts',(-0.0270315373814551,-0.153205906079514,
1.89509559942364));
#20208=CARTESIAN_POINT('Ctrl Pts',(-0.029624239166737,-0.152725756468644,
1.89491212630646));
#20209=CARTESIAN_POINT('Ctrl Pts',(-0.0329853476588799,-0.152014500059913,
1.89467030267045));
#20210=CARTESIAN_POINT('Ctrl Pts',(-0.0337660351773859,-0.151842998568413,
1.89461385319813));
#20211=CARTESIAN_POINT('Ctrl Pts',(-0.0350355787411722,-0.151553830407656,
1.8945215820698));
#20212=CARTESIAN_POINT('Ctrl Pts',(-0.0355252545715611,-0.151439795185312,
1.89448587690474));
#20213=CARTESIAN_POINT('Ctrl Pts',(-0.0364672412318426,-0.151215606113075,
1.89441696476968));
#20214=CARTESIAN_POINT('Ctrl Pts',(-0.0369196280042995,-0.151105791664543,
1.89438376902945));
#20215=CARTESIAN_POINT('Ctrl Pts',(-0.0379561795988101,-0.150849241656922,
1.89430747264136));
#20216=CARTESIAN_POINT('Ctrl Pts',(-0.0385399955190969,-0.150701141351702,
1.89426432848549));
#20217=CARTESIAN_POINT('Ctrl Pts',(-0.0400926221504664,-0.150297664497885,
1.89414912260764));
#20218=CARTESIAN_POINT('Ctrl Pts',(-0.0410598363381574,-0.150036315793711,
1.89407686932073));
#20219=CARTESIAN_POINT('Ctrl Pts',(-0.0485572933935458,-0.147932519482521,
1.89351291813367));
#20220=CARTESIAN_POINT('Ctrl Pts',(-0.0549621882698234,-0.145674203725999,
1.89300773951047));
#20221=CARTESIAN_POINT('Ctrl Pts',(-0.0741008978795629,-0.137483890272898,
1.89142450855353));
#20222=CARTESIAN_POINT('Ctrl Pts',(-0.0861955022067965,-0.130242314560421,
1.8903125268345));
#20223=CARTESIAN_POINT('Ctrl Pts',(-0.098879039056098,-0.120098351628254,
1.88909576901242));
#20224=CARTESIAN_POINT('Ctrl Pts',(-0.100574065326758,-0.118682505787086,
1.88893214655533));
#20225=CARTESIAN_POINT('Ctrl Pts',(-0.102625517080303,-0.116893410734303,
1.88873342515567));
#20226=CARTESIAN_POINT('Ctrl Pts',(-0.10301088647724,-0.116553951097115,
1.88869606410842));
#20227=CARTESIAN_POINT('Ctrl Pts',(-0.103614958337856,-0.11601650711492,
1.88863746106276));
#20228=CARTESIAN_POINT('Ctrl Pts',(-0.10383478609371,-0.115819802777138,
1.88861612660645));
#20229=CARTESIAN_POINT('Ctrl Pts',(-0.104246254115159,-0.115449503513024,
1.88857618003708));
#20230=CARTESIAN_POINT('Ctrl Pts',(-0.104438018790505,-0.115276058186642,
1.88855755776809));
#20231=CARTESIAN_POINT('Ctrl Pts',(-0.104876734918884,-0.114877259443074,
1.88851494078897));
#20232=CARTESIAN_POINT('Ctrl Pts',(-0.1051233927569,-0.114651587714078,
1.8884909704763));
#20233=CARTESIAN_POINT('Ctrl Pts',(-0.105886020358606,-0.113949315736671,
1.88841681986465));
#20234=CARTESIAN_POINT('Ctrl Pts',(-0.10639950078149,-0.113470005496947,
1.88836683949049));
#20235=CARTESIAN_POINT('Ctrl Pts',(-0.111817851503183,-0.108343103499832,
1.88783862257071));
#20236=CARTESIAN_POINT('Ctrl Pts',(-0.116418926679245,-0.103383370112628,
1.88738282152953));
#20237=CARTESIAN_POINT('Ctrl Pts',(-0.126869503787302,-0.0905321453915931,
1.88628241338247));
#20238=CARTESIAN_POINT('Ctrl Pts',(-0.132322440281414,-0.0823572333029784,
1.88564671212012));
#20239=CARTESIAN_POINT('Ctrl Pts',(-0.138939060386207,-0.070064310026673,
1.88471129199374));
#20240=CARTESIAN_POINT('Ctrl Pts',(-0.140760978814372,-0.0663280668418696,
1.88442966549942));
#20241=CARTESIAN_POINT('Ctrl Pts',(-0.143460109140074,-0.0601793491092366,
1.88396671232258));
#20242=CARTESIAN_POINT('Ctrl Pts',(-0.144431086864539,-0.0578101790553955,
1.88378846569088));
#20243=CARTESIAN_POINT('Ctrl Pts',(-0.145624889027769,-0.0546792438807589,
1.88355257238348));
#20244=CARTESIAN_POINT('Ctrl Pts',(-0.145901018598313,-0.0539381196022179,
1.88349671071365));
#20245=CARTESIAN_POINT('Ctrl Pts',(-0.146342786573112,-0.0527242092940469,
1.88340516020472));
#20246=CARTESIAN_POINT('Ctrl Pts',(-0.146511816642267,-0.0522526650147942,
1.88336958439859));
#20247=CARTESIAN_POINT('Ctrl Pts',(-0.146833750503467,-0.0513407201127665,
1.88330075341295));
#20248=CARTESIAN_POINT('Ctrl Pts',(-0.146986958146747,-0.0509004317730084,
1.88326750871833));
#20249=CARTESIAN_POINT('Ctrl Pts',(-0.147334938952497,-0.049885730911101,
1.88319085862735));
#20250=CARTESIAN_POINT('Ctrl Pts',(-0.147528335133311,-0.049310857812194,
1.88314740837475));
#20251=CARTESIAN_POINT('Ctrl Pts',(-0.148036789552355,-0.0477697016574671,
1.88303085030205));
#20252=CARTESIAN_POINT('Ctrl Pts',(-0.148345743055192,-0.0468014517256314,
1.88295754373332));
#20253=CARTESIAN_POINT('Ctrl Pts',(-0.150816816489712,-0.0387868099640734,
1.88235001412697));
#20254=CARTESIAN_POINT('Ctrl Pts',(-0.15248473235312,-0.0315990997914103,
1.8817997888244));
#20255=CARTESIAN_POINT('Ctrl Pts',(-0.154916651951674,-0.0162367237744365,
1.88061301846293));
#20256=CARTESIAN_POINT('Ctrl Pts',(-0.155556275934555,-0.00806412838761236,
1.87997532808238));
#20257=CARTESIAN_POINT('Ctrl Pts',(-0.155544457945757,0.00723429139734965,
1.87879230499606));
#20258=CARTESIAN_POINT('Ctrl Pts',(-0.155050913173091,0.0143407065639603,
1.87824740076));
#20259=CARTESIAN_POINT('Ctrl Pts',(-0.153975580461275,0.0220866218302719,
1.87767406755209));
#20260=CARTESIAN_POINT('Ctrl Pts',(-0.153874026671416,0.0227833757103862,
1.87762268415822));
#20261=CARTESIAN_POINT('Ctrl Pts',(-0.153717768952236,0.0238067137171998,
1.87754751690442));
#20262=CARTESIAN_POINT('Ctrl Pts',(-0.153666749808939,0.0241338376219465,
1.87752353393448));
#20263=CARTESIAN_POINT('Ctrl Pts',(-0.153573985083642,0.0247164033597027,
1.87748090698197));
#20264=CARTESIAN_POINT('Ctrl Pts',(-0.153532646024826,0.024971906177771,
1.87746224040361));
#20265=CARTESIAN_POINT('Ctrl Pts',(-0.153443057870261,0.025516987892864,
1.87742248000592));
#20266=CARTESIAN_POINT('Ctrl Pts',(-0.153394626806776,0.0258065330954148,
1.87740139664903));
#20267=CARTESIAN_POINT('Ctrl Pts',(-0.153260296488616,0.0265958869554173,
1.87734401669949));
#20268=CARTESIAN_POINT('Ctrl Pts',(-0.153172771200874,0.0270954214691064,
1.87730781076817));
#20269=CARTESIAN_POINT('Ctrl Pts',(-0.152706232573947,0.0296835809709499,
1.8771207322495));
#20270=CARTESIAN_POINT('Ctrl Pts',(-0.152286913802738,0.0317648475622439,
1.87697201588019));
#20271=CARTESIAN_POINT('Ctrl Pts',(-0.150917164327716,0.0379108489640523,
1.87653620315642));
#20272=CARTESIAN_POINT('Ctrl Pts',(-0.149845556839695,0.0419468470795809,
1.87625437320726));
#20273=CARTESIAN_POINT('Ctrl Pts',(-0.145434218170894,0.0562187314632048,
1.87525772836485));
#20274=CARTESIAN_POINT('Ctrl Pts',(-0.141196900559897,0.0661445512695426,
1.87456249020457));
#20275=CARTESIAN_POINT('Ctrl Pts',(-0.134996332502071,0.0773032969624332,
1.87370628778152));
#20276=CARTESIAN_POINT('Ctrl Pts',(-0.133990388490475,0.0790340739154274,
1.87357126928923));
#20277=CARTESIAN_POINT('Ctrl Pts',(-0.130775697066839,0.0843272569238734,
1.87315055681715));
#20278=CARTESIAN_POINT('Ctrl Pts',(-0.128456330161063,0.0878199013314235,
1.87286173320249));
#20279=CARTESIAN_POINT('Ctrl Pts',(-0.12548286323063,0.0919272979402839,
1.87250580958281));
#20280=CARTESIAN_POINT('Ctrl Pts',(-0.12496074350913,0.0926357900390331,
1.87244380866279));
#20281=CARTESIAN_POINT('Ctrl Pts',(-0.124089448417226,0.0937973262303442,
1.872341131904));
#20282=CARTESIAN_POINT('Ctrl Pts',(-0.123743731231153,0.0942529499888229,
1.87230059078509));
#20283=CARTESIAN_POINT('Ctrl Pts',(-0.123114986575457,0.0950721561212634,
1.87222721170615));
#20284=CARTESIAN_POINT('Ctrl Pts',(-0.122832840070679,0.0954364090943262,
1.87219440868164));
#20285=CARTESIAN_POINT('Ctrl Pts',(-0.122225581883589,0.0962132295523254,
1.87212407114285));
#20286=CARTESIAN_POINT('Ctrl Pts',(-0.12189999123172,0.096625413493972,
1.8720865178758));
#20287=CARTESIAN_POINT('Ctrl Pts',(-0.121010337686681,0.0977400237365894,
1.87198433011952));
#20288=CARTESIAN_POINT('Ctrl Pts',(-0.120442257845122,0.0984392021951439,
1.87191953534296));
#20289=CARTESIAN_POINT('Ctrl Pts',(-0.117469973491451,0.10203316996237,
1.87158280784333));
#20290=CARTESIAN_POINT('Ctrl Pts',(-0.114967576059303,0.10484471544802,
1.8713069023548));
#20291=CARTESIAN_POINT('Ctrl Pts',(-0.102060968398646,0.118327683623285,
1.86991837965263));
#20292=CARTESIAN_POINT('Ctrl Pts',(-0.0902630936237239,0.127555096863481,
1.86874389162985));
#20293=CARTESIAN_POINT('Ctrl Pts',(-0.0734494952110326,0.137189854357054,
1.86726265251107));
#20294=CARTESIAN_POINT('Ctrl Pts',(-0.0694663952417378,0.139249106793601,
1.86692486348299));
#20295=CARTESIAN_POINT('Ctrl Pts',(-0.0648307877395254,0.141397186401546,
1.86655061419595));
#20296=CARTESIAN_POINT('Ctrl Pts',(-0.0642604913790529,0.141657278824543,
1.86650489022365));
#20297=CARTESIAN_POINT('Ctrl Pts',(-0.0636886258329876,0.141913922641528,
1.86645936880636));
#20298=CARTESIAN_POINT('',(-0.155675768969518,-0.000119712528699489,1.86559437743963));
#20299=CARTESIAN_POINT('Ctrl Pts',(-0.0636886270478345,0.141913922096325,
1.85272361624831));
#20300=CARTESIAN_POINT('Ctrl Pts',(-0.0739703217922353,0.137299667114694,
1.85358706958847));
#20301=CARTESIAN_POINT('Ctrl Pts',(-0.0837207957971725,0.131581474202708,
1.8544734650818));
#20302=CARTESIAN_POINT('Ctrl Pts',(-0.0954374813874821,0.12287613518474,
1.85557961065035));
#20303=CARTESIAN_POINT('Ctrl Pts',(-0.0980423574854303,0.120807937720802,
1.85582824336486));
#20304=CARTESIAN_POINT('Ctrl Pts',(-0.101000676165513,0.118300343388413,
1.85611202326769));
#20305=CARTESIAN_POINT('Ctrl Pts',(-0.10142029150064,0.117940800100071,
1.85615230925228));
#20306=CARTESIAN_POINT('Ctrl Pts',(-0.102090117918159,0.117360647488134,
1.85621665968603));
#20307=CARTESIAN_POINT('Ctrl Pts',(-0.102341545652814,0.117141460612512,
1.85624082411406));
#20308=CARTESIAN_POINT('Ctrl Pts',(-0.102786992214986,0.11675060531303,
1.85628364972048));
#20309=CARTESIAN_POINT('Ctrl Pts',(-0.102981289211346,0.116579259244726,
1.85630233432925));
#20310=CARTESIAN_POINT('Ctrl Pts',(-0.1033562579006,0.116246913990354,1.85633840169611));
#20311=CARTESIAN_POINT('Ctrl Pts',(-0.103536980980482,0.116085979476988,
1.85635578908285));
#20312=CARTESIAN_POINT('Ctrl Pts',(-0.104043187633436,0.115633078263097,
1.85640450518398));
#20313=CARTESIAN_POINT('Ctrl Pts',(-0.104367820397992,0.11534015675098,
1.8564357632608));
#20314=CARTESIAN_POINT('Ctrl Pts',(-0.105712739453047,0.114116286474028,
1.85656535170528));
#20315=CARTESIAN_POINT('Ctrl Pts',(-0.106721881152471,0.113173099976523,
1.85666280233229));
#20316=CARTESIAN_POINT('Ctrl Pts',(-0.109358462369601,0.110642205671764,
1.85691842795796));
#20317=CARTESIAN_POINT('Ctrl Pts',(-0.110963941663144,0.109031994706482,
1.85707513982447));
#20318=CARTESIAN_POINT('Ctrl Pts',(-0.116693554900108,0.103027787559818,
1.85764101744125));
#20319=CARTESIAN_POINT('Ctrl Pts',(-0.120597001966021,0.0984301048361011,
1.85803966682445));
#20320=CARTESIAN_POINT('Ctrl Pts',(-0.131779987069992,0.0835909908354916,
1.85926402258546));
#20321=CARTESIAN_POINT('Ctrl Pts',(-0.138093314372199,0.0726884210134969,
1.86008394891692));
#20322=CARTESIAN_POINT('Ctrl Pts',(-0.143697582786388,0.0595794521520465,
1.86107518217491));
#20323=CARTESIAN_POINT('Ctrl Pts',(-0.144341638058565,0.0580017029021563,
1.86119447459827));
#20324=CARTESIAN_POINT('Ctrl Pts',(-0.145212492752673,0.0557639722027207,
1.86136380472771));
#20325=CARTESIAN_POINT('Ctrl Pts',(-0.145460988165458,0.0551125170960898,
1.86141311654423));
#20326=CARTESIAN_POINT('Ctrl Pts',(-0.145856582605158,0.0540541121188796,
1.86149326803461));
#20327=CARTESIAN_POINT('Ctrl Pts',(-0.14600638017302,0.0536481748811687,
1.86152401751783));
#20328=CARTESIAN_POINT('Ctrl Pts',(-0.14631557021811,0.0527994120318984,
1.86158833113908));
#20329=CARTESIAN_POINT('Ctrl Pts',(-0.146474650321893,0.0523564781406016,
1.86162190526874));
#20330=CARTESIAN_POINT('Ctrl Pts',(-0.146846838923133,0.0513052033476025,
1.86170162234134));
#20331=CARTESIAN_POINT('Ctrl Pts',(-0.147058179511942,0.0506962504305998,
1.86174782317378));
#20332=CARTESIAN_POINT('Ctrl Pts',(-0.14775068431541,0.0486601085436864,
1.8619023978486));
#20333=CARTESIAN_POINT('Ctrl Pts',(-0.148214890967004,0.0472272874315404,
1.86201132564933));
#20334=CARTESIAN_POINT('Ctrl Pts',(-0.149265480596585,0.0438163767856777,
1.86227108473056));
#20335=CARTESIAN_POINT('Ctrl Pts',(-0.14983344478335,0.0418329612643452,
1.86242248946604));
#20336=CARTESIAN_POINT('Ctrl Pts',(-0.153816563203144,0.0267997043518521,
1.86357309985241));
#20337=CARTESIAN_POINT('Ctrl Pts',(-0.15555984041361,0.0133688473671373,
1.86462559282136));
#20338=CARTESIAN_POINT('Ctrl Pts',(-0.155549958218615,-0.000114009591826104,
1.86566652523707));
#20339=CARTESIAN_POINT('Ctrl Pts',(-0.155675768969518,-0.000119712528699489,
1.86559437743963));
#20340=CARTESIAN_POINT('Ctrl Pts',(-0.155742030728685,-0.00790775711175682,
1.86615350633922));
#20341=CARTESIAN_POINT('Ctrl Pts',(-0.151670179225866,-0.0672314883108279,
1.87041753953273));
#20342=CARTESIAN_POINT('Ctrl Pts',(-0.0754025780794165,-0.16768394396421,
1.87838647702017));
#20343=CARTESIAN_POINT('Ctrl Pts',(0.0999993571785868,-0.154284096420481,
1.88950118990195));
#20344=CARTESIAN_POINT('Ctrl Pts',(0.183856812913126,0.000355232096483363,
1.90061590278373));
#20345=CARTESIAN_POINT('Ctrl Pts',(0.0995331275448493,0.154430543530984,
1.9117134143148));
#20346=CARTESIAN_POINT('Ctrl Pts',(-0.0170231057640074,0.163110781870857,
1.91910602155194));
#20347=CARTESIAN_POINT('Ctrl Pts',(-0.0637929161402304,0.142146585575849,
1.92279372449516));
#20348=CARTESIAN_POINT('Origin',(0.,0.,-0.129405622560373));
#20349=CARTESIAN_POINT('',(-0.0636886213818939,0.141913924639106,2.00672033358865));
#20350=CARTESIAN_POINT('',(-0.0636886415377123,0.141913915593506,1.99275019838839));
#20351=CARTESIAN_POINT('',(-0.0636886258329924,0.141913922641526,-0.129405622560373));
#20352=CARTESIAN_POINT('',(-0.155549993634555,4.4500446807104E-5,1.94954854470546));
#20353=CARTESIAN_POINT('Ctrl Pts',(-0.0636886213818939,0.141913924639106,
2.00672033358865));
#20354=CARTESIAN_POINT('Ctrl Pts',(-0.0604714569255569,0.143357734818438,
2.00648001356466));
#20355=CARTESIAN_POINT('Ctrl Pts',(-0.0572055352928224,0.144691995296332,
2.00623663332487));
#20356=CARTESIAN_POINT('Ctrl Pts',(-0.0529634226839831,0.146258906037987,
2.00591977835086));
#20357=CARTESIAN_POINT('Ctrl Pts',(-0.0520271660241615,0.146594562150063,
2.00584980477329));
#20358=CARTESIAN_POINT('Ctrl Pts',(-0.050520897669163,0.147118325172964,
2.00573713147982));
#20359=CARTESIAN_POINT('Ctrl Pts',(-0.0499528928161396,0.147312155588118,
2.00569462082771));
#20360=CARTESIAN_POINT('Ctrl Pts',(-0.0489426529835277,0.147650383106395,
2.00561896627509));
#20361=CARTESIAN_POINT('Ctrl Pts',(-0.0485008624848558,0.147796093460381,
2.00558586601961));
#20362=CARTESIAN_POINT('Ctrl Pts',(-0.0475793198585017,0.148095457699797,
2.00551678554075));
#20363=CARTESIAN_POINT('Ctrl Pts',(-0.0470994623809972,0.14824876694907,
2.00548079445697));
#20364=CARTESIAN_POINT('Ctrl Pts',(-0.0458521025636008,0.148640617430633,
2.00538718085255));
#20365=CARTESIAN_POINT('Ctrl Pts',(-0.0450834895714874,0.148875543265897,
2.00532944102159));
#20366=CARTESIAN_POINT('Ctrl Pts',(-0.0417466256309887,0.149867242375032,
2.00507849826894));
#20367=CARTESIAN_POINT('Ctrl Pts',(-0.0391610406471848,0.150563549137276,
2.00488335147288));
#20368=CARTESIAN_POINT('Ctrl Pts',(-0.0322603539253661,0.152232158534698,
2.00436026948027));
#20369=CARTESIAN_POINT('Ctrl Pts',(-0.0279198218369057,0.153087678703914,
2.00402888924305));
#20370=CARTESIAN_POINT('Ctrl Pts',(-0.0113209751961112,0.155629921774353,
2.00275348700118));
#20371=CARTESIAN_POINT('Ctrl Pts',(0.00108548628479758,0.156037230747702,
2.00177921278012));
#20372=CARTESIAN_POINT('Ctrl Pts',(0.0172812209132271,0.154635934541401,
2.00054174380077));
#20373=CARTESIAN_POINT('Ctrl Pts',(0.0211404622240561,0.15415576580977,
2.00024990730944));
#20374=CARTESIAN_POINT('Ctrl Pts',(0.0256017097638221,0.153429965195873,
1.99991897493799));
#20375=CARTESIAN_POINT('Ctrl Pts',(0.0262247728270713,0.15332469823797,
1.99987290410674));
#20376=CARTESIAN_POINT('Ctrl Pts',(0.0271667963785254,0.153159632273694,
1.99980348938374));
#20377=CARTESIAN_POINT('Ctrl Pts',(0.0274862293766622,0.153102628924415,
1.99977999338458));
#20378=CARTESIAN_POINT('Ctrl Pts',(0.0280590364333624,0.152998560073275,
1.99973793857796));
#20379=CARTESIAN_POINT('Ctrl Pts',(0.0283124726969926,0.152951864334157,
1.99971935928006));
#20380=CARTESIAN_POINT('Ctrl Pts',(0.0288624201043101,0.152849122539985,
1.99967910328604));
#20381=CARTESIAN_POINT('Ctrl Pts',(0.029158883754855,0.152792843608296,
1.99965744002884));
#20382=CARTESIAN_POINT('Ctrl Pts',(0.0299897630777745,0.152632607959033,
1.99959682703767));
#20383=CARTESIAN_POINT('Ctrl Pts',(0.0305238067040571,0.15252670634936,
1.999557985876));
#20384=CARTESIAN_POINT('Ctrl Pts',(0.0336816342138033,0.151883254942315,
1.9993289524563));
#20385=CARTESIAN_POINT('Ctrl Pts',(0.0362919410380928,0.151280775250069,
1.99914223320763));
#20386=CARTESIAN_POINT('Ctrl Pts',(0.0530689033031117,0.146949208971719,
1.99795129631909));
#20387=CARTESIAN_POINT('Ctrl Pts',(0.0666651674916582,0.141301942789719,
1.99702238066316));
#20388=CARTESIAN_POINT('Ctrl Pts',(0.0810038995866349,0.132808974960902,
1.99590253524051));
#20389=CARTESIAN_POINT('Ctrl Pts',(0.0827159391236219,0.131749491483096,
1.99576645296893));
#20390=CARTESIAN_POINT('Ctrl Pts',(0.0876815728064243,0.128541601264236,
1.99536390160295));
#20391=CARTESIAN_POINT('Ctrl Pts',(0.0908753095805218,0.126303900129376,
1.99509479698976));
#20392=CARTESIAN_POINT('Ctrl Pts',(0.0947335850372766,0.123378447797612,
1.99475481818793));
#20393=CARTESIAN_POINT('Ctrl Pts',(0.0954805306749854,0.122801309874749,
1.99468828033741));
#20394=CARTESIAN_POINT('Ctrl Pts',(0.0966467673505241,0.121883128041626,
1.9945832276294));
#20395=CARTESIAN_POINT('Ctrl Pts',(0.0970696220021085,0.121546628959793,
1.99454489314459));
#20396=CARTESIAN_POINT('Ctrl Pts',(0.0978131222422792,0.120948612296067,
1.99447705198347));
#20397=CARTESIAN_POINT('Ctrl Pts',(0.0981344958270651,0.120688004465343,
1.99444758197771));
#20398=CARTESIAN_POINT('Ctrl Pts',(0.0988685113443571,0.120087907344095,
1.99437993431787));
#20399=CARTESIAN_POINT('Ctrl Pts',(0.0992804493847016,0.119747569422287,
1.99434172259801));
#20400=CARTESIAN_POINT('Ctrl Pts',(0.100413889967894,0.118801266651526,
1.99423589202157));
#20401=CARTESIAN_POINT('Ctrl Pts',(0.101131642354956,0.118190867238116,
1.99416809294457));
#20402=CARTESIAN_POINT('Ctrl Pts',(0.105145081894065,0.114714385140549,
1.99378448509582));
#20403=CARTESIAN_POINT('Ctrl Pts',(0.108324132669722,0.1117172933804,1.99346326255191));
#20404=CARTESIAN_POINT('Ctrl Pts',(0.117981278881326,0.101812746566546,
1.99242911224421));
#20405=CARTESIAN_POINT('Ctrl Pts',(0.123956568369346,0.0944464983789309,
1.99169751173491));
#20406=CARTESIAN_POINT('Ctrl Pts',(0.130396529658678,0.0848350179764151,
1.9908002854657));
#20407=CARTESIAN_POINT('Ctrl Pts',(0.131532842463569,0.083062306311319,
1.99063706535839));
#20408=CARTESIAN_POINT('Ctrl Pts',(0.136315302920027,0.0752570374541442,
1.98992931818662));
#20409=CARTESIAN_POINT('Ctrl Pts',(0.139585554413716,0.0690027834368368,
1.98938964386267));
#20410=CARTESIAN_POINT('Ctrl Pts',(0.142703606915621,0.0619029767534948,
1.98882114286199));
#20411=CARTESIAN_POINT('Ctrl Pts',(0.142982273183565,0.0612565715941229,
1.98876977436984));
#20412=CARTESIAN_POINT('Ctrl Pts',(0.143386922127637,0.0603001245453035,
1.98869436582078));
#20413=CARTESIAN_POINT('Ctrl Pts',(0.143516302372836,0.0599915445405849,
1.98867012801401));
#20414=CARTESIAN_POINT('Ctrl Pts',(0.14374390815649,0.0594437401300686,
1.98862726482745));
#20415=CARTESIAN_POINT('Ctrl Pts',(0.143842533692127,0.059204686281806,
1.98860861554447));
#20416=CARTESIAN_POINT('Ctrl Pts',(0.144052317873465,0.0586925815079835,
1.98856878426623));
#20417=CARTESIAN_POINT('Ctrl Pts',(0.144163296323181,0.0584194608496645,
1.98854761319517));
#20418=CARTESIAN_POINT('Ctrl Pts',(0.144465163676944,0.0576704593376156,
1.98848974694982));
#20419=CARTESIAN_POINT('Ctrl Pts',(0.144654479533428,0.0571939416999642,
1.98845314503952));
#20420=CARTESIAN_POINT('Ctrl Pts',(0.145642557620112,0.0546706075163413,
1.98826040235285));
#20421=CARTESIAN_POINT('Ctrl Pts',(0.146400294784007,0.0526078410272297,
1.98810657625707));
#20422=CARTESIAN_POINT('Ctrl Pts',(0.151662877575025,0.0372861153084749,
1.98698641468158));
#20423=CARTESIAN_POINT('Ctrl Pts',(0.154403138817001,0.0234875087747944,
1.98609524939235));
#20424=CARTESIAN_POINT('Ctrl Pts',(0.155676291218612,0.00269541956444296,
1.98470463298604));
#20425=CARTESIAN_POINT('Ctrl Pts',(0.155644636198529,-0.0041352483516464,
1.9842411822829));
#20426=CARTESIAN_POINT('Ctrl Pts',(0.155094191013136,-0.011941530850703,
1.98369293930793));
#20427=CARTESIAN_POINT('Ctrl Pts',(0.155013979377042,-0.0129411884848262,
1.98362239085475));
#20428=CARTESIAN_POINT('Ctrl Pts',(0.154870105744432,-0.0145401501702901,
1.98350896883183));
#20429=CARTESIAN_POINT('Ctrl Pts',(0.154812616410037,-0.0151399934626027,
1.98346628839282));
#20430=CARTESIAN_POINT('Ctrl Pts',(0.154704534637707,-0.0162026608399094,
1.98339043820738));
#20431=CARTESIAN_POINT('Ctrl Pts',(0.154655346662608,-0.0166656231748197,
1.98335731288039));
#20432=CARTESIAN_POINT('Ctrl Pts',(0.154548731894783,-0.017627950266065,
1.98328828696969));
#20433=CARTESIAN_POINT('Ctrl Pts',(0.154490961571659,-0.018127270687945,
1.98325237596203));
#20434=CARTESIAN_POINT('Ctrl Pts',(0.154335129211849,-0.0194192779922778,
1.98315920236655));
#20435=CARTESIAN_POINT('Ctrl Pts',(0.154233381047045,-0.0202114965602983,
1.98310182453138));
#20436=CARTESIAN_POINT('Ctrl Pts',(0.153770262929164,-0.0236099980672875,
1.98285459344487));
#20437=CARTESIAN_POINT('Ctrl Pts',(0.153348915995802,-0.0262075210822798,
1.98266286686325));
#20438=CARTESIAN_POINT('Ctrl Pts',(0.152062956231254,-0.0330346839489465,
1.9821512342244));
#20439=CARTESIAN_POINT('Ctrl Pts',(0.151087858235822,-0.0372409160313285,
1.98182806772955));
#20440=CARTESIAN_POINT('Ctrl Pts',(0.1466408255629,-0.0533465025791879,
1.98056024066003));
#20441=CARTESIAN_POINT('Ctrl Pts',(0.141927179329378,-0.0648537737352712,
1.97958446705739));
#20442=CARTESIAN_POINT('Ctrl Pts',(0.135460343054487,-0.0764663958901571,
1.97857167519509));
#20443=CARTESIAN_POINT('Ctrl Pts',(0.135015159455912,-0.0772497315233394,
1.97850323477643));
#20444=CARTESIAN_POINT('Ctrl Pts',(0.132966853505567,-0.0807820845763594,
1.97819418700037));
#20445=CARTESIAN_POINT('Ctrl Pts',(0.131286263845199,-0.0834856274826196,
1.97795646698831));
#20446=CARTESIAN_POINT('Ctrl Pts',(0.129221591909066,-0.0865903022054238,
1.97768367850536));
#20447=CARTESIAN_POINT('Ctrl Pts',(0.128917034029391,-0.0870430848047933,
1.97764390083446));
#20448=CARTESIAN_POINT('Ctrl Pts',(0.128423592765812,-0.0877684069465211,
1.97758020084116));
#20449=CARTESIAN_POINT('Ctrl Pts',(0.128236213354629,-0.0880419560598212,
1.97755618170201));
#20450=CARTESIAN_POINT('Ctrl Pts',(0.127900975753297,-0.088528017718981,
1.97751351425601));
#20451=CARTESIAN_POINT('Ctrl Pts',(0.127753460378654,-0.088740762252881,
1.977494843191));
#20452=CARTESIAN_POINT('Ctrl Pts',(0.127437706578511,-0.0891937186337115,
1.97745509988986));
#20453=CARTESIAN_POINT('Ctrl Pts',(0.127269320148192,-0.0894338227663322,
1.97743403800241));
#20454=CARTESIAN_POINT('Ctrl Pts',(0.126808685480241,-0.0900867114633001,
1.97737677696216));
#20455=CARTESIAN_POINT('Ctrl Pts',(0.126515097934635,-0.0904985541826887,
1.97734066783917));
#20456=CARTESIAN_POINT('Ctrl Pts',(0.124989292510319,-0.0926170075093756,
1.97715494415612));
#20457=CARTESIAN_POINT('Ctrl Pts',(0.123724457173736,-0.0943000169714633,
1.97700744879639));
#20458=CARTESIAN_POINT('Ctrl Pts',(0.119883600746526,-0.0992003376135383,
1.9765764217289));
#20459=CARTESIAN_POINT('Ctrl Pts',(0.117213329133151,-0.10234171158765,
1.97629802048815));
#20460=CARTESIAN_POINT('Ctrl Pts',(0.107341338496447,-0.113061338500483,
1.97532531852297));
#20461=CARTESIAN_POINT('Ctrl Pts',(0.0995047140663776,-0.120016043834059,
1.97464976000939));
#20462=CARTESIAN_POINT('Ctrl Pts',(0.0858590321600602,-0.12986412210963,
1.97352352515621));
#20463=CARTESIAN_POINT('Ctrl Pts',(0.0804644437138974,-0.133273854104561,
1.97308940418812));
#20464=CARTESIAN_POINT('Ctrl Pts',(0.0740106587693025,-0.13681812882779,
1.97257345784011));
#20465=CARTESIAN_POINT('Ctrl Pts',(0.0731404578968763,-0.137285291733489,
1.97250396685572));
#20466=CARTESIAN_POINT('Ctrl Pts',(0.0717362247230707,-0.138022006649275,
1.97239192242702));
#20467=CARTESIAN_POINT('Ctrl Pts',(0.0712049731881711,-0.138296825821093,
1.97234955466334));
#20468=CARTESIAN_POINT('Ctrl Pts',(0.07026909053954,-0.138774140732129,
1.97227494746398));
#20469=CARTESIAN_POINT('Ctrl Pts',(0.0698651335014268,-0.138977949093029,
1.97224275442924));
#20470=CARTESIAN_POINT('Ctrl Pts',(0.0690212691370247,-0.139399094900101,
1.97217552066247));
#20471=CARTESIAN_POINT('Ctrl Pts',(0.0685812118368766,-0.139616118786712,
1.97214046944005));
#20472=CARTESIAN_POINT('Ctrl Pts',(0.0676825380167003,-0.140054045538962,
1.97206890499292));
#20473=CARTESIAN_POINT('Ctrl Pts',(0.0672238495825327,-0.140274786259309,
1.97203238664851));
#20474=CARTESIAN_POINT('Ctrl Pts',(0.0661008095077572,-0.140808468407406,
1.97194299272089));
#20475=CARTESIAN_POINT('Ctrl Pts',(0.0654353150787797,-0.141118961514586,
1.97189003345686));
#20476=CARTESIAN_POINT('Ctrl Pts',(0.063603008704174,-0.14195809477838,
1.97174424648088));
#20477=CARTESIAN_POINT('Ctrl Pts',(0.062431849225154,-0.142477041693043,
1.97165109157827));
#20478=CARTESIAN_POINT('Ctrl Pts',(0.0518180626325385,-0.147024076377469,
1.97080694902398));
#20479=CARTESIAN_POINT('Ctrl Pts',(0.042006506597302,-0.150121842374042,
1.9700246440002));
#20480=CARTESIAN_POINT('Ctrl Pts',(0.0215053315239889,-0.154426406878573,
1.9684030039209));
#20481=CARTESIAN_POINT('Ctrl Pts',(0.0108479864099955,-0.155538926101167,
1.96756713370226));
#20482=CARTESIAN_POINT('Ctrl Pts',(-0.000955858027842796,-0.155551065268592,
1.96669512941088));
#20483=CARTESIAN_POINT('Ctrl Pts',(-0.00207170853954404,-0.155540206336629,
1.96661324912423));
#20484=CARTESIAN_POINT('Ctrl Pts',(-0.00360320139091767,-0.155508817798688,
1.96650171335142));
#20485=CARTESIAN_POINT('Ctrl Pts',(-0.00401898546064192,-0.1554986277756,
1.96647151801203));
#20486=CARTESIAN_POINT('Ctrl Pts',(-0.00468073718734669,-0.155479753563257,
1.96642360107445));
#20487=CARTESIAN_POINT('Ctrl Pts',(-0.00492672961068839,-0.155472153154082,
1.96640582002003));
#20488=CARTESIAN_POINT('Ctrl Pts',(-0.00543559407843104,-0.155455221861582,
1.96636910349563));
#20489=CARTESIAN_POINT('Ctrl Pts',(-0.00569846076860234,-0.155445808026944,
1.9663501731504));
#20490=CARTESIAN_POINT('Ctrl Pts',(-0.0063259462810383,-0.155421742568673,
1.96630506949476));
#20491=CARTESIAN_POINT('Ctrl Pts',(-0.00669054305884584,-0.155406474447979,
1.96627893050278));
#20492=CARTESIAN_POINT('Ctrl Pts',(-0.00792530370060249,-0.155350413253704,
1.9661906277238));
#20493=CARTESIAN_POINT('Ctrl Pts',(-0.00879519914416804,-0.155303592688903,
1.96612878940414));
#20494=CARTESIAN_POINT('Ctrl Pts',(-0.0189396985458115,-0.154672071287271,
1.96541149714302));
#20495=CARTESIAN_POINT('Ctrl Pts',(-0.0281459778217095,-0.153264557204525,
1.96479752282471));
#20496=CARTESIAN_POINT('Ctrl Pts',(-0.0490372648985847,-0.148123062779557,
1.96338054238323));
#20497=CARTESIAN_POINT('Ctrl Pts',(-0.0605147332264084,-0.143815901292031,
1.96258099869321));
#20498=CARTESIAN_POINT('Ctrl Pts',(-0.0728982800061205,-0.137421263632336,
1.96161218079769));
#20499=CARTESIAN_POINT('Ctrl Pts',(-0.0744138140669874,-0.136606540071449,
1.96149175063737));
#20500=CARTESIAN_POINT('Ctrl Pts',(-0.0765273766854905,-0.135424719365902,
1.96132099965181));
#20501=CARTESIAN_POINT('Ctrl Pts',(-0.0771369531147193,-0.135078438075342,
1.96127142004941));
#20502=CARTESIAN_POINT('Ctrl Pts',(-0.0781196302719578,-0.13451138906466,
1.96119094344579));
#20503=CARTESIAN_POINT('Ctrl Pts',(-0.0784941907023739,-0.134293158578411,
1.96116013803356));
#20504=CARTESIAN_POINT('Ctrl Pts',(-0.0792650525500041,-0.133839703855469,
1.96109646609591));
#20505=CARTESIAN_POINT('Ctrl Pts',(-0.0796612301690202,-0.133604278686816,
1.96106359251929));
#20506=CARTESIAN_POINT('Ctrl Pts',(-0.0805902996664638,-0.133046585558012,
1.96098614423926));
#20507=CARTESIAN_POINT('Ctrl Pts',(-0.0811223105533769,-0.13272287307985,
1.96094151719078));
#20508=CARTESIAN_POINT('Ctrl Pts',(-0.0822430216212552,-0.132031698771067,
1.96084691083047));
#20509=CARTESIAN_POINT('Ctrl Pts',(-0.0828312336650479,-0.131663475520993,
1.96079690418931));
#20510=CARTESIAN_POINT('Ctrl Pts',(-0.0844136829933907,-0.130658054236761,
1.960661407425));
#20511=CARTESIAN_POINT('Ctrl Pts',(-0.085403142529092,-0.13001346129073,
1.96057564577962));
#20512=CARTESIAN_POINT('Ctrl Pts',(-0.0935766449473686,-0.12455519115846,
1.95985836514297));
#20513=CARTESIAN_POINT('Ctrl Pts',(-0.100353851602388,-0.119162243733623,
1.95920492475817));
#20514=CARTESIAN_POINT('Ctrl Pts',(-0.113253623320465,-0.107013002611593,
1.95783995513486));
#20515=CARTESIAN_POINT('Ctrl Pts',(-0.119302950469435,-0.100224613700158,
1.9571297266313));
#20516=CARTESIAN_POINT('Ctrl Pts',(-0.127193279130592,-0.0896366120549464,
1.95612278647015));
#20517=CARTESIAN_POINT('Ctrl Pts',(-0.129528093174465,-0.086228377536606,
1.95581227193964));
#20518=CARTESIAN_POINT('Ctrl Pts',(-0.132065883290486,-0.0821876903225205,
1.95546284378582));
#20519=CARTESIAN_POINT('Ctrl Pts',(-0.132403694690286,-0.0816423642520919,
1.95541606687148));
#20520=CARTESIAN_POINT('Ctrl Pts',(-0.132908365124097,-0.0808163077729507,
1.95534580096908));
#20521=CARTESIAN_POINT('Ctrl Pts',(-0.133077723808474,-0.0805371253105897,
1.95532215436101));
#20522=CARTESIAN_POINT('Ctrl Pts',(-0.133379244285927,-0.0800365302871452,
1.95527993779332));
#20523=CARTESIAN_POINT('Ctrl Pts',(-0.133511735243091,-0.0798153214779604,
1.95526134664775));
#20524=CARTESIAN_POINT('Ctrl Pts',(-0.133797301256218,-0.079335835604815,
1.95522118769646));
#20525=CARTESIAN_POINT('Ctrl Pts',(-0.133950178411043,-0.0790774452190182,
1.95519963278577));
#20526=CARTESIAN_POINT('Ctrl Pts',(-0.134374618096505,-0.078355301794799,
1.95513962743399));
#20527=CARTESIAN_POINT('Ctrl Pts',(-0.134644530442156,-0.07789057550641,
1.95510128208874));
#20528=CARTESIAN_POINT('Ctrl Pts',(-0.136187198456087,-0.0752024779054694,
1.95488098073415));
#20529=CARTESIAN_POINT('Ctrl Pts',(-0.137407375798178,-0.0729491661319911,
1.95470219627397));
#20530=CARTESIAN_POINT('Ctrl Pts',(-0.145268243243652,-0.0575346408648738,
1.95351124157567));
#20531=CARTESIAN_POINT('Ctrl Pts',(-0.150065138145776,-0.043516229409762,
1.95257692528643));
#20532=CARTESIAN_POINT('Ctrl Pts',(-0.153601606067318,-0.0249002894026177,
1.95130390485614));
#20533=CARTESIAN_POINT('Ctrl Pts',(-0.154218412415422,-0.0207401610576978,
1.95101799420024));
#20534=CARTESIAN_POINT('Ctrl Pts',(-0.15489124737387,-0.0144562234771152,
1.95058054668062));
#20535=CARTESIAN_POINT('Ctrl Pts',(-0.155073574330454,-0.0123477406578274,
1.95043284499954));
#20536=CARTESIAN_POINT('Ctrl Pts',(-0.155262955910089,-0.00947614583061637,
1.95023014598214));
#20537=CARTESIAN_POINT('Ctrl Pts',(-0.155307501279662,-0.00871566560299412,
1.95017631942679));
#20538=CARTESIAN_POINT('Ctrl Pts',(-0.155369221036843,-0.00751037771224534,
1.95009076532835));
#20539=CARTESIAN_POINT('Ctrl Pts',(-0.155390075623419,-0.00706576317293903,
1.95005915298214));
#20540=CARTESIAN_POINT('Ctrl Pts',(-0.155428039236629,-0.00617468537339508,
1.94999568854372));
#20541=CARTESIAN_POINT('Ctrl Pts',(-0.155445133542863,-0.00572822578035388,
1.94996383630101));
#20542=CARTESIAN_POINT('Ctrl Pts',(-0.155475548762664,-0.00483299192687254,
1.94989985476956));
#20543=CARTESIAN_POINT('Ctrl Pts',(-0.155488850626594,-0.00438422137019486,
1.94986772519707));
#20544=CARTESIAN_POINT('Ctrl Pts',(-0.155516523312597,-0.00329078632529114,
1.94978930068499));
#20545=CARTESIAN_POINT('Ctrl Pts',(-0.155528828583525,-0.00264608277559738,
1.94974294167468));
#20546=CARTESIAN_POINT('Ctrl Pts',(-0.155545899167395,-0.00131941042582578,
1.94964729242611));
#20547=CARTESIAN_POINT('Ctrl Pts',(-0.155550188730665,-0.000637452225819819,
1.94959798844521));
#20548=CARTESIAN_POINT('Ctrl Pts',(-0.155549993634555,4.4500446807104E-5,
1.94954854470546));
#20549=CARTESIAN_POINT('Ctrl Pts',(-0.155549993659165,4.44143407372304E-5,
1.94954855094842));
#20550=CARTESIAN_POINT('Ctrl Pts',(-0.155548101258003,0.00667207072290408,
1.94906802487631));
#20551=CARTESIAN_POINT('Ctrl Pts',(-0.155122636147792,0.0132920259975428,
1.94857436416224));
#20552=CARTESIAN_POINT('Ctrl Pts',(-0.152482240194681,0.0337989542877253,
1.94700207819705));
#20553=CARTESIAN_POINT('Ctrl Pts',(-0.148808679883158,0.04742510843954,
1.94588882031672));
#20554=CARTESIAN_POINT('Ctrl Pts',(-0.142496832313422,0.0624127955721348,
1.94467037371801));
#20555=CARTESIAN_POINT('Ctrl Pts',(-0.141594005450325,0.064434798587637,
1.94450631040506));
#20556=CARTESIAN_POINT('Ctrl Pts',(-0.140428729685775,0.0669017081128451,
1.94430712885515));
#20557=CARTESIAN_POINT('Ctrl Pts',(-0.140206899836237,0.0673653614850748,
1.94426973631914));
#20558=CARTESIAN_POINT('Ctrl Pts',(-0.139854102774855,0.0680934615613401,
1.94421109503832));
#20559=CARTESIAN_POINT('Ctrl Pts',(-0.139724677045046,0.0683586439229629,
1.94418975363807));
#20560=CARTESIAN_POINT('Ctrl Pts',(-0.139480430694265,0.068855492180789,
1.94414980124356));
#20561=CARTESIAN_POINT('Ctrl Pts',(-0.139365788459261,0.0690872373071932,
1.94413118005838));
#20562=CARTESIAN_POINT('Ctrl Pts',(-0.139101652413358,0.069617845835817,
1.94408857496985));
#20563=CARTESIAN_POINT('Ctrl Pts',(-0.138951773153954,0.0699165138289534,
1.94406461541404));
#20564=CARTESIAN_POINT('Ctrl Pts',(-0.138556092845935,0.0706986975422221,
1.94400191900117));
#20565=CARTESIAN_POINT('Ctrl Pts',(-0.138308720321889,0.0711814203634465,
1.94396327780331));
#20566=CARTESIAN_POINT('Ctrl Pts',(-0.136622386882318,0.0744301498470395,
1.9437035044587));
#20567=CARTESIAN_POINT('Ctrl Pts',(-0.135102939975808,0.0771538913108513,
1.94348709331092));
#20568=CARTESIAN_POINT('Ctrl Pts',(-0.132994460943277,0.0806799590927155,
1.94320628877225));
#20569=CARTESIAN_POINT('Ctrl Pts',(-0.132478311159367,0.0815247177059097,
1.94313896498887));
#20570=CARTESIAN_POINT('Ctrl Pts',(-0.125401180664853,0.0928628115699695,
1.94223388428348));
#20571=CARTESIAN_POINT('Ctrl Pts',(-0.117618537093517,0.102542095411774,
1.94144055988637));
#20572=CARTESIAN_POINT('Ctrl Pts',(-0.105686486376321,0.114213745264046,
1.94032367419196));
#20573=CARTESIAN_POINT('Ctrl Pts',(-0.102478641422242,0.117100538816519,
1.94003167995245));
#20574=CARTESIAN_POINT('Ctrl Pts',(-0.0978121326962387,0.120961264864625,
1.93961440727012));
#20575=CARTESIAN_POINT('Ctrl Pts',(-0.0964505514090239,0.12204970964807,
1.9394935083316));
#20576=CARTESIAN_POINT('Ctrl Pts',(-0.0943479378588876,0.123673375188351,
1.93930789324801));
#20577=CARTESIAN_POINT('Ctrl Pts',(-0.0936199731629827,0.124225350357299,
1.93924382275595));
#20578=CARTESIAN_POINT('Ctrl Pts',(-0.092419108691455,0.125119348610096,
1.93913841884149));
#20579=CARTESIAN_POINT('Ctrl Pts',(-0.0919490639791205,0.125465185070119,
1.93909723271501));
#20580=CARTESIAN_POINT('Ctrl Pts',(-0.0910373313247781,0.126128119133708,
1.9390174750252));
#20581=CARTESIAN_POINT('Ctrl Pts',(-0.0905959042477838,0.126445562400733,
1.93897891745529));
#20582=CARTESIAN_POINT('Ctrl Pts',(-0.0901487438348547,0.126763585110641,
1.93893991474853));
#20583=CARTESIAN_POINT('Ctrl Pts',(-0.0901446605611322,0.126766488858149,
1.9389395585975));
#20584=CARTESIAN_POINT('Ctrl Pts',(-0.0901364395265637,0.126772334502643,
1.93893884155237));
#20585=CARTESIAN_POINT('Ctrl Pts',(-0.0901323017632664,0.126775276393433,
1.93893848065817));
#20586=CARTESIAN_POINT('Ctrl Pts',(-0.0901239694976532,0.126781199901523,
1.93893775393067));
#20587=CARTESIAN_POINT('Ctrl Pts',(-0.0901197749909123,0.126784181513591,
1.9389373880971));
#20588=CARTESIAN_POINT('Ctrl Pts',(-0.0901113268814691,0.126790186114276,
1.93893665128568));
#20589=CARTESIAN_POINT('Ctrl Pts',(-0.0901070732741274,0.126793209097343,
1.93893628030756));
#20590=CARTESIAN_POINT('Ctrl Pts',(-0.0900985044965344,0.126799298166471,
1.93893553299229));
#20591=CARTESIAN_POINT('Ctrl Pts',(-0.0900941893217961,0.126802364246373,
1.9389351566549));
#20592=CARTESIAN_POINT('Ctrl Pts',(-0.0900854948267593,0.126808541315933,
1.93893439839629));
#20593=CARTESIAN_POINT('Ctrl Pts',(-0.090081115501624,0.126811652299147,
1.9389340164748));
#20594=CARTESIAN_POINT('Ctrl Pts',(-0.0900722899994163,0.126817921067967,
1.93893324681243));
#20595=CARTESIAN_POINT('Ctrl Pts',(-0.0900678438172105,0.12682107884677,
1.93893285907127));
#20596=CARTESIAN_POINT('Ctrl Pts',(-0.0900603829372504,0.126826377141611,
1.93893220843461));
#20597=CARTESIAN_POINT('Ctrl Pts',(-0.0900573683296655,0.12682851778368,
1.938931945544));
#20598=CARTESIAN_POINT('Ctrl Pts',(-0.0900511162572359,0.126832956981182,
1.93893140033362));
#20599=CARTESIAN_POINT('Ctrl Pts',(-0.0900478787803757,0.126835255520377,
1.9389311180132));
#20600=CARTESIAN_POINT('Ctrl Pts',(-0.0900411605587199,0.126840024926912,
1.93893053216451));
#20601=CARTESIAN_POINT('Ctrl Pts',(-0.090037679800594,0.126842495774667,
1.93893022863553));
#20602=CARTESIAN_POINT('Ctrl Pts',(-0.0900304521547473,0.126847625937275,
1.93892959837756));
#20603=CARTESIAN_POINT('Ctrl Pts',(-0.0900267052510161,0.126850285229312,
1.93892927164769));
#20604=CARTESIAN_POINT('Ctrl Pts',(-0.0900189196155608,0.126855810413918,
1.93892859274869));
#20605=CARTESIAN_POINT('Ctrl Pts',(-0.0900148808639589,0.126858676280229,
1.93892824057845));
#20606=CARTESIAN_POINT('Ctrl Pts',(-0.0900064825288195,0.126864635069674,
1.93892750827155));
#20607=CARTESIAN_POINT('Ctrl Pts',(-0.0900021229232172,0.126867727960606,
1.93892712813372));
#20608=CARTESIAN_POINT('Ctrl Pts',(-0.0899930500161233,0.126874163966456,
1.93892633702837));
#20609=CARTESIAN_POINT('Ctrl Pts',(-0.0899883366882774,0.126877507043088,
1.93892592605944));
#20610=CARTESIAN_POINT('Ctrl Pts',(-0.0899785189308473,0.126884469775336,
1.9389250700331));
#20611=CARTESIAN_POINT('Ctrl Pts',(-0.0899734144694325,0.126888089385367,
1.93892462497399));
#20612=CARTESIAN_POINT('Ctrl Pts',(-0.0899627716653422,0.126895635308622,
1.93892369704063));
#20613=CARTESIAN_POINT('Ctrl Pts',(-0.0899572332835722,0.12689956156762,
1.93892321416424));
#20614=CARTESIAN_POINT('Ctrl Pts',(-0.0899456733374862,0.126907755485385,
1.93892220630185));
#20615=CARTESIAN_POINT('Ctrl Pts',(-0.0899396517265052,0.126912023078093,
1.93892168131331));
#20616=CARTESIAN_POINT('Ctrl Pts',(-0.0899270690720986,0.126920939221072,
1.93892058432729));
#20617=CARTESIAN_POINT('Ctrl Pts',(-0.0899205076215407,0.126925587939331,
1.9389200122962));
#20618=CARTESIAN_POINT('Ctrl Pts',(-0.0899067785459363,0.126935313245102,
1.93891881541226));
#20619=CARTESIAN_POINT('Ctrl Pts',(-0.0898996109391876,0.126940389672184,
1.93891819056332));
#20620=CARTESIAN_POINT('Ctrl Pts',(-0.0898845921144436,0.126951024781039,
1.93891688130013));
#20621=CARTESIAN_POINT('Ctrl Pts',(-0.0898767408832245,0.126956583290319,
1.93891619688757));
#20622=CARTESIAN_POINT('Ctrl Pts',(-0.0895000149489004,0.127223244996466,
1.93888335750843));
#20623=CARTESIAN_POINT('Ctrl Pts',(-0.0891300083491297,0.127482737447264,
1.93885114137481));
#20624=CARTESIAN_POINT('Ctrl Pts',(-0.0882758946293854,0.128076207105572,
1.93877685726191));
#20625=CARTESIAN_POINT('Ctrl Pts',(-0.0877910163221103,0.128409056669391,
1.93873474707374));
#20626=CARTESIAN_POINT('Ctrl Pts',(-0.0863635310489605,0.129377103783548,
1.93861094337733));
#20627=CARTESIAN_POINT('Ctrl Pts',(-0.0854158534726185,0.130004716555484,
1.93852896683716));
#20628=CARTESIAN_POINT('Ctrl Pts',(-0.0778307606187714,0.134909313282266,
1.93787439070659));
#20629=CARTESIAN_POINT('Ctrl Pts',(-0.0708862440772289,0.138683750813039,
1.93728355898094));
#20630=CARTESIAN_POINT('Ctrl Pts',(-0.0636886188644129,0.141913925768909,
1.93667989110148));
#20631=CARTESIAN_POINT('',(-0.155681301642334,0.000117756784957245,1.93559437743963));
#20632=CARTESIAN_POINT('Ctrl Pts',(-0.0637929161402304,0.142146585575849,
1.92279372449516));
#20633=CARTESIAN_POINT('Ctrl Pts',(-0.0640110746858145,0.142048797739288,
1.92281092584587));
#20634=CARTESIAN_POINT('Ctrl Pts',(-0.111163659106404,0.120769939794772,
1.9265330314905));
#20635=CARTESIAN_POINT('Ctrl Pts',(-0.151792203072743,0.0668263219655577,
1.93079991580532));
#20636=CARTESIAN_POINT('Ctrl Pts',(-0.155745145114401,0.00770521701255957,
1.93504959876944));
#20637=CARTESIAN_POINT('Ctrl Pts',(-0.155681301642334,0.000117756784957245,
1.93559437743963));
#20638=CARTESIAN_POINT('Ctrl Pts',(-0.155549951651874,0.000122642161511279,
1.93566981437342));
#20639=CARTESIAN_POINT('Ctrl Pts',(-0.155560736539099,-0.0135560851688855,
1.93658042514193));
#20640=CARTESIAN_POINT('Ctrl Pts',(-0.153767332752135,-0.027176334668751,
1.93745914173611));
#20641=CARTESIAN_POINT('Ctrl Pts',(-0.149678189266885,-0.0423854174351624,
1.93853915783634));
#20642=CARTESIAN_POINT('Ctrl Pts',(-0.149101152578633,-0.0443726220478013,
1.93868214852758));
#20643=CARTESIAN_POINT('Ctrl Pts',(-0.148034862048453,-0.0477887131809654,
1.93893161318147));
#20644=CARTESIAN_POINT('Ctrl Pts',(-0.147564112081982,-0.0492231046750981,
1.93903749322602));
#20645=CARTESIAN_POINT('Ctrl Pts',(-0.14686248590787,-0.051260403880581,
1.93918960192921));
#20646=CARTESIAN_POINT('Ctrl Pts',(-0.146648607158145,-0.0518691118966943,
1.93923527091572));
#20647=CARTESIAN_POINT('Ctrl Pts',(-0.146272139818397,-0.0529196108580932,
1.93931447824197));
#20648=CARTESIAN_POINT('Ctrl Pts',(-0.14611131986409,-0.0533620305000578,
1.93934795762436));
#20649=CARTESIAN_POINT('Ctrl Pts',(-0.145798875265619,-0.0542095709404938,
1.93941232979911));
#20650=CARTESIAN_POINT('Ctrl Pts',(-0.145647563888115,-0.0546148032749892,
1.93944321189659));
#20651=CARTESIAN_POINT('Ctrl Pts',(-0.145248203127353,-0.0556708821345272,
1.9395239689754));
#20652=CARTESIAN_POINT('Ctrl Pts',(-0.144997471423163,-0.0563206967374926,
1.93957393317563));
#20653=CARTESIAN_POINT('Ctrl Pts',(-0.144119881127544,-0.0585504176402177,
1.9397463356803));
#20654=CARTESIAN_POINT('Ctrl Pts',(-0.143471516458125,-0.0601216689818702,
1.93986949203347));
#20655=CARTESIAN_POINT('Ctrl Pts',(-0.13778994016593,-0.0732748776776057,
1.94091500987123));
#20656=CARTESIAN_POINT('Ctrl Pts',(-0.131390254839332,-0.0842124674285625,
1.94188623597532));
#20657=CARTESIAN_POINT('Ctrl Pts',(-0.120123636345364,-0.0990038605818356,
1.94332818916026));
#20658=CARTESIAN_POINT('Ctrl Pts',(-0.116235013735456,-0.103541694654355,
1.9437907613586));
#20659=CARTESIAN_POINT('Ctrl Pts',(-0.110523633345129,-0.109478149551362,
1.94441507031621));
#20660=CARTESIAN_POINT('Ctrl Pts',(-0.108916751362631,-0.111076916040401,
1.94458528672098));
#20661=CARTESIAN_POINT('Ctrl Pts',(-0.106277395288187,-0.113590568266269,
1.94485554400103));
#20662=CARTESIAN_POINT('Ctrl Pts',(-0.105266745636878,-0.114527789496645,
1.94495692894366));
#20663=CARTESIAN_POINT('Ctrl Pts',(-0.10391954959005,-0.115744202793354,
1.94508918933754));
#20664=CARTESIAN_POINT('Ctrl Pts',(-0.103594136406815,-0.11603554706154,
1.94512091922421));
#20665=CARTESIAN_POINT('Ctrl Pts',(-0.103086545641807,-0.116486158639652,
1.94517007012003));
#20666=CARTESIAN_POINT('Ctrl Pts',(-0.102905219930328,-0.116646374826935,
1.94518756082316));
#20667=CARTESIAN_POINT('Ctrl Pts',(-0.102528959477556,-0.116977271716535,
1.94522371436903));
#20668=CARTESIAN_POINT('Ctrl Pts',(-0.102333974904538,-0.117147886072938,
1.94524237179416));
#20669=CARTESIAN_POINT('Ctrl Pts',(-0.101886782017343,-0.117537217900752,
1.94528498574661));
#20670=CARTESIAN_POINT('Ctrl Pts',(-0.101634295378522,-0.117755611120077,
1.94530891820904));
#20671=CARTESIAN_POINT('Ctrl Pts',(-0.100961303073109,-0.118333951857486,
1.94537237735447));
#20672=CARTESIAN_POINT('Ctrl Pts',(-0.100539570695256,-0.118692475032757,
1.94541180197351));
#20673=CARTESIAN_POINT('Ctrl Pts',(-0.0975562448091676,-0.121201350091304,
1.94568836694548));
#20674=CARTESIAN_POINT('Ctrl Pts',(-0.0949275562336637,-0.123271048982066,
1.94592006649189));
#20675=CARTESIAN_POINT('Ctrl Pts',(-0.0817561470005722,-0.132970103526315,
1.94703534216842));
#20676=CARTESIAN_POINT('Ctrl Pts',(-0.070350950316552,-0.139341033582169,
1.94786705265347));
#20677=CARTESIAN_POINT('Ctrl Pts',(-0.0542188616325873,-0.145860713403675,
1.94903065356432));
#20678=CARTESIAN_POINT('Ctrl Pts',(-0.0500857603310041,-0.147331070074396,
1.94932729914623));
#20679=CARTESIAN_POINT('Ctrl Pts',(-0.0433536771466576,-0.149409982102765,
1.94981258546593));
#20680=CARTESIAN_POINT('Ctrl Pts',(-0.0407914414924076,-0.150129746886196,
1.9499977434002));
#20681=CARTESIAN_POINT('Ctrl Pts',(-0.0374348984835355,-0.150980375436686,
1.95024146484683));
#20682=CARTESIAN_POINT('Ctrl Pts',(-0.0366561654422768,-0.151171329567979,
1.95029808901912));
#20683=CARTESIAN_POINT('Ctrl Pts',(-0.0353863436199081,-0.151472315699011,
1.95039056688825));
#20684=CARTESIAN_POINT('Ctrl Pts',(-0.0348961284046633,-0.151586001825782,
1.95042630302709));
#20685=CARTESIAN_POINT('Ctrl Pts',(-0.0339517266349029,-0.151800194801551,
1.9504952202802));
#20686=CARTESIAN_POINT('Ctrl Pts',(-0.0334976232380456,-0.151901047106464,
1.95052838992999));
#20687=CARTESIAN_POINT('Ctrl Pts',(-0.0324560232737575,-0.152127479352476,
1.95060454890341));
#20688=CARTESIAN_POINT('Ctrl Pts',(-0.0318682410799109,-0.152251694941682,
1.95064758127769));
#20689=CARTESIAN_POINT('Ctrl Pts',(-0.0303031505197865,-0.152572984277758,
1.9507623187657));
#20690=CARTESIAN_POINT('Ctrl Pts',(-0.0293246562348661,-0.152764069445282,
1.95083421305952));
#20691=CARTESIAN_POINT('Ctrl Pts',(-0.0218612065856581,-0.154147220851159,
1.95138389247779));
#20692=CARTESIAN_POINT('Ctrl Pts',(-0.0153091534947095,-0.154935097947975,
1.95187438267373));
#20693=CARTESIAN_POINT('Ctrl Pts',(0.00264210595473488,-0.155943908639876,
1.95324023937947));
#20694=CARTESIAN_POINT('Ctrl Pts',(0.0140474868714411,-0.155332272976203,
1.95413432988196));
#20695=CARTESIAN_POINT('Ctrl Pts',(0.0285342290034816,-0.152945947004194,
1.95525864861734));
#20696=CARTESIAN_POINT('Ctrl Pts',(0.0317686288650324,-0.152307000450994,
1.95550865138042));
#20697=CARTESIAN_POINT('Ctrl Pts',(0.0361528408756284,-0.151295149191254,
1.95584416164348));
#20698=CARTESIAN_POINT('Ctrl Pts',(0.0373220407423635,-0.151010978301856,
1.95593330400824));
#20699=CARTESIAN_POINT('Ctrl Pts',(0.0390602217786782,-0.150567096423929,
1.95606521545951));
#20700=CARTESIAN_POINT('Ctrl Pts',(0.0396317490393489,-0.150417671661262,
1.95610848980886));
#20701=CARTESIAN_POINT('Ctrl Pts',(0.0406637968119638,-0.150141553979984,
1.95618643712328));
#20702=CARTESIAN_POINT('Ctrl Pts',(0.0411246079561466,-0.150015989945517,
1.95622116968572));
#20703=CARTESIAN_POINT('Ctrl Pts',(0.0418471583835612,-0.149815526370937,
1.95627551078566));
#20704=CARTESIAN_POINT('Ctrl Pts',(0.0421092864472314,-0.149742060238919,
1.95629519999308));
#20705=CARTESIAN_POINT('Ctrl Pts',(0.0426192405377143,-0.149597691421681,
1.95633345412609));
#20706=CARTESIAN_POINT('Ctrl Pts',(0.0428670804370714,-0.149526861664821,
1.95635202248165));
#20707=CARTESIAN_POINT('Ctrl Pts',(0.0434283408213854,-0.149364949827743,
1.95639402068006));
#20708=CARTESIAN_POINT('Ctrl Pts',(0.0437416508320479,-0.149273497350764,
1.95641742871764));
#20709=CARTESIAN_POINT('Ctrl Pts',(0.0446900127946774,-0.148993436476291,
1.9564881789221));
#20710=CARTESIAN_POINT('Ctrl Pts',(0.0453241611516411,-0.148801753398515,
1.95653534662211));
#20711=CARTESIAN_POINT('Ctrl Pts',(0.0502554040324811,-0.147276744341285,
1.95690116946907));
#20712=CARTESIAN_POINT('Ctrl Pts',(0.0544945527977949,-0.145761443306784,
1.95720996619881));
#20713=CARTESIAN_POINT('Ctrl Pts',(0.0724785450229919,-0.13843842106018,
1.95851950745904));
#20714=CARTESIAN_POINT('Ctrl Pts',(0.0854134863931019,-0.130854572180079,
1.95946785406036));
#20715=CARTESIAN_POINT('Ctrl Pts',(0.0999867259902557,-0.119215689626974,
1.96074032589194));
#20716=CARTESIAN_POINT('Ctrl Pts',(0.102817442610874,-0.116783113634066,
1.96099830622388));
#20717=CARTESIAN_POINT('Ctrl Pts',(0.10621759508231,-0.113641682313828,
1.96132362886396));
#20718=CARTESIAN_POINT('Ctrl Pts',(0.106872098250807,-0.113026386384555,
1.96138699407023));
#20719=CARTESIAN_POINT('Ctrl Pts',(0.107900315546164,-0.112042847203186,
1.96148774838475));
#20720=CARTESIAN_POINT('Ctrl Pts',(0.108277566805066,-0.111678315795256,
1.96152497726155));
#20721=CARTESIAN_POINT('Ctrl Pts',(0.108982608753773,-0.110990115293288,
1.9615950535961));
#20722=CARTESIAN_POINT('Ctrl Pts',(0.10931082052639,-0.110666883985498,
1.96162788171888));
#20723=CARTESIAN_POINT('Ctrl Pts',(0.110043680296804,-0.109938704051317,
1.96170165090116));
#20724=CARTESIAN_POINT('Ctrl Pts',(0.11044753645901,-0.109532971728526,
1.96174262630041));
#20725=CARTESIAN_POINT('Ctrl Pts',(0.111467986905762,-0.108496398734033,
1.96184699482639));
#20726=CARTESIAN_POINT('Ctrl Pts',(0.11208146429014,-0.107862532633251,
1.96191052251609));
#20727=CARTESIAN_POINT('Ctrl Pts',(0.115602048949649,-0.104162476548154,
1.9622797125985));
#20728=CARTESIAN_POINT('Ctrl Pts',(0.118388376396759,-0.100984361141317,
1.96259045386355));
#20729=CARTESIAN_POINT('Ctrl Pts',(0.122266767131115,-0.0961792326710502,
1.9630518419119));
#20730=CARTESIAN_POINT('Ctrl Pts',(0.123463153748043,-0.0946385558650066,
1.9631985754465));
#20731=CARTESIAN_POINT('Ctrl Pts',(0.133411101221104,-0.0813180772806547,
1.96445686522506));
#20732=CARTESIAN_POINT('Ctrl Pts',(0.140482878825809,-0.0683786857792587,
1.965621005447));
#20733=CARTESIAN_POINT('Ctrl Pts',(0.146473468126477,-0.0524117917164091,
1.96690107004666));
#20734=CARTESIAN_POINT('Ctrl Pts',(0.14725870156279,-0.0501632263856047,
1.96707776412079));
#20735=CARTESIAN_POINT('Ctrl Pts',(0.148153895696174,-0.0473972780055289,
1.96729006915772));
#20736=CARTESIAN_POINT('Ctrl Pts',(0.148313212175785,-0.0468963739310325,
1.96732831695149));
#20737=CARTESIAN_POINT('Ctrl Pts',(0.148558747110719,-0.0461106247203761,
1.96738799185357));
#20738=CARTESIAN_POINT('Ctrl Pts',(0.148646690361068,-0.0458263298112838,
1.96740951706766));
#20739=CARTESIAN_POINT('Ctrl Pts',(0.148809376701129,-0.0452950163672011,
1.9674496197778));
#20740=CARTESIAN_POINT('Ctrl Pts',(0.148884320082321,-0.0450480669636376,
1.96746820841262));
#20741=CARTESIAN_POINT('Ctrl Pts',(0.149053707856101,-0.0444848693626846,
1.96751048770032));
#20742=CARTESIAN_POINT('Ctrl Pts',(0.149147760425931,-0.0441685068037201,
1.96753415534039));
#20743=CARTESIAN_POINT('Ctrl Pts',(0.149432761146161,-0.0431985649693213,
1.96760647523785));
#20744=CARTESIAN_POINT('Ctrl Pts',(0.149620428951448,-0.0425440172648214,
1.96765494146853));
#20745=CARTESIAN_POINT('Ctrl Pts',(0.152302537149554,-0.0329520656819254,
1.96836054361617));
#20746=CARTESIAN_POINT('Ctrl Pts',(0.153997129445366,-0.0238085451989766,
1.96897494828362));
#20747=CARTESIAN_POINT('Ctrl Pts',(0.155746566149695,-0.00520983802281561,
1.97020584323075));
#20748=CARTESIAN_POINT('Ctrl Pts',(0.155776822276914,0.00420721082647058,
1.97082027010685));
#20749=CARTESIAN_POINT('Ctrl Pts',(0.154577538798896,0.0179028727148061,
1.97175363156202));
#20750=CARTESIAN_POINT('Ctrl Pts',(0.15401643567276,0.0222184585224185,
1.97205335550352));
#20751=CARTESIAN_POINT('Ctrl Pts',(0.153114953172941,0.0274317145151927,
1.97242491744402));
#20752=CARTESIAN_POINT('Ctrl Pts',(0.152946219868382,0.0283573906583666,
1.97249125687299));
#20753=CARTESIAN_POINT('Ctrl Pts',(0.152668586831669,0.0298058754014483,
1.97259566049395));
#20754=CARTESIAN_POINT('Ctrl Pts',(0.152565373205549,0.0303297625996239,
1.97263354389921));
#20755=CARTESIAN_POINT('Ctrl Pts',(0.152377424019499,0.0312585065662062,
1.97270092603383));
#20756=CARTESIAN_POINT('Ctrl Pts',(0.152293766683983,0.0316635785518406,
1.97273039014181));
#20757=CARTESIAN_POINT('Ctrl Pts',(0.152097075569938,0.0325971500418707,
1.97279847277301));
#20758=CARTESIAN_POINT('Ctrl Pts',(0.151982901599042,0.0331254010646873,
1.97283712736884));
#20759=CARTESIAN_POINT('Ctrl Pts',(0.151661618571396,0.0345752540631672,
1.97294358591539));
#20760=CARTESIAN_POINT('Ctrl Pts',(0.151448867041889,0.0354955678896996,
1.97301156944475));
#20761=CARTESIAN_POINT('Ctrl Pts',(0.150312665755701,0.0402142416495102,
1.97336228895718));
#20762=CARTESIAN_POINT('Ctrl Pts',(0.149254734739986,0.0439784242627081,
1.97364930384012));
#20763=CARTESIAN_POINT('Ctrl Pts',(0.14744170478517,0.0496060762246703,
1.97408994132385));
#20764=CARTESIAN_POINT('Ctrl Pts',(0.146790359846765,0.0515015412662265,
1.97424037166348));
#20765=CARTESIAN_POINT('Ctrl Pts',(0.141079630016337,0.0671308543243121,
1.97549741846902));
#20766=CARTESIAN_POINT('Ctrl Pts',(0.134142594246796,0.0800980642564889,
1.97665763748276));
#20767=CARTESIAN_POINT('Ctrl Pts',(0.123907165038909,0.094074733064713,
1.97796213274712));
#20768=CARTESIAN_POINT('Ctrl Pts',(0.122261383105815,0.0962039371820799,
1.97816225282094));
#20769=CARTESIAN_POINT('Ctrl Pts',(0.120216671396456,0.0987119621131707,
1.97839867162313));
#20770=CARTESIAN_POINT('Ctrl Pts',(0.119870057847602,0.099132581936461,
1.97843834526732));
#20771=CARTESIAN_POINT('Ctrl Pts',(0.119328068000838,0.0997832941153622,
1.97849974763129));
#20772=CARTESIAN_POINT('Ctrl Pts',(0.119134225432632,0.10001464858772,1.97852158380102));
#20773=CARTESIAN_POINT('Ctrl Pts',(0.118773693421933,0.100442414401462,
1.97856196530536));
#20774=CARTESIAN_POINT('Ctrl Pts',(0.118607191035839,0.100638974042889,
1.9785805233094));
#20775=CARTESIAN_POINT('Ctrl Pts',(0.118230071907623,0.101081935404589,
1.97862235188254));
#20776=CARTESIAN_POINT('Ctrl Pts',(0.118019173255387,0.101328092440981,
1.9786456013857));
#20777=CARTESIAN_POINT('Ctrl Pts',(0.117395715765617,0.102051193492218,
1.97871391940527));
#20778=CARTESIAN_POINT('Ctrl Pts',(0.116981017506722,0.102526297859334,
1.97875883421953));
#20779=CARTESIAN_POINT('Ctrl Pts',(0.114008381015845,0.105890419083415,
1.97907717527905));
#20780=CARTESIAN_POINT('Ctrl Pts',(0.111346343472478,0.108686199328353,
1.97934337155746));
#20781=CARTESIAN_POINT('Ctrl Pts',(0.107502417612416,0.112433576911384,
1.9797075088671));
#20782=CARTESIAN_POINT('Ctrl Pts',(0.106406748769801,0.11347106712033,1.97980915839058));
#20783=CARTESIAN_POINT('Ctrl Pts',(0.0970379267721891,0.122087359682084,
1.98066225229508));
#20784=CARTESIAN_POINT('Ctrl Pts',(0.0879821903299919,0.128766590670259,
1.98138525082455));
#20785=CARTESIAN_POINT('Ctrl Pts',(0.0733075636240313,0.137313514834558,
1.98252264179783));
#20786=CARTESIAN_POINT('Ctrl Pts',(0.0681720049969127,0.13993414765087,
1.98291464267102));
#20787=CARTESIAN_POINT('Ctrl Pts',(0.0616174750374206,0.14283230052867,
1.98341484555509));
#20788=CARTESIAN_POINT('Ctrl Pts',(0.0603239672736994,0.143383395304276,
1.9835135397042));
#20789=CARTESIAN_POINT('Ctrl Pts',(0.0584431362821732,0.144154761955004,
1.98365710211376));
#20790=CARTESIAN_POINT('Ctrl Pts',(0.0578616440850284,0.144389146738122,
1.98370149445126));
#20791=CARTESIAN_POINT('Ctrl Pts',(0.0568439868182705,0.144792204005907,
1.98377920519604));
#20792=CARTESIAN_POINT('Ctrl Pts',(0.0564084452870791,0.1449624381343,1.98381247074526));
#20793=CARTESIAN_POINT('Ctrl Pts',(0.0555644131828359,0.145287953602485,
1.98387695162242));
#20794=CARTESIAN_POINT('Ctrl Pts',(0.0551560223134122,0.145443482733775,
1.98390815829549));
#20795=CARTESIAN_POINT('Ctrl Pts',(0.0541832565978876,0.145809258712592,
1.98398251089069));
#20796=CARTESIAN_POINT('Ctrl Pts',(0.0536183090507699,0.146017951422052,
1.98402570812693));
#20797=CARTESIAN_POINT('Ctrl Pts',(0.0516041997633292,0.146748702472518,
1.98417977864457));
#20798=CARTESIAN_POINT('Ctrl Pts',(0.0501485553628911,0.147252494676002,
1.98429125297095));
#20799=CARTESIAN_POINT('Ctrl Pts',(0.0350952223025728,0.152213299112027,
1.98544570799005));
#20800=CARTESIAN_POINT('Ctrl Pts',(0.0209544844935645,0.154794307967004,
1.98655363889075));
#20801=CARTESIAN_POINT('Ctrl Pts',(0.00397247037820749,0.155522618564707,
1.98786981194419));
#20802=CARTESIAN_POINT('Ctrl Pts',(0.00127734512879936,0.155568102748949,
1.98807794384487));
#20803=CARTESIAN_POINT('Ctrl Pts',(-0.00491239393441548,0.155511687676728,
1.98855270517993));
#20804=CARTESIAN_POINT('Ctrl Pts',(-0.00840533025798109,0.155362063480086,
1.98881824994742));
#20805=CARTESIAN_POINT('Ctrl Pts',(-0.013769047219835,0.154950848646218,
1.98921974672633));
#20806=CARTESIAN_POINT('Ctrl Pts',(-0.0156449340752918,0.15477270129951,
1.98935897347611));
#20807=CARTESIAN_POINT('Ctrl Pts',(-0.018001654008732,0.154505600647192,
1.98953201452612));
#20808=CARTESIAN_POINT('Ctrl Pts',(-0.0184858234917176,0.154448420275091,
1.98956746457538));
#20809=CARTESIAN_POINT('Ctrl Pts',(-0.0192567164188641,0.15435370089626,
1.98962374045148));
#20810=CARTESIAN_POINT('Ctrl Pts',(-0.0195436123189996,0.154317637776339,
1.98964464709067));
#20811=CARTESIAN_POINT('Ctrl Pts',(-0.0200880085121741,0.154247664059228,
1.98968424586134));
#20812=CARTESIAN_POINT('Ctrl Pts',(-0.0203455211128352,0.15421390898873,
1.98970294598705));
#20813=CARTESIAN_POINT('Ctrl Pts',(-0.0209384454349284,0.154134676719266,
1.98974593334415));
#20814=CARTESIAN_POINT('Ctrl Pts',(-0.0212737942596107,0.154088749583705,
1.98977019501605));
#20815=CARTESIAN_POINT('Ctrl Pts',(-0.0221728474411851,0.15396263027935,
1.98983510817946));
#20816=CARTESIAN_POINT('Ctrl Pts',(-0.0227362731291761,0.15388043604397,
1.98987565005046));
#20817=CARTESIAN_POINT('Ctrl Pts',(-0.0269596957111709,0.153240607256606,
1.99017859863609));
#20818=CARTESIAN_POINT('Ctrl Pts',(-0.0305995653447674,0.15255550191493,
1.99043432520309));
#20819=CARTESIAN_POINT('Ctrl Pts',(-0.0352501274613738,0.151506976033766,
1.99075818682216));
#20820=CARTESIAN_POINT('Ctrl Pts',(-0.0362859753383801,0.15126223375246,
1.99083013610978));
#20821=CARTESIAN_POINT('Ctrl Pts',(-0.0463681469430712,0.14877056514731,
1.99152932766559));
#20822=CARTESIAN_POINT('Ctrl Pts',(-0.0551930951174727,0.145726577715912,
1.99213366936552));
#20823=CARTESIAN_POINT('Ctrl Pts',(-0.0636886415377083,0.141913915593508,
1.99275019838839));
#20824=CARTESIAN_POINT('Origin',(0.,0.,-0.129405622560373));
#20825=CARTESIAN_POINT('',(-0.0636886254669799,0.141913922805787,2.07648623881325));
#20826=CARTESIAN_POINT('',(-0.0636886258537358,0.141913922632217,2.0626609697501));
#20827=CARTESIAN_POINT('',(-0.0636886258329924,0.141913922641526,-0.129405622560373));
#20828=CARTESIAN_POINT('Ctrl Pts',(-0.0636886254669799,0.141913922805787,
2.07648623881325));
#20829=CARTESIAN_POINT('Ctrl Pts',(-0.0622956641982391,0.142539060824529,
2.07638267759085));
#20830=CARTESIAN_POINT('Ctrl Pts',(-0.0608933350929393,0.143143763334241,
2.07627981250369));
#20831=CARTESIAN_POINT('Ctrl Pts',(-0.0501327721664988,0.147597046993911,
2.07549941429699));
#20832=CARTESIAN_POINT('Ctrl Pts',(-0.0404280348378697,0.150544919973361,
2.07484504960544));
#20833=CARTESIAN_POINT('Ctrl Pts',(-0.0239636770900797,0.153837741954139,
2.07372675016692));
#20834=CARTESIAN_POINT('Ctrl Pts',(-0.0173453381300696,0.154723722205612,
2.07327545982922));
#20835=CARTESIAN_POINT('Ctrl Pts',(-0.00917324058954642,0.155286731958653,
2.07270451787251));
#20836=CARTESIAN_POINT('Ctrl Pts',(-0.00765393403831012,0.155369026745032,
2.07259781559541));
#20837=CARTESIAN_POINT('Ctrl Pts',(-0.00548686378400635,0.155454546052616,
2.07244472355231));
#20838=CARTESIAN_POINT('Ctrl Pts',(-0.00483987275185744,0.155476034074275,
2.07239890342213));
#20839=CARTESIAN_POINT('Ctrl Pts',(-0.00372170098785285,0.15550618480947,
2.07231950943887));
#20840=CARTESIAN_POINT('Ctrl Pts',(-0.00325057630437787,0.155516746098265,
2.0722859952406));
#20841=CARTESIAN_POINT('Ctrl Pts',(-0.00234720658276474,0.155532890365862,
2.07222160905139));
#20842=CARTESIAN_POINT('Ctrl Pts',(-0.00191497130348025,0.155538812655423,
2.07219074797147));
#20843=CARTESIAN_POINT('Ctrl Pts',(-0.000788335713863414,0.155549552366646,
2.07211016307335));
#20844=CARTESIAN_POINT('Ctrl Pts',(-9.39245730269155E-5,0.15555152157355,
2.07206035083724));
#20845=CARTESIAN_POINT('Ctrl Pts',(0.00228679373086063,0.155542331271888,
2.07188906877831));
#20846=CARTESIAN_POINT('Ctrl Pts',(0.00397283951082572,0.155508399686774,
2.07176689353877));
#20847=CARTESIAN_POINT('Ctrl Pts',(0.018481944479607,0.154980299326433,
2.07070760637421));
#20848=CARTESIAN_POINT('Ctrl Pts',(0.0311962335365942,0.152928504996118,
2.06971983604702));
#20849=CARTESIAN_POINT('Ctrl Pts',(0.0513942273877773,0.147043716425067,
2.06808843719609));
#20850=CARTESIAN_POINT('Ctrl Pts',(0.0590840368682289,0.144126085969458,
2.06745302953144));
#20851=CARTESIAN_POINT('Ctrl Pts',(0.0672742269164555,0.140252268742962,
2.06678245623224));
#20852=CARTESIAN_POINT('Ctrl Pts',(0.0680372619129649,0.139883707299498,
2.06672005190177));
#20853=CARTESIAN_POINT('Ctrl Pts',(0.0692099695305363,0.139305399607361,
2.06662429172185));
#20854=CARTESIAN_POINT('Ctrl Pts',(0.0696217724159812,0.139100046951471,
2.06659069358713));
#20855=CARTESIAN_POINT('Ctrl Pts',(0.0703044445062772,0.138755829520914,
2.06653505070542));
#20856=CARTESIAN_POINT('Ctrl Pts',(0.0705758245664816,0.138617993544725,
2.06651294569131));
#20857=CARTESIAN_POINT('Ctrl Pts',(0.0711015258838092,0.138349041863207,
2.06647015581293));
#20858=CARTESIAN_POINT('Ctrl Pts',(0.071355893154698,0.138218019386713,
2.06644946536296));
#20859=CARTESIAN_POINT('Ctrl Pts',(0.0718329076586678,0.137970645371728,
2.06641069289501));
#20860=CARTESIAN_POINT('Ctrl Pts',(0.0720556317983023,0.137854457796708,
2.06639260142267));
#20861=CARTESIAN_POINT('Ctrl Pts',(0.0725737291287578,0.137582585449572,
2.06635054368474));
#20862=CARTESIAN_POINT('Ctrl Pts',(0.0728688831807168,0.137426488888788,
2.06632660368311));
#20863=CARTESIAN_POINT('Ctrl Pts',(0.0736413827011932,0.137014752700159,
2.06626399196991));
#20864=CARTESIAN_POINT('Ctrl Pts',(0.0741179055563197,0.136757565796549,
2.06622541549945));
#20865=CARTESIAN_POINT('Ctrl Pts',(0.0773134334108142,0.135011280343933,
2.0659669680923));
#20866=CARTESIAN_POINT('Ctrl Pts',(0.0799889817691292,0.133443542656156,
2.06575176360514));
#20867=CARTESIAN_POINT('Ctrl Pts',(0.0839499587037952,0.13096062448432,
2.06543217899248));
#20868=CARTESIAN_POINT('Ctrl Pts',(0.0852710787834631,0.130104281934588,
2.06532541506364));
#20869=CARTESIAN_POINT('Ctrl Pts',(0.0991200002206248,0.12082590642526,
2.06420188264494));
#20870=CARTESIAN_POINT('Ctrl Pts',(0.110371135606979,0.110643264007005,
2.06324251820545));
#20871=CARTESIAN_POINT('Ctrl Pts',(0.122213737910105,0.0962908557984671,
2.06197063074967));
#20872=CARTESIAN_POINT('Ctrl Pts',(0.124355547833521,0.0935084012003883,
2.0617276108558));
#20873=CARTESIAN_POINT('Ctrl Pts',(0.126914874213432,0.0899399455299788,
2.06141892142732));
#20874=CARTESIAN_POINT('Ctrl Pts',(0.127422369815464,0.0892194973758358,
2.06135674751774));
#20875=CARTESIAN_POINT('Ctrl Pts',(0.128220074770713,0.0880663743923654,
2.06125744846909));
#20876=CARTESIAN_POINT('Ctrl Pts',(0.12851428513708,0.0876364785720714,
2.06122047559546));
#20877=CARTESIAN_POINT('Ctrl Pts',(0.129064946059366,0.086823124805228,
2.06115060713536));
#20878=CARTESIAN_POINT('Ctrl Pts',(0.129321861696096,0.0864399871661661,
2.06111772955062));
#20879=CARTESIAN_POINT('Ctrl Pts',(0.129897051895842,0.0855739033981351,
2.0610434839389));
#20880=CARTESIAN_POINT('Ctrl Pts',(0.130214343201089,0.085090315794578,
2.06100207970718));
#20881=CARTESIAN_POINT('Ctrl Pts',(0.131019008067323,0.0838488753252864,
2.06089591357245));
#20882=CARTESIAN_POINT('Ctrl Pts',(0.131502501246128,0.083088545966045,
2.06083100906028));
#20883=CARTESIAN_POINT('Ctrl Pts',(0.134370274215221,0.0784910230070833,
2.06043919870676));
#20884=CARTESIAN_POINT('Ctrl Pts',(0.136592827608566,0.0745560390962183,
2.06010646297214));
#20885=CARTESIAN_POINT('Ctrl Pts',(0.143560052001153,0.0608606203188363,
2.05895571260128));
#20886=CARTESIAN_POINT('Ctrl Pts',(0.14745357345234,0.0507039054977666,
2.05811184178448));
#20887=CARTESIAN_POINT('Ctrl Pts',(0.152150601679885,0.0331591216091712,
2.05670598908298));
#20888=CARTESIAN_POINT('Ctrl Pts',(0.153541963938232,0.0259658791828275,
2.056144187482));
#20889=CARTESIAN_POINT('Ctrl Pts',(0.154523041124068,0.0178645303840552,
2.05554432202067));
#20890=CARTESIAN_POINT('Ctrl Pts',(0.154617496066022,0.0170276739353214,
2.05548274864821));
#20891=CARTESIAN_POINT('Ctrl Pts',(0.154742616542637,0.0158320777304281,
2.05539537736457));
#20892=CARTESIAN_POINT('Ctrl Pts',(0.154778838314392,0.0154739547903644,
2.05536928295235));
#20893=CARTESIAN_POINT('Ctrl Pts',(0.15483929429916,0.0148547695061723,
2.05532430197778));
#20894=CARTESIAN_POINT('Ctrl Pts',(0.154864112046803,0.0145937671816337,
2.05530538301099));
#20895=CARTESIAN_POINT('Ctrl Pts',(0.154911074279437,0.0140862633715494,
2.05526867841813));
#20896=CARTESIAN_POINT('Ctrl Pts',(0.154933290361797,0.0138397720427953,
2.05525088870563));
#20897=CARTESIAN_POINT('Ctrl Pts',(0.154991877454541,0.0131719130729797,
2.05520278705388));
#20898=CARTESIAN_POINT('Ctrl Pts',(0.155027118778209,0.0127504441300064,
2.05517253791291));
#20899=CARTESIAN_POINT('Ctrl Pts',(0.155152729507844,0.0111706283486375,
2.05505953482104));
#20900=CARTESIAN_POINT('Ctrl Pts',(0.155231842067868,0.0100113852145024,
2.05497738296713));
#20901=CARTESIAN_POINT('Ctrl Pts',(0.155791944253617,0.000184292898756712,
2.05428663311222));
#20902=CARTESIAN_POINT('Ctrl Pts',(0.155559588040781,-0.00851028121019744,
2.05371232045842));
#20903=CARTESIAN_POINT('Ctrl Pts',(0.153576290564738,-0.0263983953322103,
2.05252664374666));
#20904=CARTESIAN_POINT('Ctrl Pts',(0.151720657765623,-0.0355440268302073,
2.05191743976547));
#20905=CARTESIAN_POINT('Ctrl Pts',(0.147820621115431,-0.0486169568909168,
2.05099111143999));
#20906=CARTESIAN_POINT('Ctrl Pts',(0.146410455189692,-0.052711642173404,
2.05069281224681));
#20907=CARTESIAN_POINT('Ctrl Pts',(0.144488664299424,-0.0576169385761271,
2.05032281033137));
#20908=CARTESIAN_POINT('Ctrl Pts',(0.144137925963014,-0.0584888361298803,
2.05025654971203));
#20909=CARTESIAN_POINT('Ctrl Pts',(0.143575610955702,-0.0598509097843598,
2.05015223521));
#20910=CARTESIAN_POINT('Ctrl Pts',(0.143369370442994,-0.0603432769178193,
2.05011436152183));
#20911=CARTESIAN_POINT('Ctrl Pts',(0.142998787155785,-0.0612153621307606,
2.05004697991034));
#20912=CARTESIAN_POINT('Ctrl Pts',(0.142835455174496,-0.0615955065556782,
2.05001750653184));
#20913=CARTESIAN_POINT('Ctrl Pts',(0.142455079509633,-0.0624711569885374,
2.04994937828776));
#20914=CARTESIAN_POINT('Ctrl Pts',(0.142236964852003,-0.0629661889398991,
2.04991068721747));
#20915=CARTESIAN_POINT('Ctrl Pts',(0.141630197430357,-0.0643240640977797,
2.04980406592847));
#20916=CARTESIAN_POINT('Ctrl Pts',(0.141236251522508,-0.0651845014442556,
2.04973595530566));
#20917=CARTESIAN_POINT('Ctrl Pts',(0.139166658612167,-0.0695979544481655,
2.04938370417014));
#20918=CARTESIAN_POINT('Ctrl Pts',(0.137364850536351,-0.0730898544289354,
2.04909524074928));
#20919=CARTESIAN_POINT('Ctrl Pts',(0.134456082216056,-0.0782387950555005,
2.04865443721661));
#20920=CARTESIAN_POINT('Ctrl Pts',(0.133446198495531,-0.0799491001134729,
2.04850534812784));
#20921=CARTESIAN_POINT('Ctrl Pts',(0.124705413320081,-0.0941249997566661,
2.04724720115719));
#20922=CARTESIAN_POINT('Ctrl Pts',(0.115281025177264,-0.105456923556556,
2.04608427625801));
#20923=CARTESIAN_POINT('Ctrl Pts',(0.102440643361194,-0.117084491343859,
2.04478028848023));
#20924=CARTESIAN_POINT('Ctrl Pts',(0.100425413734909,-0.118817515964591,
2.04458268605807));
#20925=CARTESIAN_POINT('Ctrl Pts',(0.097945823662672,-0.120841686436793,
2.04434883590489));
#20926=CARTESIAN_POINT('Ctrl Pts',(0.097523232928543,-0.121182988148829,
2.04430929680956));
#20927=CARTESIAN_POINT('Ctrl Pts',(0.09686332253773,-0.121710271299456,
2.04424805299734));
#20928=CARTESIAN_POINT('Ctrl Pts',(0.0966272411214427,-0.121897783697298,
2.04422624174622));
#20929=CARTESIAN_POINT('Ctrl Pts',(0.0961883335620947,-0.122244318519215,
2.04418587641576));
#20930=CARTESIAN_POINT('Ctrl Pts',(0.0959856593201225,-0.122403521724124,
2.04416730981567));
#20931=CARTESIAN_POINT('Ctrl Pts',(0.0955266422449359,-0.122762244343472,
2.04412542363151));
#20932=CARTESIAN_POINT('Ctrl Pts',(0.0952700700840349,-0.122961464557996,
2.0441021253196));
#20933=CARTESIAN_POINT('Ctrl Pts',(0.0945112639360413,-0.123546852840624,
2.0440335514161));
#20934=CARTESIAN_POINT('Ctrl Pts',(0.094007284397356,-0.123930764439978,
2.0439884312012));
#20935=CARTESIAN_POINT('Ctrl Pts',(0.0903602841157865,-0.126673855575282,
2.04366485355056));
#20936=CARTESIAN_POINT('Ctrl Pts',(0.087130866571543,-0.128916505453164,
2.04339389888893));
#20937=CARTESIAN_POINT('Ctrl Pts',(0.0733305352821005,-0.137744237186509,
2.04228342656825));
#20938=CARTESIAN_POINT('Ctrl Pts',(0.0620732647582102,-0.143170522243238,
2.04148551987718));
#20939=CARTESIAN_POINT('Ctrl Pts',(0.0461828845534744,-0.14859935672349,
2.04036212179378));
#20940=CARTESIAN_POINT('Ctrl Pts',(0.0420205066458944,-0.149829568925271,
2.04006850765254));
#20941=CARTESIAN_POINT('Ctrl Pts',(0.0352505636585199,-0.151526154500328,
2.03958770926936));
#20942=CARTESIAN_POINT('Ctrl Pts',(0.0326729245129962,-0.152102782015107,
2.03940392408859));
#20943=CARTESIAN_POINT('Ctrl Pts',(0.029297282843071,-0.152768162252996,
2.03916174674579));
#20944=CARTESIAN_POINT('Ctrl Pts',(0.0285114137604122,-0.152916779401914,
2.03910526267879));
#20945=CARTESIAN_POINT('Ctrl Pts',(0.0272296083086953,-0.153148959611894,
2.03901294912769));
#20946=CARTESIAN_POINT('Ctrl Pts',(0.0267343437212509,-0.153236191070581,
2.03897723633928));
#20947=CARTESIAN_POINT('Ctrl Pts',(0.0257798507721272,-0.153399538704556,
2.03890831930405));
#20948=CARTESIAN_POINT('Ctrl Pts',(0.0253206859403374,-0.153475998238991,
2.0388751263305));
#20949=CARTESIAN_POINT('Ctrl Pts',(0.0242668610774355,-0.15364662195843,
2.03879885022507));
#20950=CARTESIAN_POINT('Ctrl Pts',(0.0236719869564152,-0.153739396383812,
2.03875572366253));
#20951=CARTESIAN_POINT('Ctrl Pts',(0.0220866021974973,-0.153977227696996,
2.03864059534232));
#20952=CARTESIAN_POINT('Ctrl Pts',(0.0210952189776232,-0.154116177914693,
2.03856840242787));
#20953=CARTESIAN_POINT('Ctrl Pts',(0.0134071135609243,-0.155118156869436,
2.03800691375735));
#20954=CARTESIAN_POINT('Ctrl Pts',(0.00666297273687062,-0.155553762860099,
2.03750427294359));
#20955=CARTESIAN_POINT('Ctrl Pts',(-0.0141459425090446,-0.155542087656156,
2.03592200441384));
#20956=CARTESIAN_POINT('Ctrl Pts',(-0.0281371985521883,-0.153628472660792,
2.03480803373935));
#20957=CARTESIAN_POINT('Ctrl Pts',(-0.0438165474941609,-0.149267641069909,
2.03358864838604));
#20958=CARTESIAN_POINT('Ctrl Pts',(-0.0459398808129136,-0.148627881769986,
2.03342434272078));
#20959=CARTESIAN_POINT('Ctrl Pts',(-0.0485380148355302,-0.147784058772046,
2.03322490826515));
#20960=CARTESIAN_POINT('Ctrl Pts',(-0.0490262957991695,-0.147622793808001,
2.03318749845901));
#20961=CARTESIAN_POINT('Ctrl Pts',(-0.049793555065181,-0.147365163708992,
2.03312883620861));
#20962=CARTESIAN_POINT('Ctrl Pts',(-0.0500730680785558,-0.14727042288991,
2.0331074910005));
#20963=CARTESIAN_POINT('Ctrl Pts',(-0.050596937468862,-0.147091193700875,
2.03306753540786));
#20964=CARTESIAN_POINT('Ctrl Pts',(-0.0508413499077227,-0.147006892650091,
2.03304891481324));
#20965=CARTESIAN_POINT('Ctrl Pts',(-0.0514011033278442,-0.146812263398327,
2.03300631622792));
#20966=CARTESIAN_POINT('Ctrl Pts',(-0.0517162995560982,-0.146701528531079,
2.03298236255744));
#20967=CARTESIAN_POINT('Ctrl Pts',(-0.0525420369383522,-0.146408438122534,
2.03291969164084));
#20968=CARTESIAN_POINT('Ctrl Pts',(-0.0530519918333324,-0.146224425404003,
2.03288106992796));
#20969=CARTESIAN_POINT('Ctrl Pts',(-0.0564831615006314,-0.144966005381496,
2.03262169656346));
#20970=CARTESIAN_POINT('Ctrl Pts',(-0.0593727811244302,-0.143806698817963,
2.0324056494206));
#20971=CARTESIAN_POINT('Ctrl Pts',(-0.0672834943167241,-0.140353789861725,
2.03181566243648));
#20972=CARTESIAN_POINT('Ctrl Pts',(-0.0722204444082067,-0.137878469120591,
2.03144906853591));
#20973=CARTESIAN_POINT('Ctrl Pts',(-0.0832715841753618,-0.131580739529127,
2.03060954000382));
#20974=CARTESIAN_POINT('Ctrl Pts',(-0.0892722067334473,-0.127585728471211,
2.03013901343866));
#20975=CARTESIAN_POINT('Ctrl Pts',(-0.100077927781603,-0.119254925037336,
2.02922907721691));
#20976=CARTESIAN_POINT('Ctrl Pts',(-0.104931359887628,-0.115007487633497,
2.02879253407257));
#20977=CARTESIAN_POINT('Ctrl Pts',(-0.110567754109858,-0.109420312700081,
2.02823919231511));
#20978=CARTESIAN_POINT('Ctrl Pts',(-0.111613216522664,-0.108353692626021,
2.02813442941121));
#20979=CARTESIAN_POINT('Ctrl Pts',(-0.113086240088601,-0.106806917631759,
2.02798363728355));
#20980=CARTESIAN_POINT('Ctrl Pts',(-0.113526459297088,-0.10633888455524,
2.02793815422475));
#20981=CARTESIAN_POINT('Ctrl Pts',(-0.114283910416013,-0.1055235120114,
2.02785915778206));
#20982=CARTESIAN_POINT('Ctrl Pts',(-0.114602492455259,-0.10517743332744,
2.02782570242702));
#20983=CARTESIAN_POINT('Ctrl Pts',(-0.115211541653921,-0.104509764894284,
2.02776129753977));
#20984=CARTESIAN_POINT('Ctrl Pts',(-0.115502244748372,-0.104188395417229,
2.02773035839867));
#20985=CARTESIAN_POINT('Ctrl Pts',(-0.1162591682289,-0.103344562661583,
2.02764927582197));
#20986=CARTESIAN_POINT('Ctrl Pts',(-0.116723205660322,-0.102820163682231,
2.02759904181125));
#20987=CARTESIAN_POINT('Ctrl Pts',(-0.118315558996756,-0.100996007108689,
2.02742481519868));
#20988=CARTESIAN_POINT('Ctrl Pts',(-0.119425794932187,-0.0996807103456938,
2.02730008422493));
#20989=CARTESIAN_POINT('Ctrl Pts',(-0.128250601605122,-0.0888668690956211,
2.02628133144113));
#20990=CARTESIAN_POINT('Ctrl Pts',(-0.134839949250607,-0.0785085994329739,
2.02534176834917));
#20991=CARTESIAN_POINT('Ctrl Pts',(-0.144172332924226,-0.0591288899052643,
2.0236736350441));
#20992=CARTESIAN_POINT('Ctrl Pts',(-0.147442357570033,-0.0504250050080329,
2.02295370601324));
#20993=CARTESIAN_POINT('Ctrl Pts',(-0.150149450267487,-0.0406411573268049,
2.02220710332032));
#20994=CARTESIAN_POINT('Ctrl Pts',(-0.15037466444079,-0.0397997672469219,
2.0221433980682));
#20995=CARTESIAN_POINT('Ctrl Pts',(-0.150684189515607,-0.0386032469044976,
2.02205355582785));
#20996=CARTESIAN_POINT('Ctrl Pts',(-0.150774330790832,-0.0382496643579215,
2.02202709937596));
#20997=CARTESIAN_POINT('Ctrl Pts',(-0.150927308030161,-0.0376406611782481,
2.02198169459924));
#20998=CARTESIAN_POINT('Ctrl Pts',(-0.150990741503492,-0.0373853937764408,
2.02196271220281));
#20999=CARTESIAN_POINT('Ctrl Pts',(-0.151112275946203,-0.0368909627182981,
2.02192604165093));
#21000=CARTESIAN_POINT('Ctrl Pts',(-0.151170456807011,-0.0366518220965108,
2.02190834879256));
#21001=CARTESIAN_POINT('Ctrl Pts',(-0.151325436000783,-0.0360081646349967,
2.02186084218308));
#21002=CARTESIAN_POINT('Ctrl Pts',(-0.151421180792036,-0.0356033919664265,
2.02183108850226));
#21003=CARTESIAN_POINT('Ctrl Pts',(-0.151767844169232,-0.0341111350924579,
2.02172182735174));
#21004=CARTESIAN_POINT('Ctrl Pts',(-0.152008688745958,-0.0330213082348758,
2.02164287205648));
#21005=CARTESIAN_POINT('Ctrl Pts',(-0.15442992732813,-0.0214767975179839,
2.02081443718909));
#21006=CARTESIAN_POINT('Ctrl Pts',(-0.155540202820391,-0.0108248506606018,
2.02011743063371));
#21007=CARTESIAN_POINT('Ctrl Pts',(-0.155560302101737,0.0112373727802485,
2.01866513464362));
#21008=CARTESIAN_POINT('Ctrl Pts',(-0.154322110730638,0.0225812930458725,
2.01791198472153));
#21009=CARTESIAN_POINT('Ctrl Pts',(-0.151636560304613,0.0346872309812885,
2.017043532115));
#21010=CARTESIAN_POINT('Ctrl Pts',(-0.151405004891444,0.035684377805913,
2.01697153646969));
#21011=CARTESIAN_POINT('Ctrl Pts',(-0.151020102685495,0.0372706528698454,
2.01685623147798));
#21012=CARTESIAN_POINT('Ctrl Pts',(-0.150873107501336,0.0378613047096332,
2.01681312567815));
#21013=CARTESIAN_POINT('Ctrl Pts',(-0.150607328735998,0.0389031191262123,
2.01673678304527));
#21014=CARTESIAN_POINT('Ctrl Pts',(-0.150489974184245,0.0393546415062859,
2.01670359257791));
#21015=CARTESIAN_POINT('Ctrl Pts',(-0.15024263460625,0.0402889968625491,
2.01663469185344));
#21016=CARTESIAN_POINT('Ctrl Pts',(-0.150112349265498,0.040771744000529,
2.0165989722337));
#21017=CARTESIAN_POINT('Ctrl Pts',(-0.149771074962268,0.0420124580669351,
2.01650685191165));
#21018=CARTESIAN_POINT('Ctrl Pts',(-0.149556660921137,0.0427694594317817,
2.01645034084643));
#21019=CARTESIAN_POINT('Ctrl Pts',(-0.148630377915502,0.0459475995510569,
2.01621177482298));
#21020=CARTESIAN_POINT('Ctrl Pts',(-0.147865423946665,0.0483527264690689,
2.01602800578432));
#21021=CARTESIAN_POINT('Ctrl Pts',(-0.145713541323103,0.0545890290017992,
2.01554265878334));
#21022=CARTESIAN_POINT('Ctrl Pts',(-0.144234082964366,0.0583859759634611,
2.01523822225201));
#21023=CARTESIAN_POINT('Ctrl Pts',(-0.13938954509522,0.0695074335783611,
2.01431977051335));
#21024=CARTESIAN_POINT('Ctrl Pts',(-0.135602763390633,0.0766328738180134,
2.01369489681868));
#21025=CARTESIAN_POINT('Ctrl Pts',(-0.128732118665179,0.0874439088646362,
2.01270179098782));
#21026=CARTESIAN_POINT('Ctrl Pts',(-0.125999973096993,0.0913367763181533,
2.01233409209679));
#21027=CARTESIAN_POINT('Ctrl Pts',(-0.12261310589936,0.0957206704723943,
2.01191213571528));
#21028=CARTESIAN_POINT('Ctrl Pts',(-0.122127775013948,0.0963391255181204,
2.01185241959857));
#21029=CARTESIAN_POINT('Ctrl Pts',(-0.119619790163518,0.0994856284254031,
2.0115477288606));
#21030=CARTESIAN_POINT('Ctrl Pts',(-0.117523064912813,0.101953997502343,
2.01130577849402));
#21031=CARTESIAN_POINT('Ctrl Pts',(-0.114982703484846,0.104762021570553,
2.01102872129042));
#21032=CARTESIAN_POINT('Ctrl Pts',(-0.11461262420535,0.105166770707655,
2.01098874083407));
#21033=CARTESIAN_POINT('Ctrl Pts',(-0.114014822348431,0.105813672377685,
2.01092477967614));
#21034=CARTESIAN_POINT('Ctrl Pts',(-0.113788455328879,0.106057062078243,
2.01090070090923));
#21035=CARTESIAN_POINT('Ctrl Pts',(-0.113384324958633,0.10648879952654,
2.01085796658071));
#21036=CARTESIAN_POINT('Ctrl Pts',(-0.113206869704387,0.106677430728051,
2.01083928799336));
#21037=CARTESIAN_POINT('Ctrl Pts',(-0.112827804047411,0.107078358440092,
2.01079957229733));
#21038=CARTESIAN_POINT('Ctrl Pts',(-0.112626065590584,0.107290528779731,
2.01077854535154));
#21039=CARTESIAN_POINT('Ctrl Pts',(-0.112075729295951,0.107866060231829,
2.01072147774326));
#21040=CARTESIAN_POINT('Ctrl Pts',(-0.111725960018593,0.108228304633786,
2.01068552608728));
#21041=CARTESIAN_POINT('Ctrl Pts',(-0.109924909567356,0.110075556614684,
2.01050198180508));
#21042=CARTESIAN_POINT('Ctrl Pts',(-0.108445668527572,0.111533187983041,
2.01035644954798));
#21043=CARTESIAN_POINT('Ctrl Pts',(-0.104006035602545,0.115736091994582,
2.00993306327408));
#21044=CARTESIAN_POINT('Ctrl Pts',(-0.100967307051048,0.118396396922867,
2.00966012666005));
#21045=CARTESIAN_POINT('Ctrl Pts',(-0.0897110258034188,0.127501920840473,
2.0086930532087));
#21046=CARTESIAN_POINT('Ctrl Pts',(-0.0809533057685513,0.133234309466336,
2.00801826008367));
#21047=CARTESIAN_POINT('Ctrl Pts',(-0.0690575512143196,0.139411751654174,
2.00712180705218));
#21048=CARTESIAN_POINT('Ctrl Pts',(-0.0663902784791855,0.140701465633334,
2.00692214555917));
#21049=CARTESIAN_POINT('Ctrl Pts',(-0.0636886213818939,0.141913924639106,
2.00672033358865));
#21050=CARTESIAN_POINT('Ctrl Pts',(-0.0636886415377083,0.141913915593508,
1.99275019838839));
#21051=CARTESIAN_POINT('Ctrl Pts',(-0.0659295067654324,0.140908251972531,
1.99291281988216));
#21052=CARTESIAN_POINT('Ctrl Pts',(-0.0681474586421175,0.139849106147085,
1.99307621311931));
#21053=CARTESIAN_POINT('Ctrl Pts',(-0.0760409509781415,0.135847058992824,
1.99366877675381));
#21054=CARTESIAN_POINT('Ctrl Pts',(-0.0815570810836566,0.132608729824859,
1.99410418843428));
#21055=CARTESIAN_POINT('Ctrl Pts',(-0.0877197972569616,0.128460573608094,
1.99462516695988));
#21056=CARTESIAN_POINT('Ctrl Pts',(-0.0885757879803293,0.127871855750594,
1.99469833746096));
#21057=CARTESIAN_POINT('Ctrl Pts',(-0.0898799526677652,0.126955522475936,
1.99481109878956));
#21058=CARTESIAN_POINT('Ctrl Pts',(-0.0903323895013006,0.126634000059944,
1.99485045751132));
#21059=CARTESIAN_POINT('Ctrl Pts',(-0.0911528169516215,0.126044332574184,
1.99492227244918));
#21060=CARTESIAN_POINT('Ctrl Pts',(-0.0915213711699218,0.125776978908624,
1.99495469797023));
#21061=CARTESIAN_POINT('Ctrl Pts',(-0.092321649304316,0.125191067702659,
1.99502546976428));
#21062=CARTESIAN_POINT('Ctrl Pts',(-0.0927529081027762,0.124871887900985,
1.99506383988522));
#21063=CARTESIAN_POINT('Ctrl Pts',(-0.0939251448602356,0.123994878451579,
1.99516877859051));
#21064=CARTESIAN_POINT('Ctrl Pts',(-0.0946627882311197,0.123432650357648,
1.99523551843242));
#21065=CARTESIAN_POINT('Ctrl Pts',(-0.0983201738720321,0.120592941957311,
1.99557002540584));
#21066=CARTESIAN_POINT('Ctrl Pts',(-0.101162728139163,0.118218494110107,
1.99584161487959));
#21067=CARTESIAN_POINT('Ctrl Pts',(-0.106137774128673,0.113751823680932,
1.99633903664036));
#21068=CARTESIAN_POINT('Ctrl Pts',(-0.108299950952198,0.111695224259176,
1.99656340298458));
#21069=CARTESIAN_POINT('Ctrl Pts',(-0.117750360549141,0.102173775519954,
1.99758138346462));
#21070=CARTESIAN_POINT('Ctrl Pts',(-0.124335348921754,0.0940495339662865,
1.99839750342246));
#21071=CARTESIAN_POINT('Ctrl Pts',(-0.132310083693187,0.0818945281708711,
1.99951703491615));
#21072=CARTESIAN_POINT('Ctrl Pts',(-0.1344264485133,0.0783722357780731,
1.99983059234704));
#21073=CARTESIAN_POINT('Ctrl Pts',(-0.137410555344571,0.0729284065147789,
2.00029512154242));
#21074=CARTESIAN_POINT('Ctrl Pts',(-0.138382735207229,0.07106639839316,
2.00045060351455));
#21075=CARTESIAN_POINT('Ctrl Pts',(-0.139541706178438,0.0687325981454354,
2.00064079708964));
#21076=CARTESIAN_POINT('Ctrl Pts',(-0.13976424258211,0.0682789449655296,
2.00067755127871));
#21077=CARTESIAN_POINT('Ctrl Pts',(-0.140112366600801,0.0675604405742558,
2.00073541291713));
#21078=CARTESIAN_POINT('Ctrl Pts',(-0.140239420301018,0.0672963104678515,
2.00075660906916));
#21079=CARTESIAN_POINT('Ctrl Pts',(-0.140477259860115,0.0667982705375294,
2.00079643410837));
#21080=CARTESIAN_POINT('Ctrl Pts',(-0.140588207116117,0.0665644462598389,
2.00081507248054));
#21081=CARTESIAN_POINT('Ctrl Pts',(-0.140839960601495,0.0660304318748239,
2.00085750625565));
#21082=CARTESIAN_POINT('Ctrl Pts',(-0.140980390860375,0.0657300679613546,
2.00088127832179));
#21083=CARTESIAN_POINT('Ctrl Pts',(-0.141349461711278,0.0649340444014101,
2.00094403294516));
#21084=CARTESIAN_POINT('Ctrl Pts',(-0.141576458335859,0.0644376203551805,
2.00098291700644));
#21085=CARTESIAN_POINT('Ctrl Pts',(-0.14311136559926,0.0610336301267154,
2.00124789887992));
#21086=CARTESIAN_POINT('Ctrl Pts',(-0.144332348369394,0.0580873819299934,
2.00146905772512));
#21087=CARTESIAN_POINT('Ctrl Pts',(-0.149151565430716,0.0453660745643028,
2.00239813675768));
#21088=CARTESIAN_POINT('Ctrl Pts',(-0.151854011060097,0.0352799077316714,
2.00307236675239));
#21089=CARTESIAN_POINT('Ctrl Pts',(-0.15487204992713,0.0167446394367718,
2.00431361254714));
#21090=CARTESIAN_POINT('Ctrl Pts',(-0.155548050857297,0.00839699159754889,
2.00487332405944));
#21091=CARTESIAN_POINT('Ctrl Pts',(-0.155550386707495,-0.00164427078440397,
2.00557165516019));
#21092=CARTESIAN_POINT('Ctrl Pts',(-0.155523545903709,-0.00332456260169045,
2.00568931425222));
#21093=CARTESIAN_POINT('Ctrl Pts',(-0.155447185702821,-0.00569698472505324,
2.00585671346099));
#21094=CARTESIAN_POINT('Ctrl Pts',(-0.15542024968967,-0.00638976808876266,
2.00590575005783));
#21095=CARTESIAN_POINT('Ctrl Pts',(-0.155369015268921,-0.00751386706984123,
2.00598557497369));
#21096=CARTESIAN_POINT('Ctrl Pts',(-0.155347549631766,-0.007945308081525,
2.00601627455787));
#21097=CARTESIAN_POINT('Ctrl Pts',(-0.155298910944775,-0.00884719239914593,
2.00608058128611));
#21098=CARTESIAN_POINT('Ctrl Pts',(-0.155271396753662,-0.00931761209518696,
2.00611419877615));
#21099=CARTESIAN_POINT('Ctrl Pts',(-0.155200977947752,-0.0104344956134807,
2.00619419707285));
#21100=CARTESIAN_POINT('Ctrl Pts',(-0.155156171393645,-0.0110808262140838,
2.00624063688124));
#21101=CARTESIAN_POINT('Ctrl Pts',(-0.15499233291652,-0.0132478660049204,
2.00639684259684));
#21102=CARTESIAN_POINT('Ctrl Pts',(-0.154854973906559,-0.0147670567423603,
2.00650717859744));
#21103=CARTESIAN_POINT('Ctrl Pts',(-0.153993412492537,-0.0229517811484808,
2.0071062994384));
#21104=CARTESIAN_POINT('Ctrl Pts',(-0.152861266896919,-0.0295662744533617,
2.00760771898174));
#21105=CARTESIAN_POINT('Ctrl Pts',(-0.148882868968545,-0.0462472926325519,
2.00891576340107));
#21106=CARTESIAN_POINT('Ctrl Pts',(-0.14544236669537,-0.0561374759163516,
2.00973461506975));
#21107=CARTESIAN_POINT('Ctrl Pts',(-0.140564199489494,-0.0666240533041674,
2.01062124352319));
#21108=CARTESIAN_POINT('Ctrl Pts',(-0.140080496477213,-0.0676351481426719,
2.01070690244764));
#21109=CARTESIAN_POINT('Ctrl Pts',(-0.138982764533249,-0.0698674585557329,
2.01089628655035));
#21110=CARTESIAN_POINT('Ctrl Pts',(-0.138363472299371,-0.0710860068342946,
2.01099984404389));
#21111=CARTESIAN_POINT('Ctrl Pts',(-0.136497972403392,-0.0746398817964052,
2.01130209409804));
#21112=CARTESIAN_POINT('Ctrl Pts',(-0.135208043454808,-0.0769519049034672,
2.01149902210868));
#21113=CARTESIAN_POINT('Ctrl Pts',(-0.133596917796872,-0.0796739109222784,
2.01173026854864));
#21114=CARTESIAN_POINT('Ctrl Pts',(-0.133331993312816,-0.0801164658845744,
2.01176784593683));
#21115=CARTESIAN_POINT('Ctrl Pts',(-0.132896011811974,-0.0808366182512552,
2.01182895191934));
#21116=CARTESIAN_POINT('Ctrl Pts',(-0.132726277524423,-0.0811150051817774,
2.01185256308669));
#21117=CARTESIAN_POINT('Ctrl Pts',(-0.132420803846081,-0.0816124968203796,
2.01189473601011));
#21118=CARTESIAN_POINT('Ctrl Pts',(-0.132285394682787,-0.0818317987438611,
2.01191331881083));
#21119=CARTESIAN_POINT('Ctrl Pts',(-0.131990981301701,-0.0823059754455963,
2.01195348175341));
#21120=CARTESIAN_POINT('Ctrl Pts',(-0.131831784095458,-0.082560725804757,
2.01197504891143));
#21121=CARTESIAN_POINT('Ctrl Pts',(-0.131385162524668,-0.0832708323799327,
2.01203514248444));
#21122=CARTESIAN_POINT('Ctrl Pts',(-0.131096106371519,-0.0837251657150525,
2.01207356325924));
#21123=CARTESIAN_POINT('Ctrl Pts',(-0.129407878379087,-0.0863485132256423,
2.0122953030524));
#21124=CARTESIAN_POINT('Ctrl Pts',(-0.127957146095269,-0.0884840979293851,
2.01247540146454));
#21125=CARTESIAN_POINT('Ctrl Pts',(-0.117882336006377,-0.102548566536947,
2.01366590282081));
#21126=CARTESIAN_POINT('Ctrl Pts',(-0.107655117128448,-0.113238416168053,
2.01459894161699));
#21127=CARTESIAN_POINT('Ctrl Pts',(-0.0946054956039685,-0.123487249446223,
2.01571369326784));
#21128=CARTESIAN_POINT('Ctrl Pts',(-0.0931139176140669,-0.124615803709299,
2.01584003214628));
#21129=CARTESIAN_POINT('Ctrl Pts',(-0.0883233405260521,-0.128106403820624,
2.01624313652608));
#21130=CARTESIAN_POINT('Ctrl Pts',(-0.0849523402498439,-0.130366246246945,
2.01652293427757));
#21131=CARTESIAN_POINT('Ctrl Pts',(-0.0807552845029284,-0.132947903467398,
2.01686885663126));
#21132=CARTESIAN_POINT('Ctrl Pts',(-0.0800096575520494,-0.133397959710826,
2.01693021839148));
#21133=CARTESIAN_POINT('Ctrl Pts',(-0.0787707053861322,-0.134131660107886,
2.0170320467989));
#21134=CARTESIAN_POINT('Ctrl Pts',(-0.0782795257203924,-0.134418905321041,
2.0170723825358));
#21135=CARTESIAN_POINT('Ctrl Pts',(-0.0773880969538388,-0.134933675965478,
2.01714553144304));
#21136=CARTESIAN_POINT('Ctrl Pts',(-0.0769883907661303,-0.135162132783489,
2.0171783105862));
#21137=CARTESIAN_POINT('Ctrl Pts',(-0.0761289369420461,-0.135648314579584,
2.01724875337051));
#21138=CARTESIAN_POINT('Ctrl Pts',(-0.0756688830354267,-0.135905483391047,
2.01728643642874));
#21139=CARTESIAN_POINT('Ctrl Pts',(-0.074411443319843,-0.136600024594322,
2.01738937399213));
#21140=CARTESIAN_POINT('Ctrl Pts',(-0.0736115254526333,-0.137032743792812,
2.01745479287816));
#21141=CARTESIAN_POINT('Ctrl Pts',(-0.0693768245629854,-0.139275746310099,
2.01780082568479));
#21142=CARTESIAN_POINT('Ctrl Pts',(-0.0658792464462353,-0.140963815223183,
2.01808567991663));
#21143=CARTESIAN_POINT('Ctrl Pts',(-0.048753792805651,-0.148452635883011,
2.01947755859141));
#21144=CARTESIAN_POINT('Ctrl Pts',(-0.0344081616866966,-0.152417350352893,
2.02064487763983));
#21145=CARTESIAN_POINT('Ctrl Pts',(-0.0153185102369249,-0.154857564493456,
2.02211552489108));
#21146=CARTESIAN_POINT('Ctrl Pts',(-0.0108910606314268,-0.155231813569472,
2.02245016133008));
#21147=CARTESIAN_POINT('Ctrl Pts',(-0.0057931781380897,-0.15544348797723,
2.02282389775578));
#21148=CARTESIAN_POINT('Ctrl Pts',(-0.00513298184586722,-0.155466689058483,
2.02287207477008));
#21149=CARTESIAN_POINT('Ctrl Pts',(-0.00414677422885363,-0.15549505793179,
2.02294368909488));
#21150=CARTESIAN_POINT('Ctrl Pts',(-0.00382087365323242,-0.155503407382418,
2.02296729710379));
#21151=CARTESIAN_POINT('Ctrl Pts',(-0.00323727622467037,-0.155516523139748,
2.0230094666264));
#21152=CARTESIAN_POINT('Ctrl Pts',(-0.00297959274270772,-0.155521673593919,
2.02302804917019));
#21153=CARTESIAN_POINT('Ctrl Pts',(-0.00242150752508936,-0.155531440742266,
2.02306821410918));
#21154=CARTESIAN_POINT('Ctrl Pts',(-0.00212110567102773,-0.155535827618446,
2.02308978350927));
#21155=CARTESIAN_POINT('Ctrl Pts',(-0.00128210490235176,-0.155545648669994,
2.02314988964436));
#21156=CARTESIAN_POINT('Ctrl Pts',(-0.000743480522906277,-0.155549155808656,
2.02318832066765));
#21157=CARTESIAN_POINT('Ctrl Pts',(0.00237865322313336,-0.155553267237506,
2.02341023810044));
#21158=CARTESIAN_POINT('Ctrl Pts',(0.00496203411082411,-0.155492306120507,
2.02359049786631));
#21159=CARTESIAN_POINT('Ctrl Pts',(0.0222427478418889,-0.154653346680389,
2.02478099672134));
#21160=CARTESIAN_POINT('Ctrl Pts',(0.0367683410044081,-0.151857156426241,
2.02571392410982));
#21161=CARTESIAN_POINT('Ctrl Pts',(0.0524565458918681,-0.146450064412463,
2.02682873158536));
#21162=CARTESIAN_POINT('Ctrl Pts',(0.0542160878541514,-0.145807839304556,
2.02695525247829));
#21163=CARTESIAN_POINT('Ctrl Pts',(0.0597462589502703,-0.143675409901083,
2.02735834430233));
#21164=CARTESIAN_POINT('Ctrl Pts',(0.0634701756898142,-0.142069598330497,
2.02763794011654));
#21165=CARTESIAN_POINT('Ctrl Pts',(0.067912342471643,-0.139944540441079,
2.0279836390518));
#21166=CARTESIAN_POINT('Ctrl Pts',(0.0686946310004803,-0.13956220217551,
2.02804498671529));
#21167=CARTESIAN_POINT('Ctrl Pts',(0.0699826999816077,-0.138919213582391,
2.02814679655859));
#21168=CARTESIAN_POINT('Ctrl Pts',(0.0704903413816263,-0.138662316277217,
2.0281871279123));
#21169=CARTESIAN_POINT('Ctrl Pts',(0.071406190636718,-0.13819251207748,
2.02826027213041));
#21170=CARTESIAN_POINT('Ctrl Pts',(0.0718148863433307,-0.137980565829659,
2.02829305098781));
#21171=CARTESIAN_POINT('Ctrl Pts',(0.0726894720928879,-0.137522074529898,
2.02836349677016));
#21172=CARTESIAN_POINT('Ctrl Pts',(0.0731550606901421,-0.13727497011088,
2.02840118312784));
#21173=CARTESIAN_POINT('Ctrl Pts',(0.0744207125545904,-0.136594976242711,
2.0285041389027));
#21174=CARTESIAN_POINT('Ctrl Pts',(0.0752182377442761,-0.136157433279345,
2.02856957279891));
#21175=CARTESIAN_POINT('Ctrl Pts',(0.079401847608405,-0.133814222606186,
2.02891582871522));
#21176=CARTESIAN_POINT('Ctrl Pts',(0.0827191925923217,-0.131789338564454,
2.02920089756358));
#21177=CARTESIAN_POINT('Ctrl Pts',(0.0982980443006547,-0.121460080779554,
2.0305928701092));
#21178=CARTESIAN_POINT('Ctrl Pts',(0.109406498338138,-0.111557733315848,
2.03176003242717));
#21179=CARTESIAN_POINT('Ctrl Pts',(0.121806201721761,-0.096844003671483,
2.03323042458583));
#21180=CARTESIAN_POINT('Ctrl Pts',(0.124520793115587,-0.0933278790597643,
2.0335649718279));
#21181=CARTESIAN_POINT('Ctrl Pts',(0.127462404890553,-0.0891603844616638,
2.03393862094529));
#21182=CARTESIAN_POINT('Ctrl Pts',(0.12783988429209,-0.0886182985843388,
2.03398679519217));
#21183=CARTESIAN_POINT('Ctrl Pts',(0.128398489373458,-0.0878051063402355,
2.03405840622056));
#21184=CARTESIAN_POINT('Ctrl Pts',(0.128582227877228,-0.0875358181102728,
2.03408201367779));
#21185=CARTESIAN_POINT('Ctrl Pts',(0.128909713173859,-0.0870525977554549,
2.03412418260647));
#21186=CARTESIAN_POINT('Ctrl Pts',(0.129053775439971,-0.0868388851538524,
2.03414276510544));
#21187=CARTESIAN_POINT('Ctrl Pts',(0.129364619923896,-0.0863752735065383,
2.0341829303934));
#21188=CARTESIAN_POINT('Ctrl Pts',(0.129531209083509,-0.0861252497175579,
2.0342045001853));
#21189=CARTESIAN_POINT('Ctrl Pts',(0.129994446390192,-0.0854256199753461,
2.03426460851578));
#21190=CARTESIAN_POINT('Ctrl Pts',(0.13028948905437,-0.0849749475159753,
2.03430304133015));
#21191=CARTESIAN_POINT('Ctrl Pts',(0.131986233785652,-0.0823535862488677,
2.03452498982694));
#21192=CARTESIAN_POINT('Ctrl Pts',(0.133336121663183,-0.0801496091288603,
2.03470527780933));
#21193=CARTESIAN_POINT('Ctrl Pts',(0.142002027821914,-0.0651752387698346,
2.03589577624097));
#21194=CARTESIAN_POINT('Ctrl Pts',(0.147529322219419,-0.051454796736749,
2.03682868415735));
#21195=CARTESIAN_POINT('Ctrl Pts',(0.151493585331642,-0.0353412780026672,
2.03794350148228));
#21196=CARTESIAN_POINT('Ctrl Pts',(0.151908232938729,-0.0335141866107135,
2.0380700542804));
#21197=CARTESIAN_POINT('Ctrl Pts',(0.153115356514492,-0.0277114093767737,
2.03847314391399));
#21198=CARTESIAN_POINT('Ctrl Pts',(0.15378542477098,-0.0237122930794578,
2.03875270434106));
#21199=CARTESIAN_POINT('Ctrl Pts',(0.154408745376138,-0.0188281690260305,
2.03909836412465));
#21200=CARTESIAN_POINT('Ctrl Pts',(0.154511714464416,-0.017963591954249,
2.03915970931702));
#21201=CARTESIAN_POINT('Ctrl Pts',(0.154669955749086,-0.0165327243716809,
2.03926151590604));
#21202=CARTESIAN_POINT('Ctrl Pts',(0.154729389912909,-0.0159669054030455,
2.03930184649137));
#21203=CARTESIAN_POINT('Ctrl Pts',(0.154831300044196,-0.0149426564381052,
2.03937498988753));
#21204=CARTESIAN_POINT('Ctrl Pts',(0.154874847585,-0.0144843374709726,2.03940776869491));
#21205=CARTESIAN_POINT('Ctrl Pts',(0.154963888522164,-0.0135008739957278,
2.03947821500318));
#21206=CARTESIAN_POINT('Ctrl Pts',(0.155008748383423,-0.0129756794247699,
2.03951590193954));
#21207=CARTESIAN_POINT('Ctrl Pts',(0.155123750300299,-0.0115434895315819,
2.03961886090853));
#21208=CARTESIAN_POINT('Ctrl Pts',(0.155188605578905,-0.0106361031847316,
2.03968429743742));
#21209=CARTESIAN_POINT('Ctrl Pts',(0.155488530187161,-0.00584982621565138,
2.04003059250408));
#21210=CARTESIAN_POINT('Ctrl Pts',(0.155586120954347,-0.00196404125308456,
2.04031569901426));
#21211=CARTESIAN_POINT('Ctrl Pts',(0.155355274765412,0.0167267659171037,
2.04170768804703));
#21212=CARTESIAN_POINT('Ctrl Pts',(0.153059088353099,0.0314295179295453,
2.04287482287781));
#21213=CARTESIAN_POINT('Ctrl Pts',(0.14742072770436,0.049826088298067,2.04434517027508));
#21214=CARTESIAN_POINT('Ctrl Pts',(0.145938587913794,0.0540134028880944,
2.04467970185316));
#21215=CARTESIAN_POINT('Ctrl Pts',(0.144032292147096,0.0587446816994504,
2.04505333563792));
#21216=CARTESIAN_POINT('Ctrl Pts',(0.143781530833612,0.0593557936702136,
2.04510150939863));
#21217=CARTESIAN_POINT('Ctrl Pts',(0.14340120603529,0.060266100583725,2.04517311984791));
#21218=CARTESIAN_POINT('Ctrl Pts',(0.143274586949353,0.060566504866436,
2.04519672720823));
#21219=CARTESIAN_POINT('Ctrl Pts',(0.143046172096064,0.0611036952659292,
2.04523889603256));
#21220=CARTESIAN_POINT('Ctrl Pts',(0.142944731838423,0.0613406273986872,
2.04525747852366));
#21221=CARTESIAN_POINT('Ctrl Pts',(0.14272376745547,0.0618532049718055,
2.04529764387293));
#21222=CARTESIAN_POINT('Ctrl Pts',(0.142604033824519,0.0621287558470869,
2.04531921373367));
#21223=CARTESIAN_POINT('Ctrl Pts',(0.142267403643778,0.0628973648551534,
2.04537932244987));
#21224=CARTESIAN_POINT('Ctrl Pts',(0.142048740364277,0.0633896523820206,
2.04541775557892));
#21225=CARTESIAN_POINT('Ctrl Pts',(0.140766338828488,0.0662368274106565,
2.04563970953407));
#21226=CARTESIAN_POINT('Ctrl Pts',(0.139646530920521,0.0685662304735617,
2.04582000247452));
#21227=CARTESIAN_POINT('Ctrl Pts',(0.131764316718353,0.0839675578371414,
2.04701050083198));
#21228=CARTESIAN_POINT('Ctrl Pts',(0.123233717778808,0.0960517886135503,
2.04794340532696));
#21229=CARTESIAN_POINT('Ctrl Pts',(0.111844816772437,0.10812053272599,2.04905822438335));
#21230=CARTESIAN_POINT('Ctrl Pts',(0.110534485942555,0.10945976276432,2.04918478278833));
#21231=CARTESIAN_POINT('Ctrl Pts',(0.10631357635864,0.113620673047407,2.04958787203721));
#21232=CARTESIAN_POINT('Ctrl Pts',(0.103316939964868,0.116352219073762,
2.04986742624574));
#21233=CARTESIAN_POINT('Ctrl Pts',(0.0995513782355839,0.119524406202461,
2.05021307914925));
#21234=CARTESIAN_POINT('Ctrl Pts',(0.0988808017010345,0.120079755107775,
2.05027442390733));
#21235=CARTESIAN_POINT('Ctrl Pts',(0.0977644013866712,0.120988627589063,
2.05037622992446));
#21236=CARTESIAN_POINT('Ctrl Pts',(0.0973212306734331,0.121345392285756,
2.05041656037475));
#21237=CARTESIAN_POINT('Ctrl Pts',(0.09651592023044,0.121986440216716,2.05048970362646));
#21238=CARTESIAN_POINT('Ctrl Pts',(0.0961544548621177,0.122271563564431,
2.05052248242505));
#21239=CARTESIAN_POINT('Ctrl Pts',(0.0953764311930852,0.122879683914416,
2.05059292882575));
#21240=CARTESIAN_POINT('Ctrl Pts',(0.0949594872700195,0.123202175755229,
2.05063061586382));
#21241=CARTESIAN_POINT('Ctrl Pts',(0.0938185158527525,0.124075445405476,
2.05073357539418));
#21242=CARTESIAN_POINT('Ctrl Pts',(0.0930912928756452,0.124621993222729,
2.05079901238577));
#21243=CARTESIAN_POINT('Ctrl Pts',(0.0892324214041446,0.127469522413765,
2.05114531433386));
#21244=CARTESIAN_POINT('Ctrl Pts',(0.0860204253786639,0.129658727421358,
2.05143042746388));
#21245=CARTESIAN_POINT('Ctrl Pts',(0.0701911626035577,0.139600304146264,
2.05282241939508));
#21246=CARTESIAN_POINT('Ctrl Pts',(0.0565927783511996,0.145643931207016,
2.05398954939497));
#21247=CARTESIAN_POINT('Ctrl Pts',(0.0380785072864503,0.150882527151424,
2.05545988892454));
#21248=CARTESIAN_POINT('Ctrl Pts',(0.0337566275612232,0.15190789615462,
2.0557944177489));
#21249=CARTESIAN_POINT('Ctrl Pts',(0.0287477011328726,0.15287186950894,
2.05616804883819));
#21250=CARTESIAN_POINT('Ctrl Pts',(0.0280982637039318,0.152992569840399,
2.05621622251342));
#21251=CARTESIAN_POINT('Ctrl Pts',(0.0271271835369517,0.153166656571019,
2.0562878328609));
#21252=CARTESIAN_POINT('Ctrl Pts',(0.0268061213803905,0.153223172639232,
2.05631144020418));
#21253=CARTESIAN_POINT('Ctrl Pts',(0.026230909977021,0.153322562880539,
2.05635360901016));
#21254=CARTESIAN_POINT('Ctrl Pts',(0.0259768308311037,0.15336581493275,
2.05637219149988));
#21255=CARTESIAN_POINT('Ctrl Pts',(0.0254263389596023,0.153458118225076,
2.05641235685994));
#21256=CARTESIAN_POINT('Ctrl Pts',(0.0251298920779448,0.153506942156976,
2.05643392673278));
#21257=CARTESIAN_POINT('Ctrl Pts',(0.0243368569494294,0.15363519387694,
2.05649147407643));
#21258=CARTESIAN_POINT('Ctrl Pts',(0.0238400161101844,0.153713073791213,
2.05652736551064));
#21259=CARTESIAN_POINT('Ctrl Pts',(0.0214381625993784,0.154077639172716,
2.05670012900236));
#21260=CARTESIAN_POINT('Ctrl Pts',(0.0195282040905837,0.154331344407538,
2.05683525062925));
#21261=CARTESIAN_POINT('Ctrl Pts',(0.0139052288375949,0.154972191310408,
2.05722774966487));
#21262=CARTESIAN_POINT('Ctrl Pts',(0.0101822269931536,0.155261270864672,
2.05748087595686));
#21263=CARTESIAN_POINT('Ctrl Pts',(-0.0064612414746064,0.155952229438248,
2.0585966452661));
#21264=CARTESIAN_POINT('Ctrl Pts',(-0.0193909164158658,0.154876907379754,
2.05942540401926));
#21265=CARTESIAN_POINT('Ctrl Pts',(-0.0365441258256776,0.151266403135661,
2.06061245465308));
#21266=CARTESIAN_POINT('Ctrl Pts',(-0.0410045087006287,0.150118690166007,
2.06092896682679));
#21267=CARTESIAN_POINT('Ctrl Pts',(-0.0462744250105808,0.148510277117373,
2.06131555053908));
#21268=CARTESIAN_POINT('Ctrl Pts',(-0.0471393986116943,0.148237990596818,
2.06137941314836));
#21269=CARTESIAN_POINT('Ctrl Pts',(-0.0485536802457966,0.147779156548596,
2.06148453169087));
#21270=CARTESIAN_POINT('Ctrl Pts',(-0.0491044220376613,0.147597068722404,
2.06152564140436));
#21271=CARTESIAN_POINT('Ctrl Pts',(-0.0500913224121013,0.147264641876094,
2.06159962874611));
#21272=CARTESIAN_POINT('Ctrl Pts',(-0.0505278573796326,0.147115434092107,
2.06163246878474));
#21273=CARTESIAN_POINT('Ctrl Pts',(-0.0514546152084873,0.146794056530645,
2.06170243226568));
#21274=CARTESIAN_POINT('Ctrl Pts',(-0.0519446509788728,0.146621368434372,
2.06173957251182));
#21275=CARTESIAN_POINT('Ctrl Pts',(-0.0532121363793322,0.146167556242658,
2.06183602088373));
#21276=CARTESIAN_POINT('Ctrl Pts',(-0.0539882175663857,0.145882686673219,
2.06189545267534));
#21277=CARTESIAN_POINT('Ctrl Pts',(-0.0576593850086255,0.144501835577831,
2.06217841341757));
#21278=CARTESIAN_POINT('Ctrl Pts',(-0.0605234069515121,0.143325851918236,
2.06240459257798));
#21279=CARTESIAN_POINT('Ctrl Pts',(-0.0634631113378447,0.142014968460715,
2.06264267791307));
#21280=CARTESIAN_POINT('Ctrl Pts',(-0.0635758997156846,0.141964512262164,
2.06265182176443));
#21281=CARTESIAN_POINT('Ctrl Pts',(-0.0636886258537358,0.141913922632217,
2.0626609697501));
#21282=CARTESIAN_POINT('Origin',(0.,0.,-0.129405622560373));
#21283=CARTESIAN_POINT('',(-0.0637081998868885,0.141956949220952,2.1466152095062));
#21284=CARTESIAN_POINT('',(-0.0636886258331689,0.141913922641447,2.13289020897179));
#21285=CARTESIAN_POINT('',(-0.0636886258329924,0.141913922641526,-0.129405622560373));
#21286=CARTESIAN_POINT('',(-0.155776797124186,5.07126225089676E-5,2.08940161016563));
#21287=CARTESIAN_POINT('Ctrl Pts',(-0.155783920579557,5.0990988608356E-5,
2.08940569613714));
#21288=CARTESIAN_POINT('Ctrl Pts',(-0.15557194890439,-0.0485975948926043,
2.09290471482211));
#21289=CARTESIAN_POINT('Ctrl Pts',(-0.104875675767394,-0.14913732793219,
2.100108637801));
#21290=CARTESIAN_POINT('Ctrl Pts',(0.0663275338242693,-0.17147627599867,
2.11101746507382));
#21291=CARTESIAN_POINT('Ctrl Pts',(0.180042327710072,-0.0372587603217594,
2.1221321779556));
#21292=CARTESIAN_POINT('Ctrl Pts',(0.128937250118005,0.131067312760423,
2.13324689083737));
#21293=CARTESIAN_POINT('Ctrl Pts',(0.00474514346942996,0.16656140244008,
2.14140790135424));
#21294=CARTESIAN_POINT('Ctrl Pts',(-0.054193003884981,0.146343230460563,
2.14586400757718));
#21295=CARTESIAN_POINT('Ctrl Pts',(-0.0637081998868965,0.141956949220948,
2.1466152095062));
#21296=CARTESIAN_POINT('Ctrl Pts',(-0.155549994370291,4.18497610693008E-5,
2.08927151745862));
#21297=CARTESIAN_POINT('Ctrl Pts',(-0.155549667422381,0.00125707164660975,
2.08918069722845));
#21298=CARTESIAN_POINT('Ctrl Pts',(-0.155535099726752,0.00247229902528903,
2.08909044289044));
#21299=CARTESIAN_POINT('Ctrl Pts',(-0.155487197254807,0.0044925239884509,
2.08894147324318));
#21300=CARTESIAN_POINT('Ctrl Pts',(-0.155461848926162,0.00529762994950571,
2.0888823885966));
#21301=CARTESIAN_POINT('Ctrl Pts',(-0.155416323820299,0.00645714646472965,
2.08879773638013));
#21302=CARTESIAN_POINT('Ctrl Pts',(-0.155401186846902,0.00681172397177014,
2.08877190946493));
#21303=CARTESIAN_POINT('Ctrl Pts',(-0.155372759727773,0.0074281052750826,
2.08872712019409));
#21304=CARTESIAN_POINT('Ctrl Pts',(-0.155360021166545,0.00768993103216972,
2.08870812825469));
#21305=CARTESIAN_POINT('Ctrl Pts',(-0.155334173705052,0.00819489257441228,
2.08867156647934));
#21306=CARTESIAN_POINT('Ctrl Pts',(-0.155321155649488,0.0084380326972423,
2.08865399161486));
#21307=CARTESIAN_POINT('Ctrl Pts',(-0.155294049603464,0.00892296575729506,
2.08861899979675));
#21308=CARTESIAN_POINT('Ctrl Pts',(-0.15527996775943,0.00916475722462516,
2.08860158251635));
#21309=CARTESIAN_POINT('Ctrl Pts',(-0.15524139928141,0.00980137405827636,
2.08855580070547));
#21310=CARTESIAN_POINT('Ctrl Pts',(-0.155215970947152,0.0101961441979767,
2.08852748855982));
#21311=CARTESIAN_POINT('Ctrl Pts',(-0.155121717123465,0.0115772612053776,
2.08842869499331));
#21312=CARTESIAN_POINT('Ctrl Pts',(-0.155044991624251,0.0125630731462905,
2.08835863795071));
#21313=CARTESIAN_POINT('Ctrl Pts',(-0.154797284725753,0.015396261847019,
2.08815844470379));
#21314=CARTESIAN_POINT('Ctrl Pts',(-0.154602641749619,0.0172414659348747,
2.08802946853944));
#21315=CARTESIAN_POINT('Ctrl Pts',(-0.152703259559245,0.0326069517581584,
2.08696386984621));
#21316=CARTESIAN_POINT('Ctrl Pts',(-0.149261473173037,0.0458541611473487,
2.08609517361747));
#21317=CARTESIAN_POINT('Ctrl Pts',(-0.14178908789031,0.064270062858469,
2.08476817861712));
#21318=CARTESIAN_POINT('Ctrl Pts',(-0.139095611857409,0.0699083838310649,
2.0843446765939));
#21319=CARTESIAN_POINT('Ctrl Pts',(-0.135359427929713,0.0766536622101196,
2.08380689327797));
#21320=CARTESIAN_POINT('Ctrl Pts',(-0.134629814998468,0.0779279880041747,
2.08370387195097));
#21321=CARTESIAN_POINT('Ctrl Pts',(-0.13355740004296,0.0797410223268643,
2.08355514833553));
#21322=CARTESIAN_POINT('Ctrl Pts',(-0.133229135137427,0.0802882760841422,
2.08350997155228));
#21323=CARTESIAN_POINT('Ctrl Pts',(-0.132653468078079,0.0812347244586077,
2.0834313352329));
#21324=CARTESIAN_POINT('Ctrl Pts',(-0.132407606395193,0.0816348504675293,
2.08339793225569));
#21325=CARTESIAN_POINT('Ctrl Pts',(-0.131930864100402,0.0824029020741967,
2.08333350578081));
#21326=CARTESIAN_POINT('Ctrl Pts',(-0.131700246588257,0.0827709865476328,
2.08330249219319));
#21327=CARTESIAN_POINT('Ctrl Pts',(-0.131090891279738,0.0837345734365021,
2.08322093832683));
#21328=CARTESIAN_POINT('Ctrl Pts',(-0.130709640908966,0.0843284667720374,
2.08317030541721));
#21329=CARTESIAN_POINT('Ctrl Pts',(-0.129366936103868,0.086389084987543,
2.08299332010484));
#21330=CARTESIAN_POINT('Ctrl Pts',(-0.128384761404647,0.0878420783737397,
2.0828661979083));
#21331=CARTESIAN_POINT('Ctrl Pts',(-0.120968342248256,0.0984235154968745,
2.081922713478));
#21332=CARTESIAN_POINT('Ctrl Pts',(-0.113593465199103,0.106850154702385,
2.08106913137985));
#21333=CARTESIAN_POINT('Ctrl Pts',(-0.0997225357481578,0.119626178768407,
2.07960761393809));
#21334=CARTESIAN_POINT('Ctrl Pts',(-0.093683674696811,0.124412175682198,
2.0790087202848));
#21335=CARTESIAN_POINT('Ctrl Pts',(-0.0856198574553641,0.129881632577302,
2.078272334449));
#21336=CARTESIAN_POINT('Ctrl Pts',(-0.0839019677366231,0.130997935995013,
2.07811885972282));
#21337=CARTESIAN_POINT('Ctrl Pts',(-0.0814287803910966,0.132536420486931,
2.07790319989135));
#21338=CARTESIAN_POINT('Ctrl Pts',(-0.0806913152668629,0.132986693914689,
2.07783954779368));
#21339=CARTESIAN_POINT('Ctrl Pts',(-0.079549918183988,0.133670605129244,
2.07774207794944));
#21340=CARTESIAN_POINT('Ctrl Pts',(-0.0791486373653939,0.13390860083106,
2.07770800760455));
#21341=CARTESIAN_POINT('Ctrl Pts',(-0.0784815167610447,0.134300217000108,
2.07765169995903));
#21342=CARTESIAN_POINT('Ctrl Pts',(-0.0782162857530849,0.134454860108218,
2.07762940028624));
#21343=CARTESIAN_POINT('Ctrl Pts',(-0.0777015914167277,0.13475291457641,
2.07758629720714));
#21344=CARTESIAN_POINT('Ctrl Pts',(-0.0774521848476985,0.134896420862542,
2.07756548786014));
#21345=CARTESIAN_POINT('Ctrl Pts',(-0.0769845126051193,0.135163790633825,
2.07752661377717));
#21346=CARTESIAN_POINT('Ctrl Pts',(-0.0767663479963998,0.135287816510729,
2.0775085390124));
#21347=CARTESIAN_POINT('Ctrl Pts',(-0.0762599613568219,0.135574076361242,
2.07746672205635));
#21348=CARTESIAN_POINT('Ctrl Pts',(-0.0759715215812175,0.135735919348897,
2.07744300507754));
#21349=CARTESIAN_POINT('Ctrl Pts',(-0.0750848941308739,0.136229692694543,
2.0773704078891));
#21350=CARTESIAN_POINT('Ctrl Pts',(-0.0744850200810121,0.136558604005474,
2.07732171573094));
#21351=CARTESIAN_POINT('Ctrl Pts',(-0.0705471595416633,0.138684066591484,
2.07700471927045));
#21352=CARTESIAN_POINT('Ctrl Pts',(-0.0671467602577074,0.140361969007692,
2.07674333761002));
#21353=CARTESIAN_POINT('Ctrl Pts',(-0.0636886254669799,0.141913922805787,
2.07648623881325));
#21354=CARTESIAN_POINT('',(-0.155549927754303,-0.000143266912413758,2.07557283338354));
#21355=CARTESIAN_POINT('Ctrl Pts',(-0.0636886258537358,0.141913922632217,
2.0626609697501));
#21356=CARTESIAN_POINT('Ctrl Pts',(-0.0685588818197047,0.139728232149738,
2.06305620223627));
#21357=CARTESIAN_POINT('Ctrl Pts',(-0.0733129487900478,0.137293486104077,
2.06345934329278));
#21358=CARTESIAN_POINT('Ctrl Pts',(-0.0840535706708943,0.131075666014453,
2.06440954394235));
#21359=CARTESIAN_POINT('Ctrl Pts',(-0.0899259662053769,0.127118625302212,
2.06495990848433));
#21360=CARTESIAN_POINT('Ctrl Pts',(-0.101448404136603,0.118155233102281,
2.06608987339327));
#21361=CARTESIAN_POINT('Ctrl Pts',(-0.107046118013571,0.113108788840649,
2.06666762379429));
#21362=CARTESIAN_POINT('Ctrl Pts',(-0.112744221473667,0.107168271130109,
2.06727110957734));
#21363=CARTESIAN_POINT('Ctrl Pts',(-0.11322796123183,0.106657051611768,
2.0673224704545));
#21364=CARTESIAN_POINT('Ctrl Pts',(-0.113936490514527,0.105898019483298,
2.06739786533489));
#21365=CARTESIAN_POINT('Ctrl Pts',(-0.114163967794944,0.105652746600751,
2.06742209704434));
#21366=CARTESIAN_POINT('Ctrl Pts',(-0.114565835517278,0.105216627311411,
2.0674649482667));
#21367=CARTESIAN_POINT('Ctrl Pts',(-0.114740542899674,0.105026078426222,
2.06748359167589));
#21368=CARTESIAN_POINT('Ctrl Pts',(-0.115113387008802,0.104617386087745,
2.06752340878616));
#21369=CARTESIAN_POINT('Ctrl Pts',(-0.115311378661106,0.104399115397032,
2.06754457157719));
#21370=CARTESIAN_POINT('Ctrl Pts',(-0.115716231343181,0.10395023939792,
2.06758788693527));
#21371=CARTESIAN_POINT('Ctrl Pts',(-0.115923026338546,0.103719575954074,
2.06761003458226));
#21372=CARTESIAN_POINT('Ctrl Pts',(-0.116865634850867,0.102661830138502,
2.06771109961662));
#21373=CARTESIAN_POINT('Ctrl Pts',(-0.117593320919101,0.101827496474286,
2.06778943505141));
#21374=CARTESIAN_POINT('Ctrl Pts',(-0.122812129741725,0.0957132676506731,
2.06835416885508));
#21375=CARTESIAN_POINT('Ctrl Pts',(-0.126955419458914,0.0901454231054279,
2.06881868869512));
#21376=CARTESIAN_POINT('Ctrl Pts',(-0.133764039990031,0.0795904912136084,
2.06965031120051));
#21377=CARTESIAN_POINT('Ctrl Pts',(-0.13655542240652,0.0746999502341629,
2.07001864757813));
#21378=CARTESIAN_POINT('Ctrl Pts',(-0.14332004812707,0.0611961442370621,
2.07101607980847));
#21379=CARTESIAN_POINT('Ctrl Pts',(-0.146780621986319,0.0523546662277312,
2.07165020659328));
#21380=CARTESIAN_POINT('Ctrl Pts',(-0.14973357521524,0.0421541275072256,
2.07239371170773));
#21381=CARTESIAN_POINT('Ctrl Pts',(-0.150039861562512,0.0410506252184793,
2.07247427047709));
#21382=CARTESIAN_POINT('Ctrl Pts',(-0.150484115587405,0.0393786175391289,
2.07259656625316));
#21383=CARTESIAN_POINT('Ctrl Pts',(-0.150631111899754,0.0388125324389542,
2.07263801175104));
#21384=CARTESIAN_POINT('Ctrl Pts',(-0.150888460275398,0.0377979937996901,
2.07271236869379));
#21385=CARTESIAN_POINT('Ctrl Pts',(-0.151000014855141,0.0373498498642456,
2.0727452410034));
#21386=CARTESIAN_POINT('Ctrl Pts',(-0.151232133818903,0.0363993285303847,
2.07281502470274));
#21387=CARTESIAN_POINT('Ctrl Pts',(-0.151352194035988,0.0358968350344211,
2.07285195184643));
#21388=CARTESIAN_POINT('Ctrl Pts',(-0.151591387263,0.0348731930303727,2.07292725423219));
#21389=CARTESIAN_POINT('Ctrl Pts',(-0.151710341314558,0.0343520102677563,
2.07296563467547));
#21390=CARTESIAN_POINT('Ctrl Pts',(-0.15199981373053,0.0330528877576283,
2.07306140929058));
#21391=CARTESIAN_POINT('Ctrl Pts',(-0.1521670469016,0.0322742398297517,
2.07311890752159));
#21392=CARTESIAN_POINT('Ctrl Pts',(-0.154480728380849,0.0210836902572564,
2.07394669144845));
#21393=CARTESIAN_POINT('Ctrl Pts',(-0.155559724762432,0.0104824683348447,
2.07475164736192));
#21394=CARTESIAN_POINT('Ctrl Pts',(-0.155549933968261,-0.000143326444609621,
2.07557282710847));
#21395=CARTESIAN_POINT('Ctrl Pts',(-0.155549934022329,-0.000143267753619253,
2.07557282257272));
#21396=CARTESIAN_POINT('Ctrl Pts',(-0.155539275057488,-0.0117160134402106,
2.0764671842731));
#21397=CARTESIAN_POINT('Ctrl Pts',(-0.154237185185774,-0.023252640275882,
2.07737557437259));
#21398=CARTESIAN_POINT('Ctrl Pts',(-0.151510568590532,-0.0352256410899354,
2.07828126275613));
#21399=CARTESIAN_POINT('Ctrl Pts',(-0.151349575070947,-0.0359110617876846,
2.07833296763677));
#21400=CARTESIAN_POINT('Ctrl Pts',(-0.151088863884984,-0.0369881195800717,
2.07841396545394));
#21401=CARTESIAN_POINT('Ctrl Pts',(-0.150992266990084,-0.037380490887096,
2.07844342042423));
#21402=CARTESIAN_POINT('Ctrl Pts',(-0.150806355107479,-0.0381231746751705,
2.07849906788549));
#21403=CARTESIAN_POINT('Ctrl Pts',(-0.150717345967773,-0.038473560008412,
2.078525276927));
#21404=CARTESIAN_POINT('Ctrl Pts',(-0.150561628668209,-0.0390777086561489,
2.0785703871));
#21405=CARTESIAN_POINT('Ctrl Pts',(-0.150495498861823,-0.0393316179150293,
2.07858932118145));
#21406=CARTESIAN_POINT('Ctrl Pts',(-0.150365886775339,-0.039824158068148,
2.07862600085319));
#21407=CARTESIAN_POINT('Ctrl Pts',(-0.150302478798175,-0.0400628049570566,
2.07864375074015));
#21408=CARTESIAN_POINT('Ctrl Pts',(-0.150129596860551,-0.0407072884352145,
2.0786916280179));
#21409=CARTESIAN_POINT('Ctrl Pts',(-0.150019044614443,-0.0411128380111044,
2.07872169361249));
#21410=CARTESIAN_POINT('Ctrl Pts',(-0.149601090166072,-0.0426219261966321,
2.07883335744952));
#21411=CARTESIAN_POINT('Ctrl Pts',(-0.149283134209527,-0.0437225435885582,
2.07891437154914));
#21412=CARTESIAN_POINT('Ctrl Pts',(-0.146088489028586,-0.0543395994523739,
2.07969265742224));
#21413=CARTESIAN_POINT('Ctrl Pts',(-0.142317370091986,-0.0635646861446651,
2.08034470014211));
#21414=CARTESIAN_POINT('Ctrl Pts',(-0.135336273678805,-0.076847281847116,
2.08133224390421));
#21415=CARTESIAN_POINT('Ctrl Pts',(-0.132764773239527,-0.0812091379441312,
2.0816651354955));
#21416=CARTESIAN_POINT('Ctrl Pts',(-0.126501829414894,-0.090737603622008,
2.0824254833909));
#21417=CARTESIAN_POINT('Ctrl Pts',(-0.122697859816682,-0.0958188150260091,
2.08285494143391));
#21418=CARTESIAN_POINT('Ctrl Pts',(-0.117582891959365,-0.101845526724964,
2.08340551780044));
#21419=CARTESIAN_POINT('Ctrl Pts',(-0.116553137326716,-0.103022393990375,
2.08351512443418));
#21420=CARTESIAN_POINT('Ctrl Pts',(-0.11516323704072,-0.104563344426577,
2.08366155945504));
#21421=CARTESIAN_POINT('Ctrl Pts',(-0.114818758889329,-0.104941492076381,
2.08369773297364));
#21422=CARTESIAN_POINT('Ctrl Pts',(-0.114133435236436,-0.105686385761821,
2.08376946820248));
#21423=CARTESIAN_POINT('Ctrl Pts',(-0.113792671706578,-0.106053199053403,
2.08380502618964));
#21424=CARTESIAN_POINT('Ctrl Pts',(-0.113131290684871,-0.106758282050102,
2.08387383096205));
#21425=CARTESIAN_POINT('Ctrl Pts',(-0.112810911656775,-0.107096768955875,
2.08390706730585));
#21426=CARTESIAN_POINT('Ctrl Pts',(-0.112070095386993,-0.107872443742654,
2.08398370995093));
#21427=CARTESIAN_POINT('Ctrl Pts',(-0.111648614895726,-0.108308620024616,
2.08402716114621));
#21428=CARTESIAN_POINT('Ctrl Pts',(-0.110513822882038,-0.109469316190258,
2.08414374780094));
#21429=CARTESIAN_POINT('Ctrl Pts',(-0.109795951459124,-0.110189315212772,
2.08421708223764));
#21430=CARTESIAN_POINT('Ctrl Pts',(-0.103796682457949,-0.116089529518788,
2.08482661157651));
#21431=CARTESIAN_POINT('Ctrl Pts',(-0.0981598405173183,-0.120893107614842,
2.08537893165665));
#21432=CARTESIAN_POINT('Ctrl Pts',(-0.0838711187023698,-0.131409576367771,
2.08673283586956));
#21433=CARTESIAN_POINT('Ctrl Pts',(-0.0749483327620099,-0.136695163080771,
2.08754373776629));
#21434=CARTESIAN_POINT('Ctrl Pts',(-0.0624525077612218,-0.142503632708605,
2.08860014208909));
#21435=CARTESIAN_POINT('Ctrl Pts',(-0.0592903211807623,-0.14384805334556,
2.08886100106461));
#21436=CARTESIAN_POINT('Ctrl Pts',(-0.0543550133917548,-0.145755888490614,
2.08925580564902));
#21437=CARTESIAN_POINT('Ctrl Pts',(-0.0526120985105431,-0.146394038251702,
2.08939292288103));
#21438=CARTESIAN_POINT('Ctrl Pts',(-0.0504005275819003,-0.147159178205275,
2.08956366271858));
#21439=CARTESIAN_POINT('Ctrl Pts',(-0.0499422327641749,-0.147315343104484,
2.08959887022755));
#21440=CARTESIAN_POINT('Ctrl Pts',(-0.0492076949578372,-0.147561816575549,
2.08965501292125));
#21441=CARTESIAN_POINT('Ctrl Pts',(-0.0489319202078071,-0.14765349349984,
2.08967602670699));
#21442=CARTESIAN_POINT('Ctrl Pts',(-0.0484095487962619,-0.147825523334772,
2.089715707014));
#21443=CARTESIAN_POINT('Ctrl Pts',(-0.0481630112734116,-0.147906031351704,
2.08973438208562));
#21444=CARTESIAN_POINT('Ctrl Pts',(-0.047596787497356,-0.148089368586787,
2.08977715474778));
#21445=CARTESIAN_POINT('Ctrl Pts',(-0.0472769688221497,-0.148191779438817,
2.08980122763603));
#21446=CARTESIAN_POINT('Ctrl Pts',(-0.0464226934864937,-0.148462284510505,
2.08986530566505));
#21447=CARTESIAN_POINT('Ctrl Pts',(-0.0458876493650725,-0.148628530416703,
2.08990520555735));
#21448=CARTESIAN_POINT('Ctrl Pts',(-0.0420192689448587,-0.149807611241837,
2.09019208323064));
#21449=CARTESIAN_POINT('Ctrl Pts',(-0.0386533127484973,-0.150711199165969,
2.09043315313171));
#21450=CARTESIAN_POINT('Ctrl Pts',(-0.0351738451268169,-0.151520991477027,
2.09067637808321));
#21451=CARTESIAN_POINT('Ctrl Pts',(-0.0350881453331679,-0.151540860154363,
2.09068236506112));
#21452=CARTESIAN_POINT('Ctrl Pts',(-0.0330029247003192,-0.152022434911937,
2.09082794965413));
#21453=CARTESIAN_POINT('Ctrl Pts',(-0.0309944023124441,-0.15244461751603,
2.09096619755381));
#21454=CARTESIAN_POINT('Ctrl Pts',(-0.0178296593580188,-0.154940829624849,
2.09186285370095));
#21455=CARTESIAN_POINT('Ctrl Pts',(-0.00648343222484846,-0.155828551932417,
2.09259400605833));
#21456=CARTESIAN_POINT('Ctrl Pts',(0.00883310285273221,-0.155349895274327,
2.09362243048698));
#21457=CARTESIAN_POINT('Ctrl Pts',(0.0128009852858482,-0.155073351939004,
2.09389232126612));
#21458=CARTESIAN_POINT('Ctrl Pts',(0.0192096306625509,-0.154379062869907,
2.09433708239329));
#21459=CARTESIAN_POINT('Ctrl Pts',(0.0216587621687042,-0.154054541628188,
2.09450915592145));
#21460=CARTESIAN_POINT('Ctrl Pts',(0.024853337552565,-0.15355356430304,
2.09473681807388));
#21461=CARTESIAN_POINT('Ctrl Pts',(0.025606767685335,-0.153429719771189,
2.09479074619171));
#21462=CARTESIAN_POINT('Ctrl Pts',(0.0267863769709881,-0.153226891718253,
2.09487556019163));
#21463=CARTESIAN_POINT('Ctrl Pts',(0.0272131975532774,-0.153151664074773,
2.0949063270881));
#21464=CARTESIAN_POINT('Ctrl Pts',(0.0280927244976935,-0.152992853617563,
2.09496989158027));
#21465=CARTESIAN_POINT('Ctrl Pts',(0.028545384832841,-0.152909042976954,
2.09500269610817));
#21466=CARTESIAN_POINT('Ctrl Pts',(0.0295562198156295,-0.15271724064329,
2.09507615701763));
#21467=CARTESIAN_POINT('Ctrl Pts',(0.0301141854047978,-0.152608196179066,
2.0951168464701));
#21468=CARTESIAN_POINT('Ctrl Pts',(0.0315238279156536,-0.152324674836719,
2.09522000556244));
#21469=CARTESIAN_POINT('Ctrl Pts',(0.0323746534130341,-0.152146114146601,
2.09528260442757));
#21470=CARTESIAN_POINT('Ctrl Pts',(0.0371649183859182,-0.151098792922337,
2.09563697986784));
#21471=CARTESIAN_POINT('Ctrl Pts',(0.0410705340794318,-0.150084249816918,
2.09593337227538));
#21472=CARTESIAN_POINT('Ctrl Pts',(0.046742365216269,-0.148372940897499,
2.0963753493966));
#21473=CARTESIAN_POINT('Ctrl Pts',(0.0485425551349078,-0.147793768902848,
2.09651736623511));
#21474=CARTESIAN_POINT('Ctrl Pts',(0.0642483240589407,-0.142422881267746,
2.09777152746878));
#21475=CARTESIAN_POINT('Ctrl Pts',(0.0774175463040418,-0.135715032924409,
2.0989378469886));
#21476=CARTESIAN_POINT('Ctrl Pts',(0.0915746681914158,-0.125764217306641,
2.10023969192907));
#21477=CARTESIAN_POINT('Ctrl Pts',(0.093663488237941,-0.124216389181719,
2.1004328880198));
#21478=CARTESIAN_POINT('Ctrl Pts',(0.0961380302185033,-0.122284801965177,
2.10066221003611));
#21479=CARTESIAN_POINT('Ctrl Pts',(0.0965616474906106,-0.121950571556939,
2.10070148388226));
#21480=CARTESIAN_POINT('Ctrl Pts',(0.097218574685019,-0.121426692369834,
2.10076240225947));
#21481=CARTESIAN_POINT('Ctrl Pts',(0.097453082825586,-0.121238564556163,
2.10078415158408));
#21482=CARTESIAN_POINT('Ctrl Pts',(0.0978876018901263,-0.120887908052338,
2.10082445379575));
#21483=CARTESIAN_POINT('Ctrl Pts',(0.0980877523498004,-0.120725563812675,
2.10084301892751));
#21484=CARTESIAN_POINT('Ctrl Pts',(0.0985399596028237,-0.120356906550316,
2.10088496687752));
#21485=CARTESIAN_POINT('Ctrl Pts',(0.0987917719262479,-0.120150299199908,
2.10090832810862));
#21486=CARTESIAN_POINT('Ctrl Pts',(0.0995512130847963,-0.119523190112429,
2.10097879728187));
#21487=CARTESIAN_POINT('Ctrl Pts',(0.100056828717749,-0.119100243784874,
2.10102573278743));
#21488=CARTESIAN_POINT('Ctrl Pts',(0.103915013534657,-0.115830969734336,
2.10138416708048));
#21489=CARTESIAN_POINT('Ctrl Pts',(0.107148590900619,-0.112846497817881,
2.10168625142364));
#21490=CARTESIAN_POINT('Ctrl Pts',(0.120645024503983,-0.0992857331299244,
2.10297766192179));
#21491=CARTESIAN_POINT('Ctrl Pts',(0.129502144886547,-0.0874192325556558,
2.10391456027543));
#21492=CARTESIAN_POINT('Ctrl Pts',(0.138467021982286,-0.0709829732157343,
2.10518925654987));
#21493=CARTESIAN_POINT('Ctrl Pts',(0.140240711343387,-0.0674109549754019,
2.10546450603147));
#21494=CARTESIAN_POINT('Ctrl Pts',(0.142251038715252,-0.0629387410611146,
2.10580899008777));
#21495=CARTESIAN_POINT('Ctrl Pts',(0.142619542019864,-0.0620991892997372,
2.1058736503358));
#21496=CARTESIAN_POINT('Ctrl Pts',(0.143188794075535,-0.0607704801661151,
2.10597599418996));
#21497=CARTESIAN_POINT('Ctrl Pts',(0.143394512078053,-0.0602834629211887,
2.10601350874638));
#21498=CARTESIAN_POINT('Ctrl Pts',(0.143774662092217,-0.0593705386413041,
2.10608383910188));
#21499=CARTESIAN_POINT('Ctrl Pts',(0.143949694876233,-0.0589448865888338,
2.10611663415434));
#21500=CARTESIAN_POINT('Ctrl Pts',(0.144336065167541,-0.0579933103904562,
2.10618996094575));
#21501=CARTESIAN_POINT('Ctrl Pts',(0.144546421373407,-0.0574669975769691,
2.10623052519959));
#21502=CARTESIAN_POINT('Ctrl Pts',(0.145070086163024,-0.0561357170685721,
2.10633315577793));
#21503=CARTESIAN_POINT('Ctrl Pts',(0.145379571249598,-0.0553292764951944,
2.10639534902532));
#21504=CARTESIAN_POINT('Ctrl Pts',(0.147067941684211,-0.0508178257031439,
2.10674344913227));
#21505=CARTESIAN_POINT('Ctrl Pts',(0.148311788598635,-0.0470642007978736,
2.1070337827555));
#21506=CARTESIAN_POINT('Ctrl Pts',(0.149957472320738,-0.0413813395434992,
2.10747486944115));
#21507=CARTESIAN_POINT('Ctrl Pts',(0.15046791368721,-0.0394849989686747,
2.10762229655842));
#21508=CARTESIAN_POINT('Ctrl Pts',(0.1544841234355,-0.0233534706240894,
2.10887821628386));
#21509=CARTESIAN_POINT('Ctrl Pts',(0.155996648345524,-0.00870038777706942,
2.11004050690006));
#21510=CARTESIAN_POINT('Ctrl Pts',(0.15533463394952,0.00860376758607486,
2.11134407375037));
#21511=CARTESIAN_POINT('Ctrl Pts',(0.155164850128709,0.0112581041147174,
2.11154181553789));
#21512=CARTESIAN_POINT('Ctrl Pts',(0.154878510889393,0.0144479896801079,
2.1117757994496));
#21513=CARTESIAN_POINT('Ctrl Pts',(0.154827113627625,0.0149887441273677,
2.11181533768871));
#21514=CARTESIAN_POINT('Ctrl Pts',(0.154742791440628,0.0158291456724525,
2.11187657616866));
#21515=CARTESIAN_POINT('Ctrl Pts',(0.154711827075869,0.0161289777301707,
2.11189838295658));
#21516=CARTESIAN_POINT('Ctrl Pts',(0.154652779836225,0.0166849203565997,
2.11193873751695));
#21517=CARTESIAN_POINT('Ctrl Pts',(0.154624932493924,0.0169410487141398,
2.11195729781535));
#21518=CARTESIAN_POINT('Ctrl Pts',(0.154560553731085,0.0175197928359585,
2.11199916624363));
#21519=CARTESIAN_POINT('Ctrl Pts',(0.154523648616741,0.0178423634662825,
2.11202245313307));
#21520=CARTESIAN_POINT('Ctrl Pts',(0.154411805251766,0.0187935539596294,
2.11209098276562));
#21521=CARTESIAN_POINT('Ctrl Pts',(0.15433403787289,0.0194218449727524,
2.11213607038085));
#21522=CARTESIAN_POINT('Ctrl Pts',(0.153746969808654,0.0239384645705222,
2.11245902428026));
#21523=CARTESIAN_POINT('Ctrl Pts',(0.153094570344407,0.0278071926000845,
2.11272941991567));
#21524=CARTESIAN_POINT('Ctrl Pts',(0.152025546843706,0.0329516274772899,
2.11308561441976));
#21525=CARTESIAN_POINT('Ctrl Pts',(0.151737803875257,0.0342522363124642,
2.11317537428777));
#21526=CARTESIAN_POINT('Ctrl Pts',(0.15050603824148,0.0394993694956073,
2.11353688721891));
#21527=CARTESIAN_POINT('Ctrl Pts',(0.149424433351358,0.0434120849051451,
2.11380508662157));
#21528=CARTESIAN_POINT('Ctrl Pts',(0.145327975164245,0.0562522256601415,
2.1146931901613));
#21529=CARTESIAN_POINT('Ctrl Pts',(0.141655936298709,0.0649469992922441,
2.11530892160966));
#21530=CARTESIAN_POINT('Ctrl Pts',(0.135168842958949,0.0770983696808988,
2.11624404231416));
#21531=CARTESIAN_POINT('Ctrl Pts',(0.132957227833877,0.0808526082722024,
2.11654412421923));
#21532=CARTESIAN_POINT('Ctrl Pts',(0.130079807788597,0.085299074325434,
2.11691608163433));
#21533=CARTESIAN_POINT('Ctrl Pts',(0.129561276838548,0.0860846324820536,
2.11698244436873));
#21534=CARTESIAN_POINT('Ctrl Pts',(0.128737432506259,0.0873084254999529,
2.11708687656539));
#21535=CARTESIAN_POINT('Ctrl Pts',(0.128436930695856,0.0877498861086389,
2.11712476507561));
#21536=CARTESIAN_POINT('Ctrl Pts',(0.127899658760918,0.0885305081531673,
2.11719215241497));
#21537=CARTESIAN_POINT('Ctrl Pts',(0.127663796604884,0.0888702909603656,
2.1172216165997));
#21538=CARTESIAN_POINT('Ctrl Pts',(0.127116674566962,0.0896518017262265,
2.11728969382767));
#21539=CARTESIAN_POINT('Ctrl Pts',(0.126804464031219,0.0900928542885824,
2.11732834291841));
#21540=CARTESIAN_POINT('Ctrl Pts',(0.125940396610847,0.0913001129030285,
2.11743477199929));
#21541=CARTESIAN_POINT('Ctrl Pts',(0.125383859158127,0.0920629236128803,
2.11750273140506));
#21542=CARTESIAN_POINT('Ctrl Pts',(0.122490277179034,0.0959540653074933,
2.11785312865737));
#21543=CARTESIAN_POINT('Ctrl Pts',(0.120043179152849,0.0989983875217004,
2.11813983605939));
#21544=CARTESIAN_POINT('Ctrl Pts',(0.116168371410419,0.103463731106798,
2.11858043259816));
#21545=CARTESIAN_POINT('Ctrl Pts',(0.114823207912509,0.104954582940407,
2.11873114189461));
#21546=CARTESIAN_POINT('Ctrl Pts',(0.103437996811253,0.117091971235299,
2.11998829786051));
#21547=CARTESIAN_POINT('Ctrl Pts',(0.0919720869577657,0.126297292122009,
2.12114832932706));
#21548=CARTESIAN_POINT('Ctrl Pts',(0.0770740535487226,0.135139359868302,
2.12245291008323));
#21549=CARTESIAN_POINT('Ctrl Pts',(0.0747224595322871,0.136453701831866,
2.12265324684281));
#21550=CARTESIAN_POINT('Ctrl Pts',(0.0718550858329579,0.13795994479323,
2.12288988734704));
#21551=CARTESIAN_POINT('Ctrl Pts',(0.0713711006441542,0.138210946542513,
2.12292957323021));
#21552=CARTESIAN_POINT('Ctrl Pts',(0.0706171024967069,0.138596964087064,
2.12299099040557));
#21553=CARTESIAN_POINT('Ctrl Pts',(0.0703480058979274,0.138733743875096,
2.12301282922946));
#21554=CARTESIAN_POINT('Ctrl Pts',(0.0698485323621824,0.138985795623522,
2.1230532131736));
#21555=CARTESIAN_POINT('Ctrl Pts',(0.0696182694072932,0.139101277581931,
2.12307177097624));
#21556=CARTESIAN_POINT('Ctrl Pts',(0.0690976519170733,0.139360762186724,
2.12311359597568));
#21557=CARTESIAN_POINT('Ctrl Pts',(0.0688071341872435,0.139504429420173,
2.12313684212222));
#21558=CARTESIAN_POINT('Ctrl Pts',(0.0679502213662177,0.13992486309541,
2.12320514115709));
#21559=CARTESIAN_POINT('Ctrl Pts',(0.0673825811031899,0.14019910019741,
2.12325004047087));
#21560=CARTESIAN_POINT('Ctrl Pts',(0.0633337264451739,0.142124902623486,
2.12356797265133));
#21561=CARTESIAN_POINT('Ctrl Pts',(0.0597935064867675,0.143650241009157,
2.12383379668596));
#21562=CARTESIAN_POINT('Ctrl Pts',(0.04460299243111,0.149536135184221,2.12493888899866));
#21563=CARTESIAN_POINT('Ctrl Pts',(0.0325084024869392,0.15262284961798,
2.12573589926957));
#21564=CARTESIAN_POINT('Ctrl Pts',(0.015809608591236,0.154807096117142,
2.12686198254668));
#21565=CARTESIAN_POINT('Ctrl Pts',(0.0114227787029252,0.155192447419367,
2.127159727511));
#21566=CARTESIAN_POINT('Ctrl Pts',(0.00436006533228581,0.155511777362201,
2.12764664434128));
#21567=CARTESIAN_POINT('Ctrl Pts',(0.00169183895864124,0.155563682337055,
2.12783230286204));
#21568=CARTESIAN_POINT('Ctrl Pts',(-0.00177884502506953,0.155541899061895,
2.1280765912983));
#21569=CARTESIAN_POINT('Ctrl Pts',(-0.00258135610695362,0.155530650389993,
2.12813327044301));
#21570=CARTESIAN_POINT('Ctrl Pts',(-0.00388701311032124,0.155502241276432,
2.12822581573446));
#21571=CARTESIAN_POINT('Ctrl Pts',(-0.00439023374664659,0.155488847669876,
2.12826156399668));
#21572=CARTESIAN_POINT('Ctrl Pts',(-0.00535825764755493,0.155458379976122,
2.12833048916073));
#21573=CARTESIAN_POINT('Ctrl Pts',(-0.00582306747507281,0.155441663354329,
2.12836365452934));
#21574=CARTESIAN_POINT('Ctrl Pts',(-0.00688768696392738,0.155398593084937,
2.12843978180993));
#21575=CARTESIAN_POINT('Ctrl Pts',(-0.00748742974726766,0.155370851003539,
2.12848278665164));
#21576=CARTESIAN_POINT('Ctrl Pts',(-0.00908132583029788,0.155287872695047,
2.12859740292566));
#21577=CARTESIAN_POINT('Ctrl Pts',(-0.0100751204578383,0.155226562633507,
2.12866920290423));
#21578=CARTESIAN_POINT('Ctrl Pts',(-0.0175925317763295,0.154690298224357,
2.12921495981637));
#21579=CARTESIAN_POINT('Ctrl Pts',(-0.0240799891881967,0.15381390346561,
2.12970141250499));
#21580=CARTESIAN_POINT('Ctrl Pts',(-0.0419292207722073,0.150245713766086,
2.13108376194071));
#21581=CARTESIAN_POINT('Ctrl Pts',(-0.0530638077777302,0.146682165595228,
2.13199949648016));
#21582=CARTESIAN_POINT('Ctrl Pts',(-0.0636886258331765,0.141913922641444,
2.1328902089718));
#21583=CARTESIAN_POINT('Origin',(0.,0.,-0.129405622560373));
#21584=CARTESIAN_POINT('',(-0.0636886258329906,0.141913922641527,2.21660530308003));
#21585=CARTESIAN_POINT('',(-0.0636886613526595,0.141913906700881,2.20284414165342));
#21586=CARTESIAN_POINT('',(-0.0636886258329924,0.141913922641526,-0.129405622560373));
#21587=CARTESIAN_POINT('',(-0.15554996116255,0.000109919649464305,2.15940562256037));
#21588=CARTESIAN_POINT('Ctrl Pts',(-0.15554996116255,0.000109919649464305,
2.15940562256037));
#21589=CARTESIAN_POINT('Ctrl Pts',(-0.155557267423461,-0.0102293473203203,
2.16014353394896));
#21590=CARTESIAN_POINT('Ctrl Pts',(-0.154529367184467,-0.0205766677469432,
2.16088144533755));
#21591=CARTESIAN_POINT('Ctrl Pts',(-0.152487668180623,-0.0307134099838537,
2.16161935672614));
#21592=CARTESIAN_POINT('Ctrl Pts',(-0.150445829414615,-0.0408508461198288,
2.16235731862761));
#21593=CARTESIAN_POINT('Ctrl Pts',(-0.147390270093583,-0.050776782287812,
2.16309528052908));
#21594=CARTESIAN_POINT('Ctrl Pts',(-0.143393161912447,-0.060284356318624,
2.16383324243055));
#21595=CARTESIAN_POINT('Ctrl Pts',(-0.139385782328791,-0.0698163620424093,
2.16457310067893));
#21596=CARTESIAN_POINT('Ctrl Pts',(-0.134432451496566,-0.0789270447473818,
2.1653129589273));
#21597=CARTESIAN_POINT('Ctrl Pts',(-0.128651965870623,-0.0874326836922218,
2.16605281717568));
#21598=CARTESIAN_POINT('Ctrl Pts',(-0.12725028813426,-0.0894951686656319,
2.16623222127802));
#21599=CARTESIAN_POINT('Ctrl Pts',(-0.125800167594638,-0.091522222466176,
2.16641162538036));
#21600=CARTESIAN_POINT('Ctrl Pts',(-0.124303651570102,-0.0935115217838889,
2.1665910294827));
#21601=CARTESIAN_POINT('Ctrl Pts',(-0.118153313802634,-0.101687085910121,
2.16732833921288));
#21602=CARTESIAN_POINT('Ctrl Pts',(-0.111169892400885,-0.109283920973333,
2.16806564894306));
#21603=CARTESIAN_POINT('Ctrl Pts',(-0.103486335854972,-0.116130877854737,
2.16880295867324));
#21604=CARTESIAN_POINT('Ctrl Pts',(-0.0957549579473897,-0.123020449220645,
2.16954485731418));
#21605=CARTESIAN_POINT('Ctrl Pts',(-0.0873152795860456,-0.129150017855905,
2.17028675595512));
#21606=CARTESIAN_POINT('Ctrl Pts',(-0.0783421409037998,-0.134381216911476,
2.17102865459605));
#21607=CARTESIAN_POINT('Ctrl Pts',(-0.0694450195957192,-0.139568099030686,
2.17176426812443));
#21608=CARTESIAN_POINT('Ctrl Pts',(-0.0600242657486143,-0.143871321381819,
2.17249988165282));
#21609=CARTESIAN_POINT('Ctrl Pts',(-0.0502782126981477,-0.147200216806497,
2.1732354951812));
#21610=CARTESIAN_POINT('Ctrl Pts',(-0.0404072536243069,-0.150571775562431,
2.17398053637841));
#21611=CARTESIAN_POINT('Ctrl Pts',(-0.0302035006824242,-0.152943492630249,
2.17472557757562));
#21612=CARTESIAN_POINT('Ctrl Pts',(-0.0198888207273883,-0.154273255329865,
2.17547061877284));
#21613=CARTESIAN_POINT('Ctrl Pts',(-0.00957414077235236,-0.155603018029482,
2.17621565997005));
#21614=CARTESIAN_POINT('Ctrl Pts',(0.000850485147299905,-0.155890834447186,
2.17696070116726));
#21615=CARTESIAN_POINT('Ctrl Pts',(0.011161779685702,-0.155149016027327,
2.17770574236447));
#21616=CARTESIAN_POINT('Ctrl Pts',(0.0213660702183622,-0.154414895723565,
2.17844305200167));
#21617=CARTESIAN_POINT('Ctrl Pts',(0.0315358720632552,-0.152666987619122,
2.17918036163887));
#21618=CARTESIAN_POINT('Ctrl Pts',(0.0414552909564462,-0.149924185346182,
2.17991767127607));
#21619=CARTESIAN_POINT('Ctrl Pts',(0.0514364484715978,-0.147164311827995,
2.18065956994025));
#21620=CARTESIAN_POINT('Ctrl Pts',(0.0611631441371558,-0.143397193035534,
2.18140146860444));
#21621=CARTESIAN_POINT('Ctrl Pts',(0.0704243105148482,-0.138694697045375,
2.18214336726862));
#21622=CARTESIAN_POINT('Ctrl Pts',(0.0796070180183042,-0.134032039724173,
2.18287898070569));
#21623=CARTESIAN_POINT('Ctrl Pts',(0.0883312262223324,-0.128450239567257,
2.18361459414276));
#21624=CARTESIAN_POINT('Ctrl Pts',(0.0964132053605308,-0.122066769974912,
2.18435020757983));
#21625=CARTESIAN_POINT('Ctrl Pts',(0.104598765547872,-0.115601487937096,
2.18509524885757));
#21626=CARTESIAN_POINT('Ctrl Pts',(0.112124722996507,-0.108314403050016,
2.18584029013531));
#21627=CARTESIAN_POINT('Ctrl Pts',(0.118835381745117,-0.100369091584473,
2.18658533141304));
#21628=CARTESIAN_POINT('Ctrl Pts',(0.125546040493727,-0.0924237801189298,
2.18733037269078));
#21629=CARTESIAN_POINT('Ctrl Pts',(0.131440875338134,-0.0838210707394638,
2.18807541396852));
#21630=CARTESIAN_POINT('Ctrl Pts',(0.136409152710375,-0.0747552376548803,
2.18882045524625));
#21631=CARTESIAN_POINT('Ctrl Pts',(0.141325872363875,-0.0657834841953472,
2.18955776494506));
#21632=CARTESIAN_POINT('Ctrl Pts',(0.145372103737932,-0.0562909566865397,
2.19029507464387));
#21633=CARTESIAN_POINT('Ctrl Pts',(0.148446647289986,-0.0464692953288783,
2.19103238434268));
#21634=CARTESIAN_POINT('Ctrl Pts',(0.151540326527584,-0.0365865048247006,
2.19177428299146));
#21635=CARTESIAN_POINT('Ctrl Pts',(0.153649728849893,-0.0263713099442799,
2.19251618164024));
#21636=CARTESIAN_POINT('Ctrl Pts',(0.154720781389452,-0.0160400220148674,
2.19325808028901));
#21637=CARTESIAN_POINT('Ctrl Pts',(0.155782760276811,-0.00579625781560798,
2.19399369378365));
#21638=CARTESIAN_POINT('Ctrl Pts',(0.155823841493419,0.004560702577827,
2.19472930727828));
#21639=CARTESIAN_POINT('Ctrl Pts',(0.154843094330516,0.0148127863061284,
2.19546492077292));
#21640=CARTESIAN_POINT('Ctrl Pts',(0.153849777767092,0.0251962622539743,
2.19620996199877));
#21641=CARTESIAN_POINT('Ctrl Pts',(0.15180829570891,0.0354711820272215,
2.19695500322462));
#21642=CARTESIAN_POINT('Ctrl Pts',(0.148771655133367,0.0454180264749404,
2.19770004445047));
#21643=CARTESIAN_POINT('Ctrl Pts',(0.145735014557825,0.0553648709226579,
2.19844508567632));
#21644=CARTESIAN_POINT('Ctrl Pts',(0.141703626904404,0.0649827494045178,
2.19919012690217));
#21645=CARTESIAN_POINT('Ctrl Pts',(0.136780673539898,0.074073273493021,
2.19993516812803));
#21646=CARTESIAN_POINT('Ctrl Pts',(0.131908805826588,0.083069464909977,
2.20067247803624));
#21647=CARTESIAN_POINT('Ctrl Pts',(0.126127338894467,0.0916166731077121,
2.20140978794444));
#21648=CARTESIAN_POINT('Ctrl Pts',(0.119542411262813,0.0995259484228733,
2.20214709785265));
#21649=CARTESIAN_POINT('Ctrl Pts',(0.112916501976755,0.107484447542105,
2.20288899644908));
#21650=CARTESIAN_POINT('Ctrl Pts',(0.105477557918341,0.11479621038619,2.20363089504551));
#21651=CARTESIAN_POINT('Ctrl Pts',(0.0973780017415188,0.121298504841687,
2.20437279364194));
#21652=CARTESIAN_POINT('Ctrl Pts',(0.0893470598209456,0.127745716019997,
2.20510840734827));
#21653=CARTESIAN_POINT('Ctrl Pts',(0.0806674030898069,0.133396550631897,
2.20584402105461));
#21654=CARTESIAN_POINT('Ctrl Pts',(0.0715217520374606,0.138131971264773,
2.20657963476094));
#21655=CARTESIAN_POINT('Ctrl Pts',(0.0622588939281335,0.142928079180902,
2.20732467580242));
#21656=CARTESIAN_POINT('Ctrl Pts',(0.0525188515825804,0.146784650332905,
2.20806971684389));
#21657=CARTESIAN_POINT('Ctrl Pts',(0.0425148093650004,0.149627181637087,
2.20881475788537));
#21658=CARTESIAN_POINT('Ctrl Pts',(0.0325107671474189,0.152469712941268,
2.20955979892685));
#21659=CARTESIAN_POINT('Ctrl Pts',(0.0222436964848991,0.154298067118003,
2.21030483996833));
#21660=CARTESIAN_POINT('Ctrl Pts',(0.0119362359789071,0.155091356208706,
2.21104988100981));
#21661=CARTESIAN_POINT('Ctrl Pts',(0.00173574192027406,0.155876412882151,
2.21178719033179));
#21662=CARTESIAN_POINT('Ctrl Pts',(-0.00858076872269995,0.155653752489481,
2.21252449965377));
#21663=CARTESIAN_POINT('Ctrl Pts',(-0.0187969842381853,0.154410089966781,
2.21326180897575));
#21664=CARTESIAN_POINT('Ctrl Pts',(-0.0289936767261386,0.153168804063645,
2.21399770931119));
#21665=CARTESIAN_POINT('Ctrl Pts',(-0.0390895324633264,0.150910415862194,
2.21473360964663));
#21666=CARTESIAN_POINT('Ctrl Pts',(-0.0488704089261867,0.147673577973134,
2.21546950998207));
#21667=CARTESIAN_POINT('Ctrl Pts',(-0.0539023638633416,0.146008326146422,
2.21584810768139));
#21668=CARTESIAN_POINT('Ctrl Pts',(-0.0588510526583658,0.144084945625908,
2.21622670538071));
#21669=CARTESIAN_POINT('Ctrl Pts',(-0.0636886258329906,0.141913922641527,
2.21660530308003));
#21670=CARTESIAN_POINT('Ctrl Pts',(-0.0637081998868965,0.141956949220948,
2.1466152095062));
#21671=CARTESIAN_POINT('Ctrl Pts',(-0.101121651380785,0.124710229304317,
2.14956891187111));
#21672=CARTESIAN_POINT('Ctrl Pts',(-0.145741622366923,0.0779923160122845,
2.15383235576962));
#21673=CARTESIAN_POINT('Ctrl Pts',(-0.15550054095579,0.0184426036431841,
2.15809579966814));
#21674=CARTESIAN_POINT('Ctrl Pts',(-0.155381214903208,0.000110939127196429,
2.15940554120174));
#21675=CARTESIAN_POINT('Ctrl Pts',(-0.0636886258331769,0.141913922641443,
2.1328902089718));
#21676=CARTESIAN_POINT('Ctrl Pts',(-0.0660169911472436,0.14086899072405,
2.13308540328567));
#21677=CARTESIAN_POINT('Ctrl Pts',(-0.0683208869914562,0.139766198311673,
2.13327922358076));
#21678=CARTESIAN_POINT('Ctrl Pts',(-0.0726221572309729,0.137575376390049,
2.13364111494803));
#21679=CARTESIAN_POINT('Ctrl Pts',(-0.074623493377058,0.136500174458298,
2.13380951295736));
#21680=CARTESIAN_POINT('Ctrl Pts',(-0.0770515419109373,0.135126350957108,
2.13401320397298));
#21681=CARTESIAN_POINT('Ctrl Pts',(-0.0775011181018852,0.134869001432455,
2.134050892937));
#21682=CARTESIAN_POINT('Ctrl Pts',(-0.0782054811963862,0.134461119929222,
2.13410988981991));
#21683=CARTESIAN_POINT('Ctrl Pts',(-0.0784611328148135,0.134312101849352,
2.13413129228043));
#21684=CARTESIAN_POINT('Ctrl Pts',(-0.0789391602791836,0.134031631350248,
2.13417128912932));
#21685=CARTESIAN_POINT('Ctrl Pts',(-0.0791616313086886,0.133900356079015,
2.13418989404401));
#21686=CARTESIAN_POINT('Ctrl Pts',(-0.0796697893692687,0.13359879405042,
2.13423237036266));
#21687=CARTESIAN_POINT('Ctrl Pts',(-0.079955257667684,0.133428145032307,
2.13425621791842));
#21688=CARTESIAN_POINT('Ctrl Pts',(-0.0808345705958355,0.13289866852993,
2.1343296369212));
#21689=CARTESIAN_POINT('Ctrl Pts',(-0.0814265746190951,0.132536775629558,
2.13437901402411));
#21690=CARTESIAN_POINT('Ctrl Pts',(-0.0870306301950694,0.129059285588559,
2.13484612591801));
#21691=CARTESIAN_POINT('Ctrl Pts',(-0.0918646957790118,0.125664342741429,
2.1352467978858));
#21692=CARTESIAN_POINT('Ctrl Pts',(-0.104292549765392,0.115834846101169,
2.13630449511134));
#21693=CARTESIAN_POINT('Ctrl Pts',(-0.111481215559507,0.108933905415754,
2.13694806206204));
#21694=CARTESIAN_POINT('Ctrl Pts',(-0.122076923861692,0.0966068036517986,
2.13803296018742));
#21695=CARTESIAN_POINT('Ctrl Pts',(-0.125895963225234,0.0915742366820963,
2.13846094260296));
#21696=CARTESIAN_POINT('Ctrl Pts',(-0.130218059858009,0.0850954789193387,
2.13900405786398));
#21697=CARTESIAN_POINT('Ctrl Pts',(-0.131020099688287,0.0838553329261292,
2.13910766737493));
#21698=CARTESIAN_POINT('Ctrl Pts',(-0.132143950138925,0.0820620979977112,
2.13925708130983));
#21699=CARTESIAN_POINT('Ctrl Pts',(-0.132480214152427,0.0815181226608786,
2.13930235324905));
#21700=CARTESIAN_POINT('Ctrl Pts',(-0.133057638284181,0.0805710125096015,
2.13938109302485));
#21701=CARTESIAN_POINT('Ctrl Pts',(-0.133300346321974,0.0801688270100914,
2.13941450381366));
#21702=CARTESIAN_POINT('Ctrl Pts',(-0.13376370459128,0.0793930857309455,
2.13947890105814));
#21703=CARTESIAN_POINT('Ctrl Pts',(-0.133984621346033,0.0790196935174879,
2.13950987743686));
#21704=CARTESIAN_POINT('Ctrl Pts',(-0.134559661831712,0.0780384189484672,
2.1395912333798));
#21705=CARTESIAN_POINT('Ctrl Pts',(-0.134911225284298,0.077429055827792,
2.13964170476628));
#21706=CARTESIAN_POINT('Ctrl Pts',(-0.136118623782933,0.0753030894724131,
2.13981763426765));
#21707=CARTESIAN_POINT('Ctrl Pts',(-0.136953086795314,0.0737745659677436,
2.13994385026327));
#21708=CARTESIAN_POINT('Ctrl Pts',(-0.143208624521256,0.0618440021030586,
2.14092731086853));
#21709=CARTESIAN_POINT('Ctrl Pts',(-0.147461917323854,0.0508749674725732,
2.14182601688876));
#21710=CARTESIAN_POINT('Ctrl Pts',(-0.151793605044927,0.0343916342501916,
2.14314750614871));
#21711=CARTESIAN_POINT('Ctrl Pts',(-0.152880620568386,0.0291822299549133,
2.14356043826949));
#21712=CARTESIAN_POINT('Ctrl Pts',(-0.15420048097391,0.0207039916653352,
2.14421732374455));
#21713=CARTESIAN_POINT('Ctrl Pts',(-0.154600784969782,0.0174655102016115,
2.14446469468069));
#21714=CARTESIAN_POINT('Ctrl Pts',(-0.15500816346531,0.013026863815089,
2.14479700796752));
#21715=CARTESIAN_POINT('Ctrl Pts',(-0.155103651586189,0.0118358524301557,
2.14488551622584));
#21716=CARTESIAN_POINT('Ctrl Pts',(-0.155243882151083,0.00979130937018618,
2.14503619349355));
#21717=CARTESIAN_POINT('Ctrl Pts',(-0.155295329555652,0.00893831033988605,
2.14509868175035));
#21718=CARTESIAN_POINT('Ctrl Pts',(-0.155358562299612,0.00772338469619673,
2.14518710950521));
#21719=CARTESIAN_POINT('Ctrl Pts',(-0.155376116359966,0.0073617948263221,
2.14521335528877));
#21720=CARTESIAN_POINT('Ctrl Pts',(-0.15540421959229,0.00673794620559497,
2.14525850844299));
#21721=CARTESIAN_POINT('Ctrl Pts',(-0.15541536756059,0.00647571745886528,
2.14527744893267));
#21722=CARTESIAN_POINT('Ctrl Pts',(-0.155435709740474,0.0059668701674449,
2.14531412503386));
#21723=CARTESIAN_POINT('Ctrl Pts',(-0.155444980785915,0.00572025811611256,
2.14533186500484));
#21724=CARTESIAN_POINT('Ctrl Pts',(-0.155465950470758,0.00512470841408515,
2.14537462337654));
#21725=CARTESIAN_POINT('Ctrl Pts',(-0.155477061388796,0.00477574919723898,
2.14539960918499));
#21726=CARTESIAN_POINT('Ctrl Pts',(-0.155513813946436,0.00348483744748929,
2.14549179721318));
#21727=CARTESIAN_POINT('Ctrl Pts',(-0.155532071846496,0.00254266870293689,
2.14555860299013));
#21728=CARTESIAN_POINT('Ctrl Pts',(-0.155547088414487,0.0010831836899177,
2.14566143200919));
#21729=CARTESIAN_POINT('Ctrl Pts',(-0.155549830254567,0.00056597405139784,
2.14569774445918));
#21730=CARTESIAN_POINT('Ctrl Pts',(-0.155553009013036,-0.00957632917392199,
2.14640748139099));
#21731=CARTESIAN_POINT('Ctrl Pts',(-0.154662648232899,-0.0191824693484842,
2.14703920233448));
#21732=CARTESIAN_POINT('Ctrl Pts',(-0.150827262360558,-0.0396528162620391,
2.14840986053697));
#21733=CARTESIAN_POINT('Ctrl Pts',(-0.147582757689397,-0.0504032958235261,
2.14914702796375));
#21734=CARTESIAN_POINT('Ctrl Pts',(-0.142528464659535,-0.0623258617002273,
2.15004688918939));
#21735=CARTESIAN_POINT('Ctrl Pts',(-0.141816961770028,-0.0639282816438271,
2.15016957519926));
#21736=CARTESIAN_POINT('Ctrl Pts',(-0.140781385131717,-0.066158157878763,
2.15034292533514));
#21737=CARTESIAN_POINT('Ctrl Pts',(-0.140479873336042,-0.0667959984688954,
2.1503928160626));
#21738=CARTESIAN_POINT('Ctrl Pts',(-0.13998579833137,-0.0678230588884798,
2.15047365561208));
#21739=CARTESIAN_POINT('Ctrl Pts',(-0.139795923496471,-0.0682135676991828,
2.1505045111557));
#21740=CARTESIAN_POINT('Ctrl Pts',(-0.139397362288651,-0.0690246209204112,
2.15056884589346));
#21741=CARTESIAN_POINT('Ctrl Pts',(-0.139188402425506,-0.0694450252184121,
2.15060233435117));
#21742=CARTESIAN_POINT('Ctrl Pts',(-0.138691015863459,-0.0704344488879261,
2.15068148655744));
#21743=CARTESIAN_POINT('Ctrl Pts',(-0.138400987391194,-0.0710026488102514,
2.15072720596713));
#21744=CARTESIAN_POINT('Ctrl Pts',(-0.137432114314633,-0.0728722926324531,
2.15087853137526));
#21745=CARTESIAN_POINT('Ctrl Pts',(-0.136738361755392,-0.0741658764413903,
2.15098465991372));
#21746=CARTESIAN_POINT('Ctrl Pts',(-0.132999201335909,-0.0809071438232189,
2.15154546334311));
#21747=CARTESIAN_POINT('Ctrl Pts',(-0.129646684549319,-0.086176975962864,
2.15201103484421));
#21748=CARTESIAN_POINT('Ctrl Pts',(-0.120134372237566,-0.0993132358241871,
2.15324450473581));
#21749=CARTESIAN_POINT('Ctrl Pts',(-0.113517547093068,-0.106813508048795,
2.15402485757897));
#21750=CARTESIAN_POINT('Ctrl Pts',(-0.104281169918516,-0.115448470096155,
2.15499880432721));
#21751=CARTESIAN_POINT('Ctrl Pts',(-0.102286881648717,-0.117219054610476,
2.15520305482506));
#21752=CARTESIAN_POINT('Ctrl Pts',(-0.0976450176969882,-0.12113150613975,
2.15566341145255));
#21753=CARTESIAN_POINT('Ctrl Pts',(-0.0949704747078093,-0.123239623089311,
2.15591812252595));
#21754=CARTESIAN_POINT('Ctrl Pts',(-0.0917805866619302,-0.125588359384388,
2.15620801789963));
#21755=CARTESIAN_POINT('Ctrl Pts',(-0.0913307485896006,-0.125915870675793,
2.1562485874287));
#21756=CARTESIAN_POINT('Ctrl Pts',(-0.090607532982875,-0.126436503743735,
2.15631330260624));
#21757=CARTESIAN_POINT('Ctrl Pts',(-0.0903352783986377,-0.126631165178803,
2.15633755000596));
#21758=CARTESIAN_POINT('Ctrl Pts',(-0.0898510596985914,-0.12697502414216,
2.15638046925827));
#21759=CARTESIAN_POINT('Ctrl Pts',(-0.0896393487143254,-0.127124572176622,
2.15639916491298));
#21760=CARTESIAN_POINT('Ctrl Pts',(-0.0891889537829955,-0.12744103675876,
2.15643878976897));
#21761=CARTESIAN_POINT('Ctrl Pts',(-0.0889501750260208,-0.127607812040246,
2.1564597093528));
#21762=CARTESIAN_POINT('Ctrl Pts',(-0.0883027004698815,-0.12805734093405,
2.15651620240084));
#21763=CARTESIAN_POINT('Ctrl Pts',(-0.0878931109526026,-0.128338811520761,
2.15655168982881));
#21764=CARTESIAN_POINT('Ctrl Pts',(-0.0858318452554503,-0.129740820200941,
2.15672907057403));
#21765=CARTESIAN_POINT('Ctrl Pts',(-0.0841599610416281,-0.130831525481305,
2.15686906486807));
#21766=CARTESIAN_POINT('Ctrl Pts',(-0.0792410325040952,-0.133907209883295,
2.15727127005465));
#21767=CARTESIAN_POINT('Ctrl Pts',(-0.0759414119874704,-0.135805702253897,
2.15752912808194));
#21768=CARTESIAN_POINT('Ctrl Pts',(-0.0634724587087657,-0.142383169019051,
2.15847274967042));
#21769=CARTESIAN_POINT('Ctrl Pts',(-0.0539154935395429,-0.146269797743455,
2.15913800836375));
#21770=CARTESIAN_POINT('Ctrl Pts',(-0.0373841405397244,-0.151150435148778,
2.16028795169779));
#21771=CARTESIAN_POINT('Ctrl Pts',(-0.0306005687088528,-0.15266830854688,
2.16075925850456));
#21772=CARTESIAN_POINT('Ctrl Pts',(-0.0227449809000074,-0.15388138239273,
2.16131609694688));
#21773=CARTESIAN_POINT('Ctrl Pts',(-0.0217495828496704,-0.15402522379476,
2.16138684483133));
#21774=CARTESIAN_POINT('Ctrl Pts',(-0.0201549390142474,-0.154239894146944,
2.16150051948653));
#21775=CARTESIAN_POINT('Ctrl Pts',(-0.019556542243215,-0.154316908179411,
2.1615432516709));
#21776=CARTESIAN_POINT('Ctrl Pts',(-0.01849562723894,-0.154447178745311,
2.16161915294675));
#21777=CARTESIAN_POINT('Ctrl Pts',(-0.0180332865962473,-0.154501844051324,
2.1616522773486));
#21778=CARTESIAN_POINT('Ctrl Pts',(-0.0170718529500173,-0.154611145826206,
2.16172126041987));
#21779=CARTESIAN_POINT('Ctrl Pts',(-0.0165727276296994,-0.154665443020899,
2.16175712933995));
#21780=CARTESIAN_POINT('Ctrl Pts',(-0.015281044667889,-0.154799634051358,
2.16185010534437));
#21781=CARTESIAN_POINT('Ctrl Pts',(-0.0144881291743909,-0.154875857052642,
2.1619073268212));
#21782=CARTESIAN_POINT('Ctrl Pts',(-0.0110918737770631,-0.155176030171966,
2.16215307741864));
#21783=CARTESIAN_POINT('Ctrl Pts',(-0.0084838442530061,-0.155340441775755,
2.16234345242823));
#21784=CARTESIAN_POINT('Ctrl Pts',(-0.00160101816005513,-0.155600499910772,
2.1628506149305));
#21785=CARTESIAN_POINT('Ctrl Pts',(0.00267546407588023,-0.155585714704597,
2.1631705929119));
#21786=CARTESIAN_POINT('Ctrl Pts',(0.0190840290486806,-0.154852313143182,
2.16441645935159));
#21787=CARTESIAN_POINT('Ctrl Pts',(0.0311156172426077,-0.152889543478955,
2.16537225069882));
#21788=CARTESIAN_POINT('Ctrl Pts',(0.0469359789972818,-0.148362271959415,
2.16662861378158));
#21789=CARTESIAN_POINT('Ctrl Pts',(0.0510259411921149,-0.147005821667162,
2.16695286356551));
#21790=CARTESIAN_POINT('Ctrl Pts',(0.0556607734020622,-0.14525185254536,
2.16731582243976));
#21791=CARTESIAN_POINT('Ctrl Pts',(0.0562653743922906,-0.145018723093558,
2.16736307886673));
#21792=CARTESIAN_POINT('Ctrl Pts',(0.0571736753913093,-0.144661953644649,
2.16743391769736));
#21793=CARTESIAN_POINT('Ctrl Pts',(0.0574784598625501,-0.144541124415357,
2.16745766153654));
#21794=CARTESIAN_POINT('Ctrl Pts',(0.058022291051215,-0.144323534960282,
2.16749997781683));
#21795=CARTESIAN_POINT('Ctrl Pts',(0.0582614803767429,-0.14422714345853,
2.16751857191401));
#21796=CARTESIAN_POINT('Ctrl Pts',(0.0587775700087398,-0.14401766982145,
2.16755865329977));
#21797=CARTESIAN_POINT('Ctrl Pts',(0.0590543834770298,-0.143904384065221,
2.16758012807128));
#21798=CARTESIAN_POINT('Ctrl Pts',(0.0598231212537174,-0.143587186851067,
2.16763970467767));
#21799=CARTESIAN_POINT('Ctrl Pts',(0.0603143342386319,-0.143381544041978,
2.16767770379636));
#21800=CARTESIAN_POINT('Ctrl Pts',(0.0630926906561102,-0.142201600190267,
2.16789229008545));
#21801=CARTESIAN_POINT('Ctrl Pts',(0.0653574414135578,-0.141175031265913,
2.16806589480209));
#21802=CARTESIAN_POINT('Ctrl Pts',(0.080923847741506,-0.133664110767473,
2.16925661359228));
#21803=CARTESIAN_POINT('Ctrl Pts',(0.0932665513474686,-0.125364381436631,
2.17019422091939));
#21804=CARTESIAN_POINT('Ctrl Pts',(0.105566661086969,-0.114256827072005,
2.17130745036735));
#21805=CARTESIAN_POINT('Ctrl Pts',(0.106861355862433,-0.113046860913555,
2.17142709209935));
#21806=CARTESIAN_POINT('Ctrl Pts',(0.111131628690177,-0.108917129366686,
2.17183073280626));
#21807=CARTESIAN_POINT('Ctrl Pts',(0.114010232381242,-0.105900149115265,
2.17211803421125));
#21808=CARTESIAN_POINT('Ctrl Pts',(0.117344395061399,-0.102112032106714,
2.17247226249401));
#21809=CARTESIAN_POINT('Ctrl Pts',(0.117919169473969,-0.101447738109457,
2.17253414778933));
#21810=CARTESIAN_POINT('Ctrl Pts',(0.118858433709445,-0.100343418598042,
2.17263666550434));
#21811=CARTESIAN_POINT('Ctrl Pts',(0.119226186195294,-0.099906183138633,
2.17267716387004));
#21812=CARTESIAN_POINT('Ctrl Pts',(0.119886027097854,-0.0991128403745894,
2.17275048725313));
#21813=CARTESIAN_POINT('Ctrl Pts',(0.120178960001454,-0.0987574411628452,
2.17278327749431));
#21814=CARTESIAN_POINT('Ctrl Pts',(0.120802671555645,-0.0979938420759882,
2.17285361142018));
#21815=CARTESIAN_POINT('Ctrl Pts',(0.121132968214345,-0.0975852577947737,
2.17289117394836));
#21816=CARTESIAN_POINT('Ctrl Pts',(0.122024630948541,-0.0964707489380403,
2.17299344669418));
#21817=CARTESIAN_POINT('Ctrl Pts',(0.122581929843276,-0.0957616121994802,
2.17305831772651));
#21818=CARTESIAN_POINT('Ctrl Pts',(0.125442527249752,-0.0920557459832751,
2.1733963285068));
#21819=CARTESIAN_POINT('Ctrl Pts',(0.127642016235695,-0.0889808917727768,
2.17367347781928));
#21820=CARTESIAN_POINT('Ctrl Pts',(0.137939983336804,-0.0734159577205989,
2.17506207928698));
#21821=CARTESIAN_POINT('Ctrl Pts',(0.144327768023264,-0.0598889390220219,
2.17623513251602));
#21822=CARTESIAN_POINT('Ctrl Pts',(0.150011388456629,-0.0413819418323274,
2.17771495930309));
#21823=CARTESIAN_POINT('Ctrl Pts',(0.151141339699327,-0.0370430362492653,
2.17805272408048));
#21824=CARTESIAN_POINT('Ctrl Pts',(0.152221410351436,-0.0320137911054857,
2.17842952082074));
#21825=CARTESIAN_POINT('Ctrl Pts',(0.152356258021773,-0.031365765958149,
2.17847779380394));
#21826=CARTESIAN_POINT('Ctrl Pts',(0.152551396518006,-0.0303970453885356,
2.17854952242973));
#21827=CARTESIAN_POINT('Ctrl Pts',(0.152614819048364,-0.0300770005169151,
2.17857314955833));
#21828=CARTESIAN_POINT('Ctrl Pts',(0.152726543271103,-0.0295037610728202,
2.17861533967494));
#21829=CARTESIAN_POINT('Ctrl Pts',(0.152775222829793,-0.029250644947397,
2.17863392378123));
#21830=CARTESIAN_POINT('Ctrl Pts',(0.152879244208359,-0.0287024273093525,
2.17867407666903));
#21831=CARTESIAN_POINT('Ctrl Pts',(0.152934360729109,-0.028407287017642,
2.17869563252361));
#21832=CARTESIAN_POINT('Ctrl Pts',(0.153085807742378,-0.0275830951462181,
2.17875566278421));
#21833=CARTESIAN_POINT('Ctrl Pts',(0.153180251145834,-0.0270536938641554,
2.17879403191009));
#21834=CARTESIAN_POINT('Ctrl Pts',(0.153710047501832,-0.0239921826632196,
2.17901487929414));
#21835=CARTESIAN_POINT('Ctrl Pts',(0.154085390504345,-0.0214498960006938,
2.17919416718502));
#21836=CARTESIAN_POINT('Ctrl Pts',(0.156187133044349,-0.00427971991433805,
2.18038468284168));
#21837=CARTESIAN_POINT('Ctrl Pts',(0.155891464619304,0.0105213047301718,
2.18131828246991));
#21838=CARTESIAN_POINT('Ctrl Pts',(0.153218677638573,0.0268940111399787,
2.18243276336411));
#21839=CARTESIAN_POINT('Ctrl Pts',(0.152886698950583,0.0287212102522075,
2.18255819625035));
#21840=CARTESIAN_POINT('Ctrl Pts',(0.151722591172594,0.0345345911704988,
2.18296134794165));
#21841=CARTESIAN_POINT('Ctrl Pts',(0.150766689182046,0.0384939363462242,
2.18324213517661));
#21842=CARTESIAN_POINT('Ctrl Pts',(0.149418884779932,0.0432499693966803,
2.18358916198354));
#21843=CARTESIAN_POINT('Ctrl Pts',(0.149174070315314,0.0440869558046919,
2.18365060252135));
#21844=CARTESIAN_POINT('Ctrl Pts',(0.148757808466609,0.0454669230190861,
2.18375253466676));
#21845=CARTESIAN_POINT('Ctrl Pts',(0.148590391998414,0.0460111079928682,
2.18379289489307));
#21846=CARTESIAN_POINT('Ctrl Pts',(0.14828219631769,0.0469936670019351,
2.1838660700102));
#21847=CARTESIAN_POINT('Ctrl Pts',(0.148142450514052,0.0474323605824498,
2.18389885076099));
#21848=CARTESIAN_POINT('Ctrl Pts',(0.147838637253949,0.0483716586027706,
2.18396927685111));
#21849=CARTESIAN_POINT('Ctrl Pts',(0.147673970629489,0.0488720616201343,
2.18400694152024));
#21850=CARTESIAN_POINT('Ctrl Pts',(0.147218469819651,0.0502329540024445,
2.18410977760331));
#21851=CARTESIAN_POINT('Ctrl Pts',(0.146922639400423,0.051091736028941,
2.18417511285159));
#21852=CARTESIAN_POINT('Ctrl Pts',(0.1453279802132,0.0555925532874534,2.18451990580471));
#21853=CARTESIAN_POINT('Ctrl Pts',(0.143901316198438,0.0591874994254227,
2.18480356770326));
#21854=CARTESIAN_POINT('Ctrl Pts',(0.136365909383786,0.076287577932957,
2.18619492745192));
#21855=CARTESIAN_POINT('Ctrl Pts',(0.128482064653812,0.0889250636299577,
2.1873631202283));
#21856=CARTESIAN_POINT('Ctrl Pts',(0.116067083713127,0.103653319518036,
2.1888351851711));
#21857=CARTESIAN_POINT('Ctrl Pts',(0.113056099038681,0.106929444877068,
2.1891703150065));
#21858=CARTESIAN_POINT('Ctrl Pts',(0.109440909998381,0.110539252576792,
2.18954453433145));
#21859=CARTESIAN_POINT('Ctrl Pts',(0.108970332334835,0.11100317947858,2.18959272662328));
#21860=CARTESIAN_POINT('Ctrl Pts',(0.108263164400714,0.111691521785521,
2.18966435914577));
#21861=CARTESIAN_POINT('Ctrl Pts',(0.10802881009828,0.111918206735427,2.18968797020011));
#21862=CARTESIAN_POINT('Ctrl Pts',(0.107607925604363,0.112322763835223,
2.18973014300443));
#21863=CARTESIAN_POINT('Ctrl Pts',(0.107421665344474,0.112500909981275,
2.18974872579851));
#21864=CARTESIAN_POINT('Ctrl Pts',(0.107017352793025,0.112885689708462,
2.18978888882276));
#21865=CARTESIAN_POINT('Ctrl Pts',(0.106799145048987,0.113092154284681,
2.18981045606867));
#21866=CARTESIAN_POINT('Ctrl Pts',(0.106188123902481,0.113666946843727,
2.18987055011425));
#21867=CARTESIAN_POINT('Ctrl Pts',(0.10579398876875,0.11403387402876,2.18990897127112));
#21868=CARTESIAN_POINT('Ctrl Pts',(0.103499602418438,0.116147739827136,
2.19013071754495));
#21869=CARTESIAN_POINT('Ctrl Pts',(0.10155786521983,0.11784934145035,2.19031082183706));
#21870=CARTESIAN_POINT('Ctrl Pts',(0.0882665781434985,0.12892425317794,
2.19150132377397));
#21871=CARTESIAN_POINT('Ctrl Pts',(0.0756774914708116,0.136694837702149,
2.19243435912003));
#21872=CARTESIAN_POINT('Ctrl Pts',(0.0604678209613985,0.143328098318324,
2.19354911717698));
#21873=CARTESIAN_POINT('Ctrl Pts',(0.058740016146079,0.144044823772724,
2.19367546635138));
#21874=CARTESIAN_POINT('Ctrl Pts',(0.0532249452615636,0.146216849267518,
2.19407857004239));
#21875=CARTESIAN_POINT('Ctrl Pts',(0.0493937358494896,0.147555127867977,
2.19435835639163));
#21876=CARTESIAN_POINT('Ctrl Pts',(0.0446820724337822,0.148996890554439,
2.19470426613834));
#21877=CARTESIAN_POINT('Ctrl Pts',(0.0438471651956738,0.149244721987937,
2.19476562711256));
#21878=CARTESIAN_POINT('Ctrl Pts',(0.0424634148965213,0.149642857035555,
2.19486745449038));
#21879=CARTESIAN_POINT('Ctrl Pts',(0.0419157416018176,0.149797185743918,
2.19490778998844));
#21880=CARTESIAN_POINT('Ctrl Pts',(0.0409234288375339,0.150070941330244,
2.19498093864806));
#21881=CARTESIAN_POINT('Ctrl Pts',(0.040479080290673,0.15019140624561,2.19501371778359));
#21882=CARTESIAN_POINT('Ctrl Pts',(0.0400330342233529,0.150310208144181,
2.19504664756934));
#21883=CARTESIAN_POINT('Ctrl Pts',(0.0400318606011181,0.150310520717236,
2.19504673421333));
#21884=CARTESIAN_POINT('Ctrl Pts',(0.0400295202429271,0.150311143999967,
2.19504690699325));
#21885=CARTESIAN_POINT('Ctrl Pts',(0.0400283532855143,0.150311454768783,
2.19504699314555));
#21886=CARTESIAN_POINT('Ctrl Pts',(0.0400260259182125,0.150312074533738,
2.1950471649671));
#21887=CARTESIAN_POINT('Ctrl Pts',(0.0400248655008104,0.150312383532041,
2.19504725063691));
#21888=CARTESIAN_POINT('Ctrl Pts',(0.040022551155019,0.15031299977204,2.19504742149782));
#21889=CARTESIAN_POINT('Ctrl Pts',(0.0400213972215343,0.150313307015252,
2.19504750668929));
#21890=CARTESIAN_POINT('Ctrl Pts',(0.0400190957973346,0.150313919757863,
2.19504767659692));
#21891=CARTESIAN_POINT('Ctrl Pts',(0.0400179482970169,0.150314225259976,
2.19504776131378));
#21892=CARTESIAN_POINT('Ctrl Pts',(0.0400156596820435,0.150314834536065,
2.19504793027641));
#21893=CARTESIAN_POINT('Ctrl Pts',(0.0400145185607507,0.150315138311965,
2.19504801452267));
#21894=CARTESIAN_POINT('Ctrl Pts',(0.0400122426538242,0.150315744149407,
2.19504818254776));
#21895=CARTESIAN_POINT('Ctrl Pts',(0.0400111078601173,0.150316046213252,
2.19504826632719));
#21896=CARTESIAN_POINT('Ctrl Pts',(0.0400088445550172,0.150316648641245,
2.19504843342258));
#21897=CARTESIAN_POINT('Ctrl Pts',(0.0400077160362043,0.15031694900752,
2.19504851673907));
#21898=CARTESIAN_POINT('Ctrl Pts',(0.0400054652336443,0.150317548053405,
2.19504868291207));
#21899=CARTESIAN_POINT('Ctrl Pts',(0.0400043429398311,0.150317846735843,
2.19504876576931));
#21900=CARTESIAN_POINT('Ctrl Pts',(0.0400021045351428,0.150318442428375,
2.19504893102764));
#21901=CARTESIAN_POINT('Ctrl Pts',(0.0400009884150471,0.150318739441071,
2.19504901342941));
#21902=CARTESIAN_POINT('Ctrl Pts',(0.0394966174363725,0.150452952480337,
2.19508625058655));
#21903=CARTESIAN_POINT('Ctrl Pts',(0.038992698963713,0.150584338874641,
2.19512348679596));
#21904=CARTESIAN_POINT('Ctrl Pts',(0.037626282433313,0.15093328527227,2.19522454917707));
#21905=CARTESIAN_POINT('Ctrl Pts',(0.0367625739951586,0.151145978527453,
2.19528853096926));
#21906=CARTESIAN_POINT('Ctrl Pts',(0.0348421117614178,0.151601468890245,
2.1954310370156));
#21907=CARTESIAN_POINT('Ctrl Pts',(0.0337845563873765,0.151840645944173,
2.19550967375551));
#21908=CARTESIAN_POINT('Ctrl Pts',(0.0305611906194461,0.152534301925005,
2.19574988237738));
#21909=CARTESIAN_POINT('Ctrl Pts',(0.0283881884900447,0.152953618688722,
2.19591254353701));
#21910=CARTESIAN_POINT('Ctrl Pts',(0.011358084511525,0.15586446272202,2.1971934091327));
#21911=CARTESIAN_POINT('Ctrl Pts',(-0.0037795157964463,0.15623150014638,
2.19837911666908));
#21912=CARTESIAN_POINT('Ctrl Pts',(-0.01976205936095,0.154293056099371,
2.19961193071215));
#21913=CARTESIAN_POINT('Ctrl Pts',(-0.0207942078137085,0.154157345448689,
2.19969140692819));
#21914=CARTESIAN_POINT('Ctrl Pts',(-0.0255731063562977,0.153480127833509,
2.20005854210484));
#21915=CARTESIAN_POINT('Ctrl Pts',(-0.0293010451904266,0.152812264396642,
2.20034255277593));
#21916=CARTESIAN_POINT('Ctrl Pts',(-0.0336146562908762,0.151875776124736,
2.20066570901339));
#21917=CARTESIAN_POINT('Ctrl Pts',(-0.0342272566340571,0.151738892280126,
2.20071147160936));
#21918=CARTESIAN_POINT('Ctrl Pts',(-0.0351543185566328,0.151525842834467,
2.20078050998261));
#21919=CARTESIAN_POINT('Ctrl Pts',(-0.0354693887289193,0.151452400536461,
2.20080393550929));
#21920=CARTESIAN_POINT('Ctrl Pts',(-0.036034884310486,0.15131872306628,
2.20084590953956));
#21921=CARTESIAN_POINT('Ctrl Pts',(-0.0362853899089312,0.151258848733661,
2.20086447823018));
#21922=CARTESIAN_POINT('Ctrl Pts',(-0.0368296030020982,0.15112734442563,
2.20090476303684));
#21923=CARTESIAN_POINT('Ctrl Pts',(-0.0371232499457968,0.151055480563059,
2.20092646549189));
#21924=CARTESIAN_POINT('Ctrl Pts',(-0.0379478727344393,0.150851121771983,
2.20098731857148));
#21925=CARTESIAN_POINT('Ctrl Pts',(-0.0384783688082745,0.150716678382996,
2.20102635919234));
#21926=CARTESIAN_POINT('Ctrl Pts',(-0.0416499751499815,0.149895062130021,
2.2012591843144));
#21927=CARTESIAN_POINT('Ctrl Pts',(-0.0442735475237671,0.14914122678078,
2.20144935995401));
#21928=CARTESIAN_POINT('Ctrl Pts',(-0.0526057991022602,0.146507817854672,
2.20204962024977));
#21929=CARTESIAN_POINT('Ctrl Pts',(-0.0582190549626605,0.144368577403726,
2.20244845233402));
#21930=CARTESIAN_POINT('Ctrl Pts',(-0.0636886613526676,0.141913906700877,
2.20284414165342));
#21931=CARTESIAN_POINT('Origin',(0.,0.,-0.129405622560373));
#21932=CARTESIAN_POINT('',(-0.0636886081915498,0.141913930558713,2.28656840831392));
#21933=CARTESIAN_POINT('',(-0.0636886258329926,0.141913922641526,2.27279455889198));
#21934=CARTESIAN_POINT('',(-0.0636886258329924,0.141913922641526,-0.129405622560373));
#21935=CARTESIAN_POINT('',(-0.155549959235335,-0.000112613879107687,2.22940562256037));
#21936=CARTESIAN_POINT('Ctrl Pts',(-0.0636886081915498,0.141913930558713,
2.28656840831392));
#21937=CARTESIAN_POINT('Ctrl Pts',(-0.0573573513556864,0.144755293167668,
2.28611116580639));
#21938=CARTESIAN_POINT('Ctrl Pts',(-0.0508393810386415,0.147171438272272,
2.28565645924617));
#21939=CARTESIAN_POINT('Ctrl Pts',(-0.0379348625092741,0.150993842402475,
2.28475646093028));
#21940=CARTESIAN_POINT('Ctrl Pts',(-0.0315829264545988,0.152448992633366,
2.28431354593895));
#21941=CARTESIAN_POINT('Ctrl Pts',(-0.0241771909634659,0.153662799599024,
2.28378773977956));
#21942=CARTESIAN_POINT('Ctrl Pts',(-0.0231937821712976,0.153814306651298,
2.28371773837351));
#21943=CARTESIAN_POINT('Ctrl Pts',(-0.0216149122255629,0.154042066862606,
2.28360503193009));
#21944=CARTESIAN_POINT('Ctrl Pts',(-0.0210203335993272,0.154124327576502,
2.28356251619436));
#21945=CARTESIAN_POINT('Ctrl Pts',(-0.019964169240911,0.154264224044377,
2.28348685968897));
#21946=CARTESIAN_POINT('Ctrl Pts',(-0.0195027702404401,0.15432323486059,
2.28345376260884));
#21947=CARTESIAN_POINT('Ctrl Pts',(-0.0185412962912334,0.154441822231064,
2.2833846959364));
#21948=CARTESIAN_POINT('Ctrl Pts',(-0.0180411835922698,0.154501041439202,
2.28334871551462));
#21949=CARTESIAN_POINT('Ctrl Pts',(-0.0167426573252954,0.154648411431805,
2.28325514536027));
#21950=CARTESIAN_POINT('Ctrl Pts',(-0.0159438416586882,0.154732807125449,
2.2831974384754));
#21951=CARTESIAN_POINT('Ctrl Pts',(-0.0124832655330437,0.155071338762232,
2.28294678745214));
#21952=CARTESIAN_POINT('Ctrl Pts',(-0.00981600324762601,0.155262991260491,
2.28275190462622));
#21953=CARTESIAN_POINT('Ctrl Pts',(-0.00273555764848378,0.155588579095533,
2.2822296970878));
#21954=CARTESIAN_POINT('Ctrl Pts',(0.00168037847960483,0.155603531053496,
2.28189894091815));
#21955=CARTESIAN_POINT('Ctrl Pts',(0.0184849974486085,0.154945035350905,
2.28062171486504));
#21956=CARTESIAN_POINT('Ctrl Pts',(0.0307753701326118,0.152978736820492,
2.27964472851734));
#21957=CARTESIAN_POINT('Ctrl Pts',(0.0464213459760401,0.148512050827812,
2.27840629214938));
#21958=CARTESIAN_POINT('Ctrl Pts',(0.0501010675833204,0.147311438723959,
2.27811586792665));
#21959=CARTESIAN_POINT('Ctrl Pts',(0.0543247881584176,0.145756708838042,
2.27778634090322));
#21960=CARTESIAN_POINT('Ctrl Pts',(0.0549157150812203,0.145535099043165,
2.27774032736285));
#21961=CARTESIAN_POINT('Ctrl Pts',(0.0558082223386521,0.145194180244331,
2.27767098375387));
#21962=CARTESIAN_POINT('Ctrl Pts',(0.0561107955107271,0.145077518209393,
2.27764750199097));
#21963=CARTESIAN_POINT('Ctrl Pts',(0.0566531351358926,0.144866459797971,
2.27760546355121));
#21964=CARTESIAN_POINT('Ctrl Pts',(0.0568930325451477,0.144772413623429,
2.27758688644834));
#21965=CARTESIAN_POINT('Ctrl Pts',(0.0574134757671532,0.144566892573746,
2.27754662409336));
#21966=CARTESIAN_POINT('Ctrl Pts',(0.057693930331708,0.144455197328433,
2.27752495232895));
#21967=CARTESIAN_POINT('Ctrl Pts',(0.0584797527270391,0.144139578177909,
2.27746429334337));
#21968=CARTESIAN_POINT('Ctrl Pts',(0.0589843835067336,0.14393381118546,
2.27742541495191));
#21969=CARTESIAN_POINT('Ctrl Pts',(0.0619707373189326,0.142697759495357,
2.27719572147635));
#21970=CARTESIAN_POINT('Ctrl Pts',(0.0644267013975265,0.141605880339322,
2.2770084026159));
#21971=CARTESIAN_POINT('Ctrl Pts',(0.0800739870305123,0.13415791258341,
2.27581742889312));
#21972=CARTESIAN_POINT('Ctrl Pts',(0.0923411546455998,0.12602938048,2.27488888769079));
#21973=CARTESIAN_POINT('Ctrl Pts',(0.104808348480506,0.114957069883973,
2.273768420861));
#21974=CARTESIAN_POINT('Ctrl Pts',(0.106298599288021,0.113580478595294,
2.273631288463));
#21975=CARTESIAN_POINT('Ctrl Pts',(0.110561457056521,0.109485350054613,
2.27322871837826));
#21976=CARTESIAN_POINT('Ctrl Pts',(0.113259539574259,0.106691846093292,
2.27296068672493));
#21977=CARTESIAN_POINT('Ctrl Pts',(0.116479193483515,0.103098441522035,
2.27262190544415));
#21978=CARTESIAN_POINT('Ctrl Pts',(0.117101852740555,0.102390659602416,
2.27255545459439));
#21979=CARTESIAN_POINT('Ctrl Pts',(0.118071101348591,0.101268500944805,
2.27245050778179));
#21980=CARTESIAN_POINT('Ctrl Pts',(0.11842203883526,0.100857894891781,2.27241219155885));
#21981=CARTESIAN_POINT('Ctrl Pts',(0.119038035523508,0.100129515275094,
2.27234436583517));
#21982=CARTESIAN_POINT('Ctrl Pts',(0.119303980194252,0.0998124943795168,
2.27231489290808));
#21983=CARTESIAN_POINT('Ctrl Pts',(0.119910650235786,0.0990834211175232,
2.27224721836863));
#21984=CARTESIAN_POINT('Ctrl Pts',(0.120250520706898,0.0986706675606195,
2.27220898259578));
#21985=CARTESIAN_POINT('Ctrl Pts',(0.121184306229015,0.0975246473260161,
2.27210302625334));
#21986=CARTESIAN_POINT('Ctrl Pts',(0.121773678588445,0.0967877267137006,
2.27203512478758));
#21987=CARTESIAN_POINT('Ctrl Pts',(0.125066621541656,0.0925927119457553,
2.27164982537739));
#21988=CARTESIAN_POINT('Ctrl Pts',(0.127629301959572,0.0890270984659791,
2.27132695774074));
#21989=CARTESIAN_POINT('Ctrl Pts',(0.135280764356334,0.0773706034538519,
2.27028440093614));
#21990=CARTESIAN_POINT('Ctrl Pts',(0.139776167646088,0.0689178634916385,
2.2695456545424));
#21991=CARTESIAN_POINT('Ctrl Pts',(0.146972611835888,0.0517410732806681,
2.26810146465739));
#21992=CARTESIAN_POINT('Ctrl Pts',(0.149739778504839,0.0430828345014801,
2.26739934261687));
#21993=CARTESIAN_POINT('Ctrl Pts',(0.151887410841179,0.0335631738011914,
2.26668414797492));
#21994=CARTESIAN_POINT('Ctrl Pts',(0.152033819262679,0.0328936172347227,
2.26663414585285));
#21995=CARTESIAN_POINT('Ctrl Pts',(0.152244370562465,0.0318992742220397,
2.26656035531206));
#21996=CARTESIAN_POINT('Ctrl Pts',(0.152311907121558,0.0315752279229992,
2.26653638098573));
#21997=CARTESIAN_POINT('Ctrl Pts',(0.152430293916657,0.0309979788080861,
2.26649380692038));
#21998=CARTESIAN_POINT('Ctrl Pts',(0.152481548328445,0.0307448632597523,
2.26647518449148));
#21999=CARTESIAN_POINT('Ctrl Pts',(0.152590420698477,0.0302002368390077,
2.26643521354255));
#22000=CARTESIAN_POINT('Ctrl Pts',(0.152647833676518,0.0299086889042221,
2.26641387679954));
#22001=CARTESIAN_POINT('Ctrl Pts',(0.152804054693212,0.0291032170932399,
2.26635509099754));
#22002=CARTESIAN_POINT('Ctrl Pts',(0.152901106425012,0.028588949804786,
2.26631774020638));
#22003=CARTESIAN_POINT('Ctrl Pts',(0.153418950685478,0.0257668606691734,
2.26611372178914));
#22004=CARTESIAN_POINT('Ctrl Pts',(0.153790120119515,0.0234500766939515,
2.26594970206205));
#22005=CARTESIAN_POINT('Ctrl Pts',(0.156078857414954,0.00675402169688695,
2.264786684186));
#22006=CARTESIAN_POINT('Ctrl Pts',(0.156029241330102,-0.0078240706720093,
2.26386612154625));
#22007=CARTESIAN_POINT('Ctrl Pts',(0.153529204700032,-0.025173349535694,
2.26269175450212));
#22008=CARTESIAN_POINT('Ctrl Pts',(0.153011820533273,-0.0281477418916587,
2.26248783645466));
#22009=CARTESIAN_POINT('Ctrl Pts',(0.152317642101105,-0.0315490688947975,
2.26225060191487));
#22010=CARTESIAN_POINT('Ctrl Pts',(0.152225087780352,-0.0319926630206638,
2.26221958289814));
#22011=CARTESIAN_POINT('Ctrl Pts',(0.151486894407884,-0.0354549377299227,
2.26197683609599));
#22012=CARTESIAN_POINT('Ctrl Pts',(0.15075350359295,-0.0384540073966083,
2.2617627292832));
#22013=CARTESIAN_POINT('Ctrl Pts',(0.149696803417965,-0.0422781922462996,
2.26148383369467));
#22014=CARTESIAN_POINT('Ctrl Pts',(0.149454979594136,-0.0431252537452708,
2.26142168374751));
#22015=CARTESIAN_POINT('Ctrl Pts',(0.149058744623597,-0.0444698149755887,
2.26132241417873));
#22016=CARTESIAN_POINT('Ctrl Pts',(0.148909003978465,-0.0449686814889762,
2.26128544666474));
#22017=CARTESIAN_POINT('Ctrl Pts',(0.14863540628562,-0.0458638296830602,
2.26121886446981));
#22018=CARTESIAN_POINT('Ctrl Pts',(0.148512462229922,-0.0462603872785091,
2.26118927986567));
#22019=CARTESIAN_POINT('Ctrl Pts',(0.148220924980014,-0.0471876034538367,
2.26111989695573));
#22020=CARTESIAN_POINT('Ctrl Pts',(0.148051068133613,-0.047717855476158,
2.26108005757885));
#22021=CARTESIAN_POINT('Ctrl Pts',(0.147553727050576,-0.0492422138340347,
2.26096505658488));
#22022=CARTESIAN_POINT('Ctrl Pts',(0.14721905687228,-0.0502339246315254,
2.26088965990593));
#22023=CARTESIAN_POINT('Ctrl Pts',(0.144699197162619,-0.0574593698189089,
2.26033597846919));
#22024=CARTESIAN_POINT('Ctrl Pts',(0.142129228447879,-0.0635507337839902,
2.25984495752987));
#22025=CARTESIAN_POINT('Ctrl Pts',(0.133612089324095,-0.0806170288581316,
2.25839672987307));
#22026=CARTESIAN_POINT('Ctrl Pts',(0.126723149867643,-0.091063143806636,
2.25741442235511));
#22027=CARTESIAN_POINT('Ctrl Pts',(0.116176032218369,-0.103507058960591,
2.25617307767612));
#22028=CARTESIAN_POINT('Ctrl Pts',(0.113582224672677,-0.106346914373026,
2.25588454096309));
#22029=CARTESIAN_POINT('Ctrl Pts',(0.110443628544838,-0.109537229009839,
2.25555688116506));
#22030=CARTESIAN_POINT('Ctrl Pts',(0.109998944927597,-0.10998377960677,
2.25551093502715));
#22031=CARTESIAN_POINT('Ctrl Pts',(0.109321461395658,-0.110655888333206,
2.255441671038));
#22032=CARTESIAN_POINT('Ctrl Pts',(0.10909065747102,-0.110883434300372,
2.25541820203834));
#22033=CARTESIAN_POINT('Ctrl Pts',(0.108675084841261,-0.111290587335218,
2.25537617645301));
#22034=CARTESIAN_POINT('Ctrl Pts',(0.108490580532803,-0.111470457224127,
2.25535759949977));
#22035=CARTESIAN_POINT('Ctrl Pts',(0.108088841023171,-0.111860163437116,
2.25531732670021));
#22036=CARTESIAN_POINT('Ctrl Pts',(0.107871441981383,-0.112069825229613,
2.25529564439006));
#22037=CARTESIAN_POINT('Ctrl Pts',(0.107259547250416,-0.112656512432037,
2.25523492308035));
#22038=CARTESIAN_POINT('Ctrl Pts',(0.106863670928656,-0.11303210220632,
2.25519599328371));
#22039=CARTESIAN_POINT('Ctrl Pts',(0.104497439687509,-0.115253533307624,
2.2549653419878));
#22040=CARTESIAN_POINT('Ctrl Pts',(0.102481120515078,-0.11705004981435,
2.2547771510607));
#22041=CARTESIAN_POINT('Ctrl Pts',(0.0892450389667769,-0.128238833966699,
2.25358621462346));
#22042=CARTESIAN_POINT('Ctrl Pts',(0.0767934630560027,-0.136061543583205,
2.25265830472956));
#22043=CARTESIAN_POINT('Ctrl Pts',(0.0615688317115607,-0.142860910162098,
2.25153783002241));
#22044=CARTESIAN_POINT('Ctrl Pts',(0.0596908032700508,-0.14365572800412,
2.25139997822199));
#22045=CARTESIAN_POINT('Ctrl Pts',(0.0542046407851404,-0.14585142381349,
2.2509975008022));
#22046=CARTESIAN_POINT('Ctrl Pts',(0.0505594023373035,-0.147154760200364,
2.25073031212824));
#22047=CARTESIAN_POINT('Ctrl Pts',(0.0459717518387923,-0.148604465522027,
2.25039247750613));
#22048=CARTESIAN_POINT('Ctrl Pts',(0.0450713584129952,-0.148880024588584,
2.25032610153214));
#22049=CARTESIAN_POINT('Ctrl Pts',(0.0436508872736459,-0.14930068318768,
2.25022124944924));
#22050=CARTESIAN_POINT('Ctrl Pts',(0.0431324499660888,-0.149451282050877,
2.2501829525775));
#22051=CARTESIAN_POINT('Ctrl Pts',(0.0422153069090767,-0.149712529756639,
2.25011514850273));
#22052=CARTESIAN_POINT('Ctrl Pts',(0.0418169216190779,-0.149824292969449,
2.25008567779496));
#22053=CARTESIAN_POINT('Ctrl Pts',(0.0409128456458104,-0.150074036135658,
2.25001875463655));
#22054=CARTESIAN_POINT('Ctrl Pts',(0.0404068961543966,-0.150211051496321,
2.24998127134972));
#22055=CARTESIAN_POINT('Ctrl Pts',(0.0390259360379312,-0.150577545197679,
2.24987887289088));
#22056=CARTESIAN_POINT('Ctrl Pts',(0.0381496126816666,-0.150801948891273,
2.24981379505647));
#22057=CARTESIAN_POINT('Ctrl Pts',(0.0361971291219298,-0.151283821648048,
2.24966856057029));
#22058=CARTESIAN_POINT('Ctrl Pts',(0.0351200875582728,-0.15153747451188,
2.24958828511914));
#22059=CARTESIAN_POINT('Ctrl Pts',(0.0266612197224183,-0.153434591836196,
2.24895646394655));
#22060=CARTESIAN_POINT('Ctrl Pts',(0.019172334738909,-0.154548965718495,
2.24838827975225));
#22061=CARTESIAN_POINT('Ctrl Pts',(0.00701306501031108,-0.15546087879246,
2.24745370584204));
#22062=CARTESIAN_POINT('Ctrl Pts',(0.00237996351554062,-0.155600772695253,
2.24709500198779));
#22063=CARTESIAN_POINT('Ctrl Pts',(-0.0113164306047466,-0.155402435418559,
2.24603275093491));
#22064=CARTESIAN_POINT('Ctrl Pts',(-0.0203527782042444,-0.154479058725245,
2.24532871700704));
#22065=CARTESIAN_POINT('Ctrl Pts',(-0.0303976650125656,-0.152555336832543,
2.24457263715985));
#22066=CARTESIAN_POINT('Ctrl Pts',(-0.0315348394857559,-0.152324334722878,
2.2444874501976));
#22067=CARTESIAN_POINT('Ctrl Pts',(-0.0330826262982139,-0.151991845179949,
2.24437215725131));
#22068=CARTESIAN_POINT('Ctrl Pts',(-0.0334955283689098,-0.151901384966118,
2.24434146434602));
#22069=CARTESIAN_POINT('Ctrl Pts',(-0.0341495492331672,-0.151755303077253,
2.24429295452869));
#22070=CARTESIAN_POINT('Ctrl Pts',(-0.0343909086614062,-0.151700788161075,
2.24427507554927));
#22071=CARTESIAN_POINT('Ctrl Pts',(-0.0348877643931869,-0.151587318558925,
2.24423831931851));
#22072=CARTESIAN_POINT('Ctrl Pts',(-0.0351432417345333,-0.15152829377319,
2.24421944662984));
#22073=CARTESIAN_POINT('Ctrl Pts',(-0.0357492293967447,-0.151386673042685,
2.24417474261723));
#22074=CARTESIAN_POINT('Ctrl Pts',(-0.0360996073778895,-0.151303504690462,
2.24414894399397));
#22075=CARTESIAN_POINT('Ctrl Pts',(-0.0372692919054918,-0.151021565156767,
2.2440629729643));
#22076=CARTESIAN_POINT('Ctrl Pts',(-0.0380872904848871,-0.150817345321459,
2.24400310314584));
#22077=CARTESIAN_POINT('Ctrl Pts',(-0.0478919991860359,-0.148284661529589,
2.24328807669048));
#22078=CARTESIAN_POINT('Ctrl Pts',(-0.056656109061988,-0.145162421860327,
2.24267451143852));
#22079=CARTESIAN_POINT('Ctrl Pts',(-0.0763483297742828,-0.136089587162927,
2.24124642652981));
#22080=CARTESIAN_POINT('Ctrl Pts',(-0.0869441918015212,-0.12957661911029,
2.24043556295722));
#22081=CARTESIAN_POINT('Ctrl Pts',(-0.0979321353685671,-0.120862561180529,
2.23945970866766));
#22082=CARTESIAN_POINT('Ctrl Pts',(-0.0991937926249771,-0.119829265982124,
2.23934548715271));
#22083=CARTESIAN_POINT('Ctrl Pts',(-0.100909884418619,-0.118378115049075,
2.23918696625747));
#22084=CARTESIAN_POINT('Ctrl Pts',(-0.10137845885781,-0.117977078094951,
2.23914335057556));
#22085=CARTESIAN_POINT('Ctrl Pts',(-0.102177897647449,-0.117284586106956,
2.23906835806864));
#22086=CARTESIAN_POINT('Ctrl Pts',(-0.102509933327922,-0.116994489048573,
2.2390370374169));
#22087=CARTESIAN_POINT('Ctrl Pts',(-0.103173756093037,-0.116409516733341,
2.23897406711934));
#22088=CARTESIAN_POINT('Ctrl Pts',(-0.103505523224592,-0.116114625206865,
2.23894241697771));
#22089=CARTESIAN_POINT('Ctrl Pts',(-0.104275045865188,-0.115424715628329,
2.23886858482094));
#22090=CARTESIAN_POINT('Ctrl Pts',(-0.104711824018052,-0.115028622790872,
2.23882635787885));
#22091=CARTESIAN_POINT('Ctrl Pts',(-0.106040249937883,-0.113810101975912,
2.23869693568919));
#22092=CARTESIAN_POINT('Ctrl Pts',(-0.106924519525045,-0.112979736625554,
2.23860940422635));
#22093=CARTESIAN_POINT('Ctrl Pts',(-0.108944428928519,-0.111038004683485,
2.23840618681019));
#22094=CARTESIAN_POINT('Ctrl Pts',(-0.110072913868205,-0.109919426697514,
2.2382901945484));
#22095=CARTESIAN_POINT('Ctrl Pts',(-0.113826445543424,-0.106083076171633,
2.23789585560581));
#22096=CARTESIAN_POINT('Ctrl Pts',(-0.116369365902476,-0.103287197261522,
2.23761415878912));
#22097=CARTESIAN_POINT('Ctrl Pts',(-0.122020273007504,-0.0966003413014661,
2.23695319887407));
#22098=CARTESIAN_POINT('Ctrl Pts',(-0.125048203122969,-0.0926472501124097,
2.23657166515618));
#22099=CARTESIAN_POINT('Ctrl Pts',(-0.134497342267141,-0.0790020291946222,
2.23528941105982));
#22100=CARTESIAN_POINT('Ctrl Pts',(-0.140022341167246,-0.068736020863521,
2.23437688134712));
#22101=CARTESIAN_POINT('Ctrl Pts',(-0.144753114888704,-0.0569516885847873,
2.23343939579434));
#22102=CARTESIAN_POINT('Ctrl Pts',(-0.14514342647292,-0.055949486392273,
2.23336051379335));
#22103=CARTESIAN_POINT('Ctrl Pts',(-0.145668050126691,-0.0545599628760283,
2.23325238773368));
#22104=CARTESIAN_POINT('Ctrl Pts',(-0.145811261042839,-0.0541760698112806,
2.23322264498015));
#22105=CARTESIAN_POINT('Ctrl Pts',(-0.14603764843099,-0.0535618121466522,
2.23317526669559));
#22106=CARTESIAN_POINT('Ctrl Pts',(-0.146121799234582,-0.0533318129301595,
2.23315757404831));
#22107=CARTESIAN_POINT('Ctrl Pts',(-0.146295489809564,-0.0528535882687254,
2.23312088651856));
#22108=CARTESIAN_POINT('Ctrl Pts',(-0.146384941334058,-0.0526053332229557,
2.2331018972893));
#22109=CARTESIAN_POINT('Ctrl Pts',(-0.146598167357355,-0.0520088111325375,
2.23305640043931));
#22110=CARTESIAN_POINT('Ctrl Pts',(-0.146721334270555,-0.0516603250613235,
2.23302992873309));
#22111=CARTESIAN_POINT('Ctrl Pts',(-0.147139857263208,-0.0504625935176851,
2.23293930390087));
#22112=CARTESIAN_POINT('Ctrl Pts',(-0.147429099150707,-0.0496112060505376,
2.23287549989638));
#22113=CARTESIAN_POINT('Ctrl Pts',(-0.148110824645266,-0.0475459100635357,
2.23272209701623));
#22114=CARTESIAN_POINT('Ctrl Pts',(-0.148495795895353,-0.0463295672201016,
2.23263289047902));
#22115=CARTESIAN_POINT('Ctrl Pts',(-0.153287006421845,-0.0305177795719035,
2.23148626158064));
#22116=CARTESIAN_POINT('Ctrl Pts',(-0.155539540945981,-0.0153552451317254,
2.23052254341945));
#22117=CARTESIAN_POINT('Ctrl Pts',(-0.155549963665145,-0.000106319198765817,
2.22949944336375));
#22118=CARTESIAN_POINT('Ctrl Pts',(-0.0636886258329906,0.141913922641527,
2.21660530308003));
#22119=CARTESIAN_POINT('Ctrl Pts',(-0.073087183706925,0.137696005014694,
2.21734085213728));
#22120=CARTESIAN_POINT('Ctrl Pts',(-0.0820645472936867,0.132540662282221,
2.21807640119453));
#22121=CARTESIAN_POINT('Ctrl Pts',(-0.0904340546464224,0.126560200142888,
2.21881195025179));
#22122=CARTESIAN_POINT('Ctrl Pts',(-0.0988235076356814,0.12056548577591,
2.21954925221916));
#22123=CARTESIAN_POINT('Ctrl Pts',(-0.106601484691876,0.113742306694471,
2.22028655418654));
#22124=CARTESIAN_POINT('Ctrl Pts',(-0.113613251576689,0.106244207212309,
2.22102385615391));
#22125=CARTESIAN_POINT('Ctrl Pts',(-0.117229403188563,0.102377241157413,
2.22140410206647));
#22126=CARTESIAN_POINT('Ctrl Pts',(-0.120642374163594,0.0983313682361586,
2.22178434797902));
#22127=CARTESIAN_POINT('Ctrl Pts',(-0.123835241219437,0.0941309488538381,
2.22216459389158));
#22128=CARTESIAN_POINT('Ctrl Pts',(-0.130041164091348,0.0859666631944461,
2.22290367158083));
#22129=CARTESIAN_POINT('Ctrl Pts',(-0.135459995160728,0.077154802997613,
2.22364274927007));
#22130=CARTESIAN_POINT('Ctrl Pts',(-0.139962212458014,0.0678703291863065,
2.22438182695931));
#22131=CARTESIAN_POINT('Ctrl Pts',(-0.144454014774706,0.058607333150994,
2.22511919493992));
#22132=CARTESIAN_POINT('Ctrl Pts',(-0.148032938209205,0.0488746759435811,
2.22585656292052));
#22133=CARTESIAN_POINT('Ctrl Pts',(-0.150614199915162,0.038873709418006,
2.22659393090113));
#22134=CARTESIAN_POINT('Ctrl Pts',(-0.153193498779847,0.0288803478205996,
2.22733073817288));
#22135=CARTESIAN_POINT('Ctrl Pts',(-0.154776376478075,0.0186199611818154,
2.22806754544463));
#22136=CARTESIAN_POINT('Ctrl Pts',(-0.155327939155893,0.00830865919285778,
2.22880435271638));
#22137=CARTESIAN_POINT('Ctrl Pts',(-0.155477972965258,0.00550382126757846,
2.22900477599771));
#22138=CARTESIAN_POINT('Ctrl Pts',(-0.155551992058767,0.00269526028780381,
2.22920519927904));
#22139=CARTESIAN_POINT('Ctrl Pts',(-0.155549959235335,-0.000112613879107687,
2.22940562256037));
#22140=CARTESIAN_POINT('',(-0.155549955602241,0.000117525064441449,2.21559437743963));
#22141=CARTESIAN_POINT('Ctrl Pts',(-0.0636886613526676,0.141913906700877,
2.20284414165342));
#22142=CARTESIAN_POINT('Ctrl Pts',(-0.0715111988820138,0.138403278636249,
2.2034100497518));
#22143=CARTESIAN_POINT('Ctrl Pts',(-0.0790398862705312,0.134247499711388,
2.20397012429285));
#22144=CARTESIAN_POINT('Ctrl Pts',(-0.0879068540018532,0.128344903044612,
2.2046859425461));
#22145=CARTESIAN_POINT('Ctrl Pts',(-0.0895954112005581,0.127171895045403,
2.20482493449157));
#22146=CARTESIAN_POINT('Ctrl Pts',(-0.0943799932002816,0.123705543211883,
2.20522740700976));
#22147=CARTESIAN_POINT('Ctrl Pts',(-0.0974145178887555,0.121330342456775,
2.20549340476745));
#22148=CARTESIAN_POINT('Ctrl Pts',(-0.101075740896878,0.118238659868456,
2.20582989426555));
#22149=CARTESIAN_POINT('Ctrl Pts',(-0.101788398222784,0.117625711489505,
2.20589615703369));
#22150=CARTESIAN_POINT('Ctrl Pts',(-0.102901184799252,0.116650930639211,
2.20600086212419));
#22151=CARTESIAN_POINT('Ctrl Pts',(-0.103305070783896,0.116293403893325,
2.20603912597705));
#22152=CARTESIAN_POINT('Ctrl Pts',(-0.104015383203998,0.115658003018652,
2.2061068886626));
#22153=CARTESIAN_POINT('Ctrl Pts',(-0.104322577905872,0.115380992101588,
2.2061363511242));
#22154=CARTESIAN_POINT('Ctrl Pts',(-0.104631399187023,0.115100272883497,
2.2061661292456));
#22155=CARTESIAN_POINT('Ctrl Pts',(-0.104634136955246,0.115097784067811,
2.20616639324787));
#22156=CARTESIAN_POINT('Ctrl Pts',(-0.104640889228299,0.115091645356859,
2.20616704439912));
#22157=CARTESIAN_POINT('Ctrl Pts',(-0.104644903632025,0.115087995348214,
2.20616743155299));
#22158=CARTESIAN_POINT('Ctrl Pts',(-0.104652854202276,0.115080765706631,
2.20616819836953));
#22159=CARTESIAN_POINT('Ctrl Pts',(-0.104656790775052,0.115077185718859,
2.20616857807037));
#22160=CARTESIAN_POINT('Ctrl Pts',(-0.104664588509522,0.115070093592429,
2.20616933025036));
#22161=CARTESIAN_POINT('Ctrl Pts',(-0.104668449726155,0.115066581417779,
2.20616970273381));
#22162=CARTESIAN_POINT('Ctrl Pts',(-0.104676100009156,0.115059621992719,
2.2061704407907));
#22163=CARTESIAN_POINT('Ctrl Pts',(-0.104679888618601,0.115056175171225,
2.20617080631911));
#22164=CARTESIAN_POINT('Ctrl Pts',(-0.104687395399258,0.115049344934214,
2.20617153062825));
#22165=CARTESIAN_POINT('Ctrl Pts',(-0.104691113576459,0.115045961525789,
2.20617188940868));
#22166=CARTESIAN_POINT('Ctrl Pts',(-0.104698481727184,0.11503925611886,
2.20617260043486));
#22167=CARTESIAN_POINT('Ctrl Pts',(-0.104702131707279,0.115035934126296,
2.20617295268038));
#22168=CARTESIAN_POINT('Ctrl Pts',(-0.104709365611245,0.115029349632079,
2.20617365084146));
#22169=CARTESIAN_POINT('Ctrl Pts',(-0.104712949541064,0.11502608713635,
2.20617399675678));
#22170=CARTESIAN_POINT('Ctrl Pts',(-0.104720053409928,0.115019619789333,
2.2061746824544));
#22171=CARTESIAN_POINT('Ctrl Pts',(-0.104723573353455,0.115016414944757,
2.20617502223637));
#22172=CARTESIAN_POINT('Ctrl Pts',(-0.105127831347595,0.114648311449253,
2.20621404788843));
#22173=CARTESIAN_POINT('Ctrl Pts',(-0.105526654944334,0.114281325353414,
2.20625282199629));
#22174=CARTESIAN_POINT('Ctrl Pts',(-0.106642123400429,0.113244085205233,
2.20636204668078));
#22175=CARTESIAN_POINT('Ctrl Pts',(-0.107354344670884,0.112569133938219,
2.20643269749459));
#22176=CARTESIAN_POINT('Ctrl Pts',(-0.108941506549535,0.111036264817846,
2.20659223388689));
#22177=CARTESIAN_POINT('Ctrl Pts',(-0.109812782152078,0.110174664376795,
2.20668127690867));
#22178=CARTESIAN_POINT('Ctrl Pts',(-0.112517216916863,0.107436310457396,
2.20696237307633));
#22179=CARTESIAN_POINT('Ctrl Pts',(-0.114313044825189,0.105523510066375,
2.20715599037422));
#22180=CARTESIAN_POINT('Ctrl Pts',(-0.120117794830169,0.0990185313458685,
2.20780578091117));
#22181=CARTESIAN_POINT('Ctrl Pts',(-0.123904778622434,0.0942366441679901,
2.20826997121257));
#22182=CARTESIAN_POINT('Ctrl Pts',(-0.130445481279453,0.0848995500202114,
2.20914861857641));
#22183=CARTESIAN_POINT('Ctrl Pts',(-0.13326539983101,0.0804007980511664,
2.20956112426964));
#22184=CARTESIAN_POINT('Ctrl Pts',(-0.139571765628049,0.0690934973332764,
2.21056351081752));
#22185=CARTESIAN_POINT('Ctrl Pts',(-0.142797435609249,0.0621539555417956,
2.2111505004814));
#22186=CARTESIAN_POINT('Ctrl Pts',(-0.145748979178899,0.0543464126688515,
2.21176243539643));
#22187=CARTESIAN_POINT('Ctrl Pts',(-0.145993306996063,0.0536866078690325,
2.21181377997955));
#22188=CARTESIAN_POINT('Ctrl Pts',(-0.146347173762537,0.0527107114756539,
2.2118891555663));
#22189=CARTESIAN_POINT('Ctrl Pts',(-0.146460178799727,0.0523959006432511,
2.21191338413341));
#22190=CARTESIAN_POINT('Ctrl Pts',(-0.146658722849685,0.0518371328317279,
2.21195623186529));
#22191=CARTESIAN_POINT('Ctrl Pts',(-0.146744669875165,0.0515933251039739,
2.21197487491199));
#22192=CARTESIAN_POINT('Ctrl Pts',(-0.146927299827461,0.0510711065216392,
2.21201469352663));
#22193=CARTESIAN_POINT('Ctrl Pts',(-0.1470237992305,0.050792635486859,2.21203585817473));
#22194=CARTESIAN_POINT('Ctrl Pts',(-0.147285969705562,0.0500290753610769,
2.21209370809432));
#22195=CARTESIAN_POINT('Ctrl Pts',(-0.147450037373086,0.0495434329866201,
2.21213030014871));
#22196=CARTESIAN_POINT('Ctrl Pts',(-0.148304511300897,0.04697233393671,
2.21232300623104));
#22197=CARTESIAN_POINT('Ctrl Pts',(-0.148953128010119,0.0448731012644384,
2.212476806311));
#22198=CARTESIAN_POINT('Ctrl Pts',(-0.153522341647447,0.0288921072323438,
2.21362608980931));
#22199=CARTESIAN_POINT('Ctrl Pts',(-0.15553960122566,0.0145385171943701,
2.214541897821));
#22200=CARTESIAN_POINT('Ctrl Pts',(-0.155549959903481,0.00011168717713736,
2.21550711968674));
#22201=CARTESIAN_POINT('Ctrl Pts',(-0.155549955602241,0.000117525064441449,
2.21559437743963));
#22202=CARTESIAN_POINT('Ctrl Pts',(-0.15555774324584,-0.0101897878636815,
2.21633029329905));
#22203=CARTESIAN_POINT('Ctrl Pts',(-0.1545366858615,-0.0205079000756088,
2.21706620915846));
#22204=CARTESIAN_POINT('Ctrl Pts',(-0.152506621271349,-0.0306191601517313,
2.21780212501788));
#22205=CARTESIAN_POINT('Ctrl Pts',(-0.150476759822646,-0.040729408429497,
2.21853796723677));
#22206=CARTESIAN_POINT('Ctrl Pts',(-0.147438301032368,-0.050631944170681,
2.21927380945567));
#22207=CARTESIAN_POINT('Ctrl Pts',(-0.143461944089335,-0.0601204881725731,
2.22000965167456));
#22208=CARTESIAN_POINT('Ctrl Pts',(-0.139475569793138,-0.0696329359883434,
2.22074734764841));
#22209=CARTESIAN_POINT('Ctrl Pts',(-0.134547003388513,-0.0787284847889013,
2.22148504362226));
#22210=CARTESIAN_POINT('Ctrl Pts',(-0.128793764580693,-0.0872236705552636,
2.22222273959611));
#22211=CARTESIAN_POINT('Ctrl Pts',(-0.126922445896272,-0.0899868445487726,
2.22246268518248));
#22212=CARTESIAN_POINT('Ctrl Pts',(-0.124964213903837,-0.092686744913992,
2.22270263076886));
#22213=CARTESIAN_POINT('Ctrl Pts',(-0.122924023262475,-0.0953178210250663,
2.22294257635523));
#22214=CARTESIAN_POINT('Ctrl Pts',(-0.116654882005318,-0.103402647738927,
2.22367988626368));
#22215=CARTESIAN_POINT('Ctrl Pts',(-0.109561201917683,-0.110896634044241,
2.22441719617213));
#22216=CARTESIAN_POINT('Ctrl Pts',(-0.101778418172752,-0.117630591659876,
2.22515450608058));
#22217=CARTESIAN_POINT('Ctrl Pts',(-0.093947197854086,-0.124406458423351,
2.22589640467695));
#22218=CARTESIAN_POINT('Ctrl Pts',(-0.0854188577963193,-0.130412054182867,
2.22663830327332));
#22219=CARTESIAN_POINT('Ctrl Pts',(-0.0763702411659673,-0.135511581660949,
2.22738020186969));
#22220=CARTESIAN_POINT('Ctrl Pts',(-0.0673982786209784,-0.140567909207971,
2.22811581557626));
#22221=CARTESIAN_POINT('Ctrl Pts',(-0.0579156509877826,-0.144733019772496,
2.22885142928283));
#22222=CARTESIAN_POINT('Ctrl Pts',(-0.0481219953059009,-0.147919153823225,
2.22958704298941));
#22223=CARTESIAN_POINT('Ctrl Pts',(-0.0382028280013022,-0.151146120109422,
2.23033208403067));
#22224=CARTESIAN_POINT('Ctrl Pts',(-0.0279655118809678,-0.153368489234519,
2.23107712507194));
#22225=CARTESIAN_POINT('Ctrl Pts',(-0.017632505234266,-0.154547394863723,
2.23182216611321));
#22226=CARTESIAN_POINT('Ctrl Pts',(-0.00729949858756426,-0.155726300492927,
2.23256720715448));
#22227=CARTESIAN_POINT('Ctrl Pts',(0.00312821776256832,-0.155861765045953,
2.23331224819575));
#22228=CARTESIAN_POINT('Ctrl Pts',(0.0134275703953657,-0.154969361014613,
2.23405728923701));
#22229=CARTESIAN_POINT('Ctrl Pts',(0.0236200397669874,-0.15408621805594,
2.23479459848979));
#22230=CARTESIAN_POINT('Ctrl Pts',(0.0337632113016459,-0.152189900448648,
2.23553190774256));
#22231=CARTESIAN_POINT('Ctrl Pts',(0.0436414900225305,-0.149302454261855,
2.23626921699533));
#22232=CARTESIAN_POINT('Ctrl Pts',(0.053581257778395,-0.146397034672549,
2.23701111575562));
#22233=CARTESIAN_POINT('Ctrl Pts',(0.0632518734402264,-0.142488195014809,
2.23775301451591));
#22234=CARTESIAN_POINT('Ctrl Pts',(0.0724433419641342,-0.137650879783122,
2.23849491327619));
#22235=CARTESIAN_POINT('Ctrl Pts',(0.0815569362388782,-0.132854548458485,
2.239230526337));
#22236=CARTESIAN_POINT('Ctrl Pts',(0.0901986504315224,-0.127145872651856,
2.23996613939781));
#22237=CARTESIAN_POINT('Ctrl Pts',(0.0981864910299422,-0.120644997738104,
2.24070175245862));
#22238=CARTESIAN_POINT('Ctrl Pts',(0.106276713916341,-0.114060799372996,
2.24144679406865));
#22239=CARTESIAN_POINT('Ctrl Pts',(0.113695395930814,-0.106664522953298,
2.24219183567868));
#22240=CARTESIAN_POINT('Ctrl Pts',(0.120289247614429,-0.0986220026584063,
2.2429368772887));
#22241=CARTESIAN_POINT('Ctrl Pts',(0.126883099298044,-0.0905794823635131,
2.24368191889873));
#22242=CARTESIAN_POINT('Ctrl Pts',(0.132651607608807,-0.0818915544490725,
2.24442696050876));
#22243=CARTESIAN_POINT('Ctrl Pts',(0.1374868894278,-0.0727540908503969,
2.24517200211879));
#22244=CARTESIAN_POINT('Ctrl Pts',(0.142271992500362,-0.0637114524317446,
2.24590931196561));
#22245=CARTESIAN_POINT('Ctrl Pts',(0.146179090611282,-0.0541608146967772,
2.24664662181244));
#22246=CARTESIAN_POINT('Ctrl Pts',(0.149109795162426,-0.0442952761208154,
2.24738393165927));
#22247=CARTESIAN_POINT('Ctrl Pts',(0.152058739418865,-0.0343683377984613,
2.24812583027104));
#22248=CARTESIAN_POINT('Ctrl Pts',(0.154018655072632,-0.0241234125626051,
2.24886772888282));
#22249=CARTESIAN_POINT('Ctrl Pts',(0.154938635682156,-0.013777578631686,
2.24960962749459));
#22250=CARTESIAN_POINT('Ctrl Pts',(0.155850822686378,-0.00351938931558706,
2.25034524112069));
#22251=CARTESIAN_POINT('Ctrl Pts',(0.155740566749862,0.00683706719978448,
2.25108085474679));
#22252=CARTESIAN_POINT('Ctrl Pts',(0.154610123611401,0.0170737276793156,
2.25181646837289));
#22253=CARTESIAN_POINT('Ctrl Pts',(0.153465192937607,0.0274415791717708,
2.2525615094775));
#22254=CARTESIAN_POINT('Ctrl Pts',(0.151273795230323,0.0376855707696601,
2.25330655058211));
#22255=CARTESIAN_POINT('Ctrl Pts',(0.14809213922491,0.0475869814107803,
2.25405159168673));
#22256=CARTESIAN_POINT('Ctrl Pts',(0.144910483219496,0.0574883920519004,
2.25479663279134));
#22257=CARTESIAN_POINT('Ctrl Pts',(0.140738993323588,0.0670463372042073,
2.25554167389595));
#22258=CARTESIAN_POINT('Ctrl Pts',(0.135683738501421,0.076063957340373,
2.25628671500057));
#22259=CARTESIAN_POINT('Ctrl Pts',(0.130680934045985,0.0849880159252763,
2.25702402599452));
#22260=CARTESIAN_POINT('Ctrl Pts',(0.12477518554404,0.0934498463198428,
2.25776133698848));
#22261=CARTESIAN_POINT('Ctrl Pts',(0.118075381672266,0.101262069616163,
2.25849864798244));
#22262=CARTESIAN_POINT('Ctrl Pts',(0.111333893601457,0.109122898256315,
2.25924054630743));
#22263=CARTESIAN_POINT('Ctrl Pts',(0.103788908687305,0.116325179858639,
2.25998244463242));
#22264=CARTESIAN_POINT('Ctrl Pts',(0.0955952107805158,0.122708427484948,
2.26072434295741));
#22265=CARTESIAN_POINT('Ctrl Pts',(0.0874709096238068,0.129037612019688,
2.26145995775411));
#22266=CARTESIAN_POINT('Ctrl Pts',(0.0787095978315592,0.134561023847159,
2.2621955725508));
#22267=CARTESIAN_POINT('Ctrl Pts',(0.069495716187678,0.139162307869486,
2.2629311873475));
#22268=CARTESIAN_POINT('Ctrl Pts',(0.0601637788311818,0.143822547268624,
2.26367622743664));
#22269=CARTESIAN_POINT('Ctrl Pts',(0.0503684379128092,0.147536380332777,
2.26442126752578));
#22270=CARTESIAN_POINT('Ctrl Pts',(0.0403239423585863,0.150232427167577,
2.26516630761492));
#22271=CARTESIAN_POINT('Ctrl Pts',(0.0302794468043635,0.152928474002378,
2.26591134770406));
#22272=CARTESIAN_POINT('Ctrl Pts',(0.0199867699267357,0.154606611536914,
2.2666563877932));
#22273=CARTESIAN_POINT('Ctrl Pts',(0.00966883048430999,0.155249206816221,
2.26740142788234));
#22274=CARTESIAN_POINT('Ctrl Pts',(-0.000542097669002817,0.155885137494557,
2.26813874087627));
#22275=CARTESIAN_POINT('Ctrl Pts',(-0.0108543084255259,0.155511753195141,
2.26887605387021));
#22276=CARTESIAN_POINT('Ctrl Pts',(-0.021051314719076,0.154118930208454,
2.26961336686414));
#22277=CARTESIAN_POINT('Ctrl Pts',(-0.0312281172117351,0.152728866886466,
2.27034921898569));
#22278=CARTESIAN_POINT('Ctrl Pts',(-0.0412892470449968,0.150323416029473,
2.27108507110724));
#22279=CARTESIAN_POINT('Ctrl Pts',(-0.0510211898583786,0.14694434553747,
2.27182092322879));
#22280=CARTESIAN_POINT('Ctrl Pts',(-0.0553134320620295,0.145454017321099,
2.27214546844985));
#22281=CARTESIAN_POINT('Ctrl Pts',(-0.0595417459102688,0.143774973896094,
2.27247001367092));
#22282=CARTESIAN_POINT('Ctrl Pts',(-0.0636886258329926,0.141913922641526,
2.27279455889198));
#22283=CARTESIAN_POINT('Origin',(0.,0.,-0.129405622560373));
#22284=CARTESIAN_POINT('',(-0.0636886247653984,0.141913923120645,2.35649769913034));
#22285=CARTESIAN_POINT('',(-0.063688625846537,0.141913922635448,2.34279739246514));
#22286=CARTESIAN_POINT('',(-0.0636886258329924,0.141913922641526,-0.129405622560373));
#22287=CARTESIAN_POINT('Ctrl Pts',(-0.0636886247653984,0.141913923120645,
2.35649769913034));
#22288=CARTESIAN_POINT('Ctrl Pts',(-0.0622878305980981,0.142542576406615,
2.35638086051576));
#22289=CARTESIAN_POINT('Ctrl Pts',(-0.0608775885458281,0.143150552227936,
2.35626465169388));
#22290=CARTESIAN_POINT('Ctrl Pts',(-0.0571970067334463,0.144673057726781,
2.35596539343815));
#22291=CARTESIAN_POINT('Ctrl Pts',(-0.0549137229840253,0.145555061980462,
2.35578366821747));
#22292=CARTESIAN_POINT('Ctrl Pts',(-0.0521132765585264,0.146561550106255,
2.3555662784368));
#22293=CARTESIAN_POINT('Ctrl Pts',(-0.0516152280238154,0.146737690526577,
2.35552782542491));
#22294=CARTESIAN_POINT('Ctrl Pts',(-0.0508322066157277,0.147010134817518,
2.35546770811077));
#22295=CARTESIAN_POINT('Ctrl Pts',(-0.050547841690524,0.147108152979743,
2.35544594531707));
#22296=CARTESIAN_POINT('Ctrl Pts',(-0.0500199124173099,0.147288414162136,
2.35540567355351));
#22297=CARTESIAN_POINT('Ctrl Pts',(-0.0497764290221712,0.147370878064146,
2.35538715190662));
#22298=CARTESIAN_POINT('Ctrl Pts',(-0.0492255612363254,0.147555927108912,
2.35534536475117));
#22299=CARTESIAN_POINT('Ctrl Pts',(-0.0489180608026368,0.147658155333656,
2.35532212051625));
#22300=CARTESIAN_POINT('Ctrl Pts',(-0.0479866671592225,0.147964567384768,
2.35525195641379));
#22301=CARTESIAN_POINT('Ctrl Pts',(-0.0473617877156281,0.148165767071775,
2.35520520897835));
#22302=CARTESIAN_POINT('Ctrl Pts',(-0.0425441923930382,0.149683351498874,
2.35484717023235));
#22303=CARTESIAN_POINT('Ctrl Pts',(-0.0382981722067958,0.150825638060988,
2.35454535351134));
#22304=CARTESIAN_POINT('Ctrl Pts',(-0.0335722986047436,0.151884507259909,
2.35421854400406));
#22305=CARTESIAN_POINT('Ctrl Pts',(-0.0331351765354773,0.151980468684479,
2.35418840070296));
#22306=CARTESIAN_POINT('Ctrl Pts',(-0.0180190020082514,0.155230606857872,
2.35314876149821));
#22307=CARTESIAN_POINT('Ctrl Pts',(-0.00296108203843076,0.156244986067882,
2.35219422806468));
#22308=CARTESIAN_POINT('Ctrl Pts',(0.0153514257203747,0.154826909522471,
2.35093757278502));
#22309=CARTESIAN_POINT('Ctrl Pts',(0.0186839142513779,0.154460178197442,
2.35070539853519));
#22310=CARTESIAN_POINT('Ctrl Pts',(0.022839970997147,0.15386635491245,2.3504102954226));
#22311=CARTESIAN_POINT('Ctrl Pts',(0.0236771794885812,0.153739749478231,
2.35035056660114));
#22312=CARTESIAN_POINT('Ctrl Pts',(0.0250279552116814,0.153524185637536,
2.35025372312775));
#22313=CARTESIAN_POINT('Ctrl Pts',(0.025542190667988,0.153439468851789,
2.35021674357695));
#22314=CARTESIAN_POINT('Ctrl Pts',(0.0265068587123853,0.153275562621882,
2.35014715843685));
#22315=CARTESIAN_POINT('Ctrl Pts',(0.0269573878814876,0.153196967614252,
2.3501145721393));
#22316=CARTESIAN_POINT('Ctrl Pts',(0.0279665901151058,0.153016322219819,
2.35004137697733));
#22317=CARTESIAN_POINT('Ctrl Pts',(0.0285250615359366,0.152913197196287,
2.35000073417393));
#22318=CARTESIAN_POINT('Ctrl Pts',(0.0299417563619243,0.152643565186706,
2.34989727636714));
#22319=CARTESIAN_POINT('Ctrl Pts',(0.0307991538417424,0.152472879001992,
2.34983432844281));
#22320=CARTESIAN_POINT('Ctrl Pts',(0.0357306460359825,0.151447850872865,
2.34947029509453));
#22321=CARTESIAN_POINT('Ctrl Pts',(0.0397701946310805,0.150437548705449,
2.34916424549396));
#22322=CARTESIAN_POINT('Ctrl Pts',(0.0457275555419092,0.148690887389623,
2.34870053983961));
#22323=CARTESIAN_POINT('Ctrl Pts',(0.047679444898215,0.148076531622052,
2.34854659782376));
#22324=CARTESIAN_POINT('Ctrl Pts',(0.06328079759921,0.142825571584371,2.3473001368566));
#22325=CARTESIAN_POINT('Ctrl Pts',(0.0762355623586698,0.136351288318933,
2.3461567201094));
#22326=CARTESIAN_POINT('Ctrl Pts',(0.0903257021524403,0.126666013171159,
2.34486886168383));
#22327=CARTESIAN_POINT('Ctrl Pts',(0.0924987625491884,0.125087939784361,
2.34466911782051));
#22328=CARTESIAN_POINT('Ctrl Pts',(0.0950599237290633,0.123124760996137,
2.34443334106692));
#22329=CARTESIAN_POINT('Ctrl Pts',(0.0954880850004677,0.122793002717387,
2.34439391298474));
#22330=CARTESIAN_POINT('Ctrl Pts',(0.0961503586843689,0.122274284993161,
2.34433291844597));
#22331=CARTESIAN_POINT('Ctrl Pts',(0.0963856728034501,0.122088878806069,
2.34431124479288));
#22332=CARTESIAN_POINT('Ctrl Pts',(0.0968218667143772,0.121743150439679,
2.34427106851226));
#22333=CARTESIAN_POINT('Ctrl Pts',(0.0970228824131831,0.12158301214552,
2.3442525536978));
#22334=CARTESIAN_POINT('Ctrl Pts',(0.097476345921773,0.121219921634605,
2.34421078506096));
#22335=CARTESIAN_POINT('Ctrl Pts',(0.097728557500299,0.121016678476366,
2.34418755241403));
#22336=CARTESIAN_POINT('Ctrl Pts',(0.0984685943473138,0.120416501982828,
2.34411937305476));
#22337=CARTESIAN_POINT('Ctrl Pts',(0.0989546573390958,0.120017389779382,
2.34407457893583));
#22338=CARTESIAN_POINT('Ctrl Pts',(0.102366453987248,0.11718110411787,2.34375995322933));
#22339=CARTESIAN_POINT('Ctrl Pts',(0.105204553397637,0.114639915018339,
2.34349715605987));
#22340=CARTESIAN_POINT('Ctrl Pts',(0.108627801617633,0.111340459121465,
2.34317449610659));
#22341=CARTESIAN_POINT('Ctrl Pts',(0.109302826118583,0.110677863138308,
2.34311058143381));
#22342=CARTESIAN_POINT('Ctrl Pts',(0.110760795350055,0.109220389080328,
2.34297178443598));
#22343=CARTESIAN_POINT('Ctrl Pts',(0.111541319238087,0.108423158814631,
2.34289699681766));
#22344=CARTESIAN_POINT('Ctrl Pts',(0.122286387272624,0.0972092565142343,
2.34185949304597));
#22345=CARTESIAN_POINT('Ctrl Pts',(0.13076393203542,0.0854657964949122,
2.34093726750333));
#22346=CARTESIAN_POINT('Ctrl Pts',(0.138925231320378,0.0700344977818755,
2.33973905824407));
#22347=CARTESIAN_POINT('Ctrl Pts',(0.140267774344386,0.0673052753624433,
2.33952794273069));
#22348=CARTESIAN_POINT('Ctrl Pts',(0.141878635797227,0.063772750588508,
2.33925483803145));
#22349=CARTESIAN_POINT('Ctrl Pts',(0.142221646981817,0.0630040799734087,
2.33919542118767));
#22350=CARTESIAN_POINT('Ctrl Pts',(0.14276366953388,0.0617624514560131,
2.33909944405467));
#22351=CARTESIAN_POINT('Ctrl Pts',(0.142966612332954,0.0612912187447158,
2.33906301773306));
#22352=CARTESIAN_POINT('Ctrl Pts',(0.143348760632995,0.0603916460324446,
2.33899347578859));
#22353=CARTESIAN_POINT('Ctrl Pts',(0.143528387257957,0.0599634899591847,
2.3389603748524));
#22354=CARTESIAN_POINT('Ctrl Pts',(0.143934156468139,0.0589840332043454,
2.33888464430861));
#22355=CARTESIAN_POINT('Ctrl Pts',(0.144159052303033,0.058432227341634,
2.33884197327949));
#22356=CARTESIAN_POINT('Ctrl Pts',(0.144736393405761,0.0569920376945332,
2.33873058051624));
#22357=CARTESIAN_POINT('Ctrl Pts',(0.14508382658787,0.0561016855687722,
2.33866169243442));
#22358=CARTESIAN_POINT('Ctrl Pts',(0.147375110664908,0.0500662519809027,
2.33819449695654));
#22359=CARTESIAN_POINT('Ctrl Pts',(0.149052859461297,0.0448250397748916,
2.33778747731663));
#22360=CARTESIAN_POINT('Ctrl Pts',(0.15422980213956,0.0251101363304353,
2.33625021870314));
#22361=CARTESIAN_POINT('Ctrl Pts',(0.155923832282781,0.0102480922114691,
2.33507032285342));
#22362=CARTESIAN_POINT('Ctrl Pts',(0.155404149723066,-0.00721505828116631,
2.33375641176293));
#22363=CARTESIAN_POINT('Ctrl Pts',(0.155262513318454,-0.00980106623130346,
2.33356399780182));
#22364=CARTESIAN_POINT('Ctrl Pts',(0.155013314022462,-0.0129215871342742,
2.33333533037815));
#22365=CARTESIAN_POINT('Ctrl Pts',(0.154967454023022,-0.0134604292336566,
2.33329597209172));
#22366=CARTESIAN_POINT('Ctrl Pts',(0.154891621803753,-0.0142996183530743,
2.3332348853593));
#22367=CARTESIAN_POINT('Ctrl Pts',(0.154863584605737,-0.0146001286745855,
2.33321305236033));
#22368=CARTESIAN_POINT('Ctrl Pts',(0.154809902503556,-0.0151579500788135,
2.33317260510611));
#22369=CARTESIAN_POINT('Ctrl Pts',(0.154784490825486,-0.0154152770317063,
2.33315397846414));
#22370=CARTESIAN_POINT('Ctrl Pts',(0.154725501208146,-0.0159977695661447,
2.33311188642505));
#22371=CARTESIAN_POINT('Ctrl Pts',(0.154691539962111,-0.0163228926562672,
2.33308844272013));
#22372=CARTESIAN_POINT('Ctrl Pts',(0.154585569263784,-0.0173073443193214,
2.33301760251964));
#22373=CARTESIAN_POINT('Ctrl Pts',(0.154510366320208,-0.017966333338465,
2.33297038054363));
#22374=CARTESIAN_POINT('Ctrl Pts',(0.153892301836982,-0.0230911183375703,
2.33260454883558));
#22375=CARTESIAN_POINT('Ctrl Pts',(0.153160089114337,-0.0275324712237907,
2.33229577604474));
#22376=CARTESIAN_POINT('Ctrl Pts',(0.149143960590367,-0.0466768288702718,
2.33097646186338));
#22377=CARTESIAN_POINT('Ctrl Pts',(0.1439274079896,-0.060890029549738,2.33001919513146));
#22378=CARTESIAN_POINT('Ctrl Pts',(0.135037290984816,-0.0772892468845399,
2.32874492216824));
#22379=CARTESIAN_POINT('Ctrl Pts',(0.133217216620147,-0.0803857409580274,
2.32849644056927));
#22380=CARTESIAN_POINT('Ctrl Pts',(0.130815578221392,-0.0841657616905167,
2.3281816507435));
#22381=CARTESIAN_POINT('Ctrl Pts',(0.130333003175463,-0.0849111251320017,
2.32811900702467));
#22382=CARTESIAN_POINT('Ctrl Pts',(0.129556330041332,-0.0860885179992524,
2.32801911913909));
#22383=CARTESIAN_POINT('Ctrl Pts',(0.129266385106025,-0.0865232757966593,
2.32798203019436));
#22384=CARTESIAN_POINT('Ctrl Pts',(0.128716357150386,-0.0873390790886988,
2.32791204288386));
#22385=CARTESIAN_POINT('Ctrl Pts',(0.128456758294247,-0.0877204455884917,
2.32787916301725));
#22386=CARTESIAN_POINT('Ctrl Pts',(0.127868917245048,-0.0885758145443564,
2.32780504613579));
#22387=CARTESIAN_POINT('Ctrl Pts',(0.127539729985038,-0.0890491559668797,
2.32776377357674));
#22388=CARTESIAN_POINT('Ctrl Pts',(0.126693074955339,-0.0902522440487524,
2.32765820373673));
#22389=CARTESIAN_POINT('Ctrl Pts',(0.126171935609659,-0.0909793679898886,
2.32759376672507));
#22390=CARTESIAN_POINT('Ctrl Pts',(0.123043202073309,-0.0952661731389925,
2.32721004747348));
#22391=CARTESIAN_POINT('Ctrl Pts',(0.120291626198591,-0.0987177326470451,
2.32688521268492));
#22392=CARTESIAN_POINT('Ctrl Pts',(0.116402704292327,-0.103191625078317,
2.32644162287713));
#22393=CARTESIAN_POINT('Ctrl Pts',(0.115391433353489,-0.104321224599612,
2.32632757795555));
#22394=CARTESIAN_POINT('Ctrl Pts',(0.104395121950214,-0.116248672770863,
2.32510136923459));
#22395=CARTESIAN_POINT('Ctrl Pts',(0.0929450050055603,-0.125591580949708,
2.32393492748763));
#22396=CARTESIAN_POINT('Ctrl Pts',(0.0781478439210853,-0.134518993348186,
2.32263501971058));
#22397=CARTESIAN_POINT('Ctrl Pts',(0.0759081183462432,-0.135795451921587,
2.32244347278898));
#22398=CARTESIAN_POINT('Ctrl Pts',(0.0731633907447485,-0.137270574046965,
2.32221584288785));
#22399=CARTESIAN_POINT('Ctrl Pts',(0.0726879201603291,-0.137522938196781,
2.32217666349231));
#22400=CARTESIAN_POINT('Ctrl Pts',(0.0719450993619771,-0.13791227428643,
2.32211585827971));
#22401=CARTESIAN_POINT('Ctrl Pts',(0.071678652575637,-0.138050945270857,
2.32209412825292));
#22402=CARTESIAN_POINT('Ctrl Pts',(0.0711829088526831,-0.138307130586625,
2.32205384968041));
#22403=CARTESIAN_POINT('Ctrl Pts',(0.0709537238005797,-0.138424845907807,
2.3220352889418));
#22404=CARTESIAN_POINT('Ctrl Pts',(0.0704339850649211,-0.138690167106335,
2.32199333287592));
#22405=CARTESIAN_POINT('Ctrl Pts',(0.0701432599400468,-0.138837429371094,
2.32196995923314));
#22406=CARTESIAN_POINT('Ctrl Pts',(0.0692617996533039,-0.139280443848806,
2.32189937304643));
#22407=CARTESIAN_POINT('Ctrl Pts',(0.0686696307340983,-0.139573352709093,
2.32185233407845));
#22408=CARTESIAN_POINT('Ctrl Pts',(0.0640737093931769,-0.141810336390388,
2.32149005601268));
#22409=CARTESIAN_POINT('Ctrl Pts',(0.059989579155983,-0.143585763411402,
2.32118447340646));
#22410=CARTESIAN_POINT('Ctrl Pts',(0.0420295968950637,-0.15049277568158,
2.31988629511711));
#22411=CARTESIAN_POINT('Ctrl Pts',(0.0275381540075679,-0.153805918183178,
2.31894590935921));
#22412=CARTESIAN_POINT('Ctrl Pts',(0.00892024207663318,-0.155342707186809,
2.3176730678394));
#22413=CARTESIAN_POINT('Ctrl Pts',(0.00503402763356657,-0.15551714240138,
2.31740444208039));
#22414=CARTESIAN_POINT('Ctrl Pts',(0.000236148989807116,-0.155552479634794,
2.31706732785458));
#22415=CARTESIAN_POINT('Ctrl Pts',(-0.000673348055767362,-0.15555120130186,
2.3170031839142));
#22416=CARTESIAN_POINT('Ctrl Pts',(-0.00210956804403887,-0.15553658660679,
2.31690149064174));
#22417=CARTESIAN_POINT('Ctrl Pts',(-0.00263633488942848,-0.155528549715288,
2.31686410706024));
#22418=CARTESIAN_POINT('Ctrl Pts',(-0.00362299322545797,-0.155508482276909,
2.31679392159595));
#22419=CARTESIAN_POINT('Ctrl Pts',(-0.0040828931970336,-0.155497087158457,
2.31676113994206));
#22420=CARTESIAN_POINT('Ctrl Pts',(-0.00511087117510107,-0.15546705295409,
2.31668771276117));
#22421=CARTESIAN_POINT('Ctrl Pts',(-0.00567890867194311,-0.155447340082818,
2.31664703409218));
#22422=CARTESIAN_POINT('Ctrl Pts',(-0.00711571039481541,-0.155389592181557,
2.3165438700161));
#22423=CARTESIAN_POINT('Ctrl Pts',(-0.007984277411045,-0.155347384753823,
2.31648125508628));
#22424=CARTESIAN_POINT('Ctrl Pts',(-0.01288900493283,-0.15506780111924,
2.31612621134544));
#22425=CARTESIAN_POINT('Ctrl Pts',(-0.016914694462103,-0.15468043474138,
2.31582914032079));
#22426=CARTESIAN_POINT('Ctrl Pts',(-0.0334724592352452,-0.15243311160776,
2.31458243592057));
#22427=CARTESIAN_POINT('Ctrl Pts',(-0.045768055606153,-0.149202703142092,
2.31359213945788));
#22428=CARTESIAN_POINT('Ctrl Pts',(-0.0616041272279759,-0.142898327077771,
2.31227748502557));
#22429=CARTESIAN_POINT('Ctrl Pts',(-0.0656049953992499,-0.141106311662637,
2.31194231365037));
#22430=CARTESIAN_POINT('Ctrl Pts',(-0.0714850425700971,-0.138168344186125,
2.31144993863582));
#22431=CARTESIAN_POINT('Ctrl Pts',(-0.0734241700131549,-0.137147713228804,
2.3112876122622));
#22432=CARTESIAN_POINT('Ctrl Pts',(-0.0757890541065996,-0.135838447462043,
2.31109027544619));
#22433=CARTESIAN_POINT('Ctrl Pts',(-0.0762356743359717,-0.135588297834739,
2.31105303571891));
#22434=CARTESIAN_POINT('Ctrl Pts',(-0.0769372110193267,-0.13519080862986,
2.31099459507163));
#22435=CARTESIAN_POINT('Ctrl Pts',(-0.0771929524300621,-0.135044945394115,
2.31097330228848));
#22436=CARTESIAN_POINT('Ctrl Pts',(-0.0776724937269196,-0.13476962959015,
2.31093339985487));
#22437=CARTESIAN_POINT('Ctrl Pts',(-0.0778963821967603,-0.134640346789623,
2.3109147802163));
#22438=CARTESIAN_POINT('Ctrl Pts',(-0.0784093972709849,-0.134342401928793,
2.31087213694262));
#22439=CARTESIAN_POINT('Ctrl Pts',(-0.0786983024056535,-0.134173364497457,
2.31084813786164));
#22440=CARTESIAN_POINT('Ctrl Pts',(-0.0795934567921234,-0.133645726680182,
2.3107738192145));
#22441=CARTESIAN_POINT('Ctrl Pts',(-0.0801978292286563,-0.133283933244755,
2.31072370082422));
#22442=CARTESIAN_POINT('Ctrl Pts',(-0.0870062445747519,-0.129145155782385,
2.31015952041146));
#22443=CARTESIAN_POINT('Ctrl Pts',(-0.0929418963855798,-0.124941566437214,
2.30967142059025));
#22444=CARTESIAN_POINT('Ctrl Pts',(-0.105657439832881,-0.114526892973744,
2.30858204222566));
#22445=CARTESIAN_POINT('Ctrl Pts',(-0.112224199928664,-0.108100100314215,
2.30798608777209));
#22446=CARTESIAN_POINT('Ctrl Pts',(-0.120941984603689,-0.0979122061325489,
2.30708826970452));
#22447=CARTESIAN_POINT('Ctrl Pts',(-0.123564454556539,-0.0945811009747796,
2.30680123264976));
#22448=CARTESIAN_POINT('Ctrl Pts',(-0.127569356035594,-0.0890427263891966,
2.30633019370055));
#22449=CARTESIAN_POINT('Ctrl Pts',(-0.129038175931453,-0.0869004919454911,
2.30614941239417));
#22450=CARTESIAN_POINT('Ctrl Pts',(-0.130885742992438,-0.08405567896223,
2.30591062617438));
#22451=CARTESIAN_POINT('Ctrl Pts',(-0.131313746553809,-0.0833854592141237,
2.3058544612963));
#22452=CARTESIAN_POINT('Ctrl Pts',(-0.13200353461866,-0.0822868238743171,
2.30576252840975));
#22453=CARTESIAN_POINT('Ctrl Pts',(-0.132268421278512,-0.0818603643826864,
2.30572687512221));
#22454=CARTESIAN_POINT('Ctrl Pts',(-0.132775237377736,-0.0810355235260071,
2.30565797433472));
#22455=CARTESIAN_POINT('Ctrl Pts',(-0.133017450188594,-0.0806373218211241,
2.30562473767779));
#22456=CARTESIAN_POINT('Ctrl Pts',(-0.13356984545034,-0.0797199139045481,
2.30554822052624));
#22457=CARTESIAN_POINT('Ctrl Pts',(-0.133878794969277,-0.079199978062087,
2.30550489579634));
#22458=CARTESIAN_POINT('Ctrl Pts',(-0.134695533067784,-0.0778070423704681,
2.30538892728303));
#22459=CARTESIAN_POINT('Ctrl Pts',(-0.135197857267318,-0.07693088958118,
2.30531608809641));
#22460=CARTESIAN_POINT('Ctrl Pts',(-0.139159029865383,-0.0698631922559838,
2.3047292527764));
#22461=CARTESIAN_POINT('Ctrl Pts',(-0.142198727525374,-0.063447572256919,
2.30420049045902));
#22462=CARTESIAN_POINT('Ctrl Pts',(-0.147965869834655,-0.0487588297400476,
2.30299830421891));
#22463=CARTESIAN_POINT('Ctrl Pts',(-0.150458203950497,-0.0404182165755456,
2.30232084932417));
#22464=CARTESIAN_POINT('Ctrl Pts',(-0.153666102340847,-0.0251153907349569,
2.30111260790511));
#22465=CARTESIAN_POINT('Ctrl Pts',(-0.154634474418508,-0.0182280067856629,
2.30058131794673));
#22466=CARTESIAN_POINT('Ctrl Pts',(-0.15518748566797,-0.010634362502773,
2.30002357022452));
#22467=CARTESIAN_POINT('Ctrl Pts',(-0.155231563393175,-0.00997031309190796,
2.29997503237368));
#22468=CARTESIAN_POINT('Ctrl Pts',(-0.155290953329751,-0.00897938553177951,
2.29990297366899));
#22469=CARTESIAN_POINT('Ctrl Pts',(-0.155309497394042,-0.00865272067933687,
2.29987927934808));
#22470=CARTESIAN_POINT('Ctrl Pts',(-0.155339510580998,-0.00809280462923168,
2.29983877232926));
#22471=CARTESIAN_POINT('Ctrl Pts',(-0.155351485262566,-0.00785958421389333,
2.29982193162328));
#22472=CARTESIAN_POINT('Ctrl Pts',(-0.155377199402237,-0.00733573818004885,
2.29978417653917));
#22473=CARTESIAN_POINT('Ctrl Pts',(-0.155390648711314,-0.00704510082247598,
2.29976327857965));
#22474=CARTESIAN_POINT('Ctrl Pts',(-0.155424784455485,-0.0062597183010564,
2.29970693499892));
#22475=CARTESIAN_POINT('Ctrl Pts',(-0.155443924299087,-0.00576490352588302,
2.29967157455729));
#22476=CARTESIAN_POINT('Ctrl Pts',(-0.155519581091093,-0.00353308850723159,
2.29951267115722));
#22477=CARTESIAN_POINT('Ctrl Pts',(-0.155549351313571,-0.00179521709333132,
2.29939053766916));
#22478=CARTESIAN_POINT('Ctrl Pts',(-0.155551162562828,0.00313761411625181,
2.29904747749142));
#22479=CARTESIAN_POINT('Ctrl Pts',(-0.155453913840257,0.00633186507260315,
2.29882961760291));
#22480=CARTESIAN_POINT('Ctrl Pts',(-0.154565299748118,0.0208223160512951,
2.29785168407958));
#22481=CARTESIAN_POINT('Ctrl Pts',(-0.15264043241771,0.0320144805920024,
2.29712269225997));
#22482=CARTESIAN_POINT('Ctrl Pts',(-0.147644349853505,0.049427503961895,
2.2959131258933));
#22483=CARTESIAN_POINT('Ctrl Pts',(-0.145345904140758,0.0558254485291349,
2.29545178914122));
#22484=CARTESIAN_POINT('Ctrl Pts',(-0.142237316937904,0.062971043102483,
2.29490586140212));
#22485=CARTESIAN_POINT('Ctrl Pts',(-0.141828717961668,0.0638860022015219,
2.29483536976228));
#22486=CARTESIAN_POINT('Ctrl Pts',(-0.141160391942814,0.0653445413663976,
2.29472202109309));
#22487=CARTESIAN_POINT('Ctrl Pts',(-0.140906292577498,0.065890682447694,
2.29467935677631));
#22488=CARTESIAN_POINT('Ctrl Pts',(-0.140450196798941,0.0668562745815855,
2.29460352438548));
#22489=CARTESIAN_POINT('Ctrl Pts',(-0.140249476154686,0.0672763231865496,
2.29457040065216));
#22490=CARTESIAN_POINT('Ctrl Pts',(-0.139828065169565,0.0681481289365589,
2.2945013671757));
#22491=CARTESIAN_POINT('Ctrl Pts',(-0.139607064439,0.0685997291131404,2.29446544696394));
#22492=CARTESIAN_POINT('Ctrl Pts',(-0.13902908301142,0.0697664345199909,
2.2943722259436));
#22493=CARTESIAN_POINT('Ctrl Pts',(-0.138668777080451,0.0704798661135457,
2.2943148096748));
#22494=CARTESIAN_POINT('Ctrl Pts',(-0.137096615368179,0.0735341323943068,
2.29406719813965));
#22495=CARTESIAN_POINT('Ctrl Pts',(-0.135830931378845,0.0758466022510134,
2.29387512241506));
#22496=CARTESIAN_POINT('Ctrl Pts',(-0.132333980292388,0.0818672225739584,
2.29336233840094));
#22497=CARTESIAN_POINT('Ctrl Pts',(-0.130005813280161,0.0855161193777704,
2.29303835140121));
#22498=CARTESIAN_POINT('Ctrl Pts',(-0.120413358372476,0.0992515071173619,
2.29176696873169));
#22499=CARTESIAN_POINT('Ctrl Pts',(-0.112103539956648,0.108549482409988,
2.29078831055915));
#22500=CARTESIAN_POINT('Ctrl Pts',(-0.102205596553945,0.117262088814938,
2.28978386143935));
#22501=CARTESIAN_POINT('Ctrl Pts',(-0.10163077149136,0.117760637582091,
2.28972605354729));
#22502=CARTESIAN_POINT('Ctrl Pts',(-0.0985673771601378,0.120378397205244,
2.28942083866504));
#22503=CARTESIAN_POINT('Ctrl Pts',(-0.096015895619844,0.122423192972991,
2.28917651209152));
#22504=CARTESIAN_POINT('Ctrl Pts',(-0.0929618957269405,0.124716441781122,
2.2888970624849));
#22505=CARTESIAN_POINT('Ctrl Pts',(-0.0925203961023893,0.125044317092071,
2.28885697162915));
#22506=CARTESIAN_POINT('Ctrl Pts',(-0.0918089232626336,0.125566854184183,
2.28879286946916));
#22507=CARTESIAN_POINT('Ctrl Pts',(-0.0915400534011034,0.125762998888008,
2.28876875939932));
#22508=CARTESIAN_POINT('Ctrl Pts',(-0.0910608181521888,0.126110257245867,
2.28872599163525));
#22509=CARTESIAN_POINT('Ctrl Pts',(-0.0908507028094057,0.126261709905648,
2.28870731076351));
#22510=CARTESIAN_POINT('Ctrl Pts',(-0.0904025387994706,0.12658305180383,
2.28866761548282));
#22511=CARTESIAN_POINT('Ctrl Pts',(-0.0901643895298115,0.126752794406786,
2.28864661112834));
#22512=CARTESIAN_POINT('Ctrl Pts',(-0.0895159781805926,0.12721220211381,
2.28858966017326));
#22513=CARTESIAN_POINT('Ctrl Pts',(-0.0891047848199081,0.127500557085662,
2.28855380199679));
#22514=CARTESIAN_POINT('Ctrl Pts',(-0.0869996819098929,0.12896163147066,
2.28837149523992));
#22515=CARTESIAN_POINT('Ctrl Pts',(-0.0852838866305113,0.130102678055038,
2.28822707448014));
#22516=CARTESIAN_POINT('Ctrl Pts',(-0.080180324903344,0.133352302910331,
2.2878079733219));
#22517=CARTESIAN_POINT('Ctrl Pts',(-0.0767333407592146,0.135365139240659,
2.2875380941227));
#22518=CARTESIAN_POINT('Ctrl Pts',(-0.0700901186741811,0.138908967681779,
2.28703496338495));
#22519=CARTESIAN_POINT('Ctrl Pts',(-0.0669135888792809,0.140466612944173,
2.28680131598053));
#22520=CARTESIAN_POINT('Ctrl Pts',(-0.0636886081915498,0.141913930558713,
2.28656840831392));
#22521=CARTESIAN_POINT('',(-0.155549964955187,-0.000104414750328626,2.28559437743963));
#22522=CARTESIAN_POINT('Ctrl Pts',(-0.0636886258329926,0.141913922641526,
2.27279455889198));
#22523=CARTESIAN_POINT('Ctrl Pts',(-0.0730870322701466,0.13769607297702,
2.27353010174628));
#22524=CARTESIAN_POINT('Ctrl Pts',(-0.0820652852127109,0.132540364111075,
2.27426564460058));
#22525=CARTESIAN_POINT('Ctrl Pts',(-0.0904363479891319,0.126558561395066,
2.27500118745488));
#22526=CARTESIAN_POINT('Ctrl Pts',(-0.0988275156773907,0.120562392090315,
2.27573849687391));
#22527=CARTESIAN_POINT('Ctrl Pts',(-0.106607849649866,0.113736743601892,
2.27647580629294));
#22528=CARTESIAN_POINT('Ctrl Pts',(-0.113622041823003,0.106234806499431,
2.27721311571197));
#22529=CARTESIAN_POINT('Ctrl Pts',(-0.117754033036061,0.101815489574099,
2.27764745739602));
#22530=CARTESIAN_POINT('Ctrl Pts',(-0.121620840829677,0.0971622129555324,
2.27808179908007));
#22531=CARTESIAN_POINT('Ctrl Pts',(-0.125197443581938,0.0923114436055868,
2.27851614076412));
#22532=CARTESIAN_POINT('Ctrl Pts',(-0.131302103576993,0.0840319953003109,
2.27925748904529));
#22533=CARTESIAN_POINT('Ctrl Pts',(-0.136604901482101,0.0751133412550397,
2.27999883732645));
#22534=CARTESIAN_POINT('Ctrl Pts',(-0.140978435979441,0.0657334244413799,
2.28074018560762));
#22535=CARTESIAN_POINT('Ctrl Pts',(-0.145341634266567,0.0563756756915671,
2.28147978182037));
#22536=CARTESIAN_POINT('Ctrl Pts',(-0.14877946960056,0.046559610988197,
2.28221937803311));
#22537=CARTESIAN_POINT('Ctrl Pts',(-0.151209668956078,0.0364888820628031,
2.28295897424586));
#22538=CARTESIAN_POINT('Ctrl Pts',(-0.15363754951923,0.0264277621965591,
2.28369786476751));
#22539=CARTESIAN_POINT('Ctrl Pts',(-0.155059453099014,0.0161133364418129,
2.28443675528916));
#22540=CARTESIAN_POINT('Ctrl Pts',(-0.155443196067471,0.00576327132190011,
2.28517564581081));
#22541=CARTESIAN_POINT('Ctrl Pts',(-0.155515685524535,0.00380813295380514,
2.28531522302041));
#22542=CARTESIAN_POINT('Ctrl Pts',(-0.155551278048855,0.00185174253079008,
2.28545480023002));
#22543=CARTESIAN_POINT('Ctrl Pts',(-0.155549964955187,-0.000104414750328626,
2.28559437743963));
#22544=CARTESIAN_POINT('Ctrl Pts',(-0.0636886258465365,0.141913922635448,
2.34279739246514));
#22545=CARTESIAN_POINT('Ctrl Pts',(-0.0530015079944167,0.146710124710772,
2.3418890487664));
#22546=CARTESIAN_POINT('Ctrl Pts',(-0.0418044881726883,0.150284807036787,
2.34099118900849));
#22547=CARTESIAN_POINT('Ctrl Pts',(-0.0286036919340213,0.15290735101411,
2.34000864466546));
#22548=CARTESIAN_POINT('Ctrl Pts',(-0.0268916737630272,0.15321771283392,
2.33988254320508));
#22549=CARTESIAN_POINT('Ctrl Pts',(-0.024481200040181,0.153613043989164,
2.33970677757529));
#22550=CARTESIAN_POINT('Ctrl Pts',(-0.0237868842987554,0.153722088863226,
2.33965635601679));
#22551=CARTESIAN_POINT('Ctrl Pts',(-0.0226632431977504,0.153890765625645,
2.33957508212066));
#22552=CARTESIAN_POINT('Ctrl Pts',(-0.0222343727673696,0.153953314390246,
2.33954413803104));
#22553=CARTESIAN_POINT('Ctrl Pts',(-0.0213406382486043,0.154079848919459,
2.33947980943997));
#22554=CARTESIAN_POINT('Ctrl Pts',(-0.0208757341446579,0.15414352538027,
2.33944643499923));
#22555=CARTESIAN_POINT('Ctrl Pts',(-0.0197772878657009,0.154288915427545,
2.33936778390241));
#22556=CARTESIAN_POINT('Ctrl Pts',(-0.0191435127150886,0.154368832612304,
2.33932256421805));
#22557=CARTESIAN_POINT('Ctrl Pts',(-0.0170448491715186,0.154620344392983,
2.33917333871667));
#22558=CARTESIAN_POINT('Ctrl Pts',(-0.0155779793154829,0.154775012862032,
2.33906986456883));
#22559=CARTESIAN_POINT('Ctrl Pts',(-0.00783451502552429,0.15548028722424,
2.33852764030594));
#22560=CARTESIAN_POINT('Ctrl Pts',(-0.00153053058273112,0.155670074982046,
2.33810038589204));
#22561=CARTESIAN_POINT('Ctrl Pts',(0.0124127457534963,0.15524245276642,
2.33716937993307));
#22562=CARTESIAN_POINT('Ctrl Pts',(0.0200295063764908,0.154444543425745,
2.33667024015484));
#22563=CARTESIAN_POINT('Ctrl Pts',(0.0323143233411157,0.152233224586033,
2.33584586065423));
#22564=CARTESIAN_POINT('Ctrl Pts',(0.037029046826082,0.151155593218615,
2.33552451551866));
#22565=CARTESIAN_POINT('Ctrl Pts',(0.0450544662884326,0.148923218548605,
2.33495748521316));
#22566=CARTESIAN_POINT('Ctrl Pts',(0.0483904535159426,0.147872881621639,
2.33471560034705));
#22567=CARTESIAN_POINT('Ctrl Pts',(0.0522164532777445,0.146524941819857,
2.3344278489321));
#22568=CARTESIAN_POINT('Ctrl Pts',(0.0527440054880084,0.146335868561983,
2.33438794029564));
#22569=CARTESIAN_POINT('Ctrl Pts',(0.0535858805145219,0.146028999106245,
2.334323864636));
#22570=CARTESIAN_POINT('Ctrl Pts',(0.0539008703363946,0.145913026634763,
2.33429980311827));
#22571=CARTESIAN_POINT('Ctrl Pts',(0.0544584136093846,0.145705699495882,
2.33425705402176));
#22572=CARTESIAN_POINT('Ctrl Pts',(0.054701117101631,0.145614757029952,
2.33423839116031));
#22573=CARTESIAN_POINT('Ctrl Pts',(0.055215384782725,0.14542059064302,2.33419873055255));
#22574=CARTESIAN_POINT('Ctrl Pts',(0.0554868831893145,0.145317214017533,
2.33417772424008));
#22575=CARTESIAN_POINT('Ctrl Pts',(0.0562188328229594,0.145036164183714,
2.33412091076026));
#22576=CARTESIAN_POINT('Ctrl Pts',(0.0566787252806646,0.144857061159592,
2.33408502016328));
#22577=CARTESIAN_POINT('Ctrl Pts',(0.0589552135095668,0.143957992794488,
2.3339064231794));
#22578=CARTESIAN_POINT('Ctrl Pts',(0.0607588781406035,0.14320607057419,
2.33376195469208));
#22579=CARTESIAN_POINT('Ctrl Pts',(0.0659237938550596,0.140937758068222,
2.3333405802116));
#22580=CARTESIAN_POINT('Ctrl Pts',(0.0692457653622815,0.139335630751505,
2.33306003069803));
#22581=CARTESIAN_POINT('Ctrl Pts',(0.0790024955367837,0.134195026847908,
2.33221302313821));
#22582=CARTESIAN_POINT('Ctrl Pts',(0.085247107347394,0.130317421189606,
2.33164029131531));
#22583=CARTESIAN_POINT('Ctrl Pts',(0.0930193405561323,0.124692737036863,
2.33090008741605));
#22584=CARTESIAN_POINT('Ctrl Pts',(0.0948152934516282,0.123332627707784,
2.33072692548805));
#22585=CARTESIAN_POINT('Ctrl Pts',(0.102673874001872,0.117108024289342,
2.32996039764098));
#22586=CARTESIAN_POINT('Ctrl Pts',(0.10839717868291,0.111831581951046,2.32937894396787));
#22587=CARTESIAN_POINT('Ctrl Pts',(0.114402229443738,0.105399159905103,
2.32874142540456));
#22588=CARTESIAN_POINT('Ctrl Pts',(0.11509425129291,0.104643042880166,2.32866748840836));
#22589=CARTESIAN_POINT('Ctrl Pts',(0.116185522574125,0.103426775166139,
2.32855011857869));
#22590=CARTESIAN_POINT('Ctrl Pts',(0.116589619494865,0.10297103535781,2.32850648274694));
#22591=CARTESIAN_POINT('Ctrl Pts',(0.117298563479992,0.10216196578903,2.32842961377933));
#22592=CARTESIAN_POINT('Ctrl Pts',(0.117604514672402,0.101809618336083,
2.3283963350043));
#22593=CARTESIAN_POINT('Ctrl Pts',(0.118234957400573,0.101076937454874,
2.32832753835453));
#22594=CARTESIAN_POINT('Ctrl Pts',(0.11855921061435,0.100696405228326,2.32829203053596));
#22595=CARTESIAN_POINT('Ctrl Pts',(0.119388660875931,0.0997134308705711,
2.32820087444282));
#22596=CARTESIAN_POINT('Ctrl Pts',(0.119891139884938,0.0991087042572439,
2.32814533723447));
#22597=CARTESIAN_POINT('Ctrl Pts',(0.121983560761576,0.0965513029354718,
2.32791269533805));
#22598=CARTESIAN_POINT('Ctrl Pts',(0.123530616193694,0.0945639006882726,
2.32773731260164));
#22599=CARTESIAN_POINT('Ctrl Pts',(0.127445153977421,0.0892750357863676,
2.32728348013581));
#22600=CARTESIAN_POINT('Ctrl Pts',(0.129732833737647,0.0859167929890493,
2.32700795256521));
#22601=CARTESIAN_POINT('Ctrl Pts',(0.136152312607891,0.0756510449344167,
2.32619597017108));
#22602=CARTESIAN_POINT('Ctrl Pts',(0.139882407007321,0.0685087653338176,
2.32567043438522));
#22603=CARTESIAN_POINT('Ctrl Pts',(0.144786099957893,0.057030399456948,
2.32484688521895));
#22604=CARTESIAN_POINT('Ctrl Pts',(0.146353467827657,0.052878534115516,
2.32455279974261));
#22605=CARTESIAN_POINT('Ctrl Pts',(0.149081033426038,0.0445980727842855,
2.32396371123359));
#22606=CARTESIAN_POINT('Ctrl Pts',(0.150252173729564,0.0404773829726443,
2.32366933549607));
#22607=CARTESIAN_POINT('Ctrl Pts',(0.151402869711126,0.0356846278700788,
2.32331994877204));
#22608=CARTESIAN_POINT('Ctrl Pts',(0.151550073666467,0.0350541974024073,
2.32327385317321));
#22609=CARTESIAN_POINT('Ctrl Pts',(0.151765892115636,0.0341031375527303,
2.32320408076961));
#22610=CARTESIAN_POINT('Ctrl Pts',(0.151837437635468,0.0337831692936692,
2.32318056736433));
#22611=CARTESIAN_POINT('Ctrl Pts',(0.151963473478506,0.0332110191631024,
2.32313844720577));
#22612=CARTESIAN_POINT('Ctrl Pts',(0.15201834853869,0.0329589255192188,
2.32311986270344));
#22613=CARTESIAN_POINT('Ctrl Pts',(0.152135535614555,0.0324140540885293,
2.32307963711892));
#22614=CARTESIAN_POINT('Ctrl Pts',(0.152197628880029,0.0321212368744975,
2.32305798431743));
#22615=CARTESIAN_POINT('Ctrl Pts',(0.152368024104424,0.0313061060122979,
2.32299761344817));
#22616=CARTESIAN_POINT('Ctrl Pts',(0.152474483631643,0.0307834186205562,
2.32295879359515));
#22617=CARTESIAN_POINT('Ctrl Pts',(0.153064466997916,0.0278085996563416,
2.32273727937973));
#22618=CARTESIAN_POINT('Ctrl Pts',(0.15349148794031,0.0253458175261111,
2.32255167809452));
#22619=CARTESIAN_POINT('Ctrl Pts',(0.156034164148296,0.00824285191596339,
2.32125220228198));
#22620=CARTESIAN_POINT('Ctrl Pts',(0.156111509125902,-0.00662412420394627,
2.32007857379173));
#22621=CARTESIAN_POINT('Ctrl Pts',(0.153840848749251,-0.0230661747018645,
2.31882428925722));
#22622=CARTESIAN_POINT('Ctrl Pts',(0.153563063333852,-0.0248483637352175,
2.31868877315135));
#22623=CARTESIAN_POINT('Ctrl Pts',(0.152547371719703,-0.0306946330303252,
2.31824574247194));
#22624=CARTESIAN_POINT('Ctrl Pts',(0.151678561686477,-0.0347344355171594,
2.31794208325195));
#22625=CARTESIAN_POINT('Ctrl Pts',(0.150431745102537,-0.0395835804017798,
2.31758019106565));
#22626=CARTESIAN_POINT('Ctrl Pts',(0.150206451356824,-0.0404300853469675,
2.31751711082726));
#22627=CARTESIAN_POINT('Ctrl Pts',(0.149822617567476,-0.0418247690743199,
2.31741332415453));
#22628=CARTESIAN_POINT('Ctrl Pts',(0.149668193027019,-0.0423740493103708,
2.31737248574901));
#22629=CARTESIAN_POINT('Ctrl Pts',(0.1493836748254,-0.0433651042254198,
2.31729886369866));
#22630=CARTESIAN_POINT('Ctrl Pts',(0.14925463562904,-0.0438071720205702,
2.31726604632634));
#22631=CARTESIAN_POINT('Ctrl Pts',(0.148974021448409,-0.0447528775388686,
2.31719588548058));
#22632=CARTESIAN_POINT('Ctrl Pts',(0.148821851098604,-0.0452563339485949,
2.31715856180815));
#22633=CARTESIAN_POINT('Ctrl Pts',(0.148401082425138,-0.0466233754167217,
2.31705728374322));
#22634=CARTESIAN_POINT('Ctrl Pts',(0.148127498366406,-0.0474854155467141,
2.31699349245682));
#22635=CARTESIAN_POINT('Ctrl Pts',(0.146661483065464,-0.0519687111838243,
2.31666203787263));
#22636=CARTESIAN_POINT('Ctrl Pts',(0.14534366354283,-0.0555478277151331,
2.31639853774858));
#22637=CARTESIAN_POINT('Ctrl Pts',(0.138254173709412,-0.0728164363552954,
2.31512578325496));
#22638=CARTESIAN_POINT('Ctrl Pts',(0.130674397762153,-0.0856773278012026,
2.31418146184917));
#22639=CARTESIAN_POINT('Ctrl Pts',(0.11858667356339,-0.100762371833234,
2.3128775623731));
#22640=CARTESIAN_POINT('Ctrl Pts',(0.115637257034872,-0.104133904437349,
2.31257023946688));
#22641=CARTESIAN_POINT('Ctrl Pts',(0.112090133970917,-0.107851946131488,
2.3122060398644));
#22642=CARTESIAN_POINT('Ctrl Pts',(0.111630298353429,-0.108327821291003,
2.31215892421139));
#22643=CARTESIAN_POINT('Ctrl Pts',(0.110939273374976,-0.109033877960786,
2.31208823823891));
#22644=CARTESIAN_POINT('Ctrl Pts',(0.110710365381722,-0.109266298152218,
2.31206484195021));
#22645=CARTESIAN_POINT('Ctrl Pts',(0.110299305468879,-0.109681047300221,
2.3120228583086));
#22646=CARTESIAN_POINT('Ctrl Pts',(0.110117429916292,-0.109863645263576,
2.31200429271565));
#22647=CARTESIAN_POINT('Ctrl Pts',(0.109722710186307,-0.110257967952639,
2.31196402152518));
#22648=CARTESIAN_POINT('Ctrl Pts',(0.109509709591646,-0.110469525791773,
2.31194230382787));
#22649=CARTESIAN_POINT('Ctrl Pts',(0.10891347724871,-0.111058300613369,
2.3118815529489));
#22650=CARTESIAN_POINT('Ctrl Pts',(0.108528904981357,-0.111434143879265,
2.3118424158559));
#22651=CARTESIAN_POINT('Ctrl Pts',(0.106295078545265,-0.113594735232751,
2.31161539775766));
#22652=CARTESIAN_POINT('Ctrl Pts',(0.104403902020008,-0.115335297047218,
2.3114244402375));
#22653=CARTESIAN_POINT('Ctrl Pts',(0.0913914081128948,-0.126729131983352,
2.31012362675339));
#22654=CARTESIAN_POINT('Ctrl Pts',(0.0789905509696638,-0.1348081325099,
2.3089555088151));
#22655=CARTESIAN_POINT('Ctrl Pts',(0.0604174829504804,-0.143452706174698,
2.30740748590841));
#22656=CARTESIAN_POINT('Ctrl Pts',(0.0550662828774975,-0.145590766905035,
2.30698076857946));
#22657=CARTESIAN_POINT('Ctrl Pts',(0.0486947663130901,-0.147734731729573,
2.30649419254587));
#22658=CARTESIAN_POINT('Ctrl Pts',(0.0477785304627239,-0.148033588519964,
2.30642472063432));
#22659=CARTESIAN_POINT('Ctrl Pts',(0.0462900058302921,-0.148503853908897,
2.3063126441547));
#22660=CARTESIAN_POINT('Ctrl Pts',(0.0457194158866239,-0.148680510810826,
2.30626986865034));
#22661=CARTESIAN_POINT('Ctrl Pts',(0.044704535775544,-0.148988326904816,
2.30619411089933));
#22662=CARTESIAN_POINT('Ctrl Pts',(0.0442606537383057,-0.14912079537071,
2.30616108629661));
#22663=CARTESIAN_POINT('Ctrl Pts',(0.0433439256866625,-0.149389922196192,
2.30609310530312));
#22664=CARTESIAN_POINT('Ctrl Pts',(0.0428710089901583,-0.149526323254562,
2.30605815760138));
#22665=CARTESIAN_POINT('Ctrl Pts',(0.041638306356025,-0.149875536661246,
2.3059673749103));
#22666=CARTESIAN_POINT('Ctrl Pts',(0.0408775272656315,-0.150084818857559,
2.3059116546327));
#22667=CARTESIAN_POINT('Ctrl Pts',(0.0392106841493979,-0.150529735074436,
2.30579022419615));
#22668=CARTESIAN_POINT('Ctrl Pts',(0.0383040144313007,-0.150762997577024,
2.30572459108073));
#22669=CARTESIAN_POINT('Ctrl Pts',(0.0356443258621845,-0.151421723744951,
2.3055332292586));
#22670=CARTESIAN_POINT('Ctrl Pts',(0.0338859066404297,-0.151824906288308,
2.30540819652155));
#22671=CARTESIAN_POINT('Ctrl Pts',(0.027684854229208,-0.153133619775831,
2.30497195035553));
#22672=CARTESIAN_POINT('Ctrl Pts',(0.0232098347193774,-0.153875487792479,
2.304665590818));
#22673=CARTESIAN_POINT('Ctrl Pts',(0.00758520190213225,-0.155768451287645,
2.30361433606078));
#22674=CARTESIAN_POINT('Ctrl Pts',(-0.00365031097533175,-0.155910218561,
2.30289265779029));
#22675=CARTESIAN_POINT('Ctrl Pts',(-0.0156077146023947,-0.154767100120844,
2.30208476417693));
#22676=CARTESIAN_POINT('Ctrl Pts',(-0.0164118367845981,-0.154683895765872,
2.30203022697767));
#22677=CARTESIAN_POINT('Ctrl Pts',(-0.0183521753656967,-0.154467824354113,
2.30189805132988));
#22678=CARTESIAN_POINT('Ctrl Pts',(-0.0194876297847783,-0.154328685785224,
2.3018202247326));
#22679=CARTESIAN_POINT('Ctrl Pts',(-0.0235967877031521,-0.153779079562254,
2.30153650103275));
#22680=CARTESIAN_POINT('Ctrl Pts',(-0.0265597550136452,-0.15329510734718,
2.30132797565328));
#22681=CARTESIAN_POINT('Ctrl Pts',(-0.0300330182196448,-0.152624073389732,
2.3010768796363));
#22682=CARTESIAN_POINT('Ctrl Pts',(-0.0305588983299304,-0.152519650117446,
2.30103868036519));
#22683=CARTESIAN_POINT('Ctrl Pts',(-0.0314097200720829,-0.152346126776305,
2.3009765681056));
#22684=CARTESIAN_POINT('Ctrl Pts',(-0.0317350047007945,-0.152278699527575,
2.30095274798034));
#22685=CARTESIAN_POINT('Ctrl Pts',(-0.0323127866945208,-0.152157001208942,
2.30091030305215));
#22686=CARTESIAN_POINT('Ctrl Pts',(-0.0325653676357921,-0.152103142735537,
2.30089170197761));
#22687=CARTESIAN_POINT('Ctrl Pts',(-0.0331072912876139,-0.151986175236567,
2.30085169252804));
#22688=CARTESIAN_POINT('Ctrl Pts',(-0.0333965839233371,-0.151922869831011,
2.30083027353632));
#22689=CARTESIAN_POINT('Ctrl Pts',(-0.034192402860361,-0.151746339256154,
2.3007711872005));
#22690=CARTESIAN_POINT('Ctrl Pts',(-0.0346985395758841,-0.151631405789171,
2.30073342485367));
#22691=CARTESIAN_POINT('Ctrl Pts',(-0.0374304819687104,-0.150996642273901,
2.30052863766208));
#22692=CARTESIAN_POINT('Ctrl Pts',(-0.0396450526568146,-0.150430366785879,
2.30035918695675));
#22693=CARTESIAN_POINT('Ctrl Pts',(-0.0555856099153824,-0.145977882427733,
2.29911817184775));
#22694=CARTESIAN_POINT('Ctrl Pts',(-0.0687319353566795,-0.140268570800756,
2.29798722909077));
#22695=CARTESIAN_POINT('Ctrl Pts',(-0.0864509634863847,-0.129475964106872,
2.29641219325171));
#22696=CARTESIAN_POINT('Ctrl Pts',(-0.0917698688313938,-0.125762107635986,
2.29593026562642));
#22697=CARTESIAN_POINT('Ctrl Pts',(-0.0976197527097639,-0.121108106566357,
2.29538895531626));
#22698=CARTESIAN_POINT('Ctrl Pts',(-0.0983913157112131,-0.120482109348251,
2.29531730941778));
#22699=CARTESIAN_POINT('Ctrl Pts',(-0.0996189600708093,-0.11946641796668,
2.29520288954043));
#22700=CARTESIAN_POINT('Ctrl Pts',(-0.100078865983213,-0.119081412611466,
2.29515992807081));
#22701=CARTESIAN_POINT('Ctrl Pts',(-0.100891393009271,-0.118393182150484,
2.29508384869341));
#22702=CARTESIAN_POINT('Ctrl Pts',(-0.10124490026642,-0.118091019733701,
2.29505068805746));
#22703=CARTESIAN_POINT('Ctrl Pts',(-0.101607125717096,-0.117778583284636,
2.29501664536663));
#22704=CARTESIAN_POINT('Ctrl Pts',(-0.10161719976442,-0.117769891691691,
2.29501569853566));
#22705=CARTESIAN_POINT('Ctrl Pts',(-0.101633283523633,-0.117756011495156,
2.29501418678699));
#22706=CARTESIAN_POINT('Ctrl Pts',(-0.101639293870939,-0.117750823795233,
2.29501362184264));
#22707=CARTESIAN_POINT('Ctrl Pts',(-0.10165299888429,-0.117738992781383,
2.29501233359418));
#22708=CARTESIAN_POINT('Ctrl Pts',(-0.101660693111013,-0.117732349333234,
2.29501161031966));
#22709=CARTESIAN_POINT('Ctrl Pts',(-0.101675342103734,-0.117719698404918,
2.29501023322438));
#22710=CARTESIAN_POINT('Ctrl Pts',(-0.101682296928704,-0.117713691114315,
2.29500957940358));
#22711=CARTESIAN_POINT('Ctrl Pts',(-0.10169554829551,-0.11770224308024,
2.29500833360016));
#22712=CARTESIAN_POINT('Ctrl Pts',(-0.101701844857993,-0.117696802512736,
2.29500774162002));
#22713=CARTESIAN_POINT('Ctrl Pts',(-0.101713850186109,-0.117686427583007,
2.29500661288387));
#22714=CARTESIAN_POINT('Ctrl Pts',(-0.10171955930256,-0.11768149307447,
2.29500607609845));
#22715=CARTESIAN_POINT('Ctrl Pts',(-0.101730451612529,-0.117672077238649,
2.29500505194457));
#22716=CARTESIAN_POINT('Ctrl Pts',(-0.10173563486942,-0.117667595984042,
2.29500456457307));
#22717=CARTESIAN_POINT('Ctrl Pts',(-0.101745529775735,-0.117659040066871,
2.29500363414828));
#22718=CARTESIAN_POINT('Ctrl Pts',(-0.101750241475586,-0.117654965464542,
2.29500319109262));
#22719=CARTESIAN_POINT('Ctrl Pts',(-0.101759240998286,-0.117647181876978,
2.29500234481817));
#22720=CARTESIAN_POINT('Ctrl Pts',(-0.101763528863751,-0.117643472939804,
2.29500194159731));
#22721=CARTESIAN_POINT('Ctrl Pts',(-0.101771722869697,-0.117636384468466,
2.29500117103421));
#22722=CARTESIAN_POINT('Ctrl Pts',(-0.101775629043845,-0.117633004974832,
2.2950008036904));
#22723=CARTESIAN_POINT('Ctrl Pts',(-0.101783097003189,-0.117626543291154,
2.29500010137486));
#22724=CARTESIAN_POINT('Ctrl Pts',(-0.101786658817873,-0.117623461132889,
2.29499976640168));
#22725=CARTESIAN_POINT('Ctrl Pts',(-0.101793471223949,-0.117617565587205,
2.29499912571213));
#22726=CARTESIAN_POINT('Ctrl Pts',(-0.101796721838939,-0.117614752226611,
2.29499881999463));
#22727=CARTESIAN_POINT('Ctrl Pts',(-0.101802941384818,-0.117609368847974,
2.29499823504145));
#22728=CARTESIAN_POINT('Ctrl Pts',(-0.101805910334738,-0.11760679885251,
2.29499795580487));
#22729=CARTESIAN_POINT('Ctrl Pts',(-0.101813013726995,-0.117600649512374,
2.2949972877037));
#22730=CARTESIAN_POINT('Ctrl Pts',(-0.101817147709411,-0.117597070381089,
2.29499689887815));
#22731=CARTESIAN_POINT('Ctrl Pts',(-0.1018253341519,-0.117589981943983,
2.29499612887739));
#22732=CARTESIAN_POINT('Ctrl Pts',(-0.101829386571973,-0.117586472687579,
2.2949957477063));
#22733=CARTESIAN_POINT('Ctrl Pts',(-0.1018374121774,-0.117579522063298,
2.29499499280031));
#22734=CARTESIAN_POINT('Ctrl Pts',(-0.101841385801765,-0.117576080329339,
2.29499461902444));
#22735=CARTESIAN_POINT('Ctrl Pts',(-0.101849256544208,-0.117569262428486,
2.29499387865321));
#22736=CARTESIAN_POINT('Ctrl Pts',(-0.101853153668494,-0.11756588626965,
2.29499351205757));
#22737=CARTESIAN_POINT('Ctrl Pts',(-0.101860874049315,-0.117559197273126,
2.29499278579951));
#22738=CARTESIAN_POINT('Ctrl Pts',(-0.101864697312784,-0.117555884442111,
2.29499242613672));
#22739=CARTESIAN_POINT('Ctrl Pts',(-0.101872272364746,-0.117549320065628,
2.29499171352012));
#22740=CARTESIAN_POINT('Ctrl Pts',(-0.101876024158912,-0.117546068527285,
2.29499136056605));
#22741=CARTESIAN_POINT('Ctrl Pts',(-0.101883458568497,-0.117539624781915,
2.29499066115168));
#22742=CARTESIAN_POINT('Ctrl Pts',(-0.101887141188776,-0.117536432582116,
2.29499031469119));
#22743=CARTESIAN_POINT('Ctrl Pts',(-0.101894439453545,-0.117530105638289,
2.2949896280575));
#22744=CARTESIAN_POINT('Ctrl Pts',(-0.101898055103377,-0.117526970900507,
2.29498928788406));
#22745=CARTESIAN_POINT('Ctrl Pts',(-0.102309596041633,-0.11717013512522,
2.29495056785704));
#22746=CARTESIAN_POINT('Ctrl Pts',(-0.102715681769539,-0.116814308795776,
2.29491227575156));
#22747=CARTESIAN_POINT('Ctrl Pts',(-0.103850390269405,-0.115809545907973,
2.29480502946776));
#22748=CARTESIAN_POINT('Ctrl Pts',(-0.104574781649206,-0.115155849190516,
2.29473627408903));
#22749=CARTESIAN_POINT('Ctrl Pts',(-0.10618677031788,-0.113673421464368,
2.29458257605452));
#22750=CARTESIAN_POINT('Ctrl Pts',(-0.10707091726593,-0.112841019833296,
2.29449779078458));
#22751=CARTESIAN_POINT('Ctrl Pts',(-0.109810328884732,-0.110200744145112,
2.29423343432206));
#22752=CARTESIAN_POINT('Ctrl Pts',(-0.111630297294349,-0.108356773289963,
2.29405537427602));
#22753=CARTESIAN_POINT('Ctrl Pts',(-0.11752884350704,-0.102073995804524,
2.29346839907961));
#22754=CARTESIAN_POINT('Ctrl Pts',(-0.12139557014892,-0.097443597040058,
2.29306733138319));
#22755=CARTESIAN_POINT('Ctrl Pts',(-0.130028326557518,-0.0857918089324549,
2.2921098405174));
#22756=CARTESIAN_POINT('Ctrl Pts',(-0.134507522177228,-0.0785831410819303,
2.29155834678455));
#22757=CARTESIAN_POINT('Ctrl Pts',(-0.138920994462656,-0.0699869794310976,
2.29090750736873));
#22758=CARTESIAN_POINT('Ctrl Pts',(-0.139452593225423,-0.0689216519102421,
2.29082694740148));
#22759=CARTESIAN_POINT('Ctrl Pts',(-0.141512862266604,-0.0646714195041184,
2.29050552859275));
#22760=CARTESIAN_POINT('Ctrl Pts',(-0.142944931834371,-0.0614412253729993,
2.29026121758013));
#22761=CARTESIAN_POINT('Ctrl Pts',(-0.144475991736227,-0.0576437910777903,
2.28997078127456));
#22762=CARTESIAN_POINT('Ctrl Pts',(-0.144683471855134,-0.0571210275133582,
2.2899307295005));
#22763=CARTESIAN_POINT('Ctrl Pts',(-0.145010532902854,-0.056283754835779,
2.28986645250326));
#22764=CARTESIAN_POINT('Ctrl Pts',(-0.145131938897866,-0.0559699563797075,
2.28984233353715));
#22765=CARTESIAN_POINT('Ctrl Pts',(-0.145345158906176,-0.0554134875444801,
2.28979950738275));
#22766=CARTESIAN_POINT('Ctrl Pts',(-0.145437385110067,-0.0551709781533011,
2.28978082509871));
#22767=CARTESIAN_POINT('Ctrl Pts',(-0.145631510470751,-0.0546566548701083,
2.28974116201168));
#22768=CARTESIAN_POINT('Ctrl Pts',(-0.145733254029886,-0.0543847904258592,
2.28972017279199));
#22769=CARTESIAN_POINT('Ctrl Pts',(-0.14600559322731,-0.053650832995713,
2.28966344660182));
#22770=CARTESIAN_POINT('Ctrl Pts',(-0.146174753863473,-0.053188217210018,
2.2896276266137));
#22771=CARTESIAN_POINT('Ctrl Pts',(-0.147000317391728,-0.0508968031751458,
2.28944990874089));
#22772=CARTESIAN_POINT('Ctrl Pts',(-0.147624573347133,-0.0490567251148018,
2.28930626890348));
#22773=CARTESIAN_POINT('Ctrl Pts',(-0.14932388052995,-0.0437213069692471,
2.2888880528355));
#22774=CARTESIAN_POINT('Ctrl Pts',(-0.150310308005517,-0.0401992679072003,
2.28860989262441));
#22775=CARTESIAN_POINT('Ctrl Pts',(-0.154071104219069,-0.0246852926814152,
2.28738409848849));
#22776=CARTESIAN_POINT('Ctrl Pts',(-0.155541082746387,-0.0124211275142716,
2.28641821317254));
#22777=CARTESIAN_POINT('Ctrl Pts',(-0.15554995955069,-0.000112177443420774,
2.28549129411633));
#22778=CARTESIAN_POINT('Origin',(0.,0.,0.));
#22779=CARTESIAN_POINT('',(-0.195399959231026,0.000126224060331325,0.022586969212423));
#22780=CARTESIAN_POINT('',(0.0861527862262976,0.175382032789696,3.89164997704322E-6));
#22781=CARTESIAN_POINT('Ctrl Pts',(-0.195399959231026,0.000126224060331325,
0.022586969212423));
#22782=CARTESIAN_POINT('Ctrl Pts',(-0.195395691015159,0.00673359514406753,
0.0222084605749147));
#22783=CARTESIAN_POINT('Ctrl Pts',(-0.195056309456599,0.0133308173981378,
0.0218299519374064));
#22784=CARTESIAN_POINT('Ctrl Pts',(-0.194384733506787,0.0198930987906703,
0.0214514432998981));
#22785=CARTESIAN_POINT('Ctrl Pts',(-0.193146662383657,0.031990868367168,
0.0207536508698904));
#22786=CARTESIAN_POINT('Ctrl Pts',(-0.190770597340965,0.0440147328451167,
0.0200558584398827));
#22787=CARTESIAN_POINT('Ctrl Pts',(-0.187282282163595,0.0557360456759846,
0.019358066009875));
#22788=CARTESIAN_POINT('Ctrl Pts',(-0.183801324713759,0.0674326353319801,
0.0186617453982992));
#22789=CARTESIAN_POINT('Ctrl Pts',(-0.179212949381552,0.07882709146759,
0.0179654247867235));
#22790=CARTESIAN_POINT('Ctrl Pts',(-0.173593710691015,0.0897016365989175,
0.0172691041751478));
#22791=CARTESIAN_POINT('Ctrl Pts',(-0.167975543236407,0.100574108637412,
0.0165729163081836));
#22792=CARTESIAN_POINT('Ctrl Pts',(-0.161327261645753,0.1109260719967,0.0158767284412195));
#22793=CARTESIAN_POINT('Ctrl Pts',(-0.153772634205927,0.120561755832312,
0.0151805405742553));
#22794=CARTESIAN_POINT('Ctrl Pts',(-0.146218660721959,0.130196605568303,
0.0144844129718293));
#22795=CARTESIAN_POINT('Ctrl Pts',(-0.137759054868081,0.139114627980258,
0.0137882853694032));
#22796=CARTESIAN_POINT('Ctrl Pts',(-0.128557927835573,0.147153046827525,
0.0130921577669772));
#22797=CARTESIAN_POINT('Ctrl Pts',(-0.119336310503073,0.155209366700727,
0.0123944799345243));
#22798=CARTESIAN_POINT('Ctrl Pts',(-0.109370572659015,0.162381645799003,
0.0116968021020714));
#22799=CARTESIAN_POINT('Ctrl Pts',(-0.0988569646754872,0.168548095614129,
0.0109991242696186));
#22800=CARTESIAN_POINT('Ctrl Pts',(-0.0955296651869108,0.17049962598775,
0.0107783263191197));
#22801=CARTESIAN_POINT('Ctrl Pts',(-0.092147681027628,0.17235076076533,
0.0105575283686208));
#22802=CARTESIAN_POINT('Ctrl Pts',(-0.088717691762081,0.174098624832043,
0.0103367304181219));
#22803=CARTESIAN_POINT('Ctrl Pts',(-0.0779973467121408,0.179561529944827,
0.00964663198561551));
#22804=CARTESIAN_POINT('Ctrl Pts',(-0.0667297219952147,0.18405116145512,
0.00895653355310913));
#22805=CARTESIAN_POINT('Ctrl Pts',(-0.0551164653379072,0.187465557499652,
0.00826643512060275));
#22806=CARTESIAN_POINT('Ctrl Pts',(-0.0435178297514944,0.190875654825219,
0.00757720552087978));
#22807=CARTESIAN_POINT('Ctrl Pts',(-0.0315752486213366,0.193212862185595,
0.00688797592115681));
#22808=CARTESIAN_POINT('Ctrl Pts',(-0.0195095720492338,0.19442360092966,
0.00619874632143384));
#22809=CARTESIAN_POINT('Ctrl Pts',(-0.00745527551376608,0.195633197736,
0.00551016678538927));
#22810=CARTESIAN_POINT('Ctrl Pts',(0.00472099927633243,0.195718325467519,
0.0048215872493447));
#22811=CARTESIAN_POINT('Ctrl Pts',(0.0167919026286014,0.194677148135346,
0.00413300771330014));
#22812=CARTESIAN_POINT('Ctrl Pts',(0.0288902804919299,0.193633600985663,
0.00344286090548424));
#22813=CARTESIAN_POINT('Ctrl Pts',(0.0408819121079928,0.191458712987708,
0.00275271409766835));
#22814=CARTESIAN_POINT('Ctrl Pts',(0.0525441651269303,0.188202738319914,
0.00206256728985245));
#22815=CARTESIAN_POINT('Ctrl Pts',(0.0641401501764159,0.184965264951094,
0.00137634207656065));
#22816=CARTESIAN_POINT('Ctrl Pts',(0.0754096998225287,0.180659351176491,
0.000690116863268847));
#22817=CARTESIAN_POINT('Ctrl Pts',(0.0861527862262976,0.175382032789696,
3.89164997704322E-6));
#22818=CARTESIAN_POINT('',(-0.0861525859670424,0.175382131162759,0.));
#22819=CARTESIAN_POINT('Origin',(0.,0.,0.));
#22820=CARTESIAN_POINT('',(-0.195399889995494,0.000207339694122921,0.0124130307921719));
#22821=CARTESIAN_POINT('Ctrl Pts',(-0.0861525859670426,0.175382131162759,
-6.38378239159465E-16));
#22822=CARTESIAN_POINT('Ctrl Pts',(-0.0973787392951184,0.169867532079808,
0.000713121939821653));
#22823=CARTESIAN_POINT('Ctrl Pts',(-0.108088311316424,0.163263883278222,
0.00142624387964394));
#22824=CARTESIAN_POINT('Ctrl Pts',(-0.118072608656115,0.155692064939546,
0.00213936581946623));
#22825=CARTESIAN_POINT('Ctrl Pts',(-0.128544465897827,0.14775049449096,
0.00288731140799201));
#22826=CARTESIAN_POINT('Ctrl Pts',(-0.138217415582637,0.138744057021195,
0.00363525699651779));
#22827=CARTESIAN_POINT('Ctrl Pts',(-0.146886675695703,0.128862191906957,
0.00438320258504356));
#22828=CARTESIAN_POINT('Ctrl Pts',(-0.155156273697141,0.119435891284598,
0.00509666708644155));
#22829=CARTESIAN_POINT('Ctrl Pts',(-0.162512351578732,0.109213971190783,
0.00581013158783954));
#22830=CARTESIAN_POINT('Ctrl Pts',(-0.168817837730545,0.098395618113732,
0.00652359608923752));
#22831=CARTESIAN_POINT('Ctrl Pts',(-0.175127968716422,0.0875692958724215,
0.00723758615268405));
#22832=CARTESIAN_POINT('Ctrl Pts',(-0.180385602605581,0.0761463975398017,
0.00795157621613059));
#22833=CARTESIAN_POINT('Ctrl Pts',(-0.184499920041503,0.0643501321263515,
0.00866556627957712));
#22834=CARTESIAN_POINT('Ctrl Pts',(-0.188625481498626,0.0525216286903234,
0.00938150760700247));
#22835=CARTESIAN_POINT('Ctrl Pts',(-0.19160129016889,0.040318514344953,
0.0100974489344278));
#22836=CARTESIAN_POINT('Ctrl Pts',(-0.19338664446451,0.0279779510107032,
0.0108133902618532));
#22837=CARTESIAN_POINT('Ctrl Pts',(-0.193637115470647,0.0262466681374884,
0.0109138311351606));
#22838=CARTESIAN_POINT('Ctrl Pts',(-0.19386423961171,0.0245126879456285,
0.0110142720084681));
#22839=CARTESIAN_POINT('Ctrl Pts',(-0.194067986277009,0.0227766701338622,
0.0111147128817756));
#22840=CARTESIAN_POINT('Ctrl Pts',(-0.194945875709514,0.0152966375681304,
0.0115474855170436));
#22841=CARTESIAN_POINT('Ctrl Pts',(-0.195391874966475,0.00776081463203696,
0.0119802581523117));
#22842=CARTESIAN_POINT('Ctrl Pts',(-0.195399889995409,0.000207339774271115,
0.0124130307875798));
#22843=CARTESIAN_POINT('',(-0.195388139417384,8.91918474211534E-5,0.0824130265070756));
#22844=CARTESIAN_POINT('Ctrl Pts',(-0.195399889995494,0.000207339694122791,
0.0124130307921719));
#22845=CARTESIAN_POINT('Ctrl Pts',(-0.19541248349625,-0.0116609553406007,
0.0130930189320593));
#22846=CARTESIAN_POINT('Ctrl Pts',(-0.194339510846434,-0.0235796520165797,
0.0137730070719468));
#22847=CARTESIAN_POINT('Ctrl Pts',(-0.192179861920935,-0.0353279021744901,
0.0144529952118342));
#22848=CARTESIAN_POINT('Ctrl Pts',(-0.190022526011279,-0.0470635697832568,
0.0151322550743976));
#22849=CARTESIAN_POINT('Ctrl Pts',(-0.186780890382315,-0.0586282396042047,
0.015811514936961));
#22850=CARTESIAN_POINT('Ctrl Pts',(-0.182505705615822,-0.0698056402998427,
0.0164907747995244));
#22851=CARTESIAN_POINT('Ctrl Pts',(-0.178233893778169,-0.0809742225281551,
0.0171694987565525));
#22852=CARTESIAN_POINT('Ctrl Pts',(-0.172930468207996,-0.0917552796565982,
0.0178482227135805));
#22853=CARTESIAN_POINT('Ctrl Pts',(-0.166695188924135,-0.10195035061022,
0.0185269466706086));
#22854=CARTESIAN_POINT('Ctrl Pts',(-0.160445205209005,-0.112169464227099,
0.0192072712375409));
#22855=CARTESIAN_POINT('Ctrl Pts',(-0.153259486033948,-0.121799059378327,
0.0198875958044733));
#22856=CARTESIAN_POINT('Ctrl Pts',(-0.145281699930208,-0.13066900039944,
0.0205679203714056));
#22857=CARTESIAN_POINT('Ctrl Pts',(-0.138787184776203,-0.137889796448328,
0.021121755502121));
#22858=CARTESIAN_POINT('Ctrl Pts',(-0.131768746190028,-0.144607600314278,
0.0216755906328364));
#22859=CARTESIAN_POINT('Ctrl Pts',(-0.124320713498993,-0.150749859685179,
0.0222294257635518));
#22860=CARTESIAN_POINT('Ctrl Pts',(-0.114940365634237,-0.158485664825235,
0.0229269477000608));
#22861=CARTESIAN_POINT('Ctrl Pts',(-0.104802633402424,-0.165369479385504,
0.0236244696365698));
#22862=CARTESIAN_POINT('Ctrl Pts',(-0.0940864764685079,-0.171256809925156,
0.0243219915730788));
#22863=CARTESIAN_POINT('Ctrl Pts',(-0.0833927779248148,-0.177131802089451,
0.0250180516777076));
#22864=CARTESIAN_POINT('Ctrl Pts',(-0.0721237827245387,-0.182013975205295,
0.0257141117823364));
#22865=CARTESIAN_POINT('Ctrl Pts',(-0.0604869483569958,-0.185802284911833,
0.0264101718869652));
#22866=CARTESIAN_POINT('Ctrl Pts',(-0.0488520442556239,-0.189589966230458,
0.0271061165322491));
#22867=CARTESIAN_POINT('Ctrl Pts',(-0.0368502364226137,-0.192283831461089,
0.027802061177533));
#22868=CARTESIAN_POINT('Ctrl Pts',(-0.0247070928623388,-0.193831678428196,
0.0284980058228169));
#22869=CARTESIAN_POINT('Ctrl Pts',(-0.0125648311255019,-0.195379412992142,
0.0291938999292682));
#22870=CARTESIAN_POINT('Ctrl Pts',(-0.000282122853219399,-0.195781209666355,
0.0298897940357194));
#22871=CARTESIAN_POINT('Ctrl Pts',(0.0119099790838408,-0.195036695004357,
0.0305856881421707));
#22872=CARTESIAN_POINT('Ctrl Pts',(0.0241295498036195,-0.194290502952226,
0.0312831500967342));
#22873=CARTESIAN_POINT('Ctrl Pts',(0.036257240023152,-0.192392959679809,
0.0319806120512976));
#22874=CARTESIAN_POINT('Ctrl Pts',(0.0480679653519524,-0.189395434757344,
0.0326780740058611));
#22875=CARTESIAN_POINT('Ctrl Pts',(0.0518276478486094,-0.18844123917066,
0.03290009555235));
#22876=CARTESIAN_POINT('Ctrl Pts',(0.0555553214346533,-0.187375961169439,
0.0331221170988389));
#22877=CARTESIAN_POINT('Ctrl Pts',(0.0592440995815707,-0.186202300374536,
0.0333441386453279));
#22878=CARTESIAN_POINT('Ctrl Pts',(0.0708356461158782,-0.182514210937394,
0.0340418149449709));
#22879=CARTESIAN_POINT('Ctrl Pts',(0.0821208716200282,-0.177727063673689,
0.034739491244614));
#22880=CARTESIAN_POINT('Ctrl Pts',(0.0928813521728905,-0.171913392202398,
0.035437167544257));
#22881=CARTESIAN_POINT('Ctrl Pts',(0.10361992062053,-0.166111559401358,
0.0361334231307253));
#22882=CARTESIAN_POINT('Ctrl Pts',(0.113835071487107,-0.159287699999734,
0.0368296787171935));
#22883=CARTESIAN_POINT('Ctrl Pts',(0.123329561574715,-0.151561800074387,
0.0375259343036618));
#22884=CARTESIAN_POINT('Ctrl Pts',(0.132823263600492,-0.14383654141432,
0.0382221320995117));
#22885=CARTESIAN_POINT('Ctrl Pts',(0.14159572037423,-0.135209906558148,
0.0389183298953617));
#22886=CARTESIAN_POINT('Ctrl Pts',(0.149480998995562,-0.125843517668924,
0.0396145276912116));
#22887=CARTESIAN_POINT('Ctrl Pts',(0.157366087284026,-0.116477354863234,
0.0403107086824147));
#22888=CARTESIAN_POINT('Ctrl Pts',(0.164363499650161,-0.106372158645069,
0.0410068896736177));
#22889=CARTESIAN_POINT('Ctrl Pts',(0.170347959658608,-0.0957221637874385,
0.0417030706648208));
#22890=CARTESIAN_POINT('Ctrl Pts',(0.176346285302151,-0.0850474935301456,
0.0424008646656473));
#22891=CARTESIAN_POINT('Ctrl Pts',(0.181326603057855,-0.0738262963564154,
0.0430986586664738));
#22892=CARTESIAN_POINT('Ctrl Pts',(0.185210396967689,-0.0622757485307955,
0.0437964526673002));
#22893=CARTESIAN_POINT('Ctrl Pts',(0.186439327308421,-0.0586208638987797,
0.0440172522872349));
#22894=CARTESIAN_POINT('Ctrl Pts',(0.187558844857637,-0.0549331151734461,
0.0442380519071695));
#22895=CARTESIAN_POINT('Ctrl Pts',(0.188567520760656,-0.0512196262596647,
0.0444588515271041));
#22896=CARTESIAN_POINT('Ctrl Pts',(0.191744677001402,-0.039522772550707,
0.0451543324921298));
#22897=CARTESIAN_POINT('Ctrl Pts',(0.193840871021327,-0.0274866554491859,
0.0458498134571554));
#22898=CARTESIAN_POINT('Ctrl Pts',(0.194797524331189,-0.0153324660260424,
0.0465452944221811));
#22899=CARTESIAN_POINT('Ctrl Pts',(0.195752137868602,-0.0032041917180958,
0.0472392924854106));
#22900=CARTESIAN_POINT('Ctrl Pts',(0.195571888140668,0.00904079464269347,
0.0479332905486402));
#22901=CARTESIAN_POINT('Ctrl Pts',(0.194249488119407,0.0211730103043578,
0.0486272886118697));
#22902=CARTESIAN_POINT('Ctrl Pts',(0.192927305321299,0.0333032330757399,
0.0493211726759721));
#22903=CARTESIAN_POINT('Ctrl Pts',(0.190463392484403,0.045319844906771,
0.0500150567400744));
#22904=CARTESIAN_POINT('Ctrl Pts',(0.186902439992509,0.056996823813669,
0.0507089408041768));
#22905=CARTESIAN_POINT('Ctrl Pts',(0.183341753083698,0.0686729318277191,
0.0514027731169937));
#22906=CARTESIAN_POINT('Ctrl Pts',(0.178684470441836,0.0800086245418753,
0.0520966054298106));
#22907=CARTESIAN_POINT('Ctrl Pts',(0.173024791587216,0.0907941710474873,
0.0527904377426275));
#22908=CARTESIAN_POINT('Ctrl Pts',(0.16735202485232,0.101604658887229,0.0534858745270894));
#22909=CARTESIAN_POINT('Ctrl Pts',(0.160672700054938,0.11186171361103,0.0541813113115513));
#22910=CARTESIAN_POINT('Ctrl Pts',(0.153125715666315,0.1213823512776,0.0548767480960132));
#22911=CARTESIAN_POINT('Ctrl Pts',(0.150605063920322,0.124562192485883,
0.0551090202003022));
#22912=CARTESIAN_POINT('Ctrl Pts',(0.14798795211152,0.127660164716599,0.0553412923045913));
#22913=CARTESIAN_POINT('Ctrl Pts',(0.145280482942679,0.130670353469874,
0.0555735644088803));
#22914=CARTESIAN_POINT('Ctrl Pts',(0.13715996025331,0.139698824172913,0.0562702190244504));
#22915=CARTESIAN_POINT('Ctrl Pts',(0.128165982374556,0.147999250676689,
0.0569668736400205));
#22916=CARTESIAN_POINT('Ctrl Pts',(0.118453589953988,0.155402403543229,
0.0576635282555905));
#22917=CARTESIAN_POINT('Ctrl Pts',(0.108761558649387,0.162790036397035,
0.0583587224003721));
#22918=CARTESIAN_POINT('Ctrl Pts',(0.0983547461448614,0.169283544951386,
0.0590539165451536));
#22919=CARTESIAN_POINT('Ctrl Pts',(0.0874228563386221,0.174752408251207,
0.0597491106899351));
#22920=CARTESIAN_POINT('Ctrl Pts',(0.0764925301188179,0.180220489340394,
0.0604442054012103));
#22921=CARTESIAN_POINT('Ctrl Pts',(0.0650380365633925,0.18466378412364,
0.0611393001124855));
#22922=CARTESIAN_POINT('Ctrl Pts',(0.0532742562263546,0.187997376640018,
0.0618343948237606));
#22923=CARTESIAN_POINT('Ctrl Pts',(0.0415111862009438,0.191330767869951,
0.0625294475643562));
#22924=CARTESIAN_POINT('Ctrl Pts',(0.0294397157166617,0.193554376859989,
0.0632245003049518));
#22925=CARTESIAN_POINT('Ctrl Pts',(0.017287816857642,0.194633736511162,
0.0639195530455473));
#22926=CARTESIAN_POINT('Ctrl Pts',(0.00510800481860889,0.195715575475289,
0.064616202337636));
#22927=CARTESIAN_POINT('Ctrl Pts',(-0.00715172753794594,0.195647904879166,
0.0653128516297247));
#22928=CARTESIAN_POINT('Ctrl Pts',(-0.0192616770895324,0.194448316515465,
0.0660095009218133));
#22929=CARTESIAN_POINT('Ctrl Pts',(-0.0231947644535041,0.194058712428748,
0.0662357597114277));
#22930=CARTESIAN_POINT('Ctrl Pts',(-0.0271121067131916,0.193550118186344,
0.0664620185010421));
#22931=CARTESIAN_POINT('Ctrl Pts',(-0.0310060669591839,0.192924295545487,
0.0666882772906565));
#22932=CARTESIAN_POINT('Ctrl Pts',(-0.0429945409988469,0.190997553100938,
0.0673848682813658));
#22933=CARTESIAN_POINT('Ctrl Pts',(-0.0548449574354469,0.187942291874567,
0.068081459272075));
#22934=CARTESIAN_POINT('Ctrl Pts',(-0.0663310882544109,0.183797025903537,
0.0687780502627842));
#22935=CARTESIAN_POINT('Ctrl Pts',(-0.0777932036131686,0.17966042694767,
0.06947318480541));
#22936=CARTESIAN_POINT('Ctrl Pts',(-0.0888917048713986,0.174438571179859,
0.0701683193480358));
#22937=CARTESIAN_POINT('Ctrl Pts',(-0.0994140975485735,0.168220085627736,
0.0708634538906616));
#22938=CARTESIAN_POINT('Ctrl Pts',(-0.109935089131981,0.162002428088937,
0.0715584958736667));
#22939=CARTESIAN_POINT('Ctrl Pts',(-0.119879348724295,0.154788809414352,
0.0722535378566717));
#22940=CARTESIAN_POINT('Ctrl Pts',(-0.129059053527509,0.146713737266091,
0.0729485798396768));
#22941=CARTESIAN_POINT('Ctrl Pts',(-0.138238256019874,0.138639106983493,
0.0736435837901813));
#22942=CARTESIAN_POINT('Ctrl Pts',(-0.146652347325546,0.12970371515905,
0.0743385877406857));
#22943=CARTESIAN_POINT('Ctrl Pts',(-0.154148802646238,0.120080417399054,
0.0750335916911901));
#22944=CARTESIAN_POINT('Ctrl Pts',(-0.161662552042581,0.110434919007913,
0.0757301989929297));
#22945=CARTESIAN_POINT('Ctrl Pts',(-0.168253952897313,0.10009907648672,
0.0764268062946693));
#22946=CARTESIAN_POINT('Ctrl Pts',(-0.173813289290223,0.0892754191595494,
0.0771234135964089));
#22947=CARTESIAN_POINT('Ctrl Pts',(-0.175621096348529,0.0857557393399034,
0.0773499391217501));
#22948=CARTESIAN_POINT('Ctrl Pts',(-0.177320141305075,0.0821846514608763,
0.0775764646470914));
#22949=CARTESIAN_POINT('Ctrl Pts',(-0.178907755968516,0.0785695542453295,
0.0778029901724326));
#22950=CARTESIAN_POINT('Ctrl Pts',(-0.184292698038043,0.0663077066259412,
0.0785713295304148));
#22951=CARTESIAN_POINT('Ctrl Pts',(-0.18842496616365,0.0534633499586128,
0.0793396688883969));
#22952=CARTESIAN_POINT('Ctrl Pts',(-0.191200323201082,0.0402938755619492,
0.0801080082463791));
#22953=CARTESIAN_POINT('Ctrl Pts',(-0.193975680238514,0.0271244011652855,
0.0808763476043612));
#22954=CARTESIAN_POINT('Ctrl Pts',(-0.195393798080322,0.0136303363268635,
0.0816446869623434));
#22955=CARTESIAN_POINT('Ctrl Pts',(-0.195399979639876,8.92005390054972E-5,
0.0824130263203255));
#22956=CARTESIAN_POINT('',(-0.195296072527608,-0.000171556393799694,0.15241303078758));
#22957=CARTESIAN_POINT('Ctrl Pts',(-0.195116749400228,8.89926274127593E-5,
0.0824130307875797));
#22958=CARTESIAN_POINT('Ctrl Pts',(-0.194962860530686,-0.0380682611678014,
0.0845812548764561));
#22959=CARTESIAN_POINT('Ctrl Pts',(-0.165715764002923,-0.1416455872943,
0.090454383259258));
#22960=CARTESIAN_POINT('Ctrl Pts',(0.00247549259342833,-0.230944160436683,
0.100032415935985));
#22961=CARTESIAN_POINT('Ctrl Pts',(0.195382766643704,-0.123157545007233,
0.111147128817761));
#22962=CARTESIAN_POINT('Ctrl Pts',(0.209427835089859,0.0973768392715823,
0.122261841699537));
#22963=CARTESIAN_POINT('Ctrl Pts',(0.0317514812939098,0.228765894785075,
0.133376554581314));
#22964=CARTESIAN_POINT('Ctrl Pts',(-0.155194310144234,0.158204250355088,
0.143426950943994));
#22965=CARTESIAN_POINT('Ctrl Pts',(-0.194905030259773,0.0461907277712621,
0.14977244301275));
#22966=CARTESIAN_POINT('Ctrl Pts',(-0.195296072527608,-0.000171556393799694,
0.15241303078758));
#22967=CARTESIAN_POINT('',(-0.195431294938471,1.28888134066882E-5,0.22241303078758));
#22968=CARTESIAN_POINT('Ctrl Pts',(-0.195296072527608,-0.000171556393799694,
0.15241303078758));
#22969=CARTESIAN_POINT('Ctrl Pts',(-0.195453686203354,-0.0188583599040719,
0.153477347306675));
#22970=CARTESIAN_POINT('Ctrl Pts',(-0.184414778781475,-0.102411837350248,
0.158246568119694));
#22971=CARTESIAN_POINT('Ctrl Pts',(-0.0652778999832005,-0.221542065857058,
0.166720693226644));
#22972=CARTESIAN_POINT('Ctrl Pts',(0.150741393243207,-0.174983271977123,
0.177835406108417));
#22973=CARTESIAN_POINT('Ctrl Pts',(0.228764398331316,0.0317641428286245,
0.188950118990195));
#22974=CARTESIAN_POINT('Ctrl Pts',(0.0973648674331604,0.209433016993645,
0.20006483187197));
#22975=CARTESIAN_POINT('Ctrl Pts',(-0.123167391259255,0.195376311478096,
0.211179544753746));
#22976=CARTESIAN_POINT('Ctrl Pts',(-0.195403696181917,0.0660797489631491,
0.218628944392284));
#22977=CARTESIAN_POINT('Ctrl Pts',(-0.195720085887096,0.000704139451294379,
0.222373439736894));
#22978=CARTESIAN_POINT('Ctrl Pts',(-0.195719426634615,1.29078158682454E-5,
0.22241303078758));
#22979=CARTESIAN_POINT('',(-0.195399931451662,0.000163672496008518,0.292413028611086));
#22980=CARTESIAN_POINT('Ctrl Pts',(-0.195399999575055,1.28867494583334E-5,
0.22241303078758));
#22981=CARTESIAN_POINT('Ctrl Pts',(-0.195400798685208,-0.0121039099641912,
0.223108168176893));
#22982=CARTESIAN_POINT('Ctrl Pts',(-0.194270226249095,-0.0242644285419508,
0.223803305566206));
#22983=CARTESIAN_POINT('Ctrl Pts',(-0.192009952717491,-0.0362400063110751,
0.224498442955518));
#22984=CARTESIAN_POINT('Ctrl Pts',(-0.189754413542218,-0.0481905001018107,
0.225192124313933));
#22985=CARTESIAN_POINT('Ctrl Pts',(-0.186373957051199,-0.0599559525316625,
0.225885805672348));
#22986=CARTESIAN_POINT('Ctrl Pts',(-0.181921919938222,-0.0713132178911548,
0.226579487030763));
#22987=CARTESIAN_POINT('Ctrl Pts',(-0.177470480318604,-0.0826689590291572,
0.227273075292468));
#22988=CARTESIAN_POINT('Ctrl Pts',(-0.171948023705749,-0.0936157877531208,
0.227966663554174));
#22989=CARTESIAN_POINT('Ctrl Pts',(-0.16545710676997,-0.103947610936042,
0.228660251815879));
#22990=CARTESIAN_POINT('Ctrl Pts',(-0.158966419617711,-0.114279068364367,
0.229353815524019));
#22991=CARTESIAN_POINT('Ctrl Pts',(-0.151507832196829,-0.123994834102582,
0.230047379232159));
#22992=CARTESIAN_POINT('Ctrl Pts',(-0.143227346908922,-0.13291759513861,
0.230740942940299));
#22993=CARTESIAN_POINT('Ctrl Pts',(-0.134927937041833,-0.14186074863859,
0.231436091748933));
#22994=CARTESIAN_POINT('Ctrl Pts',(-0.1258035275967,-0.150006682752804,
0.232131240557566));
#22995=CARTESIAN_POINT('Ctrl Pts',(-0.116036115709074,-0.157215711209632,
0.232826389366199));
#22996=CARTESIAN_POINT('Ctrl Pts',(-0.113307534437414,-0.159229593726359,
0.233020583083232));
#22997=CARTESIAN_POINT('Ctrl Pts',(-0.110528948520751,-0.161170620676228,
0.233214776800265));
#22998=CARTESIAN_POINT('Ctrl Pts',(-0.107704695813929,-0.163036371707754,
0.233408970517299));
#22999=CARTESIAN_POINT('Ctrl Pts',(-0.0975759729852575,-0.169727584225665,
0.234105414688228));
#23000=CARTESIAN_POINT('Ctrl Pts',(-0.0867854693978241,-0.175494992900072,
0.234801858859158));
#23001=CARTESIAN_POINT('Ctrl Pts',(-0.0755256889197688,-0.180213846064042,
0.235498303030088));
#23002=CARTESIAN_POINT('Ctrl Pts',(-0.0642895405604371,-0.184922795260663,
0.236193285498335));
#23003=CARTESIAN_POINT('Ctrl Pts',(-0.0525868409204017,-0.188587153133365,
0.236888267966582));
#23004=CARTESIAN_POINT('Ctrl Pts',(-0.0406339125343382,-0.191128347327527,
0.237583250434829));
#23005=CARTESIAN_POINT('Ctrl Pts',(-0.028682668364382,-0.193669183457116,
0.238278134977227));
#23006=CARTESIAN_POINT('Ctrl Pts',(-0.0164821110971703,-0.195086943165573,
0.238973019519625));
#23007=CARTESIAN_POINT('Ctrl Pts',(-0.00426145998030663,-0.195353525585888,
0.239667904062022));
#23008=CARTESIAN_POINT('Ctrl Pts',(0.00795846468967088,-0.195620092159423,
0.240362747297561));
#23009=CARTESIAN_POINT('Ctrl Pts',(0.0201976047040516,-0.194735624932464,
0.241057590533099));
#23010=CARTESIAN_POINT('Ctrl Pts',(0.0322267690432934,-0.192724143160711,
0.241752433768638));
#23011=CARTESIAN_POINT('Ctrl Pts',(0.0442836575924967,-0.190708025427439,
0.242448878443745));
#23012=CARTESIAN_POINT('Ctrl Pts',(0.056128751836065,-0.187559915954382,
0.243145323118853));
#23013=CARTESIAN_POINT('Ctrl Pts',(0.0675442942408393,-0.183354651742209,
0.24384176779396));
#23014=CARTESIAN_POINT('Ctrl Pts',(0.0712700922282979,-0.181982140092488,
0.244069072995665));
#23015=CARTESIAN_POINT('Ctrl Pts',(0.0749502895998998,-0.180497401018055,
0.24429637819737));
#23016=CARTESIAN_POINT('Ctrl Pts',(0.0785778410801077,-0.178904116473572,
0.244523683399075));
#23017=CARTESIAN_POINT('Ctrl Pts',(0.0896923560591145,-0.174022425605202,
0.245220127566151));
#23018=CARTESIAN_POINT('Ctrl Pts',(0.100389556815391,-0.168083750291963,
0.245916571733227));
#23019=CARTESIAN_POINT('Ctrl Pts',(0.110460236869427,-0.161182182857629,
0.246613015900303));
#23020=CARTESIAN_POINT('Ctrl Pts',(0.12050978049426,-0.154295100491898,
0.24730799836442));
#23021=CARTESIAN_POINT('Ctrl Pts',(0.129934656102679,-0.146449565744652,
0.248002980828537));
#23022=CARTESIAN_POINT('Ctrl Pts',(0.138551540872232,-0.137784725285245,
0.248697963292654));
#23023=CARTESIAN_POINT('Ctrl Pts',(0.147167211483506,-0.129121105741289,
0.249392847830579));
#23024=CARTESIAN_POINT('Ctrl Pts',(0.154974468037342,-0.119638997132723,
0.250087732368505));
#23025=CARTESIAN_POINT('Ctrl Pts',(0.161825400358542,-0.109515751373023,
0.25078261690643));
#23026=CARTESIAN_POINT('Ctrl Pts',(0.168675925429507,-0.099393107384586,
0.251477460137292));
#23027=CARTESIAN_POINT('Ctrl Pts',(0.174569770435743,-0.0886301421763397,
0.252172303368155));
#23028=CARTESIAN_POINT('Ctrl Pts',(0.179402831902806,-0.0774324473670666,
0.252867146599017));
#23029=CARTESIAN_POINT('Ctrl Pts',(0.184247032364217,-0.0662089446801096,
0.253563591269231));
#23030=CARTESIAN_POINT('Ctrl Pts',(0.188025281244286,-0.0545495414013264,
0.254260035939445));
#23031=CARTESIAN_POINT('Ctrl Pts',(0.190682372292722,-0.0426777798956278,
0.254956480609659));
#23032=CARTESIAN_POINT('Ctrl Pts',(0.191549592189821,-0.0388030809847963,
0.25518378583339));
#23033=CARTESIAN_POINT('Ctrl Pts',(0.192297790378953,-0.0349058376759882,
0.255411091057121));
#23034=CARTESIAN_POINT('Ctrl Pts',(0.192926239968484,-0.0309939660518479,
0.255638396280852));
#23035=CARTESIAN_POINT('Ctrl Pts',(0.194851756905226,-0.0190083188461995,
0.256334840459343));
#23036=CARTESIAN_POINT('Ctrl Pts',(0.195662895185079,-0.00680012371250248,
0.257031284637835));
#23037=CARTESIAN_POINT('Ctrl Pts',(0.195325263932807,0.00540381990626342,
0.257727728816327));
#23038=CARTESIAN_POINT('Ctrl Pts',(0.194988341303727,0.0175821497898641,
0.258422711292167));
#23039=CARTESIAN_POINT('Ctrl Pts',(0.193507384081088,0.0297553772293582,
0.259117693768007));
#23040=CARTESIAN_POINT('Ctrl Pts',(0.190899892160004,0.041694018435488,
0.259812676243847));
#23041=CARTESIAN_POINT('Ctrl Pts',(0.188292767645379,0.0536309774374055,
0.260507560793766));
#23042=CARTESIAN_POINT('Ctrl Pts',(0.184559565079072,0.0653325517697591,
0.261202445343684));
#23043=CARTESIAN_POINT('Ctrl Pts',(0.179769087832285,0.0765782936604638,
0.261897329893602));
#23044=CARTESIAN_POINT('Ctrl Pts',(0.174978895351844,0.0878233670564318,
0.262592173136627));
#23045=CARTESIAN_POINT('Ctrl Pts',(0.169131920778233,0.0986118665811072,
0.263287016379651));
#23046=CARTESIAN_POINT('Ctrl Pts',(0.162344449782597,0.10874483723279,0.263981859622676));
#23047=CARTESIAN_POINT('Ctrl Pts',(0.155541335368905,0.11890116184004,0.264678304305079));
#23048=CARTESIAN_POINT('Ctrl Pts',(0.147793938166803,0.128398250377176,
0.265374748987482));
#23049=CARTESIAN_POINT('Ctrl Pts',(0.139260141812556,0.137068497118582,
0.266071193669885));
#23050=CARTESIAN_POINT('Ctrl Pts',(0.136474886887117,0.139898286632982,
0.266298498834133));
#23051=CARTESIAN_POINT('Ctrl Pts',(0.133606147718333,0.142640299256972,
0.26652580399838));
#23052=CARTESIAN_POINT('Ctrl Pts',(0.130660181228968,0.145289631568165,
0.266753109162628));
#23053=CARTESIAN_POINT('Ctrl Pts',(0.12163398421183,0.153406966062983,0.267449553335677));
#23054=CARTESIAN_POINT('Ctrl Pts',(0.111816502841543,0.160708680302889,
0.268145997508725));
#23055=CARTESIAN_POINT('Ctrl Pts',(0.101379644996105,0.167042891439485,
0.268842441681773));
#23056=CARTESIAN_POINT('Ctrl Pts',(0.0909646921136319,0.173363808281725,
0.269537424152071));
#23057=CARTESIAN_POINT('Ctrl Pts',(0.0799336453451763,0.178720738884986,
0.270232406622369));
#23058=CARTESIAN_POINT('Ctrl Pts',(0.0684888070103471,0.183003943439204,
0.270927389092667));
#23059=CARTESIAN_POINT('Ctrl Pts',(0.0570455813018427,0.187286544471711,
0.271622273636983));
#23060=CARTESIAN_POINT('Ctrl Pts',(0.0451894825021334,0.190495370158818,
0.2723171581813));
#23061=CARTESIAN_POINT('Ctrl Pts',(0.0331430414331587,0.192568685939744,
0.273012042725616));
#23062=CARTESIAN_POINT('Ctrl Pts',(0.0210973164565891,0.19464187847384,
0.273706885962999));
#23063=CARTESIAN_POINT('Ctrl Pts',(0.00886213927854251,0.195579572915857,
0.274401729200381));
#23064=CARTESIAN_POINT('Ctrl Pts',(-0.00333226908389658,0.195371584378979,
0.275096572437764));
#23065=CARTESIAN_POINT('Ctrl Pts',(-0.0155547824997445,0.195163116480678,
0.27579301711457));
#23066=CARTESIAN_POINT('Ctrl Pts',(-0.0277354655587635,0.193803773974419,
0.276489461791376));
#23067=CARTESIAN_POINT('Ctrl Pts',(-0.0396478794232672,0.191335322555032,
0.277185906468182));
#23068=CARTESIAN_POINT('Ctrl Pts',(-0.0435358458500477,0.19052967087487,
0.277413211660256));
#23069=CARTESIAN_POINT('Ctrl Pts',(-0.0473953334042183,0.189606276414027,
0.27764051685233));
#23070=CARTESIAN_POINT('Ctrl Pts',(-0.0512188292505198,0.188567737246344,
0.277867822044403));
#23071=CARTESIAN_POINT('Ctrl Pts',(-0.0629337020096656,0.185385739751415,
0.278564266217401));
#23072=CARTESIAN_POINT('Ctrl Pts',(-0.0743923830398956,0.181096613933035,
0.279260710390398));
#23073=CARTESIAN_POINT('Ctrl Pts',(-0.085374038891261,0.17576243479024,
0.279957154563396));
#23074=CARTESIAN_POINT('Ctrl Pts',(-0.0963326463526684,0.170439451066666,
0.280652137033613));
#23075=CARTESIAN_POINT('Ctrl Pts',(-0.106815403444239,0.164076079160796,
0.281347119503831));
#23076=CARTESIAN_POINT('Ctrl Pts',(-0.116620403215248,0.15678278462227,
0.282042101974049));
#23077=CARTESIAN_POINT('Ctrl Pts',(-0.126424021419587,0.149490517740336,
0.282736986518245));
#23078=CARTESIAN_POINT('Ctrl Pts',(-0.135549342818769,0.141269073197698,
0.283431871062442));
#23079=CARTESIAN_POINT('Ctrl Pts',(-0.143823825129738,0.132271944587847,
0.284126755606638));
#23080=CARTESIAN_POINT('Ctrl Pts',(-0.152097815569515,0.123275350806426,
0.284821598843877));
#23081=CARTESIAN_POINT('Ctrl Pts',(-0.159520494186149,0.113503827200428,
0.285516442081116));
#23082=CARTESIAN_POINT('Ctrl Pts',(-0.165958460600679,0.103145282757151,
0.286211285318355));
#23083=CARTESIAN_POINT('Ctrl Pts',(-0.172411264913106,0.0927628644669315,
0.286907729994984));
#23084=CARTESIAN_POINT('Ctrl Pts',(-0.177874419363226,0.0817915019588945,
0.287604174671613));
#23085=CARTESIAN_POINT('Ctrl Pts',(-0.182260223497348,0.0704440979124345,
0.288300619348242));
#23086=CARTESIAN_POINT('Ctrl Pts',(-0.183691659599983,0.0667405390378119,
0.288527924540888));
#23087=CARTESIAN_POINT('Ctrl Pts',(-0.185008724695846,0.0629970592217985,
0.288755229733534));
#23088=CARTESIAN_POINT('Ctrl Pts',(-0.186209527669695,0.0592213796278757,
0.28898253492618));
#23089=CARTESIAN_POINT('Ctrl Pts',(-0.190617370485671,0.0453618185375623,
0.289816914572349));
#23090=CARTESIAN_POINT('Ctrl Pts',(-0.193480354578723,0.0309884032053344,
0.290651294218517));
#23091=CARTESIAN_POINT('Ctrl Pts',(-0.1947089295262,0.0164192802144656,
0.291485673864686));
#23092=CARTESIAN_POINT('Ctrl Pts',(-0.195164087964002,0.0110217590666684,
0.291794792113486));
#23093=CARTESIAN_POINT('Ctrl Pts',(-0.195395379853359,0.00559758483881988,
0.292103910362286));
#23094=CARTESIAN_POINT('Ctrl Pts',(-0.195399931451662,0.000163672496008518,
0.292413028611086));
#23095=CARTESIAN_POINT('',(-0.195138177948142,-0.000106777846584659,0.36241303078758));
#23096=CARTESIAN_POINT('Ctrl Pts',(-0.195258340825392,0.000163515663356278,
0.29241303078758));
#23097=CARTESIAN_POINT('Ctrl Pts',(-0.194901896811807,-0.0448304971854093,
0.294974436461039));
#23098=CARTESIAN_POINT('Ctrl Pts',(-0.157071388863312,-0.155446575493477,
0.301240746428423));
#23099=CARTESIAN_POINT('Ctrl Pts',(0.0268669425771182,-0.229391098189835,
0.311211960689732));
#23100=CARTESIAN_POINT('Ctrl Pts',(0.207303956765325,-0.101819340194787,
0.322326673571509));
#23101=CARTESIAN_POINT('Ctrl Pts',(0.197964422771547,0.118963001998054,
0.333441386453286));
#23102=CARTESIAN_POINT('Ctrl Pts',(0.00739822334892354,0.230840583131222,
0.344556099335061));
#23103=CARTESIAN_POINT('Ctrl Pts',(-0.164063175527352,0.144435526251838,
0.354213314113159));
#23104=CARTESIAN_POINT('Ctrl Pts',(-0.19494196408341,0.0394326521564634,
0.360165624597332));
#23105=CARTESIAN_POINT('Ctrl Pts',(-0.195138177948142,-0.000106777846584659,
0.36241303078758));
#23106=CARTESIAN_POINT('',(-0.195399971017471,-0.000106425426877684,0.43241303078758));
#23107=CARTESIAN_POINT('Ctrl Pts',(-0.195138177948142,-0.000106777846584659,
0.36241303078758));
#23108=CARTESIAN_POINT('Ctrl Pts',(-0.195265427457823,-0.0257490691689222,
0.363870528891258));
#23109=CARTESIAN_POINT('Ctrl Pts',(-0.17864031290789,-0.116414623642343,
0.369032931288858));
#23110=CARTESIAN_POINT('Ctrl Pts',(-0.0415002571887793,-0.227199993798136,
0.377900237980392));
#23111=CARTESIAN_POINT('Ctrl Pts',(0.168389188041786,-0.158073368658769,
0.389014950862164));
#23112=CARTESIAN_POINT('Ctrl Pts',(0.224126636583553,0.0557616293005508,
0.400129663743943));
#23113=CARTESIAN_POINT('Ctrl Pts',(0.0746872032705934,0.218549605801867,
0.411244376625718));
#23114=CARTESIAN_POINT('Ctrl Pts',(-0.136194829554037,0.182452397202414,
0.422005466425645));
#23115=CARTESIAN_POINT('Ctrl Pts',(-0.195262132691462,0.0584632240203973,
0.429061651931645));
#23116=CARTESIAN_POINT('Ctrl Pts',(-0.195647644016423,-0.000104853873465957,
0.432412933143721));
#23117=CARTESIAN_POINT('',(-0.195399922987737,0.000173483101027086,0.502413030787579));
#23118=CARTESIAN_POINT('Ctrl Pts',(-0.195399971017471,-0.000106425426877684,
0.43241303078758));
#23119=CARTESIAN_POINT('Ctrl Pts',(-0.195396609620896,-0.00627804073125874,
0.432766621321477));
#23120=CARTESIAN_POINT('Ctrl Pts',(-0.19510088201498,-0.0124415176703404,
0.433120211855374));
#23121=CARTESIAN_POINT('Ctrl Pts',(-0.194514937660211,-0.0185768411481667,
0.433473802389271));
#23122=CARTESIAN_POINT('Ctrl Pts',(-0.193360841345552,-0.0306611869693582,
0.434170246563104));
#23123=CARTESIAN_POINT('Ctrl Pts',(-0.191072232655043,-0.0426803484164101,
0.434866690736937));
#23124=CARTESIAN_POINT('Ctrl Pts',(-0.187672929088017,-0.0544061732483001,
0.43556313491077));
#23125=CARTESIAN_POINT('Ctrl Pts',(-0.184280760007233,-0.0661073878227418,
0.436258117381852));
#23126=CARTESIAN_POINT('Ctrl Pts',(-0.179782692702317,-0.0775156343635371,
0.436953099852933));
#23127=CARTESIAN_POINT('Ctrl Pts',(-0.174253439762954,-0.0884132271256893,
0.437648082324015));
#23128=CARTESIAN_POINT('Ctrl Pts',(-0.168724965918913,-0.099309284370541,
0.438342966869103));
#23129=CARTESIAN_POINT('Ctrl Pts',(-0.162165949397607,-0.109694030088432,
0.43903785141419));
#23130=CARTESIAN_POINT('Ctrl Pts',(-0.154698478704145,-0.119371439995601,
0.439732735959278));
#23131=CARTESIAN_POINT('Ctrl Pts',(-0.147231451909415,-0.129048274635699,
0.440427579197425));
#23132=CARTESIAN_POINT('Ctrl Pts',(-0.138856634330092,-0.138017179935642,
0.441122422435572));
#23133=CARTESIAN_POINT('Ctrl Pts',(-0.129736656101347,-0.146114886523039,
0.441817265673719));
#23134=CARTESIAN_POINT('Ctrl Pts',(-0.120595658610059,-0.154231256293231,
0.442513710351264));
#23135=CARTESIAN_POINT('Ctrl Pts',(-0.110706769418908,-0.161471886288798,
0.44321015502881));
#23136=CARTESIAN_POINT('Ctrl Pts',(-0.100264983963729,-0.167714319575739,
0.443906599706355));
#23137=CARTESIAN_POINT('Ctrl Pts',(-0.0968570004082841,-0.169751721136916,
0.444133904894586));
#23138=CARTESIAN_POINT('Ctrl Pts',(-0.0933903211066352,-0.171683154698311,
0.444361210082816));
#23139=CARTESIAN_POINT('Ctrl Pts',(-0.0898722359545557,-0.173505450071543,
0.444588515271047));
#23140=CARTESIAN_POINT('Ctrl Pts',(-0.0790931159252374,-0.179088811391074,
0.445284959444882));
#23141=CARTESIAN_POINT('Ctrl Pts',(-0.0677535465776804,-0.183683606124434,
0.445981403618718));
#23142=CARTESIAN_POINT('Ctrl Pts',(-0.0560581373434789,-0.187186124586145,
0.446677847792554));
#23143=CARTESIAN_POINT('Ctrl Pts',(-0.0443872745302157,-0.190681291933347,
0.447372830263638));
#23144=CARTESIAN_POINT('Ctrl Pts',(-0.0323628632506873,-0.193088413034795,
0.448067812734723));
#23145=CARTESIAN_POINT('Ctrl Pts',(-0.0202083180909325,-0.194352216040712,
0.448762795205808));
#23146=CARTESIAN_POINT('Ctrl Pts',(-0.00805548555843536,-0.195615840971395,
0.449457679750898));
#23147=CARTESIAN_POINT('Ctrl Pts',(0.00422657955392215,-0.19573633133975,
0.450152564295988));
#23148=CARTESIAN_POINT('Ctrl Pts',(0.0164069718891545,-0.194709967062368,
0.450847448841078));
#23149=CARTESIAN_POINT('Ctrl Pts',(0.0285866401692253,-0.193683663796515,
0.451542292079227));
#23150=CARTESIAN_POINT('Ctrl Pts',(0.0406637772497165,-0.191510741408034,
0.452237135317377));
#23151=CARTESIAN_POINT('Ctrl Pts',(0.0524130137934869,-0.188239305101468,
0.452931978555526));
#23152=CARTESIAN_POINT('Ctrl Pts',(0.0641893293808049,-0.184960328954686,
0.453628423233074));
#23153=CARTESIAN_POINT('Ctrl Pts',(0.0756354100046736,-0.180578081754846,
0.454324867910622));
#23154=CARTESIAN_POINT('Ctrl Pts',(0.0865426261085684,-0.175189993624729,
0.45502131258817));
#23155=CARTESIAN_POINT('Ctrl Pts',(0.0901025166344817,-0.173431432713816,
0.455248617776388));
#23156=CARTESIAN_POINT('Ctrl Pts',(0.0936052019270259,-0.171566091800692,
0.455475922964606));
#23157=CARTESIAN_POINT('Ctrl Pts',(0.0970440652641103,-0.1695983767523,
0.455703228152823));
#23158=CARTESIAN_POINT('Ctrl Pts',(0.107580456248006,-0.163569461653763,
0.456399672326659));
#23159=CARTESIAN_POINT('Ctrl Pts',(0.117590169783062,-0.156533581710509,
0.457096116500494));
#23160=CARTESIAN_POINT('Ctrl Pts',(0.126875114348702,-0.148606410894698,
0.45779256067433));
#23161=CARTESIAN_POINT('Ctrl Pts',(0.136140571596443,-0.140695877690089,
0.458487543145414));
#23162=CARTESIAN_POINT('Ctrl Pts',(0.144683571368738,-0.131898272703116,
0.459182525616499));
#23163=CARTESIAN_POINT('Ctrl Pts',(0.152336522117895,-0.122371336631681,
0.459877508087583));
#23164=CARTESIAN_POINT('Ctrl Pts',(0.159988394533649,-0.112845742946173,
0.460572392632673));
#23165=CARTESIAN_POINT('Ctrl Pts',(0.166749883378749,-0.10259167497533,
0.461267277177763));
#23166=CARTESIAN_POINT('Ctrl Pts',(0.172492648910389,-0.0918011223889852,
0.461962161722853));
#23167=CARTESIAN_POINT('Ctrl Pts',(0.178235073067225,-0.0810112112397224,
0.462657004961003));
#23168=CARTESIAN_POINT('Ctrl Pts',(0.182958506296677,-0.0696856644408173,
0.463351848199152));
#23169=CARTESIAN_POINT('Ctrl Pts',(0.186581154572559,-0.0580399238315401,
0.464046691437302));
#23170=CARTESIAN_POINT('Ctrl Pts',(0.190212152144164,-0.0463673427108855,
0.46474313611485));
#23171=CARTESIAN_POINT('Ctrl Pts',(0.192737101910838,-0.0343739494944365,
0.465439580792398));
#23172=CARTESIAN_POINT('Ctrl Pts',(0.194124730264744,-0.0222878688896088,
0.466136025469946));
#23173=CARTESIAN_POINT('Ctrl Pts',(0.194577623558826,-0.0183432212883551,
0.466363330658164));
#23174=CARTESIAN_POINT('Ctrl Pts',(0.194909779209757,-0.0143887335080788,
0.466590635846381));
#23175=CARTESIAN_POINT('Ctrl Pts',(0.195121310951865,-0.0104323541171564,
0.466817941034599));
#23176=CARTESIAN_POINT('Ctrl Pts',(0.195769426599936,0.00168966297313779,
0.467514385208434));
#23177=CARTESIAN_POINT('Ctrl Pts',(0.195285885260745,0.0139152165149137,
0.468210829382269));
#23178=CARTESIAN_POINT('Ctrl Pts',(0.193660456341936,0.0260151426948438,
0.468907273556104));
#23179=CARTESIAN_POINT('Ctrl Pts',(0.192038438886689,0.0380896734503476,
0.469602256027188));
#23180=CARTESIAN_POINT('Ctrl Pts',(0.189279332201416,0.0500382310585006,
0.470297238498273));
#23181=CARTESIAN_POINT('Ctrl Pts',(0.185424789573062,0.0616344661028701,
0.470992220969357));
#23182=CARTESIAN_POINT('Ctrl Pts',(0.181570790066204,0.0732290671882591,
0.471687105514446));
#23183=CARTESIAN_POINT('Ctrl Pts',(0.176621893083348,0.0844706000021562,
0.472381990059536));
#23184=CARTESIAN_POINT('Ctrl Pts',(0.170669813200684,0.0951471221952799,
0.473076874604625));
#23185=CARTESIAN_POINT('Ctrl Pts',(0.164718087135373,0.105823009729781,
0.473771717842774));
#23186=CARTESIAN_POINT('Ctrl Pts',(0.157763746352208,0.115933201421272,
0.474466561080923));
#23187=CARTESIAN_POINT('Ctrl Pts',(0.149943450532847,0.125292145174004,
0.475161404319072));
#23188=CARTESIAN_POINT('Ctrl Pts',(0.142105130892935,0.134672658944884,
0.475857848996619));
#23189=CARTESIAN_POINT('Ctrl Pts',(0.13339748282169,0.143297838203064,0.476554293674167));
#23190=CARTESIAN_POINT('Ctrl Pts',(0.12399521810552,0.151017700575014,0.477250738351715));
#23191=CARTESIAN_POINT('Ctrl Pts',(0.120926512693726,0.153537304537915,
0.477478043539935));
#23192=CARTESIAN_POINT('Ctrl Pts',(0.117784066586514,0.155960800658072,
0.477705348728155));
#23193=CARTESIAN_POINT('Ctrl Pts',(0.114574619856465,0.158283974187997,
0.477932653916375));
#23194=CARTESIAN_POINT('Ctrl Pts',(0.104741142258005,0.165401984482409,
0.478629098090211));
#23195=CARTESIAN_POINT('Ctrl Pts',(0.0942070042923155,0.17162532032016,
0.479325542264046));
#23196=CARTESIAN_POINT('Ctrl Pts',(0.0831592018979891,0.176821116215483,
0.480021986437881));
#23197=CARTESIAN_POINT('Ctrl Pts',(0.0721345867220473,0.182006007131716,
0.480716968908965));
#23198=CARTESIAN_POINT('Ctrl Pts',(0.060599199670287,0.186167202174279,
0.48141195138005));
#23199=CARTESIAN_POINT('Ctrl Pts',(0.0487658073344321,0.189216954935389,
0.482106933851134));
#23200=CARTESIAN_POINT('Ctrl Pts',(0.0369340823740317,0.192266277973327,
0.482801818396224));
#23201=CARTESIAN_POINT('Ctrl Pts',(0.0248052706711634,0.194204206772151,
0.483496702941313));
#23202=CARTESIAN_POINT('Ctrl Pts',(0.0126071809498785,0.194992869070889,
0.484191587486403));
#23203=CARTESIAN_POINT('Ctrl Pts',(0.000409816335766259,0.195781484488132,
0.484886430724552));
#23204=CARTESIAN_POINT('Ctrl Pts',(-0.0118559424614858,0.19542093921384,
0.485581273962701));
#23205=CARTESIAN_POINT('Ctrl Pts',(-0.0239600872508721,0.193925434688002,
0.48627611720085));
#23206=CARTESIAN_POINT('Ctrl Pts',(-0.0360921290583036,0.192426483399302,
0.486972561878398));
#23207=CARTESIAN_POINT('Ctrl Pts',(-0.0480609526199101,0.189787522482648,
0.487669006555946));
#23208=CARTESIAN_POINT('Ctrl Pts',(-0.0596458007786993,0.186074013364219,
0.488365451233494));
#23209=CARTESIAN_POINT('Ctrl Pts',(-0.0634268564405725,0.184862000527694,
0.488592756421713));
#23210=CARTESIAN_POINT('Ctrl Pts',(-0.0671671498803667,0.183535913816646,
0.488820061609932));
#23211=CARTESIAN_POINT('Ctrl Pts',(-0.0708594848912776,0.182099130697933,
0.489047366798151));
#23212=CARTESIAN_POINT('Ctrl Pts',(-0.0821724919825079,0.177696946832565,
0.489743810971986));
#23213=CARTESIAN_POINT('Ctrl Pts',(-0.093113742811342,0.172220907942076,
0.490440255145822));
#23214=CARTESIAN_POINT('Ctrl Pts',(-0.10347020046737,0.165756078667547,
0.491136699319657));
#23215=CARTESIAN_POINT('Ctrl Pts',(-0.113804921905028,0.159304817829786,
0.491831681790741));
#23216=CARTESIAN_POINT('Ctrl Pts',(-0.12355651140328,0.151869281475647,
0.492526664261825));
#23217=CARTESIAN_POINT('Ctrl Pts',(-0.132535866386685,0.143580653714666,
0.49322164673291));
#23218=CARTESIAN_POINT('Ctrl Pts',(-0.141513956140674,0.135293193856689,
0.493916531277999));
#23219=CARTESIAN_POINT('Ctrl Pts',(-0.149719353643204,0.126153440403864,
0.494611415823089));
#23220=CARTESIAN_POINT('Ctrl Pts',(-0.156996703673694,0.116332261370587,
0.495306300368179));
#23221=CARTESIAN_POINT('Ctrl Pts',(-0.164273621107045,0.106511666150637,
0.496001143606328));
#23222=CARTESIAN_POINT('Ctrl Pts',(-0.170622100687362,0.0960104453270628,
0.496695986844477));
#23223=CARTESIAN_POINT('Ctrl Pts',(-0.17592934686914,0.0850295531576978,
0.497390830082626));
#23224=CARTESIAN_POINT('Ctrl Pts',(-0.181248824922321,0.0740233527858678,
0.498087274760174));
#23225=CARTESIAN_POINT('Ctrl Pts',(-0.185521956306638,0.0625360902598858,
0.498783719437722));
#23226=CARTESIAN_POINT('Ctrl Pts',(-0.188684030783989,0.0507887440985386,
0.499480164115269));
#23227=CARTESIAN_POINT('Ctrl Pts',(-0.189716066719374,0.0469546524378999,
0.499707469303489));
#23228=CARTESIAN_POINT('Ctrl Pts',(-0.190630153319104,0.0430929498769562,
0.499934774491708));
#23229=CARTESIAN_POINT('Ctrl Pts',(-0.19142522601456,0.0392115141925761,
0.500162079679927));
#23230=CARTESIAN_POINT('Ctrl Pts',(-0.194049700153669,0.0263991919552629,
0.500912396715811));
#23231=CARTESIAN_POINT('Ctrl Pts',(-0.195388255538518,0.0133149283794744,
0.501662713751695));
#23232=CARTESIAN_POINT('Ctrl Pts',(-0.195399922987737,0.000173483101027086,
0.502413030787579));
#23233=CARTESIAN_POINT('',(-0.195079266632945,-5.12429904213991E-7,0.57241303078758));
#23234=CARTESIAN_POINT('Ctrl Pts',(-0.195459766443919,0.000172969825184949,
0.502413063116928));
#23235=CARTESIAN_POINT('Ctrl Pts',(-0.194982758876813,-0.0515913455672025,
0.50536763959852));
#23236=CARTESIAN_POINT('Ctrl Pts',(-0.147284875895773,-0.169042238585059,
0.512027120374039));
#23237=CARTESIAN_POINT('Ctrl Pts',(0.0509580899086067,-0.225267355827217,
0.522391505443478));
#23238=CARTESIAN_POINT('Ctrl Pts',(0.21690320188124,-0.0793417263625358,
0.533506218325257));
#23239=CARTESIAN_POINT('Ctrl Pts',(0.184284130208876,0.139217340448956,
0.544620931207032));
#23240=CARTESIAN_POINT('Ctrl Pts',(-0.0170379737667661,0.230329798285947,
0.555735644088809));
#23241=CARTESIAN_POINT('Ctrl Pts',(-0.17183815729343,0.130524775720848,
0.564999677282324));
#23242=CARTESIAN_POINT('Ctrl Pts',(-0.19507850314188,0.0326461576927833,
0.570558806181915));
#23243=CARTESIAN_POINT('Ctrl Pts',(-0.195079266632945,-5.12429904213991E-7,
0.57241303078758));
#23244=CARTESIAN_POINT('',(-0.195399923222036,-0.000173219001145046,0.64241303078758));
#23245=CARTESIAN_POINT('Ctrl Pts',(-0.195079266632945,-5.12429904213991E-7,
0.57241303078758));
#23246=CARTESIAN_POINT('Ctrl Pts',(-0.195080028664364,-0.0325847684584389,
0.57426371047584));
#23247=CARTESIAN_POINT('Ctrl Pts',(-0.171903476033457,-0.130398931487736,
0.579819294458025));
#23248=CARTESIAN_POINT('Ctrl Pts',(-0.0172578326063497,-0.230313429357155,
0.589079782734138));
#23249=CARTESIAN_POINT('Ctrl Pts',(0.18415115313644,-0.139393189672384,
0.600194495615913));
#23250=CARTESIAN_POINT('Ctrl Pts',(0.216978840527336,0.0791346402780385,
0.61130920849769));
#23251=CARTESIAN_POINT('Ctrl Pts',(0.0511731008232275,0.225218609978527,
0.622423921379466));
#23252=CARTESIAN_POINT('Ctrl Pts',(-0.147191262382175,0.169163591660262,
0.632791851033313));
#23253=CARTESIAN_POINT('Ctrl Pts',(-0.194984294593638,0.0516524436523172,
0.639454876393235));
#23254=CARTESIAN_POINT('Ctrl Pts',(-0.195461647808511,-0.000172689824079368,
0.642412997459232));
#23255=CARTESIAN_POINT('',(-0.195399970524701,0.000107326353575181,0.712413030787581));
#23256=CARTESIAN_POINT('Ctrl Pts',(-0.195399923222036,-0.000173219001145046,
0.64241303078758));
#23257=CARTESIAN_POINT('Ctrl Pts',(-0.195388328972743,-0.0132521272423538,
0.643159802906059));
#23258=CARTESIAN_POINT('Ctrl Pts',(-0.194062470003487,-0.0262744897130095,
0.643906575024539));
#23259=CARTESIAN_POINT('Ctrl Pts',(-0.191462569052284,-0.0390287669789766,
0.644653347143019));
#23260=CARTESIAN_POINT('Ctrl Pts',(-0.189037885771796,-0.0509234827477472,
0.645349791316854));
#23261=CARTESIAN_POINT('Ctrl Pts',(-0.185491931481621,-0.0626334861551503,
0.646046235490689));
#23262=CARTESIAN_POINT('Ctrl Pts',(-0.180872500984137,-0.0739344195063672,
0.646742679664524));
#23263=CARTESIAN_POINT('Ctrl Pts',(-0.176262765785313,-0.0852116343658677,
0.647437662135608));
#23264=CARTESIAN_POINT('Ctrl Pts',(-0.170584285221288,-0.0960806525873972,
0.648132644606691));
#23265=CARTESIAN_POINT('Ctrl Pts',(-0.163934358114472,-0.106332902855118,
0.648827627077775));
#23266=CARTESIAN_POINT('Ctrl Pts',(-0.15728536801075,-0.116583708537047,
0.649522511622864));
#23267=CARTESIAN_POINT('Ctrl Pts',(-0.14966564023064,-0.126217160146402,
0.650217396167953));
#23268=CARTESIAN_POINT('Ctrl Pts',(-0.141217295086143,-0.135051233124889,
0.650912280713043));
#23269=CARTESIAN_POINT('Ctrl Pts',(-0.132769452147797,-0.143884780967896,
0.651607123951191));
#23270=CARTESIAN_POINT('Ctrl Pts',(-0.123493714240925,-0.151918430079598,
0.652301967189339));
#23271=CARTESIAN_POINT('Ctrl Pts',(-0.113569054817426,-0.159007011756955,
0.652996810427488));
#23272=CARTESIAN_POINT('Ctrl Pts',(-0.10362152154304,-0.166111930837277,
0.653693255105035));
#23273=CARTESIAN_POINT('Ctrl Pts',(-0.0930228308847063,-0.172266978237357,
0.654389699782582));
#23274=CARTESIAN_POINT('Ctrl Pts',(-0.0819798273856736,-0.177370989459424,
0.655086144460129));
#23275=CARTESIAN_POINT('Ctrl Pts',(-0.0783756186526551,-0.179036833522736,
0.65531344964835));
#23276=CARTESIAN_POINT('Ctrl Pts',(-0.0747242413317422,-0.18059110011559,
0.655540754836572));
#23277=CARTESIAN_POINT('Ctrl Pts',(-0.0710332795173808,-0.182031407182952,
0.655768060024794));
#23278=CARTESIAN_POINT('Ctrl Pts',(-0.0597244797861847,-0.186444388133568,
0.656464504198629));
#23279=CARTESIAN_POINT('Ctrl Pts',(-0.047962838762106,-0.189815110912198,
0.657160948372464));
#23280=CARTESIAN_POINT('Ctrl Pts',(-0.0359627799780109,-0.192062069280358,
0.6578573925463));
#23281=CARTESIAN_POINT('Ctrl Pts',(-0.0239879070158319,-0.194304311713844,
0.658552375017384));
#23282=CARTESIAN_POINT('Ctrl Pts',(-0.0117764478623286,-0.195427238229025,
0.659247357488468));
#23283=CARTESIAN_POINT('Ctrl Pts',(0.000443592909847119,-0.195399496481773,
0.659942339959553));
#23284=CARTESIAN_POINT('Ctrl Pts',(0.0126619118261549,-0.195371758643451,
0.660637224504643));
#23285=CARTESIAN_POINT('Ctrl Pts',(0.0248879355031087,-0.194193630295803,
0.661332109049732));
#23286=CARTESIAN_POINT('Ctrl Pts',(0.03689165842973,-0.191885813801605,
0.662026993594822));
#23287=CARTESIAN_POINT('Ctrl Pts',(0.0488946678031806,-0.189578134493993,
0.662721836832971));
#23288=CARTESIAN_POINT('Ctrl Pts',(0.060674547700274,-0.186141091960471,
0.663416680071121));
#23289=CARTESIAN_POINT('Ctrl Pts',(0.072012274422929,-0.181646338615555,
0.66411152330927));
#23290=CARTESIAN_POINT('Ctrl Pts',(0.0833761317622014,-0.177141225991453,
0.664807967986818));
#23291=CARTESIAN_POINT('Ctrl Pts',(0.0942950118476686,-0.171573918756561,
0.665504412664366));
#23292=CARTESIAN_POINT('Ctrl Pts',(0.104571749584314,-0.165063349017508,
0.666200857341914));
#23293=CARTESIAN_POINT('Ctrl Pts',(0.107925864966069,-0.162938433245075,
0.666428162530133));
#23294=CARTESIAN_POINT('Ctrl Pts',(0.111211811144147,-0.1607133807298,0.666655467718352));
#23295=CARTESIAN_POINT('Ctrl Pts',(0.11442347405062,-0.15839327190947,0.666882772906571));
#23296=CARTESIAN_POINT('Ctrl Pts',(0.124263741829205,-0.151284651630083,
0.667579217080406));
#23297=CARTESIAN_POINT('Ctrl Pts',(0.133473867314389,-0.14323036332032,
0.668275661254241));
#23298=CARTESIAN_POINT('Ctrl Pts',(0.141869092411777,-0.134366367139469,
0.668972105428076));
#23299=CARTESIAN_POINT('Ctrl Pts',(0.150246697541793,-0.12552097478659,
0.669667087899161));
#23300=CARTESIAN_POINT('Ctrl Pts',(0.15781214669954,-0.115869825753562,
0.670362070370245));
#23301=CARTESIAN_POINT('Ctrl Pts',(0.164415456503192,-0.105587488192717,
0.671057052841329));
#23302=CARTESIAN_POINT('Ctrl Pts',(0.171017835872326,-0.0953065994570916,
0.671751937386419));
#23303=CARTESIAN_POINT('Ctrl Pts',(0.176657833757992,-0.084395409549357,
0.672446821931509));
#23304=CARTESIAN_POINT('Ctrl Pts',(0.18122811815165,-0.0730583957612789,
0.673141706476599));
#23305=CARTESIAN_POINT('Ctrl Pts',(0.18579813086785,-0.0617220558942993,
0.673836549714748));
#23306=CARTESIAN_POINT('Ctrl Pts',(0.189298253693658,-0.0499607646398732,
0.674531392952897));
#23307=CARTESIAN_POINT('Ctrl Pts',(0.191669918078142,-0.0379974012784856,
0.675226236191046));
#23308=CARTESIAN_POINT('Ctrl Pts',(0.194047048554224,-0.0260064653649362,
0.675922680868594));
#23309=CARTESIAN_POINT('Ctrl Pts',(0.195290421868306,-0.0138133986887334,
0.676619125546141));
#23310=CARTESIAN_POINT('Ctrl Pts',(0.195393047293897,-0.00164835348302706,
0.677315570223689));
#23311=CARTESIAN_POINT('Ctrl Pts',(0.195426542117581,0.00232206653642397,
0.677542875411908));
#23312=CARTESIAN_POINT('Ctrl Pts',(0.195338935489874,0.00628951232178161,
0.677770180600127));
#23313=CARTESIAN_POINT('Ctrl Pts',(0.19513118049701,0.0102460918326651,
0.677997485788346));
#23314=CARTESIAN_POINT('Ctrl Pts',(0.194494636494213,0.0223687220737979,
0.678693929962181));
#23315=CARTESIAN_POINT('Ctrl Pts',(0.19272183080269,0.0344747177622865,
0.679390374136016));
#23316=CARTESIAN_POINT('Ctrl Pts',(0.189826807689656,0.0463351171613335,
0.680086818309852));
#23317=CARTESIAN_POINT('Ctrl Pts',(0.186937860674904,0.0581706238567293,
0.680781800780936));
#23318=CARTESIAN_POINT('Ctrl Pts',(0.182931504261327,0.0697606974934034,
0.68147678325202));
#23319=CARTESIAN_POINT('Ctrl Pts',(0.177873078646798,0.0808846579563145,
0.682171765723104));
#23320=CARTESIAN_POINT('Ctrl Pts',(0.172815365786014,0.092007051005748,
0.682866650268194));
#23321=CARTESIAN_POINT('Ctrl Pts',(0.166706197981058,0.102662646253495,
0.683561534813284));
#23322=CARTESIAN_POINT('Ctrl Pts',(0.159659173886027,0.11265038035458,0.684256419358373));
#23323=CARTESIAN_POINT('Ctrl Pts',(0.152612568696564,0.122637520741584,
0.684951262596522));
#23324=CARTESIAN_POINT('Ctrl Pts',(0.144628744630301,0.131956178640988,
0.685646105834671));
#23325=CARTESIAN_POINT('Ctrl Pts',(0.135863204903233,0.140436282895205,
0.686340949072821));
#23326=CARTESIAN_POINT('Ctrl Pts',(0.127077462805474,0.148935931662935,
0.687037393750368));
#23327=CARTESIAN_POINT('Ctrl Pts',(0.117507082402367,0.156592606601072,
0.687733838427916));
#23328=CARTESIAN_POINT('Ctrl Pts',(0.107341647001269,0.163275628368275,
0.688430283105464));
#23329=CARTESIAN_POINT('Ctrl Pts',(0.104023858407757,0.165456828928265,
0.688657588293683));
#23330=CARTESIAN_POINT('Ctrl Pts',(0.100642898521159,0.167534667041848,
0.688884893481903));
#23331=CARTESIAN_POINT('Ctrl Pts',(0.0972059150784287,0.169505663839782,
0.689112198670122));
#23332=CARTESIAN_POINT('Ctrl Pts',(0.086675283934427,0.175544633945664,
0.689808642843958));
#23333=CARTESIAN_POINT('Ctrl Pts',(0.0755424632419164,0.180619895028409,
0.690505087017793));
#23334=CARTESIAN_POINT('Ctrl Pts',(0.0640074427957508,0.184619086951346,
0.691201531191628));
#23335=CARTESIAN_POINT('Ctrl Pts',(0.052496632145219,0.188609885337435,
0.691896513662712));
#23336=CARTESIAN_POINT('Ctrl Pts',(0.0405860918632403,0.19152874278642,
0.692591496133797));
#23337=CARTESIAN_POINT('Ctrl Pts',(0.0284966699988162,0.193310888981916,
0.693286478604881));
#23338=CARTESIAN_POINT('Ctrl Pts',(0.016408951585498,0.195092784065411,
0.69398136314997));
#23339=CARTESIAN_POINT('Ctrl Pts',(0.00414325991087987,0.195738112738375,
0.69467624769506));
#23340=CARTESIAN_POINT('Ctrl Pts',(-0.0080698696734386,0.195233289178495,
0.69537113224015));
#23341=CARTESIAN_POINT('Ctrl Pts',(-0.0202822732565491,0.194728495627508,
0.696065975478299));
#23342=CARTESIAN_POINT('Ctrl Pts',(-0.0324412470448402,0.193073748461682,
0.696760818716448));
#23343=CARTESIAN_POINT('Ctrl Pts',(-0.0443195715802094,0.190307476403179,
0.697455661954597));
#23344=CARTESIAN_POINT('Ctrl Pts',(-0.0562252726745748,0.187534828781357,
0.698152106632145));
#23345=CARTESIAN_POINT('Ctrl Pts',(-0.0678481955474909,0.183645803703173,
0.698848551309693));
#23346=CARTESIAN_POINT('Ctrl Pts',(-0.0789757370253823,0.178728825210982,
0.699544995987241));
#23347=CARTESIAN_POINT('Ctrl Pts',(-0.0826075372122331,0.177124024775759,
0.69977230117546));
#23348=CARTESIAN_POINT('Ctrl Pts',(-0.0861867483306558,0.17541009690366,
0.699999606363679));
#23349=CARTESIAN_POINT('Ctrl Pts',(-0.0897065713936311,0.173591160629795,
0.700226911551899));
#23350=CARTESIAN_POINT('Ctrl Pts',(-0.100491016237783,0.168018091310812,
0.700923355725734));
#23351=CARTESIAN_POINT('Ctrl Pts',(-0.110792303658588,0.161416466578702,
0.701619799899569));
#23352=CARTESIAN_POINT('Ctrl Pts',(-0.120407579127232,0.153893388060434,
0.702316244073404));
#23353=CARTESIAN_POINT('Ctrl Pts',(-0.130002673976764,0.146386099041138,
0.703011226544489));
#23354=CARTESIAN_POINT('Ctrl Pts',(-0.138913885927463,0.137961670266092,
0.703706209015573));
#23355=CARTESIAN_POINT('Ctrl Pts',(-0.14696703457582,0.128770535247741,
0.704401191486657));
#23356=CARTESIAN_POINT('Ctrl Pts',(-0.155019048501184,0.119580695299517,
0.705096076031747));
#23357=CARTESIAN_POINT('Ctrl Pts',(-0.162212628261905,0.109624990825244,
0.705790960576836));
#23358=CARTESIAN_POINT('Ctrl Pts',(-0.168411345553256,0.0990897506755452,
0.706485845121926));
#23359=CARTESIAN_POINT('Ctrl Pts',(-0.17460969436606,0.0885551367860546,
0.707180688360075));
#23360=CARTESIAN_POINT('Ctrl Pts',(-0.179812877054423,0.0774418239730975,
0.707875531598224));
#23361=CARTESIAN_POINT('Ctrl Pts',(-0.18392996612555,0.0659615612387541,
0.708570374836373));
#23362=CARTESIAN_POINT('Ctrl Pts',(-0.18805654405443,0.0544548393780323,
0.709266819513921));
#23363=CARTESIAN_POINT('Ctrl Pts',(-0.191091796750165,0.0425803249356859,
0.709963264191469));
#23364=CARTESIAN_POINT('Ctrl Pts',(-0.192994728892767,0.0305645974880667,
0.710659708869017));
#23365=CARTESIAN_POINT('Ctrl Pts',(-0.193615806722475,0.0266429117072331,
0.710887014057236));
#23366=CARTESIAN_POINT('Ctrl Pts',(-0.194116677820692,0.0227062342853432,
0.711114319245456));
#23367=CARTESIAN_POINT('Ctrl Pts',(-0.194497116087621,0.018762511388367,
0.711341624433675));
#23368=CARTESIAN_POINT('Ctrl Pts',(-0.195094849879869,0.0125662460604494,
0.711698759884977));
#23369=CARTESIAN_POINT('Ctrl Pts',(-0.195396546603586,0.00634096853455841,
0.712055895336279));
#23370=CARTESIAN_POINT('Ctrl Pts',(-0.195399970524701,0.000107326353575181,
0.712413030787581));
#23371=CARTESIAN_POINT('',(-0.195137151677628,0.000105948740446043,0.78241303078758));
#23372=CARTESIAN_POINT('Ctrl Pts',(-0.195646315966217,0.000105752649902963,
0.712413128576354));
#23373=CARTESIAN_POINT('Ctrl Pts',(-0.195258600286138,-0.0584014188700451,
0.715760864822719));
#23374=CARTESIAN_POINT('Ctrl Pts',(-0.136299473324216,-0.18233426378207,
0.72281350536301));
#23375=CARTESIAN_POINT('Ctrl Pts',(0.0744785476940125,-0.218620800615839,
0.733571050197228));
#23376=CARTESIAN_POINT('Ctrl Pts',(0.224073305925668,-0.0559755491269474,
0.744685763079003));
#23377=CARTESIAN_POINT('Ctrl Pts',(0.168540003889559,0.157912556870666,
0.75580047596078));
#23378=CARTESIAN_POINT('Ctrl Pts',(-0.0412833593056294,0.227239505308745,
0.766915188842555));
#23379=CARTESIAN_POINT('Ctrl Pts',(-0.178583972525577,0.116540859079365,
0.77578604045149));
#23380=CARTESIAN_POINT('Ctrl Pts',(-0.195263680442012,0.025810945614826,
0.780951987766498));
#23381=CARTESIAN_POINT('Ctrl Pts',(-0.195137151677628,0.000105948740446043,
0.78241303078758));
#23382=CARTESIAN_POINT('',(-0.195399931100211,-0.000164091537283115,0.852413032945658));
#23383=CARTESIAN_POINT('Ctrl Pts',(-0.195137151677628,0.000105948740446043,
0.78241303078758));
#23384=CARTESIAN_POINT('Ctrl Pts',(-0.194942829545969,-0.0393716341730415,
0.784656892060423));
#23385=CARTESIAN_POINT('Ctrl Pts',(-0.164138066225684,-0.144310627331788,
0.790605657627189));
#23386=CARTESIAN_POINT('Ctrl Pts',(0.00717786579426044,-0.230847540102041,
0.800259327487886));
#23387=CARTESIAN_POINT('Ctrl Pts',(0.197850773711331,-0.119151919289399,
0.811374040369659));
#23388=CARTESIAN_POINT('Ctrl Pts',(0.207401056306211,0.101621407053779,
0.822488753251437));
#23389=CARTESIAN_POINT('Ctrl Pts',(0.0270859008837076,0.229365347212347,
0.833603466133214));
#23390=CARTESIAN_POINT('Ctrl Pts',(-0.156988350126302,0.155570214827098,
0.843578225311926));
#23391=CARTESIAN_POINT('Ctrl Pts',(-0.194901910843352,0.0448913918449987,
0.849848080196716));
#23392=CARTESIAN_POINT('Ctrl Pts',(-0.195259979386646,-0.000163936101596873,
0.85241303078758));
#23393=CARTESIAN_POINT('',(-0.195431382385093,-1.17372835601258E-5,0.922413030787581));
#23394=CARTESIAN_POINT('Ctrl Pts',(-0.195399931100211,-0.000164091537283115,
0.852413032945658));
#23395=CARTESIAN_POINT('Ctrl Pts',(-0.195387601258696,-0.014846446413594,
0.853248290872073));
#23396=CARTESIAN_POINT('Ctrl Pts',(-0.193716398613149,-0.0294560944962259,
0.854083548798487));
#23397=CARTESIAN_POINT('Ctrl Pts',(-0.190458429453141,-0.0436663102430562,
0.854918806724902));
#23398=CARTESIAN_POINT('Ctrl Pts',(-0.189269949741117,-0.0488500772737278,
0.85522350178219));
#23399=CARTESIAN_POINT('Ctrl Pts',(-0.187870778448972,-0.0539808948332623,
0.855528196839478));
#23400=CARTESIAN_POINT('Ctrl Pts',(-0.186265973958097,-0.0590436020703462,
0.855832891896766));
#23401=CARTESIAN_POINT('Ctrl Pts',(-0.182597858210626,-0.0706154765552344,
0.856529336070601));
#23402=CARTESIAN_POINT('Ctrl Pts',(-0.177834270151388,-0.0818851793211283,
0.857225780244437));
#23403=CARTESIAN_POINT('Ctrl Pts',(-0.172046446622527,-0.0926346598448002,
0.857922224418272));
#23404=CARTESIAN_POINT('Ctrl Pts',(-0.166270770625217,-0.103361579270478,
0.858617206889356));
#23405=CARTESIAN_POINT('Ctrl Pts',(-0.159475471208498,-0.113569644927268,
0.859312189360441));
#23406=CARTESIAN_POINT('Ctrl Pts',(-0.151779343759101,-0.123061735759158,
0.860007171831525));
#23407=CARTESIAN_POINT('Ctrl Pts',(-0.144084300726887,-0.132552489114963,
0.860702056376615));
#23408=CARTESIAN_POINT('Ctrl Pts',(-0.135489196498889,-0.14132675972071,
0.861396940921705));
#23409=CARTESIAN_POINT('Ctrl Pts',(-0.126154591561029,-0.149218561271948,
0.862091825466795));
#23410=CARTESIAN_POINT('Ctrl Pts',(-0.11682054151243,-0.157109893700393,
0.862786668704944));
#23411=CARTESIAN_POINT('Ctrl Pts',(-0.106747764067875,-0.164118316227588,
0.863481511943094));
#23412=CARTESIAN_POINT('Ctrl Pts',(-0.0961295716375537,-0.170118386592339,
0.864176355181243));
#23413=CARTESIAN_POINT('Ctrl Pts',(-0.0854869069367005,-0.176132285614475,
0.864872799858791));
#23414=CARTESIAN_POINT('Ctrl Pts',(-0.0742971116057915,-0.181132818848136,
0.865569244536339));
#23415=CARTESIAN_POINT('Ctrl Pts',(-0.0627765628032877,-0.185041247192632,
0.866265689213887));
#23416=CARTESIAN_POINT('Ctrl Pts',(-0.0590164931260377,-0.18631687764703,
0.866492994402105));
#23417=CARTESIAN_POINT('Ctrl Pts',(-0.0552213102693736,-0.187476570738043,
0.866720299590323));
#23418=CARTESIAN_POINT('Ctrl Pts',(-0.0513988075906684,-0.188518759221085,
0.866947604778542));
#23419=CARTESIAN_POINT('Ctrl Pts',(-0.0396869776015631,-0.191711937972271,
0.867644048952377));
#23420=CARTESIAN_POINT('Ctrl Pts',(-0.0276349858024966,-0.193820839417297,
0.868340493126212));
#23421=CARTESIAN_POINT('Ctrl Pts',(-0.0154646684568284,-0.19478707356886,
0.869036937300047));
#23422=CARTESIAN_POINT('Ctrl Pts',(-0.00331989427314309,-0.195751279780251,
0.869731919771132));
#23423=CARTESIAN_POINT('Ctrl Pts',(0.00894185425223248,-0.195577435837087,
0.870426902242216));
#23424=CARTESIAN_POINT('Ctrl Pts',(0.0210905360275125,-0.19425846002188,
0.8711218847133));
#23425=CARTESIAN_POINT('Ctrl Pts',(0.033237506001712,-0.19293967005599,
0.87181676925839));
#23426=CARTESIAN_POINT('Ctrl Pts',(0.045270566630233,-0.190476117080456,
0.872511653803479));
#23427=CARTESIAN_POINT('Ctrl Pts',(0.0569631881244799,-0.186912694054457,
0.873206538348569));
#23428=CARTESIAN_POINT('Ctrl Pts',(0.0686551145587711,-0.183349482853724,
0.873901381586718));
#23429=CARTESIAN_POINT('Ctrl Pts',(0.0800058121102576,-0.178686812281845,
0.874596224824868));
#23430=CARTESIAN_POINT('Ctrl Pts',(0.0908050556088387,-0.173019079514011,
0.875291068063017));
#23431=CARTESIAN_POINT('Ctrl Pts',(0.101629188655255,-0.167338284043603,
0.875987512740565));
#23432=CARTESIAN_POINT('Ctrl Pts',(0.111898585544175,-0.160648266128358,
0.876683957418112));
#23433=CARTESIAN_POINT('Ctrl Pts',(0.121429753732272,-0.153088127915002,
0.87738040209566));
#23434=CARTESIAN_POINT('Ctrl Pts',(0.12454053058044,-0.150620654625375,
0.877607707283879));
#23435=CARTESIAN_POINT('Ctrl Pts',(0.127572937694772,-0.1480608093031,0.877835012472099));
#23436=CARTESIAN_POINT('Ctrl Pts',(0.130521432134136,-0.145414290060001,
0.878062317660318));
#23437=CARTESIAN_POINT('Ctrl Pts',(0.13955537363792,-0.137305575418522,
0.878758761834154));
#23438=CARTESIAN_POINT('Ctrl Pts',(0.147862765089638,-0.128323080280893,
0.879455206007989));
#23439=CARTESIAN_POINT('Ctrl Pts',(0.155274250962847,-0.118621528349313,
0.880151650181824));
#23440=CARTESIAN_POINT('Ctrl Pts',(0.162670181548645,-0.108940338114593,
0.880846632652908));
#23441=CARTESIAN_POINT('Ctrl Pts',(0.169173353157778,-0.0985437301274514,
0.881541615123992));
#23442=CARTESIAN_POINT('Ctrl Pts',(0.174653070267297,-0.0876211449720145,
0.882236597595076));
#23443=CARTESIAN_POINT('Ctrl Pts',(0.180132015261302,-0.0767000988554146,
0.882931482140165));
#23444=CARTESIAN_POINT('Ctrl Pts',(0.18458735875612,-0.0652539835451398,
0.883626366685255));
#23445=CARTESIAN_POINT('Ctrl Pts',(0.18793397850948,-0.053497473973997,
0.884321251230345));
#23446=CARTESIAN_POINT('Ctrl Pts',(0.191280399325297,-0.0417416632605951,
0.885016094468493));
#23447=CARTESIAN_POINT('Ctrl Pts',(0.19351801319233,-0.0296763445350412,
0.885710937706643));
#23448=CARTESIAN_POINT('Ctrl Pts',(0.194612132955479,-0.0175293384506979,
0.886405780944792));
#23449=CARTESIAN_POINT('Ctrl Pts',(0.195708774390279,-0.00535433656377403,
0.887102225622339));
#23450=CARTESIAN_POINT('Ctrl Pts',(0.195656646472601,0.00690185105100441,
0.887798670299887));
#23451=CARTESIAN_POINT('Ctrl Pts',(0.194473119647808,0.0190096221543002,
0.888495114977434));
#23452=CARTESIAN_POINT('Ctrl Pts',(0.194086840886055,0.022961349087221,
0.888722420165654));
#23453=CARTESIAN_POINT('Ctrl Pts',(0.193580453103342,0.0268973206819572,
0.888949725353874));
#23454=CARTESIAN_POINT('Ctrl Pts',(0.192955738064007,0.0308097898106166,
0.889177030542093));
#23455=CARTESIAN_POINT('Ctrl Pts',(0.191041663190223,0.0427972695127193,
0.889873474715929));
#23456=CARTESIAN_POINT('Ctrl Pts',(0.187999447141525,0.0546481299516366,
0.890569918889764));
#23457=CARTESIAN_POINT('Ctrl Pts',(0.183867251760222,0.0661361756540484,
0.891266363063599));
#23458=CARTESIAN_POINT('Ctrl Pts',(0.179743729064517,0.0776001101518047,
0.891961345534684));
#23459=CARTESIAN_POINT('Ctrl Pts',(0.174534990886009,0.0887019003319478,
0.892656328005768));
#23460=CARTESIAN_POINT('Ctrl Pts',(0.168329332575936,0.0992290068202845,
0.893351310476852));
#23461=CARTESIAN_POINT('Ctrl Pts',(0.162124548669588,0.109754629994414,
0.894046195021942));
#23462=CARTESIAN_POINT('Ctrl Pts',(0.15492352779897,0.11970495359588,0.894741079567032));
#23463=CARTESIAN_POINT('Ctrl Pts',(0.146860480482702,0.128892045031453,
0.895435964112122));
#23464=CARTESIAN_POINT('Ctrl Pts',(0.138797912468814,0.138078590346605,
0.896130807350271));
#23465=CARTESIAN_POINT('Ctrl Pts',(0.129874017515357,0.146501352994742,
0.89682565058842));
#23466=CARTESIAN_POINT('Ctrl Pts',(0.120261400861954,0.154007647416355,
0.897520493826569));
#23467=CARTESIAN_POINT('Ctrl Pts',(0.110626629537989,0.161531241964047,
0.898216938504117));
#23468=CARTESIAN_POINT('Ctrl Pts',(0.100300697351395,0.168133663992845,
0.898913383181665));
#23469=CARTESIAN_POINT('Ctrl Pts',(0.0894859359502034,0.173705000696917,
0.899609827859213));
#23470=CARTESIAN_POINT('Ctrl Pts',(0.0859562207336297,0.175523370165416,
0.899837133047432));
#23471=CARTESIAN_POINT('Ctrl Pts',(0.0823746110938788,0.177232280159951,
0.900064438235651));
#23472=CARTESIAN_POINT('Ctrl Pts',(0.0787485823833833,0.178829026650059,
0.900291743423871));
#23473=CARTESIAN_POINT('Ctrl Pts',(0.0676387322767088,0.183721324968634,
0.900988187597706));
#23474=CARTESIAN_POINT('Ctrl Pts',(0.056031907477925,0.187591672462066,
0.901684631771541));
#23475=CARTESIAN_POINT('Ctrl Pts',(0.0441388519136026,0.190349472685766,
0.902381075945376));
#23476=CARTESIAN_POINT('Ctrl Pts',(0.0322707575919605,0.193101484815709,
0.90307605841646));
#23477=CARTESIAN_POINT('Ctrl Pts',(0.0201184525329993,0.194745315819805,
0.903771040887544));
#23478=CARTESIAN_POINT('Ctrl Pts',(0.00790839292281639,0.195239896848411,
0.904466023358628));
#23479=CARTESIAN_POINT('Ctrl Pts',(-0.00429994623788739,0.195734408188442,
0.905160907903718));
#23480=CARTESIAN_POINT('Ctrl Pts',(-0.0165651520216134,0.195079909574438,
0.905855792448807));
#23481=CARTESIAN_POINT('Ctrl Pts',(-0.0286565442593787,0.193287253773006,
0.906550676993897));
#23482=CARTESIAN_POINT('Ctrl Pts',(-0.040747217732531,0.191494704534782,
0.907245520232046));
#23483=CARTESIAN_POINT('Ctrl Pts',(-0.0526632358035508,0.188564287312229,
0.907940363470195));
#23484=CARTESIAN_POINT('Ctrl Pts',(-0.0641827124220688,0.18455822773896,
0.908635206708344));
#23485=CARTESIAN_POINT('Ctrl Pts',(-0.0757287385451317,0.180542935203087,
0.909331651385891));
#23486=CARTESIAN_POINT('Ctrl Pts',(-0.0868755933593291,0.175447399910341,
0.910028096063439));
#23487=CARTESIAN_POINT('Ctrl Pts',(-0.0974212086587235,0.169382018241233,
0.910724540740986));
#23488=CARTESIAN_POINT('Ctrl Pts',(-0.100863080135097,0.167402402678979,
0.910951845929206));
#23489=CARTESIAN_POINT('Ctrl Pts',(-0.104241124651882,0.165319828256848,
0.911179151117426));
#23490=CARTESIAN_POINT('Ctrl Pts',(-0.107549016585019,0.163139109448333,
0.911406456305646));
#23491=CARTESIAN_POINT('Ctrl Pts',(-0.117666821493063,0.156468973933073,
0.91210171165119));
#23492=CARTESIAN_POINT('Ctrl Pts',(-0.127198156063682,0.14882995897731,
0.912796966996734));
#23493=CARTESIAN_POINT('Ctrl Pts',(-0.135952990562336,0.140349365360722,
0.913492222342278));
#23494=CARTESIAN_POINT('Ctrl Pts',(-0.14468945725879,0.131886564183969,
0.914186019029447));
#23495=CARTESIAN_POINT('Ctrl Pts',(-0.152651979732653,0.122586239953042,
0.914879815716616));
#23496=CARTESIAN_POINT('Ctrl Pts',(-0.159683572942223,0.112615791665316,
0.915573612403784));
#23497=CARTESIAN_POINT('Ctrl Pts',(-0.166714187837885,0.102646730577892,
0.916267312562197));
#23498=CARTESIAN_POINT('Ctrl Pts',(-0.172813587453725,0.0920084215366531,
0.916961012720609));
#23499=CARTESIAN_POINT('Ctrl Pts',(-0.177866113483614,0.0808999732647313,
0.917654712879021));
#23500=CARTESIAN_POINT('Ctrl Pts',(-0.182918437048923,0.0697919701300136,
0.918348385239514));
#23501=CARTESIAN_POINT('Ctrl Pts',(-0.186923632136932,0.0582146770278337,
0.919042057600007));
#23502=CARTESIAN_POINT('Ctrl Pts',(-0.189813979213258,0.0463876416217614,
0.9197357299605));
#23503=CARTESIAN_POINT('Ctrl Pts',(-0.192710927053388,0.0345335964950021,
0.920430986479327));
#23504=CARTESIAN_POINT('Ctrl Pts',(-0.194487802582643,0.0224295396783319,
0.921126242998154));
#23505=CARTESIAN_POINT('Ctrl Pts',(-0.195128111370912,0.0103043754211897,
0.921821499516981));
#23506=CARTESIAN_POINT('Ctrl Pts',(-0.195309705099675,0.00686563800316279,
0.922018676607181));
#23507=CARTESIAN_POINT('Ctrl Pts',(-0.195400206064584,0.00342520612777168,
0.922215853697381));
#23508=CARTESIAN_POINT('Ctrl Pts',(-0.195399999647596,-1.17353987651412E-5,
0.922413030787581));
#23509=CARTESIAN_POINT('',(-0.195294337528581,0.000171262189333537,0.99241303078758));
#23510=CARTESIAN_POINT('Ctrl Pts',(-0.195719607651052,-1.17545938899131E-5,
0.922413030787581));
#23511=CARTESIAN_POINT('Ctrl Pts',(-0.195720155584114,-0.000641092913902824,
0.922449076920861));
#23512=CARTESIAN_POINT('Ctrl Pts',(-0.195717382600782,-0.00127042626739718,
0.922485123054142));
#23513=CARTESIAN_POINT('Ctrl Pts',(-0.195083429571586,-0.0665807256656151,
0.926226073481348));
#23514=CARTESIAN_POINT('Ctrl Pts',(-0.123353837031904,-0.19525864748591,
0.933635882069198));
#23515=CARTESIAN_POINT('Ctrl Pts',(0.0971649057626222,-0.209525868609732,
0.944750594950976));
#23516=CARTESIAN_POINT('Ctrl Pts',(0.228733969509715,-0.0319824908481484,
0.955865307832749));
#23517=CARTESIAN_POINT('Ctrl Pts',(0.150908365342008,0.174839279906791,
0.966980020714528));
#23518=CARTESIAN_POINT('Ctrl Pts',(-0.0650664044878207,0.2216043129895,
0.978094733596303));
#23519=CARTESIAN_POINT('Ctrl Pts',(-0.184366805427636,0.102537997645834,
0.986572403620654));
#23520=CARTESIAN_POINT('Ctrl Pts',(-0.195452091727079,0.0189207190229355,
0.99134516935108));
#23521=CARTESIAN_POINT('Ctrl Pts',(-0.195294337528581,0.000171262189333537,
0.99241303078758));
#23522=CARTESIAN_POINT('',(-0.195387463526517,-8.85805956595877E-5,1.06241303507908));
#23523=CARTESIAN_POINT('Ctrl Pts',(-0.195294337528581,0.000171262189333537,
0.99241303078758));
#23524=CARTESIAN_POINT('Ctrl Pts',(-0.194904769586374,-0.0461298022874415,
0.995050073645006));
#23525=CARTESIAN_POINT('Ctrl Pts',(-0.155279374437814,-0.158080892225847,
1.00139202079636));
#23526=CARTESIAN_POINT('Ctrl Pts',(0.0315331778821316,-0.228796344422667,
1.01143887224164));
#23527=CARTESIAN_POINT('Ctrl Pts',(0.209334625055623,-0.0975762434270945,
1.0225535851234));
#23528=CARTESIAN_POINT('Ctrl Pts',(0.19550054738536,0.122970095960548,1.03366829800519));
#23529=CARTESIAN_POINT('Ctrl Pts',(0.0026953606810326,0.230943377387883,
1.04478301088697));
#23530=CARTESIAN_POINT('Ctrl Pts',(-0.165641881126728,0.141768188472822,
1.05436458848109));
#23531=CARTESIAN_POINT('Ctrl Pts',(-0.194962120753271,0.0381301666874187,
1.0602412617813));
#23532=CARTESIAN_POINT('Ctrl Pts',(-0.195118116536412,-8.83829588442778E-5,
1.06241303078758));
#23533=CARTESIAN_POINT('',(-0.195399960265364,-0.000124612576654666,1.13241303078758));
#23534=CARTESIAN_POINT('Ctrl Pts',(-0.195399979917734,-8.85897797224884E-5,
1.0624130352785));
#23535=CARTESIAN_POINT('Ctrl Pts',(-0.195393855063461,-0.01359800819892,
1.06317960217384));
#23536=CARTESIAN_POINT('Ctrl Pts',(-0.193982436345336,-0.0270604850983458,
1.06394616906917));
#23537=CARTESIAN_POINT('Ctrl Pts',(-0.191219944617096,-0.0402006564701958,
1.06471273596451));
#23538=CARTESIAN_POINT('Ctrl Pts',(-0.188457452888856,-0.0533408278420449,
1.06547930285984));
#23539=CARTESIAN_POINT('Ctrl Pts',(-0.184344210097986,-0.066158178502653,
1.06624586975518));
#23540=CARTESIAN_POINT('Ctrl Pts',(-0.178983350055113,-0.0783971963978877,
1.06701243665052));
#23541=CARTESIAN_POINT('Ctrl Pts',(-0.174112881781141,-0.0895166339296635,
1.06770888082435));
#23542=CARTESIAN_POINT('Ctrl Pts',(-0.168185008300444,-0.100219824464572,
1.06840532499819));
#23543=CARTESIAN_POINT('Ctrl Pts',(-0.161293610699711,-0.110297466641124,
1.06910176917202));
#23544=CARTESIAN_POINT('Ctrl Pts',(-0.154416676820853,-0.120353957779523,
1.06979675164311));
#23545=CARTESIAN_POINT('Ctrl Pts',(-0.146580660429029,-0.129786748762222,
1.07049173411419));
#23546=CARTESIAN_POINT('Ctrl Pts',(-0.137924523062689,-0.13841237639001,
1.07118671658528));
#23547=CARTESIAN_POINT('Ctrl Pts',(-0.129269605383025,-0.147036788630075,
1.07188160113037));
#23548=CARTESIAN_POINT('Ctrl Pts',(-0.119795382948273,-0.154853613472036,
1.07257648567545));
#23549=CARTESIAN_POINT('Ctrl Pts',(-0.109679058270219,-0.161714761778132,
1.07327137022054));
#23550=CARTESIAN_POINT('Ctrl Pts',(-0.0995633349502271,-0.168575502227918,
1.07396621345869));
#23551=CARTESIAN_POINT('Ctrl Pts',(-0.0888063249583923,-0.174480209485929,
1.07466105669684));
#23552=CARTESIAN_POINT('Ctrl Pts',(-0.0776135147199785,-0.179324572585052,
1.07535589993499));
#23553=CARTESIAN_POINT('Ctrl Pts',(-0.0663949078610987,-0.184180100726163,
1.07605234461253));
#23554=CARTESIAN_POINT('Ctrl Pts',(-0.0547393245482148,-0.187970117850791,
1.07674878929008));
#23555=CARTESIAN_POINT('Ctrl Pts',(-0.0428702513051903,-0.19063919206981,
1.07744523396763));
#23556=CARTESIAN_POINT('Ctrl Pts',(-0.0389964304340447,-0.19151032288218,
1.07767253915585));
#23557=CARTESIAN_POINT('Ctrl Pts',(-0.035099945031278,-0.19226245484328,
1.07789984434406));
#23558=CARTESIAN_POINT('Ctrl Pts',(-0.0311887104378679,-0.192894853070845,
1.07812714953228));
#23559=CARTESIAN_POINT('Ctrl Pts',(-0.0192050132489323,-0.194832468593762,
1.07882359370612));
#23560=CARTESIAN_POINT('Ctrl Pts',(-0.00699764327111413,-0.195655930708425,
1.07952003787995));
#23561=CARTESIAN_POINT('Ctrl Pts',(0.0052066348891197,-0.195330619599517,
1.08021648205379));
#23562=CARTESIAN_POINT('Ctrl Pts',(0.0173852986101341,-0.195005991256236,
1.08091146452487));
#23563=CARTESIAN_POINT('Ctrl Pts',(0.0295600148048395,-0.193537323766802,
1.08160644699596));
#23564=CARTESIAN_POINT('Ctrl Pts',(0.0415012821371695,-0.190941885349891,
1.08230142946704));
#23565=CARTESIAN_POINT('Ctrl Pts',(0.0534408668939978,-0.188346812641325,
1.08299631401213));
#23566=CARTESIAN_POINT('Ctrl Pts',(0.0651462038917023,-0.184625424846013,
1.08369119855722));
#23567=CARTESIAN_POINT('Ctrl Pts',(0.0763967760151574,-0.179846302754574,
1.08438608310231));
#23568=CARTESIAN_POINT('Ctrl Pts',(0.0876466793559811,-0.175067464754807,
1.08508092634046));
#23569=CARTESIAN_POINT('Ctrl Pts',(0.0984410758960655,-0.169231384297636,
1.08577576957861));
#23570=CARTESIAN_POINT('Ctrl Pts',(0.10858089334579,-0.162454146146629,
1.08647061281676));
#23571=CARTESIAN_POINT('Ctrl Pts',(0.118744080531691,-0.1556612881614,1.08716705749431));
#23572=CARTESIAN_POINT('Ctrl Pts',(0.128248985254343,-0.147923482375403,
1.08786350217186));
#23573=CARTESIAN_POINT('Ctrl Pts',(0.136927842490727,-0.13939844314351,
1.08855994684941));
#23574=CARTESIAN_POINT('Ctrl Pts',(0.139760442611373,-0.136616046049164,
1.08878725203763));
#23575=CARTESIAN_POINT('Ctrl Pts',(0.142505350145887,-0.133750076124693,
1.08901455722585));
#23576=CARTESIAN_POINT('Ctrl Pts',(0.145157655356412,-0.130806785341698,
1.08924186241407));
#23577=CARTESIAN_POINT('Ctrl Pts',(0.153284097720414,-0.121788787407829,
1.0899383065879));
#23578=CARTESIAN_POINT('Ctrl Pts',(0.160595719048788,-0.111978682149472,
1.09063475076174));
#23579=CARTESIAN_POINT('Ctrl Pts',(0.166940463028469,-0.101548224030952,
1.09133119493557));
#23580=CARTESIAN_POINT('Ctrl Pts',(0.173271890607384,-0.0911396574435826,
1.09202617740665));
#23581=CARTESIAN_POINT('Ctrl Pts',(0.17863995438636,-0.0801140241338391,
1.09272115987774));
#23582=CARTESIAN_POINT('Ctrl Pts',(0.182934710385865,-0.0686735155357568,
1.09341614234882));
#23583=CARTESIAN_POINT('Ctrl Pts',(0.187228861235931,-0.0572346189541328,
1.09411102689391));
#23584=CARTESIAN_POINT('Ctrl Pts',(0.190449654083029,-0.0453817655091186,
1.094805911439));
#23585=CARTESIAN_POINT('Ctrl Pts',(0.192535129751674,-0.0333374235883074,
1.09550079598409));
#23586=CARTESIAN_POINT('Ctrl Pts',(0.194620481450631,-0.0212937976352359,
1.09619563922224));
#23587=CARTESIAN_POINT('Ctrl Pts',(0.195570526886726,-0.00905957328563089,
1.09689048246039));
#23588=CARTESIAN_POINT('Ctrl Pts',(0.195374848768871,0.00313503884199943,
1.09758532569853));
#23589=CARTESIAN_POINT('Ctrl Pts',(0.19517871966203,0.0153577564922006,
1.09828177037608));
#23590=CARTESIAN_POINT('Ctrl Pts',(0.193831674303266,0.0275398056207277,
1.09897821505363));
#23591=CARTESIAN_POINT('Ctrl Pts',(0.191375249774799,0.0394547053421153,
1.09967465973118));
#23592=CARTESIAN_POINT('Ctrl Pts',(0.190573523438463,0.0433434830312887,
1.0999019649194));
#23593=CARTESIAN_POINT('Ctrl Pts',(0.189654025635844,0.0472039007252778,
1.10012927010761));
#23594=CARTESIAN_POINT('Ctrl Pts',(0.188619346855062,0.0510284429702684,
1.10035657529583));
#23595=CARTESIAN_POINT('Ctrl Pts',(0.185449177206451,0.0627465220205966,
1.10105301946967));
#23596=CARTESIAN_POINT('Ctrl Pts',(0.181171621168803,0.0742095271228536,
1.1017494636435));
#23597=CARTESIAN_POINT('Ctrl Pts',(0.17584853077764,0.085196562274222,1.10244590781734));
#23598=CARTESIAN_POINT('Ctrl Pts',(0.170536612532301,0.0961605377459927,
1.10314089028842));
#23599=CARTESIAN_POINT('Ctrl Pts',(0.164183826259085,0.106649713365788,
1.10383587275951));
#23600=CARTESIAN_POINT('Ctrl Pts',(0.156900433625811,0.116462070769983,
1.10453085523059));
#23601=CARTESIAN_POINT('Ctrl Pts',(0.149618067253625,0.126273045571166,
1.10522573977568));
#23602=CARTESIAN_POINT('Ctrl Pts',(0.141405838948271,0.135406661920326,
1.10592062432077));
#23603=CARTESIAN_POINT('Ctrl Pts',(0.132417068043232,0.143690222669582,
1.10661550886586));
#23604=CARTESIAN_POINT('Ctrl Pts',(0.123428831469583,0.151973291008187,
1.10731035210401));
#23605=CARTESIAN_POINT('Ctrl Pts',(0.113664806061235,0.15940583025075,1.10800519534216));
#23606=CARTESIAN_POINT('Ctrl Pts',(0.103312766041843,0.165854250391069,
1.10870003858031));
#23607=CARTESIAN_POINT('Ctrl Pts',(0.0929368671664764,0.172317532522561,
1.10939648325786));
#23608=CARTESIAN_POINT('Ctrl Pts',(0.0819710253158985,0.177791759835756,
1.11009292793541));
#23609=CARTESIAN_POINT('Ctrl Pts',(0.0706280545274067,0.18218901699519,
1.11078937261296));
#23610=CARTESIAN_POINT('Ctrl Pts',(0.0669259426538131,0.183624191099465,
1.11101667780118));
#23611=CARTESIAN_POINT('Ctrl Pts',(0.0631837944026711,0.18494503456012,
1.1112439829894));
#23612=CARTESIAN_POINT('Ctrl Pts',(0.0594093290239704,0.186149648468434,
1.11147128817762));
#23613=CARTESIAN_POINT('Ctrl Pts',(0.0478446813230984,0.189840485200924,
1.11216773235145));
#23614=CARTESIAN_POINT('Ctrl Pts',(0.0358938395025882,0.19246257433198,
1.11286417652529));
#23615=CARTESIAN_POINT('Ctrl Pts',(0.0237759414585748,0.193948097716266,
1.11356062069913));
#23616=CARTESIAN_POINT('Ctrl Pts',(0.0116834765584835,0.195430503271876,
1.11425560317021));
#23617=CARTESIAN_POINT('Ctrl Pts',(-0.000574497253568146,0.195780898248486,
1.1149505856413));
#23618=CARTESIAN_POINT('Ctrl Pts',(-0.0127684517811844,0.194982375201226,
1.11564556811238));
#23619=CARTESIAN_POINT('Ctrl Pts',(-0.0249606881285953,0.194183964669268,
1.11634045265747));
#23620=CARTESIAN_POINT('Ctrl Pts',(-0.0370880476003977,0.192236968625343,
1.11703533720257));
#23621=CARTESIAN_POINT('Ctrl Pts',(-0.0489222886422267,0.189176556882735,
1.11773022174766));
#23622=CARTESIAN_POINT('Ctrl Pts',(-0.0607558262056203,0.186116327064228,
1.11842506498581));
#23623=CARTESIAN_POINT('Ctrl Pts',(-0.072295438759328,0.181943058096389,
1.11911990822396));
#23624=CARTESIAN_POINT('Ctrl Pts',(-0.0833270586056728,0.176742075647331,
1.11981475146211));
#23625=CARTESIAN_POINT('Ctrl Pts',(-0.0943841035690545,0.171529106238124,
1.12051119613965));
#23626=CARTESIAN_POINT('Ctrl Pts',(-0.104930054533146,0.16528412661991,
1.1212076408172));
#23627=CARTESIAN_POINT('Ctrl Pts',(-0.11477564126072,0.158138269160854,
1.12190408549475));
#23628=CARTESIAN_POINT('Ctrl Pts',(-0.117989037839574,0.155806008570674,
1.12213139068297));
#23629=CARTESIAN_POINT('Ctrl Pts',(-0.121128084378196,0.153378110753885,
1.12235869587118));
#23630=CARTESIAN_POINT('Ctrl Pts',(-0.124186999457379,0.150860031704136,
1.1225860010594));
#23631=CARTESIAN_POINT('Ctrl Pts',(-0.133433078336889,0.1432487195506,1.12327306874371));
#23632=CARTESIAN_POINT('Ctrl Pts',(-0.142013719396526,0.134753546717402,
1.12396013642802));
#23633=CARTESIAN_POINT('Ctrl Pts',(-0.149755525370193,0.125516702558255,
1.12464720411233));
#23634=CARTESIAN_POINT('Ctrl Pts',(-0.157486281429236,0.116293042188485,
1.12533329114183));
#23635=CARTESIAN_POINT('Ctrl Pts',(-0.164379931087259,0.106330434043949,
1.12601937817133));
#23636=CARTESIAN_POINT('Ctrl Pts',(-0.17029965108117,0.0958080833835636,
1.12670546520084));
#23637=CARTESIAN_POINT('Ctrl Pts',(-0.176213704663528,0.0852958048160153,
1.12739089550139));
#23638=CARTESIAN_POINT('Ctrl Pts',(-0.181155218960983,0.0742256220721924,
1.12807632580195));
#23639=CARTESIAN_POINT('Ctrl Pts',(-0.185032122360298,0.0628034528895012,
1.12876175610251));
#23640=CARTESIAN_POINT('Ctrl Pts',(-0.188916347707919,0.0513597117139882,
1.12944848091178));
#23641=CARTESIAN_POINT('Ctrl Pts',(-0.191731670618013,0.0395635195003829,
1.13013520572105));
#23642=CARTESIAN_POINT('Ctrl Pts',(-0.19343566509094,0.0276369946055204,
1.13082193053031));
#23643=CARTESIAN_POINT('Ctrl Pts',(-0.194751682806556,0.0184259799592059,
1.13135229728274));
#23644=CARTESIAN_POINT('Ctrl Pts',(-0.195405867097655,0.0091376531278688,
1.13188266403516));
#23645=CARTESIAN_POINT('Ctrl Pts',(-0.195399960265364,-0.000124612576654666,
1.13241303078758));
#23646=CARTESIAN_POINT('',(-0.195499582979996,0.000166550639662629,1.20241303078758));
#23647=CARTESIAN_POINT('Ctrl Pts',(-0.195617452784838,-0.000124751278337231,
1.13241303078758));
#23648=CARTESIAN_POINT('Ctrl Pts',(-0.195673257048185,-0.00762911832956361,
1.13284225850544));
#23649=CARTESIAN_POINT('Ctrl Pts',(-0.191874449616845,-0.0798508440029845,
1.13697639051729));
#23650=CARTESIAN_POINT('Ctrl Pts',(-0.102028562826224,-0.207201063935842,
1.14481542682289));
#23651=CARTESIAN_POINT('Ctrl Pts',(0.118763095185579,-0.198084415718343,
1.15593013970476));
#23652=CARTESIAN_POINT('Ctrl Pts',(0.230832996956899,-0.00763125444448434,
1.16704485258647));
#23653=CARTESIAN_POINT('Ctrl Pts',(0.131586674709796,0.189807943899515,
1.17815956546829));
#23654=CARTESIAN_POINT('Ctrl Pts',(-0.0881207583724611,0.213487330941126,
1.18927427835005));
#23655=CARTESIAN_POINT('Ctrl Pts',(-0.18925201110573,0.08855622028932,1.19735876678982));
#23656=CARTESIAN_POINT('Ctrl Pts',(-0.195606518663776,0.011980768958621,
1.20173835093566));
#23657=CARTESIAN_POINT('Ctrl Pts',(-0.195499582979996,0.000166550639662629,
1.20241303078758));
#23658=CARTESIAN_POINT('',(-0.195369097555756,2.13661978956508E-5,1.27241302913566));
#23659=CARTESIAN_POINT('Ctrl Pts',(-0.195499582979996,0.000166550639662629,
1.20241303078758));
#23660=CARTESIAN_POINT('Ctrl Pts',(-0.195019297224031,-0.0528952578782005,
1.20544325522959));
#23661=CARTESIAN_POINT('Ctrl Pts',(-0.145266592861051,-0.171625975326032,
1.21217838396553));
#23662=CARTESIAN_POINT('Ctrl Pts',(0.0555353437883074,-0.224182814057769,
1.22261841699537));
#23663=CARTESIAN_POINT('Ctrl Pts',(0.218474097288274,-0.0749077922687062,
1.23373312987716));
#23664=CARTESIAN_POINT('Ctrl Pts',(0.181410589874887,0.142941618886128,
1.24484784275894));
#23665=CARTESIAN_POINT('Ctrl Pts',(-0.0217253653892236,0.229935027838755,
1.2559625556407));
#23666=CARTESIAN_POINT('Ctrl Pts',(-0.173213681772595,0.127838529215634,
1.26515094597265));
#23667=CARTESIAN_POINT('Ctrl Pts',(-0.195111799500146,0.0313356137564543,
1.27063443201065));
#23668=CARTESIAN_POINT('Ctrl Pts',(-0.195081377439699,2.16055737428584E-5,
1.27241301375474));
#23669=CARTESIAN_POINT('',(-0.195399919414568,-0.000177462052753457,1.34241303078758));
#23670=CARTESIAN_POINT('Ctrl Pts',(-0.195399998834656,2.13404888144855E-5,
1.27241303078758));
#23671=CARTESIAN_POINT('Ctrl Pts',(-0.195401390143229,-0.0127179034900279,
1.27313541813527));
#23672=CARTESIAN_POINT('Ctrl Pts',(-0.194152666432573,-0.0254370179035737,
1.27385780548296));
#23673=CARTESIAN_POINT('Ctrl Pts',(-0.191691147325218,-0.0378901575233157,
1.27458019283064));
#23674=CARTESIAN_POINT('Ctrl Pts',(-0.189219297789346,-0.0503955601006223,
1.27530561187158));
#23675=CARTESIAN_POINT('Ctrl Pts',(-0.185524695317359,-0.0626320086384815,
1.27603103091251));
#23676=CARTESIAN_POINT('Ctrl Pts',(-0.180695285645632,-0.0743664826749485,
1.27675644995344));
#23677=CARTESIAN_POINT('Ctrl Pts',(-0.177509646687822,-0.0821069313386492,
1.27723496043705));
#23678=CARTESIAN_POINT('Ctrl Pts',(-0.173831273018624,-0.0896293197676277,
1.27771347092065));
#23679=CARTESIAN_POINT('Ctrl Pts',(-0.16969625686245,-0.096872805300937,
1.27819198140425));
#23680=CARTESIAN_POINT('Ctrl Pts',(-0.163677981381863,-0.107415277139654,
1.27888842557809));
#23681=CARTESIAN_POINT('Ctrl Pts',(-0.15665220988582,-0.117432088334572,
1.27958486975192));
#23682=CARTESIAN_POINT('Ctrl Pts',(-0.148734416313031,-0.126725030692527,
1.28028131392576));
#23683=CARTESIAN_POINT('Ctrl Pts',(-0.140833240670413,-0.135998468946749,
1.28097629639684));
#23684=CARTESIAN_POINT('Ctrl Pts',(-0.132044264372559,-0.144550345597606,
1.28167127886792));
#23685=CARTESIAN_POINT('Ctrl Pts',(-0.122525058852388,-0.152212909942682,
1.28236626133901));
#23686=CARTESIAN_POINT('Ctrl Pts',(-0.113007194628873,-0.159874394599761,
1.2830611458841));
#23687=CARTESIAN_POINT('Ctrl Pts',(-0.102759957644003,-0.166646231538767,
1.28375603042919));
#23688=CARTESIAN_POINT('Ctrl Pts',(-0.0919752079100879,-0.172399887267643,
1.28445091497428));
#23689=CARTESIAN_POINT('Ctrl Pts',(-0.0811910992683102,-0.178153200974355,
1.28514575821242));
#23690=CARTESIAN_POINT('Ctrl Pts',(-0.0698703265727585,-0.182888065000111,
1.28584060145057));
#23691=CARTESIAN_POINT('Ctrl Pts',(-0.0582282489813947,-0.186522467870658,
1.28653544468872));
#23692=CARTESIAN_POINT('Ctrl Pts',(-0.0465593393209889,-0.190165247128322,
1.28723188936627));
#23693=CARTESIAN_POINT('Ctrl Pts',(-0.0345685011667856,-0.19270230300626,
1.28792833404382));
#23694=CARTESIAN_POINT('Ctrl Pts',(-0.022483827539076,-0.194102131619395,
1.28862477872137));
#23695=CARTESIAN_POINT('Ctrl Pts',(-0.0185396391460514,-0.194559006826641,
1.28885208390959));
#23696=CARTESIAN_POINT('Ctrl Pts',(-0.0145854886936885,-0.194895154385967,
1.28907938909781));
#23697=CARTESIAN_POINT('Ctrl Pts',(-0.0106293248611298,-0.195110680007519,
1.28930669428604));
#23698=CARTESIAN_POINT('Ctrl Pts',(0.00149203177601938,-0.195771032569711,
1.29000313845987));
#23699=CARTESIAN_POINT('Ctrl Pts',(0.0137180672259798,-0.1952998332419,
1.29069958263371));
#23700=CARTESIAN_POINT('Ctrl Pts',(0.0258196281200339,-0.193686620094789,
1.29139602680755));
#23701=CARTESIAN_POINT('Ctrl Pts',(0.0378957901587132,-0.192076792772678,
1.29209100927863));
#23702=CARTESIAN_POINT('Ctrl Pts',(0.0498471270121964,-0.18932974962934,
1.29278599174972));
#23703=CARTESIAN_POINT('Ctrl Pts',(0.0614472473301596,-0.185486915429488,
1.29348097422081));
#23704=CARTESIAN_POINT('Ctrl Pts',(0.0730457331416889,-0.181644622701367,
1.2941758587659));
#23705=CARTESIAN_POINT('Ctrl Pts',(0.0842922561667842,-0.176707076630744,
1.29487074331099));
#23706=CARTESIAN_POINT('Ctrl Pts',(0.0949747815777786,-0.170765777790087,
1.29556562785608));
#23707=CARTESIAN_POINT('Ctrl Pts',(0.105656671973292,-0.16482483212591,
1.29626047109423));
#23708=CARTESIAN_POINT('Ctrl Pts',(0.115773878959235,-0.157880701181627,
1.29695531433238));
#23709=CARTESIAN_POINT('Ctrl Pts',(0.125140712575688,-0.150069857253377,
1.29765015757053));
#23710=CARTESIAN_POINT('Ctrl Pts',(0.134529134394443,-0.142241011288818,
1.29834660224808));
#23711=CARTESIAN_POINT('Ctrl Pts',(0.143163099677314,-0.133542074821454,
1.29904304692563));
#23712=CARTESIAN_POINT('Ctrl Pts',(0.150892449754659,-0.124147608140623,
1.29973949160317));
#23713=CARTESIAN_POINT('Ctrl Pts',(0.153415150308972,-0.121081447846931,
1.29996679679139));
#23714=CARTESIAN_POINT('Ctrl Pts',(0.155841817511163,-0.117941449873993,
1.3001941019796));
#23715=CARTESIAN_POINT('Ctrl Pts',(0.158168229811754,-0.114734350036143,
1.30042140716782));
#23716=CARTESIAN_POINT('Ctrl Pts',(0.165296163430056,-0.104908063119737,
1.30111785134165));
#23717=CARTESIAN_POINT('Ctrl Pts',(0.171530130368159,-0.0943802130142339,
1.30181429551548));
#23718=CARTESIAN_POINT('Ctrl Pts',(0.176737076434546,-0.0833376614344879,
1.30251073968932));
#23719=CARTESIAN_POINT('Ctrl Pts',(0.181933094119773,-0.0723182860526738,
1.3032057221604));
#23720=CARTESIAN_POINT('Ctrl Pts',(0.186105932080036,-0.0607871056285705,
1.30390070463148));
#23721=CARTESIAN_POINT('Ctrl Pts',(0.189167629163193,-0.0489567980649938,
1.30459568710257));
#23722=CARTESIAN_POINT('Ctrl Pts',(0.192228894840173,-0.0371281574422114,
1.30529057164766));
#23723=CARTESIAN_POINT('Ctrl Pts',(0.194179066755089,-0.0250013082696133,
1.30598545619274));
#23724=CARTESIAN_POINT('Ctrl Pts',(0.194980042692081,-0.0128040209229106,
1.30668034073783));
#23725=CARTESIAN_POINT('Ctrl Pts',(0.195780971015601,-0.000607458635683858,
1.30737518397598));
#23726=CARTESIAN_POINT('Ctrl Pts',(0.195432808277455,0.0116586578840071,
1.30807002721413));
#23727=CARTESIAN_POINT('Ctrl Pts',(0.193949523715838,0.0237643062259244,
1.30876487045228));
#23728=CARTESIAN_POINT('Ctrl Pts',(0.192462820555311,0.0358978550511995,
1.30946131512983));
#23729=CARTESIAN_POINT('Ctrl Pts',(0.189835943577989,0.0478693365599423,
1.31015775980737));
#23730=CARTESIAN_POINT('Ctrl Pts',(0.186134131321106,0.059457927623971,
1.31085420448492));
#23731=CARTESIAN_POINT('Ctrl Pts',(0.18492593609909,0.0632402048930077,
1.31108150967314));
#23732=CARTESIAN_POINT('Ctrl Pts',(0.183603625910985,0.0669818351189525,
1.31130881486136));
#23733=CARTESIAN_POINT('Ctrl Pts',(0.182170570957313,0.0706756186890956,
1.31153612004958));
#23734=CARTESIAN_POINT('Ctrl Pts',(0.177779809879307,0.0819930640451269,
1.31223256422342));
#23735=CARTESIAN_POINT('Ctrl Pts',(0.172314819033327,0.0929398373908723,
1.31292900839726));
#23736=CARTESIAN_POINT('Ctrl Pts',(0.16586044795515,0.103302816051243,1.31362545257109));
#23737=CARTESIAN_POINT('Ctrl Pts',(0.159419623363995,0.113644044806901,
1.31432043504218));
#23738=CARTESIAN_POINT('Ctrl Pts',(0.15199393508303,0.123403135551954,1.31501541751326));
#23739=CARTESIAN_POINT('Ctrl Pts',(0.143714376254833,0.132390853376222,
1.31571039998435));
#23740=CARTESIAN_POINT('Ctrl Pts',(0.13543598405179,0.141377304792712,1.31640528452944));
#23741=CARTESIAN_POINT('Ctrl Pts',(0.126304518651016,0.149591924746643,
1.31710016907453));
#23742=CARTESIAN_POINT('Ctrl Pts',(0.116490691147871,0.156879185604373,
1.31779505361962));
#23743=CARTESIAN_POINT('Ctrl Pts',(0.106677447021047,0.164166013275823,
1.31848989685777));
#23744=CARTESIAN_POINT('Ctrl Pts',(0.0961826403741802,0.170525090662696,
1.31918474009592));
#23745=CARTESIAN_POINT('Ctrl Pts',(0.0852071114949725,0.175843419412508,
1.31987958333407));
#23746=CARTESIAN_POINT('Ctrl Pts',(0.074206286774338,0.181174005576264,
1.32057602801161));
#23747=CARTESIAN_POINT('Ctrl Pts',(0.0627233438518345,0.18545873123927,
1.32127247268916));
#23748=CARTESIAN_POINT('Ctrl Pts',(0.0509791958083,0.188632663117338,1.32196891736671));
#23749=CARTESIAN_POINT('Ctrl Pts',(0.0471461479474023,0.189668569063922,
1.32219622255493));
#23750=CARTESIAN_POINT('Ctrl Pts',(0.0432853701297518,0.190586553608311,
1.32242352774315));
#23751=CARTESIAN_POINT('Ctrl Pts',(0.0394047390535147,0.191385544229768,
1.32265083293137));
#23752=CARTESIAN_POINT('Ctrl Pts',(0.0275148084935359,0.193833584978958,
1.3233472771052));
#23753=CARTESIAN_POINT('Ctrl Pts',(0.0153537894493235,0.19517805046233,
1.32404372127904));
#23754=CARTESIAN_POINT('Ctrl Pts',(0.00314675961872812,0.195374660342384,
1.32474016545288));
#23755=CARTESIAN_POINT('Ctrl Pts',(-0.0090346499974204,0.195570857576007,
1.32543514792396));
#23756=CARTESIAN_POINT('Ctrl Pts',(-0.0212610131337285,0.194623892383761,
1.32613013039504));
#23757=CARTESIAN_POINT('Ctrl Pts',(-0.0333023001143408,0.192541208075296,
1.32682511286613));
#23758=CARTESIAN_POINT('Ctrl Pts',(-0.0453418904262554,0.190458817225934,
1.32751999741122));
#23759=CARTESIAN_POINT('Ctrl Pts',(-0.0571955869326572,0.187241128538841,
1.32821488195631));
#23760=CARTESIAN_POINT('Ctrl Pts',(-0.0686401428152857,0.182947235000415,
1.3289097665014));
#23761=CARTESIAN_POINT('Ctrl Pts',(-0.0800840183840454,0.178653596709581,
1.32960460973955));
#23762=CARTESIAN_POINT('Ctrl Pts',(-0.0911179910588212,0.173284213245967,
1.3302994529777));
#23763=CARTESIAN_POINT('Ctrl Pts',(-0.101538208880341,0.16694655473346,
1.33099429621585));
#23764=CARTESIAN_POINT('Ctrl Pts',(-0.111982442690575,0.160594289507551,
1.33169074089339));
#23765=CARTESIAN_POINT('Ctrl Pts',(-0.121809383652032,0.153269804303219,
1.33238718557094));
#23766=CARTESIAN_POINT('Ctrl Pts',(-0.130844679170331,0.145123498899431,
1.33308363024849));
#23767=CARTESIAN_POINT('Ctrl Pts',(-0.13379361339957,0.14246471272045,1.33331093543671));
#23768=CARTESIAN_POINT('Ctrl Pts',(-0.136658507168464,0.139718682007989,
1.33353824062492));
#23769=CARTESIAN_POINT('Ctrl Pts',(-0.139434188009896,0.136891443173125,
1.33376554581314));
#23770=CARTESIAN_POINT('Ctrl Pts',(-0.148233905898102,0.127928271407112,
1.33448616956101));
#23771=CARTESIAN_POINT('Ctrl Pts',(-0.156202650445079,0.118075218915444,
1.33520679330888));
#23772=CARTESIAN_POINT('Ctrl Pts',(-0.16315981320051,0.107517604867179,
1.33592741705675));
#23773=CARTESIAN_POINT('Ctrl Pts',(-0.169780924334577,0.0974699549297682,
1.33661323253761));
#23774=CARTESIAN_POINT('Ctrl Pts',(-0.175485519694319,0.0867851739644082,
1.33729904801846));
#23775=CARTESIAN_POINT('Ctrl Pts',(-0.180158736660967,0.0756570525775642,
1.33798486349931));
#23776=CARTESIAN_POINT('Ctrl Pts',(-0.184827594402669,0.0645393116170316,
1.33867003924442));
#23777=CARTESIAN_POINT('Ctrl Pts',(-0.188466618912098,0.0529798735468401,
1.33935521498952));
#23778=CARTESIAN_POINT('Ctrl Pts',(-0.191008466011499,0.0411937605947046,
1.34004039073463));
#23779=CARTESIAN_POINT('Ctrl Pts',(-0.193552742713279,0.0293963819893101,
1.34072622139899));
#23780=CARTESIAN_POINT('Ctrl Pts',(-0.194997590648736,0.017372783340044,
1.34141205206336));
#23781=CARTESIAN_POINT('Ctrl Pts',(-0.195326811815141,0.005347577594793,
1.34209788272772));
#23782=CARTESIAN_POINT('Ctrl Pts',(-0.195377238943025,0.00350566507571935,
1.34220293208101));
#23783=CARTESIAN_POINT('Ctrl Pts',(-0.195401591571816,0.00166371687160794,
1.34230798143429));
#23784=CARTESIAN_POINT('Ctrl Pts',(-0.195399919414568,-0.000177462052753457,
1.34241303078758));
#23785=CARTESIAN_POINT('',(-0.195672555088735,8.72824817547956E-5,1.41241303078758));
#23786=CARTESIAN_POINT('Ctrl Pts',(-0.195421369810842,-0.000177481533986374,
1.34241303078758));
#23787=CARTESIAN_POINT('Ctrl Pts',(-0.19555443758116,-0.0145933993525209,
1.34323544009003));
#23788=CARTESIAN_POINT('Ctrl Pts',(-0.187517725154066,-0.0938051227660867,
1.34776275368636));
#23789=CARTESIAN_POINT('Ctrl Pts',(-0.0795606509348802,-0.21682299543957,
1.35599497157673));
#23790=CARTESIAN_POINT('Ctrl Pts',(0.139031233645666,-0.184424576994089,
1.36710968445844));
#23791=CARTESIAN_POINT('Ctrl Pts',(0.23034688085148,0.0168054458595032,
1.37822439734026));
#23792=CARTESIAN_POINT('Ctrl Pts',(0.110791319357882,0.202650911874206,
1.38933911022202));
#23793=CARTESIAN_POINT('Ctrl Pts',(-0.110188230774172,0.202979462821721,
1.4004538231038));
#23794=CARTESIAN_POINT('Ctrl Pts',(-0.193301926424826,0.0746222231139512,
1.40814512995899));
#23795=CARTESIAN_POINT('Ctrl Pts',(-0.195699991939521,0.00500518314638453,
1.41213153252024));
#23796=CARTESIAN_POINT('Ctrl Pts',(-0.195672555088735,8.72824817547956E-5,
1.41241303078758));
#23797=CARTESIAN_POINT('',(-0.195399961286389,0.000123001129209823,1.48241303078758));
#23798=CARTESIAN_POINT('Ctrl Pts',(-0.195672555088735,8.72824817547956E-5,
1.41241303078758));
#23799=CARTESIAN_POINT('Ctrl Pts',(-0.195338885254029,-0.0597211523368212,
1.41583643681417));
#23800=CARTESIAN_POINT('Ctrl Pts',(-0.134045287995802,-0.184847342684257,
1.42296474713469));
#23801=CARTESIAN_POINT('Ctrl Pts',(0.0789155585961739,-0.217058616829523,
1.43379796174912));
#23802=CARTESIAN_POINT('Ctrl Pts',(0.225166835685404,-0.0514004342001738,
1.44491267463091));
#23803=CARTESIAN_POINT('Ctrl Pts',(0.165288979944631,0.161312310867416,
1.45602738751267));
#23804=CARTESIAN_POINT('Ctrl Pts',(-0.0459027848741339,0.226351591267424,
1.46714210039446));
#23805=CARTESIAN_POINT('Ctrl Pts',(-0.17976876762693,0.113847497486333,
1.47593728692968));
#23806=CARTESIAN_POINT('Ctrl Pts',(-0.195300781734273,0.0244906930800311,
1.48102756917097));
#23807=CARTESIAN_POINT('Ctrl Pts',(-0.195160815401549,0.0001243221805799,
1.48241294711835));
#23808=CARTESIAN_POINT('',(-0.195399939368468,-0.00015393115033595,1.55241303078758));
#23809=CARTESIAN_POINT('Ctrl Pts',(-0.195399961286389,0.000123001129209823,
1.48241303078758));
#23810=CARTESIAN_POINT('Ctrl Pts',(-0.195407720443864,-0.0122032196137622,
1.48311299720329));
#23811=CARTESIAN_POINT('Ctrl Pts',(-0.194244791461965,-0.0245341129591015,
1.48381296361899));
#23812=CARTESIAN_POINT('Ctrl Pts',(-0.191934714154944,-0.0366363958688599,
1.4845129300347));
#23813=CARTESIAN_POINT('Ctrl Pts',(-0.189623997762733,-0.0487420268872529,
1.48521309009681));
#23814=CARTESIAN_POINT('Ctrl Pts',(-0.186165702326191,-0.0606180869632981,
1.48591325015893));
#23815=CARTESIAN_POINT('Ctrl Pts',(-0.181634190272556,-0.0720429102968012,
1.48661341022104));
#23816=CARTESIAN_POINT('Ctrl Pts',(-0.177090695339426,-0.0834979448003588,
1.48731542174764));
#23817=CARTESIAN_POINT('Ctrl Pts',(-0.171468700646835,-0.0944985906177856,
1.48801743327425));
#23818=CARTESIAN_POINT('Ctrl Pts',(-0.164889693248902,-0.1048453578385,
1.48871944480085));
#23819=CARTESIAN_POINT('Ctrl Pts',(-0.162852666832545,-0.108048977606294,
1.48893680525324));
#23820=CARTESIAN_POINT('Ctrl Pts',(-0.160724203558817,-0.111190127957947,
1.48915416570562));
#23821=CARTESIAN_POINT('Ctrl Pts',(-0.158508702339993,-0.11426351684808,
1.48937152615801));
#23822=CARTESIAN_POINT('Ctrl Pts',(-0.151410019488453,-0.124110955804618,
1.49006797033184));
#23823=CARTESIAN_POINT('Ctrl Pts',(-0.143365032956223,-0.133329207446043,
1.49076441450568));
#23824=CARTESIAN_POINT('Ctrl Pts',(-0.134509516318977,-0.141733376519558,
1.49146085867951));
#23825=CARTESIAN_POINT('Ctrl Pts',(-0.125672585712767,-0.150119906854011,
1.49215584115059));
#23826=CARTESIAN_POINT('Ctrl Pts',(-0.116029078960968,-0.157695095045935,
1.49285082362167));
#23827=CARTESIAN_POINT('Ctrl Pts',(-0.105753412717894,-0.164308781562395,
1.49354580609275));
#23828=CARTESIAN_POINT('Ctrl Pts',(-0.0954791943600241,-0.170921536182214,
1.49424069063784));
#23829=CARTESIAN_POINT('Ctrl Pts',(-0.0845737036217037,-0.17657254610153,
1.49493557518293));
#23830=CARTESIAN_POINT('Ctrl Pts',(-0.0732413093382392,-0.181154272945521,
1.49563045972802));
#23831=CARTESIAN_POINT('Ctrl Pts',(-0.061909588701269,-0.185735727431866,
1.49632530296616));
#23832=CARTESIAN_POINT('Ctrl Pts',(-0.0501518368335319,-0.189247721563803,
1.49702014620431));
#23833=CARTESIAN_POINT('Ctrl Pts',(-0.0381908737766618,-0.191631461822361,
1.49771498944245));
#23834=CARTESIAN_POINT('Ctrl Pts',(-0.0262023436997301,-0.194020696004378,
1.49841143412));
#23835=CARTESIAN_POINT('Ctrl Pts',(-0.014010538428915,-0.195276377654251,
1.49910787879754));
#23836=CARTESIAN_POINT('Ctrl Pts',(-0.0018456030229129,-0.195391283709079,
1.49980432347509));
#23837=CARTESIAN_POINT('Ctrl Pts',(0.00212478116040987,-0.19542878667703,
1.50003162866332));
#23838=CARTESIAN_POINT('Ctrl Pts',(0.00609231336375039,-0.195345185252779,
1.50025893385155));
#23839=CARTESIAN_POINT('Ctrl Pts',(0.0100491005886018,-0.195141424555014,
1.50048623903978));
#23840=CARTESIAN_POINT('Ctrl Pts',(0.0221723672473985,-0.194517118739913,
1.50118268321362));
#23841=CARTESIAN_POINT('Ctrl Pts',(0.0342801464245863,-0.192756535022393,
1.50187912738746));
#23842=CARTESIAN_POINT('Ctrl Pts',(0.0461434623222685,-0.189873486524352,
1.50257557156129));
#23843=CARTESIAN_POINT('Ctrl Pts',(0.0579818793951278,-0.186996488992173,
1.50327055403238));
#23844=CARTESIAN_POINT('Ctrl Pts',(0.0695759915653924,-0.183001834864492,
1.50396553650346));
#23845=CARTESIAN_POINT('Ctrl Pts',(0.080705052869171,-0.177954641528071,
1.50466051897455));
#23846=CARTESIAN_POINT('Ctrl Pts',(0.0918325460407418,-0.172908159362719,
1.50535540351964));
#23847=CARTESIAN_POINT('Ctrl Pts',(0.102494303098156,-0.166809751553959,
1.50605028806473));
#23848=CARTESIAN_POINT('Ctrl Pts',(0.112489146120411,-0.159772813723426,
1.50674517260982));
#23849=CARTESIAN_POINT('Ctrl Pts',(0.122483395006,-0.152736294198892,1.50744001584797));
#23850=CARTESIAN_POINT('Ctrl Pts',(0.131810107872335,-0.144761881438288,
1.50813485908612));
#23851=CARTESIAN_POINT('Ctrl Pts',(0.14029905666712,-0.136004906890584,
1.50882970232427));
#23852=CARTESIAN_POINT('Ctrl Pts',(0.148807570359864,-0.12722774971278,
1.50952614700182));
#23853=CARTESIAN_POINT('Ctrl Pts',(0.156473902749328,-0.117665103642622,
1.51022259167937));
#23854=CARTESIAN_POINT('Ctrl Pts',(0.163167183175346,-0.107506419969335,
1.51091903635692));
#23855=CARTESIAN_POINT('Ctrl Pts',(0.165351731950102,-0.104190835000663,
1.51114634154513));
#23856=CARTESIAN_POINT('Ctrl Pts',(0.167432982102897,-0.100811974426125,
1.51137364673335));
#23857=CARTESIAN_POINT('Ctrl Pts',(0.169407447550582,-0.0973769824670943,
1.51160095192157));
#23858=CARTESIAN_POINT('Ctrl Pts',(0.175457045310609,-0.0868524530632367,
1.5122973960954));
#23859=CARTESIAN_POINT('Ctrl Pts',(0.18054354245229,-0.0757247615480432,
1.51299384026924));
#23860=CARTESIAN_POINT('Ctrl Pts',(0.184554377005386,-0.0641937841862738,
1.51369028444307));
#23861=CARTESIAN_POINT('Ctrl Pts',(0.188556793585986,-0.0526870081344792,
1.51438526691415));
#23862=CARTESIAN_POINT('Ctrl Pts',(0.191487673305,-0.0407794205245224,1.51508024938524));
#23863=CARTESIAN_POINT('Ctrl Pts',(0.193282022931698,-0.0286918039068726,
1.51577523185632));
#23864=CARTESIAN_POINT('Ctrl Pts',(0.195076119726881,-0.0166058904859631,
1.51647011640141));
#23865=CARTESIAN_POINT('Ctrl Pts',(0.195733830355679,-0.00434085652426346,
1.5171650009465));
#23866=CARTESIAN_POINT('Ctrl Pts',(0.195241336275968,0.00787277645905997,
1.51785988549159));
#23867=CARTESIAN_POINT('Ctrl Pts',(0.194748871472234,0.0200856834112485,
1.51855472872974));
#23868=CARTESIAN_POINT('Ctrl Pts',(0.193106399701943,0.0322463214804775,
1.51924957196789));
#23869=CARTESIAN_POINT('Ctrl Pts',(0.190352120288359,0.0441274325304136,
1.51994441520604));
#23870=CARTESIAN_POINT('Ctrl Pts',(0.187591492951492,0.0560359265615691,
1.52064085988358));
#23871=CARTESIAN_POINT('Ctrl Pts',(0.183714203260911,0.0676627695046786,
1.52133730456113));
#23872=CARTESIAN_POINT('Ctrl Pts',(0.178808460589818,0.0787952690299328,
1.52203374923868));
#23873=CARTESIAN_POINT('Ctrl Pts',(0.177207327295025,0.0824286874212366,
1.5222610544269));
#23874=CARTESIAN_POINT('Ctrl Pts',(0.175497013530002,0.0860096269356705,
1.52248835961512));
#23875=CARTESIAN_POINT('Ctrl Pts',(0.173681631464147,0.0895312844314901,
1.52271566480333));
#23876=CARTESIAN_POINT('Ctrl Pts',(0.168119451942595,0.10032134982521,1.52341210897717));
#23877=CARTESIAN_POINT('Ctrl Pts',(0.161528229781885,0.110629296374245,
1.524108553151));
#23878=CARTESIAN_POINT('Ctrl Pts',(0.154014861771623,0.120252161533454,
1.52480499732484));
#23879=CARTESIAN_POINT('Ctrl Pts',(0.146517262879838,0.129854830144247,
1.52549997979592));
#23880=CARTESIAN_POINT('Ctrl Pts',(0.138101834316003,0.138774542062417,
1.52619496226701));
#23881=CARTESIAN_POINT('Ctrl Pts',(0.128918833679812,0.146836965109733,
1.52688994473809));
#23882=CARTESIAN_POINT('Ctrl Pts',(0.119737126967578,0.154898252127254,
1.52758482928318));
#23883=CARTESIAN_POINT('Ctrl Pts',(0.109788689525428,0.162101878562092,
1.52827971382827));
#23884=CARTESIAN_POINT('Ctrl Pts',(0.0992597123839005,0.168311228079012,
1.52897459837336));
#23885=CARTESIAN_POINT('Ctrl Pts',(0.0887313611302768,0.174520208485363,
1.52966944161151));
#23886=CARTESIAN_POINT('Ctrl Pts',(0.0776233066222674,0.179734607474173,
1.53036428484966));
#23887=CARTESIAN_POINT('Ctrl Pts',(0.0661472059622404,0.183863283837173,
1.53105912808781));
#23888=CARTESIAN_POINT('Ctrl Pts',(0.0546446557683793,0.188001475763725,
1.53175557276536));
#23889=CARTESIAN_POINT('Ctrl Pts',(0.042773211481347,0.191048714301895,
1.53245201744291));
#23890=CARTESIAN_POINT('Ctrl Pts',(0.0307594111770352,0.192963775419228,
1.53314846212046));
#23891=CARTESIAN_POINT('Ctrl Pts',(0.0268383543760548,0.193588811896296,
1.53337576730868));
#23892=CARTESIAN_POINT('Ctrl Pts',(0.022902184592286,0.19409365683727,1.5336030724969));
#23893=CARTESIAN_POINT('Ctrl Pts',(0.018958847759401,0.19447807612077,1.53383037768512));
#23894=CARTESIAN_POINT('Ctrl Pts',(0.00687679198126068,0.195655904802991,
1.53452682185895));
#23895=CARTESIAN_POINT('Ctrl Pts',(-0.00535821067313899,0.195707689708688,
1.53522326603279));
#23896=CARTESIAN_POINT('Ctrl Pts',(-0.0175176633930722,0.194613184212291,
1.53591971020662));
#23897=CARTESIAN_POINT('Ctrl Pts',(-0.0296515957537918,0.193520975873016,
1.53661469267771));
#23898=CARTESIAN_POINT('Ctrl Pts',(-0.0417094227996702,0.191287255758967,
1.53730967514879));
#23899=CARTESIAN_POINT('Ctrl Pts',(-0.0534631895223959,0.187943734575251,
1.53800465761987));
#23900=CARTESIAN_POINT('Ctrl Pts',(-0.0652153000892538,0.184600684507931,
1.53869954216496));
#23901=CARTESIAN_POINT('Ctrl Pts',(-0.0766625817815175,0.180148338698035,
1.53939442671005));
#23902=CARTESIAN_POINT('Ctrl Pts',(-0.087589282701494,0.174669051511244,
1.54008931125514));
#23903=CARTESIAN_POINT('Ctrl Pts',(-0.0985153340911449,0.169190090036964,
1.54078415449329));
#23904=CARTESIAN_POINT('Ctrl Pts',(-0.108920095284611,0.162684724845514,
1.54147899773144));
#23905=CARTESIAN_POINT('Ctrl Pts',(-0.118612213038698,0.15528136693777,
1.54217384096959));
#23906=CARTESIAN_POINT('Ctrl Pts',(-0.128326668693444,0.147860946146797,
1.54287028564714));
#23907=CARTESIAN_POINT('Ctrl Pts',(-0.137324545832395,0.139538983688291,
1.54356673032468));
#23908=CARTESIAN_POINT('Ctrl Pts',(-0.145448362112576,0.130483462395696,
1.54426317500223));
#23909=CARTESIAN_POINT('Ctrl Pts',(-0.148099808305136,0.127527926890607,
1.54449048019045));
#23910=CARTESIAN_POINT('Ctrl Pts',(-0.150658464802673,0.124494516613643,
1.54471778537867));
#23911=CARTESIAN_POINT('Ctrl Pts',(-0.153119826017623,0.121389780790364,
1.54494509056688));
#23912=CARTESIAN_POINT('Ctrl Pts',(-0.160650574807049,0.111890571409546,
1.54564055056707));
#23913=CARTESIAN_POINT('Ctrl Pts',(-0.167321842354435,0.101652732245817,
1.54633601056725));
#23914=CARTESIAN_POINT('Ctrl Pts',(-0.172992199724487,0.0908562536894579,
1.54703147056743));
#23915=CARTESIAN_POINT('Ctrl Pts',(-0.178650312965688,0.0800830882095001,
1.54772542884536));
#23916=CARTESIAN_POINT('Ctrl Pts',(-0.183311330666581,0.068754408789931,
1.54841938712329));
#23917=CARTESIAN_POINT('Ctrl Pts',(-0.186877610749096,0.0570781797249134,
1.54911334540122));
#23918=CARTESIAN_POINT('Ctrl Pts',(-0.190442306291453,0.0454071385457058,
1.54980699534533));
#23919=CARTESIAN_POINT('Ctrl Pts',(-0.19291293103831,0.0333896787299648,
1.55050064528944));
#23920=CARTESIAN_POINT('Ctrl Pts',(-0.194240964325203,0.0212510653383588,
1.55119429523355));
#23921=CARTESIAN_POINT('Ctrl Pts',(-0.195018744432406,0.0141419272480706,
1.55160054041823));
#23922=CARTESIAN_POINT('Ctrl Pts',(-0.195405568361647,0.00699150317808594,
1.5520067856029));
#23923=CARTESIAN_POINT('Ctrl Pts',(-0.195399939368468,-0.00015393115033595,
1.55241303078758));
#23924=CARTESIAN_POINT('',(-0.195712283470102,-3.61459064724743E-5,1.62241303078758));
#23925=CARTESIAN_POINT('Ctrl Pts',(-0.195226198903123,-0.000155160406305955,
1.55241310852604));
#23926=CARTESIAN_POINT('Ctrl Pts',(-0.195383351547435,-0.0215168196864403,
1.55362867350025));
#23927=CARTESIAN_POINT('Ctrl Pts',(-0.182302395685712,-0.107798996787892,
1.55854914276838));
#23928=CARTESIAN_POINT('Ctrl Pts',(-0.0562017238658613,-0.224016684117646,
1.56717451633045));
#23929=CARTESIAN_POINT('Ctrl Pts',(0.157742334325191,-0.168699331623246,
1.57828922921221));
#23930=CARTESIAN_POINT('Ctrl Pts',(0.227281065301869,0.0410539387122334,
1.589403942094));
#23931=CARTESIAN_POINT('Ctrl Pts',(0.0887551905086346,0.21322435293907,
1.60051865497576));
#23932=CARTESIAN_POINT('Ctrl Pts',(-0.128813312714937,0.190429758735974,
1.6115216845403));
#23933=CARTESIAN_POINT('Ctrl Pts',(-0.195552549538933,0.0627050974813158,
1.6188198098109));
#23934=CARTESIAN_POINT('Ctrl Pts',(-0.195712283470102,-3.61459064724743E-5,
1.62241303078758));
#23935=CARTESIAN_POINT('',(-0.195399920371161,0.000176405623024491,1.69241303078758));
#23936=CARTESIAN_POINT('Ctrl Pts',(-0.195712283470102,-3.61459064724743E-5,
1.62241303078758));
#23937=CARTESIAN_POINT('Ctrl Pts',(-0.195717248267821,-0.00198624867923799,
1.62252471410483));
#23938=CARTESIAN_POINT('Ctrl Pts',(-0.195690623309908,-0.0039362125300576,
1.62263639742207));
#23939=CARTESIAN_POINT('Ctrl Pts',(-0.193686975727267,-0.0705400096200497,
1.62645298503325));
#23940=CARTESIAN_POINT('Ctrl Pts',(-0.119351590043147,-0.197730388364331,
1.63386279362109));
#23941=CARTESIAN_POINT('Ctrl Pts',(0.101411982740744,-0.207503538006193,
1.64497750650288));
#23942=CARTESIAN_POINT('Ctrl Pts',(0.229337886969936,-0.0273174326888311,
1.65609221938464));
#23943=CARTESIAN_POINT('Ctrl Pts',(0.14731626663462,0.177876434957931,1.66720693226643));
#23944=CARTESIAN_POINT('Ctrl Pts',(-0.069566130158676,0.220233199275866,
1.67832164514821));
#23945=CARTESIAN_POINT('Ctrl Pts',(-0.185374172661697,0.0998458182017167,
1.686723666339));
#23946=CARTESIAN_POINT('Ctrl Pts',(-0.195485375409074,0.0175896061910127,
1.69142078323589));
#23947=CARTESIAN_POINT('Ctrl Pts',(-0.195332205722473,0.000176957812133139,
1.69241299583884));
#23948=CARTESIAN_POINT('',(-0.195379429215978,-6.88592766845772E-5,1.76241303461069));
#23949=CARTESIAN_POINT('Ctrl Pts',(-0.195399920371161,0.000176405623024491,
1.69241303078758));
#23950=CARTESIAN_POINT('Ctrl Pts',(-0.195410833012155,-0.0119112429713591,
1.69310157998606));
#23951=CARTESIAN_POINT('Ctrl Pts',(-0.194295777173492,-0.0240245763136542,
1.69379012918454));
#23952=CARTESIAN_POINT('Ctrl Pts',(-0.192066928524843,-0.0359368191000951,
1.69447867838301));
#23953=CARTESIAN_POINT('Ctrl Pts',(-0.189839819899382,-0.0478397622067734,
1.69516669004317));
#23954=CARTESIAN_POINT('Ctrl Pts',(-0.186500797960111,-0.0595410443737312,
1.69585470170332));
#23955=CARTESIAN_POINT('Ctrl Pts',(-0.182113456174281,-0.0708226593701344,
1.69654271336347));
#23956=CARTESIAN_POINT('Ctrl Pts',(-0.177715401429773,-0.0821318216790538,
1.69723240500226));
#23957=CARTESIAN_POINT('Ctrl Pts',(-0.17226425745159,-0.0930184370182762,
1.69792209664105));
#23958=CARTESIAN_POINT('Ctrl Pts',(-0.165872091364467,-0.103284119332925,
1.69861178827985));
#23959=CARTESIAN_POINT('Ctrl Pts',(-0.159880903430725,-0.112905839290898,
1.69925821582381));
#23960=CARTESIAN_POINT('Ctrl Pts',(-0.153063879326051,-0.121981825796497,
1.69990464336778));
#23961=CARTESIAN_POINT('Ctrl Pts',(-0.14554597808314,-0.130374569083936,
1.70055107091175));
#23962=CARTESIAN_POINT('Ctrl Pts',(-0.137446387388151,-0.139416691777484,
1.70124751508559));
#23963=CARTESIAN_POINT('Ctrl Pts',(-0.128472283185883,-0.147733146875496,
1.70194395925943));
#23964=CARTESIAN_POINT('Ctrl Pts',(-0.118778218134343,-0.155154422743377,
1.70264040343326));
#23965=CARTESIAN_POINT('Ctrl Pts',(-0.109104499066135,-0.162560122776527,
1.70333538590435));
#23966=CARTESIAN_POINT('Ctrl Pts',(-0.0987144613648414,-0.169073786506153,
1.70403036837544));
#23967=CARTESIAN_POINT('Ctrl Pts',(-0.0877974135801952,-0.174564527234568,
1.70472535084652));
#23968=CARTESIAN_POINT('Ctrl Pts',(-0.0768819040541493,-0.180054494294193,
1.70542023539162));
#23969=CARTESIAN_POINT('Ctrl Pts',(-0.0654402922705117,-0.184521390436504,
1.70611511993671));
#23970=CARTESIAN_POINT('Ctrl Pts',(-0.0536871671213206,-0.187879876747052,
1.7068100044818));
#23971=CARTESIAN_POINT('Ctrl Pts',(-0.0419347406286866,-0.191238163414658,
1.70750484771995));
#23972=CARTESIAN_POINT('Ctrl Pts',(-0.0298716869347652,-0.193487956148545,
1.7081996909581));
#23973=CARTESIAN_POINT('Ctrl Pts',(-0.017725791559956,-0.194594337825058,
1.70889453419625));
#23974=CARTESIAN_POINT('Ctrl Pts',(-0.00555190294247328,-0.195703269433858,
1.7095909788738));
#23975=CARTESIAN_POINT('Ctrl Pts',(0.00670433105061121,-0.19566351423298,
1.71028742355135));
#23976=CARTESIAN_POINT('Ctrl Pts',(0.0188132907613911,-0.194492210874182,
1.7109838682289));
#23977=CARTESIAN_POINT('Ctrl Pts',(0.0227654056311449,-0.194109921599805,
1.71121117341711));
#23978=CARTESIAN_POINT('Ctrl Pts',(0.0267018864214747,-0.193607507460575,
1.71143847860533));
#23979=CARTESIAN_POINT('Ctrl Pts',(0.0306149842097358,-0.192986742399155,
1.71166578379354));
#23980=CARTESIAN_POINT('Ctrl Pts',(0.0426043900729254,-0.191084769928805,
1.71236222796737));
#23981=CARTESIAN_POINT('Ctrl Pts',(0.0544583156073996,-0.188054518940477,
1.7130586721412));
#23982=CARTESIAN_POINT('Ctrl Pts',(0.0659505269305032,-0.183933922911433,
1.71375511631504));
#23983=CARTESIAN_POINT('Ctrl Pts',(0.0774186183061158,-0.17982197522317,
1.71445009878612));
#23984=CARTESIAN_POINT('Ctrl Pts',(0.0885256610797746,-0.174624447018356,
1.7151450812572));
#23985=CARTESIAN_POINT('Ctrl Pts',(0.0990590268509342,-0.168429419043544,
1.71584006372829));
#23986=CARTESIAN_POINT('Ctrl Pts',(0.109590908425927,-0.162235263974599,
1.71653494827337));
#23987=CARTESIAN_POINT('Ctrl Pts',(0.119548496428216,-0.155044291680869,
1.71722983281846));
#23988=CARTESIAN_POINT('Ctrl Pts',(0.12874372287406,-0.146990522893577,
1.71792471736355));
#23989=CARTESIAN_POINT('Ctrl Pts',(0.137938402715909,-0.138937232857105,
1.7186195606017));
#23990=CARTESIAN_POINT('Ctrl Pts',(0.146370169794315,-0.130021845277062,
1.71931440383985));
#23991=CARTESIAN_POINT('Ctrl Pts',(0.153886164381613,-0.120416811168189,
1.720009247078));
#23992=CARTESIAN_POINT('Ctrl Pts',(0.161419481451435,-0.110789639864622,
1.72070569175554));
#23993=CARTESIAN_POINT('Ctrl Pts',(0.168032324202524,-0.100470378121775,
1.72140213643309));
#23994=CARTESIAN_POINT('Ctrl Pts',(0.173614575630121,-0.0896612465269868,
1.72209858111064));
#23995=CARTESIAN_POINT('Ctrl Pts',(0.175436507439444,-0.0861333687631246,
1.72232588629886));
#23996=CARTESIAN_POINT('Ctrl Pts',(0.177149032218288,-0.0825534861025725,
1.72255319148708));
#23997=CARTESIAN_POINT('Ctrl Pts',(0.178749438391155,-0.0789290711642203,
1.7227804966753));
#23998=CARTESIAN_POINT('Ctrl Pts',(0.183652949672968,-0.0678241655212152,
1.72347694084914));
#23999=CARTESIAN_POINT('Ctrl Pts',(0.187535012349117,-0.0562212537742335,
1.72417338502297));
#24000=CARTESIAN_POINT('Ctrl Pts',(0.190304817273997,-0.0443309882848414,
1.72486982919681));
#24001=CARTESIAN_POINT('Ctrl Pts',(0.193068808909556,-0.0324656781822966,
1.72556481166789));
#24002=CARTESIAN_POINT('Ctrl Pts',(0.194724906896276,-0.0203150387721786,
1.72625979413898));
#24003=CARTESIAN_POINT('Ctrl Pts',(0.19523181379665,-0.00810548466595916,
1.72695477661007));
#24004=CARTESIAN_POINT('Ctrl Pts',(0.19573864927168,0.00410234906200601,
1.72764966115516));
#24005=CARTESIAN_POINT('Ctrl Pts',(0.195096532785329,0.0163682093160225,
1.72834454570025));
#24006=CARTESIAN_POINT('Ctrl Pts',(0.193316084225746,0.0284614050887209,
1.72903943024534));
#24007=CARTESIAN_POINT('Ctrl Pts',(0.19153574150372,0.0405538819896001,
1.72973427348349));
#24008=CARTESIAN_POINT('Ctrl Pts',(0.188617355061553,0.0524728522614664,
1.73042911672164));
#24009=CARTESIAN_POINT('Ctrl Pts',(0.184622926505938,0.0639963671498853,
1.73112395995979));
#24010=CARTESIAN_POINT('Ctrl Pts',(0.180619291794299,0.0755464408500449,
1.73182040463734));
#24011=CARTESIAN_POINT('Ctrl Pts',(0.175535011910544,0.0866984339558695,
1.73251684931489));
#24012=CARTESIAN_POINT('Ctrl Pts',(0.169480279189942,0.0972501669186187,
1.73321329399243));
#24013=CARTESIAN_POINT('Ctrl Pts',(0.167504139225009,0.100694035074194,
1.73344059918065));
#24014=CARTESIAN_POINT('Ctrl Pts',(0.165424976018988,0.104074180240251,
1.73366790436887));
#24015=CARTESIAN_POINT('Ctrl Pts',(0.163247597657166,0.107384271935717,
1.73389520955709));
#24016=CARTESIAN_POINT('Ctrl Pts',(0.156576291620506,0.117526117329728,
1.73459165373093));
#24017=CARTESIAN_POINT('Ctrl Pts',(0.148932654521822,0.127079796387206,
1.73528809790476));
#24018=CARTESIAN_POINT('Ctrl Pts',(0.140444433246649,0.135854779709907,
1.7359845420786));
#24019=CARTESIAN_POINT('Ctrl Pts',(0.131974027119994,0.144611346025552,
1.73667952454968));
#24020=CARTESIAN_POINT('Ctrl Pts',(0.122663104291756,0.152591785531161,
1.73737450702076));
#24021=CARTESIAN_POINT('Ctrl Pts',(0.112679504054717,0.159638621160367,
1.73806948949185));
#24022=CARTESIAN_POINT('Ctrl Pts',(0.102697310549535,0.166684463860375,
1.73876437403694));
#24023=CARTESIAN_POINT('Ctrl Pts',(0.0920433155485732,0.172796421964969,
1.73945925858203));
#24024=CARTESIAN_POINT('Ctrl Pts',(0.0809171048280429,0.177858320430188,
1.74015414312712));
#24025=CARTESIAN_POINT('Ctrl Pts',(0.0697915554975698,0.182919917994283,
1.74084898636527));
#24026=CARTESIAN_POINT('Ctrl Pts',(0.0581946543876748,0.186931241518287,
1.74154382960342));
#24027=CARTESIAN_POINT('Ctrl Pts',(0.0463465050264075,0.189824027646231,
1.74223867284156));
#24028=CARTESIAN_POINT('Ctrl Pts',(0.0344710486523428,0.192723480920699,
1.74293511751911));
#24029=CARTESIAN_POINT('Ctrl Pts',(0.0223440536103823,0.194499105717973,
1.74363156219666));
#24030=CARTESIAN_POINT('Ctrl Pts',(0.0101951459275736,0.195133848933278,
1.74432800687421));
#24031=CARTESIAN_POINT('Ctrl Pts',(0.00622999286299049,0.19534101603596,
1.74455531206242));
#24032=CARTESIAN_POINT('Ctrl Pts',(0.00226251304281278,0.195427067517,1.74478261725064));
#24033=CARTESIAN_POINT('Ctrl Pts',(-0.00169936735183612,0.195392610276345,
1.74500992243886));
#24034=CARTESIAN_POINT('Ctrl Pts',(-0.0138382390595514,0.195287036159498,
1.7457063666127));
#24035=CARTESIAN_POINT('Ctrl Pts',(-0.0260102031537887,0.194045560538314,
1.74640281078653));
#24036=CARTESIAN_POINT('Ctrl Pts',(-0.0379859026910966,0.191672197245043,
1.74709925496037));
#24037=CARTESIAN_POINT('Ctrl Pts',(-0.0499364675318776,0.18930381518614,
1.74779423743145));
#24038=CARTESIAN_POINT('Ctrl Pts',(-0.0616907205410164,0.185808356015568,
1.74848921990253));
#24039=CARTESIAN_POINT('Ctrl Pts',(-0.0730253342901441,0.181241442699546,
1.74918420237362));
#24040=CARTESIAN_POINT('Ctrl Pts',(-0.0843583509438475,0.176675172881089,
1.7498790869187));
#24041=CARTESIAN_POINT('Ctrl Pts',(-0.0952710174916307,0.17103803263362,
1.75057397146379));
#24042=CARTESIAN_POINT('Ctrl Pts',(-0.105557493203762,0.16443471539957,
1.75126885600888));
#24043=CARTESIAN_POINT('Ctrl Pts',(-0.115843357443317,0.157831790695238,
1.75196369924703));
#24044=CARTESIAN_POINT('Ctrl Pts',(-0.125502382214613,0.150263298623869,
1.75265854248518));
#24045=CARTESIAN_POINT('Ctrl Pts',(-0.134357855992658,0.141877152963598,
1.75335338572333));
#24046=CARTESIAN_POINT('Ctrl Pts',(-0.143233739416826,0.133471679340809,
1.75404983040087));
#24047=CARTESIAN_POINT('Ctrl Pts',(-0.151301783760117,0.12424543890156,
1.75474627507842));
#24048=CARTESIAN_POINT('Ctrl Pts',(-0.158423140606298,0.114382116261403,
1.75544271975596));
#24049=CARTESIAN_POINT('Ctrl Pts',(-0.160747404701511,0.111162931046114,
1.75567002494419));
#24050=CARTESIAN_POINT('Ctrl Pts',(-0.162971169036832,0.107876112955241,
1.75589733013241));
#24051=CARTESIAN_POINT('Ctrl Pts',(-0.165090645363197,0.104528650682782,
1.75612463532063));
#24052=CARTESIAN_POINT('Ctrl Pts',(-0.171745889793215,0.0940174789530729,
1.75683838313136));
#24053=CARTESIAN_POINT('Ctrl Pts',(-0.177414693780258,0.0828351242330211,
1.75755213094209));
#24054=CARTESIAN_POINT('Ctrl Pts',(-0.181971776211685,0.0711859021321252,
1.75826587875282));
#24055=CARTESIAN_POINT('Ctrl Pts',(-0.186516759932967,0.0595676078372813,
1.75897773161695));
#24056=CARTESIAN_POINT('Ctrl Pts',(-0.189955514046892,0.0474856300317684,
1.75968958448107));
#24057=CARTESIAN_POINT('Ctrl Pts',(-0.192209326398065,0.035167241086016,
1.7604014373452));
#24058=CARTESIAN_POINT('Ctrl Pts',(-0.194332309191495,0.0235639113939933,
1.76107196849266));
#24059=CARTESIAN_POINT('Ctrl Pts',(-0.1954041497732,0.0117515712181993,
1.76174249964012));
#24060=CARTESIAN_POINT('Ctrl Pts',(-0.195399987888093,-6.87992227970692E-5,
1.76241303078758));
#24061=CARTESIAN_POINT('',(-0.195583821122648,-0.000140590296505579,1.83241303078758));
#24062=CARTESIAN_POINT('Ctrl Pts',(-0.195102051502741,-6.96695240533898E-5,
1.76241308619214));
#24063=CARTESIAN_POINT('Ctrl Pts',(-0.195191304682355,-0.0283861708385786,
1.76402184019557));
#24064=CARTESIAN_POINT('Ctrl Pts',(-0.17616558588852,-0.121800052143105,
1.76933549849292));
#24065=CARTESIAN_POINT('Ctrl Pts',(-0.0322133827789196,-0.228701566453772,
1.77835406108418));
#24066=CARTESIAN_POINT('Ctrl Pts',(0.174686847974585,-0.151084789682017,
1.78946877396597));
#24067=CARTESIAN_POINT('Ctrl Pts',(0.221669884971711,0.0648426605340514,
1.80058348684773));
#24068=CARTESIAN_POINT('Ctrl Pts',(0.0657250750476474,0.221409853074599,
1.81169819972952));
#24069=CARTESIAN_POINT('Ctrl Pts',(-0.14057127916716,0.177382277682992,
1.82230804770946));
#24070=CARTESIAN_POINT('Ctrl Pts',(-0.195129223210545,0.0558321996894708,
1.82921299139548));
#24071=CARTESIAN_POINT('Ctrl Pts',(-0.195583821122648,-0.000140590296505579,
1.83241303078758));
#24072=CARTESIAN_POINT('',(-0.19539993725538,0.000156590528830125,1.90241303078758));
#24073=CARTESIAN_POINT('Ctrl Pts',(-0.195583821122648,-0.000140590296505579,
1.83241303078758));
#24074=CARTESIAN_POINT('Ctrl Pts',(-0.195655542280467,-0.0089713244403536,
1.83291789568941));
#24075=CARTESIAN_POINT('Ctrl Pts',(-0.191100149777636,-0.0825311564103834,
1.83712766488517));
#24076=CARTESIAN_POINT('Ctrl Pts',(-0.0977875181872751,-0.209236014622781,
1.84504233837484));
#24077=CARTESIAN_POINT('Ctrl Pts',(0.122772674400008,-0.195624586770786,
1.85615705125663));
#24078=CARTESIAN_POINT('Ctrl Pts',(0.23094053872867,-0.00292849794470196,
1.86727176413839));
#24079=CARTESIAN_POINT('Ctrl Pts',(0.127693729850807,0.19244848631601,1.87838647702018));
#24080=CARTESIAN_POINT('Ctrl Pts',(-0.0924503908440486,0.211648372923799,
1.88950118990194));
#24081=CARTESIAN_POINT('Ctrl Pts',(-0.190094138242322,0.0858713855005268,
1.89751004115775));
#24082=CARTESIAN_POINT('Ctrl Pts',(-0.195629876801359,0.0106410776720159,
1.90181398811963));
#24083=CARTESIAN_POINT('Ctrl Pts',(-0.195538264906755,0.000156701382499669,
1.90241303078758));
#24084=CARTESIAN_POINT('',(-0.195372356109538,4.29160852750294E-5,1.9724130286148));
#24085=CARTESIAN_POINT('Ctrl Pts',(-0.19539993725538,0.000156590528830125,
1.90241303078758));
#24086=CARTESIAN_POINT('Ctrl Pts',(-0.195409542393633,-0.0118290859102397,
1.90309834283115));
#24087=CARTESIAN_POINT('Ctrl Pts',(-0.194312055128761,-0.0238549391754707,
1.90378365487473));
#24088=CARTESIAN_POINT('Ctrl Pts',(-0.19211167027849,-0.0356968646075353,
1.90446896691831));
#24089=CARTESIAN_POINT('Ctrl Pts',(-0.189912810686787,-0.0475305814763519,
1.90515380391859));
#24090=CARTESIAN_POINT('Ctrl Pts',(-0.186612662947961,-0.0591797252615298,
1.90583864091887));
#24091=CARTESIAN_POINT('Ctrl Pts',(-0.18226715366032,-0.0704261648577097,
1.90652347791916));
#24092=CARTESIAN_POINT('Ctrl Pts',(-0.177923622048415,-0.0816674861100453,
1.90720800324469));
#24093=CARTESIAN_POINT('Ctrl Pts',(-0.172536007022654,-0.0925056261125338,
1.90789252857022));
#24094=CARTESIAN_POINT('Ctrl Pts',(-0.166208799716543,-0.10274139816445,
1.90857705389576));
#24095=CARTESIAN_POINT('Ctrl Pts',(-0.159867367576225,-0.113000182289999,
1.90926311817186));
#24096=CARTESIAN_POINT('Ctrl Pts',(-0.152582645835605,-0.122653150995453,
1.90994918244796));
#24097=CARTESIAN_POINT('Ctrl Pts',(-0.144502250188905,-0.131530451570513,
1.91063524672406));
#24098=CARTESIAN_POINT('Ctrl Pts',(-0.140201868657935,-0.13625494540807,
1.91100036970454));
#24099=CARTESIAN_POINT('Ctrl Pts',(-0.135676795206366,-0.1407603317352,
1.91136549268502));
#24100=CARTESIAN_POINT('Ctrl Pts',(-0.130953256157671,-0.145025531206417,
1.91173061566551));
#24101=CARTESIAN_POINT('Ctrl Pts',(-0.121943466508167,-0.153161073149159,
1.91242705983934));
#24102=CARTESIAN_POINT('Ctrl Pts',(-0.112140747371382,-0.160482594108263,
1.91312350401317));
#24103=CARTESIAN_POINT('Ctrl Pts',(-0.101716699622421,-0.166837864461046,
1.91381994818701));
#24104=CARTESIAN_POINT('Ctrl Pts',(-0.0913145299504756,-0.173179796320223,
1.91451493065809));
#24105=CARTESIAN_POINT('Ctrl Pts',(-0.0802943213494162,-0.178558987802671,
1.91520991312917));
#24106=CARTESIAN_POINT('Ctrl Pts',(-0.0688581541611845,-0.18286529087149,
1.91590489560026));
#24107=CARTESIAN_POINT('Ctrl Pts',(-0.0574235983776863,-0.187170987163839,
1.91659978014534));
#24108=CARTESIAN_POINT('Ctrl Pts',(-0.0455740023807954,-0.190403743891933,
1.91729466469043));
#24109=CARTESIAN_POINT('Ctrl Pts',(-0.0335317718966106,-0.19250137732877,
1.91798954923552));
#24110=CARTESIAN_POINT('Ctrl Pts',(-0.021490257254648,-0.194598886073211,
1.91868439247367));
#24111=CARTESIAN_POINT('Ctrl Pts',(-0.00925699821522074,-0.195561281543439,
1.91937923571182));
#24112=CARTESIAN_POINT('Ctrl Pts',(0.00293780523678198,-0.195377914054764,
1.92007407894997));
#24113=CARTESIAN_POINT('Ctrl Pts',(0.0151607146523066,-0.195194123950016,
1.92077052362751));
#24114=CARTESIAN_POINT('Ctrl Pts',(0.0273441174233028,-0.193859377124696,
1.92146696830506));
#24115=CARTESIAN_POINT('Ctrl Pts',(0.0392614908477917,-0.191414982006134,
1.9221634129826));
#24116=CARTESIAN_POINT('Ctrl Pts',(0.0431510759027313,-0.190617181821239,
1.92239071817083));
#24117=CARTESIAN_POINT('Ctrl Pts',(0.0470124198678937,-0.189701581600493,
1.92261802335905));
#24118=CARTESIAN_POINT('Ctrl Pts',(0.0508380046781814,-0.188670764243804,
1.92284532854727));
#24119=CARTESIAN_POINT('Ctrl Pts',(0.0625592780616349,-0.185512425677198,
1.92354177272111));
#24120=CARTESIAN_POINT('Ctrl Pts',(0.0740265955397715,-0.18124644378724,
1.92423821689495));
#24121=CARTESIAN_POINT('Ctrl Pts',(0.0850189987823538,-0.175934447582178,
1.92493466106878));
#24122=CARTESIAN_POINT('Ctrl Pts',(0.0959883310787419,-0.170633600238373,
1.92562964353987));
#24123=CARTESIAN_POINT('Ctrl Pts',(0.106483914527211,-0.164291406083945,
1.92632462601095));
#24124=CARTESIAN_POINT('Ctrl Pts',(0.116303619557301,-0.15701792279186,
1.92701960848203));
#24125=CARTESIAN_POINT('Ctrl Pts',(0.12612194094907,-0.149745464364593,
1.92771449302713));
#24126=CARTESIAN_POINT('Ctrl Pts',(0.135263842934809,-0.141542460680806,
1.92840937757222));
#24127=CARTESIAN_POINT('Ctrl Pts',(0.143556473677907,-0.132562056657116,
1.92910426211731));
#24128=CARTESIAN_POINT('Ctrl Pts',(0.151848611471193,-0.123582186467455,
1.92979910535546));
#24129=CARTESIAN_POINT('Ctrl Pts',(0.159291003765012,-0.113825669224495,
1.93049394859361));
#24130=CARTESIAN_POINT('Ctrl Pts',(0.165749871062098,-0.103480144196352,
1.93118879183176));
#24131=CARTESIAN_POINT('Ctrl Pts',(0.172223624428435,-0.0931107753276527,
1.9318852365093));
#24132=CARTESIAN_POINT('Ctrl Pts',(0.177708919031196,-0.0821504653279504,
1.93258168118685));
#24133=CARTESIAN_POINT('Ctrl Pts',(0.182117624742747,-0.0708119393750788,
1.9332781258644));
#24134=CARTESIAN_POINT('Ctrl Pts',(0.183556535418455,-0.0671112782042444,
1.93350543105262));
#24135=CARTESIAN_POINT('Ctrl Pts',(0.18488115592575,-0.0633704652588357,
1.93373273624084));
#24136=CARTESIAN_POINT('Ctrl Pts',(0.186089579564252,-0.0595972178679496,
1.93396004142906));
#24137=CARTESIAN_POINT('Ctrl Pts',(0.18979208899291,-0.0480363019802609,
1.93465648560289));
#24138=CARTESIAN_POINT('Ctrl Pts',(0.192426241229846,-0.0360881132630105,
1.93535292977673));
#24139=CARTESIAN_POINT('Ctrl Pts',(0.193923996943345,-0.023971721037874,
1.93604937395057));
#24140=CARTESIAN_POINT('Ctrl Pts',(0.195418609154853,-0.0118807587962363,
1.93674435642166));
#24141=CARTESIAN_POINT('Ctrl Pts',(0.195781378446354,0.000376855044065903,
1.93743933889274));
#24142=CARTESIAN_POINT('Ctrl Pts',(0.194995165671587,0.0125716094717537,
1.93813432136383));
#24143=CARTESIAN_POINT('Ctrl Pts',(0.194209063677554,0.0247646456065269,
1.93882920590892));
#24144=CARTESIAN_POINT('Ctrl Pts',(0.192274311263242,0.0368939644022763,
1.93952409045401));
#24145=CARTESIAN_POINT('Ctrl Pts',(0.189225847812887,0.0487312889168142,
1.9402189749991));
#24146=CARTESIAN_POINT('Ctrl Pts',(0.186177565576376,0.060567909769619,
1.94091381823725));
#24147=CARTESIAN_POINT('Ctrl Pts',(0.182015948038732,0.0721117293817821,
1.9416086614754));
#24148=CARTESIAN_POINT('Ctrl Pts',(0.176826104722049,0.0831485940279631,
1.94230350471355));
#24149=CARTESIAN_POINT('Ctrl Pts',(0.171624300118122,0.0942108958791325,
1.9429999493911));
#24150=CARTESIAN_POINT('Ctrl Pts',(0.165389969878783,0.104763145811543,
1.94369639406865));
#24151=CARTESIAN_POINT('Ctrl Pts',(0.158254055236014,0.114615941305548,
1.9443928387462));
#24152=CARTESIAN_POINT('Ctrl Pts',(0.155925039776173,0.117831690677135,
1.94462014393441));
#24153=CARTESIAN_POINT('Ctrl Pts',(0.153500312081673,0.120973186592694,
1.94484744912262));
#24154=CARTESIAN_POINT('Ctrl Pts',(0.15098532230701,0.12403464212811,1.94507475431084));
#24155=CARTESIAN_POINT('Ctrl Pts',(0.143279603006913,0.133414687026621,
1.94577119848467));
#24156=CARTESIAN_POINT('Ctrl Pts',(0.134669153546287,0.142107105085762,
1.9464676426585));
#24157=CARTESIAN_POINT('Ctrl Pts',(0.12530114024442,0.149935933829914,1.94716408683234));
#24158=CARTESIAN_POINT('Ctrl Pts',(0.115952788605793,0.157748331364014,
1.94785906930342));
#24159=CARTESIAN_POINT('Ctrl Pts',(0.105850646345792,0.164700123965514,
1.9485540517745));
#24160=CARTESIAN_POINT('Ctrl Pts',(0.0951782547854528,0.170652453296152,
1.94924903424558));
#24161=CARTESIAN_POINT('Ctrl Pts',(0.0845073670106115,0.176603943918196,
1.94994391879067));
#24162=CARTESIAN_POINT('Ctrl Pts',(0.0732671306095171,0.181555784687013,
1.95063880333576));
#24163=CARTESIAN_POINT('Ctrl Pts',(0.0616682909041917,0.185413542916789,
1.95133368788085));
#24164=CARTESIAN_POINT('Ctrl Pts',(0.0500701406840297,0.189271071824742,
1.95202853111899));
#24165=CARTESIAN_POINT('Ctrl Pts',(0.0381142689195054,0.192034396292956,
1.95272337435714));
#24166=CARTESIAN_POINT('Ctrl Pts',(0.0260267605822,0.193658895312343,1.95341821759529));
#24167=CARTESIAN_POINT('Ctrl Pts',(0.0139113935696971,0.195287138394548,
1.95411466227283));
#24168=CARTESIAN_POINT('Ctrl Pts',(0.0016646603449519,0.19577126388408,
1.95481110695038));
#24169=CARTESIAN_POINT('Ctrl Pts',(-0.0104832967402934,0.195118580584871,
1.95550755162792));
#24170=CARTESIAN_POINT('Ctrl Pts',(-0.0144481395495736,0.194905558208562,
1.95573485681615));
#24171=CARTESIAN_POINT('Ctrl Pts',(-0.0184024968294661,0.194571852522418,
1.95596216200438));
#24172=CARTESIAN_POINT('Ctrl Pts',(-0.022338550918238,0.194118904650921,
1.9561894671926));
#24173=CARTESIAN_POINT('Ctrl Pts',(-0.0343982929743568,0.192731110080032,
1.95688591136644));
#24174=CARTESIAN_POINT('Ctrl Pts',(-0.0463709023191962,0.190210277458485,
1.95758235554028));
#24175=CARTESIAN_POINT('Ctrl Pts',(-0.0580287304895212,0.186584636124667,
1.95827879971411));
#24176=CARTESIAN_POINT('Ctrl Pts',(-0.0696620911143581,0.182966604316652,
1.9589737821852));
#24177=CARTESIAN_POINT('Ctrl Pts',(-0.0809811319250672,0.178248552415478,
1.95966876465628));
#24178=CARTESIAN_POINT('Ctrl Pts',(-0.0917696541604555,0.172509392716079,
1.96036374712737));
#24179=CARTESIAN_POINT('Ctrl Pts',(-0.102556656247037,0.166771041688765,
1.96105863167246));
#24180=CARTESIAN_POINT('Ctrl Pts',(-0.112812494578821,0.160012238431858,
1.96175351621755));
#24181=CARTESIAN_POINT('Ctrl Pts',(-0.122343544844339,0.152358842982353,
1.96244840076264));
#24182=CARTESIAN_POINT('Ctrl Pts',(-0.131874028543028,0.144705902483758,
1.96314324400079));
#24183=CARTESIAN_POINT('Ctrl Pts',(-0.140679143598295,0.136159044544678,
1.96383808723894));
#24184=CARTESIAN_POINT('Ctrl Pts',(-0.14859879923003,0.126884029205385,
1.96453293047709));
#24185=CARTESIAN_POINT('Ctrl Pts',(-0.156536707681768,0.117587637281885,
1.96522937515464));
#24186=CARTESIAN_POINT('Ctrl Pts',(-0.163584563634262,0.107560445319938,
1.96592581983219));
#24187=CARTESIAN_POINT('Ctrl Pts',(-0.169623707588393,0.0969997825975262,
1.96662226450974));
#24188=CARTESIAN_POINT('Ctrl Pts',(-0.171594759701241,0.0935529999524722,
1.96684956969795));
#24189=CARTESIAN_POINT('Ctrl Pts',(-0.173458727505659,0.0900495837618375,
1.96707687488617));
#24190=CARTESIAN_POINT('Ctrl Pts',(-0.175212582516426,0.0864968839203154,
1.96730418007439));
#24191=CARTESIAN_POINT('Ctrl Pts',(-0.180970069375756,0.0748342193744243,
1.9680503686853));
#24192=CARTESIAN_POINT('Ctrl Pts',(-0.18557358731148,0.0625657075161415,
1.9687965572962));
#24193=CARTESIAN_POINT('Ctrl Pts',(-0.188913584232968,0.0499281252627537,
1.96954274590711));
#24194=CARTESIAN_POINT('Ctrl Pts',(-0.192235407018057,0.0373593086846153,
1.97028487423476));
#24195=CARTESIAN_POINT('Ctrl Pts',(-0.194307127941387,0.0244260431589578,
1.97102700256241));
#24196=CARTESIAN_POINT('Ctrl Pts',(-0.195068230692454,0.0113818001438891,
1.97176913089005));
#24197=CARTESIAN_POINT('Ctrl Pts',(-0.195288350830162,0.00760924700998056,
1.9719837633946));
#24198=CARTESIAN_POINT('Ctrl Pts',(-0.19539916387975,0.00382750994004229,
1.97219839589914));
#24199=CARTESIAN_POINT('Ctrl Pts',(-0.195399995284978,4.29258736808888E-5,
1.97241302840369));
#24200=CARTESIAN_POINT('',(-0.195381194231368,-0.000178768183475579,2.04241303078758));
#24201=CARTESIAN_POINT('Ctrl Pts',(-0.195087892673083,4.28153426326047E-5,
1.97241303078758));
#24202=CARTESIAN_POINT('Ctrl Pts',(-0.195018847371885,-0.0352009863002633,
1.97441498484377));
#24203=CARTESIAN_POINT('Ctrl Pts',(-0.169041111820685,-0.135763402236124,
1.98012184319391));
#24204=CARTESIAN_POINT('Ctrl Pts',(-0.00786427776343007,-0.230825175541495,
1.98953360583792));
#24205=CARTESIAN_POINT('Ctrl Pts',(0.189675009695224,-0.131778219845546,
2.00064831871973));
#24206=CARTESIAN_POINT('Ctrl Pts',(0.213576180559187,0.0879051968103242,
2.01176303160147));
#24207=CARTESIAN_POINT('Ctrl Pts',(0.041958891709634,0.227115741275293,
2.02287774448327));
#24208=CARTESIAN_POINT('Ctrl Pts',(-0.151099805097311,0.163964067429302,
2.03309441087863));
#24209=CARTESIAN_POINT('Ctrl Pts',(-0.194932378367354,0.0490481979593188,
2.03960617298007));
#24210=CARTESIAN_POINT('Ctrl Pts',(-0.195381194231368,-0.000178768183475579,
2.04241303078758));
#24211=CARTESIAN_POINT('',(-0.19541850016519,6.52473648468253E-5,2.11241303078758));
#24212=CARTESIAN_POINT('Ctrl Pts',(-0.195381194231368,-0.000178768183475579,
2.04241303078758));
#24213=CARTESIAN_POINT('Ctrl Pts',(-0.195524791640772,-0.0159288014993712,
2.04331107727399));
#24214=CARTESIAN_POINT('Ctrl Pts',(-0.186583102676833,-0.0964948299411469,
2.04791402805432));
#24215=CARTESIAN_POINT('Ctrl Pts',(-0.0751283049278637,-0.2183983661272,
2.0562218831286));
#24216=CARTESIAN_POINT('Ctrl Pts',(0.1427584110397,-0.181554797804677,2.06733659601036));
#24217=CARTESIAN_POINT('Ctrl Pts',(0.229956842554754,0.0214932336169986,
2.07845130889215));
#24218=CARTESIAN_POINT('Ctrl Pts',(0.106641126190405,0.204865269707955,
2.08956602177393));
#24219=CARTESIAN_POINT('Ctrl Pts',(-0.114299281647457,0.200693255350358,
2.10068073465569));
#24220=CARTESIAN_POINT('Ctrl Pts',(-0.193990126770331,0.0719485985092084,
2.10829640432692));
#24221=CARTESIAN_POINT('Ctrl Pts',(-0.195709494543343,0.00366078499822498,
2.11220716970421));
#24222=CARTESIAN_POINT('Ctrl Pts',(-0.195693853754418,6.53393013630089E-5,
2.11241303078758));
#24223=CARTESIAN_POINT('',(-0.195399951179357,0.000138127132403044,2.18241302809352));
#24224=CARTESIAN_POINT('Ctrl Pts',(-0.195399989108464,6.52411842770674E-5,
2.11241303078758));
#24225=CARTESIAN_POINT('Ctrl Pts',(-0.195404009954938,-0.0119773568441924,
2.11310358064536));
#24226=CARTESIAN_POINT('Ctrl Pts',(-0.194290431945964,-0.0240652292057775,
2.11379413050314));
#24227=CARTESIAN_POINT('Ctrl Pts',(-0.192060322024632,-0.0359721100825972,
2.11448468036092));
#24228=CARTESIAN_POINT('Ctrl Pts',(-0.189792835897659,-0.0480785479516255,
2.11518680369912));
#24229=CARTESIAN_POINT('Ctrl Pts',(-0.186370972563584,-0.0599969165405934,
2.11588892703731));
#24230=CARTESIAN_POINT('Ctrl Pts',(-0.181851010938754,-0.0714938446340174,
2.1165910503755));
#24231=CARTESIAN_POINT('Ctrl Pts',(-0.177414767965862,-0.0827778268218566,
2.11728016899723));
#24232=CARTESIAN_POINT('Ctrl Pts',(-0.171921179356806,-0.093655022735873,
2.11796928761896));
#24233=CARTESIAN_POINT('Ctrl Pts',(-0.165473021615391,-0.103922274404827,
2.11865840624069));
#24234=CARTESIAN_POINT('Ctrl Pts',(-0.158842334058695,-0.114480164055317,
2.11936703193712));
#24235=CARTESIAN_POINT('Ctrl Pts',(-0.151202616365141,-0.124392135141495,
2.12007565763354));
#24236=CARTESIAN_POINT('Ctrl Pts',(-0.142713033203458,-0.133469660050023,
2.12078428332997));
#24237=CARTESIAN_POINT('Ctrl Pts',(-0.134223450041775,-0.14254718495855,
2.1214929090264));
#24238=CARTESIAN_POINT('Ctrl Pts',(-0.124884795392853,-0.150789626260811,
2.12220153472282));
#24239=CARTESIAN_POINT('Ctrl Pts',(-0.114893963288023,-0.15805232424729,
2.12291016041925));
#24240=CARTESIAN_POINT('Ctrl Pts',(-0.10507487705743,-0.165190173932654,
2.12360660459381));
#24241=CARTESIAN_POINT('Ctrl Pts',(-0.0945533255298709,-0.171434765623136,
2.12430304876837));
#24242=CARTESIAN_POINT('Ctrl Pts',(-0.0835160360064994,-0.176652856557037,
2.12499949294294));
#24243=CARTESIAN_POINT('Ctrl Pts',(-0.0725019116369707,-0.181859995718858,
2.12569447541475));
#24244=CARTESIAN_POINT('Ctrl Pts',(-0.0609749495797634,-0.186044472344931,
2.12638945788656));
#24245=CARTESIAN_POINT('Ctrl Pts',(-0.0491477388324685,-0.189118110628399,
2.12708444035837));
#24246=CARTESIAN_POINT('Ctrl Pts',(-0.0373221945897685,-0.192191315823083,
2.12777932490418));
#24247=CARTESIAN_POINT('Ctrl Pts',(-0.025197320293739,-0.194153728862889,
2.12847420944999));
#24248=CARTESIAN_POINT('Ctrl Pts',(-0.0130008477400179,-0.194967017615906,
2.1291690939958));
#24249=CARTESIAN_POINT('Ctrl Pts',(-0.00080510019741124,-0.195780258023519,
2.12986393723466));
#24250=CARTESIAN_POINT('Ctrl Pts',(0.0114613615557843,-0.195444478168219,
2.13055878047352));
#24251=CARTESIAN_POINT('Ctrl Pts',(0.023568501124126,-0.193973415072174,
2.13125362371239));
#24252=CARTESIAN_POINT('Ctrl Pts',(0.0357035446123529,-0.192498961544679,
2.13195006839063));
#24253=CARTESIAN_POINT('Ctrl Pts',(0.0476776718778061,-0.189884171171409,
2.13264651306887));
#24254=CARTESIAN_POINT('Ctrl Pts',(0.0592699940457487,-0.186194059534178,
2.13334295774711));
#24255=CARTESIAN_POINT('Ctrl Pts',(0.0630534890067612,-0.184989683173448,
2.13357026293175));
#24256=CARTESIAN_POINT('Ctrl Pts',(0.0667964521463349,-0.183671150874965,
2.13379756811639));
#24257=CARTESIAN_POINT('Ctrl Pts',(0.0704916804535371,-0.182241825569314,
2.13402487330102));
#24258=CARTESIAN_POINT('Ctrl Pts',(0.081813552527267,-0.177862491759065,
2.13472131747394));
#24259=CARTESIAN_POINT('Ctrl Pts',(0.0927658372219972,-0.172408554535117,
2.13541776164686));
#24260=CARTESIAN_POINT('Ctrl Pts',(0.103135326315513,-0.165964648241102,
2.13611420581978));
#24261=CARTESIAN_POINT('Ctrl Pts',(0.11348305184025,-0.159534266470481,
2.13680918828995));
#24262=CARTESIAN_POINT('Ctrl Pts',(0.123249633878203,-0.152118433842278,
2.13750417076013));
#24263=CARTESIAN_POINT('Ctrl Pts',(0.132245705377629,-0.143847952398264,
2.1381991532303));
#24264=CARTESIAN_POINT('Ctrl Pts',(0.141240509292515,-0.135578636300082,
2.13889403777451));
#24265=CARTESIAN_POINT('Ctrl Pts',(0.149464343322348,-0.126455468272226,
2.13958892231871));
#24266=CARTESIAN_POINT('Ctrl Pts',(0.156761507579238,-0.116649002316713,
2.14028380686291));
#24267=CARTESIAN_POINT('Ctrl Pts',(0.164058238061282,-0.106843119299737,
2.14097865010019));
#24268=CARTESIAN_POINT('Ctrl Pts',(0.170427906774986,-0.0963547375420952,
2.14167349333747));
#24269=CARTESIAN_POINT('Ctrl Pts',(0.175757312676377,-0.0853845831563189,
2.14236833657474));
#24270=CARTESIAN_POINT('Ctrl Pts',(0.181099001522049,-0.074389145315392,
2.14306478125145));
#24271=CARTESIAN_POINT('Ctrl Pts',(0.185395317103463,-0.0629105337170144,
2.14376122592816));
#24272=CARTESIAN_POINT('Ctrl Pts',(0.188581103156866,-0.0511695957785429,
2.14445767060487));
#24273=CARTESIAN_POINT('Ctrl Pts',(0.18962087808345,-0.0473375955505419,
2.14468497579752));
#24274=CARTESIAN_POINT('Ctrl Pts',(0.190542759656903,-0.0434777463364903,
2.14491228099016));
#24275=CARTESIAN_POINT('Ctrl Pts',(0.191345667405416,-0.0395979237482983,
2.14513958618281));
#24276=CARTESIAN_POINT('Ctrl Pts',(0.193805709855286,-0.0277104705725173,
2.1458360303559));
#24277=CARTESIAN_POINT('Ctrl Pts',(0.195162451269964,-0.0155508149849334,
2.14653247452899));
#24278=CARTESIAN_POINT('Ctrl Pts',(0.195371384116943,-0.00334398986690795,
2.14722891870209));
#24279=CARTESIAN_POINT('Ctrl Pts',(0.195579878453941,0.00883721546595823,
2.14792390117241));
#24280=CARTESIAN_POINT('Ctrl Pts',(0.194645256331035,0.0210645283257843,
2.14861888364273));
#24281=CARTESIAN_POINT('Ctrl Pts',(0.192574728837452,0.0331079116402994,
2.14931386611306));
#24282=CARTESIAN_POINT('Ctrl Pts',(0.190504493090074,0.0451495979904483,
2.15000875065737));
#24283=CARTESIAN_POINT('Ctrl Pts',(0.187298772424921,0.057006536720609,
2.15070363520168));
#24284=CARTESIAN_POINT('Ctrl Pts',(0.18301643442899,0.0684554214719283,
2.15139851974599));
#24285=CARTESIAN_POINT('Ctrl Pts',(0.178734350993801,0.0799036256518854,
2.15209336298335));
#24286=CARTESIAN_POINT('Ctrl Pts',(0.173376109136668,0.0909430131191398,
2.15278820622072));
#24287=CARTESIAN_POINT('Ctrl Pts',(0.167048973136666,0.1013696235269,2.15348304945808));
#24288=CARTESIAN_POINT('Ctrl Pts',(0.160707254675002,0.111820264656703,
2.15417949413484));
#24289=CARTESIAN_POINT('Ctrl Pts',(0.153392693571326,0.121654594715726,
2.1548759388116));
#24290=CARTESIAN_POINT('Ctrl Pts',(0.145255513517713,0.130698109369284,
2.15557238348836));
#24291=CARTESIAN_POINT('Ctrl Pts',(0.14259970561691,0.133649726208252,2.15579968868043));
#24292=CARTESIAN_POINT('Ctrl Pts',(0.139856568384743,0.136517390700739,
2.1560269938725));
#24293=CARTESIAN_POINT('Ctrl Pts',(0.137032133007897,0.139295924288208,
2.15625429906457));
#24294=CARTESIAN_POINT('Ctrl Pts',(0.128378298230296,0.147809119805824,
2.15695074324326));
#24295=CARTESIAN_POINT('Ctrl Pts',(0.118897466433838,0.155542928834054,
2.15764718742195));
#24296=CARTESIAN_POINT('Ctrl Pts',(0.108754575230515,0.162337926457222,
2.15834363160064));
#24297=CARTESIAN_POINT('Ctrl Pts',(0.0986329720101885,0.169118662683814,
2.15903861407659));
#24298=CARTESIAN_POINT('Ctrl Pts',(0.0878527460907765,0.174963953922716,
2.15973359655254));
#24299=CARTESIAN_POINT('Ctrl Pts',(0.0766110853095108,0.179755115664892,
2.16042857902849));
#24300=CARTESIAN_POINT('Ctrl Pts',(0.0653710085270541,0.184545602311579,
2.16112346357839));
#24301=CARTESIAN_POINT('Ctrl Pts',(0.0536704122311272,0.188281869105566,
2.16181834812829));
#24302=CARTESIAN_POINT('Ctrl Pts',(0.0417288411143926,0.1908922832889,2.16251323267819));
#24303=CARTESIAN_POINT('Ctrl Pts',(0.02978797985669,0.193502542297839,2.16320807592113));
#24304=CARTESIAN_POINT('Ctrl Pts',(0.0176070334827736,0.194986920660723,
2.16390291916406));
#24305=CARTESIAN_POINT('Ctrl Pts',(0.00541553644085428,0.195324939434415,
2.164597762407));
#24306=CARTESIAN_POINT('Ctrl Pts',(-0.00680405894173796,0.195663737256539,
2.16529420708921));
#24307=CARTESIAN_POINT('Ctrl Pts',(-0.0190333768825485,0.194850941551038,
2.16599065177142));
#24308=CARTESIAN_POINT('Ctrl Pts',(-0.0310443361113374,0.192918141177563,
2.16668709645363));
#24309=CARTESIAN_POINT('Ctrl Pts',(-0.0349644652041019,0.192287315043677,
2.16691440161787));
#24310=CARTESIAN_POINT('Ctrl Pts',(-0.0388614139166113,0.191537589492705,
2.16714170678211));
#24311=CARTESIAN_POINT('Ctrl Pts',(-0.0427275606604851,0.190671223733432,
2.16736901194636));
#24312=CARTESIAN_POINT('Ctrl Pts',(-0.0545731135566909,0.188016750918818,
2.16806545611286));
#24313=CARTESIAN_POINT('Ctrl Pts',(-0.0662122844687849,0.184244792641138,
2.16876190027937));
#24314=CARTESIAN_POINT('Ctrl Pts',(-0.0774216828963899,0.179407477596367,
2.16945834444588));
#24315=CARTESIAN_POINT('Ctrl Pts',(-0.0886075549469531,0.17458031514795,
2.17015332690968));
#24316=CARTESIAN_POINT('Ctrl Pts',(-0.0993646193415472,0.168692508981423,
2.17084830937347));
#24317=CARTESIAN_POINT('Ctrl Pts',(-0.109486227241,0.161845376963731,2.17154329183727));
#24318=CARTESIAN_POINT('Ctrl Pts',(-0.119606408965187,0.154999209734482,
2.17223817637524));
#24319=CARTESIAN_POINT('Ctrl Pts',(-0.12909056190635,0.147194436732592,
2.17293306091322));
#24320=CARTESIAN_POINT('Ctrl Pts',(-0.137759446610311,0.138576675056161,
2.17362794545119));
#24321=CARTESIAN_POINT('Ctrl Pts',(-0.146427815999421,0.129959425655613,
2.17432278868231));
#24322=CARTESIAN_POINT('Ctrl Pts',(-0.1542804111314,0.120529919908332,2.17501763191344));
#24323=CARTESIAN_POINT('Ctrl Pts',(-0.161175554861648,0.110469907735273,
2.17571247514456));
#24324=CARTESIAN_POINT('Ctrl Pts',(-0.168086590171654,0.100386709753177,
2.17640891981534));
#24325=CARTESIAN_POINT('Ctrl Pts',(-0.174035327454208,0.089670862891376,
2.17710536448613));
#24326=CARTESIAN_POINT('Ctrl Pts',(-0.178924625021148,0.0785311311585511,
2.17780180915691));
#24327=CARTESIAN_POINT('Ctrl Pts',(-0.180520391237771,0.0748953517202774,
2.17802911438065));
#24328=CARTESIAN_POINT('Ctrl Pts',(-0.182003687820427,0.0712145723022263,
2.17825641960439));
#24329=CARTESIAN_POINT('Ctrl Pts',(-0.183372279963377,0.0674964216905826,
2.17848372482813));
#24330=CARTESIAN_POINT('Ctrl Pts',(-0.188182590555252,0.0544279123019244,
2.17928265439306));
#24331=CARTESIAN_POINT('Ctrl Pts',(-0.191600390049941,0.040820586561108,
2.180081583958));
#24332=CARTESIAN_POINT('Ctrl Pts',(-0.19353130983678,0.0269590821961754,
2.18088051352294));
#24333=CARTESIAN_POINT('Ctrl Pts',(-0.19476594629612,0.0180959907374373,
2.18139135171313));
#24334=CARTESIAN_POINT('Ctrl Pts',(-0.195393595265852,0.00912944670203462,
2.18190218990332));
#24335=CARTESIAN_POINT('Ctrl Pts',(-0.195399951179357,0.000138127132403044,
2.18241302809352));
#24336=CARTESIAN_POINT('',(-0.195399948757862,-0.000141511218596957,2.25241303346085));
#24337=CARTESIAN_POINT('Ctrl Pts',(-0.19518796491764,0.000137929913403057,
2.18241303078758));
#24338=CARTESIAN_POINT('Ctrl Pts',(-0.194913552398402,-0.0419735976389966,
2.18480816642835));
#24339=CARTESIAN_POINT('Ctrl Pts',(-0.16086256744259,-0.149629643335042,
2.19090820636306));
#24340=CARTESIAN_POINT('Ctrl Pts',(0.0165728994326759,-0.230363729251873,
2.20071315059169));
#24341=CARTESIAN_POINT('Ctrl Pts',(0.202538966804153,-0.110995839031369,
2.21182786347345));
#24342=CARTESIAN_POINT('Ctrl Pts',(0.203090589989405,0.109983263613663,
2.22294257635524));
#24343=CARTESIAN_POINT('Ctrl Pts',(0.0177228121885867,0.230278120197377,
2.23405728923701));
#24344=CARTESIAN_POINT('Ctrl Pts',(-0.160449819017681,0.150279904486619,
2.24388077404779));
#24345=CARTESIAN_POINT('Ctrl Pts',(-0.194911113219737,0.0422922816017406,
2.24999935456465));
#24346=CARTESIAN_POINT('Ctrl Pts',(-0.195195111391083,-0.000141315875587933,
2.25241303078758));
#24347=CARTESIAN_POINT('',(-0.195423887338554,-5.94508832628922E-5,2.32241303078758));
#24348=CARTESIAN_POINT('Ctrl Pts',(-0.195399948757862,-0.000141511218596957,
2.25241303346085));
#24349=CARTESIAN_POINT('Ctrl Pts',(-0.19538972200811,-0.0142626981980689,
2.25321542657059));
#24350=CARTESIAN_POINT('Ctrl Pts',(-0.193844609223536,-0.028321132308972,
2.25401781968034));
#24351=CARTESIAN_POINT('Ctrl Pts',(-0.190829150317375,-0.0420166084917452,
2.25482021279009));
#24352=CARTESIAN_POINT('Ctrl Pts',(-0.18899207191704,-0.0503601688786147,
2.25530904686025));
#24353=CARTESIAN_POINT('Ctrl Pts',(-0.186610260799985,-0.0585693700250536,
2.25579788093041));
#24354=CARTESIAN_POINT('Ctrl Pts',(-0.1837069757175,-0.0665800801496189,
2.25628671500057));
#24355=CARTESIAN_POINT('Ctrl Pts',(-0.179570644684268,-0.0779929961895826,
2.25698316039847));
#24356=CARTESIAN_POINT('Ctrl Pts',(-0.174352052153745,-0.0890593770579522,
2.25767960579638));
#24357=CARTESIAN_POINT('Ctrl Pts',(-0.168131256433172,-0.0995642536767232,
2.25837605119428));
#24358=CARTESIAN_POINT('Ctrl Pts',(-0.161923516865908,-0.110047082749524,
2.25907103489849));
#24359=CARTESIAN_POINT('Ctrl Pts',(-0.15471812658239,-0.119969962728062,
2.2597660186027));
#24360=CARTESIAN_POINT('Ctrl Pts',(-0.146641810605223,-0.129140773508687,
2.2604610023069));
#24361=CARTESIAN_POINT('Ctrl Pts',(-0.13856663267905,-0.138310292010708,
2.26115588807947));
#24362=CARTESIAN_POINT('Ctrl Pts',(-0.12962131595782,-0.146727265055829,
2.26185077385203));
#24363=CARTESIAN_POINT('Ctrl Pts',(-0.119973047942276,-0.154232382356755,
2.2625456596246));
#24364=CARTESIAN_POINT('Ctrl Pts',(-0.110325353488193,-0.161737053500295,
2.26324050408822));
#24365=CARTESIAN_POINT('Ctrl Pts',(-0.0999754983665426,-0.168329459918655,
2.26393534855185));
#24366=CARTESIAN_POINT('Ctrl Pts',(-0.089121743707153,-0.173892135528311,
2.26463019301547));
#24367=CARTESIAN_POINT('Ctrl Pts',(-0.0782429743078843,-0.179467631483348,
2.26532663889299));
#24368=CARTESIAN_POINT('Ctrl Pts',(-0.0668587953570758,-0.184008317362891,
2.26602308477051));
#24369=CARTESIAN_POINT('Ctrl Pts',(-0.0551886116770029,-0.187444330778941,
2.26671953064803));
#24370=CARTESIAN_POINT('Ctrl Pts',(-0.0513798132084584,-0.18856574266034,
2.26694682972613));
#24371=CARTESIAN_POINT('Ctrl Pts',(-0.0475406538048195,-0.1895698896982,
2.26717412880423));
#24372=CARTESIAN_POINT('Ctrl Pts',(-0.0436789835309181,-0.190455523410863,
2.26740142788233));
#24373=CARTESIAN_POINT('Ctrl Pts',(-0.0318468808551804,-0.193169092482813,
2.26809786901775));
#24374=CARTESIAN_POINT('Ctrl Pts',(-0.0197190546916775,-0.194785440763548,
2.26879431015317));
#24375=CARTESIAN_POINT('Ctrl Pts',(-0.00751953334359756,-0.19525526015525,
2.26949075128859));
#24376=CARTESIAN_POINT('Ctrl Pts',(0.00465438351031375,-0.195724093484669,
2.27018573072543));
#24377=CARTESIAN_POINT('Ctrl Pts',(0.0168988334777028,-0.195051066224396,
2.27088071016227));
#24378=CARTESIAN_POINT('Ctrl Pts',(0.0289836795020654,-0.193238470089477,
2.27157568959911));
#24379=CARTESIAN_POINT('Ctrl Pts',(0.0410668236085626,-0.191426129223821,
2.27227057116148));
#24380=CARTESIAN_POINT('Ctrl Pts',(0.0529895368640161,-0.188474622183162,
2.27296545272385));
#24381=CARTESIAN_POINT('Ctrl Pts',(0.0645273070894692,-0.184438029266693,
2.27366033428623));
#24382=CARTESIAN_POINT('Ctrl Pts',(0.0760643919002142,-0.180401676148737,
2.27435517456835));
#24383=CARTESIAN_POINT('Ctrl Pts',(0.08721576127461,-0.175280679575768,
2.27505001485047));
#24384=CARTESIAN_POINT('Ctrl Pts',(0.0977752101557561,-0.1691779190054,
2.27574485513259));
#24385=CARTESIAN_POINT('Ctrl Pts',(0.108358997437004,-0.163061092224744,
2.27644129694723));
#24386=CARTESIAN_POINT('Ctrl Pts',(0.11834741527388,-0.155958478066104,
2.27713773876187));
#24387=CARTESIAN_POINT('Ctrl Pts',(0.127562789698037,-0.148016535172441,
2.27783418057652));
#24388=CARTESIAN_POINT('Ctrl Pts',(0.130570707152647,-0.145424268428428,
2.27806150063905));
#24389=CARTESIAN_POINT('Ctrl Pts',(0.133496547523929,-0.1427428860611,2.27828882070159));
#24390=CARTESIAN_POINT('Ctrl Pts',(0.136335003486585,-0.139978308406385,
2.27851614076412));
#24391=CARTESIAN_POINT('Ctrl Pts',(0.145031250161049,-0.131508404503551,
2.27921258677698));
#24392=CARTESIAN_POINT('Ctrl Pts',(0.15296596216631,-0.122195029690922,
2.27990903278983));
#24393=CARTESIAN_POINT('Ctrl Pts',(0.159976224875834,-0.112199676802015,
2.28060547880269));
#24394=CARTESIAN_POINT('Ctrl Pts',(0.166971774010696,-0.102225302780391,
2.28130046307141));
#24395=CARTESIAN_POINT('Ctrl Pts',(0.173046166156125,-0.0915724586430868,
2.28199544734013));
#24396=CARTESIAN_POINT('Ctrl Pts',(0.178076528417178,-0.080435750925108,
2.28269043160885));
#24397=CARTESIAN_POINT('Ctrl Pts',(0.183106181259049,-0.0693006137886638,
2.2833853178657));
#24398=CARTESIAN_POINT('Ctrl Pts',(0.187091694573998,-0.0576825263938266,
2.28408020412256));
#24399=CARTESIAN_POINT('Ctrl Pts',(0.189956758562106,-0.0457994527978004,
2.28477509037942));
#24400=CARTESIAN_POINT('Ctrl Pts',(0.192821652041564,-0.0339170863995334,
2.28546993528149));
#24401=CARTESIAN_POINT('Ctrl Pts',(0.194566049299117,-0.0217706227331317,
2.28616478018355));
#24402=CARTESIAN_POINT('Ctrl Pts',(0.195164569092226,-0.00958910689510555,
2.28685962508562));
#24403=CARTESIAN_POINT('Ctrl Pts',(0.195764468234045,0.00262048246421898,
2.28755607132724));
#24404=CARTESIAN_POINT('Ctrl Pts',(0.195213239780637,0.0148644079464561,
2.28825251756887));
#24405=CARTESIAN_POINT('Ctrl Pts',(0.193537589456231,0.0269139641723655,
2.28894896381049));
#24406=CARTESIAN_POINT('Ctrl Pts',(0.192990713590533,0.030846533752276,
2.28917626042229));
#24407=CARTESIAN_POINT('Ctrl Pts',(0.192324478908695,0.0347584713101603,
2.28940355703409));
#24408=CARTESIAN_POINT('Ctrl Pts',(0.191540980908215,0.0386421095790456,
2.28963085364589));
#24409=CARTESIAN_POINT('Ctrl Pts',(0.189140292853597,0.0505418259725163,
2.29032730502224));
#24410=CARTESIAN_POINT('Ctrl Pts',(0.185617940255705,0.0622590833852615,
2.2910237563986));
#24411=CARTESIAN_POINT('Ctrl Pts',(0.181021268785419,0.073569424677084,
2.29172020777495));
#24412=CARTESIAN_POINT('Ctrl Pts',(0.176434244283268,0.0848560291187227,
2.29241519751884));
#24413=CARTESIAN_POINT('Ctrl Pts',(0.170777633329243,0.0957365812876027,
2.29311018726273));
#24414=CARTESIAN_POINT('Ctrl Pts',(0.164148317176213,0.106002311145642,
2.29380517700663));
#24415=CARTESIAN_POINT('Ctrl Pts',(0.157519935201171,0.11626659439612,2.29450006881521));
#24416=CARTESIAN_POINT('Ctrl Pts',(0.149919555733696,0.125915467828864,
2.29519496062379));
#24417=CARTESIAN_POINT('Ctrl Pts',(0.141488934767856,0.13476661804118,2.29588985243238));
#24418=CARTESIAN_POINT('Ctrl Pts',(0.133058814923699,0.143617242135276,
2.29658470293613));
#24419=CARTESIAN_POINT('Ctrl Pts',(0.123799174908022,0.151669621464244,
2.29727955343989));
#24420=CARTESIAN_POINT('Ctrl Pts',(0.113888698061204,0.158778224117553,
2.29797440394364));
#24421=CARTESIAN_POINT('Ctrl Pts',(0.103955382158895,0.165903208805044,
2.29867085575574));
#24422=CARTESIAN_POINT('Ctrl Pts',(0.0933689840818892,0.172079617408341,
2.29936730756783));
#24423=CARTESIAN_POINT('Ctrl Pts',(0.0823361470535406,0.177205865840772,
2.30006375937993));
#24424=CARTESIAN_POINT('Ctrl Pts',(0.0787358658303617,0.178878684530037,
2.30029102842917));
#24425=CARTESIAN_POINT('Ctrl Pts',(0.0750882063564142,0.180440056483083,
2.30051829747842));
#24426=CARTESIAN_POINT('Ctrl Pts',(0.071400744166959,0.181887585426836,
2.30074556652767));
#24427=CARTESIAN_POINT('Ctrl Pts',(0.0601012195165049,0.186323261819383,
2.30144198918702));
#24428=CARTESIAN_POINT('Ctrl Pts',(0.0483467618574154,0.189717665048775,
2.30213841184638));
#24429=CARTESIAN_POINT('Ctrl Pts',(0.0363516163698731,0.191988853810052,
2.30283483450573));
#24430=CARTESIAN_POINT('Ctrl Pts',(0.024381647087459,0.194255275650062,
2.30352979546713));
#24431=CARTESIAN_POINT('Ctrl Pts',(0.0121728306059993,0.195402927618314,
2.30422475642852));
#24432=CARTESIAN_POINT('Ctrl Pts',(-4.69041769829161E-5,0.195399994370517,
2.30491971738991));
#24433=CARTESIAN_POINT('Ctrl Pts',(-0.0122649228945991,0.195397061534648,
2.30561458075521));
#24434=CARTESIAN_POINT('Ctrl Pts',(-0.0244929824437572,0.194243818350495,
2.3063094441205));
#24435=CARTESIAN_POINT('Ctrl Pts',(-0.0365010469752692,0.191960500024638,
2.3070043074858));
#24436=CARTESIAN_POINT('Ctrl Pts',(-0.0485084005892147,0.189677316878861,
2.30769912971286));
#24437=CARTESIAN_POINT('Ctrl Pts',(-0.0602949296388099,0.186264381307076,
2.30839395193992));
#24438=CARTESIAN_POINT('Ctrl Pts',(-0.0716414773323995,0.181792900646949,
2.30908877416698));
#24439=CARTESIAN_POINT('Ctrl Pts',(-0.0830141870764818,0.17731110996954,
2.30978519846497));
#24440=CARTESIAN_POINT('Ctrl Pts',(-0.0939440996977907,0.17176628294015,
2.31048162276295));
#24441=CARTESIAN_POINT('Ctrl Pts',(-0.104233822067019,0.165276950411426,
2.31117804706094));
#24442=CARTESIAN_POINT('Ctrl Pts',(-0.107593833809719,0.1631579201095,2.31140545784378));
#24443=CARTESIAN_POINT('Ctrl Pts',(-0.110885816438744,0.160938522031444,
2.31163286862661));
#24444=CARTESIAN_POINT('Ctrl Pts',(-0.114103637106889,0.15862383174977,
2.31186027940945));
#24445=CARTESIAN_POINT('Ctrl Pts',(-0.12388277810694,0.151589355633677,
2.31255139378145));
#24446=CARTESIAN_POINT('Ctrl Pts',(-0.133046136579518,0.143620245172889,
2.31324250815345));
#24447=CARTESIAN_POINT('Ctrl Pts',(-0.141410229922725,0.13484920049152,
2.31393362252545));
#24448=CARTESIAN_POINT('Ctrl Pts',(-0.149961945465167,0.125881404934092,
2.31464023988062));
#24449=CARTESIAN_POINT('Ctrl Pts',(-0.157677242816501,0.116075733836457,
2.3153468572358));
#24450=CARTESIAN_POINT('Ctrl Pts',(-0.164396399278085,0.105617157244457,
2.31605347459098));
#24451=CARTESIAN_POINT('Ctrl Pts',(-0.170953214755027,0.0954112694582027,
2.31674301942257));
#24452=CARTESIAN_POINT('Ctrl Pts',(-0.176561081723516,0.0845845189451643,
2.31743256425415));
#24453=CARTESIAN_POINT('Ctrl Pts',(-0.181114728188128,0.0733390430353466,
2.31812210908574));
#24454=CARTESIAN_POINT('Ctrl Pts',(-0.185837491075197,0.0616759249854399,
2.31883726270271));
#24455=CARTESIAN_POINT('Ctrl Pts',(-0.189425605345656,0.049563234804578,
2.31955241631969));
#24456=CARTESIAN_POINT('Ctrl Pts',(-0.191817193500518,0.0372468022464341,
2.32026756993666));
#24457=CARTESIAN_POINT('Ctrl Pts',(-0.19420878165538,0.0249303696882902,
2.32098272355363));
#24458=CARTESIAN_POINT('Ctrl Pts',(-0.19540378473205,0.0124112548288328,
2.32169787717061));
#24459=CARTESIAN_POINT('Ctrl Pts',(-0.19539999095818,-5.94436136248776E-5,
2.32241303078758));
#24460=CARTESIAN_POINT('',(-0.195373072924931,0.000178337447204722,2.39241301734378));
#24461=CARTESIAN_POINT('Ctrl Pts',(-0.195697752751996,-5.95341972371984E-5,
2.32241303078758));
#24462=CARTESIAN_POINT('Ctrl Pts',(-0.195710914677712,-0.00333097164176583,
2.32260035128879));
#24463=CARTESIAN_POINT('Ctrl Pts',(-0.194154341293038,-0.0712935330070171,
2.32649257608402));
#24464=CARTESIAN_POINT('Ctrl Pts',(-0.115302964228223,-0.200121413881382,
2.33408970517291));
#24465=CARTESIAN_POINT('Ctrl Pts',(0.105622948018936,-0.205392642805891,
2.34520441805482));
#24466=CARTESIAN_POINT('Ctrl Pts',(0.229835338308407,-0.0226457751156926,
2.35631913093652));
#24467=CARTESIAN_POINT('Ctrl Pts',(0.143684619655393,0.180848806972626,
2.36743384381834));
#24468=CARTESIAN_POINT('Ctrl Pts',(-0.0740780534647926,0.218753590559664,
2.3785485567001));
#24469=CARTESIAN_POINT('Ctrl Pts',(-0.186300605867557,0.0971745928305562,
2.38687494787525));
#24470=CARTESIAN_POINT('Ctrl Pts',(-0.195509800817246,0.0162592722445891,
2.39149643475648));
#24471=CARTESIAN_POINT('Ctrl Pts',(-0.195373072924931,0.000178337447204722,
2.39241301734378));
#24472=CARTESIAN_POINT('',(-0.151810369570276,-0.123111383537865,2.39999996557186));
#24473=CARTESIAN_POINT('Ctrl Pts',(-0.195399918810391,0.000178126057700033,
2.39241303078758));
#24474=CARTESIAN_POINT('Ctrl Pts',(-0.195410720541781,-0.0116711084889103,
2.39308832752325));
#24475=CARTESIAN_POINT('Ctrl Pts',(-0.194339373404496,-0.0235537033023695,
2.39376362425893));
#24476=CARTESIAN_POINT('Ctrl Pts',(-0.192194137897985,-0.0352501540088856,
2.3944389209946));
#24477=CARTESIAN_POINT('Ctrl Pts',(-0.190050922889026,-0.0469355883724696,
2.39511358169969));
#24478=CARTESIAN_POINT('Ctrl Pts',(-0.186835972891341,-0.0584343092701696,
2.39578824240477));
#24479=CARTESIAN_POINT('Ctrl Pts',(-0.182609043029114,-0.0695348646650817,
2.39646290310986));
#24480=CARTESIAN_POINT('Ctrl Pts',(-0.178373466969652,-0.0806581262780969,
2.39713894383536));
#24481=CARTESIAN_POINT('Ctrl Pts',(-0.173122133999952,-0.0913807328435216,
2.39781498456087));
#24482=CARTESIAN_POINT('Ctrl Pts',(-0.166963196588413,-0.101510841711508,
2.39849102528638));
#24483=CARTESIAN_POINT('Ctrl Pts',(-0.162380916207106,-0.109047693610556,
2.39899400298309));
#24484=CARTESIAN_POINT('Ctrl Pts',(-0.157297305620373,-0.11625696509648,
2.3994969806798));
#24485=CARTESIAN_POINT('Ctrl Pts',(-0.151771747278466,-0.123071104358584,
2.39999995837652));
#24486=CARTESIAN_POINT('',(-0.190155688860645,0.0449663651403318,2.4));
#24487=CARTESIAN_POINT('Origin',(0.,0.,2.4));
#24488=CARTESIAN_POINT('',(-0.195465158332937,-7.38788922412424E-5,2.33258696921242));
#24489=CARTESIAN_POINT('Ctrl Pts',(-0.190155688860645,0.0449663651403318,
2.4));
#24490=CARTESIAN_POINT('Ctrl Pts',(-0.175202059751608,0.108202911730688,
2.39629509570607));
#24491=CARTESIAN_POINT('Ctrl Pts',(-0.0775128162224373,0.217492107202676,
2.38888528711823));
#24492=CARTESIAN_POINT('Ctrl Pts',(0.141144990674223,0.183006228893533,
2.37777057423644));
#24493=CARTESIAN_POINT('Ctrl Pts',(0.230080867601978,-0.0193251643494339,
2.36665586135468));
#24494=CARTESIAN_POINT('Ctrl Pts',(0.108644616799767,-0.203806378129402,
2.35554114847289));
#24495=CARTESIAN_POINT('Ctrl Pts',(-0.112383257382277,-0.20179584998626,
2.34442643559113));
#24496=CARTESIAN_POINT('Ctrl Pts',(-0.193667652393877,-0.0732104317508976,
2.3367750425043));
#24497=CARTESIAN_POINT('Ctrl Pts',(-0.195702355486801,-0.0042939273868865,
2.3328285537114));
#24498=CARTESIAN_POINT('Ctrl Pts',(-0.195681353759257,-7.39606064390219E-5,
2.33258696921242));
#24499=CARTESIAN_POINT('',(-0.195399955977075,-0.000131164618793305,2.26258696921762));
#24500=CARTESIAN_POINT('Ctrl Pts',(-0.195399986042856,-7.38542594287352E-5,
2.33258696921242));
#24501=CARTESIAN_POINT('Ctrl Pts',(-0.195404534495383,0.011960218888881,
2.33189704962616));
#24502=CARTESIAN_POINT('Ctrl Pts',(-0.194293060880465,0.024039361424141,
2.3312071300399));
#24503=CARTESIAN_POINT('Ctrl Pts',(-0.192066782359531,0.0359376002823843,
2.33051721045363));
#24504=CARTESIAN_POINT('Ctrl Pts',(-0.189829434182476,0.047895000387246,
2.32982386040146));
#24505=CARTESIAN_POINT('Ctrl Pts',(-0.186466168721113,0.0596687783725439,
2.32913051034929));
#24506=CARTESIAN_POINT('Ctrl Pts',(-0.182031165904908,0.0710338978185751,
2.32843716029712));
#24507=CARTESIAN_POINT('Ctrl Pts',(-0.177626922118394,0.0823201943053074,
2.32774861898481));
#24508=CARTESIAN_POINT('Ctrl Pts',(-0.17216610444674,0.0932026472019881,
2.3270600776725));
#24509=CARTESIAN_POINT('Ctrl Pts',(-0.165751051963725,0.103478252656868,
2.32637153636019));
#24510=CARTESIAN_POINT('Ctrl Pts',(-0.159268795847343,0.11386150462336,
2.32567578193809));
#24511=CARTESIAN_POINT('Ctrl Pts',(-0.151812660159517,0.123624316111712,
2.32498002751599));
#24512=CARTESIAN_POINT('Ctrl Pts',(-0.143532878472785,0.132587604237036,
2.32428427309388));
#24513=CARTESIAN_POINT('Ctrl Pts',(-0.135253096786052,0.14155089236236,
2.32358851867178));
#24514=CARTESIAN_POINT('Ctrl Pts',(-0.126150395337392,0.149714068944035,
2.32289276424968));
#24515=CARTESIAN_POINT('Ctrl Pts',(-0.116410373116421,0.156938793900347,
2.32219700982757));
#24516=CARTESIAN_POINT('Ctrl Pts',(-0.10666267899715,0.16416920953722,2.32150070738237));
#24517=CARTESIAN_POINT('Ctrl Pts',(-0.0962041275241309,0.170513681286887,
2.32080440493716));
#24518=CARTESIAN_POINT('Ctrl Pts',(-0.0852200357042007,0.175837156240013,
2.32010810249196));
#24519=CARTESIAN_POINT('Ctrl Pts',(-0.0742590544158008,0.181149430600703,
2.31941326506725));
#24520=CARTESIAN_POINT('Ctrl Pts',(-0.0627754752192831,0.185444526224622,
2.31871842764254));
#24521=CARTESIAN_POINT('Ctrl Pts',(-0.0509809272286206,0.188632195181284,
2.31802359021783));
#24522=CARTESIAN_POINT('Ctrl Pts',(-0.0391880861055844,0.191819402829132,
2.31732885334767));
#24523=CARTESIAN_POINT('Ctrl Pts',(-0.0270851978963677,0.193899229028121,
2.31663411647752));
#24524=CARTESIAN_POINT('Ctrl Pts',(-0.0148995281149728,0.194831116770271,
2.31593937960736));
#24525=CARTESIAN_POINT('Ctrl Pts',(-0.00271461230998617,0.195762946852778,
2.31524468572337));
#24526=CARTESIAN_POINT('Ctrl Pts',(0.00955219924219646,0.19554693927595,
2.31454999183938));
#24527=CARTESIAN_POINT('Ctrl Pts',(0.0216708253165105,0.194194581103854,
2.31385529795539));
#24528=CARTESIAN_POINT('Ctrl Pts',(0.033817392293072,0.192839104912664,
2.31315900237383));
#24529=CARTESIAN_POINT('Ctrl Pts',(0.0458142287108722,0.190342209310646,
2.31246270679227));
#24530=CARTESIAN_POINT('Ctrl Pts',(0.0574399014123331,0.186766746841458,
2.31176641121071));
#24531=CARTESIAN_POINT('Ctrl Pts',(0.0612473306827593,0.185595776282586,
2.3115383731224));
#24532=CARTESIAN_POINT('Ctrl Pts',(0.0650150862563916,0.184309516170192,
2.3113103350341));
#24533=CARTESIAN_POINT('Ctrl Pts',(0.0687358611679654,0.182911293772414,
2.31108229694579));
#24534=CARTESIAN_POINT('Ctrl Pts',(0.0801000235662201,0.178640778416109,
2.31038581249562));
#24535=CARTESIAN_POINT('Ctrl Pts',(0.0911048671551245,0.173292037415153,
2.30968932804546));
#24536=CARTESIAN_POINT('Ctrl Pts',(0.101536364443804,0.166947676520325,
2.30899284359529));
#24537=CARTESIAN_POINT('Ctrl Pts',(0.111945975994884,0.160616626372165,
2.30829782039996));
#24538=CARTESIAN_POINT('Ctrl Pts',(0.121783849507209,0.153294489116926,
2.30760279720464));
#24539=CARTESIAN_POINT('Ctrl Pts',(0.130859357472746,0.145110263461342,
2.30690777400931));
#24540=CARTESIAN_POINT('Ctrl Pts',(0.139933587031676,0.136927190663337,
2.30621284871729));
#24541=CARTESIAN_POINT('Ctrl Pts',(0.148244984148803,0.127882821814845,
2.30551792342527));
#24542=CARTESIAN_POINT('Ctrl Pts',(0.155636206910171,0.118146227610595,
2.30482299813326));
#24543=CARTESIAN_POINT('Ctrl Pts',(0.163026990914559,0.108410211389013,
2.30412811409332));
#24544=CARTESIAN_POINT('Ctrl Pts',(0.169497200848164,0.0979827649999601,
2.30343323005338));
#24545=CARTESIAN_POINT('Ctrl Pts',(0.174931702176024,0.0870635375676792,
2.30273834601344));
#24546=CARTESIAN_POINT('Ctrl Pts',(0.180378722645977,0.0761191561513398,
2.30204186120988));
#24547=CARTESIAN_POINT('Ctrl Pts',(0.184784939522097,0.0646815443369111,
2.30134537640632));
#24548=CARTESIAN_POINT('Ctrl Pts',(0.188083067286571,0.052970933539775,
2.30064889160276));
#24549=CARTESIAN_POINT('Ctrl Pts',(0.189158486447766,0.0491524595024168,
2.30042178908985));
#24550=CARTESIAN_POINT('Ctrl Pts',(0.190116494591209,0.0453050584863319,
2.30019468657693));
#24551=CARTESIAN_POINT('Ctrl Pts',(0.190955938265016,0.0414365737160732,
2.29996758406401));
#24552=CARTESIAN_POINT('Ctrl Pts',(0.193530279104264,0.0295730042583024,
2.29927112366776));
#24553=CARTESIAN_POINT('Ctrl Pts',(0.195003921748024,0.0174266432872976,
2.2985746632715));
#24554=CARTESIAN_POINT('Ctrl Pts',(0.19533020681641,0.00522209776415546,
2.29787820287524));
#24555=CARTESIAN_POINT('Ctrl Pts',(0.195655807402106,-0.00695684499329843,
2.2971832035176));
#24556=CARTESIAN_POINT('Ctrl Pts',(0.194838730104721,-0.0191928654653601,
2.29648820415997));
#24557=CARTESIAN_POINT('Ctrl Pts',(0.192883984062965,-0.0312558585228103,
2.29579320480233));
#24558=CARTESIAN_POINT('Ctrl Pts',(0.190929511434308,-0.0433171643123228,
2.29509830265523));
#24559=CARTESIAN_POINT('Ctrl Pts',(0.187837780341885,-0.0552046203101992,
2.29440340050814));
#24560=CARTESIAN_POINT('Ctrl Pts',(0.183665518511083,-0.0666943574079165,
2.29370849836105));
#24561=CARTESIAN_POINT('Ctrl Pts',(0.179493502089677,-0.078183418687684,
2.29301363708759));
#24562=CARTESIAN_POINT('Ctrl Pts',(0.174241405162099,-0.0892739935231876,
2.29231877581414));
#24563=CARTESIAN_POINT('Ctrl Pts',(0.168014535251855,-0.0997610943409465,
2.29162391454068));
#24564=CARTESIAN_POINT('Ctrl Pts',(0.161773311531892,-0.110272369399023,
2.29092745151439));
#24565=CARTESIAN_POINT('Ctrl Pts',(0.154553331620299,-0.120176673950064,
2.29023098848811));
#24566=CARTESIAN_POINT('Ctrl Pts',(0.146503142947681,-0.129298063042148,
2.28953452546182));
#24567=CARTESIAN_POINT('Ctrl Pts',(0.143876803212438,-0.132273877347549,
2.28930730736863));
#24568=CARTESIAN_POINT('Ctrl Pts',(0.141162400596626,-0.135166646046722,
2.28908008927543));
#24569=CARTESIAN_POINT('Ctrl Pts',(0.138365909076259,-0.13797113903096,
2.28885287118223));
#24570=CARTESIAN_POINT('Ctrl Pts',(0.129794658348867,-0.146566914257183,
2.28815644738391));
#24571=CARTESIAN_POINT('Ctrl Pts',(0.120388986389258,-0.154391364591959,
2.28746002358559));
#24572=CARTESIAN_POINT('Ctrl Pts',(0.110312271898818,-0.161283485417824,
2.28676359978727));
#24573=CARTESIAN_POINT('Ctrl Pts',(0.10025671438214,-0.16816113561245,2.28606863819373));
#24574=CARTESIAN_POINT('Ctrl Pts',(0.0895335842429653,-0.174109790576425,
2.28537367660018));
#24575=CARTESIAN_POINT('Ctrl Pts',(0.0783389032088239,-0.179008871970186,
2.28467871500663));
#24576=CARTESIAN_POINT('Ctrl Pts',(0.0671458062673354,-0.183907260124111,
2.28398385175296));
#24577=CARTESIAN_POINT('Ctrl Pts',(0.0554820734628567,-0.187755976720076,
2.2832889884993));
#24578=CARTESIAN_POINT('Ctrl Pts',(0.0435665370192763,-0.19048127690707,
2.28259412524562));
#24579=CARTESIAN_POINT('Ctrl Pts',(0.0316517134033498,-0.193206414057399,
2.28189930356102));
#24580=CARTESIAN_POINT('Ctrl Pts',(0.0194859757854752,-0.19480809900496,
2.28120448187642));
#24581=CARTESIAN_POINT('Ctrl Pts',(0.0072986392893096,-0.195263641942182,
2.28050966019182));
#24582=CARTESIAN_POINT('Ctrl Pts',(-0.00491678697174241,-0.195720234829407,
2.27981323705987));
#24583=CARTESIAN_POINT('Ctrl Pts',(-0.0171530344283273,-0.195025444127289,
2.27911681392791));
#24584=CARTESIAN_POINT('Ctrl Pts',(-0.0291817392893931,-0.19320865946444,
2.27842039079596));
#24585=CARTESIAN_POINT('Ctrl Pts',(-0.0331096067779737,-0.192615404455411,
2.27819297996413));
#24586=CARTESIAN_POINT('Ctrl Pts',(-0.0370154202602093,-0.191902920682419,
2.2779655691323));
#24587=CARTESIAN_POINT('Ctrl Pts',(-0.0408915258148231,-0.191073397197348,
2.27773815830047));
#24588=CARTESIAN_POINT('Ctrl Pts',(-0.0527621951405048,-0.188532960965564,
2.27704170699188));
#24589=CARTESIAN_POINT('Ctrl Pts',(-0.0644372291389193,-0.184873082766647,
2.27634525568329));
#24590=CARTESIAN_POINT('Ctrl Pts',(-0.0756927429004167,-0.180143744471495,
2.2756488043747));
#24591=CARTESIAN_POINT('Ctrl Pts',(-0.0869246354015522,-0.175424331350225,
2.274953814666));
#24592=CARTESIAN_POINT('Ctrl Pts',(-0.0977379270613595,-0.169640179971889,
2.27425882495731));
#24593=CARTESIAN_POINT('Ctrl Pts',(-0.107925001512165,-0.162890619891383,
2.27356383524861));
#24594=CARTESIAN_POINT('Ctrl Pts',(-0.118110641138565,-0.156142010469831,
2.27286894342751));
#24595=CARTESIAN_POINT('Ctrl Pts',(-0.127669484326053,-0.148428706780985,
2.2721740516064));
#24596=CARTESIAN_POINT('Ctrl Pts',(-0.13642089721442,-0.139894598906508,
2.2714791597853));
#24597=CARTESIAN_POINT('Ctrl Pts',(-0.145171790261192,-0.131360997965518,
2.27078430924138));
#24598=CARTESIAN_POINT('Ctrl Pts',(-0.15311473991902,-0.122007320184588,
2.27008945869746));
#24599=CARTESIAN_POINT('Ctrl Pts',(-0.160106325535196,-0.112013947897652,
2.26939460815353));
#24600=CARTESIAN_POINT('Ctrl Pts',(-0.167114023916195,-0.10199754494696,
2.26869815626136));
#24601=CARTESIAN_POINT('Ctrl Pts',(-0.173165532670347,-0.0913392586629627,
2.26800170436919));
#24602=CARTESIAN_POINT('Ctrl Pts',(-0.178161704725289,-0.0802469125224081,
2.26730525247702));
#24603=CARTESIAN_POINT('Ctrl Pts',(-0.179792075949294,-0.0766272129293224,
2.26707798345757));
#24604=CARTESIAN_POINT('Ctrl Pts',(-0.181310451134443,-0.0729614488210793,
2.26685071443813));
#24605=CARTESIAN_POINT('Ctrl Pts',(-0.1827145232587,-0.0692572233802802,
2.26662344541869));
#24606=CARTESIAN_POINT('Ctrl Pts',(-0.187610819374939,-0.0563398067275817,
2.26583091033589));
#24607=CARTESIAN_POINT('Ctrl Pts',(-0.19114228617701,-0.0428779645722903,
2.2650383752531));
#24608=CARTESIAN_POINT('Ctrl Pts',(-0.1932133790389,-0.029150474445028,
2.2642458401703));
#24609=CARTESIAN_POINT('Ctrl Pts',(-0.194658394266399,-0.0195727135274749,
2.26369288318608));
#24610=CARTESIAN_POINT('Ctrl Pts',(-0.195393421250955,-0.00986614656641785,
2.26313992620185));
#24611=CARTESIAN_POINT('Ctrl Pts',(-0.195399955977075,-0.000131164618793936,
2.26258696921762));
#24612=CARTESIAN_POINT('',(-0.195399944228081,0.000147633542831837,2.19258696921242));
#24613=CARTESIAN_POINT('Ctrl Pts',(-0.195399955977136,-0.000131164527281134,
2.26258696921242));
#24614=CARTESIAN_POINT('Ctrl Pts',(-0.195408209090474,0.0121637601469669,
2.26188860484918));
#24615=CARTESIAN_POINT('Ctrl Pts',(-0.194251688243831,0.0244657020173597,
2.26119024048593));
#24616=CARTESIAN_POINT('Ctrl Pts',(-0.191952657528546,0.0365422668663097,
2.26049187612269));
#24617=CARTESIAN_POINT('Ctrl Pts',(-0.189653287505934,0.0486206140607155,
2.25979340868985));
#24618=CARTESIAN_POINT('Ctrl Pts',(-0.18621126803752,0.06047267665518,2.25909494125702));
#24619=CARTESIAN_POINT('Ctrl Pts',(-0.181699758673365,0.0718773795991548,
2.25839647382419));
#24620=CARTESIAN_POINT('Ctrl Pts',(-0.177176507344299,0.0833117652082813,
2.25769618851193));
#24621=CARTESIAN_POINT('Ctrl Pts',(-0.171578588528802,0.0942956888981793,
2.25699590319966));
#24622=CARTESIAN_POINT('Ctrl Pts',(-0.165026426292338,0.104630008244192,
2.2562956178874));
#24623=CARTESIAN_POINT('Ctrl Pts',(-0.162572283489123,0.108500775562497,
2.25603332277057));
#24624=CARTESIAN_POINT('Ctrl Pts',(-0.159984704674147,0.112280704945645,
2.25577102765374));
#24625=CARTESIAN_POINT('Ctrl Pts',(-0.157271491326974,0.115960501964201,
2.25550873253691));
#24626=CARTESIAN_POINT('Ctrl Pts',(-0.150067415690632,0.12573103330693,
2.25481229122586));
#24627=CARTESIAN_POINT('Ctrl Pts',(-0.141923859667923,0.134862252170482,
2.2541158499148));
#24628=CARTESIAN_POINT('Ctrl Pts',(-0.132978573695544,0.143170733524344,
2.25341940860375));
#24629=CARTESIAN_POINT('Ctrl Pts',(-0.124052063191857,0.151461776013532,
2.25272442906955));
#24630=CARTESIAN_POINT('Ctrl Pts',(-0.114327747182382,0.158932863893428,
2.25202944953536));
#24631=CARTESIAN_POINT('Ctrl Pts',(-0.103981643917688,0.165435720834937,
2.25133447000116));
#24632=CARTESIAN_POINT('Ctrl Pts',(-0.0936369994124027,0.171937660899482,
2.25063958845632));
#24633=CARTESIAN_POINT('Ctrl Pts',(-0.0826714574396618,0.177471136713466,
2.24994470691147));
#24634=CARTESIAN_POINT('Ctrl Pts',(-0.0712905288926859,0.18193081237163,
2.24924982536663));
#24635=CARTESIAN_POINT('Ctrl Pts',(-0.0599102775329535,0.186390222670473,
2.24855498516858));
#24636=CARTESIAN_POINT('Ctrl Pts',(-0.0481155138222969,0.189775665035088,
2.24786014497053));
#24637=CARTESIAN_POINT('Ctrl Pts',(-0.0361296751148883,0.192030743830493,
2.24716530477248));
#24638=CARTESIAN_POINT('Ctrl Pts',(-0.0241162119893341,0.194291020029361,
2.24646886313821));
#24639=CARTESIAN_POINT('Ctrl Pts',(-0.0119116668126163,0.195415633644518,
2.24577242150395));
#24640=CARTESIAN_POINT('Ctrl Pts',(0.000253752594602635,0.195399835234375,
2.24507597986968));
#24641=CARTESIAN_POINT('Ctrl Pts',(0.00422457207697346,0.195394678598776,
2.24484865979816));
#24642=CARTESIAN_POINT('Ctrl Pts',(0.00819123791521547,0.19526843924573,
2.24462133972665));
#24643=CARTESIAN_POINT('Ctrl Pts',(0.0121458661306949,0.195022147295981,
2.24439401965513));
#24644=CARTESIAN_POINT('Ctrl Pts',(0.0242617453322618,0.194267577372112,
2.24369757428113));
#24645=CARTESIAN_POINT('Ctrl Pts',(0.0363499239593466,0.192376957475244,
2.24300112890712));
#24646=CARTESIAN_POINT('Ctrl Pts',(0.0481815872380622,0.189366561597398,
2.24230468353311));
#24647=CARTESIAN_POINT('Ctrl Pts',(0.0599884185091095,0.18636248386534,
2.24160969984175));
#24648=CARTESIAN_POINT('Ctrl Pts',(0.0715389444731538,0.182243436301947,
2.24091471615039));
#24649=CARTESIAN_POINT('Ctrl Pts',(0.0826131312729343,0.177076905725396,
2.24021973245903));
#24650=CARTESIAN_POINT('Ctrl Pts',(0.0936857578434941,0.171911103055293,
2.23952484668311));
#24651=CARTESIAN_POINT('Ctrl Pts',(0.10428136662625,0.165698438236002,2.23882996090718));
#24652=CARTESIAN_POINT('Ctrl Pts',(0.114200009660928,0.158554463177307,
2.23813507513126));
#24653=CARTESIAN_POINT('Ctrl Pts',(0.124118063195132,0.151410912710632,
2.23744023065489));
#24654=CARTESIAN_POINT('Ctrl Pts',(0.133358535866462,0.143336695417527,
2.23674538617851));
#24655=CARTESIAN_POINT('Ctrl Pts',(0.141752878559905,0.134488963933777,
2.23605054170214));
#24656=CARTESIAN_POINT('Ctrl Pts',(0.150166567929309,0.125620840836263,
2.2353540957983));
#24657=CARTESIAN_POINT('Ctrl Pts',(0.157729678906863,0.115976324109947,
2.23465764989447));
#24658=CARTESIAN_POINT('Ctrl Pts',(0.164313384223064,0.105746261234919,
2.23396120399063));
#24659=CARTESIAN_POINT('Ctrl Pts',(0.166462108342548,0.102407475279642,
2.23373390491821));
#24660=CARTESIAN_POINT('Ctrl Pts',(0.168506865290859,0.0990065310496776,
2.23350660584578));
#24661=CARTESIAN_POINT('Ctrl Pts',(0.170444246243508,0.0955506092208851,
2.23327930677336));
#24662=CARTESIAN_POINT('Ctrl Pts',(0.176380380824278,0.0849616659114767,
2.23258286249266));
#24663=CARTESIAN_POINT('Ctrl Pts',(0.181346987238524,0.0737799464835854,
2.23188641821197));
#24664=CARTESIAN_POINT('Ctrl Pts',(0.185233658322928,0.0622065255765414,
2.23118997393128));
#24665=CARTESIAN_POINT('Ctrl Pts',(0.189112172081714,0.0506573949067717,
2.23049499134432));
#24666=CARTESIAN_POINT('Ctrl Pts',(0.191914902566601,0.0387189925502746,
2.22980000875736));
#24667=CARTESIAN_POINT('Ctrl Pts',(0.193579233316941,0.0266127869345781,
2.22910502617041));
#24668=CARTESIAN_POINT('Ctrl Pts',(0.195243329583537,0.0145082869344427,
2.22841014149795));
#24669=CARTESIAN_POINT('Ctrl Pts',(0.195769179760362,0.00223689053688691,
2.2277152568255));
#24670=CARTESIAN_POINT('Ctrl Pts',(0.195145443797342,-0.00997074546552755,
2.22702037215304));
#24671=CARTESIAN_POINT('Ctrl Pts',(0.194521744905773,-0.0221776559128915,
2.22632552878073));
#24672=CARTESIAN_POINT('Ctrl Pts',(0.192748666911091,-0.0343199402350793,
2.22563068540842));
#24673=CARTESIAN_POINT('Ctrl Pts',(0.189866849548342,-0.046170763937663,
2.2249358420361));
#24674=CARTESIAN_POINT('Ctrl Pts',(0.186978390288739,-0.0580489009424982,
2.22423939721671));
#24675=CARTESIAN_POINT('Ctrl Pts',(0.182976360035834,-0.0696334011972714,
2.22354295239731));
#24676=CARTESIAN_POINT('Ctrl Pts',(0.177951249129385,-0.080712532690355,
2.22284650757792));
#24677=CARTESIAN_POINT('Ctrl Pts',(0.176311161354537,-0.0843285221592478,
2.2226192030158));
#24678=CARTESIAN_POINT('Ctrl Pts',(0.174562464071665,-0.0878908626194418,
2.22239189845369));
#24679=CARTESIAN_POINT('Ctrl Pts',(0.172709342296327,-0.0913927955780434,
2.22216459389158));
#24680=CARTESIAN_POINT('Ctrl Pts',(0.167031519007738,-0.102122450138284,
2.22146815011032));
#24681=CARTESIAN_POINT('Ctrl Pts',(0.160329895247707,-0.112358954932852,
2.22077170632906));
#24682=CARTESIAN_POINT('Ctrl Pts',(0.152713542682258,-0.121900508126234,
2.2200752625478));
#24683=CARTESIAN_POINT('Ctrl Pts',(0.145113175506104,-0.131422035271589,
2.21938028047998));
#24684=CARTESIAN_POINT('Ctrl Pts',(0.136602372643736,-0.140250781795649,
2.21868529841216));
#24685=CARTESIAN_POINT('Ctrl Pts',(0.127333256389287,-0.148214040553856,
2.21799031634435));
#24686=CARTESIAN_POINT('Ctrl Pts',(0.11806544631989,-0.1561761771458,2.217295432212));
#24687=CARTESIAN_POINT('Ctrl Pts',(0.108040168168097,-0.163272463345915,
2.21660054807964));
#24688=CARTESIAN_POINT('Ctrl Pts',(0.0974450702572235,-0.169368291845212,
2.21590566394729));
#24689=CARTESIAN_POINT('Ctrl Pts',(0.0868506022553824,-0.175463757929978,
2.2152108211278));
#24690=CARTESIAN_POINT('Ctrl Pts',(0.0756871541742055,-0.180558470837561,
2.2145159783083));
#24691=CARTESIAN_POINT('Ctrl Pts',(0.0641673502122027,-0.18456356944626,
2.21382113548881));
#24692=CARTESIAN_POINT('Ctrl Pts',(0.0526209959931669,-0.188577898802102,
2.213124691231));
#24693=CARTESIAN_POINT('Ctrl Pts',(0.040717494220899,-0.191497374290718,
2.21242824697319));
#24694=CARTESIAN_POINT('Ctrl Pts',(0.0286838127307998,-0.193283209015228,
2.21173180271538));
#24695=CARTESIAN_POINT('Ctrl Pts',(0.024756229384345,-0.193866074261352,
2.21150449548019));
#24696=CARTESIAN_POINT('Ctrl Pts',(0.0208148254210547,-0.194328590304711,
2.211277188245));
#24697=CARTESIAN_POINT('Ctrl Pts',(0.0168675490533827,-0.194670608436229,
2.21104988100981));
#24698=CARTESIAN_POINT('Ctrl Pts',(0.00477352840614477,-0.195718514374155,
2.21035343664169));
#24699=CARTESIAN_POINT('Ctrl Pts',(-0.00746132769261978,-0.195638797031868,
2.20965699227356));
#24700=CARTESIAN_POINT('Ctrl Pts',(-0.0196083179009098,-0.194413666878378,
2.20896054790544));
#24701=CARTESIAN_POINT('Ctrl Pts',(-0.0317298139764309,-0.193191108031051,
2.20826556523646));
#24702=CARTESIAN_POINT('Ctrl Pts',(-0.0437629401733625,-0.190827920682833,
2.20757058256749));
#24703=CARTESIAN_POINT('Ctrl Pts',(-0.0554800953712026,-0.187358263809212,
2.20687559989851));
#24704=CARTESIAN_POINT('Ctrl Pts',(-0.0671955996098305,-0.183889095813811,
2.2061807151533));
#24705=CARTESIAN_POINT('Ctrl Pts',(-0.0785943697721386,-0.17931397184433,
2.2054858304081));
#24706=CARTESIAN_POINT('Ctrl Pts',(-0.0894615514669536,-0.173717560451227,
2.20479094566289));
#24707=CARTESIAN_POINT('Ctrl Pts',(-0.100328087193093,-0.168121481720864,
2.20409610222313));
#24708=CARTESIAN_POINT('Ctrl Pts',(-0.110662330845803,-0.161504660815807,
2.20340125878337));
#24709=CARTESIAN_POINT('Ctrl Pts',(-0.120274320293943,-0.153997558025541,
2.20270641534361));
#24710=CARTESIAN_POINT('Ctrl Pts',(-0.129908462939838,-0.146473153267398,
2.20200997046596));
#24711=CARTESIAN_POINT('Ctrl Pts',(-0.138816378390958,-0.138054960174133,
2.20131352558831));
#24712=CARTESIAN_POINT('Ctrl Pts',(-0.146842398771829,-0.128912644542478,
2.20061708071065));
#24713=CARTESIAN_POINT('Ctrl Pts',(-0.14946191419064,-0.125928795059882,
2.20038977651645));
#24714=CARTESIAN_POINT('Ctrl Pts',(-0.151987809105506,-0.122868073272702,
2.20016247232224));
#24715=CARTESIAN_POINT('Ctrl Pts',(-0.154415648637008,-0.119737076363222,
2.19993516812803));
#24716=CARTESIAN_POINT('Ctrl Pts',(-0.161858322763002,-0.110138835052628,
2.19923835475837));
#24717=CARTESIAN_POINT('Ctrl Pts',(-0.168429868223669,-0.0998089199701452,
2.1985415413887));
#24718=CARTESIAN_POINT('Ctrl Pts',(-0.17399049677386,-0.088929562196074,
2.19784472801903));
#24719=CARTESIAN_POINT('Ctrl Pts',(-0.179538968532555,-0.0780739891583648,
2.19714943804097));
#24720=CARTESIAN_POINT('Ctrl Pts',(-0.18408044524445,-0.0666720904675441,
2.19645414806291));
#24721=CARTESIAN_POINT('Ctrl Pts',(-0.187519231564517,-0.0549335761939177,
2.19575885808484));
#24722=CARTESIAN_POINT('Ctrl Pts',(-0.190956001269814,-0.0432019457621682,
2.19506397584716));
#24723=CARTESIAN_POINT('Ctrl Pts',(-0.193291077571079,-0.0311349154882965,
2.19436909360947));
#24724=CARTESIAN_POINT('Ctrl Pts',(-0.194478068348997,-0.0189589274813421,
2.19367421137179));
#24725=CARTESIAN_POINT('Ctrl Pts',(-0.19509714035216,-0.0126085720900598,
2.19331179731867));
#24726=CARTESIAN_POINT('Ctrl Pts',(-0.195404761902858,-0.0062287858313775,
2.19294938326554));
#24727=CARTESIAN_POINT('Ctrl Pts',(-0.195399944228081,0.000147633542831837,
2.19258696921242));
#24728=CARTESIAN_POINT('',(-0.195424404543861,4.85723203800092E-5,2.12258697393042));
#24729=CARTESIAN_POINT('Ctrl Pts',(-0.19520943667287,0.00014891838008839,
2.19258688792652));
#24730=CARTESIAN_POINT('Ctrl Pts',(-0.195364193218957,0.02221674989384,
2.19133141036643));
#24731=CARTESIAN_POINT('Ctrl Pts',(-0.181722525948205,0.109220630806636,
2.1863710285124));
#24732=CARTESIAN_POINT('Ctrl Pts',(-0.0537908007947809,0.224607784190422,
2.17770574236448));
#24733=CARTESIAN_POINT('Ctrl Pts',(0.159546357810677,0.166994209782184,
2.1665910294827));
#24734=CARTESIAN_POINT('Ctrl Pts',(0.226826697041784,-0.0434943260391223,
2.15547631660093));
#24735=CARTESIAN_POINT('Ctrl Pts',(0.0864583809916583,-0.214165952291804,
2.14436160371914));
#24736=CARTESIAN_POINT('Ctrl Pts',(-0.130063871440271,-0.189125514256134,
2.13339850761495));
#24737=CARTESIAN_POINT('Ctrl Pts',(-0.195497536487265,-0.0620019008509531,
2.12614031580466));
#24738=CARTESIAN_POINT('Ctrl Pts',(-0.195705648609306,4.76931131101887E-5,
2.1225870282883));
#24739=CARTESIAN_POINT('',(-0.195399918942337,-0.000177981257815075,2.05258697083887));
#24740=CARTESIAN_POINT('Ctrl Pts',(-0.195399993943988,4.86486312413049E-5,
2.12258696921242));
#24741=CARTESIAN_POINT('Ctrl Pts',(-0.195399335882766,0.00269178895453019,
2.12243537212681));
#24742=CARTESIAN_POINT('Ctrl Pts',(-0.19534505029102,0.00533419421920633,
2.12228377504121));
#24743=CARTESIAN_POINT('Ctrl Pts',(-0.195237212099404,0.00797439725949685,
2.1221321779556));
#24744=CARTESIAN_POINT('Ctrl Pts',(-0.194741798352652,0.0201036147544585,
2.1214357337826));
#24745=CARTESIAN_POINT('Ctrl Pts',(-0.193110006278211,0.0322294230105758,
2.12073928960961));
#24746=CARTESIAN_POINT('Ctrl Pts',(-0.190353214459758,0.044122712346788,
2.12004284543661));
#24747=CARTESIAN_POINT('Ctrl Pts',(-0.187602208618729,0.0559910399491707,
2.11934786296639));
#24748=CARTESIAN_POINT('Ctrl Pts',(-0.183731012630555,0.0676269558939791,
2.11865288049617));
#24749=CARTESIAN_POINT('Ctrl Pts',(-0.178802393919666,0.0788090345620136,
2.11795789802595));
#24750=CARTESIAN_POINT('Ctrl Pts',(-0.173874469672371,0.089989537627024,
2.11726301348176));
#24751=CARTESIAN_POINT('Ctrl Pts',(-0.167889728949696,0.100715511684815,
2.11656812893756));
#24752=CARTESIAN_POINT('Ctrl Pts',(-0.160959422670306,0.110784584909823,
2.11587324439336));
#24753=CARTESIAN_POINT('Ctrl Pts',(-0.154029528358444,0.120853059585353,
2.11517840115613));
#24754=CARTESIAN_POINT('Ctrl Pts',(-0.146154698628647,0.130264004710846,
2.11448355791889));
#24755=CARTESIAN_POINT('Ctrl Pts',(-0.137488446820663,0.138845550850006,
2.11378871468165));
#24756=CARTESIAN_POINT('Ctrl Pts',(-0.128802221475821,0.147446875300703,
2.11309227000502));
#24757=CARTESIAN_POINT('Ctrl Pts',(-0.119321600162659,0.155214414894748,
2.11239582532839));
#24758=CARTESIAN_POINT('Ctrl Pts',(-0.109234632459035,0.162015292708866,
2.11169938065176));
#24759=CARTESIAN_POINT('Ctrl Pts',(-0.105942454036197,0.164234959099585,
2.11147207545912));
#24760=CARTESIAN_POINT('Ctrl Pts',(-0.102585905630071,0.166352005248618,
2.11124477026647));
#24761=CARTESIAN_POINT('Ctrl Pts',(-0.0991720940057208,0.168362869334424,
2.11101746507382));
#24762=CARTESIAN_POINT('Ctrl Pts',(-0.0887124595775196,0.174523989377577,
2.11032102089929));
#24763=CARTESIAN_POINT('Ctrl Pts',(-0.0776394604237156,0.179728474144029,
2.10962457672476));
#24764=CARTESIAN_POINT('Ctrl Pts',(-0.0661517651108088,0.18386164356038,
2.10892813255023));
#24765=CARTESIAN_POINT('Ctrl Pts',(-0.0546881802668738,0.187986138246923,
2.10823315007844));
#24766=CARTESIAN_POINT('Ctrl Pts',(-0.0428124172643358,0.191043416778346,
2.10753816760664));
#24767=CARTESIAN_POINT('Ctrl Pts',(-0.0307445553769932,0.192966142923237,
2.10684318513485));
#24768=CARTESIAN_POINT('Ctrl Pts',(-0.0186783939026507,0.194888598147847,
2.10614830058904));
#24769=CARTESIAN_POINT('Ctrl Pts',(-0.00642104348885204,0.195676635247699,
2.10545341604322));
#24770=CARTESIAN_POINT('Ctrl Pts',(0.00579713424226331,0.195313986274862,
2.10475853149741));
#24771=CARTESIAN_POINT('Ctrl Pts',(0.0180145856722261,0.194951358859445,
2.10406368825853));
#24772=CARTESIAN_POINT('Ctrl Pts',(0.0301919944621731,0.193438233877237,
2.10336884501965));
#24773=CARTESIAN_POINT('Ctrl Pts',(0.0421017092966201,0.190810392993419,
2.10267400178077));
#24774=CARTESIAN_POINT('Ctrl Pts',(0.0540388730367656,0.188176495595434,
2.10197755710249));
#24775=CARTESIAN_POINT('Ctrl Pts',(0.0657062704727992,0.184423005283176,
2.10128111242421));
#24776=CARTESIAN_POINT('Ctrl Pts',(0.0768902837219441,0.17963586576505,
2.10058466774594));
#24777=CARTESIAN_POINT('Ctrl Pts',(0.0805405150695424,0.178073442121128,
2.10035736256131));
#24778=CARTESIAN_POINT('Ctrl Pts',(0.084139430972879,0.176401286385976,
2.10013005737668));
#24779=CARTESIAN_POINT('Ctrl Pts',(0.0876801849670647,0.174623438186692,
2.09990275219204));
#24780=CARTESIAN_POINT('Ctrl Pts',(0.0985287606106727,0.169176259222985,
2.09920630801837));
#24781=CARTESIAN_POINT('Ctrl Pts',(0.108906182219367,0.162694971363788,
2.0985098638447));
#24782=CARTESIAN_POINT('Ctrl Pts',(0.118608362519414,0.155284308094743,
2.09781341967103));
#24783=CARTESIAN_POINT('Ctrl Pts',(0.128290179803753,0.14788919838664,2.09711843720011));
#24784=CARTESIAN_POINT('Ctrl Pts',(0.137298834480476,0.139569051785541,
2.09642345472919));
#24785=CARTESIAN_POINT('Ctrl Pts',(0.145458407148424,0.130472264446676,
2.09572847225827));
#24786=CARTESIAN_POINT('Ctrl Pts',(0.153616830097789,0.121376758883937,
2.09503358771335));
#24787=CARTESIAN_POINT('Ctrl Pts',(0.160925790405014,0.111505449927463,
2.09433870316842));
#24788=CARTESIAN_POINT('Ctrl Pts',(0.167246700449144,0.101043066010856,
2.0936438186235));
#24789=CARTESIAN_POINT('Ctrl Pts',(0.173567234751064,0.0905813040235646,
2.09294897538551));
#24790=CARTESIAN_POINT('Ctrl Pts',(0.17889940541699,0.0795293002373924,
2.09225413214753));
#24791=CARTESIAN_POINT('Ctrl Pts',(0.183149826708185,0.0680977310691177,
2.09155928890955));
#24792=CARTESIAN_POINT('Ctrl Pts',(0.187410044154482,0.0566398150008621,
2.09086284423216));
#24793=CARTESIAN_POINT('Ctrl Pts',(0.190583290771611,0.0448014300600738,
2.09016639955477));
#24794=CARTESIAN_POINT('Ctrl Pts',(0.192625937008771,0.0328086633603517,
2.08946995487739));
#24795=CARTESIAN_POINT('Ctrl Pts',(0.193292614641838,0.0288944714793296,
2.08924264968835));
#24796=CARTESIAN_POINT('Ctrl Pts',(0.193839268161496,0.024963889967138,
2.08901534449931));
#24797=CARTESIAN_POINT('Ctrl Pts',(0.194265579003178,0.0210248618202367,
2.08878803931026));
#24798=CARTESIAN_POINT('Ctrl Pts',(0.195571759927345,0.00895600754258418,
2.08809159513653));
#24799=CARTESIAN_POINT('Ctrl Pts',(0.195753586338233,-0.00327775356099378,
2.08739515096279));
#24800=CARTESIAN_POINT('Ctrl Pts',(0.194788384087688,-0.0154481527862555,
2.08669870678906));
#24801=CARTESIAN_POINT('Ctrl Pts',(0.193825207611557,-0.0275930086776184,
2.08600372431807));
#24802=CARTESIAN_POINT('Ctrl Pts',(0.191719774928313,-0.0396738965501845,
2.08530874184709));
#24803=CARTESIAN_POINT('Ctrl Pts',(0.188501372044258,-0.0514625372230354,
2.08461375937611));
#24804=CARTESIAN_POINT('Ctrl Pts',(0.185283422646914,-0.063249516826069,
2.08391887483113));
#24805=CARTESIAN_POINT('Ctrl Pts',(0.180953000178471,-0.0747434753502994,
2.08322399028614));
#24806=CARTESIAN_POINT('Ctrl Pts',(0.175590161150493,-0.0857277977504609,
2.08252910574116));
#24807=CARTESIAN_POINT('Ctrl Pts',(0.170227640912861,-0.0967114671949902,
2.08183426250312));
#24808=CARTESIAN_POINT('Ctrl Pts',(0.163833234204669,-0.107184785416907,
2.08113941926508));
#24809=CARTESIAN_POINT('Ctrl Pts',(0.156533310901506,-0.116955045116543,
2.08044457602704));
#24810=CARTESIAN_POINT('Ctrl Pts',(0.149216563105947,-0.126747822814408,
2.0797481313496));
#24811=CARTESIAN_POINT('Ctrl Pts',(0.140990708139181,-0.135833644857258,
2.07905168667216));
#24812=CARTESIAN_POINT('Ctrl Pts',(0.132022045483914,-0.144053252327892,
2.07835524199472));
#24813=CARTESIAN_POINT('Ctrl Pts',(0.129094858840565,-0.146735962797271,
2.07812793680598));
#24814=CARTESIAN_POINT('Ctrl Pts',(0.126088815573014,-0.149326716534686,
2.07790063161724));
#24815=CARTESIAN_POINT('Ctrl Pts',(0.123010416647546,-0.151820938596088,
2.0776733264285));
#24816=CARTESIAN_POINT('Ctrl Pts',(0.113578458633071,-0.159463027334912,
2.07697688225456));
#24817=CARTESIAN_POINT('Ctrl Pts',(0.10339823673046,-0.166249856763262,
2.07628043808062));
#24818=CARTESIAN_POINT('Ctrl Pts',(0.0926492469816981,-0.172038591698852,
2.07558399390668));
#24819=CARTESIAN_POINT('Ctrl Pts',(0.0819228173008448,-0.177815177190047,
2.0748890114355));
#24820=CARTESIAN_POINT('Ctrl Pts',(0.0706307170348819,-0.182597349316079,
2.07419402896431));
#24821=CARTESIAN_POINT('Ctrl Pts',(0.0589806277033746,-0.186285924201792,
2.07349904649312));
#24822=CARTESIAN_POINT('Ctrl Pts',(0.0473321799191163,-0.189973979351581,
2.07280416194792));
#24823=CARTESIAN_POINT('Ctrl Pts',(0.0353266628643546,-0.192568435295037,
2.07210927740272));
#24824=CARTESIAN_POINT('Ctrl Pts',(0.02318948939539,-0.194019090765783,
2.07141439285753));
#24825=CARTESIAN_POINT('Ctrl Pts',(0.0110530374124521,-0.195469660003301,
2.07071954961927));
#24826=CARTESIAN_POINT('Ctrl Pts',(-0.0012141827041594,-0.195776486369715,
2.07002470638101));
#24827=CARTESIAN_POINT('Ctrl Pts',(-0.0133817308529137,-0.194941245711061,
2.06932986314276));
#24828=CARTESIAN_POINT('Ctrl Pts',(-0.0255773221485489,-0.194104080032166,
2.0686334184651));
#24829=CARTESIAN_POINT('Ctrl Pts',(-0.037671914178917,-0.192119717205115,
2.06793697378745));
#24830=CARTESIAN_POINT('Ctrl Pts',(-0.0494415174021831,-0.189041520193236,
2.06724052910979));
#24831=CARTESIAN_POINT('Ctrl Pts',(-0.0532828732996088,-0.188036860136247,
2.0670132239221));
#24832=CARTESIAN_POINT('Ctrl Pts',(-0.057089728982391,-0.186916078838091,
2.0667859187344));
#24833=CARTESIAN_POINT('Ctrl Pts',(-0.0608547152675041,-0.185682157542697,
2.06655861354671));
#24834=CARTESIAN_POINT('Ctrl Pts',(-0.0723903198409249,-0.181901525407417,
2.06586216937291));
#24835=CARTESIAN_POINT('Ctrl Pts',(-0.083613098991688,-0.177028415543164,
2.0651657251991));
#24836=CARTESIAN_POINT('Ctrl Pts',(-0.0943057062615288,-0.171136184854385,
2.0644692810253));
#24837=CARTESIAN_POINT('Ctrl Pts',(-0.104975871799426,-0.165256320827762,
2.06377429855425));
#24838=CARTESIAN_POINT('Ctrl Pts',(-0.115117278778348,-0.158361934481534,
2.06307931608319));
#24839=CARTESIAN_POINT('Ctrl Pts',(-0.124533972353925,-0.15057373519227,
2.06238433361214));
#24840=CARTESIAN_POINT('Ctrl Pts',(-0.133949339077209,-0.142786633293507,
2.06168944906708));
#24841=CARTESIAN_POINT('Ctrl Pts',(-0.142639491963759,-0.134106490198566,
2.06099456452202));
#24842=CARTESIAN_POINT('Ctrl Pts',(-0.15044001616525,-0.12469547520339,
2.06029967997696));
#24843=CARTESIAN_POINT('Ctrl Pts',(-0.158240076669868,-0.115285019639621,
2.05960483673885));
#24844=CARTESIAN_POINT('Ctrl Pts',(-0.16515007519435,-0.10514446974595,
2.05890999350073));
#24845=CARTESIAN_POINT('Ctrl Pts',(-0.171046457958986,-0.0944683503597094,
2.05821515026261));
#24846=CARTESIAN_POINT('Ctrl Pts',(-0.1769564304071,-0.0837676251958226,
2.0575187055851));
#24847=CARTESIAN_POINT('Ctrl Pts',(-0.181847756999623,-0.0725296638005962,
2.05682226090758));
#24848=CARTESIAN_POINT('Ctrl Pts',(-0.185643809514086,-0.0609715998568009,
2.05612581623006));
#24849=CARTESIAN_POINT('Ctrl Pts',(-0.186882762814667,-0.0571992860078933,
2.05589851104169));
#24850=CARTESIAN_POINT('Ctrl Pts',(-0.188005442306769,-0.0533929896767407,
2.05567120585331));
#24851=CARTESIAN_POINT('Ctrl Pts',(-0.189010356714131,-0.0495605191134747,
2.05544390066494));
#24852=CARTESIAN_POINT('Ctrl Pts',(-0.192954623393621,-0.0345181574634848,
2.05455173286038));
#24853=CARTESIAN_POINT('Ctrl Pts',(-0.195103729759499,-0.0189863514340268,
2.05365956505583));
#24854=CARTESIAN_POINT('Ctrl Pts',(-0.195371401502571,-0.00334297396360765,
2.05276739725128));
#24855=CARTESIAN_POINT('Ctrl Pts',(-0.195389445586527,-0.00228843449970702,
2.05270725511381));
#24856=CARTESIAN_POINT('Ctrl Pts',(-0.195398957610215,-0.00123339698559899,
2.05264711297634));
#24857=CARTESIAN_POINT('Ctrl Pts',(-0.195399918942337,-0.000177981257815075,
2.05258697083887));
#24858=CARTESIAN_POINT('',(-0.195095239123403,5.78821923055833E-5,1.98258696921242));
#24859=CARTESIAN_POINT('Ctrl Pts',(-0.195352761517788,-0.000177909769055379,
2.05258696921242));
#24860=CARTESIAN_POINT('Ctrl Pts',(-0.194920193265683,0.0481152823703308,
2.04983437540267));
#24861=CARTESIAN_POINT('Ctrl Pts',(-0.152459071887738,0.162089108104644,
2.043376877299));
#24862=CARTESIAN_POINT('Ctrl Pts',(0.0386358748098384,0.227704580377005,
2.03321447490137));
#24863=CARTESIAN_POINT('Ctrl Pts',(0.212268936067669,0.0910165123910808,
2.02209976201962));
#24864=CARTESIAN_POINT('Ctrl Pts',(0.191580255470213,-0.128992683750082,
2.01098504913783));
#24865=CARTESIAN_POINT('Ctrl Pts',(-0.00449070026177847,-0.230915439843693,
1.99987033625606));
#24866=CARTESIAN_POINT('Ctrl Pts',(-0.167976517319539,-0.137684430050128,
1.99040430961426));
#24867=CARTESIAN_POINT('Ctrl Pts',(-0.194999162430299,-0.0361378162802388,
1.98464318726638));
#24868=CARTESIAN_POINT('Ctrl Pts',(-0.195095239123403,5.78821923055833E-5,
1.98258696921242));
#24869=CARTESIAN_POINT('',(-0.195399944102376,0.000147799825339807,1.91258696921242));
#24870=CARTESIAN_POINT('Ctrl Pts',(-0.195095239123403,5.78821923055833E-5,
1.98258696921242));
#24871=CARTESIAN_POINT('Ctrl Pts',(-0.19517227391142,0.0290797798957806,
1.98093828297245));
#24872=CARTESIAN_POINT('Ctrl Pts',(-0.175488771239349,0.123219939451178,
1.97558469243856));
#24873=CARTESIAN_POINT('Ctrl Pts',(-0.0297534949941362,0.229034574426429,
1.96652619761072));
#24874=CARTESIAN_POINT('Ctrl Pts',(0.176300576512053,0.149198570598455,
1.95541148472896));
#24875=CARTESIAN_POINT('Ctrl Pts',(0.220960165374942,-0.0672213661311054,
1.94429677184717));
#24876=CARTESIAN_POINT('Ctrl Pts',(0.0633416206041068,-0.222103457529017,
1.93318205896541));
#24877=CARTESIAN_POINT('Ctrl Pts',(-0.14169482387435,-0.176035287593829,
1.92261215264593));
#24878=CARTESIAN_POINT('Ctrl Pts',(-0.19509928885621,-0.0551416107203375,
1.9157471506204));
#24879=CARTESIAN_POINT('Ctrl Pts',(-0.195564927186827,0.000146460652338079,
1.91258705288877));
#24880=CARTESIAN_POINT('',(-0.195399942226119,-0.000150259872500694,1.84258696921242));
#24881=CARTESIAN_POINT('Ctrl Pts',(-0.195399944102376,0.000147799825339807,
1.91258696921242));
#24882=CARTESIAN_POINT('Ctrl Pts',(-0.195392740812671,0.009670966733785,
1.91204219054223));
#24883=CARTESIAN_POINT('Ctrl Pts',(-0.194689255056053,0.0191682791699718,
1.91149741187204));
#24884=CARTESIAN_POINT('Ctrl Pts',(-0.193301244059132,0.0285620210277918,
1.91095263320185));
#24885=CARTESIAN_POINT('Ctrl Pts',(-0.191526813038009,0.0405709654770123,
1.91025618902801));
#24886=CARTESIAN_POINT('Ctrl Pts',(-0.188622727228528,0.0524564295926097,
1.90955974485417));
#24887=CARTESIAN_POINT('Ctrl Pts',(-0.184624513351351,0.0639917890809184,
1.90886330068033));
#24888=CARTESIAN_POINT('Ctrl Pts',(-0.180634690958291,0.0755029380620095,
1.90816831820924));
#24889=CARTESIAN_POINT('Ctrl Pts',(-0.175555511827247,0.0866645973460532,
1.90747333573815));
#24890=CARTESIAN_POINT('Ctrl Pts',(-0.169472791726541,0.0972632143434115,
1.90677835326706));
#24891=CARTESIAN_POINT('Ctrl Pts',(-0.163390928707041,0.107860337950431,
1.90608346872197));
#24892=CARTESIAN_POINT('Ctrl Pts',(-0.156306200671082,0.117893795480693,
1.90538858417687));
#24893=CARTESIAN_POINT('Ctrl Pts',(-0.148350621826422,0.127174105083204,
1.90469369963178));
#24894=CARTESIAN_POINT('Ctrl Pts',(-0.140395515895752,0.136453863024004,
1.90399885639362));
#24895=CARTESIAN_POINT('Ctrl Pts',(-0.131570252208174,0.144979914432134,
1.90330401315547));
#24896=CARTESIAN_POINT('Ctrl Pts',(-0.122045647308596,0.152597575252773,
1.90260916991731));
#24897=CARTESIAN_POINT('Ctrl Pts',(-0.112499090583478,0.160232792871109,
1.90191272523976));
#24898=CARTESIAN_POINT('Ctrl Pts',(-0.102250698898779,0.166954944315969,
1.90121628056221));
#24899=CARTESIAN_POINT('Ctrl Pts',(-0.0915015109978395,0.172651769423636,
1.90051983588465));
#24900=CARTESIAN_POINT('Ctrl Pts',(-0.0879931976206115,0.174511095720389,
1.90029253069646));
#24901=CARTESIAN_POINT('Ctrl Pts',(-0.0844317194096779,0.176261573920934,
1.90006522550827));
#24902=CARTESIAN_POINT('Ctrl Pts',(-0.0808245197407886,0.177900413177347,
1.89983792032007));
#24903=CARTESIAN_POINT('Ctrl Pts',(-0.0697723602489291,0.182921680228243,
1.89914147614624));
#24904=CARTESIAN_POINT('Ctrl Pts',(-0.058211365925296,0.186926849622628,
1.8984450319724));
#24905=CARTESIAN_POINT('Ctrl Pts',(-0.0463512120321626,0.189822878344918,
1.89774858779857));
#24906=CARTESIAN_POINT('Ctrl Pts',(-0.0345159503274129,0.192712828858344,
1.89705360532749));
#24907=CARTESIAN_POINT('Ctrl Pts',(-0.022383599759184,0.194497981038102,
1.89635862285641));
#24908=CARTESIAN_POINT('Ctrl Pts',(-0.0101801232035018,0.195134633244746,
1.89566364038532));
#24909=CARTESIAN_POINT('Ctrl Pts',(0.00202163383028259,0.195771195744378,
1.89496875584024));
#24910=CARTESIAN_POINT('Ctrl Pts',(0.0142936261900098,0.195259487942096,
1.89427387129515));
#24911=CARTESIAN_POINT('Ctrl Pts',(0.0264050630220646,0.193607677138074,
1.89357898675006));
#24912=CARTESIAN_POINT('Ctrl Pts',(0.038515779897971,0.191955964524826,
1.89288414351191));
#24913=CARTESIAN_POINT('Ctrl Pts',(0.0504650960812098,0.189164428295551,
1.89218930027376));
#24914=CARTESIAN_POINT('Ctrl Pts',(0.0620304163469142,0.185292707486907,
1.89149445703562));
#24915=CARTESIAN_POINT('Ctrl Pts',(0.0736223917752728,0.181412063332819,
1.89079801235807));
#24916=CARTESIAN_POINT('Ctrl Pts',(0.0848277951488816,0.176446603897648,
1.89010156768052));
#24917=CARTESIAN_POINT('Ctrl Pts',(0.0954432871181529,0.170504366349023,
1.88940512300298));
#24918=CARTESIAN_POINT('Ctrl Pts',(0.098907964899463,0.168564942489481,
1.88917781781475));
#24919=CARTESIAN_POINT('Ctrl Pts',(0.102310018312978,0.166521823904143,
1.88895051262652));
#24920=CARTESIAN_POINT('Ctrl Pts',(0.105643066130638,0.164379751120744,
1.88872320743829));
#24921=CARTESIAN_POINT('Ctrl Pts',(0.115855247171571,0.157816618437492,
1.88802676326446));
#24922=CARTESIAN_POINT('Ctrl Pts',(0.125489629894986,0.150274958065372,
1.88733031909062));
#24923=CARTESIAN_POINT('Ctrl Pts',(0.134354337858408,0.141880484558761,
1.88663387491679));
#24924=CARTESIAN_POINT('Ctrl Pts',(0.143200440499962,0.133503629442078,
1.8859388924457));
#24925=CARTESIAN_POINT('Ctrl Pts',(0.151279393928429,0.124278055740848,
1.88524390997462));
#24926=CARTESIAN_POINT('Ctrl Pts',(0.158431946028575,0.114369919461363,
1.88454892750353));
#24927=CARTESIAN_POINT('Ctrl Pts',(0.165583490303622,0.104463179280541,
1.88385404295844));
#24928=CARTESIAN_POINT('Ctrl Pts',(0.171808343237217,0.0938747494012774,
1.88315915841336));
#24929=CARTESIAN_POINT('Ctrl Pts',(0.17698821497375,0.0828029695144176,
1.88246427386827));
#24930=CARTESIAN_POINT('Ctrl Pts',(0.18216777879632,0.071731847782006,1.88176943063012));
#24931=CARTESIAN_POINT('Ctrl Pts',(0.186302137850502,0.0601782376545026,
1.88107458739197));
#24932=CARTESIAN_POINT('Ctrl Pts',(0.189320693181421,0.0483615046633797,
1.88037974415382));
#24933=CARTESIAN_POINT('Ctrl Pts',(0.192346205525331,0.0365175370663244,
1.87968329947627));
#24934=CARTESIAN_POINT('Ctrl Pts',(0.194250626450532,0.0244100999672413,
1.87898685479872));
#24935=CARTESIAN_POINT('Ctrl Pts',(0.195014463147026,0.0122686251665398,
1.87829041012118));
#24936=CARTESIAN_POINT('Ctrl Pts',(0.195263763701203,0.0083058980414455,
1.87806310493295));
#24937=CARTESIAN_POINT('Ctrl Pts',(0.195391980206155,0.00433955696823603,
1.87783579974473));
#24938=CARTESIAN_POINT('Ctrl Pts',(0.195399635281082,0.000377534130968309,
1.87760849455651));
#24939=CARTESIAN_POINT('Ctrl Pts',(0.195423089793383,-0.0117617740089863,
1.87691205038268));
#24940=CARTESIAN_POINT('Ctrl Pts',(0.194311058701514,-0.0239462460320362,
1.87621560620884));
#24941=CARTESIAN_POINT('Ctrl Pts',(0.192065117802532,-0.0359464952881283,
1.87551916203501));
#24942=CARTESIAN_POINT('Ctrl Pts',(0.189823890702752,-0.0479215583225406,
1.87482417956392));
#24943=CARTESIAN_POINT('Ctrl Pts',(0.186453563582058,-0.0597123001870613,
1.87412919709284));
#24944=CARTESIAN_POINT('Ctrl Pts',(0.182007382543185,-0.0710948148586,1.87343421462176));
#24945=CARTESIAN_POINT('Ctrl Pts',(0.177561827990185,-0.082475725685272,
1.87273933007667));
#24946=CARTESIAN_POINT('Ctrl Pts',(0.172040995646972,-0.0934476923089527,
1.87204444553158));
#24947=CARTESIAN_POINT('Ctrl Pts',(0.165547385184692,-0.103803772852971,
1.87134956098649));
#24948=CARTESIAN_POINT('Ctrl Pts',(0.159054160730682,-0.114159237786806,
1.87065471774834));
#24949=CARTESIAN_POINT('Ctrl Pts',(0.15158876084847,-0.123898161565435,
1.86995987451019));
#24950=CARTESIAN_POINT('Ctrl Pts',(0.14329721271442,-0.132842270487515,
1.86926503127204));
#24951=CARTESIAN_POINT('Ctrl Pts',(0.134986554641424,-0.141806993337497,
1.86856858659449));
#24952=CARTESIAN_POINT('Ctrl Pts',(0.125846589687305,-0.149972646575667,
1.86787214191694));
#24953=CARTESIAN_POINT('Ctrl Pts',(0.116059516287823,-0.157198437266522,
1.86717569723939));
#24954=CARTESIAN_POINT('Ctrl Pts',(0.112865217253207,-0.159556786416059,
1.86694839205118));
#24955=CARTESIAN_POINT('Ctrl Pts',(0.10960222096313,-0.161815360344783,
1.86672108686296));
#24956=CARTESIAN_POINT('Ctrl Pts',(0.106277475451947,-0.1639702967356,1.86649378167475));
#24957=CARTESIAN_POINT('Ctrl Pts',(0.0960907319863873,-0.170572842441436,
1.86579733750091));
#24958=CARTESIAN_POINT('Ctrl Pts',(0.085250296698416,-0.176245842917108,
1.86510089332707));
#24959=CARTESIAN_POINT('Ctrl Pts',(0.0739497550601322,-0.180866231581648,
1.86440444915324));
#24960=CARTESIAN_POINT('Ctrl Pts',(0.062672931091436,-0.185476922936518,
1.86370946668215));
#24961=CARTESIAN_POINT('Ctrl Pts',(0.0509386916758748,-0.189038990307366,
1.86301448421107));
#24962=CARTESIAN_POINT('Ctrl Pts',(0.0389640369531972,-0.191475752575385,
1.86231950173999));
#24963=CARTESIAN_POINT('Ctrl Pts',(0.0269910695104469,-0.193912171493206,
1.8616246171949));
#24964=CARTESIAN_POINT('Ctrl Pts',(0.0147786016129055,-0.195223380555294,
1.86092973264981));
#24965=CARTESIAN_POINT('Ctrl Pts',(0.00255608906482942,-0.195383280780861,
1.86023484810472));
#24966=CARTESIAN_POINT('Ctrl Pts',(-0.00966569692427573,-0.195543171501267,
1.85954000486657));
#24967=CARTESIAN_POINT('Ctrl Pts',(-0.0218966503446213,-0.194551904535922,
1.85884516162842));
#24968=CARTESIAN_POINT('Ctrl Pts',(-0.0339077985664993,-0.192435498794723,
1.85815031839027));
#24969=CARTESIAN_POINT('Ctrl Pts',(-0.045946629472656,-0.19031421526908,
1.85745387371272));
#24970=CARTESIAN_POINT('Ctrl Pts',(-0.0577637931741429,-0.187062831837246,
1.85675742903517));
#24971=CARTESIAN_POINT('Ctrl Pts',(-0.0691421936713439,-0.182758083417162,
1.85606098435762));
#24972=CARTESIAN_POINT('Ctrl Pts',(-0.0728558690716212,-0.181353102258696,
1.8558336791694));
#24973=CARTESIAN_POINT('Ctrl Pts',(-0.0765229659843777,-0.179836296004219,
1.85560637398118));
#24974=CARTESIAN_POINT('Ctrl Pts',(-0.0801364715428752,-0.178211407964412,
1.85537906879296));
#24975=CARTESIAN_POINT('Ctrl Pts',(-0.0912079517543113,-0.173232886280332,
1.85468262461913));
#24976=CARTESIAN_POINT('Ctrl Pts',(-0.101852907383098,-0.16720106306582,
1.85398618044529));
#24977=CARTESIAN_POINT('Ctrl Pts',(-0.111862961234152,-0.160211853194221,
1.85328973627146));
#24978=CARTESIAN_POINT('Ctrl Pts',(-0.121852005901985,-0.153237312333693,
1.85259475380037));
#24979=CARTESIAN_POINT('Ctrl Pts',(-0.131208040160781,-0.145309808214192,
1.85189977132929));
#24980=CARTESIAN_POINT('Ctrl Pts',(-0.139748962759259,-0.136570082403545,
1.8512047888582));
#24981=CARTESIAN_POINT('Ctrl Pts',(-0.148288681905313,-0.127831588057544,
1.85050990431311));
#24982=CARTESIAN_POINT('Ctrl Pts',(-0.156012873316546,-0.118281692330579,
1.84981501976802));
#24983=CARTESIAN_POINT('Ctrl Pts',(-0.162775180527617,-0.108099031467454,
1.84912013522293));
#24984=CARTESIAN_POINT('Ctrl Pts',(-0.169537085757921,-0.0979169759057006,
1.84842529198478));
#24985=CARTESIAN_POINT('Ctrl Pts',(-0.175336758091339,-0.0871029742137949,
1.84773044874663));
#24986=CARTESIAN_POINT('Ctrl Pts',(-0.180071892594372,-0.0758635188841185,
1.84703560550848));
#24987=CARTESIAN_POINT('Ctrl Pts',(-0.184817940394873,-0.0645981594287393,
1.84633916083093));
#24988=CARTESIAN_POINT('Ctrl Pts',(-0.188494272298144,-0.0529062205003197,
1.84564271615338));
#24989=CARTESIAN_POINT('Ctrl Pts',(-0.191047635421175,-0.0410117178374409,
1.84494627147583));
#24990=CARTESIAN_POINT('Ctrl Pts',(-0.19188100051674,-0.0371295973278517,
1.84471896628762));
#24991=CARTESIAN_POINT('Ctrl Pts',(-0.192595151689876,-0.0332259722072379,
1.8444916610994));
#24992=CARTESIAN_POINT('Ctrl Pts',(-0.193189431175088,-0.0293087645977445,
1.84426435591119));
#24993=CARTESIAN_POINT('Ctrl Pts',(-0.194651249258628,-0.0196731553212535,
1.8437052270116));
#24994=CARTESIAN_POINT('Ctrl Pts',(-0.195392425178056,-0.00992552942978188,
1.84314609811201));
#24995=CARTESIAN_POINT('Ctrl Pts',(-0.195399942226119,-0.000150259872500694,
1.84258696921242));
#24996=CARTESIAN_POINT('',(-0.195093080635393,-5.39352580709168E-5,1.77258696921242));
#24997=CARTESIAN_POINT('Ctrl Pts',(-0.195557977360755,-0.000148962866409501,
1.84258688814036));
#24998=CARTESIAN_POINT('Ctrl Pts',(-0.195089261513762,0.0548931456497789,
1.83944113977005));
#24999=CARTESIAN_POINT('Ctrl Pts',(-0.142095896418624,0.175550050373891,
1.83259048710581));
#25000=CARTESIAN_POINT('Ctrl Pts',(0.062482893039627,0.2223465646789,1.82203493014763));
#25001=CARTESIAN_POINT('Ctrl Pts',(0.220698758115634,0.0680747009781973,
1.81092021726587));
#25002=CARTESIAN_POINT('Ctrl Pts',(0.176875795011213,-0.148516194020201,
1.79980550438408));
#25003=CARTESIAN_POINT('Ctrl Pts',(-0.0288682349025461,-0.229147838219507,
1.78869079150232));
#25004=CARTESIAN_POINT('Ctrl Pts',(-0.175242829187112,-0.123730409759538,
1.77961794644509));
#25005=CARTESIAN_POINT('Ctrl Pts',(-0.195165441948141,-0.0293292493376349,
1.77425000568179));
#25006=CARTESIAN_POINT('Ctrl Pts',(-0.195093080635393,-5.39352580709168E-5,
1.77258696921242));
#25007=CARTESIAN_POINT('',(-0.195399918614881,0.00017834039939344,1.70258696783654));
#25008=CARTESIAN_POINT('Ctrl Pts',(-0.195093080635393,-5.39352580709168E-5,
1.77258696921242));
#25009=CARTESIAN_POINT('Ctrl Pts',(-0.195004235779033,0.0358901483346491,
1.77054510138787));
#25010=CARTESIAN_POINT('Ctrl Pts',(-0.168260013010392,0.137176597591161,
1.76479832926938));
#25011=CARTESIAN_POINT('Ctrl Pts',(-0.00538297274404453,0.230896362794104,
1.75534665285699));
#25012=CARTESIAN_POINT('Ctrl Pts',(0.191080370151619,0.129732027232178,
1.7442319399752));
#25013=CARTESIAN_POINT('Ctrl Pts',(0.21261905826749,-0.0901955808703668,
1.73311722709344));
#25014=CARTESIAN_POINT('Ctrl Pts',(0.0395154849224769,-0.227553583136816,
1.72200251421165));
#25015=CARTESIAN_POINT('Ctrl Pts',(-0.152101786416837,-0.162585420427312,
1.71182576158465));
#25016=CARTESIAN_POINT('Ctrl Pts',(-0.194923096983834,-0.0483619519122345,
1.70535391325157));
#25017=CARTESIAN_POINT('Ctrl Pts',(-0.19536023340508,0.000178280042280071,
1.70258696921242));
#25018=CARTESIAN_POINT('',(-0.19542299523852,-5.30184440618641E-5,1.6325869643989));
#25019=CARTESIAN_POINT('Ctrl Pts',(-0.195399918614881,0.00017834039939344,
1.70258696783654));
#25020=CARTESIAN_POINT('Ctrl Pts',(-0.195384897736442,0.0166360719863644,
1.7016490080404));
#25021=CARTESIAN_POINT('Ctrl Pts',(-0.193286029281731,0.0329994316677939,
1.70071104824424));
#25022=CARTESIAN_POINT('Ctrl Pts',(-0.189200457854557,0.048829773167875,
1.69977308844809));
#25023=CARTESIAN_POINT('Ctrl Pts',(-0.186166881757879,0.0605839540536817,
1.69907664427426));
#25024=CARTESIAN_POINT('Ctrl Pts',(-0.182023025638628,0.0720959663926433,
1.69838020010042));
#25025=CARTESIAN_POINT('Ctrl Pts',(-0.176828166483167,0.0831442092884478,
1.69768375592658));
#25026=CARTESIAN_POINT('Ctrl Pts',(-0.171644210340761,0.094169264041337,
1.6969887734555));
#25027=CARTESIAN_POINT('Ctrl Pts',(-0.165413930789739,0.104731665062508,
1.69629379098442));
#25028=CARTESIAN_POINT('Ctrl Pts',(-0.158245230874246,0.114628124409137,
1.69559880851333));
#25029=CARTESIAN_POINT('Ctrl Pts',(-0.151077541059146,0.124523189302436,
1.69490392396824));
#25030=CARTESIAN_POINT('Ctrl Pts',(-0.142972168968596,0.133751763657475,
1.69420903942316));
#25031=CARTESIAN_POINT('Ctrl Pts',(-0.134080413646127,0.1421393776421,1.69351415487807));
#25032=CARTESIAN_POINT('Ctrl Pts',(-0.125189186888024,0.150526493030699,
1.69281931163992));
#25033=CARTESIAN_POINT('Ctrl Pts',(-0.115512325101232,0.158072165812252,
1.69212446840178));
#25034=CARTESIAN_POINT('Ctrl Pts',(-0.105236035027638,0.164640629650344,
1.69142962516363));
#25035=CARTESIAN_POINT('Ctrl Pts',(-0.094936060682695,0.171224232150226,
1.69073318048609));
#25036=CARTESIAN_POINT('Ctrl Pts',(-0.0840346723739042,0.176825712767813,
1.69003673580854));
#25037=CARTESIAN_POINT('Ctrl Pts',(-0.07274364653769,0.181354685322436,
1.68934029113099));
#25038=CARTESIAN_POINT('Ctrl Pts',(-0.0690584884258506,0.182832848616902,
1.68911298594277));
#25039=CARTESIAN_POINT('Ctrl Pts',(-0.0653319660305362,0.184197154967573,
1.68888568075455));
#25040=CARTESIAN_POINT('Ctrl Pts',(-0.0615717759788079,0.185445615755174,
1.68865837556633));
#25041=CARTESIAN_POINT('Ctrl Pts',(-0.0500508666914383,0.18927079567558,
1.6879619313925));
#25042=CARTESIAN_POINT('Ctrl Pts',(-0.0381313510056416,0.192031795032008,
1.68726548721866));
#25043=CARTESIAN_POINT('Ctrl Pts',(-0.0260315626860645,0.193658249873641,
1.68656904304482));
#25044=CARTESIAN_POINT('Ctrl Pts',(-0.013957169501573,0.195281291098496,
1.68587406057374));
#25045=CARTESIAN_POINT('Ctrl Pts',(-0.00170410390458325,0.195774324659698,
1.68517907810265));
#25046=CARTESIAN_POINT('Ctrl Pts',(0.0104983182282932,0.195117772933112,
1.68448409563156));
#25047=CARTESIAN_POINT('Ctrl Pts',(0.0226990209878445,0.194461313717464,
1.68378921108647));
#25048=CARTESIAN_POINT('Ctrl Pts',(0.0348482188803095,0.192655591722484,
1.68309432654138));
#25049=CARTESIAN_POINT('Ctrl Pts',(0.0467172764917712,0.189733118029487,
1.68239944199629));
#25050=CARTESIAN_POINT('Ctrl Pts',(0.0585856285551509,0.186810818060958,
1.68170459875814));
#25051=CARTESIAN_POINT('Ctrl Pts',(0.0701730294300375,0.18277213353102,
1.68100975551999));
#25052=CARTESIAN_POINT('Ctrl Pts',(0.0812644328689661,0.177699892938868,
1.68031491228184));
#25053=CARTESIAN_POINT('Ctrl Pts',(0.0923813992111206,0.17261596210426,
1.67961846760428));
#25054=CARTESIAN_POINT('Ctrl Pts',(0.102999317042159,0.166494142676805,
1.67892202292674));
#25055=CARTESIAN_POINT('Ctrl Pts',(0.112927402782206,0.159463355354343,
1.67822557824919));
#25056=CARTESIAN_POINT('Ctrl Pts',(0.116167725338327,0.157168651285021,
1.67799827306097));
#25057=CARTESIAN_POINT('Ctrl Pts',(0.11933481594715,0.15477745115624,1.67777096787276));
#25058=CARTESIAN_POINT('Ctrl Pts',(0.122422830082389,0.152295143306077,
1.67754366268454));
#25059=CARTESIAN_POINT('Ctrl Pts',(0.131884248319679,0.144689558702015,
1.67684721851071));
#25060=CARTESIAN_POINT('Ctrl Pts',(0.140667694832778,0.136171986337727,
1.67615077433687));
#25061=CARTESIAN_POINT('Ctrl Pts',(0.148595652872058,0.126887713934513,
1.67545433016304));
#25062=CARTESIAN_POINT('Ctrl Pts',(0.156506971647905,0.117622927438457,
1.67475934769195));
#25063=CARTESIAN_POINT('Ctrl Pts',(0.163565746058623,0.107595245630855,
1.67406436522087));
#25064=CARTESIAN_POINT('Ctrl Pts',(0.1696311747703,0.0969867235555868,1.67336938274979));
#25065=CARTESIAN_POINT('Ctrl Pts',(0.175695748837201,0.0863796962663287,
1.6726744982047));
#25066=CARTESIAN_POINT('Ctrl Pts',(0.180766781060075,0.0751927273494488,
1.67197961365961));
#25067=CARTESIAN_POINT('Ctrl Pts',(0.18474760409975,0.0636355465082373,
1.67128472911452));
#25068=CARTESIAN_POINT('Ctrl Pts',(0.188728190502099,0.0520790526758044,
1.67058988587638));
#25069=CARTESIAN_POINT('Ctrl Pts',(0.191618436455313,0.0401532273334309,
1.66989504263823));
#25070=CARTESIAN_POINT('Ctrl Pts',(0.193371320439812,0.0280836684100158,
1.66920019940008));
#25071=CARTESIAN_POINT('Ctrl Pts',(0.195128244382275,0.0159862921803006,
1.66850375472253));
#25072=CARTESIAN_POINT('Ctrl Pts',(0.19574251163749,0.00374539646522498,
1.66780731004499));
#25073=CARTESIAN_POINT('Ctrl Pts',(0.195218984440051,-0.00840881169936014,
1.66711086536744));
#25074=CARTESIAN_POINT('Ctrl Pts',(0.195048115953308,-0.0123756947319901,
1.66688356017922));
#25075=CARTESIAN_POINT('Ctrl Pts',(0.194756459524436,-0.016333375556504,
1.666656254991));
#25076=CARTESIAN_POINT('Ctrl Pts',(0.194345373103489,-0.0202740216352289,
1.66642894980278));
#25077=CARTESIAN_POINT('Ctrl Pts',(0.193085838532137,-0.032347833166574,
1.66573250562894));
#25078=CARTESIAN_POINT('Ctrl Pts',(0.19069240378987,-0.0443465598391951,
1.66503606145511));
#25079=CARTESIAN_POINT('Ctrl Pts',(0.187190876971227,-0.0560422660029291,
1.66433961728127));
#25080=CARTESIAN_POINT('Ctrl Pts',(0.183696699185824,-0.0677134251225244,
1.66364463481019));
#25081=CARTESIAN_POINT('Ctrl Pts',(0.179099222576406,-0.0790819741698788,
1.6629496523391));
#25082=CARTESIAN_POINT('Ctrl Pts',(0.173475057028626,-0.0899308878468068,
1.66225466986802));
#25083=CARTESIAN_POINT('Ctrl Pts',(0.167851683949762,-0.100778272865523,
1.66155978532293));
#25084=CARTESIAN_POINT('Ctrl Pts',(0.161202270606598,-0.111105370402818,
1.66086490077784));
#25085=CARTESIAN_POINT('Ctrl Pts',(0.153650611916079,-0.120717229332911,
1.66017001623275));
#25086=CARTESIAN_POINT('Ctrl Pts',(0.146099402128791,-0.130328516892565,
1.6594751729946));
#25087=CARTESIAN_POINT('Ctrl Pts',(0.137646615537259,-0.139223978128796,
1.65878032975645));
#25088=CARTESIAN_POINT('Ctrl Pts',(0.128456301231854,-0.147241769460405,
1.6580854865183));
#25089=CARTESIAN_POINT('Ctrl Pts',(0.119244805556886,-0.155278039790189,
1.65738904184075));
#25090=CARTESIAN_POINT('Ctrl Pts',(0.10929309085982,-0.162432075487393,
1.6566925971632));
#25091=CARTESIAN_POINT('Ctrl Pts',(0.0987972140537528,-0.168583126365651,
1.65599615248565));
#25092=CARTESIAN_POINT('Ctrl Pts',(0.0953715761964439,-0.170590702592023,
1.65576884729743));
#25093=CARTESIAN_POINT('Ctrl Pts',(0.0918881698059328,-0.172491802510378,
1.65554154210921));
#25094=CARTESIAN_POINT('Ctrl Pts',(0.0883543121723104,-0.174283319685384,
1.65531423692099));
#25095=CARTESIAN_POINT('Ctrl Pts',(0.0775268665720683,-0.179772379168067,
1.65461779274716));
#25096=CARTESIAN_POINT('Ctrl Pts',(0.0661476220366477,-0.184268017658048,
1.65392134857332));
#25097=CARTESIAN_POINT('Ctrl Pts',(0.0544220854670605,-0.187668315422226,
1.65322490439949));
#25098=CARTESIAN_POINT('Ctrl Pts',(0.0427211585499092,-0.191061476613535,
1.65252992192841));
#25099=CARTESIAN_POINT('Ctrl Pts',(0.030676194008489,-0.193363546945208,
1.65183493945732));
#25100=CARTESIAN_POINT('Ctrl Pts',(0.0185110803761076,-0.194521206821542,
1.65113995698624));
#25101=CARTESIAN_POINT('Ctrl Pts',(0.00634768086012452,-0.195678703578663,
1.65044507244115));
#25102=CARTESIAN_POINT('Ctrl Pts',(-0.00593496808282118,-0.195691981273954,
1.64975018789606));
#25103=CARTESIAN_POINT('Ctrl Pts',(-0.0181059374205579,-0.194559335499798,
1.64905530335097));
#25104=CARTESIAN_POINT('Ctrl Pts',(-0.0302761832632767,-0.193426757055001,
1.64836046011282));
#25105=CARTESIAN_POINT('Ctrl Pts',(-0.042333893166877,-0.191148498147918,
1.64766561687467));
#25106=CARTESIAN_POINT('Ctrl Pts',(-0.0540541262823569,-0.187774629361506,
1.64697077363653));
#25107=CARTESIAN_POINT('Ctrl Pts',(-0.0658013715957562,-0.184392984653702,
1.64627432895898));
#25108=CARTESIAN_POINT('Ctrl Pts',(-0.0772087642590092,-0.179910993489646,
1.64557788428143));
#25109=CARTESIAN_POINT('Ctrl Pts',(-0.0880685331149196,-0.174427903372672,
1.64488143960388));
#25110=CARTESIAN_POINT('Ctrl Pts',(-0.0916129378370585,-0.172638335771338,
1.64465413441567));
#25111=CARTESIAN_POINT('Ctrl Pts',(-0.0950992074404759,-0.170742491570658,
1.64442682922745));
#25112=CARTESIAN_POINT('Ctrl Pts',(-0.0985207639132304,-0.16874483422598,
1.64419952403923));
#25113=CARTESIAN_POINT('Ctrl Pts',(-0.109004128105527,-0.162624178424318,
1.64350307986539));
#25114=CARTESIAN_POINT('Ctrl Pts',(-0.118952045286865,-0.15550119341922,
1.64280663569156));
#25115=CARTESIAN_POINT('Ctrl Pts',(-0.128167441182025,-0.147493277883612,
1.64211019151772));
#25116=CARTESIAN_POINT('Ctrl Pts',(-0.137363495728602,-0.139502169426891,
1.64141520904664));
#25117=CARTESIAN_POINT('Ctrl Pts',(-0.145829377222639,-0.130630329192478,
1.64072022657555));
#25118=CARTESIAN_POINT('Ctrl Pts',(-0.153398877393225,-0.121036954747293,
1.64002524410447));
#25119=CARTESIAN_POINT('Ctrl Pts',(-0.160967310988954,-0.111444932049483,
1.63933035955938));
#25120=CARTESIAN_POINT('Ctrl Pts',(-0.167639036205313,-0.101132234827594,
1.63863547501429));
#25121=CARTESIAN_POINT('Ctrl Pts',(-0.173287394034427,-0.0902919656932838,
1.6379405904692));
#25122=CARTESIAN_POINT('Ctrl Pts',(-0.178935416100738,-0.0794523409514253,
1.63724574723105));
#25123=CARTESIAN_POINT('Ctrl Pts',(-0.183559810586553,-0.06808599556662,
1.6365509039929));
#25124=CARTESIAN_POINT('Ctrl Pts',(-0.18708066713741,-0.0564090771367656,
1.63585606075475));
#25125=CARTESIAN_POINT('Ctrl Pts',(-0.190609638379593,-0.0447052463384756,
1.6351596160772));
#25126=CARTESIAN_POINT('Ctrl Pts',(-0.193029803639046,-0.0326902701718145,
1.63446317139965));
#25127=CARTESIAN_POINT('Ctrl Pts',(-0.194311881761601,-0.0205925376354037,
1.6337667267221));
#25128=CARTESIAN_POINT('Ctrl Pts',(-0.19473032563569,-0.0166440870837835,
1.63353942153388));
#25129=CARTESIAN_POINT('Ctrl Pts',(-0.195027950573094,-0.0126868506266221,
1.63331211634566));
#25130=CARTESIAN_POINT('Ctrl Pts',(-0.195204939685526,-0.00872877553671252,
1.63308481115744));
#25131=CARTESIAN_POINT('Ctrl Pts',(-0.195334153049388,-0.00583912775127325,
1.63291886384244));
#25132=CARTESIAN_POINT('Ctrl Pts',(-0.195399206533935,-0.00294658962844581,
1.63275291652743));
#25133=CARTESIAN_POINT('Ctrl Pts',(-0.195399992786049,-5.30962533302248E-5,
1.63258696921242));
#25134=CARTESIAN_POINT('',(-0.195203598247727,-0.000145069483009505,1.56258696921242));
#25135=CARTESIAN_POINT('Ctrl Pts',(-0.195702830166494,-5.20718601689164E-5,
1.63258690584025));
#25136=CARTESIAN_POINT('Ctrl Pts',(-0.195478538915108,0.061749283732994,
1.6290479699854));
#25137=CARTESIAN_POINT('Ctrl Pts',(-0.13051040340586,0.188655383227059,
1.6218041298366));
#25138=CARTESIAN_POINT('Ctrl Pts',(0.0856301532178521,0.214498446630602,
1.6108553853939));
#25139=CARTESIAN_POINT('Ctrl Pts',(0.226656931919608,0.0443705077713918,
1.59974067251211));
#25140=CARTESIAN_POINT('Ctrl Pts',(0.16019046818058,-0.166376442596738,
1.58862595963034));
#25141=CARTESIAN_POINT('Ctrl Pts',(-0.0529224685754463,-0.224813965462503,
1.57751124674856));
#25142=CARTESIAN_POINT('Ctrl Pts',(-0.181512116776874,-0.109731403433318,
1.56883158327592));
#25143=CARTESIAN_POINT('Ctrl Pts',(-0.195357411599742,-0.0224672944395423,
1.56385682409721));
#25144=CARTESIAN_POINT('Ctrl Pts',(-0.195203598247727,-0.000145069483009505,
1.56258696921242));
#25145=CARTESIAN_POINT('',(-0.195399954007542,0.000134066589732251,1.49258696650567));
#25146=CARTESIAN_POINT('Ctrl Pts',(-0.195203598247727,-0.000145069483009505,
1.56258696921242));
#25147=CARTESIAN_POINT('Ctrl Pts',(-0.194908648709454,0.0426596016193331,
1.56015191980329));
#25148=CARTESIAN_POINT('Ctrl Pts',(-0.159970883662516,0.151029040268688,
1.55401196610022));
#25149=CARTESIAN_POINT('Ctrl Pts',(0.0190478344627849,0.230172297962467,
1.54416710810324));
#25150=CARTESIAN_POINT('Ctrl Pts',(0.203720217624868,0.108812589703487,
1.53305239522145));
#25151=CARTESIAN_POINT('Ctrl Pts',(0.201896789043055,-0.112159677786471,
1.52193768233969));
#25152=CARTESIAN_POINT('Ctrl Pts',(0.0152468076525971,-0.230455291984146,
1.5108229694579));
#25153=CARTESIAN_POINT('Ctrl Pts',(-0.16133530721145,-0.148879556632701,
1.5010393984155));
#25154=CARTESIAN_POINT('Ctrl Pts',(-0.194916683322746,-0.0416061777329493,
1.49496073166699));
#25155=CARTESIAN_POINT('Ctrl Pts',(-0.195179950177078,0.000133868047100166,
1.49258696921242));
#25156=CARTESIAN_POINT('',(-0.195415762289312,7.15973788392893E-5,1.42258696921242));
#25157=CARTESIAN_POINT('Ctrl Pts',(-0.195399954007542,0.000134066589732251,
1.49258696650567));
#25158=CARTESIAN_POINT('Ctrl Pts',(-0.195390351133564,0.0141301049573953,
1.49179190213383));
#25159=CARTESIAN_POINT('Ctrl Pts',(-0.193872852752641,0.0280660265355398,
1.49099683776198));
#25160=CARTESIAN_POINT('Ctrl Pts',(-0.190910121066081,0.0416471568601563,
1.49020177339012));
#25161=CARTESIAN_POINT('Ctrl Pts',(-0.188912482783523,0.0508043093555799,
1.48966569682487));
#25162=CARTESIAN_POINT('Ctrl Pts',(-0.186258880595048,0.0598005076247773,
1.48912962025961));
#25163=CARTESIAN_POINT('Ctrl Pts',(-0.182980778986252,0.0685506711971836,
1.48859354369435));
#25164=CARTESIAN_POINT('Ctrl Pts',(-0.178722031421712,0.0799184511657234,
1.48789709952051));
#25165=CARTESIAN_POINT('Ctrl Pts',(-0.173384812841909,0.0909280864667609,
1.48720065534668));
#25166=CARTESIAN_POINT('Ctrl Pts',(-0.167051486644434,0.101365481352798,
1.48650421117284));
#25167=CARTESIAN_POINT('Ctrl Pts',(-0.160731452883988,0.111780970148742,
1.48580922870175));
#25168=CARTESIAN_POINT('Ctrl Pts',(-0.153419847023285,0.121625822527253,
1.48511424623067));
#25169=CARTESIAN_POINT('Ctrl Pts',(-0.145245450955154,0.130709291853464,
1.48441926375958));
#25170=CARTESIAN_POINT('Ctrl Pts',(-0.137072206694295,0.139791481280103,
1.48372437921449));
#25171=CARTESIAN_POINT('Ctrl Pts',(-0.128036964184847,0.148111819863908,
1.4830294946694));
#25172=CARTESIAN_POINT('Ctrl Pts',(-0.11830861287875,0.15551280371309,1.48233461012431));
#25173=CARTESIAN_POINT('Ctrl Pts',(-0.108580839867898,0.162913347615806,
1.48163976688616));
#25174=CARTESIAN_POINT('Ctrl Pts',(-0.098160753035793,0.169394136316214,
1.48094492364801));
#25175=CARTESIAN_POINT('Ctrl Pts',(-0.0872478639558456,0.174839841669862,
1.48025008040986));
#25176=CARTESIAN_POINT('Ctrl Pts',(-0.0763098234035006,0.180298098008577,
1.47955363573231));
#25177=CARTESIAN_POINT('Ctrl Pts',(-0.0648775252347868,0.184716175729808,
1.47885719105476));
#25178=CARTESIAN_POINT('Ctrl Pts',(-0.0531711118537846,0.188026574888318,
1.47816074637721));
#25179=CARTESIAN_POINT('Ctrl Pts',(-0.0493503798091365,0.189107020942446,
1.477933441189));
#25180=CARTESIAN_POINT('Ctrl Pts',(-0.0455005472779019,0.190069876311248,
1.47770613600079));
#25181=CARTESIAN_POINT('Ctrl Pts',(-0.0416294779424288,0.190913976875034,
1.47747883081258));
#25182=CARTESIAN_POINT('Ctrl Pts',(-0.0297688437596777,0.193500230732273,
1.47678238663874));
#25183=CARTESIAN_POINT('Ctrl Pts',(-0.0176242956823007,0.194986139082841,
1.47608594246491));
#25184=CARTESIAN_POINT('Ctrl Pts',(-0.00542038081509231,0.195324805060236,
1.47538949829107));
#25185=CARTESIAN_POINT('Ctrl Pts',(0.00675792037537916,0.195662760242697,
1.47469451581999));
#25186=CARTESIAN_POINT('Ctrl Pts',(0.0189944765403277,0.194858153606765,
1.4739995333489));
#25187=CARTESIAN_POINT('Ctrl Pts',(0.0310591869555855,0.192915750797228,
1.47330455087782));
#25188=CARTESIAN_POINT('Ctrl Pts',(0.0431221974016848,0.190973621680531,
1.47260966633273));
#25189=CARTESIAN_POINT('Ctrl Pts',(0.0550125396006769,0.187894108124109,
1.47191478178764));
#25190=CARTESIAN_POINT('Ctrl Pts',(0.0665062941107382,0.183733700892504,
1.47121989724254));
#25191=CARTESIAN_POINT('Ctrl Pts',(0.0779993653823561,0.179573540973485,
1.47052505400439));
#25192=CARTESIAN_POINT('Ctrl Pts',(0.0890950813965693,0.174332938155153,
1.46983021076624));
#25193=CARTESIAN_POINT('Ctrl Pts',(0.099588353227997,0.168116982786795,
1.46913536752809));
#25194=CARTESIAN_POINT('Ctrl Pts',(0.110105809419304,0.161886701200264,
1.46843892285055));
#25195=CARTESIAN_POINT('Ctrl Pts',(0.120017329584307,0.154677081225006,
1.467742478173));
#25196=CARTESIAN_POINT('Ctrl Pts',(0.129146822535201,0.146636483281144,
1.46704603349545));
#25197=CARTESIAN_POINT('Ctrl Pts',(0.13212650086488,0.144012197838365,1.46681872830723));
#25198=CARTESIAN_POINT('Ctrl Pts',(0.135023159806546,0.141299695680558,
1.46659142311902));
#25199=CARTESIAN_POINT('Ctrl Pts',(0.137831556989672,0.138504952611099,
1.4663641179308));
#25200=CARTESIAN_POINT('Ctrl Pts',(0.146436252163398,0.129942092504961,
1.46566767375697));
#25201=CARTESIAN_POINT('Ctrl Pts',(0.15427039494324,0.120543998095244,1.46497122958313));
#25202=CARTESIAN_POINT('Ctrl Pts',(0.161172816316964,0.110473903164767,
1.4642747854093));
#25203=CARTESIAN_POINT('Ctrl Pts',(0.168060750832027,0.100424943432224,
1.46357980293822));
#25204=CARTESIAN_POINT('Ctrl Pts',(0.174020293639803,0.089707455473858,
1.46288482046713));
#25205=CARTESIAN_POINT('Ctrl Pts',(0.178930671049179,0.0785173545013498,
1.46218983799605));
#25206=CARTESIAN_POINT('Ctrl Pts',(0.183840356565433,0.0673288302617974,
1.46149495345096));
#25207=CARTESIAN_POINT('Ctrl Pts',(0.187700776603113,0.0556686073443341,
1.46080006890588));
#25208=CARTESIAN_POINT('Ctrl Pts',(0.19043796893578,0.0437554566610235,
1.46010518436079));
#25209=CARTESIAN_POINT('Ctrl Pts',(0.193174998557906,0.0318430141468777,
1.45941034112264));
#25210=CARTESIAN_POINT('Ctrl Pts',(0.194788762984549,0.0196785332232306,
1.45871549788449));
#25211=CARTESIAN_POINT('Ctrl Pts',(0.195256344734548,0.00749131770139881,
1.45802065464634));
#25212=CARTESIAN_POINT('Ctrl Pts',(0.195725004143213,-0.00472398629568257,
1.4573242099688));
#25213=CARTESIAN_POINT('Ctrl Pts',(0.195042238430193,-0.016961252458877,
1.45662776529125));
#25214=CARTESIAN_POINT('Ctrl Pts',(0.193237210421569,-0.0289920766501849,
1.4559313206137));
#25215=CARTESIAN_POINT('Ctrl Pts',(0.192648086483255,-0.0329186896971232,
1.45570401542548));
#25216=CARTESIAN_POINT('Ctrl Pts',(0.19193982343752,-0.0368233874370288,
1.45547671023725));
#25217=CARTESIAN_POINT('Ctrl Pts',(0.191114599357323,-0.0406985246967225,
1.45524940504903));
#25218=CARTESIAN_POINT('Ctrl Pts',(0.188586181474533,-0.0525716226598113,
1.45455296087519));
#25219=CARTESIAN_POINT('Ctrl Pts',(0.184938147622258,-0.0642502279122655,
1.45385651670135));
#25220=CARTESIAN_POINT('Ctrl Pts',(0.18022024916266,-0.0755104084994154,
1.45316007252752));
#25221=CARTESIAN_POINT('Ctrl Pts',(0.175512252667091,-0.0867469561270848,
1.45246509005643));
#25222=CARTESIAN_POINT('Ctrl Pts',(0.169739114602154,-0.0975659937691164,
1.45177010758535));
#25223=CARTESIAN_POINT('Ctrl Pts',(0.162999950667442,-0.107759807360682,
1.45107512511426));
#25224=CARTESIAN_POINT('Ctrl Pts',(0.156261736309674,-0.117952184600432,
1.45038024056917));
#25225=CARTESIAN_POINT('Ctrl Pts',(0.148558210037661,-0.127518757880856,
1.44968535602408));
#25226=CARTESIAN_POINT('Ctrl Pts',(0.140033075610836,-0.136278750122571,
1.44899047147899));
#25227=CARTESIAN_POINT('Ctrl Pts',(0.131508447954845,-0.145038221632486,
1.44829562824084));
#25228=CARTESIAN_POINT('Ctrl Pts',(0.122162939052251,-0.152990598328739,
1.44760078500269));
#25229=CARTESIAN_POINT('Ctrl Pts',(0.112176782689824,-0.15999227926797,
1.44690594176454));
#25230=CARTESIAN_POINT('Ctrl Pts',(0.10216761074149,-0.167010097325757,
1.44620949708699));
#25231=CARTESIAN_POINT('Ctrl Pts',(0.0915155974866367,-0.173072396047143,
1.44551305240944));
#25232=CARTESIAN_POINT('Ctrl Pts',(0.080428462636264,-0.178079820299682,
1.44481660773189));
#25233=CARTESIAN_POINT('Ctrl Pts',(0.0768098503398591,-0.179714140366867,
1.44458930254368));
#25234=CARTESIAN_POINT('Ctrl Pts',(0.0731450451935352,-0.181236475487685,
1.44436199735546));
#25235=CARTESIAN_POINT('Ctrl Pts',(0.0694416517953648,-0.182644509898139,
1.44413469216724));
#25236=CARTESIAN_POINT('Ctrl Pts',(0.0580947627260293,-0.186958610114745,
1.44343824799341));
#25237=CARTESIAN_POINT('Ctrl Pts',(0.0463041473121616,-0.190226539090695,
1.44274180381957));
#25238=CARTESIAN_POINT('Ctrl Pts',(0.0342849323719999,-0.192368665359635,
1.44204535964574));
#25239=CARTESIAN_POINT('Ctrl Pts',(0.0222909434588516,-0.194506295716373,
1.44135037717466));
#25240=CARTESIAN_POINT('Ctrl Pts',(0.0100701476881834,-0.195522587676248,
1.44065539470357));
#25241=CARTESIAN_POINT('Ctrl Pts',(-0.00214918538429394,-0.19538818030317,
1.43996041223249));
#25242=CARTESIAN_POINT('Ctrl Pts',(-0.0143667967006226,-0.195253791868663,
1.4392655276874));
#25243=CARTESIAN_POINT('Ctrl Pts',(-0.0265820709186002,-0.193968989497673,
1.43857064314231));
#25244=CARTESIAN_POINT('Ctrl Pts',(-0.0385651919972097,-0.191556482443739,
1.43787575859722));
#25245=CARTESIAN_POINT('Ctrl Pts',(-0.0505476007473118,-0.18914411879965,
1.43718091535907));
#25246=CARTESIAN_POINT('Ctrl Pts',(-0.0622970304997711,-0.185604382614689,
1.43648607212092));
#25247=CARTESIAN_POINT('Ctrl Pts',(-0.0735950913425348,-0.181010835394691,
1.43579122888277));
#25248=CARTESIAN_POINT('Ctrl Pts',(-0.0849191913820126,-0.176406701200403,
1.43509478420523));
#25249=CARTESIAN_POINT('Ctrl Pts',(-0.0957890594016855,-0.170744296993414,
1.43439833952768));
#25250=CARTESIAN_POINT('Ctrl Pts',(-0.106008575956307,-0.164144271370389,
1.43370189485013));
#25251=CARTESIAN_POINT('Ctrl Pts',(-0.109344015523638,-0.161990159041222,
1.43347458966191));
#25252=CARTESIAN_POINT('Ctrl Pts',(-0.112610414407529,-0.159736508821645,
1.43324728447369));
#25253=CARTESIAN_POINT('Ctrl Pts',(-0.115801703119268,-0.157388454324569,
1.43301997928548));
#25254=CARTESIAN_POINT('Ctrl Pts',(-0.125492033249174,-0.150258600119908,
1.43232976836662));
#25255=CARTESIAN_POINT('Ctrl Pts',(-0.134558675788076,-0.142202839596349,
1.43163955744776));
#25256=CARTESIAN_POINT('Ctrl Pts',(-0.142819844890049,-0.133355359493281,
1.43094934652889));
#25257=CARTESIAN_POINT('Ctrl Pts',(-0.151160654346282,-0.124422586807406,
1.43025248175252));
#25258=CARTESIAN_POINT('Ctrl Pts',(-0.158679605738282,-0.11468327090578,
1.42955561697615));
#25259=CARTESIAN_POINT('Ctrl Pts',(-0.165224794108631,-0.104316477182468,
1.42885875219978));
#25260=CARTESIAN_POINT('Ctrl Pts',(-0.171692724670043,-0.094072050566634,
1.42817011304545));
#25261=CARTESIAN_POINT('Ctrl Pts',(-0.177209306120145,-0.0832156728885014,
1.42748147389112));
#25262=CARTESIAN_POINT('Ctrl Pts',(-0.181671077724288,-0.0719498402951364,
1.42679283473679));
#25263=CARTESIAN_POINT('Ctrl Pts',(-0.186212791443188,-0.0604821563830781,
1.4260918571494));
#25264=CARTESIAN_POINT('Ctrl Pts',(-0.189661094091221,-0.0485910563735383,
1.425390879562));
#25265=CARTESIAN_POINT('Ctrl Pts',(-0.191959025352893,-0.0365088014808403,
1.42468990197461));
#25266=CARTESIAN_POINT('Ctrl Pts',(-0.194256956614565,-0.0244265465881405,
1.42398892438721));
#25267=CARTESIAN_POINT('Ctrl Pts',(-0.195404466195307,-0.0121541052075848,
1.42328794679982));
#25268=CARTESIAN_POINT('Ctrl Pts',(-0.195399986884961,7.15915989697979E-5,
1.42258696921242));
#25269=CARTESIAN_POINT('',(-0.195392498133114,-0.000178699422991063,1.35258696921242));
#25270=CARTESIAN_POINT('Ctrl Pts',(-0.195688377393879,7.16972608892641E-5,
1.42258696921242));
#25271=CARTESIAN_POINT('Ctrl Pts',(-0.195707099359798,0.0040407295163859,
1.42235973494285));
#25272=CARTESIAN_POINT('Ctrl Pts',(-0.193798549159007,0.0727038566799422,
1.41842759637929));
#25273=CARTESIAN_POINT('Ctrl Pts',(-0.113142331553771,0.201347757766985,
1.41079055352198));
#25274=CARTESIAN_POINT('Ctrl Pts',(0.107818424683884,0.204248118830208,
1.39967584064012));
#25275=CARTESIAN_POINT('Ctrl Pts',(0.230076730733924,0.0201694006329071,
1.38856112775837));
#25276=CARTESIAN_POINT('Ctrl Pts',(0.141711137193357,-0.182373409088167,
1.3774464148766));
#25277=CARTESIAN_POINT('Ctrl Pts',(-0.0763840132470003,-0.217962357455062,
1.36633170199481));
#25278=CARTESIAN_POINT('Ctrl Pts',(-0.186850444349053,-0.0957346434792127,
1.35804522010676));
#25279=CARTESIAN_POINT('Ctrl Pts',(-0.195533353731187,-0.0155516148321636,
1.35346364251263));
#25280=CARTESIAN_POINT('Ctrl Pts',(-0.195392498133114,-0.000178699422991063,
1.35258696921242));
#25281=CARTESIAN_POINT('',(-0.19537121115614,3.68736377462065E-5,1.28258696733929));
#25282=CARTESIAN_POINT('Ctrl Pts',(-0.195392498133114,-0.000178699422991063,
1.35258696921242));
#25283=CARTESIAN_POINT('Ctrl Pts',(-0.194938084649759,0.0494157798589555,
1.3497587382187));
#25284=CARTESIAN_POINT('Ctrl Pts',(-0.150558264293769,0.164701191617148,
1.34322560293105));
#25285=CARTESIAN_POINT('Ctrl Pts',(0.0432653212731082,0.226870488874589,
1.33298756334949));
#25286=CARTESIAN_POINT('Ctrl Pts',(0.214078562825376,0.0866745388549855,
1.32187285046771));
#25287=CARTESIAN_POINT('Ctrl Pts',(0.188913438476778,-0.132867676693533,
1.31075813758593));
#25288=CARTESIAN_POINT('Ctrl Pts',(-0.00919262157656059,-0.23077608726999,
1.29964342470415));
#25289=CARTESIAN_POINT('Ctrl Pts',(-0.169454903792707,-0.135006243596358,
1.29025303524633));
#25290=CARTESIAN_POINT('Ctrl Pts',(-0.195026953550068,-0.0348317645878951,
1.28456755008241));
#25291=CARTESIAN_POINT('Ctrl Pts',(-0.195085605073228,3.67867518197285E-5,
1.28258696921242));
#25292=CARTESIAN_POINT('',(-0.19539993476676,0.000159665732175137,1.21258696921242));
#25293=CARTESIAN_POINT('Ctrl Pts',(-0.195399996519163,3.68823947128292E-5,
1.2825869671505));
#25294=CARTESIAN_POINT('Ctrl Pts',(-0.195397534591892,0.0130799774522216,
1.2818472934737));
#25295=CARTESIAN_POINT('Ctrl Pts',(-0.194084875265927,0.0260895437433635,
1.28110761979689));
#25296=CARTESIAN_POINT('Ctrl Pts',(-0.191507126714693,0.0388095402895012,
1.28036794612009));
#25297=CARTESIAN_POINT('Ctrl Pts',(-0.188915309047009,0.0515989614164704,
1.27962423537183));
#25298=CARTESIAN_POINT('Ctrl Pts',(-0.185044815819923,0.0640949892409484,
1.27888052462358));
#25299=CARTESIAN_POINT('Ctrl Pts',(-0.179990958120247,0.0760553416595802,
1.27813681387532));
#25300=CARTESIAN_POINT('Ctrl Pts',(-0.178353671118658,0.0799301103438472,
1.27789587556375));
#25301=CARTESIAN_POINT('Ctrl Pts',(-0.176592551635074,0.0837488379902776,
1.27765493725218));
#25302=CARTESIAN_POINT('Ctrl Pts',(-0.17471186284551,0.087503856949576,
1.27741399894062));
#25303=CARTESIAN_POINT('Ctrl Pts',(-0.169275638353994,0.0983579260257119,
1.27671755476678));
#25304=CARTESIAN_POINT('Ctrl Pts',(-0.162804829860834,0.108741885245363,
1.27602111059294));
#25305=CARTESIAN_POINT('Ctrl Pts',(-0.155403964771163,0.118451541709693,
1.27532466641911));
#25306=CARTESIAN_POINT('Ctrl Pts',(-0.148018632677917,0.128140819467302,
1.27462968394802));
#25307=CARTESIAN_POINT('Ctrl Pts',(-0.139707584601259,0.137157868789804,
1.27393470147693));
#25308=CARTESIAN_POINT('Ctrl Pts',(-0.130619039029278,0.145326620558891,
1.27323971900585));
#25309=CARTESIAN_POINT('Ctrl Pts',(-0.121531774072133,0.153494221316013,
1.27254483446076));
#25310=CARTESIAN_POINT('Ctrl Pts',(-0.111667848579019,0.160813143041246,
1.27184994991566));
#25311=CARTESIAN_POINT('Ctrl Pts',(-0.101211850984521,0.167144611699831,
1.27115506537057));
#25312=CARTESIAN_POINT('Ctrl Pts',(-0.0907564749397088,0.173475703988555,
1.27046022213242));
#25313=CARTESIAN_POINT('Ctrl Pts',(-0.0797098596379881,0.178819028996811,
1.26976537889427));
#25314=CARTESIAN_POINT('Ctrl Pts',(-0.0682825871154466,0.183080988354393,
1.26907053565611));
#25315=CARTESIAN_POINT('Ctrl Pts',(-0.0568289775956777,0.187352770459404,
1.26837409097856));
#25316=CARTESIAN_POINT('Ctrl Pts',(-0.0449938020940338,0.19053796637405,
1.26767764630101));
#25317=CARTESIAN_POINT('Ctrl Pts',(-0.033003103564723,0.192592718333524,
1.26698120162346));
#25318=CARTESIAN_POINT('Ctrl Pts',(-0.029089586707128,0.193263347022247,
1.26675389643525));
#25319=CARTESIAN_POINT('Ctrl Pts',(-0.0251595590618304,0.193813968205019,
1.26652659124704));
#25320=CARTESIAN_POINT('Ctrl Pts',(-0.0212209632995607,0.194244255298937,
1.26629928605883));
#25321=CARTESIAN_POINT('Ctrl Pts',(-0.00915343376659917,0.1955626191339,
1.26560284188499));
#25322=CARTESIAN_POINT('Ctrl Pts',(0.00308013755035486,0.195756795502481,
1.26490639771116));
#25323=CARTESIAN_POINT('Ctrl Pts',(0.0152515049529862,0.19480387982961,
1.26420995353733));
#25324=CARTESIAN_POINT('Ctrl Pts',(0.0273973269897674,0.193852964143977,
1.26351497106624));
#25325=CARTESIAN_POINT('Ctrl Pts',(0.0394803341542351,0.191759728256867,
1.26281998859516));
#25326=CARTESIAN_POINT('Ctrl Pts',(0.0512722178173541,0.188553227710612,
1.26212500612408));
#25327=CARTESIAN_POINT('Ctrl Pts',(0.0630624399537676,0.18534717897396,
1.26143012157899));
#25328=CARTESIAN_POINT('Ctrl Pts',(0.0745607642082807,0.181028361926375,
1.2607352370339));
#25329=CARTESIAN_POINT('Ctrl Pts',(0.0855504948284708,0.175676614364587,
1.26004035248881));
#25330=CARTESIAN_POINT('Ctrl Pts',(0.0965395721715766,0.170325184933803,
1.25934550925066));
#25331=CARTESIAN_POINT('Ctrl Pts',(0.10701934024705,0.16394135435562,1.25865066601251));
#25332=CARTESIAN_POINT('Ctrl Pts',(0.116796964282291,0.156651297902192,
1.25795582277437));
#25333=CARTESIAN_POINT('Ctrl Pts',(0.126597123288727,0.149344439696969,
1.25725937809682));
#25334=CARTESIAN_POINT('Ctrl Pts',(0.135691244748885,0.141127761107914,
1.25656293341927));
#25335=CARTESIAN_POINT('Ctrl Pts',(0.143919901946437,0.132167400760279,
1.25586648874173));
#25336=CARTESIAN_POINT('Ctrl Pts',(0.146605566053609,0.129242923826164,
1.2556391835535));
#25337=CARTESIAN_POINT('Ctrl Pts',(0.149199353082293,0.126239497477568,
1.25541187836528));
#25338=CARTESIAN_POINT('Ctrl Pts',(0.151696681528045,0.123163618058982,
1.25518457317706));
#25339=CARTESIAN_POINT('Ctrl Pts',(0.15934828798626,0.113739379583673,1.25448812900322));
#25340=CARTESIAN_POINT('Ctrl Pts',(0.166145390946764,0.103566014212564,
1.25379168482939));
#25341=CARTESIAN_POINT('Ctrl Pts',(0.171944974097777,0.0928228737031702,
1.25309524065555));
#25342=CARTESIAN_POINT('Ctrl Pts',(0.17773238503605,0.082102280985295,1.25240025818446));
#25343=CARTESIAN_POINT('Ctrl Pts',(0.182525954163857,0.0708150141047222,
1.25170527571338));
#25344=CARTESIAN_POINT('Ctrl Pts',(0.186226288000902,0.0591686543484393,
1.25101029324229));
#25345=CARTESIAN_POINT('Ctrl Pts',(0.189926100445126,0.0475239356139243,
1.2503154086972));
#25346=CARTESIAN_POINT('Ctrl Pts',(0.192532674704041,0.0355210437962889,
1.24962052415211));
#25347=CARTESIAN_POINT('Ctrl Pts',(0.193995581981284,0.0233853409584502,
1.24892563960702));
#25348=CARTESIAN_POINT('Ctrl Pts',(0.195458402296995,0.011250359519239,
1.24823079636887));
#25349=CARTESIAN_POINT('Ctrl Pts',(0.195777612335889,-0.00101654460194885,
1.24753595313072));
#25350=CARTESIAN_POINT('Ctrl Pts',(0.194954655312547,-0.0131849297292836,
1.24684110989257));
#25351=CARTESIAN_POINT('Ctrl Pts',(0.194129801579661,-0.0253813599325303,
1.24614466521503));
#25352=CARTESIAN_POINT('Ctrl Pts',(0.192157649324152,-0.0374779490240786,
1.24544822053748));
#25353=CARTESIAN_POINT('Ctrl Pts',(0.189091335363429,-0.0492506537060681,
1.24475177585993));
#25354=CARTESIAN_POINT('Ctrl Pts',(0.188090553686938,-0.053093021865166,
1.24452447067171));
#25355=CARTESIAN_POINT('Ctrl Pts',(0.186973615999746,-0.0569010070520961,
1.24429716548349));
#25356=CARTESIAN_POINT('Ctrl Pts',(0.185743496105052,-0.0606672370779526,
1.24406986029527));
#25357=CARTESIAN_POINT('Ctrl Pts',(0.181974511153627,-0.0722066523433209,
1.24337341612144));
#25358=CARTESIAN_POINT('Ctrl Pts',(0.177112733230786,-0.0834343452077754,
1.2426769719476));
#25359=CARTESIAN_POINT('Ctrl Pts',(0.171231299791148,-0.0941328952695809,
1.24198052777377));
#25360=CARTESIAN_POINT('Ctrl Pts',(0.165362210352309,-0.104808991126666,
1.24128554530269));
#25361=CARTESIAN_POINT('Ctrl Pts',(0.158478065326005,-0.114957352860113,
1.2405905628316));
#25362=CARTESIAN_POINT('Ctrl Pts',(0.150699376209801,-0.124381903868597,
1.23989558036052));
#25363=CARTESIAN_POINT('Ctrl Pts',(0.142921783144072,-0.133805126917645,
1.23920069581543));
#25364=CARTESIAN_POINT('Ctrl Pts',(0.134250417229716,-0.142504038029514,
1.23850581127034));
#25365=CARTESIAN_POINT('Ctrl Pts',(0.124847281702347,-0.150314058728833,
1.23781092672525));
#25366=CARTESIAN_POINT('Ctrl Pts',(0.115444705137994,-0.158123615166766,
1.2371160834871));
#25367=CARTESIAN_POINT('Ctrl Pts',(0.105311136093151,-0.165043847112332,
1.23642124024895));
#25368=CARTESIAN_POINT('Ctrl Pts',(0.0946409745778109,-0.170951004474856,
1.23572639701081));
#25369=CARTESIAN_POINT('Ctrl Pts',(0.0839462210162306,-0.176871776353598,
1.23502995233326));
#25370=CARTESIAN_POINT('Ctrl Pts',(0.0727132031683232,-0.181774445238699,
1.23433350765571));
#25371=CARTESIAN_POINT('Ctrl Pts',(0.0611589772496136,-0.185582163749056,
1.23363706297816));
#25372=CARTESIAN_POINT('Ctrl Pts',(0.0573879160557474,-0.18682492458934,
1.23340975778994));
#25373=CARTESIAN_POINT('Ctrl Pts',(0.0535827550179384,-0.187951445986059,
1.23318245260173));
#25374=CARTESIAN_POINT('Ctrl Pts',(0.049751300876871,-0.188960228781241,
1.23295514741351));
#25375=CARTESIAN_POINT('Ctrl Pts',(0.0380120443523155,-0.192051055285797,
1.23225870323967));
#25376=CARTESIAN_POINT('Ctrl Pts',(0.0259421034513624,-0.194054676576599,
1.23156225906584));
#25377=CARTESIAN_POINT('Ctrl Pts',(0.0137638156624678,-0.194914641262296,
1.230865814892));
#25378=CARTESIAN_POINT('Ctrl Pts',(0.00161108776398865,-0.195772801047049,
1.23017083242092));
#25379=CARTESIAN_POINT('Ctrl Pts',(-0.010648676171227,-0.195491932984147,
1.22947584994983));
#25380=CARTESIAN_POINT('Ctrl Pts',(-0.0227853820001425,-0.194066963615932,
1.22878086747875));
#25381=CARTESIAN_POINT('Ctrl Pts',(-0.0349203777154394,-0.192642195031979,
1.22808598293366));
#25382=CARTESIAN_POINT('Ctrl Pts',(-0.0469314759806912,-0.190073701345935,
1.22739109838857));
#25383=CARTESIAN_POINT('Ctrl Pts',(-0.0585925475005012,-0.186408351147156,
1.22669621384348));
#25384=CARTESIAN_POINT('Ctrl Pts',(-0.0702529258358215,-0.182743218832635,
1.22600137060533));
#25385=CARTESIAN_POINT('Ctrl Pts',(-0.0815624912920071,-0.177981647562636,
1.22530652736718));
#25386=CARTESIAN_POINT('Ctrl Pts',(-0.0923118506849833,-0.172219865936289,
1.22461168412903));
#25387=CARTESIAN_POINT('Ctrl Pts',(-0.103085984655443,-0.166444804848336,
1.22391523945149));
#25388=CARTESIAN_POINT('Ctrl Pts',(-0.113296594269027,-0.159665401962586,
1.22321879477394));
#25389=CARTESIAN_POINT('Ctrl Pts',(-0.122761408172187,-0.152022355801973,
1.22252235009639));
#25390=CARTESIAN_POINT('Ctrl Pts',(-0.125850528349432,-0.149527823067158,
1.22229504490817));
#25391=CARTESIAN_POINT('Ctrl Pts',(-0.128860475478536,-0.146941605895026,
1.22206773971995));
#25392=CARTESIAN_POINT('Ctrl Pts',(-0.131785756567397,-0.144269450563724,
1.22184043453172));
#25393=CARTESIAN_POINT('Ctrl Pts',(-0.140615130944615,-0.13620408552787,
1.22115435940125));
#25394=CARTESIAN_POINT('Ctrl Pts',(-0.148736969234767,-0.127292292619823,
1.22046828427079));
#25395=CARTESIAN_POINT('Ctrl Pts',(-0.155985658870892,-0.11768446892693,
1.21978220914032));
#25396=CARTESIAN_POINT('Ctrl Pts',(-0.163222788613678,-0.108091967371237,
1.21909722813247));
#25397=CARTESIAN_POINT('Ctrl Pts',(-0.169588919704724,-0.0978062968135252,
1.21841224712463));
#25398=CARTESIAN_POINT('Ctrl Pts',(-0.174956910238458,-0.0870128700814545,
1.21772726611678));
#25399=CARTESIAN_POINT('Ctrl Pts',(-0.180319767440095,-0.0762297649480411,
1.21704294014642));
#25400=CARTESIAN_POINT('Ctrl Pts',(-0.184685958470788,-0.0649406667622732,
1.21635861417606));
#25401=CARTESIAN_POINT('Ctrl Pts',(-0.187974379745736,-0.0533553423679934,
1.21567428820569));
#25402=CARTESIAN_POINT('Ctrl Pts',(-0.19126753333635,-0.041753345714432,
1.21498897743252));
#25403=CARTESIAN_POINT('Ctrl Pts',(-0.193479596159008,-0.029855149983414,
1.21430366665935));
#25404=CARTESIAN_POINT('Ctrl Pts',(-0.194579881002083,-0.0178837890061103,
1.21361835588617));
#25405=CARTESIAN_POINT('Ctrl Pts',(-0.1951318539993,-0.0118781914183708,
1.21327456032826));
#25406=CARTESIAN_POINT('Ctrl Pts',(-0.195404848907981,-0.00585429143267565,
1.21293076477034));
#25407=CARTESIAN_POINT('Ctrl Pts',(-0.19539993476676,0.000159665732175137,
1.21258696921242));
#25408=CARTESIAN_POINT('',(-0.195593625707714,-0.000136366597080911,1.14258696921242));
#25409=CARTESIAN_POINT('Ctrl Pts',(-0.195527484430252,0.000159769955907059,
1.21258696921242));
#25410=CARTESIAN_POINT('Ctrl Pts',(-0.195623513973876,0.0110197689033327,
1.21196655335827));
#25411=CARTESIAN_POINT('Ctrl Pts',(-0.18985927784004,0.0866298604487836,
1.20764123321016));
#25412=CARTESIAN_POINT('Ctrl Pts',(-0.0912307526971303,0.212176946224813,
1.1996110087682));
#25413=CARTESIAN_POINT('Ctrl Pts',(0.128799216677344,0.191710376689535,
1.18849629588638));
#25414=CARTESIAN_POINT('Ctrl Pts',(0.230919855567683,-0.00425758753962621,
1.17738158300462));
#25415=CARTESIAN_POINT('Ctrl Pts',(0.121644755665287,-0.196327940360556,
1.16626687012284));
#25416=CARTESIAN_POINT('Ctrl Pts',(-0.0989901185229759,-0.208669746685701,
1.15515215724107));
#25417=CARTESIAN_POINT('Ctrl Pts',(-0.191321962564428,-0.0817735492630111,
1.1472588569376));
#25418=CARTESIAN_POINT('Ctrl Pts',(-0.195660812389172,-0.00859214891261325,
1.14307046092805));
#25419=CARTESIAN_POINT('Ctrl Pts',(-0.195593625707714,-0.000136366597080911,
1.14258696921242));
#25420=CARTESIAN_POINT('',(-0.195381487698991,-7.45427749785765E-5,1.07258697294116));
#25421=CARTESIAN_POINT('Ctrl Pts',(-0.195593625707714,-0.000136366597080911,
1.14258696921242));
#25422=CARTESIAN_POINT('Ctrl Pts',(-0.195145973734063,0.0562028893414784,
1.13936555663412));
#25423=CARTESIAN_POINT('Ctrl Pts',(-0.139964136507604,0.178102071649159,
1.1324392397619));
#25424=CARTESIAN_POINT('Ctrl Pts',(0.0669982713500039,0.221027913131385,
1.12180801859573));
#25425=CARTESIAN_POINT('Ctrl Pts',(0.222039400633985,0.0635658030166764,
1.11069330571397));
#25426=CARTESIAN_POINT('Ctrl Pts',(0.173814409632558,-0.152087664691053,
1.09957859283218));
#25427=CARTESIAN_POINT('Ctrl Pts',(-0.0335291008517759,-0.228512376345667,
1.08846387995042));
#25428=CARTESIAN_POINT('Ctrl Pts',(-0.176523953997762,-0.121039463917083,
1.07946669181885));
#25429=CARTESIAN_POINT('Ctrl Pts',(-0.195201636949265,-0.028014216980228,
1.07417440798122));
#25430=CARTESIAN_POINT('Ctrl Pts',(-0.195106173000238,-7.54145949441056E-5,
1.07258702843751));
#25431=CARTESIAN_POINT('',(-0.19539992140511,0.000175256603135645,1.00258696921242));
#25432=CARTESIAN_POINT('Ctrl Pts',(-0.195399985803746,-7.44841983129522E-5,
1.07258696921242));
#25433=CARTESIAN_POINT('Ctrl Pts',(-0.195404755662087,0.0124386430582194,
1.07187708757107));
#25434=CARTESIAN_POINT('Ctrl Pts',(-0.194203212211483,0.0249440138070227,
1.07116720592972));
#25435=CARTESIAN_POINT('Ctrl Pts',(-0.1918257233382,0.0372028475492977,
1.07045732428836));
#25436=CARTESIAN_POINT('Ctrl Pts',(-0.189439939565944,0.0495044515390223,
1.06974496591765));
#25437=CARTESIAN_POINT('Ctrl Pts',(-0.185870207066471,0.0615569932970218,
1.06903260754694));
#25438=CARTESIAN_POINT('Ctrl Pts',(-0.181197963915298,0.0731331516683816,
1.06832024917622));
#25439=CARTESIAN_POINT('Ctrl Pts',(-0.176637833436752,0.0844315346732244,
1.06762498417977));
#25440=CARTESIAN_POINT('Ctrl Pts',(-0.171028039873804,0.0952755705208773,
1.06692971918331));
#25441=CARTESIAN_POINT('Ctrl Pts',(-0.16448631462972,0.105477070017767,
1.06623445418686));
#25442=CARTESIAN_POINT('Ctrl Pts',(-0.157933494544858,0.115695871374393,
1.06553801001302));
#25443=CARTESIAN_POINT('Ctrl Pts',(-0.15040156397909,0.125337862537118,
1.06484156583919));
#25444=CARTESIAN_POINT('Ctrl Pts',(-0.142016043722388,0.13421104025169,
1.06414512166535));
#25445=CARTESIAN_POINT('Ctrl Pts',(-0.133648123064461,0.143065594868009,
1.06345013919427));
#25446=CARTESIAN_POINT('Ctrl Pts',(-0.124430709813014,0.151153857448322,
1.06275515672319));
#25447=CARTESIAN_POINT('Ctrl Pts',(-0.114529799123765,0.158316408223121,
1.0620601742521));
#25448=CARTESIAN_POINT('Ctrl Pts',(-0.10463028351506,0.165477949763969,
1.06136528970701));
#25449=CARTESIAN_POINT('Ctrl Pts',(-0.0940481430551521,0.17171348860514,
1.06067040516192));
#25450=CARTESIAN_POINT('Ctrl Pts',(-0.082981597919551,0.17690453472627,
1.05997552061683));
#25451=CARTESIAN_POINT('Ctrl Pts',(-0.0719157106272202,0.182095272269183,
1.05928067737868));
#25452=CARTESIAN_POINT('Ctrl Pts',(-0.0603662800455644,0.186241292651039,
1.05858583414053));
#25453=CARTESIAN_POINT('Ctrl Pts',(-0.0485526003242364,0.189271775502199,
1.05789099090239));
#25454=CARTESIAN_POINT('Ctrl Pts',(-0.0367116930340006,0.192309242856292,
1.05719454622484));
#25455=CARTESIAN_POINT('Ctrl Pts',(-0.0246061846279033,0.194225885336874,
1.05649810154729));
#25456=CARTESIAN_POINT('Ctrl Pts',(-0.0124654871113448,0.195001978531185,
1.05580165686974));
#25457=CARTESIAN_POINT('Ctrl Pts',(-0.00850301367579334,0.195255279353628,
1.05557435168152));
#25458=CARTESIAN_POINT('Ctrl Pts',(-0.00453680405894013,0.195387499836847,
1.0553470464933));
#25459=CARTESIAN_POINT('Ctrl Pts',(-0.000574790968387507,0.19539915459219,
1.05511974130508));
#25460=CARTESIAN_POINT('Ctrl Pts',(0.0115644873085008,0.195434863792319,
1.05442329713125));
#25461=CARTESIAN_POINT('Ctrl Pts',(0.0237500757245702,0.194335133560062,
1.05372685295741));
#25462=CARTESIAN_POINT('Ctrl Pts',(0.0357525861558755,0.192101308124559,
1.05303040878358));
#25463=CARTESIAN_POINT('Ctrl Pts',(0.0477299056197295,0.189872171060223,
1.05233542631249));
#25464=CARTESIAN_POINT('Ctrl Pts',(0.0595240438404298,0.186513748477051,
1.05164044384141));
#25465=CARTESIAN_POINT('Ctrl Pts',(0.0709110411567376,0.182079060416258,
1.05094546137032));
#25466=CARTESIAN_POINT('Ctrl Pts',(0.0822964339965533,0.177644997221929,
1.05025057682523));
#25467=CARTESIAN_POINT('Ctrl Pts',(0.093273968340728,0.172135243953825,
1.04955569228014));
#25468=CARTESIAN_POINT('Ctrl Pts',(0.103636598944045,0.165652091321876,
1.04886080773505));
#25469=CARTESIAN_POINT('Ctrl Pts',(0.113998613547812,0.159169324076539,
1.04816596449691));
#25470=CARTESIAN_POINT('Ctrl Pts',(0.123745068727093,0.151713759496613,
1.04747112125876));
#25471=CARTESIAN_POINT('Ctrl Pts',(0.132697543456127,0.14343124471575,1.04677627802061));
#25472=CARTESIAN_POINT('Ctrl Pts',(0.14167065139415,0.135129640815553,1.04607983334306));
#25473=CARTESIAN_POINT('Ctrl Pts',(0.149845527317485,0.125997923791544,
1.04538338866551));
#25474=CARTESIAN_POINT('Ctrl Pts',(0.157081194432025,0.116218149855383,
1.04468694398796));
#25475=CARTESIAN_POINT('Ctrl Pts',(0.159442767042723,0.1130262332151,1.04445963879974));
#25476=CARTESIAN_POINT('Ctrl Pts',(0.161704633833709,0.109765518630711,
1.04423233361152));
#25477=CARTESIAN_POINT('Ctrl Pts',(0.163862925475782,0.106442950234003,
1.04400502842331));
#25478=CARTESIAN_POINT('Ctrl Pts',(0.170475751392048,0.0962628772660957,
1.04330858424947));
#25479=CARTESIAN_POINT('Ctrl Pts',(0.176159692457368,0.0854281744277342,
1.04261214007564));
#25480=CARTESIAN_POINT('Ctrl Pts',(0.180791486727862,0.0741323028559712,
1.0419156959018));
#25481=CARTESIAN_POINT('Ctrl Pts',(0.185413559750507,0.0628601391522177,
1.04122071343072));
#25482=CARTESIAN_POINT('Ctrl Pts',(0.188987471086921,0.0511295016428723,
1.04052573095963));
#25483=CARTESIAN_POINT('Ctrl Pts',(0.191436320594509,0.0391573129470908,
1.03983074848855));
#25484=CARTESIAN_POINT('Ctrl Pts',(0.193884825048757,0.0271868111837602,
1.03913586394346));
#25485=CARTESIAN_POINT('Ctrl Pts',(0.195208361997676,0.0149756731820053,
1.03844097939837));
#25486=CARTESIAN_POINT('Ctrl Pts',(0.195380600836856,0.0027533282820952,
1.03774609485328));
#25487=CARTESIAN_POINT('Ctrl Pts',(0.195552829437415,-0.00946829006880504,
1.03705125161513));
#25488=CARTESIAN_POINT('Ctrl Pts',(0.19457391019337,-0.0217002379464254,
1.03635640837698));
#25489=CARTESIAN_POINT('Ctrl Pts',(0.192469630852204,-0.0337135165714957,
1.03566156513883));
#25490=CARTESIAN_POINT('Ctrl Pts',(0.190360501674904,-0.0457544827908924,
1.03496512046129));
#25491=CARTESIAN_POINT('Ctrl Pts',(0.187121049392968,-0.0575749227607743,
1.03426867578374));
#25492=CARTESIAN_POINT('Ctrl Pts',(0.182827789725607,-0.0689576631278162,
1.03357223110619));
#25493=CARTESIAN_POINT('Ctrl Pts',(0.181426558259242,-0.0726727549721334,
1.03334492591797));
#25494=CARTESIAN_POINT('Ctrl Pts',(0.179913454732605,-0.076341381240727,
1.03311762072975));
#25495=CARTESIAN_POINT('Ctrl Pts',(0.178292215374938,-0.0799565252915397,
1.03289031554153));
#25496=CARTESIAN_POINT('Ctrl Pts',(0.173324872949159,-0.0910330257070951,
1.0321938713677));
#25497=CARTESIAN_POINT('Ctrl Pts',(0.167303798950699,-0.101684065071151,
1.03149742719386));
#25498=CARTESIAN_POINT('Ctrl Pts',(0.160324697846078,-0.111701169468202,
1.03080098302003));
#25499=CARTESIAN_POINT('Ctrl Pts',(0.153360244536167,-0.121697249884283,
1.03010600054894));
#25500=CARTESIAN_POINT('Ctrl Pts',(0.145442189425305,-0.131061282235646,
1.02941101807786));
#25501=CARTESIAN_POINT('Ctrl Pts',(0.136711090177366,-0.139611023284395,
1.02871603560678));
#25502=CARTESIAN_POINT('Ctrl Pts',(0.12798122117855,-0.148159559638166,
1.02802115106169));
#25503=CARTESIAN_POINT('Ctrl Pts',(0.118439127932392,-0.155893387786925,
1.0273262665166));
#25504=CARTESIAN_POINT('Ctrl Pts',(0.108263298844997,-0.162665971005613,
1.02663138197151));
#25505=CARTESIAN_POINT('Ctrl Pts',(0.0980880746528624,-0.169438151632684,
1.02593653873336));
#25506=CARTESIAN_POINT('Ctrl Pts',(0.0872799332730697,-0.175248737806347,
1.02524169549521));
#25507=CARTESIAN_POINT('Ctrl Pts',(0.0760452638153761,-0.179995216189903,
1.02454685225706));
#25508=CARTESIAN_POINT('Ctrl Pts',(0.0647847012622126,-0.184752634015727,
1.02385040757951));
#25509=CARTESIAN_POINT('Ctrl Pts',(0.0530964795691645,-0.188440767123773,
1.02315396290196));
#25510=CARTESIAN_POINT('Ctrl Pts',(0.0412045606015807,-0.191006136513021,
1.02245751822441));
#25511=CARTESIAN_POINT('Ctrl Pts',(0.0373232833567963,-0.191843420206434,
1.02223021303619));
#25512=CARTESIAN_POINT('Ctrl Pts',(0.0334203811648193,-0.192561511747185,
1.02200290784797));
#25513=CARTESIAN_POINT('Ctrl Pts',(0.029503775479741,-0.193159745372686,
1.02177560265975));
#25514=CARTESIAN_POINT('Ctrl Pts',(0.0175036217131327,-0.19499268339903,
1.02107915848592));
#25515=CARTESIAN_POINT('Ctrl Pts',(0.00528952893680135,-0.195709558060808,
1.02038271431208));
#25516=CARTESIAN_POINT('Ctrl Pts',(-0.00691144469128197,-0.195277730251761,
1.01968627013825));
#25517=CARTESIAN_POINT('Ctrl Pts',(-0.0190868108157334,-0.194846808766465,
1.01899128766716));
#25518=CARTESIAN_POINT('Ctrl Pts',(-0.0312482434387783,-0.193271926176745,
1.01829630519608));
#25519=CARTESIAN_POINT('Ctrl Pts',(-0.0431664006990371,-0.190572353322013,
1.01760132272499));
#25520=CARTESIAN_POINT('Ctrl Pts',(-0.0550828786400965,-0.187873160848612,
1.0169064381799));
#25521=CARTESIAN_POINT('Ctrl Pts',(-0.0667552863310145,-0.184049740907001,
1.01621155363481));
#25522=CARTESIAN_POINT('Ctrl Pts',(-0.0779637136878998,-0.179172596531923,
1.01551666908972));
#25523=CARTESIAN_POINT('Ctrl Pts',(-0.0891714747674275,-0.174295742075382,
1.01482182585157));
#25524=CARTESIAN_POINT('Ctrl Pts',(-0.0999145179078746,-0.16836566148151,
1.01412698261342));
#25525=CARTESIAN_POINT('Ctrl Pts',(-0.10999479168807,-0.161500172759964,
1.01343213937528));
#25526=CARTESIAN_POINT('Ctrl Pts',(-0.120098297971212,-0.154618860808768,
1.01273569469773));
#25527=CARTESIAN_POINT('Ctrl Pts',(-0.129535298579093,-0.14679838309348,
1.01203925002018));
#25528=CARTESIAN_POINT('Ctrl Pts',(-0.138139411542142,-0.138197912353229,
1.01134280534263));
#25529=CARTESIAN_POINT('Ctrl Pts',(-0.140947616672534,-0.135390895969288,
1.01111550015441));
#25530=CARTESIAN_POINT('Ctrl Pts',(-0.143667403064424,-0.132501075392946,
1.0108881949662));
#25531=CARTESIAN_POINT('Ctrl Pts',(-0.146293915739412,-0.129534745213899,
1.01066088977798));
#25532=CARTESIAN_POINT('Ctrl Pts',(-0.154268340861462,-0.12052859111255,
1.00997076243895));
#25533=CARTESIAN_POINT('Ctrl Pts',(-0.161438925506145,-0.11074811353596,
1.00928063509993));
#25534=CARTESIAN_POINT('Ctrl Pts',(-0.167655952100067,-0.100362551409478,
1.0085905077609));
#25535=CARTESIAN_POINT('Ctrl Pts',(-0.173860147416604,-0.0899984239714956,
1.00790180477083));
#25536=CARTESIAN_POINT('Ctrl Pts',(-0.17911416591557,-0.079032407179903,
1.00721310178076));
#25537=CARTESIAN_POINT('Ctrl Pts',(-0.183310450496771,-0.0676641614052141,
1.00652439879068));
#25538=CARTESIAN_POINT('Ctrl Pts',(-0.187507835192076,-0.0562929352874952,
1.00583551524759));
#25539=CARTESIAN_POINT('Ctrl Pts',(-0.190646574248882,-0.0445200902450065,
1.00514663170449));
#25540=CARTESIAN_POINT('Ctrl Pts',(-0.192667192514708,-0.0325655174763189,
1.00445774816139));
#25541=CARTESIAN_POINT('Ctrl Pts',(-0.194496301925863,-0.0217439674946309,
1.0038341551784));
#25542=CARTESIAN_POINT('Ctrl Pts',(-0.195409742132129,-0.0107742269164684,
1.00321056219541));
#25543=CARTESIAN_POINT('Ctrl Pts',(-0.19539992140511,0.000175256603135645,
1.00258696921242));
#25544=CARTESIAN_POINT('',(-0.195715067010162,-2.931307771456E-5,0.932586969212424));
#25545=CARTESIAN_POINT('Ctrl Pts',(-0.195321343181372,0.000175890211630183,
1.00258692909733));
#25546=CARTESIAN_POINT('Ctrl Pts',(-0.195476088018098,0.017966105673101,
1.00157334503028));
#25547=CARTESIAN_POINT('Ctrl Pts',(-0.185092782119974,0.100606533622347,
0.996854856669318));
#25548=CARTESIAN_POINT('Ctrl Pts',(-0.0682974629270655,0.220629923865294,
0.988431464014426));
#25549=CARTESIAN_POINT('Ctrl Pts',(0.148337561234701,0.177025632816321,
0.97731675113265));
#25550=CARTESIAN_POINT('Ctrl Pts',(0.229176864102385,-0.0286368941625076,
0.966202038250874));
#25551=CARTESIAN_POINT('Ctrl Pts',(0.100216050899271,-0.208083756908689,
0.955087325369096));
#25552=CARTESIAN_POINT('Ctrl Pts',(-0.120487614241236,-0.197040202906743,
0.943972612487321));
#25553=CARTESIAN_POINT('Ctrl Pts',(-0.194986802068985,-0.0678687340701233,
0.93647249376843));
#25554=CARTESIAN_POINT('Ctrl Pts',(-0.195718367640748,-0.0016061582711675,
0.932677279343464));
#25555=CARTESIAN_POINT('Ctrl Pts',(-0.195715067010162,-2.931307771456E-5,
0.932586969212424));
#25556=CARTESIAN_POINT('',(-0.195399936896884,-0.000157037236289389,0.862586969212423));
#25557=CARTESIAN_POINT('Ctrl Pts',(-0.195715067010162,-2.931307771456E-5,
0.932586969212424));
#25558=CARTESIAN_POINT('Ctrl Pts',(-0.195582961786627,0.0630827139603783,
0.928972375049538));
#25559=CARTESIAN_POINT('Ctrl Pts',(-0.128138062480741,0.191126119272836,
0.921652876592728));
#25560=CARTESIAN_POINT('Ctrl Pts',(0.0899808947771039,0.212710002872902,
0.910628473841993));
#25561=CARTESIAN_POINT('Ctrl Pts',(0.227513576082653,0.0397451814080767,
0.899513760960215));
#25562=CARTESIAN_POINT('Ctrl Pts',(0.156768799466018,-0.16960439340141,
0.888399048078441));
#25563=CARTESIAN_POINT('Ctrl Pts',(-0.0574900812163511,-0.223689510949474,
0.877284335196663));
#25564=CARTESIAN_POINT('Ctrl Pts',(-0.182608995805481,-0.107037763309046,
0.868680334011459));
#25565=CARTESIAN_POINT('Ctrl Pts',(-0.195393515914344,-0.0211417834289091,
0.86378123712018));
#25566=CARTESIAN_POINT('Ctrl Pts',(-0.195235485275365,-0.000158228367462752,
0.862587044522825));
#25567=CARTESIAN_POINT('',(-0.195399964130102,0.000118397444788799,0.792586969212424));
#25568=CARTESIAN_POINT('Ctrl Pts',(-0.195399936896884,-0.000157037236289389,
0.862586969212423));
#25569=CARTESIAN_POINT('Ctrl Pts',(-0.195409734496894,0.0120340231065371,
0.861893744600403));
#25570=CARTESIAN_POINT('Ctrl Pts',(-0.194274282005615,0.0242406068532915,
0.861200519988384));
#25571=CARTESIAN_POINT('Ctrl Pts',(-0.19201123716182,0.0362332002945821,
0.860507295376365));
#25572=CARTESIAN_POINT('Ctrl Pts',(-0.18974885363775,0.048222289192595,
0.85981427334235));
#25573=CARTESIAN_POINT('Ctrl Pts',(-0.186359709838977,0.0599966493212796,
0.859121251308335));
#25574=CARTESIAN_POINT('Ctrl Pts',(-0.181912610531916,0.0713369618743564,
0.858428229274321));
#25575=CARTESIAN_POINT('Ctrl Pts',(-0.177454434501244,0.0827055205940107,
0.857733481078376));
#25576=CARTESIAN_POINT('Ctrl Pts',(-0.171933407141078,0.0936370683755064,
0.85703873288243));
#25577=CARTESIAN_POINT('Ctrl Pts',(-0.165466127853881,0.103933250372743,
0.856343984686485));
#25578=CARTESIAN_POINT('Ctrl Pts',(-0.161466208777956,0.110301290618271,
0.85591429293536));
#25579=CARTESIAN_POINT('Ctrl Pts',(-0.157105246349051,0.116426790052616,
0.855484601184236));
#25580=CARTESIAN_POINT('Ctrl Pts',(-0.152418652238814,0.1222690248988,0.855054909433111));
#25581=CARTESIAN_POINT('Ctrl Pts',(-0.144822622865053,0.131738116195417,
0.854358465259276));
#25582=CARTESIAN_POINT('Ctrl Pts',(-0.136313921779505,0.140530156770072,
0.853662021085441));
#25583=CARTESIAN_POINT('Ctrl Pts',(-0.12703765742528,0.148467483294818,
0.852965576911606));
#25584=CARTESIAN_POINT('Ctrl Pts',(-0.117780862170854,0.156388150893478,
0.852270594440521));
#25585=CARTESIAN_POINT('Ctrl Pts',(-0.107760311345287,0.163457044708525,
0.851575611969437));
#25586=CARTESIAN_POINT('Ctrl Pts',(-0.0971579177599562,0.169533179692205,
0.850880629498353));
#25587=CARTESIAN_POINT('Ctrl Pts',(-0.0865570180971057,0.175608458522548,
0.850185744953263));
#25588=CARTESIAN_POINT('Ctrl Pts',(-0.0753751741160683,0.180690781469455,
0.849490860408173));
#25589=CARTESIAN_POINT('Ctrl Pts',(-0.0638220178270438,0.184683269519696,
0.848795975863083));
#25590=CARTESIAN_POINT('Ctrl Pts',(-0.0522695483075639,0.18867552023919,
0.848101132624934));
#25591=CARTESIAN_POINT('Ctrl Pts',(-0.0403466467615257,0.191577803907368,
0.847406289386786));
#25592=CARTESIAN_POINT('Ctrl Pts',(-0.0282788635343871,0.193342871286229,
0.846711446148637));
#25593=CARTESIAN_POINT('Ctrl Pts',(-0.016183267093484,0.195112006702725,
0.846015001471089));
#25594=CARTESIAN_POINT('Ctrl Pts',(-0.00394299772200419,0.195738630897938,
0.845318556793542));
#25595=CARTESIAN_POINT('Ctrl Pts',(0.00821173275305,0.19522737370869,0.844622112115994));
#25596=CARTESIAN_POINT('Ctrl Pts',(0.0121787862570268,0.195060509899723,
0.844394806927775));
#25597=CARTESIAN_POINT('Ctrl Pts',(0.0161367594936829,0.194772848920495,
0.844167501739555));
#25598=CARTESIAN_POINT('Ctrl Pts',(0.0200778185584785,0.194365740813377,
0.843940196551335));
#25599=CARTESIAN_POINT('Ctrl Pts',(0.0321528954448271,0.193118395464401,
0.8432437523775));
#25600=CARTESIAN_POINT('Ctrl Pts',(0.0441540321893043,0.190737074723704,
0.842547308203665));
#25601=CARTESIAN_POINT('Ctrl Pts',(0.0558532672044756,0.187247356570354,
0.841850864029829));
#25602=CARTESIAN_POINT('Ctrl Pts',(0.067527947769125,0.183764962666122,
0.841155881558745));
#25603=CARTESIAN_POINT('Ctrl Pts',(0.0789011322020904,0.179178965013493,
0.84046089908766));
#25604=CARTESIAN_POINT('Ctrl Pts',(0.0897557179776617,0.173565754370828,
0.839765916616576));
#25605=CARTESIAN_POINT('Ctrl Pts',(0.100608774295799,0.167953334653484,
0.839071032071486));
#25606=CARTESIAN_POINT('Ctrl Pts',(0.11094257919104,0.161314349961526,0.838376147526397));
#25607=CARTESIAN_POINT('Ctrl Pts',(0.120562056665277,0.153772398344562,
0.837681262981307));
#25608=CARTESIAN_POINT('Ctrl Pts',(0.130180962316199,0.146230895053796,
0.836986419743158));
#25609=CARTESIAN_POINT('Ctrl Pts',(0.139084952155297,0.137787092787488,
0.836291576505009));
#25610=CARTESIAN_POINT('Ctrl Pts',(0.147112017075362,0.128604877170418,
0.835596733266859));
#25611=CARTESIAN_POINT('Ctrl Pts',(0.155157582366897,0.119401498849231,
0.834900288589311));
#25612=CARTESIAN_POINT('Ctrl Pts',(0.162321660730657,0.109457011262306,
0.834203843911763));
#25613=CARTESIAN_POINT('Ctrl Pts',(0.168483304121249,0.0989673493248495,
0.833507399234215));
#25614=CARTESIAN_POINT('Ctrl Pts',(0.170494337525317,0.0955437398725704,
0.833280094045996));
#25615=CARTESIAN_POINT('Ctrl Pts',(0.172398952993282,0.0920622544280945,
0.833052788857778));
#25616=CARTESIAN_POINT('Ctrl Pts',(0.174194036704551,0.08853020714182,0.832825483669559));
#25617=CARTESIAN_POINT('Ctrl Pts',(0.179694023757454,0.0777083082950995,
0.832129039495724));
#25618=CARTESIAN_POINT('Ctrl Pts',(0.184201147367978,0.066333607930296,
0.831432595321889));
#25619=CARTESIAN_POINT('Ctrl Pts',(0.187613280394586,0.0546115099551607,
0.830736151148054));
#25620=CARTESIAN_POINT('Ctrl Pts',(0.191018252008375,0.0429140144155199,
0.83004116867697));
#25621=CARTESIAN_POINT('Ctrl Pts',(0.193332480626411,0.0308713799645606,
0.829346186205886));
#25622=CARTESIAN_POINT('Ctrl Pts',(0.194502420663427,0.0187074411950771,
0.828651203734802));
#25623=CARTESIAN_POINT('Ctrl Pts',(0.195672195850902,0.00654521637644226,
0.827956319189712));
#25624=CARTESIAN_POINT('Ctrl Pts',(0.195697872942552,-0.00573741290396437,
0.827261434644622));
#25625=CARTESIAN_POINT('Ctrl Pts',(0.194577514407471,-0.0179095194522505,
0.826566550099533));
#25626=CARTESIAN_POINT('Ctrl Pts',(0.193457222471343,-0.0300809024379134,
0.825871706861383));
#25627=CARTESIAN_POINT('Ctrl Pts',(0.191191137051048,-0.0421409061126653,
0.825176863623234));
#25628=CARTESIAN_POINT('Ctrl Pts',(0.18782910162498,-0.0538645391955886,
0.824482020385085));
#25629=CARTESIAN_POINT('Ctrl Pts',(0.184459317550445,-0.0656151923125061,
0.823785575707537));
#25630=CARTESIAN_POINT('Ctrl Pts',(0.179988844497181,-0.0770271037583809,
0.82308913102999));
#25631=CARTESIAN_POINT('Ctrl Pts',(0.174516720171798,-0.0878924022909733,
0.822392686352442));
#25632=CARTESIAN_POINT('Ctrl Pts',(0.172730731578815,-0.0914386117856203,
0.822165381164222));
#25633=CARTESIAN_POINT('Ctrl Pts',(0.170838407752911,-0.0949267934779921,
0.821938075976002));
#25634=CARTESIAN_POINT('Ctrl Pts',(0.168844205506616,-0.0983503648536164,
0.821710770787783));
#25635=CARTESIAN_POINT('Ctrl Pts',(0.162734135838796,-0.108839902540525,
0.821014326613947));
#25636=CARTESIAN_POINT('Ctrl Pts',(0.15562119694151,-0.118795005346275,
0.820317882440112));
#25637=CARTESIAN_POINT('Ctrl Pts',(0.147622588480279,-0.128018480581446,
0.819621438266277));
#25638=CARTESIAN_POINT('Ctrl Pts',(0.139640767564166,-0.137222597511057,
0.818926455795193));
#25639=CARTESIAN_POINT('Ctrl Pts',(0.130777478205338,-0.145697430863864,
0.818231473324109));
#25640=CARTESIAN_POINT('Ctrl Pts',(0.121191750101413,-0.153276611742811,
0.817536490853024));
#25641=CARTESIAN_POINT('Ctrl Pts',(0.111607372667467,-0.160854724682844,
0.816841606307935));
#25642=CARTESIAN_POINT('Ctrl Pts',(0.101301415844516,-0.167536857225407,
0.816146721762845));
#25643=CARTESIAN_POINT('Ctrl Pts',(0.0904668542828406,-0.173196155488993,
0.815451837217755));
#25644=CARTESIAN_POINT('Ctrl Pts',(0.0796329367743329,-0.178855117339429,
0.814756993979606));
#25645=CARTESIAN_POINT('Ctrl Pts',(0.0682712655334758,-0.183490983858409,
0.814062150741457));
#25646=CARTESIAN_POINT('Ctrl Pts',(0.0565979073780773,-0.187023626529972,
0.813367307503308));
#25647=CARTESIAN_POINT('Ctrl Pts',(0.0448976450597862,-0.190564411056914,
0.812670862825761));
#25648=CARTESIAN_POINT('Ctrl Pts',(0.0328851181857995,-0.192996704269116,
0.811974418148213));
#25649=CARTESIAN_POINT('Ctrl Pts',(0.0207886860788731,-0.194290994467356,
0.811277973470666));
#25650=CARTESIAN_POINT('Ctrl Pts',(0.0168406599606547,-0.19471342411124,
0.811050668282446));
#25651=CARTESIAN_POINT('Ctrl Pts',(0.0128837259739765,-0.195015043749426,
0.810823363094226));
#25652=CARTESIAN_POINT('Ctrl Pts',(0.00892583157243448,-0.195196028470716,
0.810596057906007));
#25653=CARTESIAN_POINT('Ctrl Pts',(-0.00320082738417567,-0.195750550589998,
0.809899613732172));
#25654=CARTESIAN_POINT('Ctrl Pts',(-0.0154222840393251,-0.195172650204224,
0.809203169558337));
#25655=CARTESIAN_POINT('Ctrl Pts',(-0.0275093024339257,-0.193453866023915,
0.808506725384502));
#25656=CARTESIAN_POINT('Ctrl Pts',(-0.0395709524950678,-0.191738689241957,
0.807811742913417));
#25657=CARTESIAN_POINT('Ctrl Pts',(-0.0514978555606483,-0.188887429541335,
0.807116760442333));
#25658=CARTESIAN_POINT('Ctrl Pts',(-0.0630639904949814,-0.184943486240659,
0.806421777971249));
#25659=CARTESIAN_POINT('Ctrl Pts',(-0.0746284957115704,-0.181000098658416,
0.805726893426159));
#25660=CARTESIAN_POINT('Ctrl Pts',(-0.0858314912680433,-0.175964571683546,
0.805032008881069));
#25661=CARTESIAN_POINT('Ctrl Pts',(-0.0964617491077431,-0.169930253219004,
0.804337124335979));
#25662=CARTESIAN_POINT('Ctrl Pts',(-0.10709137503898,-0.163896293460428,
0.80364228109783));
#25663=CARTESIAN_POINT('Ctrl Pts',(-0.117147582437623,-0.156864115666681,
0.80294743785968));
#25664=CARTESIAN_POINT('Ctrl Pts',(-0.126445879661726,-0.14897180779118,
0.80225259462153));
#25665=CARTESIAN_POINT('Ctrl Pts',(-0.135765607128928,-0.141061310125409,
0.801556149943982));
#25666=CARTESIAN_POINT('Ctrl Pts',(-0.144323311928957,-0.132287340628995,
0.800859705266435));
#25667=CARTESIAN_POINT('Ctrl Pts',(-0.1519703648202,-0.122825763650853,
0.800163260588887));
#25668=CARTESIAN_POINT('Ctrl Pts',(-0.154466205269271,-0.119737699939265,
0.799935955400668));
#25669=CARTESIAN_POINT('Ctrl Pts',(-0.156865371508102,-0.116576639620415,
0.79970865021245));
#25670=CARTESIAN_POINT('Ctrl Pts',(-0.159163700943832,-0.11334935510122,
0.799481345024231));
#25671=CARTESIAN_POINT('Ctrl Pts',(-0.16627106320176,-0.103369288784035,
0.798778425638236));
#25672=CARTESIAN_POINT('Ctrl Pts',(-0.17246084605519,-0.092683670684521,
0.79807550625224));
#25673=CARTESIAN_POINT('Ctrl Pts',(-0.177599482383803,-0.0814836416528211,
0.797372586866245));
#25674=CARTESIAN_POINT('Ctrl Pts',(-0.18272618655519,-0.070309619619629,
0.796671299692396));
#25675=CARTESIAN_POINT('Ctrl Pts',(-0.186806164619108,-0.0586242921696647,
0.795970012518547));
#25676=CARTESIAN_POINT('Ctrl Pts',(-0.189751053307921,-0.0466443755294713,
0.795268725344698));
#25677=CARTESIAN_POINT('Ctrl Pts',(-0.192692582140228,-0.0346781269104265,
0.794568238277245));
#25678=CARTESIAN_POINT('Ctrl Pts',(-0.194501349927928,-0.0224187725981258,
0.793867751209792));
#25679=CARTESIAN_POINT('Ctrl Pts',(-0.195138918234439,-0.0100976527120339,
0.793167264142338));
#25680=CARTESIAN_POINT('Ctrl Pts',(-0.19531497556794,-0.00669531371441858,
0.792973832499034));
#25681=CARTESIAN_POINT('Ctrl Pts',(-0.195402028337336,-0.00328831475456294,
0.792780400855729));
#25682=CARTESIAN_POINT('Ctrl Pts',(-0.195399964130102,0.000118397444788799,
0.792586969212424));
#25683=CARTESIAN_POINT('',(-0.195665606136028,9.31787759667347E-5,0.722586969212424));
#25684=CARTESIAN_POINT('Ctrl Pts',(-0.195153759558878,0.000119703465488583,
0.792586886482477));
#25685=CARTESIAN_POINT('Ctrl Pts',(-0.195290253173666,0.024864238661261,
0.791180135035802));
#25686=CARTESIAN_POINT('Ctrl Pts',(-0.179437438454886,0.114608714513428,
0.786068479295203));
#25687=CARTESIAN_POINT('Ctrl Pts',(-0.0445992966086936,0.226612024149397,
0.777251919260677));
#25688=CARTESIAN_POINT('Ctrl Pts',(0.166214644641796,0.16035834450904,0.766137206378902));
#25689=CARTESIAN_POINT('Ctrl Pts',(0.224867276437698,-0.0526954906473987,
0.755022493497125));
#25690=CARTESIAN_POINT('Ctrl Pts',(0.0776650071207437,-0.217509203060494,
0.74390778061535));
#25691=CARTESIAN_POINT('Ctrl Pts',(-0.134687138099445,-0.184138771498097,
0.733095939187116));
#25692=CARTESIAN_POINT('Ctrl Pts',(-0.195315412358655,-0.0593474407707721,
0.725989002052807));
#25693=CARTESIAN_POINT('Ctrl Pts',(-0.195665606136028,9.31787759667347E-5,
0.722586969212424));
#25694=CARTESIAN_POINT('',(-0.195399920232252,-0.000176559421619332,0.652586969212424));
#25695=CARTESIAN_POINT('Ctrl Pts',(-0.195665606136028,9.31787759667347E-5,
0.722586969212424));
#25696=CARTESIAN_POINT('Ctrl Pts',(-0.195696782701144,0.0053849756768864,
0.722284097758882));
#25697=CARTESIAN_POINT('Ctrl Pts',(-0.19310225815126,0.0753781479809831,
0.718276322011416));
#25698=CARTESIAN_POINT('Ctrl Pts',(-0.109018190962289,0.203610266898278,
0.71056364197002));
#25699=CARTESIAN_POINT('Ctrl Pts',(0.111955804692466,0.202009911991322,
0.699448929088245));
#25700=CARTESIAN_POINT('Ctrl Pts',(0.230439782817406,0.015479445795746,
0.688334216206469));
#25701=CARTESIAN_POINT('Ctrl Pts',(0.137967505075176,-0.185221689578759,
0.677219503324693));
#25702=CARTESIAN_POINT('Ctrl Pts',(-0.080807218998807,-0.216361503287337,
0.666104790442915));
#25703=CARTESIAN_POINT('Ctrl Pts',(-0.18777605090878,-0.0930453392534147,
0.657893945738827));
#25704=CARTESIAN_POINT('Ctrl Pts',(-0.195562463745895,-0.0142157590911969,
0.653388005328663));
#25705=CARTESIAN_POINT('Ctrl Pts',(-0.195432764861167,-0.000176589099362662,
0.652586969212424));
#25706=CARTESIAN_POINT('',(-0.195368572466251,1.52014745227871E-5,0.582586968017739));
#25707=CARTESIAN_POINT('Ctrl Pts',(-0.195399920232252,-0.000176559421619332,
0.652586969212424));
#25708=CARTESIAN_POINT('Ctrl Pts',(-0.195410776640569,0.0118383265557513,
0.651901311615086));
#25709=CARTESIAN_POINT('Ctrl Pts',(-0.19430915187813,0.0238869003000631,
0.651215654017748));
#25710=CARTESIAN_POINT('Ctrl Pts',(-0.192102813592723,0.0357444962163329,
0.65052999642041));
#25711=CARTESIAN_POINT('Ctrl Pts',(-0.189897203385873,0.0475981791962381,
0.649844565086015));
#25712=CARTESIAN_POINT('Ctrl Pts',(-0.18658771446154,0.0592601148205221,
0.649159133751619));
#25713=CARTESIAN_POINT('Ctrl Pts',(-0.182233720267025,0.0705126314757841,
0.648473702417224));
#25714=CARTESIAN_POINT('Ctrl Pts',(-0.177880280221303,0.081763715982024,
0.647788358320186));
#25715=CARTESIAN_POINT('Ctrl Pts',(-0.172482949831443,0.0926046537378351,
0.647103014223148));
#25716=CARTESIAN_POINT('Ctrl Pts',(-0.166149261678216,0.10283765285042,
0.646417670126111));
#25717=CARTESIAN_POINT('Ctrl Pts',(-0.159801609071076,0.11309321357972,
0.645730814989087));
#25718=CARTESIAN_POINT('Ctrl Pts',(-0.152514017080856,0.122737435692944,
0.645043959852063));
#25719=CARTESIAN_POINT('Ctrl Pts',(-0.144436353403315,0.131602810819346,
0.644357104715039));
#25720=CARTESIAN_POINT('Ctrl Pts',(-0.142547874655067,0.133675448798569,
0.644196524703148));
#25721=CARTESIAN_POINT('Ctrl Pts',(-0.14061636936524,0.135705677700539,
0.644035944691256));
#25722=CARTESIAN_POINT('Ctrl Pts',(-0.138644023767034,0.137691665229549,
0.643875364679365));
#25723=CARTESIAN_POINT('Ctrl Pts',(-0.130089854512213,0.146305000274161,
0.643178920505529));
#25724=CARTESIAN_POINT('Ctrl Pts',(-0.120699673502432,0.154148626491242,
0.642482476331694));
#25725=CARTESIAN_POINT('Ctrl Pts',(-0.110636551736313,0.16106121016526,
0.641786032157858));
#25726=CARTESIAN_POINT('Ctrl Pts',(-0.100594550532793,0.167959285651899,
0.641091049686774));
#25727=CARTESIAN_POINT('Ctrl Pts',(-0.0898830842274528,0.173929644787307,
0.64039606721569));
#25728=CARTESIAN_POINT('Ctrl Pts',(-0.0786979460104241,0.178851316164406,
0.639701084744605));
#25729=CARTESIAN_POINT('Ctrl Pts',(-0.0675143838270778,0.183772294057016,
0.639006200199515));
#25730=CARTESIAN_POINT('Ctrl Pts',(-0.0558580639667775,0.187644483188165,
0.638311315654425));
#25731=CARTESIAN_POINT('Ctrl Pts',(-0.04394768256483,0.190393700518638,
0.637616431109335));
#25732=CARTESIAN_POINT('Ctrl Pts',(-0.0320380091674312,0.193142754423751,
0.636921587871186));
#25733=CARTESIAN_POINT('Ctrl Pts',(-0.019875163546431,0.194768798139928,
0.636226744633037));
#25734=CARTESIAN_POINT('Ctrl Pts',(-0.00768842626097916,0.195248682714198,
0.635531901394887));
#25735=CARTESIAN_POINT('Ctrl Pts',(0.00452639839750962,0.195729673302058,
0.634835456717339));
#25736=CARTESIAN_POINT('Ctrl Pts',(0.0167643475810499,0.195059261525867,
0.634139012039792));
#25737=CARTESIAN_POINT('Ctrl Pts',(0.0287969878279878,0.193266379621585,
0.633442567362243));
#25738=CARTESIAN_POINT('Ctrl Pts',(0.0327241935979091,0.192681219921404,
0.633215262174025));
#25739=CARTESIAN_POINT('Ctrl Pts',(0.0366296043435642,0.191976899050893,
0.632987956985806));
#25740=CARTESIAN_POINT('Ctrl Pts',(0.0405055726968939,0.191155587364054,
0.632760651797587));
#25741=CARTESIAN_POINT('Ctrl Pts',(0.0523812170620796,0.188639156728729,
0.632064207623752));
#25742=CARTESIAN_POINT('Ctrl Pts',(0.0640634990743473,0.185002914352939,
0.631367763449917));
#25743=CARTESIAN_POINT('Ctrl Pts',(0.0753284366688527,0.180296385512929,
0.630671319276082));
#25744=CARTESIAN_POINT('Ctrl Pts',(0.0865697313198354,0.175599734774294,
0.629976336804997));
#25745=CARTESIAN_POINT('Ctrl Pts',(0.0973945914643227,0.169837521530361,
0.629281354333913));
#25746=CARTESIAN_POINT('Ctrl Pts',(0.107595203085472,0.163108651741702,
0.628586371862828));
#25747=CARTESIAN_POINT('Ctrl Pts',(0.117794377396932,0.1563807300795,0.627891487317738));
#25748=CARTESIAN_POINT('Ctrl Pts',(0.127368722555747,0.148686865242318,
0.627196602772649));
#25749=CARTESIAN_POINT('Ctrl Pts',(0.136137316504897,0.140170578420885,
0.626501718227559));
#25750=CARTESIAN_POINT('Ctrl Pts',(0.144905389210927,0.131654797844346,
0.62580687498941));
#25751=CARTESIAN_POINT('Ctrl Pts',(0.152867196198784,0.122317321672737,
0.62511203175126));
#25752=CARTESIAN_POINT('Ctrl Pts',(0.159878954651258,0.11233823863503,0.624417188513111));
#25753=CARTESIAN_POINT('Ctrl Pts',(0.16690687344843,0.102336156313655,0.623720743835563));
#25754=CARTESIAN_POINT('Ctrl Pts',(0.172979922348,0.0916902684111838,0.623024299158015));
#25755=CARTESIAN_POINT('Ctrl Pts',(0.177998536573932,0.0806081942332073,
0.622327854480467));
#25756=CARTESIAN_POINT('Ctrl Pts',(0.179636508817812,0.0769912336359282,
0.622100549292249));
#25757=CARTESIAN_POINT('Ctrl Pts',(0.181162542804326,0.0733279671628344,
0.62187324410403));
#25758=CARTESIAN_POINT('Ctrl Pts',(0.182574315093772,0.0696259970703467,
0.621645938915812));
#25759=CARTESIAN_POINT('Ctrl Pts',(0.186899867860399,0.0582834688912404,
0.620949494741977));
#25760=CARTESIAN_POINT('Ctrl Pts',(0.190179697863685,0.0464961584779568,
0.620253050568142));
#25761=CARTESIAN_POINT('Ctrl Pts',(0.192333956506123,0.0344791121507029,
0.619556606394306));
#25762=CARTESIAN_POINT('Ctrl Pts',(0.194483693772832,0.0224872872989626,
0.618861623923222));
#25763=CARTESIAN_POINT('Ctrl Pts',(0.195512322176856,0.0102675237078589,
0.618166641452139));
#25764=CARTESIAN_POINT('Ctrl Pts',(0.195390250357663,-0.00195193882324224,
0.617471658981055));
#25765=CARTESIAN_POINT('Ctrl Pts',(0.195268195738911,-0.0141696795799548,
0.616776774435965));
#25766=CARTESIAN_POINT('Ctrl Pts',(0.193995725410556,-0.0263862445888409,
0.616081889890875));
#25767=CARTESIAN_POINT('Ctrl Pts',(0.19159531661398,-0.0383717950008675,
0.615387005345786));
#25768=CARTESIAN_POINT('Ctrl Pts',(0.189195050508078,-0.050356632939979,
0.614692162107637));
#25769=CARTESIAN_POINT('Ctrl Pts',(0.185667177242148,-0.0621096300890771,
0.613997318869487));
#25770=CARTESIAN_POINT('Ctrl Pts',(0.181085037818701,-0.073412322386637,
0.613302475631338));
#25771=CARTESIAN_POINT('Ctrl Pts',(0.176492337713076,-0.0847410645552472,
0.612606030953791));
#25772=CARTESIAN_POINT('Ctrl Pts',(0.170840909584216,-0.0956166432650318,
0.611909586276243));
#25773=CARTESIAN_POINT('Ctrl Pts',(0.164251203983628,-0.105842817375241,
0.611213141598696));
#25774=CARTESIAN_POINT('Ctrl Pts',(0.162100459897061,-0.109180429831521,
0.610985836410476));
#25775=CARTESIAN_POINT('Ctrl Pts',(0.159850108273844,-0.112449102123599,
0.610758531222256));
#25776=CARTESIAN_POINT('Ctrl Pts',(0.157505276597089,-0.115642759583445,
0.610531226034036));
#25777=CARTESIAN_POINT('Ctrl Pts',(0.150320907543799,-0.125427860172448,
0.6098347818602));
#25778=CARTESIAN_POINT('Ctrl Pts',(0.142195762931484,-0.134575537290636,
0.609138337686365));
#25779=CARTESIAN_POINT('Ctrl Pts',(0.133267225082851,-0.142902087873889,
0.60844189351253));
#25780=CARTESIAN_POINT('Ctrl Pts',(0.124357426522772,-0.151211162624404,
0.607746911041446));
#25781=CARTESIAN_POINT('Ctrl Pts',(0.114648164614459,-0.158701885674412,
0.607051928570361));
#25782=CARTESIAN_POINT('Ctrl Pts',(0.104315160084808,-0.165225625665273,
0.606356946099277));
#25783=CARTESIAN_POINT('Ctrl Pts',(0.0939836115195674,-0.171748446433344,
0.605662061554187));
#25784=CARTESIAN_POINT('Ctrl Pts',(0.0830292095313433,-0.177304048869929,
0.604967177009097));
#25785=CARTESIAN_POINT('Ctrl Pts',(0.0716572538540142,-0.181786682598317,
0.604272292464007));
#25786=CARTESIAN_POINT('Ctrl Pts',(0.0602859741748835,-0.186269049859581,
0.603577449225858));
#25787=CARTESIAN_POINT('Ctrl Pts',(0.0484980146352318,-0.189678278754606,
0.602882605987709));
#25788=CARTESIAN_POINT('Ctrl Pts',(0.036516699986673,-0.191957522962981,
0.60218776274956));
#25789=CARTESIAN_POINT('Ctrl Pts',(0.0245077714127372,-0.194242020257626,
0.601491318072013));
#25790=CARTESIAN_POINT('Ctrl Pts',(0.0123054699786841,-0.195391233850034,
0.600794873394465));
#25791=CARTESIAN_POINT('Ctrl Pts',(0.000139995024282486,-0.195399949850027,
0.600098428716917));
#25792=CARTESIAN_POINT('Ctrl Pts',(-0.00383056525628826,-0.195402794572778,
0.599871123528698));
#25793=CARTESIAN_POINT('Ctrl Pts',(-0.007797216565637,-0.195284564411506,
0.599643818340479));
#25794=CARTESIAN_POINT('Ctrl Pts',(-0.0117520744557401,-0.195046273345549,
0.59941651315226));
#25795=CARTESIAN_POINT('Ctrl Pts',(-0.023869429794117,-0.194316169356887,
0.598720068978424));
#25796=CARTESIAN_POINT('Ctrl Pts',(-0.0359613798620174,-0.192449965942189,
0.598023624804589));
#25797=CARTESIAN_POINT('Ctrl Pts',(-0.047799078157251,-0.189463474388382,
0.597327180630754));
#25798=CARTESIAN_POINT('Ctrl Pts',(-0.0596119313940944,-0.186483250907572,
0.59663219815967));
#25799=CARTESIAN_POINT('Ctrl Pts',(-0.0711707331989876,-0.182387545907051,
0.595937215688586));
#25800=CARTESIAN_POINT('Ctrl Pts',(-0.0822553144165228,-0.177243401147233,
0.595242233217501));
#25801=CARTESIAN_POINT('Ctrl Pts',(-0.0933383337692836,-0.172099981219354,
0.594547348672412));
#25802=CARTESIAN_POINT('Ctrl Pts',(-0.103946452668831,-0.165908741055547,
0.593852464127323));
#25803=CARTESIAN_POINT('Ctrl Pts',(-0.113879490669761,-0.158784828005687,
0.593157579582233));
#25804=CARTESIAN_POINT('Ctrl Pts',(-0.123811938207988,-0.151661338432005,
0.592462736344084));
#25805=CARTESIAN_POINT('Ctrl Pts',(-0.133068688445595,-0.143605818162909,
0.591767893105934));
#25806=CARTESIAN_POINT('Ctrl Pts',(-0.141480875677578,-0.134775078621775,
0.591073049867785));
#25807=CARTESIAN_POINT('Ctrl Pts',(-0.149912450891368,-0.125923986440734,
0.590376605190237));
#25808=CARTESIAN_POINT('Ctrl Pts',(-0.15749502048588,-0.11629478655119,
0.58968016051269));
#25809=CARTESIAN_POINT('Ctrl Pts',(-0.164099372475197,-0.106078065372849,
0.588983715835142));
#25810=CARTESIAN_POINT('Ctrl Pts',(-0.166254896841161,-0.102743538158704,
0.588756410646923));
#25811=CARTESIAN_POINT('Ctrl Pts',(-0.168306574198394,-0.0993466394256172,
0.588529105458703));
#25812=CARTESIAN_POINT('Ctrl Pts',(-0.170250980957266,-0.095894543552221,
0.588301800270483));
#25813=CARTESIAN_POINT('Ctrl Pts',(-0.176472841648792,-0.0848482645161776,
0.587574451834201));
#25814=CARTESIAN_POINT('Ctrl Pts',(-0.181633608107616,-0.0731628494365437,
0.586847103397918));
#25815=CARTESIAN_POINT('Ctrl Pts',(-0.185615753856331,-0.0610569563632686,
0.586119754961635));
#25816=CARTESIAN_POINT('Ctrl Pts',(-0.189582653754339,-0.0489974113269807,
0.585395191216413));
#25817=CARTESIAN_POINT('Ctrl Pts',(-0.192379592139015,-0.0365212802349419,
0.584670627471192));
#25818=CARTESIAN_POINT('Ctrl Pts',(-0.193936890827428,-0.0238671819909773,
0.58394606372597));
#25819=CARTESIAN_POINT('Ctrl Pts',(-0.194910587582813,-0.0159552415943475,
0.583493032221454));
#25820=CARTESIAN_POINT('Ctrl Pts',(-0.195400620193043,-0.00797414202748591,
0.583040000716939));
#25821=CARTESIAN_POINT('Ctrl Pts',(-0.195399999410133,1.51828823620237E-5,
0.582586969212423));
#25822=CARTESIAN_POINT('',(-0.195488415809582,0.000168817958016994,0.512586969212423));
#25823=CARTESIAN_POINT('Ctrl Pts',(-0.195080329228051,1.5371999046063E-5,
0.582586957060278));
#25824=CARTESIAN_POINT('Ctrl Pts',(-0.195102226640896,0.0317061316006451,
0.580787000503088));
#25825=CARTESIAN_POINT('Ctrl Pts',(-0.172828823719728,0.128597837672465,
0.57528213965197));
#25826=CARTESIAN_POINT('Ctrl Pts',(-0.0204016541079559,0.230056252374797,
0.566072374506932));
#25827=CARTESIAN_POINT('Ctrl Pts',(0.182230257970378,0.141895171965532,
0.554957661625154));
#25828=CARTESIAN_POINT('Ctrl Pts',(0.218039356482699,-0.0761639401008706,
0.543842948743379));
#25829=CARTESIAN_POINT('Ctrl Pts',(0.0542441778475854,-0.224498721414439,
0.532728235861602));
#25830=CARTESIAN_POINT('Ctrl Pts',(-0.145841485605917,-0.170897033639993,
0.52230957601795));
#25831=CARTESIAN_POINT('Ctrl Pts',(-0.195008257896402,-0.052526494143854,
0.515595820468224));
#25832=CARTESIAN_POINT('Ctrl Pts',(-0.195488415809582,0.000168817958016994,
0.512586969212423));
#25833=CARTESIAN_POINT('',(-0.195399963336573,-0.000119699900101725,0.442586969212423));
#25834=CARTESIAN_POINT('Ctrl Pts',(-0.195488415809582,0.000168817958016994,
0.512586969212423));
#25835=CARTESIAN_POINT('Ctrl Pts',(-0.195599493209505,0.0123590955640317,
0.511890916174299));
#25836=CARTESIAN_POINT('Ctrl Pts',(-0.189008463564054,0.0893152196074113,
0.507489958842245));
#25837=CARTESIAN_POINT('Ctrl Pts',(-0.086890608201959,0.213990955307397,
0.499384097216276));
#25838=CARTESIAN_POINT('Ctrl Pts',(0.132676899813103,0.189047472881976,
0.488269384334496));
#25839=CARTESIAN_POINT('Ctrl Pts',(0.230785249680916,-0.00895964713562786,
0.477154671452722));
#25840=CARTESIAN_POINT('Ctrl Pts',(0.117621085806451,-0.198764652090832,
0.466039958570945));
#25841=CARTESIAN_POINT('Ctrl Pts',(-0.103219381045709,-0.206610421139929,
0.454925245689168));
#25842=CARTESIAN_POINT('Ctrl Pts',(-0.192087873248582,-0.079093845467276,
0.447107582569661));
#25843=CARTESIAN_POINT('Ctrl Pts',(-0.195677774776043,-0.00724967654898506,
0.44299482374408));
#25844=CARTESIAN_POINT('Ctrl Pts',(-0.195626364086859,-0.000119838590748017,
0.442586969212423));
#25845=CARTESIAN_POINT('',(-0.195390096198874,-9.39320554627862E-5,0.372586973725733));
#25846=CARTESIAN_POINT('Ctrl Pts',(-0.195399963336573,-0.000119699900101725,
0.442586969212423));
#25847=CARTESIAN_POINT('Ctrl Pts',(-0.195407310566176,0.0118740310377059,
0.441900082807232));
#25848=CARTESIAN_POINT('Ctrl Pts',(-0.194306083298946,0.0239118037275281,
0.441213196402041));
#25849=CARTESIAN_POINT('Ctrl Pts',(-0.192098246916485,0.0357690303420858,
0.44052630999685));
#25850=CARTESIAN_POINT('Ctrl Pts',(-0.189892534040976,0.0476148526228203,
0.439840084242089));
#25851=CARTESIAN_POINT('Ctrl Pts',(-0.186582402621779,0.0592795776638148,
0.439153858487328));
#25852=CARTESIAN_POINT('Ctrl Pts',(-0.182221619809175,0.0705438960798197,
0.438467632732567));
#25853=CARTESIAN_POINT('Ctrl Pts',(-0.177863933633089,0.0818002155880018,
0.437781894273739));
#25854=CARTESIAN_POINT('Ctrl Pts',(-0.172457395824743,0.0926558495972733,
0.437096155814912));
#25855=CARTESIAN_POINT('Ctrl Pts',(-0.166104625509635,0.102909734157193,
0.436410417356085));
#25856=CARTESIAN_POINT('Ctrl Pts',(-0.159737017950417,0.113187567227877,
0.435723077317411));
#25857=CARTESIAN_POINT('Ctrl Pts',(-0.152419265438923,0.122860088840632,
0.435035737278736));
#25858=CARTESIAN_POINT('Ctrl Pts',(-0.144297762712538,0.131754755800904,
0.434348397240062));
#25859=CARTESIAN_POINT('Ctrl Pts',(-0.13778889742042,0.138883262804243,
0.433797538135247));
#25860=CARTESIAN_POINT('Ctrl Pts',(-0.130764771052242,0.145512637421945,
0.433246679030432));
#25861=CARTESIAN_POINT('Ctrl Pts',(-0.123316693953183,0.151572269866414,
0.432695819925617));
#25862=CARTESIAN_POINT('Ctrl Pts',(-0.113900184619716,0.159233386247437,
0.431999375751781));
#25863=CARTESIAN_POINT('Ctrl Pts',(-0.103733686146086,0.166040755813973,
0.431302931577945));
#25864=CARTESIAN_POINT('Ctrl Pts',(-0.0929964058226484,0.171851181270509,
0.43060648740411));
#25865=CARTESIAN_POINT('Ctrl Pts',(-0.0822816609913256,0.177649411758383,
0.429911504933026));
#25866=CARTESIAN_POINT('Ctrl Pts',(-0.0709992389971638,0.182454373002956,
0.429216522461941));
#25867=CARTESIAN_POINT('Ctrl Pts',(-0.0593566206831002,0.186166462020103,
0.428521539990857));
#25868=CARTESIAN_POINT('Ctrl Pts',(-0.0477156428636164,0.189878027988075,
0.427826655445767));
#25869=CARTESIAN_POINT('Ctrl Pts',(-0.0357153885134297,0.192496717905539,
0.427131770900677));
#25870=CARTESIAN_POINT('Ctrl Pts',(-0.0235811686724703,0.193971875497559,
0.426436886355588));
#25871=CARTESIAN_POINT('Ctrl Pts',(-0.0114476701419841,0.195446945399835,
0.425742043117439));
#25872=CARTESIAN_POINT('Ctrl Pts',(0.000818905484256999,0.195778538784712,
0.425047199879289));
#25873=CARTESIAN_POINT('Ctrl Pts',(0.0129881151909117,0.194967866233868,
0.42435235664114));
#25874=CARTESIAN_POINT('Ctrl Pts',(0.0251853718739311,0.19415532528611,
0.423655911963592));
#25875=CARTESIAN_POINT('Ctrl Pts',(0.0372839457004307,0.192195385610171,
0.422959467286044));
#25876=CARTESIAN_POINT('Ctrl Pts',(0.049059739844796,0.18914095782342,0.422263022608497));
#25877=CARTESIAN_POINT('Ctrl Pts',(0.0529031163407337,0.188144055549127,
0.422035717420278));
#25878=CARTESIAN_POINT('Ctrl Pts',(0.0567122271421686,0.187030962613515,
0.421808412232059));
#25879=CARTESIAN_POINT('Ctrl Pts',(0.060479697061881,0.185804645376005,
0.42158110704384));
#25880=CARTESIAN_POINT('Ctrl Pts',(0.0720229112588168,0.182047311449621,
0.420884662870005));
#25881=CARTESIAN_POINT('Ctrl Pts',(0.0832555063943229,0.177196870423139,
0.42018821869617));
#25882=CARTESIAN_POINT('Ctrl Pts',(0.0939599883447792,0.171326240226793,
0.419491774522335));
#25883=CARTESIAN_POINT('Ctrl Pts',(0.104642003640618,0.165467931357311,
0.418796792051251));
#25884=CARTESIAN_POINT('Ctrl Pts',(0.114797309786046,0.158594034667023,
0.418101809580167));
#25885=CARTESIAN_POINT('Ctrl Pts',(0.124229708622614,0.150824863651655,
0.417406827109083));
#25886=CARTESIAN_POINT('Ctrl Pts',(0.133660778393953,0.143056787345623,
0.416711942563993));
#25887=CARTESIAN_POINT('Ctrl Pts',(0.1423684388659,0.134394207449415,0.416017058018904));
#25888=CARTESIAN_POINT('Ctrl Pts',(0.150187948103768,0.124998960973201,
0.415322173473814));
#25889=CARTESIAN_POINT('Ctrl Pts',(0.158006992516213,0.115604272991042,
0.414627330235665));
#25890=CARTESIAN_POINT('Ctrl Pts',(0.164937450830462,0.105477695122798,
0.413932486997516));
#25891=CARTESIAN_POINT('Ctrl Pts',(0.170855376770996,0.0948135023529931,
0.413237643759367));
#25892=CARTESIAN_POINT('Ctrl Pts',(0.176786942046618,0.0841247312934131,
0.412541199081819));
#25893=CARTESIAN_POINT('Ctrl Pts',(0.181700948228195,0.0728966684410854,
0.411844754404271));
#25894=CARTESIAN_POINT('Ctrl Pts',(0.185520328854313,0.0613462923230709,
0.411148309726724));
#25895=CARTESIAN_POINT('Ctrl Pts',(0.186766895968817,0.0575764876247876,
0.410921004538504));
#25896=CARTESIAN_POINT('Ctrl Pts',(0.187897258122969,0.0537724657555652,
0.410693699350284));
#25897=CARTESIAN_POINT('Ctrl Pts',(0.188909908278612,0.0499420319387021,
0.410466394162065));
#25898=CARTESIAN_POINT('Ctrl Pts',(0.192012584053656,0.0382059016026106,
0.409769949988229));
#25899=CARTESIAN_POINT('Ctrl Pts',(0.194028388996668,0.0261379895188498,
0.409073505814394));
#25900=CARTESIAN_POINT('Ctrl Pts',(0.194900647294117,0.0139605760745879,
0.408377061640559));
#25901=CARTESIAN_POINT('Ctrl Pts',(0.195771074888688,0.00180872068565739,
0.407682079169474));
#25902=CARTESIAN_POINT('Ctrl Pts',(0.195502583269476,-0.0104513205404809,
0.40698709669839));
#25903=CARTESIAN_POINT('Ctrl Pts',(0.194089866700077,-0.0225894586997189,
0.406292114227305));
#25904=CARTESIAN_POINT('Ctrl Pts',(0.192677349188469,-0.0347258865435164,
0.405597229682215));
#25905=CARTESIAN_POINT('Ctrl Pts',(0.190120982082382,-0.0467395715973172,
0.404902345137126));
#25906=CARTESIAN_POINT('Ctrl Pts',(0.186467405668497,-0.058404337366844,
0.404207460592036));
#25907=CARTESIAN_POINT('Ctrl Pts',(0.182814046438984,-0.0700684097322835,
0.403512617353886));
#25908=CARTESIAN_POINT('Ctrl Pts',(0.17806389466511,-0.0813827762586296,
0.402817774115737));
#25909=CARTESIAN_POINT('Ctrl Pts',(0.172312967513375,-0.0921379467251932,
0.402122930877587));
#25910=CARTESIAN_POINT('Ctrl Pts',(0.166548785916879,-0.102917905162302,
0.401426486200039));
#25911=CARTESIAN_POINT('Ctrl Pts',(0.159779694153344,-0.113135353418367,
0.400730041522491));
#25912=CARTESIAN_POINT('Ctrl Pts',(0.152146206670055,-0.122607878196765,
0.400033596844944));
#25913=CARTESIAN_POINT('Ctrl Pts',(0.149654793690548,-0.125699515044703,
0.399806291656725));
#25914=CARTESIAN_POINT('Ctrl Pts',(0.147071616394809,-0.128712071440798,
0.399578986468507));
#25915=CARTESIAN_POINT('Ctrl Pts',(0.144402415512848,-0.131640048594851,
0.399351681280288));
#25916=CARTESIAN_POINT('Ctrl Pts',(0.136224206218077,-0.14061112684452,
0.398655237106453));
#25917=CARTESIAN_POINT('Ctrl Pts',(0.12717785096287,-0.148848931662931,
0.397958792932618));
#25918=CARTESIAN_POINT('Ctrl Pts',(0.117419376155819,-0.156185306937555,
0.397262348758782));
#25919=CARTESIAN_POINT('Ctrl Pts',(0.107681382515825,-0.16350628456751,
0.396567366287698));
#25920=CARTESIAN_POINT('Ctrl Pts',(0.0972348839673393,-0.169929007252841,
0.395872383816614));
#25921=CARTESIAN_POINT('Ctrl Pts',(0.0862703243360016,-0.175324245724774,
0.395177401345529));
#25922=CARTESIAN_POINT('Ctrl Pts',(0.0753073096578856,-0.180718723984593,
0.394482516800439));
#25923=CARTESIAN_POINT('Ctrl Pts',(0.0638271429792277,-0.185085578044804,
0.39378763225535));
#25924=CARTESIAN_POINT('Ctrl Pts',(0.0520451499259236,-0.188341345352496,
0.39309274771026));
#25925=CARTESIAN_POINT('Ctrl Pts',(0.0402638572452036,-0.191596919123309,
0.392397904472111));
#25926=CARTESIAN_POINT('Ctrl Pts',(0.0281816250544544,-0.19374132977803,
0.391703061233961));
#25927=CARTESIAN_POINT('Ctrl Pts',(0.0160265349818396,-0.194741649824776,
0.391008217995812));
#25928=CARTESIAN_POINT('Ctrl Pts',(0.00384343047508048,-0.195744275358352,
0.390311773318264));
#25929=CARTESIAN_POINT('Ctrl Pts',(-0.00841198957600976,-0.195597539064805,
0.389615328640716));
#25930=CARTESIAN_POINT('Ctrl Pts',(-0.0205102638617534,-0.194320583254377,
0.388918883963168));
#25931=CARTESIAN_POINT('Ctrl Pts',(-0.0244588912291522,-0.193903811197394,
0.388691578774949));
#25932=CARTESIAN_POINT('Ctrl Pts',(-0.0283908365629753,-0.193367055319197,
0.38846427358673));
#25933=CARTESIAN_POINT('Ctrl Pts',(-0.0322983667202349,-0.192712157133911,
0.388236968398512));
#25934=CARTESIAN_POINT('Ctrl Pts',(-0.044270713825152,-0.190705603613638,
0.387540524224677));
#25935=CARTESIAN_POINT('Ctrl Pts',(-0.0560977372091341,-0.187571997144415,
0.386844080050843));
#25936=CARTESIAN_POINT('Ctrl Pts',(-0.0675535427233033,-0.183351244515904,
0.386147635877009));
#25937=CARTESIAN_POINT('Ctrl Pts',(-0.078985304698777,-0.179139350437673,
0.385452653405926));
#25938=CARTESIAN_POINT('Ctrl Pts',(-0.0900465559772294,-0.173845068732815,
0.384757670934844));
#25939=CARTESIAN_POINT('Ctrl Pts',(-0.100525445100651,-0.167558332789856,
0.384062688463761));
#25940=CARTESIAN_POINT('Ctrl Pts',(-0.111002857703909,-0.1612724826748,
0.383367803918672));
#25941=CARTESIAN_POINT('Ctrl Pts',(-0.120897297563241,-0.153994866222789,
0.382672919373584));
#25942=CARTESIAN_POINT('Ctrl Pts',(-0.130021873704177,-0.14586114067309,
0.381978034828495));
#25943=CARTESIAN_POINT('Ctrl Pts',(-0.13914590744087,-0.137727898627193,
0.381283191590347));
#25944=CARTESIAN_POINT('Ctrl Pts',(-0.147499532374186,-0.128739251218365,
0.380588348352199));
#25945=CARTESIAN_POINT('Ctrl Pts',(-0.154931399895884,-0.119068977178364,
0.379893505114051));
#25946=CARTESIAN_POINT('Ctrl Pts',(-0.162380396008324,-0.109376415581983,
0.379197060436504));
#25947=CARTESIAN_POINT('Ctrl Pts',(-0.168902911728162,-0.0989998245785479,
0.378500615758957));
#25948=CARTESIAN_POINT('Ctrl Pts',(-0.174390599395294,-0.0881423782442364,
0.377804171081411));
#25949=CARTESIAN_POINT('Ctrl Pts',(-0.176181667542286,-0.0845987315451845,
0.377576865893186));
#25950=CARTESIAN_POINT('Ctrl Pts',(-0.177862878884868,-0.0810040369262574,
0.377349560704961));
#25951=CARTESIAN_POINT('Ctrl Pts',(-0.179431587178082,-0.0773657903905484,
0.377122255516736));
#25952=CARTESIAN_POINT('Ctrl Pts',(-0.184725790511809,-0.0650871423961478,
0.376355127625286));
#25953=CARTESIAN_POINT('Ctrl Pts',(-0.188767040765519,-0.0522371217977153,
0.375587999733836));
#25954=CARTESIAN_POINT('Ctrl Pts',(-0.191453853265823,-0.0390714994550838,
0.374820871842387));
#25955=CARTESIAN_POINT('Ctrl Pts',(-0.194061877734694,-0.0262919455362255,
0.374076239192573));
#25956=CARTESIAN_POINT('Ctrl Pts',(-0.195393669118938,-0.0132155597336468,
0.373331606542758));
#25957=CARTESIAN_POINT('Ctrl Pts',(-0.195399977418944,-9.39397482887344E-5,
0.372586973892944));
#25958=CARTESIAN_POINT('',(-0.19539992650912,0.000169470441615271,0.302586967349177));
#25959=CARTESIAN_POINT('Ctrl Pts',(-0.195123386395527,-9.37244138880245E-5,
0.372586969212423));
#25960=CARTESIAN_POINT('Ctrl Pts',(-0.19495607068899,0.0384983387935844,
0.370393827019935));
#25961=CARTESIAN_POINT('Ctrl Pts',(-0.165199853610515,0.142522406630586,
0.364495780533521));
#25962=CARTESIAN_POINT('Ctrl Pts',(0.00402447047846805,0.230924035961026,
0.354892829753184));
#25963=CARTESIAN_POINT('Ctrl Pts',(0.196205039257053,0.121842887839667,
0.343778116871407));
#25964=CARTESIAN_POINT('Ctrl Pts',(0.208769571438819,-0.0987794148000683,
0.332663403989631));
#25965=CARTESIAN_POINT('Ctrl Pts',(0.0302158574941567,-0.22897403499859,
0.321548691107855));
#25966=CARTESIAN_POINT('Ctrl Pts',(-0.155790063617848,-0.157337309383673,
0.311523212848785));
#25967=CARTESIAN_POINT('Ctrl Pts',(-0.194903398518234,-0.0457626416864486,
0.305202638883641));
#25968=CARTESIAN_POINT('Ctrl Pts',(-0.195283952697599,0.000169337138534779,
0.302586969212423));
#25969=CARTESIAN_POINT('',(-0.195399999941521,-4.78056065513374E-6,0.232586969207602));
#25970=CARTESIAN_POINT('Ctrl Pts',(-0.19539992650912,0.000169470441615271,
0.302586967349177));
#25971=CARTESIAN_POINT('Ctrl Pts',(-0.195386996090356,0.0150782819843667,
0.301738458498935));
#25972=CARTESIAN_POINT('Ctrl Pts',(-0.19366378775983,0.0299110432009344,
0.300889949648692));
#25973=CARTESIAN_POINT('Ctrl Pts',(-0.190305156722521,0.0443295310692184,
0.30004144079845));
#25974=CARTESIAN_POINT('Ctrl Pts',(-0.189352300468089,0.0484201102939455,
0.299800715647067));
#25975=CARTESIAN_POINT('Ctrl Pts',(-0.188268106887131,0.0524774798667048,
0.299559990495685));
#25976=CARTESIAN_POINT('Ctrl Pts',(-0.187054971073491,0.0564942279945073,
0.299319265344302));
#25977=CARTESIAN_POINT('Ctrl Pts',(-0.183545236571318,0.0681151193507628,
0.298622821170576));
#25978=CARTESIAN_POINT('Ctrl Pts',(-0.178936005112572,0.0794488282295186,
0.29792637699685));
#25979=CARTESIAN_POINT('Ctrl Pts',(-0.173295528940874,0.0902763515495762,
0.297229932823124));
#25980=CARTESIAN_POINT('Ctrl Pts',(-0.167666891046876,0.101081149974792,
0.296534950352147));
#25981=CARTESIAN_POINT('Ctrl Pts',(-0.161011638749481,0.111381068199425,
0.295839967881171));
#25982=CARTESIAN_POINT('Ctrl Pts',(-0.153445864238863,0.120977381142049,
0.295144985410195));
#25983=CARTESIAN_POINT('Ctrl Pts',(-0.145881155778107,0.130572341923294,
0.29445010086521));
#25984=CARTESIAN_POINT('Ctrl Pts',(-0.137406684932671,0.13946317907191,
0.293755216320225));
#25985=CARTESIAN_POINT('Ctrl Pts',(-0.128180730309582,0.147481728960919,
0.29306033177524));
#25986=CARTESIAN_POINT('Ctrl Pts',(-0.118955324117087,0.155499802192688,
0.292365488537193));
#25987=CARTESIAN_POINT('Ctrl Pts',(-0.108979201367998,0.162645136797938,
0.291670645299147));
#25988=CARTESIAN_POINT('Ctrl Pts',(-0.0984439432562392,0.168789662112827,
0.290975802061101));
#25989=CARTESIAN_POINT('Ctrl Pts',(-0.0878844040166807,0.174948349017575,
0.290279357383651));
#25990=CARTESIAN_POINT('Ctrl Pts',(-0.0767639454581824,0.180101236904367,
0.289582912706202));
#25991=CARTESIAN_POINT('Ctrl Pts',(-0.0652978492051816,0.184166638914808,
0.288886468028752));
#25992=CARTESIAN_POINT('Ctrl Pts',(-0.0615555517086098,0.185493502341605,
0.288659162840011));
#25993=CARTESIAN_POINT('Ctrl Pts',(-0.0577765609300914,0.186704918764145,
0.288431857651269));
#25994=CARTESIAN_POINT('Ctrl Pts',(-0.0539686480960809,0.187799214648734,
0.288204552462527));
#25995=CARTESIAN_POINT('Ctrl Pts',(-0.042301520206118,0.191152046131886,
0.287508108288854));
#25996=CARTESIAN_POINT('Ctrl Pts',(-0.0302794540633588,0.193425347083275,
0.28681166411518));
#25997=CARTESIAN_POINT('Ctrl Pts',(-0.018123467799382,0.194557703303993,
0.286115219941507));
#25998=CARTESIAN_POINT('Ctrl Pts',(-0.00599299461925058,0.195687682926172,
0.285420237470587));
#25999=CARTESIAN_POINT('Ctrl Pts',(0.00626998454611778,0.19568131607234,
0.284725254999667));
#26000=CARTESIAN_POINT('Ctrl Pts',(0.0184355467757656,0.194528379973408,
0.284030272528747));
#26001=CARTESIAN_POINT('Ctrl Pts',(0.0305993948257797,0.193375606328092,
0.283335387983823));
#26002=CARTESIAN_POINT('Ctrl Pts',(0.0426649783854545,0.1910766207582,0.2826405034389));
#26003=CARTESIAN_POINT('Ctrl Pts',(0.05440517568215,0.18767321827846,0.281945618893976));
#26004=CARTESIAN_POINT('Ctrl Pts',(0.0661446750907626,0.184270018111676,
0.281250775655993));
#26005=CARTESIAN_POINT('Ctrl Pts',(0.0775579929528,0.179762800890329,0.280555932418011));
#26006=CARTESIAN_POINT('Ctrl Pts',(0.0884336345056216,0.174243083903282,
0.279861089180029));
#26007=CARTESIAN_POINT('Ctrl Pts',(0.099334341684665,0.168710645352898,
0.279164644502646));
#26008=CARTESIAN_POINT('Ctrl Pts',(0.109694147573257,0.162161502351643,
0.278468199825263));
#26009=CARTESIAN_POINT('Ctrl Pts',(0.119327676998619,0.154732238082803,
0.277771755147881));
#26010=CARTESIAN_POINT('Ctrl Pts',(0.122471862456992,0.152307479341837,
0.277544449958837));
#26011=CARTESIAN_POINT('Ctrl Pts',(0.125538947031261,0.149789286873123,
0.277317144769794));
#26012=CARTESIAN_POINT('Ctrl Pts',(0.128523310477063,0.147183282556194,
0.27708983958075));
#26013=CARTESIAN_POINT('Ctrl Pts',(0.137667151606952,0.139198702296266,
0.276393395406186));
#26014=CARTESIAN_POINT('Ctrl Pts',(0.146096443818796,0.130330500407694,
0.275696951231621));
#26015=CARTESIAN_POINT('Ctrl Pts',(0.15363973429167,0.120731073244567,0.275000507057057));
#26016=CARTESIAN_POINT('Ctrl Pts',(0.161167192844588,0.111151793437958,
0.274305524585242));
#26017=CARTESIAN_POINT('Ctrl Pts',(0.167811746267886,0.100844970032632,
0.273610542113427));
#26018=CARTESIAN_POINT('Ctrl Pts',(0.173440124003984,0.0899982410132693,
0.272915559641613));
#26019=CARTESIAN_POINT('Ctrl Pts',(0.179067708677579,0.0791530403444332,
0.272220675095802));
#26020=CARTESIAN_POINT('Ctrl Pts',(0.18367895827777,0.067768839943914,0.271525790549991));
#26021=CARTESIAN_POINT('Ctrl Pts',(0.187185826647367,0.0560591321939784,
0.27083090600418));
#26022=CARTESIAN_POINT('Ctrl Pts',(0.190692486553528,0.0443501205197569,
0.270136062765314));
#26023=CARTESIAN_POINT('Ctrl Pts',(0.19309466992589,0.0323164865258053,
0.269441219526448));
#26024=CARTESIAN_POINT('Ctrl Pts',(0.194354581457236,0.0201855558898628,
0.268746376287582));
#26025=CARTESIAN_POINT('Ctrl Pts',(0.195617396768639,0.00802666650159185,
0.268049931609338));
#26026=CARTESIAN_POINT('Ctrl Pts',(0.19573265863162,-0.00422908998952003,
0.267353486931093));
#26027=CARTESIAN_POINT('Ctrl Pts',(0.194714600152907,-0.0163518955260133,
0.266657042252849));
#26028=CARTESIAN_POINT('Ctrl Pts',(0.194382326854407,-0.0203085293215227,
0.266429737068224));
#26029=CARTESIAN_POINT('Ctrl Pts',(0.193929740567102,-0.0242510495988667,
0.266202431883599));
#26030=CARTESIAN_POINT('Ctrl Pts',(0.193358517085165,-0.0281716856191818,
0.265975126698974));
#26031=CARTESIAN_POINT('Ctrl Pts',(0.191608335864775,-0.0401841881715449,
0.265278682526058));
#26032=CARTESIAN_POINT('Ctrl Pts',(0.188728252853097,-0.0520754914273812,
0.264582238353142));
#26033=CARTESIAN_POINT('Ctrl Pts',(0.184753337141331,-0.0636188998265577,
0.263885794180226));
#26034=CARTESIAN_POINT('Ctrl Pts',(0.180786764015271,-0.0751380808254853,
0.263190811710053));
#26035=CARTESIAN_POINT('Ctrl Pts',(0.175730130750634,-0.0863099722633644,
0.262495829239881));
#26036=CARTESIAN_POINT('Ctrl Pts',(0.1696688217757,-0.0969208487233055,
0.261800846769709));
#26037=CARTESIAN_POINT('Ctrl Pts',(0.163608366864844,-0.107530230065861,
0.261105962225507));
#26038=CARTESIAN_POINT('Ctrl Pts',(0.156543910936009,-0.117577971276881,
0.260411077681305));
#26039=CARTESIAN_POINT('Ctrl Pts',(0.148607085361824,-0.126874324353919,
0.259716193137103));
#26040=CARTESIAN_POINT('Ctrl Pts',(0.140670731586706,-0.136170124815726,
0.259021349899829));
#26041=CARTESIAN_POINT('Ctrl Pts',(0.131862700088761,-0.144713977140462,
0.258326506662554));
#26042=CARTESIAN_POINT('Ctrl Pts',(0.12235349475577,-0.15235085270864,0.25763166342528));
#26043=CARTESIAN_POINT('Ctrl Pts',(0.11282237308887,-0.160005329360096,
0.256935218748572));
#26044=CARTESIAN_POINT('Ctrl Pts',(0.102587574404305,-0.166748158713353,
0.256238774071864));
#26045=CARTESIAN_POINT('Ctrl Pts',(0.0918499103809251,-0.172466674934655,
0.255542329395156));
#26046=CARTESIAN_POINT('Ctrl Pts',(0.0883453580868168,-0.174333080802694,
0.255315024202503));
#26047=CARTESIAN_POINT('Ctrl Pts',(0.0847874212998323,-0.176090746132482,
0.255087719009851));
#26048=CARTESIAN_POINT('Ctrl Pts',(0.081183537746253,-0.177736865053378,
0.254860413817198));
#26049=CARTESIAN_POINT('Ctrl Pts',(0.070141538783967,-0.182780436285939,
0.254163969644105));
#26050=CARTESIAN_POINT('Ctrl Pts',(0.0585886545158649,-0.186808939278657,
0.253467525471012));
#26051=CARTESIAN_POINT('Ctrl Pts',(0.0467343719214419,-0.189728907868855,
0.252771081297919));
#26052=CARTESIAN_POINT('Ctrl Pts',(0.0349049691930304,-0.192642748004909,
0.252076098827597));
#26053=CARTESIAN_POINT('Ctrl Pts',(0.0227762476073445,-0.194452391887296,
0.251381116357274));
#26054=CARTESIAN_POINT('Ctrl Pts',(0.0105740813452859,-0.195113681744011,
0.250686133886952));
#26055=CARTESIAN_POINT('Ctrl Pts',(-0.0016263655792097,-0.195774878422149,
0.249991249342641));
#26056=CARTESIAN_POINT('Ctrl Pts',(-0.0138993660566686,-0.195287948947145,
0.249296364798329));
#26057=CARTESIAN_POINT('Ctrl Pts',(-0.0260141132144387,-0.193660594633153,
0.248601480254018));
#26058=CARTESIAN_POINT('Ctrl Pts',(-0.0381281402190967,-0.192033337056159,
0.247906637016657));
#26059=CARTESIAN_POINT('Ctrl Pts',(-0.0500830681767129,-0.189265932318957,
0.247211793779297));
#26060=CARTESIAN_POINT('Ctrl Pts',(-0.0616561819046621,-0.18541756991434,
0.246516950541937));
#26061=CARTESIAN_POINT('Ctrl Pts',(-0.0732559687572675,-0.181560337999533,
0.245820505865178));
#26062=CARTESIAN_POINT('Ctrl Pts',(-0.0844713745976783,-0.176617512523793,
0.245124061188419));
#26063=CARTESIAN_POINT('Ctrl Pts',(-0.0950988423629525,-0.170696719890062,
0.24442761651166));
#26064=CARTESIAN_POINT('Ctrl Pts',(-0.0985674288599389,-0.168764295173807,
0.244200311319581));
#26065=CARTESIAN_POINT('Ctrl Pts',(-0.101973600475422,-0.166728049500301,
0.243973006127501));
#26066=CARTESIAN_POINT('Ctrl Pts',(-0.105310966422842,-0.164592710504102,
0.243745700935422));
#26067=CARTESIAN_POINT('Ctrl Pts',(-0.115543810534397,-0.158045453949777,
0.243048750516156));
#26068=CARTESIAN_POINT('Ctrl Pts',(-0.125199707284002,-0.15051727213275,
0.242351800096891));
#26069=CARTESIAN_POINT('Ctrl Pts',(-0.134086365345269,-0.142133763154625,
0.241654849677626));
#26070=CARTESIAN_POINT('Ctrl Pts',(-0.142954369225497,-0.133767852186139,
0.240959362242444));
#26071=CARTESIAN_POINT('Ctrl Pts',(-0.151055658945902,-0.124550717705166,
0.240263874807263));
#26072=CARTESIAN_POINT('Ctrl Pts',(-0.158230506826314,-0.114648448351854,
0.239568387372081));
#26073=CARTESIAN_POINT('Ctrl Pts',(-0.165404331796768,-0.104747590753899,
0.238872999091757));
#26074=CARTESIAN_POINT('Ctrl Pts',(-0.17165142749491,-0.0941624718976632,
0.238177610811433));
#26075=CARTESIAN_POINT('Ctrl Pts',(-0.176852967045611,-0.0830914438866242,
0.237482222531109));
#26076=CARTESIAN_POINT('Ctrl Pts',(-0.182054153530154,-0.072021167346431,
0.236786881451824));
#26077=CARTESIAN_POINT('Ctrl Pts',(-0.18620957656066,-0.0604658495818994,
0.236091540372539));
#26078=CARTESIAN_POINT('Ctrl Pts',(-0.18924805461596,-0.0486449773776757,
0.235396199293253));
#26079=CARTESIAN_POINT('Ctrl Pts',(-0.192293556288096,-0.0367967805472705,
0.234699250893059));
#26080=CARTESIAN_POINT('Ctrl Pts',(-0.194216802258729,-0.0246826660200671,
0.234002302492864));
#26081=CARTESIAN_POINT('Ctrl Pts',(-0.194997693637588,-0.0125323372130376,
0.233305354092669));
#26082=CARTESIAN_POINT('Ctrl Pts',(-0.195265996886212,-0.00835765584372756,
0.233065892465921));
#26083=CARTESIAN_POINT('Ctrl Pts',(-0.195399897822299,-0.00417871467006272,
0.232826430839172));
#26084=CARTESIAN_POINT('Ctrl Pts',(-0.195399999941518,-4.78064468390912E-6,
0.232586969212423));
#26085=CARTESIAN_POINT('',(-0.19539992906386,-0.00016649876455978,0.162586971253333));
#26086=CARTESIAN_POINT('Ctrl Pts',(-0.195399999941521,-4.78056065513374E-6,
0.232586969207602));
#26087=CARTESIAN_POINT('Ctrl Pts',(-0.19540029672657,0.0121259720518583,
0.231891019119132));
#26088=CARTESIAN_POINT('Ctrl Pts',(-0.194266622200123,0.0242999913662591,
0.231195069030662));
#26089=CARTESIAN_POINT('Ctrl Pts',(-0.192000856353013,0.0362881683157171,
0.230499118942192));
#26090=CARTESIAN_POINT('Ctrl Pts',(-0.189739844128247,0.0482511938286821,
0.229804628971012));
#26091=CARTESIAN_POINT('Ctrl Pts',(-0.186351542393054,0.0600282837654985,
0.229110138999833));
#26092=CARTESIAN_POINT('Ctrl Pts',(-0.181889493436239,0.0713958834773282,
0.228415649028654));
#26093=CARTESIAN_POINT('Ctrl Pts',(-0.177428065158018,0.0827619019367191,
0.22772125566221));
#26094=CARTESIAN_POINT('Ctrl Pts',(-0.171893463435113,0.0937177112672988,
0.227026862295766));
#26095=CARTESIAN_POINT('Ctrl Pts',(-0.165388451631415,0.104056811727839,
0.226332468929322));
#26096=CARTESIAN_POINT('Ctrl Pts',(-0.158883771142894,0.114395385594271,
0.225638110929926));
#26097=CARTESIAN_POINT('Ctrl Pts',(-0.151409268985664,0.124116585139044,
0.224943752930529));
#26098=CARTESIAN_POINT('Ctrl Pts',(-0.143111171736177,0.133042671817348,
0.224249394931133));
#26099=CARTESIAN_POINT('Ctrl Pts',(-0.134794009745904,0.141989266031734,
0.22355344165575));
#26100=CARTESIAN_POINT('Ctrl Pts',(-0.125650120571794,0.150136503959947,
0.222857488380368));
#26101=CARTESIAN_POINT('Ctrl Pts',(-0.115861791947887,0.157344225081903,
0.222161535104985));
#26102=CARTESIAN_POINT('Ctrl Pts',(-0.11283667685439,0.159571794955527,
0.221946448460613));
#26103=CARTESIAN_POINT('Ctrl Pts',(-0.109750220520155,0.161709939439695,
0.221731361816241));
#26104=CARTESIAN_POINT('Ctrl Pts',(-0.106608316477594,0.163755387263483,
0.221516275171868));
#26105=CARTESIAN_POINT('Ctrl Pts',(-0.0964349244294766,0.170378486614536,
0.220819831000477));
#26106=CARTESIAN_POINT('Ctrl Pts',(-0.0856059651325258,0.176073362452133,
0.220123386829086));
#26107=CARTESIAN_POINT('Ctrl Pts',(-0.0743147751887864,0.18071655759404,
0.219426942657695));
#26108=CARTESIAN_POINT('Ctrl Pts',(-0.0630472832895308,0.185350007558906,
0.218731960189192));
#26109=CARTESIAN_POINT('Ctrl Pts',(-0.0513202596931032,0.188935759214472,
0.218036977720689));
#26110=CARTESIAN_POINT('Ctrl Pts',(-0.0393505492747393,0.191396693471377,
0.217341995252186));
#26111=CARTESIAN_POINT('Ctrl Pts',(-0.0273825254423316,0.193857280971594,
0.216647110709834));
#26112=CARTESIAN_POINT('Ctrl Pts',(-0.0151727298308682,0.195193144473447,
0.215952226167483));
#26113=CARTESIAN_POINT('Ctrl Pts',(-0.00295056508101129,0.195377721774267,
0.215257341625131));
#26114=CARTESIAN_POINT('Ctrl Pts',(0.00927087312890606,0.195562288102988,
0.214562498389813));
#26115=CARTESIAN_POINT('Ctrl Pts',(0.0215038029545236,0.194595717610321,
0.213867655154495));
#26116=CARTESIAN_POINT('Ctrl Pts',(0.0335191997017815,0.192503566853583,
0.213172811919178));
#26117=CARTESIAN_POINT('Ctrl Pts',(0.0455622889237909,0.190406594214287,
0.212476367244543));
#26118=CARTESIAN_POINT('Ctrl Pts',(0.0573859930816696,0.187179076431562,
0.211779922569909));
#26119=CARTESIAN_POINT('Ctrl Pts',(0.0687730616908222,0.182897309946512,
0.211083477895275));
#26120=CARTESIAN_POINT('Ctrl Pts',(0.0724895664205764,0.181499829529067,
0.210856172693548));
#26121=CARTESIAN_POINT('Ctrl Pts',(0.076159718528558,0.179990430187524,
0.21062886749182));
#26122=CARTESIAN_POINT('Ctrl Pts',(0.0797764976032439,0.178372841066569,
0.210401562290093));
#26123=CARTESIAN_POINT('Ctrl Pts',(0.0908580074399471,0.173416682731915,
0.209705118084665));
#26124=CARTESIAN_POINT('Ctrl Pts',(0.101515120126267,0.167406363771345,
0.209008673879237));
#26125=CARTESIAN_POINT('Ctrl Pts',(0.111539265227651,0.160437378165051,
0.208312229673809));
#26126=CARTESIAN_POINT('Ctrl Pts',(0.121542371573814,0.153483019121006,
0.207617247171001));
#26127=CARTESIAN_POINT('Ctrl Pts',(0.130914392769052,0.145574420638768,
0.206922264668194));
#26128=CARTESIAN_POINT('Ctrl Pts',(0.139472943765809,0.136851956351744,
0.206227282165386));
#26129=CARTESIAN_POINT('Ctrl Pts',(0.148030288822697,0.128130721100737,
0.205532397588864));
#26130=CARTESIAN_POINT('Ctrl Pts',(0.155773745952015,0.11859643951404,0.204837513012342));
#26131=CARTESIAN_POINT('Ctrl Pts',(0.16255659831078,0.108427451992692,0.20414262843582));
#26132=CARTESIAN_POINT('Ctrl Pts',(0.169339047466181,0.098259068961871,
0.203447785166374));
#26133=CARTESIAN_POINT('Ctrl Pts',(0.175160541501862,0.0874567982968869,
0.202752941896928));
#26134=CARTESIAN_POINT('Ctrl Pts',(0.179918358774935,0.0762269255298523,
0.202058098627482));
#26135=CARTESIAN_POINT('Ctrl Pts',(0.184687141617781,0.0649711707361879,
0.201361653919412));
#26136=CARTESIAN_POINT('Ctrl Pts',(0.188387071916958,0.0532866775537924,
0.200665209211341));
#26137=CARTESIAN_POINT('Ctrl Pts',(0.190964444600237,0.0413973537623237,
0.19996876450327));
#26138=CARTESIAN_POINT('Ctrl Pts',(0.191805645305132,0.0375169263724499,
0.199741459471619));
#26139=CARTESIAN_POINT('Ctrl Pts',(0.192527675912343,0.033614753752915,
0.199514154439968));
#26140=CARTESIAN_POINT('Ctrl Pts',(0.193129862663858,0.0296987566648717,
0.199286849408317));
#26141=CARTESIAN_POINT('Ctrl Pts',(0.194974913860842,0.0177004602950171,
0.198590405290818));
#26142=CARTESIAN_POINT('Ctrl Pts',(0.195704118410672,0.00548709834586105,
0.197893961173319));
#26143=CARTESIAN_POINT('Ctrl Pts',(0.195284607996036,-0.00671430412138008,
0.197197517055821));
#26144=CARTESIAN_POINT('Ctrl Pts',(0.194865978053238,-0.0188900981868488,
0.196502534640845));
#26145=CARTESIAN_POINT('Ctrl Pts',(0.193303373686754,-0.0310531136309142,
0.19580755222587));
#26146=CARTESIAN_POINT('Ctrl Pts',(0.190615834192916,-0.0429739892835024,
0.195112569810894));
#26147=CARTESIAN_POINT('Ctrl Pts',(0.187928673380375,-0.0548931852537454,
0.194417685320746));
#26148=CARTESIAN_POINT('Ctrl Pts',(0.184117039430817,-0.0665694460773828,
0.193722800830599));
#26149=CARTESIAN_POINT('Ctrl Pts',(0.179251213331651,-0.0777827906360454,
0.193027916340451));
#26150=CARTESIAN_POINT('Ctrl Pts',(0.174385676473917,-0.0889954686349565,
0.192333073156626));
#26151=CARTESIAN_POINT('Ctrl Pts',(0.168466445016061,-0.099744492260233,
0.191638229972801));
#26152=CARTESIAN_POINT('Ctrl Pts',(0.161611136962421,-0.109831691281313,
0.190943386788976));
#26153=CARTESIAN_POINT('Ctrl Pts',(0.154740029123084,-0.119942138795614,
0.190246942163858));
#26154=CARTESIAN_POINT('Ctrl Pts',(0.1469290832769,-0.129387029182578,0.189550497538739));
#26155=CARTESIAN_POINT('Ctrl Pts',(0.138337304105884,-0.137999819901028,
0.188854052913621));
#26156=CARTESIAN_POINT('Ctrl Pts',(0.135533120877919,-0.14081086087379,
0.188626747451261));
#26157=CARTESIAN_POINT('Ctrl Pts',(0.132646044039451,-0.143533566533357,
0.188399441988901));
#26158=CARTESIAN_POINT('Ctrl Pts',(0.129682363299695,-0.146163075532112,
0.188172136526541));
#26159=CARTESIAN_POINT('Ctrl Pts',(0.120601903162391,-0.154219662506403,
0.187475692350802));
#26160=CARTESIAN_POINT('Ctrl Pts',(0.110735649197369,-0.161455338184431,
0.186779248175063));
#26161=CARTESIAN_POINT('Ctrl Pts',(0.100256524520575,-0.167719376611814,
0.186082803999324));
#26162=CARTESIAN_POINT('Ctrl Pts',(0.089799393530819,-0.17397026801547,
0.185387821527279));
#26163=CARTESIAN_POINT('Ctrl Pts',(0.0787326507484688,-0.17925306098191,
0.184692839055233));
#26164=CARTESIAN_POINT('Ctrl Pts',(0.0672593302743625,-0.183459375587742,
0.183997856583187));
#26165=CARTESIAN_POINT('Ctrl Pts',(0.0557876264624159,-0.187665097497704,
0.183302972038491));
#26166=CARTESIAN_POINT('Ctrl Pts',(0.0439102637455561,-0.190794297918841,
0.182608087493795));
#26167=CARTESIAN_POINT('Ctrl Pts',(0.0318501821642357,-0.192786736826227,
0.181913202949099));
#26168=CARTESIAN_POINT('Ctrl Pts',(0.0197908174998791,-0.194779057292188,
0.181218359712126));
#26169=CARTESIAN_POINT('Ctrl Pts',(0.00754962393995063,-0.195634634032994,
0.180523516475154));
#26170=CARTESIAN_POINT('Ctrl Pts',(-0.00464311434237927,-0.195344827137049,
0.179828673238181));
#26171=CARTESIAN_POINT('Ctrl Pts',(-0.0168639538091138,-0.195054352309353,
0.17913222856292));
#26172=CARTESIAN_POINT('Ctrl Pts',(-0.0290352416459393,-0.193613309459193,
0.178435783887658));
#26173=CARTESIAN_POINT('Ctrl Pts',(-0.040930824353633,-0.19106498270937,
0.177739339212397));
#26174=CARTESIAN_POINT('Ctrl Pts',(-0.0448132973973497,-0.19023326137584,
0.177512034023186));
#26175=CARTESIAN_POINT('Ctrl Pts',(-0.0486665021716956,-0.18928399100357,
0.177284728833975));
#26176=CARTESIAN_POINT('Ctrl Pts',(-0.0524829434433919,-0.188219820017759,
0.177057423644765));
#26177=CARTESIAN_POINT('Ctrl Pts',(-0.0641762050919854,-0.184959287786276,
0.176360979270988));
#26178=CARTESIAN_POINT('Ctrl Pts',(-0.0756058517517343,-0.180593370571617,
0.175664534897211));
#26179=CARTESIAN_POINT('Ctrl Pts',(-0.0865514713732667,-0.175185623848313,
0.174968090523434));
#26180=CARTESIAN_POINT('Ctrl Pts',(-0.0974741182626512,-0.169789226936284,
0.174273107851288));
#26181=CARTESIAN_POINT('Ctrl Pts',(-0.107913944199139,-0.163355657667378,
0.173578125179142));
#26182=CARTESIAN_POINT('Ctrl Pts',(-0.117669787918049,-0.155996733976457,
0.172883142506997));
#26183=CARTESIAN_POINT('Ctrl Pts',(-0.127424256977318,-0.148638847204092,
0.172188257762273));
#26184=CARTESIAN_POINT('Ctrl Pts',(-0.136494209348649,-0.140356354588377,
0.17149337301755));
#26185=CARTESIAN_POINT('Ctrl Pts',(-0.144708136496583,-0.131303904099178,
0.170798488272827));
#26186=CARTESIAN_POINT('Ctrl Pts',(-0.15292157536601,-0.122251991734671,
0.170103644835663));
#26187=CARTESIAN_POINT('Ctrl Pts',(-0.160278521350541,-0.112430878895252,
0.169408801398499));
#26188=CARTESIAN_POINT('Ctrl Pts',(-0.166646837862244,-0.102029365530298,
0.168713957961336));
#26189=CARTESIAN_POINT('Ctrl Pts',(-0.17302983170028,-0.0916038793609551,
0.168017513089341));
#26190=CARTESIAN_POINT('Ctrl Pts',(-0.178419245622511,-0.0805961024668422,
0.167321068217346));
#26191=CARTESIAN_POINT('Ctrl Pts',(-0.182728809640674,-0.0692195212877294,
0.166624623345351));
#26192=CARTESIAN_POINT('Ctrl Pts',(-0.184135355966955,-0.0655064569509017,
0.16639731915123));
#26193=CARTESIAN_POINT('Ctrl Pts',(-0.18542726699935,-0.0617542403422105,
0.166170014957109));
#26194=CARTESIAN_POINT('Ctrl Pts',(-0.186602703495507,-0.0579706050353778,
0.165942710762988));
#26195=CARTESIAN_POINT('Ctrl Pts',(-0.190950036443863,-0.0439768907958402,
0.165102029862207));
#26196=CARTESIAN_POINT('Ctrl Pts',(-0.193725456221651,-0.0294728360944788,
0.164261348961425));
#26197=CARTESIAN_POINT('Ctrl Pts',(-0.19484001101867,-0.0147827638229339,
0.163420668060643));
#26198=CARTESIAN_POINT('Ctrl Pts',(-0.195208442835856,-0.00992675312154956,
0.163142769124873));
#26199=CARTESIAN_POINT('Ctrl Pts',(-0.195395767369531,-0.0050505877175918,
0.162864870189103));
#26200=CARTESIAN_POINT('Ctrl Pts',(-0.19539992906386,-0.00016649876455978,
0.162586971253333));
#26201=CARTESIAN_POINT('',(-0.195131096902049,0.000101113969644753,0.092586969212423));
#26202=CARTESIAN_POINT('Ctrl Pts',(-0.195269961073647,-0.00016635217456426,
0.162586969212423));
#26203=CARTESIAN_POINT('Ctrl Pts',(-0.194902238792413,0.0452585421341261,
0.160000645435353));
#26204=CARTESIAN_POINT('Ctrl Pts',(-0.156485712116744,0.156315318469729,
0.153709417364356));
#26205=CARTESIAN_POINT('Ctrl Pts',(0.0284055178284113,0.229205619323633,
0.143713284999436));
#26206=CARTESIAN_POINT('Ctrl Pts',(0.207982494406922,0.100426132144768,
0.132598572117659));
#26207=CARTESIAN_POINT('Ctrl Pts',(0.197161712231624,-0.120288773936243,
0.121483859235884));
#26208=CARTESIAN_POINT('Ctrl Pts',(0.00584918801334944,-0.230884768458966,
0.110369146354108));
#26209=CARTESIAN_POINT('Ctrl Pts',(-0.16458778281091,-0.143557725929993,
0.100736849679621));
#26210=CARTESIAN_POINT('Ctrl Pts',(-0.19494818999653,-0.0390035530360715,
0.0948094572990591));
#26211=CARTESIAN_POINT('Ctrl Pts',(-0.195131096902049,0.000101113969644753,
0.092586969212423));
#26212=CARTESIAN_POINT('Ctrl Pts',(-0.195131096902049,0.000101113969644753,
0.092586969212423));
#26213=CARTESIAN_POINT('Ctrl Pts',(-0.195253097178586,0.026184219880761,
0.0911045530051337));
#26214=CARTESIAN_POINT('Ctrl Pts',(-0.178242552021087,0.117302317988555,
0.0859172325039191));
#26215=CARTESIAN_POINT('Ctrl Pts',(-0.0399751411601922,0.227471578691004,
0.077025007708779));
#26216=CARTESIAN_POINT('Ctrl Pts',(0.169446625860149,0.15694328133998,0.0659102948270026));
#26217=CARTESIAN_POINT('Ctrl Pts',(0.223746334253747,-0.0572705996896112,
0.0547955819452267));
#26218=CARTESIAN_POINT('Ctrl Pts',(0.073221170054178,-0.219033718527302,
0.0436808690634503));
#26219=CARTESIAN_POINT('Ctrl Pts',(-0.136932020372999,-0.181643133843283,
0.0329446976177534));
#26220=CARTESIAN_POINT('Ctrl Pts',(-0.195234758244009,-0.0580117927957973,
0.0259134304659814));
#26221=CARTESIAN_POINT('Ctrl Pts',(-0.19563576606976,0.000124656684744311,
0.022587067608135));
#26222=CARTESIAN_POINT('Origin',(0.,0.,-0.129405622560373));
#26223=CARTESIAN_POINT('',(0.104759235283674,0.114983934194216,2.4));
#26224=CARTESIAN_POINT('Ctrl Pts',(0.104759235283674,0.114983934194216,
2.4));
#26225=CARTESIAN_POINT('Ctrl Pts',(0.116569373796386,0.104223986834125,
2.39879406899067));
#26226=CARTESIAN_POINT('Ctrl Pts',(0.126656121123575,0.0917046658947872,
2.39752488696204));
#26227=CARTESIAN_POINT('Ctrl Pts',(0.136910041192079,0.0739705316573757,
2.39599244051318));
#26228=CARTESIAN_POINT('Ctrl Pts',(0.138990080658535,0.0699840267182179,
2.39566173348939));
#26229=CARTESIAN_POINT('Ctrl Pts',(0.141302013217873,0.0650420429405182,
2.39526750720927));
#26230=CARTESIAN_POINT('Ctrl Pts',(0.141701216126826,0.0641676843380198,
2.39519833532576));
#26231=CARTESIAN_POINT('Ctrl Pts',(0.142313711985314,0.0627925633649434,
2.39509042818814));
#26232=CARTESIAN_POINT('Ctrl Pts',(0.142532518921949,0.0622942990681896,
2.39505150836491));
#26233=CARTESIAN_POINT('Ctrl Pts',(0.142915965079838,0.06140852286273,2.39498263294686));
#26234=CARTESIAN_POINT('Ctrl Pts',(0.143081653201886,0.0610214739101778,
2.39495264259946));
#26235=CARTESIAN_POINT('Ctrl Pts',(0.143459931281017,0.0601278011410767,
2.39488363652743));
#26236=CARTESIAN_POINT('Ctrl Pts',(0.143671413572795,0.05962071191288,2.39484465788404));
#26237=CARTESIAN_POINT('Ctrl Pts',(0.144244563817985,0.0582256606757036,
2.39473790025333));
#26238=CARTESIAN_POINT('Ctrl Pts',(0.144600720111675,0.0573354477356837,
2.39467030328277));
#26239=CARTESIAN_POINT('Ctrl Pts',(0.146388334651106,0.0527446755254263,
2.39432431936592));
#26240=CARTESIAN_POINT('Ctrl Pts',(0.147686139758198,0.0489934067215972,
2.39405032203227));
#26241=CARTESIAN_POINT('Ctrl Pts',(0.153461192843779,0.0299751782671007,
2.39269589807151));
#26242=CARTESIAN_POINT('Ctrl Pts',(0.155720448807173,0.0141377171635735,
2.39168795703575));
#26243=CARTESIAN_POINT('Ctrl Pts',(0.1555095411221,-0.00444786906095659,
2.39040901501096));
#26244=CARTESIAN_POINT('Ctrl Pts',(0.155409692815497,-0.00712923865114926,
2.39022190320889));
#26245=CARTESIAN_POINT('Ctrl Pts',(0.15520553410147,-0.0103611578266905,
2.38999178303995));
#26246=CARTESIAN_POINT('Ctrl Pts',(0.155167522712346,-0.0109156437366008,
2.38995213882522));
#26247=CARTESIAN_POINT('Ctrl Pts',(0.155104024069529,-0.0117744413034399,
2.38989046700507));
#26248=CARTESIAN_POINT('Ctrl Pts',(0.155080610331675,-0.0120789091181799,
2.38986854995593));
#26249=CARTESIAN_POINT('Ctrl Pts',(0.155056210688231,-0.0123844268449986,
2.38984650266975));
#26250=CARTESIAN_POINT('Ctrl Pts',(0.155056120886389,-0.0123855511358104,
2.38984642153603));
#26251=CARTESIAN_POINT('Ctrl Pts',(0.155055940024575,-0.0123878151585674,
2.3898462581528));
#26252=CARTESIAN_POINT('Ctrl Pts',(0.155055848964433,-0.0123889548883746,
2.38984617590343));
#26253=CARTESIAN_POINT('Ctrl Pts',(0.155055665561528,-0.0123912500828242,
2.38984601026762));
#26254=CARTESIAN_POINT('Ctrl Pts',(0.155055573218514,-0.0123924055462099,
2.38984592688126));
#26255=CARTESIAN_POINT('Ctrl Pts',(0.155055387224824,-0.0123947325078486,
2.38984575894976));
#26256=CARTESIAN_POINT('Ctrl Pts',(0.155055293573659,-0.0123959040076737,
2.3898456744045));
#26257=CARTESIAN_POINT('Ctrl Pts',(0.155055104937755,-0.012398263352653,
2.38984550413272));
#26258=CARTESIAN_POINT('Ctrl Pts',(0.155055009952702,-0.0123994511970267,
2.38984541840624));
#26259=CARTESIAN_POINT('Ctrl Pts',(0.155054818622254,-0.0124018435516719,
2.38984524574885));
#26260=CARTESIAN_POINT('Ctrl Pts',(0.15505472227678,-0.0124030480580616,
2.38984515881818));
#26261=CARTESIAN_POINT('Ctrl Pts',(0.155054528198523,-0.0124054740592664,
2.38984498372906));
#26262=CARTESIAN_POINT('Ctrl Pts',(0.155054430465124,-0.0124066955567403,
2.38984489557038));
#26263=CARTESIAN_POINT('Ctrl Pts',(0.155054233583061,-0.0124091558743604,
2.38984471800104));
#26264=CARTESIAN_POINT('Ctrl Pts',(0.155054134434034,-0.012410394693849,
2.3898446285904));
#26265=CARTESIAN_POINT('Ctrl Pts',(0.155053934692053,-0.0124128899979582,
2.38984444849233));
#26266=CARTESIAN_POINT('Ctrl Pts',(0.155053834098541,-0.0124141464841883,
2.38984435780476));
#26267=CARTESIAN_POINT('Ctrl Pts',(0.155053631438168,-0.0124166774731176,
2.3898441751274));
#26268=CARTESIAN_POINT('Ctrl Pts',(0.155053529370771,-0.0124179519769673,
2.3898440831375));
#26269=CARTESIAN_POINT('Ctrl Pts',(0.155053323732169,-0.0124205193647189,
2.38984389782916));
#26270=CARTESIAN_POINT('Ctrl Pts',(0.155053220160708,-0.0124218122461009,
2.38984380451087));
#26271=CARTESIAN_POINT('Ctrl Pts',(0.155053011482959,-0.0124244167588192,
2.38984361651896));
#26272=CARTESIAN_POINT('Ctrl Pts',(0.155052906376181,-0.012425728390341,
2.3898435218453));
#26273=CARTESIAN_POINT('Ctrl Pts',(0.155052694596044,-0.0124283707817298,
2.38984333111526));
#26274=CARTESIAN_POINT('Ctrl Pts',(0.155052587922058,-0.012429701543272,
2.38984323505873));
#26275=CARTESIAN_POINT('Ctrl Pts',(0.155052372974972,-0.0124323825819943,
2.38984304153488));
#26276=CARTESIAN_POINT('Ctrl Pts',(0.155052264700915,-0.0124337328647711,
2.38984294406714));
#26277=CARTESIAN_POINT('Ctrl Pts',(0.155052046519325,-0.0124364533553029,
2.38984274769124));
#26278=CARTESIAN_POINT('Ctrl Pts',(0.155051936611995,-0.0124378235539526,
2.38984264878371));
#26279=CARTESIAN_POINT('Ctrl Pts',(0.155051715129383,-0.0124405842862295,
2.38984244949855));
#26280=CARTESIAN_POINT('Ctrl Pts',(0.155051603553495,-0.0124419748205716,
2.38984234912083));
#26281=CARTESIAN_POINT('Ctrl Pts',(0.155051378698546,-0.0124447766426194,
2.38984214686499));
#26282=CARTESIAN_POINT('Ctrl Pts',(0.155051265418725,-0.012446187932723,
2.38984204498665));
#26283=CARTESIAN_POINT('Ctrl Pts',(0.155051037119204,-0.0124490317022854,
2.389841839698));
#26284=CARTESIAN_POINT('Ctrl Pts',(0.155050922098996,-0.0124504641807515,
2.38984173628772));
#26285=CARTESIAN_POINT('Ctrl Pts',(0.155050690280845,-0.0124533507764655,
2.38984152790262));
#26286=CARTESIAN_POINT('Ctrl Pts',(0.155050573482625,-0.0124548048895616,
2.38984142292807));
#26287=CARTESIAN_POINT('Ctrl Pts',(0.15505033807006,-0.0124577352096343,
2.38984121138146));
#26288=CARTESIAN_POINT('Ctrl Pts',(0.155050219454883,-0.0124592114191003,
2.38984110480919));
#26289=CARTESIAN_POINT('Ctrl Pts',(0.155049980368852,-0.012462186400449,
2.3898408900332));
#26290=CARTESIAN_POINT('Ctrl Pts',(0.155049859897092,-0.0124636851754628,
2.38984078182922));
#26291=CARTESIAN_POINT('Ctrl Pts',(0.15504961705678,-0.0124667057748541,
2.38984056375454));
#26292=CARTESIAN_POINT('Ctrl Pts',(0.155049494687644,-0.0124682275980645,
2.38984045388388));
#26293=CARTESIAN_POINT('Ctrl Pts',(0.155049248010524,-0.012471294791423,
2.38984023243981));
#26294=CARTESIAN_POINT('Ctrl Pts',(0.155049123701721,-0.012472840163012,
2.38984012086624));
#26295=CARTESIAN_POINT('Ctrl Pts',(0.155048873101805,-0.0124759549670296,
2.38983989597911));
#26296=CARTESIAN_POINT('Ctrl Pts',(0.155048746810194,-0.0124775243965821,
2.38983978266571));
#26297=CARTESIAN_POINT('Ctrl Pts',(0.155048492200137,-0.0124806878424747,
2.3898395542608));
#26298=CARTESIAN_POINT('Ctrl Pts',(0.155048363880935,-0.0124822818587952,
2.38983943916926));
#26299=CARTESIAN_POINT('Ctrl Pts',(0.155048105170051,-0.0124854950168308,
2.38983920716902));
#26300=CARTESIAN_POINT('Ctrl Pts',(0.155047974777361,-0.0124871141613046,
2.3898390902601));
#26301=CARTESIAN_POINT('Ctrl Pts',(0.155047711872207,-0.0124903781334359,
2.38983885458469));
#26302=CARTESIAN_POINT('Ctrl Pts',(0.155047579358919,-0.0124920229611797,
2.38983873581815));
#26303=CARTESIAN_POINT('Ctrl Pts',(0.155047312163825,-0.0124953388743151,
2.3898384963859));
#26304=CARTESIAN_POINT('Ctrl Pts',(0.155047177481234,-0.0124970099589203,
2.38983837572019));
#26305=CARTESIAN_POINT('Ctrl Pts',(0.1550262042962,-0.0127571838369673,
2.38981958882283));
#26306=CARTESIAN_POINT('Ctrl Pts',(0.1550047198774,-0.0130156279923222,
2.38980088721687));
#26307=CARTESIAN_POINT('Ctrl Pts',(0.15495389007473,-0.0136090981167331,
2.38975785013479));
#26308=CARTESIAN_POINT('Ctrl Pts',(0.154924104929042,-0.0139440778482577,
2.38973349109876));
#26309=CARTESIAN_POINT('Ctrl Pts',(0.154829757429084,-0.0149675274166969,
2.38965886812692));
#26310=CARTESIAN_POINT('Ctrl Pts',(0.154761691475387,-0.0156556528715037,
2.38960841819265));
#26311=CARTESIAN_POINT('Ctrl Pts',(0.153884679363036,-0.0239565647087003,
2.38899667448546));
#26312=CARTESIAN_POINT('Ctrl Pts',(0.152519468505603,-0.0314990607237558,
2.38840917103484));
#26313=CARTESIAN_POINT('Ctrl Pts',(0.148526520284105,-0.0469544457626036,
2.38717440265638));
#26314=CARTESIAN_POINT('Ctrl Pts',(0.145806548278979,-0.0548207718843048,
2.38652854545728));
#26315=CARTESIAN_POINT('Ctrl Pts',(0.140675311565931,-0.0665302598501802,
2.38555744753643));
#26316=CARTESIAN_POINT('Ctrl Pts',(0.138703525794674,-0.0705489726079016,
2.38522206495621));
#26317=CARTESIAN_POINT('Ctrl Pts',(0.13526802848711,-0.0768482638195142,
2.38469328468739));
#26318=CARTESIAN_POINT('Ctrl Pts',(0.1339134391031,-0.0791851482048425,
2.38449638440864));
#26319=CARTESIAN_POINT('Ctrl Pts',(0.132074980580046,-0.082174545623346,
2.38424333895301));
#26320=CARTESIAN_POINT('Ctrl Pts',(0.13164598316403,-0.0828600724473197,
2.38418522797746));
#26321=CARTESIAN_POINT('Ctrl Pts',(0.130939638441512,-0.0839694593102859,
2.38409104100489));
#26322=CARTESIAN_POINT('Ctrl Pts',(0.130665537400066,-0.0843953574501554,
2.38405484681215));
#26323=CARTESIAN_POINT('Ctrl Pts',(0.130134459947668,-0.0852117559223193,
2.38398539468413));
#26324=CARTESIAN_POINT('Ctrl Pts',(0.129877794261211,-0.0856024507813227,
2.38395212576083));
#26325=CARTESIAN_POINT('Ctrl Pts',(0.12928616605323,-0.0864942370727429,
2.38387611015374));
#26326=CARTESIAN_POINT('Ctrl Pts',(0.128950042879631,-0.0869945529289769,
2.38383340720542));
#26327=CARTESIAN_POINT('Ctrl Pts',(0.128049619270603,-0.0883181389949518,
2.38372027667117));
#26328=CARTESIAN_POINT('Ctrl Pts',(0.127480281856383,-0.0891379632401997,
2.38365003851123));
#26329=CARTESIAN_POINT('Ctrl Pts',(0.123161191456086,-0.0952312601868546,
2.38312660497771));
#26330=CARTESIAN_POINT('Ctrl Pts',(0.119093248057888,-0.100272068148527,
2.38268608754341));
#26331=CARTESIAN_POINT('Ctrl Pts',(0.10762137765009,-0.11280077759827,2.38154957650148));
#26332=CARTESIAN_POINT('Ctrl Pts',(0.0997523984692161,-0.119815795561994,
2.38087010831843));
#26333=CARTESIAN_POINT('Ctrl Pts',(0.0879178224206822,-0.128386312542348,
2.3798944733156));
#26334=CARTESIAN_POINT('Ctrl Pts',(0.0845061164354837,-0.130657182580203,
2.37961761469993));
#26335=CARTESIAN_POINT('Ctrl Pts',(0.0792176263915553,-0.133883433784787,
2.37918863032341));
#26336=CARTESIAN_POINT('Ctrl Pts',(0.0774043624997727,-0.134939874273829,
2.37904156940106));
#26337=CARTESIAN_POINT('Ctrl Pts',(0.0751285530480621,-0.136204840481189,
2.37885630925911));
#26338=CARTESIAN_POINT('Ctrl Pts',(0.0746855116924439,-0.136448277298856,
2.37882021217369));
#26339=CARTESIAN_POINT('Ctrl Pts',(0.0739851104910756,-0.136828691875197,
2.37876308390526));
#26340=CARTESIAN_POINT('Ctrl Pts',(0.073728533316691,-0.136967116001675,
2.37874214299667));
#26341=CARTESIAN_POINT('Ctrl Pts',(0.0732501280673066,-0.137223483256614,
2.37870306990078));
#26342=CARTESIAN_POINT('Ctrl Pts',(0.0730284030408225,-0.137341610466722,
2.37868494968358));
#26343=CARTESIAN_POINT('Ctrl Pts',(0.0725233253336301,-0.137609129013633,
2.3786436473589));
#26344=CARTESIAN_POINT('Ctrl Pts',(0.0722397996698917,-0.137758181041784,
2.37862044445164));
#26345=CARTESIAN_POINT('Ctrl Pts',(0.0713940185817091,-0.138199486819721,
2.37855117971983));
#26346=CARTESIAN_POINT('Ctrl Pts',(0.0708304449827274,-0.138489176735052,
2.37850496259013));
#26347=CARTESIAN_POINT('Ctrl Pts',(0.0665719760524741,-0.140645335941587,
2.3781553468359));
#26348=CARTESIAN_POINT('Ctrl Pts',(0.062806042893632,-0.142366891756567,
2.37784399831596));
#26349=CARTESIAN_POINT('Ctrl Pts',(0.0475972922137978,-0.148598530202747,
2.37659008370091));
#26350=CARTESIAN_POINT('Ctrl Pts',(0.0357051342040492,-0.151895406406671,
2.37562152280738));
#26351=CARTESIAN_POINT('Ctrl Pts',(0.0192972601592593,-0.154408253241854,
2.3743618554564));
#26352=CARTESIAN_POINT('Ctrl Pts',(0.0150212780361088,-0.154882731056818,
2.3740398479449));
#26353=CARTESIAN_POINT('Ctrl Pts',(0.00811726951375727,-0.15536014729364,
2.37353021394204));
#26354=CARTESIAN_POINT('Ctrl Pts',(0.00549950352845257,-0.155474829010473,
2.37333932123971));
#26355=CARTESIAN_POINT('Ctrl Pts',(0.00208643395044463,-0.155538031209154,
2.37309329505412));
#26356=CARTESIAN_POINT('Ctrl Pts',(0.00129281909216219,-0.155546652234968,
2.37303628892556));
#26357=CARTESIAN_POINT('Ctrl Pts',(1.62816883083261E-7,-0.155550800383033,
2.37294375214716));
#26358=CARTESIAN_POINT('Ctrl Pts',(-0.000498843587911407,-0.155550000532587,
2.37290810667281));
#26359=CARTESIAN_POINT('Ctrl Pts',(-0.00145968219985443,-0.155543836689673,
2.37283961528841));
#26360=CARTESIAN_POINT('Ctrl Pts',(-0.00192151049930675,-0.15553881705271,
2.37280675892364));
#26361=CARTESIAN_POINT('Ctrl Pts',(-0.00298051274202501,-0.155522589271181,
2.37273156053725));
#26362=CARTESIAN_POINT('Ctrl Pts',(-0.00357766107942544,-0.155509998357584,
2.3726892623878));
#26363=CARTESIAN_POINT('Ctrl Pts',(-0.00516715045182625,-0.155467323463744,
2.37257694168457));
#26364=CARTESIAN_POINT('Ctrl Pts',(-0.00615931330712721,-0.155431177856745,
2.37250710968175));
#26365=CARTESIAN_POINT('Ctrl Pts',(-0.0137410745203418,-0.155082253463266,
2.37197546235925));
#26366=CARTESIAN_POINT('Ctrl Pts',(-0.0203056524830594,-0.154360038189527,
2.37152701798302));
#26367=CARTESIAN_POINT('Ctrl Pts',(-0.037285816274013,-0.151389475245343,
2.37037570735659));
#26368=CARTESIAN_POINT('Ctrl Pts',(-0.0475499993521492,-0.148485651933286,
2.36968957644462));
#26369=CARTESIAN_POINT('Ctrl Pts',(-0.0610558234716782,-0.143119359274682,
2.36871834511214));
#26370=CARTESIAN_POINT('Ctrl Pts',(-0.0646189346133087,-0.141546292094857,
2.36845489966616));
#26371=CARTESIAN_POINT('Ctrl Pts',(-0.0699384917027309,-0.138955050627056,
2.36804496020318));
#26372=CARTESIAN_POINT('Ctrl Pts',(-0.0717404232971153,-0.138033363048832,
2.36790308473609));
#26373=CARTESIAN_POINT('Ctrl Pts',(-0.0739612288765335,-0.136842192252523,
2.36772378993123));
#26374=CARTESIAN_POINT('Ctrl Pts',(-0.0743975817882275,-0.136605449244348,
2.36768834457107));
#26375=CARTESIAN_POINT('Ctrl Pts',(-0.0750866579090631,-0.136227310638504,
2.36763201391692));
#26376=CARTESIAN_POINT('Ctrl Pts',(-0.0753401375512388,-0.136087288273885,
2.36761121565407));
#26377=CARTESIAN_POINT('Ctrl Pts',(-0.0758192264837021,-0.135820890390524,
2.36757175744182));
#26378=CARTESIAN_POINT('Ctrl Pts',(-0.0760449135485121,-0.13569465903409,
2.36755310681805));
#26379=CARTESIAN_POINT('Ctrl Pts',(-0.0765606930099079,-0.135404482271449,
2.36751034080948));
#26380=CARTESIAN_POINT('Ctrl Pts',(-0.0768505748603377,-0.135240166634578,
2.36748620178436));
#26381=CARTESIAN_POINT('Ctrl Pts',(-0.0776185794178367,-0.134801566996752,
2.36742197813306));
#26382=CARTESIAN_POINT('Ctrl Pts',(-0.0780957700560277,-0.134525674168724,
2.36738179420472));
#26383=CARTESIAN_POINT('Ctrl Pts',(-0.0814141682137354,-0.132583500873867,
2.36710045245604));
#26384=CARTESIAN_POINT('Ctrl Pts',(-0.0842030383169656,-0.130830026029818,
2.36685425420449));
#26385=CARTESIAN_POINT('Ctrl Pts',(-0.0880805307994597,-0.128216748570522,
2.36650001274247));
#26386=CARTESIAN_POINT('Ctrl Pts',(-0.0892167937467142,-0.127428717417893,
2.36639468937984));
#26387=CARTESIAN_POINT('Ctrl Pts',(-0.0913568074056298,-0.125901902927371,
2.36619361249075));
#26388=CARTESIAN_POINT('Ctrl Pts',(-0.0923624946677538,-0.125165989324826,
2.36609794737246));
#26389=CARTESIAN_POINT('Ctrl Pts',(-0.104880435575903,-0.115772940957153,
2.36489324984584));
#26390=CARTESIAN_POINT('Ctrl Pts',(-0.115148035305615,-0.105566905191347,
2.36376479872363));
#26391=CARTESIAN_POINT('Ctrl Pts',(-0.125701779821125,-0.091673827059514,
2.36247507984567));
#26392=CARTESIAN_POINT('Ctrl Pts',(-0.127467955827375,-0.0892017413483719,
2.36225321909189));
#26393=CARTESIAN_POINT('Ctrl Pts',(-0.129629484486658,-0.0859808518666029,
2.36197342586439));
#26394=CARTESIAN_POINT('Ctrl Pts',(-0.130092578962798,-0.0852785499775909,
2.36191296224966));
#26395=CARTESIAN_POINT('Ctrl Pts',(-0.130828799568427,-0.0841420865015539,
2.36181597908327));
#26396=CARTESIAN_POINT('Ctrl Pts',(-0.131105509857546,-0.0837102790219607,
2.36177932687718));
#26397=CARTESIAN_POINT('Ctrl Pts',(-0.131628582559035,-0.0828850662123731,
2.36170965286161));
#26398=CARTESIAN_POINT('Ctrl Pts',(-0.131875328951331,-0.0824919121492293,
2.36167661716648));
#26399=CARTESIAN_POINT('Ctrl Pts',(-0.132434749791534,-0.0815916323945268,
2.3616013272399));
#26400=CARTESIAN_POINT('Ctrl Pts',(-0.132746279469288,-0.0810838006882076,
2.36155911523679));
#26401=CARTESIAN_POINT('Ctrl Pts',(-0.133549926558461,-0.0797567109642289,
2.36144946386094));
#26402=CARTESIAN_POINT('Ctrl Pts',(-0.134037430604619,-0.0789346761347597,
2.36138219189014));
#26403=CARTESIAN_POINT('Ctrl Pts',(-0.137280067956952,-0.0733502300511387,
2.36092942835196));
#26404=CARTESIAN_POINT('Ctrl Pts',(-0.139788635886577,-0.0684486805213911,
2.36055293618593));
#26405=CARTESIAN_POINT('Ctrl Pts',(-0.148095241906383,-0.0498467703231422,
2.35918168311549));
#26406=CARTESIAN_POINT('Ctrl Pts',(-0.152179113346546,-0.0354726472762498,
2.35823929183334));
#26407=CARTESIAN_POINT('Ctrl Pts',(-0.154507966389611,-0.018161934973515,
2.35703742847534));
#26408=CARTESIAN_POINT('Ctrl Pts',(-0.154790021417189,-0.0155760937493597,
2.35685598884916));
#26409=CARTESIAN_POINT('Ctrl Pts',(-0.155052295667947,-0.0124451271287232,
2.35663267220013));
#26410=CARTESIAN_POINT('Ctrl Pts',(-0.155094669173755,-0.0119054253128199,
2.35659404801459));
#26411=CARTESIAN_POINT('Ctrl Pts',(-0.155156281376314,-0.0110644468220585,
2.35653364497798));
#26412=CARTESIAN_POINT('Ctrl Pts',(-0.155177462272496,-0.010763309549938,
2.35651197242452));
#26413=CARTESIAN_POINT('Ctrl Pts',(-0.155215151605479,-0.0102042161232831,
2.35647165116354));
#26414=CARTESIAN_POINT('Ctrl Pts',(-0.155231893726048,-0.00994627979441159,
2.35645301568399));
#26415=CARTESIAN_POINT('Ctrl Pts',(-0.155268332411986,-0.00936237637902016,
2.3564107540604));
#26416=CARTESIAN_POINT('Ctrl Pts',(-0.155287645260742,-0.00903639117765526,
2.35638710704518));
#26417=CARTESIAN_POINT('Ctrl Pts',(-0.155342996497391,-0.00804947633369134,
2.35631536070114));
#26418=CARTESIAN_POINT('Ctrl Pts',(-0.155375842157526,-0.00738838694983366,
2.35626709021258));
#26419=CARTESIAN_POINT('Ctrl Pts',(-0.155597422658225,-0.00226961719401098,
2.3558918046594));
#26420=CARTESIAN_POINT('Ctrl Pts',(-0.155598482864865,0.00219363379957986,
2.35555564534585));
#26421=CARTESIAN_POINT('Ctrl Pts',(-0.154768234457253,0.0215955998681862,
2.35407160552423));
#26422=CARTESIAN_POINT('Ctrl Pts',(-0.151975677561831,0.0363747912655102,
2.35289228841612));
#26423=CARTESIAN_POINT('Ctrl Pts',(-0.145908861679386,0.0540387766803025,
2.35150345769644));
#26424=CARTESIAN_POINT('Ctrl Pts',(-0.144577515450517,0.057505927437592,
2.3512312760094));
#26425=CARTESIAN_POINT('Ctrl Pts',(-0.142771863936644,0.0617478929263152,
2.3508984255192));
#26426=CARTESIAN_POINT('Ctrl Pts',(-0.142413338486806,0.0625703483803747,
2.35083389562364));
#26427=CARTESIAN_POINT('Ctrl Pts',(-0.141833964948203,0.0638686463804223,
2.35073202472981));
#26428=CARTESIAN_POINT('Ctrl Pts',(-0.141617796089092,0.0643465418394741,
2.35069452527094));
#26429=CARTESIAN_POINT('Ctrl Pts',(-0.141207132078897,0.0652423236229802,
2.35062422855432));
#26430=CARTESIAN_POINT('Ctrl Pts',(-0.141013189305969,0.0656604553122312,
2.35059141283929));
#26431=CARTESIAN_POINT('Ctrl Pts',(-0.140573878375023,0.0665966652099511,
2.3505179278292));
#26432=CARTESIAN_POINT('Ctrl Pts',(-0.140327498128499,0.0671142636362083,
2.35047729385793));
#26433=CARTESIAN_POINT('Ctrl Pts',(-0.139693852958658,0.0684266880519785,
2.35037423703304));
#26434=CARTESIAN_POINT('Ctrl Pts',(-0.139302658561361,0.0692196039236709,
2.35031195055833));
#26435=CARTESIAN_POINT('Ctrl Pts',(-0.136991318876314,0.0738055181699215,
2.34995149497577));
#26436=CARTESIAN_POINT('Ctrl Pts',(-0.134922960566627,0.0775221018112844,
2.3496585801293));
#26437=CARTESIAN_POINT('Ctrl Pts',(-0.131842760910188,0.0825591842526366,
2.34925765971958));
#26438=CARTESIAN_POINT('Ctrl Pts',(-0.130958354020009,0.0839550015511547,
2.34914611366222));
#26439=CARTESIAN_POINT('Ctrl Pts',(-0.122055105888294,0.0975234507064667,
2.3480558432599));
#26440=CARTESIAN_POINT('Ctrl Pts',(-0.112386401634549,0.108524038230606,
2.34713140761696));
#26441=CARTESIAN_POINT('Ctrl Pts',(-0.0992539383505594,0.119799601629702,
2.34594251052381));
#26442=CARTESIAN_POINT('Ctrl Pts',(-0.0971315254245216,0.121526758883124,
2.34575187953925));
#26443=CARTESIAN_POINT('Ctrl Pts',(-0.0945311764809605,0.123531206609171,
2.34551855845236));
#26444=CARTESIAN_POINT('Ctrl Pts',(-0.0940957427491966,0.123863204809224,
2.34547949606559));
#26445=CARTESIAN_POINT('Ctrl Pts',(-0.0934171873717764,0.124374929182501,
2.34541861931852));
#26446=CARTESIAN_POINT('Ctrl Pts',(-0.0931752733715439,0.124556261719363,
2.34539691514289));
#26447=CARTESIAN_POINT('Ctrl Pts',(-0.0927264357954126,0.124890659585645,
2.34535664137385));
#26448=CARTESIAN_POINT('Ctrl Pts',(-0.0925196603170567,0.125043917079547,
2.34533808550703));
#26449=CARTESIAN_POINT('Ctrl Pts',(-0.0920524846099039,0.125388384413902,
2.34529615694643));
#26450=CARTESIAN_POINT('Ctrl Pts',(-0.0917918703910129,0.125579295243042,
2.34527276418319));
#26451=CARTESIAN_POINT('Ctrl Pts',(-0.0910241728054328,0.126137999324275,
2.34520385159877));
#26452=CARTESIAN_POINT('Ctrl Pts',(-0.090515468499498,0.126503536847386,
2.34515818257502));
#26453=CARTESIAN_POINT('Ctrl Pts',(-0.0869340474896806,0.129044362151233,
2.34483670254938));
#26454=CARTESIAN_POINT('Ctrl Pts',(-0.0837857480964293,0.131110329595634,
2.34455434347846));
#26455=CARTESIAN_POINT('Ctrl Pts',(-0.0797111245064023,0.133577459955539,
2.34419206343651));
#26456=CARTESIAN_POINT('Ctrl Pts',(-0.078851322236165,0.134086800562523,
2.34411578760551));
#26457=CARTESIAN_POINT('Ctrl Pts',(-0.0733888200384716,0.137252038576912,
2.34363250315201));
#26458=CARTESIAN_POINT('Ctrl Pts',(-0.0686576019598595,0.139678813674574,
2.34321990111197));
#26459=CARTESIAN_POINT('Ctrl Pts',(-0.0637706568557826,0.141877087107655,
2.34280436535828));
#26460=CARTESIAN_POINT('Ctrl Pts',(-0.0637296451045094,0.141895513869592,
2.34280087886671));
#26461=CARTESIAN_POINT('Ctrl Pts',(-0.063688625846537,0.141913922635448,
2.34279739246514));
#26462=CARTESIAN_POINT('',(0.143545299885862,-0.0599211930845659,2.4));
#26463=CARTESIAN_POINT('Origin',(0.,0.,2.4));
#26464=CARTESIAN_POINT('',(-0.155549935368252,0.000141798916507806,2.36940562256037));
#26465=CARTESIAN_POINT('Ctrl Pts',(-0.155549935368252,0.000141798916507806,
2.36940562256037));
#26466=CARTESIAN_POINT('Ctrl Pts',(-0.155559235828691,-0.0100605781955904,
2.37013602172971));
#26467=CARTESIAN_POINT('Ctrl Pts',(-0.154560452504158,-0.0202869430343912,
2.37086642089906));
#26468=CARTESIAN_POINT('Ctrl Pts',(-0.152565879395267,-0.0303225154686899,
2.3715968200684));
#26469=CARTESIAN_POINT('Ctrl Pts',(-0.150573087012895,-0.0403491282865703,
2.37232656714775));
#26470=CARTESIAN_POINT('Ctrl Pts',(-0.147586439117774,-0.0501843583611561,
2.37305631422709));
#26471=CARTESIAN_POINT('Ctrl Pts',(-0.143669539331068,-0.0596226967555041,
2.37378606130644));
#26472=CARTESIAN_POINT('Ctrl Pts',(-0.139743199481172,-0.0690837823518981,
2.3745175671386));
#26473=CARTESIAN_POINT('Ctrl Pts',(-0.134882515659627,-0.078145198024074,
2.37524907297077));
#26474=CARTESIAN_POINT('Ctrl Pts',(-0.12919902487086,-0.0866222516009543,
2.37598057880293));
#26475=CARTESIAN_POINT('Ctrl Pts',(-0.124563189169144,-0.0935367041931399,
2.37657724394744));
#26476=CARTESIAN_POINT('Ctrl Pts',(-0.119380988048105,-0.100062643096905,
2.37717390909194));
#26477=CARTESIAN_POINT('Ctrl Pts',(-0.113732697104638,-0.106116332905471,
2.37777057423645));
#26478=CARTESIAN_POINT('Ctrl Pts',(-0.106829383557614,-0.113515122961299,
2.37849981545584));
#26479=CARTESIAN_POINT('Ctrl Pts',(-0.0991717628314197,-0.120268582175319,
2.37922905667523));
#26480=CARTESIAN_POINT('Ctrl Pts',(-0.0909057529026238,-0.126221815028968,
2.37995829789462));
#26481=CARTESIAN_POINT('Ctrl Pts',(-0.0824734057365558,-0.13229484501742,
2.38070221366325));
#26482=CARTESIAN_POINT('Ctrl Pts',(-0.0734085507228057,-0.137534273118749,
2.38144612943189));
#26483=CARTESIAN_POINT('Ctrl Pts',(-0.0639035509383708,-0.141817272140833,
2.38219004520052));
#26484=CARTESIAN_POINT('Ctrl Pts',(-0.0546060702612576,-0.146006762046254,
2.38291771933425));
#26485=CARTESIAN_POINT('Ctrl Pts',(-0.0448884161511158,-0.149280862880942,
2.38364539346799));
#26486=CARTESIAN_POINT('Ctrl Pts',(-0.0349538919347246,-0.151571857343689,
2.38437306760172));
#26487=CARTESIAN_POINT('Ctrl Pts',(-0.0246867609076323,-0.153939554056588,
2.3851251041878));
#26488=CARTESIAN_POINT('Ctrl Pts',(-0.0141889885206651,-0.155256727301847,
2.38587714077389));
#26489=CARTESIAN_POINT('Ctrl Pts',(-0.00369546276844564,-0.155506096520127,
2.38662917735997));
#26490=CARTESIAN_POINT('Ctrl Pts',(0.00679806298377526,-0.155755465738407,
2.38738121394606));
#26491=CARTESIAN_POINT('Ctrl Pts',(0.017286243111928,-0.154937181577277,
2.38813325053214));
#26492=CARTESIAN_POINT('Ctrl Pts',(0.0275400002621714,-0.153092621917451,
2.38888528711823));
#26493=CARTESIAN_POINT('Ctrl Pts',(0.0378733824294785,-0.151233738425664,
2.38964316360525));
#26494=CARTESIAN_POINT('Ctrl Pts',(0.0480492838063025,-0.148318709903011,
2.39040104009227));
#26495=CARTESIAN_POINT('Ctrl Pts',(0.0578456617134533,-0.144394189360004,
2.39115891657929));
#26496=CARTESIAN_POINT('Ctrl Pts',(0.0676191605628735,-0.140478834381343,
2.3919150230754));
#26497=CARTESIAN_POINT('Ctrl Pts',(0.0770140719283949,-0.13555891450073,
2.39267112957151));
#26498=CARTESIAN_POINT('Ctrl Pts',(0.0858240262363051,-0.129730640253527,
2.39342723606762));
#26499=CARTESIAN_POINT('Ctrl Pts',(0.0946200577567245,-0.123911576703786,
2.39418214765287));
#26500=CARTESIAN_POINT('Ctrl Pts',(0.102832228730433,-0.117187452514392,
2.39493705923811));
#26501=CARTESIAN_POINT('Ctrl Pts',(0.110281164467125,-0.109698984789171,
2.39569197082336));
#26502=CARTESIAN_POINT('Ctrl Pts',(0.117734845393054,-0.102205746691685,
2.3964473633093));
#26503=CARTESIAN_POINT('Ctrl Pts',(0.124423690575448,-0.0939477881347089,
2.39720275579524));
#26504=CARTESIAN_POINT('Ctrl Pts',(0.130204459076775,-0.0851034742917383,
2.39795814828117));
#26505=CARTESIAN_POINT('Ctrl Pts',(0.135412997384256,-0.0771346467138956,
2.39863876552078));
#26506=CARTESIAN_POINT('Ctrl Pts',(0.139884590728665,-0.0686906712393692,
2.39931938276039));
#26507=CARTESIAN_POINT('Ctrl Pts',(0.143545299885862,-0.059921193084566,
2.4));
#26508=CARTESIAN_POINT('Ctrl Pts',(-0.155549934503847,0.000142743998182768,
2.36941789089093));
#26509=CARTESIAN_POINT('Ctrl Pts',(-0.155540753141536,0.0101477902640131,
2.36864722383324));
#26510=CARTESIAN_POINT('Ctrl Pts',(-0.154566316755707,0.020129469112165,
2.36786767664586));
#26511=CARTESIAN_POINT('Ctrl Pts',(-0.15240769985127,0.0311311135252802,
2.36703279674523));
#26512=CARTESIAN_POINT('Ctrl Pts',(-0.152162069399693,0.0323103396982948,
2.36694365403721));
#26513=CARTESIAN_POINT('Ctrl Pts',(-0.151774510091642,0.0340683940983547,
2.36681138487069));
#26514=CARTESIAN_POINT('Ctrl Pts',(-0.151642919170991,0.0346494225623182,
2.36676777389633));
#26515=CARTESIAN_POINT('Ctrl Pts',(-0.151425582149855,0.0355840970733577,
2.36669780064557));
#26516=CARTESIAN_POINT('Ctrl Pts',(-0.151341929135608,0.0359382162374241,
2.3666713321065));
#26517=CARTESIAN_POINT('Ctrl Pts',(-0.151194151876046,0.0365541184547088,
2.36662537386571));
#26518=CARTESIAN_POINT('Ctrl Pts',(-0.151130588873795,0.0368160324731053,
2.36660585435635));
#26519=CARTESIAN_POINT('Ctrl Pts',(-0.151001834577968,0.0373406172652141,
2.36656680954848));
#26520=CARTESIAN_POINT('Ctrl Pts',(-0.150936637827199,0.0376032858681038,
2.36654728462139));
#26521=CARTESIAN_POINT('Ctrl Pts',(-0.150809816011158,0.0381085890813387,
2.36650977476321));
#26522=CARTESIAN_POINT('Ctrl Pts',(-0.150748291449749,0.0383512423927614,
2.36649178484732));
#26523=CARTESIAN_POINT('Ctrl Pts',(-0.150580647257716,0.0390057955904033,
2.36644331682817));
#26524=CARTESIAN_POINT('Ctrl Pts',(-0.150473423017106,0.039417412333195,
2.36641290113435));
#26525=CARTESIAN_POINT('Ctrl Pts',(-0.150067489463824,0.0409499295291554,
2.36629987749851));
#26526=CARTESIAN_POINT('Ctrl Pts',(-0.149757923034017,0.0420679548025645,
2.36621786027761));
#26527=CARTESIAN_POINT('Ctrl Pts',(-0.146872923428985,0.0520516949238728,
2.36548852253291));
#26528=CARTESIAN_POINT('Ctrl Pts',(-0.143525042585431,0.0606765989985166,
2.36487954022323));
#26529=CARTESIAN_POINT('Ctrl Pts',(-0.13712921829303,0.0736094174797964,
2.3639285884703));
#26530=CARTESIAN_POINT('Ctrl Pts',(-0.134595612222951,0.0781459401903763,
2.36358716336465));
#26531=CARTESIAN_POINT('Ctrl Pts',(-0.128241386927552,0.0882945737058474,
2.3627897749356));
#26532=CARTESIAN_POINT('Ctrl Pts',(-0.124271295392331,0.093799851503765,
2.36233139260164));
#26533=CARTESIAN_POINT('Ctrl Pts',(-0.1189513152358,0.100244068046163,2.36174923267517));
#26534=CARTESIAN_POINT('Ctrl Pts',(-0.117929122285336,0.101444617278949,
2.36163869328799));
#26535=CARTESIAN_POINT('Ctrl Pts',(-0.116549163734938,0.103016309666412,
2.36149107166756));
#26536=CARTESIAN_POINT('Ctrl Pts',(-0.116207523949633,0.103401542496564,
2.36145465165947));
#26537=CARTESIAN_POINT('Ctrl Pts',(-0.115527842945404,0.104160327443861,
2.36138244022979));
#26538=CARTESIAN_POINT('Ctrl Pts',(-0.11518988700805,0.104533947735041,
2.36134665261909));
#26539=CARTESIAN_POINT('Ctrl Pts',(-0.114534093651337,0.105251904857536,
2.36127742994386));
#26540=CARTESIAN_POINT('Ctrl Pts',(-0.114216503077476,0.105596460644433,
2.36124400550691));
#26541=CARTESIAN_POINT('Ctrl Pts',(-0.11348237371508,0.10638573510344,2.36116696593551));
#26542=CARTESIAN_POINT('Ctrl Pts',(-0.113064771349945,0.106829449299423,
2.36112330582322));
#26543=CARTESIAN_POINT('Ctrl Pts',(-0.111940987178267,0.108009531116785,
2.36100623968675));
#26544=CARTESIAN_POINT('Ctrl Pts',(-0.111230160081044,0.108741412621635,
2.36093263441049));
#26545=CARTESIAN_POINT('Ctrl Pts',(-0.105348184852228,0.114679591069475,
2.36032704882579));
#26546=CARTESIAN_POINT('Ctrl Pts',(-0.0998226113658964,0.119520137638094,
2.35977927590904));
#26547=CARTESIAN_POINT('Ctrl Pts',(-0.0875313188339863,0.128839041187233,
2.35860231343413));
#26548=CARTESIAN_POINT('Ctrl Pts',(-0.0807146275283843,0.133215479215336,
2.35797216234008));
#26549=CARTESIAN_POINT('Ctrl Pts',(-0.0703474097044516,0.138782504958481,
2.35706121510311));
#26550=CARTESIAN_POINT('Ctrl Pts',(-0.0670451391377526,0.140407574908435,
2.3567776620958));
#26551=CARTESIAN_POINT('Ctrl Pts',(-0.0636886247653984,0.141913923120645,
2.35649769913034));
#26552=CARTESIAN_POINT('Ctrl Pts',(-0.0684401807326106,0.139375953783005,
-0.0231689358544845));
#26553=CARTESIAN_POINT('Ctrl Pts',(-0.114796989999545,0.116613226798551,
-0.0194634912834569));
#26554=CARTESIAN_POINT('Ctrl Pts',(-0.182204502677244,0.021600584598116,
-0.0120531424185038));
#26555=CARTESIAN_POINT('Ctrl Pts',(-0.116820455017618,-0.141707599811532,
-0.000937889259625344));
#26556=CARTESIAN_POINT('Ctrl Pts',(0.0556554964189628,-0.174830787340543,
0.0101768236221509));
#26557=CARTESIAN_POINT('Ctrl Pts',(0.177103618810993,-0.0481310406253423,
0.021291536503927));
#26558=CARTESIAN_POINT('Ctrl Pts',(0.136462891783692,0.122747837682665,
0.0324062493857032));
#26559=CARTESIAN_POINT('Ctrl Pts',(-0.0291242938817204,0.181195489255479,
0.0435209622674794));
#26560=CARTESIAN_POINT('Ctrl Pts',(-0.168038372731085,0.0737999881880242,
0.0546356751492556));
#26561=CARTESIAN_POINT('Ctrl Pts',(-0.153127523366183,-0.101172781343492,
0.0657503880310317));
#26562=CARTESIAN_POINT('Ctrl Pts',(0.00196713021444944,-0.18351791358781,
0.076865100912808));
#26563=CARTESIAN_POINT('Ctrl Pts',(0.155259338957376,-0.0978661493738991,
0.087979813794584));
#26564=CARTESIAN_POINT('Ctrl Pts',(0.166420139267564,0.0773797195872082,
0.0990945266763604));
#26565=CARTESIAN_POINT('Ctrl Pts',(0.0252310584054888,0.18178697236432,
0.110209239558137));
#26566=CARTESIAN_POINT('Ctrl Pts',(-0.139055574687841,0.11977790064492,
0.121323952439913));
#26567=CARTESIAN_POINT('Ctrl Pts',(-0.176043812140842,-0.0518822906588397,
0.132438665321689));
#26568=CARTESIAN_POINT('Ctrl Pts',(-0.0518725564901114,-0.176046614996211,
0.143553378203466));
#26569=CARTESIAN_POINT('Ctrl Pts',(0.119785431798764,-0.139049045125415,
0.154668091085242));
#26570=CARTESIAN_POINT('Ctrl Pts',(0.181785783219421,0.0252411197918558,
0.165782803967018));
#26571=CARTESIAN_POINT('Ctrl Pts',(0.077370206262428,0.166424257025588,
0.176897516848794));
#26572=CARTESIAN_POINT('Ctrl Pts',(-0.097873973618601,0.155254209412122,
0.18801222973057));
#26573=CARTESIAN_POINT('Ctrl Pts',(-0.183519360433008,0.00195658265477414,
0.199126942612347));
#26574=CARTESIAN_POINT('Ctrl Pts',(-0.101161822572116,-0.153132195043624,
0.210241655494122));
#26575=CARTESIAN_POINT('Ctrl Pts',(0.0738043738200084,-0.168036002759876,
0.221356368375899));
#26576=CARTESIAN_POINT('Ctrl Pts',(0.181206306397723,-0.0291111363940454,
0.232471081257675));
#26577=CARTESIAN_POINT('Ctrl Pts',(0.122722802371927,0.136463538999617,
0.243585794139451));
#26578=CARTESIAN_POINT('Ctrl Pts',(-0.0481073744247173,0.177112575131921,
0.254700507021226));
#26579=CARTESIAN_POINT('Ctrl Pts',(-0.174897622649273,0.0556237837726867,
0.265815219903004));
#26580=CARTESIAN_POINT('Ctrl Pts',(-0.141577723269147,-0.116785838178545,
0.27692993278478));
#26581=CARTESIAN_POINT('Ctrl Pts',(0.0213495991278188,-0.182283785205111,
0.288044645666556));
#26582=CARTESIAN_POINT('Ctrl Pts',(0.164732416494676,-0.08090991709903,
0.299159358548332));
#26583=CARTESIAN_POINT('Ctrl Pts',(0.157310831167827,0.094532989617669,
0.310274071430108));
#26584=CARTESIAN_POINT('Ctrl Pts',(0.00587893848749207,0.1834356067178,
0.321388784311885));
#26585=CARTESIAN_POINT('Ctrl Pts',(-0.150934832429759,0.104411972918147,
0.332503497193661));
#26586=CARTESIAN_POINT('Ctrl Pts',(-0.16957520837079,-0.0701956724823281,
0.343618210075437));
#26587=CARTESIAN_POINT('Ctrl Pts',(-0.0329778445068435,-0.180542641780405,
0.354732922957213));
#26588=CARTESIAN_POINT('Ctrl Pts',(0.133809109534271,-0.125611726900579,
0.365847635838989));
#26589=CARTESIAN_POINT('Ctrl Pts',(0.17810042326896,0.0443105287795206,
0.376962348720765));
#26590=CARTESIAN_POINT('Ctrl Pts',(0.0593495834231662,0.173668680759705,
0.388077061602541));
#26591=CARTESIAN_POINT('Ctrl Pts',(-0.113732872921998,0.144041720852737,
0.399191774484318));
#26592=CARTESIAN_POINT('Ctrl Pts',(-0.182698493418309,-0.0174483303496573,
0.410306487366094));
#26593=CARTESIAN_POINT('Ctrl Pts',(-0.0844126538894276,-0.162965295669527,
0.42142120024787));
#26594=CARTESIAN_POINT('Ctrl Pts',(0.0911488070387178,-0.159295570260851,
0.432535913129646));
#26595=CARTESIAN_POINT('Ctrl Pts',(0.183268030586852,-0.0097986067442389,
0.443650626011422));
#26596=CARTESIAN_POINT('Ctrl Pts',(0.10761441092159,0.148668497978929,0.454765338893199));
#26597=CARTESIAN_POINT('Ctrl Pts',(-0.0665548943940058,0.171036925140492,
0.465880051774975));
#26598=CARTESIAN_POINT('Ctrl Pts',(-0.179796476382766,0.03682948288604,
0.476994764656751));
#26599=CARTESIAN_POINT('Ctrl Pts',(-0.128443251814735,-0.131093534518557,
0.488109477538528));
#26600=CARTESIAN_POINT('Ctrl Pts',(0.0404934349617796,-0.179006886611403,
0.499224190420303));
#26601=CARTESIAN_POINT('Ctrl Pts',(0.172360379169117,-0.0630482626405321,
0.51033890330208));
#26602=CARTESIAN_POINT('Ctrl Pts',(0.146439897070056,0.11062793623413,0.521453616183855));
#26603=CARTESIAN_POINT('Ctrl Pts',(-0.013539088373249,0.183029715662056,
0.532568329065633));
#26604=CARTESIAN_POINT('Ctrl Pts',(-0.161123706159393,0.0878768174365303,
0.543683041947407));
#26605=CARTESIAN_POINT('Ctrl Pts',(-0.161207517586238,-0.0877229730629007,
0.554797754829185));
#26606=CARTESIAN_POINT('Ctrl Pts',(-0.0137137974260919,-0.183016708224871,
0.56591246771096));
#26607=CARTESIAN_POINT('Ctrl Pts',(0.146334227912434,-0.110767673400607,
0.577027180592736));
#26608=CARTESIAN_POINT('Ctrl Pts',(0.17242048480891,0.0628837033544609,
0.588141893474512));
#26609=CARTESIAN_POINT('Ctrl Pts',(0.0406642916501698,0.178968151116062,
0.599256606356289));
#26610=CARTESIAN_POINT('Ctrl Pts',(-0.128318054949308,0.131216083249494,
0.610371319238065));
#26611=CARTESIAN_POINT('Ctrl Pts',(-0.179831550895884,-0.0366578372478885,
0.621486032119841));
#26612=CARTESIAN_POINT('Ctrl Pts',(-0.0667181312987861,-0.170973315711281,
0.632600745001618));
#26613=CARTESIAN_POINT('Ctrl Pts',(0.10747244696062,-0.148771156053881,
0.643715457883394));
#26614=CARTESIAN_POINT('Ctrl Pts',(0.183277300574292,0.00962365956964026,
0.654830170765169));
#26615=CARTESIAN_POINT('Ctrl Pts',(0.0913008247582609,0.159208489496549,
0.665944883646947));
#26616=CARTESIAN_POINT('Ctrl Pts',(-0.0842570531624994,0.163045799460407,
0.677059596528721));
#26617=CARTESIAN_POINT('Ctrl Pts',(-0.182681754475266,0.01762272144563,
0.688174309410499));
#26618=CARTESIAN_POINT('Ctrl Pts',(-0.113870319439624,-0.143933088899077,
0.699289022292274));
#26619=CARTESIAN_POINT('Ctrl Pts',(0.0591837769528756,-0.173725255144161,
0.710403735174051));
#26620=CARTESIAN_POINT('Ctrl Pts',(0.178058044491996,-0.0444805184434471,
0.721518448055827));
#26621=CARTESIAN_POINT('Ctrl Pts',(0.133928954130774,0.125483939110744,
0.732633160937603));
#26622=CARTESIAN_POINT('Ctrl Pts',(-0.032805488354141,0.180574039283497,
0.743747873819379));
#26623=CARTESIAN_POINT('Ctrl Pts',(-0.169508124219243,0.0703575124132829,
0.754862586701155));
#26624=CARTESIAN_POINT('Ctrl Pts',(-0.151034432511191,-0.104267847035095,
0.765977299582931));
#26625=CARTESIAN_POINT('Ctrl Pts',(0.00570383313473486,-0.183441135018519,
0.777092012464709));
#26626=CARTESIAN_POINT('Ctrl Pts',(0.15722052085916,-0.0946831112188752,
0.788206725346483));
#26627=CARTESIAN_POINT('Ctrl Pts',(0.164809575861347,0.0807526311256457,
0.799321438228262));
#26628=CARTESIAN_POINT('Ctrl Pts',(0.0215235925793826,0.182263322398634,
0.810436151110036));
#26629=CARTESIAN_POINT('Ctrl Pts',(-0.141466178164294,0.116920931252278,
0.821550863991813));
#26630=CARTESIAN_POINT('Ctrl Pts',(-0.174950639917874,-0.0554568059090855,
0.832665576873588));
#26631=CARTESIAN_POINT('Ctrl Pts',(-0.0482764194013637,-0.177066572393253,
0.843780289755366));
#26632=CARTESIAN_POINT('Ctrl Pts',(0.122592482081562,-0.136580624784021,
0.854895002637141));
#26633=CARTESIAN_POINT('Ctrl Pts',(0.181234012486454,0.0289381486514157,
0.866009715518918));
#26634=CARTESIAN_POINT('Ctrl Pts',(0.0739647429309842,0.167965474227488,
0.877124428400693));
#26635=CARTESIAN_POINT('Ctrl Pts',(-0.101015600832807,0.15322869221428,
0.88823914128247));
#26636=CARTESIAN_POINT('Ctrl Pts',(-0.183521144128887,-0.00178140027397675,
0.899353854164246));
#26637=CARTESIAN_POINT('Ctrl Pts',(-0.0980221312474096,-0.155160708670163,
0.910468567046022));
#26638=CARTESIAN_POINT('Ctrl Pts',(0.077211308334424,-0.166498040813092,
0.921583279927798));
#26639=CARTESIAN_POINT('Ctrl Pts',(0.181761603201863,-0.0254146282837278,
0.932697992809575));
#26640=CARTESIAN_POINT('Ctrl Pts',(0.119918114829785,0.138934622988592,
0.943812705691351));
#26641=CARTESIAN_POINT('Ctrl Pts',(-0.0517044933012578,0.176096079177736,
0.954927418573126));
#26642=CARTESIAN_POINT('Ctrl Pts',(-0.175994187883316,0.052050259947511,
0.966042131454904));
#26643=CARTESIAN_POINT('Ctrl Pts',(-0.139169883500762,-0.119645005143115,
0.977156844336678));
#26644=CARTESIAN_POINT('Ctrl Pts',(0.0250575853607977,-0.181811168923138,
0.988271557218456));
#26645=CARTESIAN_POINT('Ctrl Pts',(0.16634607066597,-0.0775381744904013,
0.999386270100231));
#26646=CARTESIAN_POINT('Ctrl Pts',(0.155352932473362,0.0977171945014716,
1.01050098298201));
#26647=CARTESIAN_POINT('Ctrl Pts',(0.00214184661615762,0.183517291344398,
1.02161569586379));
#26648=CARTESIAN_POINT('Ctrl Pts',(-0.153029994182151,0.101316359043948,
1.03273040874556));
#26649=CARTESIAN_POINT('Ctrl Pts',(-0.168110422754029,-0.0736347030331013,
1.04384512162734));
#26650=CARTESIAN_POINT('Ctrl Pts',(-0.0292940505094485,-0.181176826150757,
1.05495983450911));
#26651=CARTESIAN_POINT('Ctrl Pts',(0.136339580192428,-0.122860500577948,
1.06607454739089));
#26652=CARTESIAN_POINT('Ctrl Pts',(0.177161049503372,0.0479285537876487,
1.07718926027266));
#26653=CARTESIAN_POINT('Ctrl Pts',(0.0558003155862178,0.174841380999436,
1.08830397315444));
#26654=CARTESIAN_POINT('Ctrl Pts',(-0.116642855175632,0.141695547092308,
1.09941868603622));
#26655=CARTESIAN_POINT('Ctrl Pts',(-0.182305244855916,-0.0211655717460261,
1.11053339891799));
#26656=CARTESIAN_POINT('Ctrl Pts',(-0.0810761741748326,-0.16465065353798,
1.12164811179977));
#26657=CARTESIAN_POINT('Ctrl Pts',(0.0943741352821535,-0.157406182594767,
1.13276282468155));
#26658=CARTESIAN_POINT('Ctrl Pts',(0.183429578425622,-0.00606411476721494,
1.14387753756332));
#26659=CARTESIAN_POINT('Ctrl Pts',(0.104564289276848,0.150829351047266,
1.1549922504451));
#26660=CARTESIAN_POINT('Ctrl Pts',(-0.0700244495886578,0.169645984889467,
1.16610696332687));
#26661=CARTESIAN_POINT('Ctrl Pts',(-0.180509258465268,0.0331600865142199,
1.17722167620865));
#26662=CARTESIAN_POINT('Ctrl Pts',(-0.125746743943006,-0.133682235607592,
1.18833638909043));
#26663=CARTESIAN_POINT('Ctrl Pts',(0.0441307128230818,-0.178145064245514,
1.1994511019722));
#26664=CARTESIAN_POINT('Ctrl Pts',(0.173608678528705,-0.059524872690566,
1.21056581485398));
#26665=CARTESIAN_POINT('Ctrl Pts',(0.144156461430417,0.113587404042756,
1.22168052773576));
#26666=CARTESIAN_POINT('Ctrl Pts',(-0.017263886303192,0.182716014511652,
1.23279524061753));
#26667=CARTESIAN_POINT('Ctrl Pts',(-0.162879997582005,0.0845771252585338,
1.24390995349931));
#26668=CARTESIAN_POINT('Ctrl Pts',(-0.159387504324502,-0.0909879508205247,
1.25502466638108));
#26669=CARTESIAN_POINT('Ctrl Pts',(-0.00998361185797865,-0.183258045453892,
1.26613937926286));
#26670=CARTESIAN_POINT('Ctrl Pts',(0.148559784872265,-0.107764437770621,
1.27725409214463));
#26671=CARTESIAN_POINT('Ctrl Pts',(0.17110402552832,0.0663821977439403,
1.28836880502641));
#26672=CARTESIAN_POINT('Ctrl Pts',(0.0370109696726974,0.179759205197393,
1.29948351790819));
#26673=CARTESIAN_POINT('Ctrl Pts',(-0.130963803535317,0.128575526026046,
1.31059823078997));
#26674=CARTESIAN_POINT('Ctrl Pts',(-0.179047673748397,-0.0403127058704685,
1.32171294367174));
#26675=CARTESIAN_POINT('Ctrl Pts',(-0.0632222292854659,-0.172296643767334,
1.33282765655352));
#26676=CARTESIAN_POINT('Ctrl Pts',(0.110480047964651,-0.146551501974699,
1.34394236943529));
#26677=CARTESIAN_POINT('Ctrl Pts',(0.183043290184881,0.0133543119480212,
1.35505708231707));
#26678=CARTESIAN_POINT('Ctrl Pts',(0.0880394279455103,0.161034911917692,
1.36617179519885));
#26679=CARTESIAN_POINT('Ctrl Pts',(-0.087560188468778,0.161295992277005,
1.37728650808062));
#26680=CARTESIAN_POINT('Ctrl Pts',(-0.183002770812981,0.0138985468335057,
1.3884012209624));
#26681=CARTESIAN_POINT('Ctrl Pts',(-0.11091534218414,-0.14622233275901,
1.39951593384417));
#26682=CARTESIAN_POINT('Ctrl Pts',(0.0627096118637963,-0.172483878403762,
1.41063064672595));
#26683=CARTESIAN_POINT('Ctrl Pts',(0.178927009091768,-0.0408449402837847,
1.42174535960773));
#26684=CARTESIAN_POINT('Ctrl Pts',(0.131345554185685,0.128185526191403,
1.4328600724895));
#26685=CARTESIAN_POINT('Ctrl Pts',(-0.0364762776077821,0.179868465555226,
1.44397478537128));
#26686=CARTESIAN_POINT('Ctrl Pts',(-0.170905876263246,0.0668906958253804,
1.45508949825306));
#26687=CARTESIAN_POINT('Ctrl Pts',(-0.148879574286476,-0.10732220687998,
1.46620421113483));
#26688=CARTESIAN_POINT('Ctrl Pts',(0.00943863520116258,-0.183286922323583,
1.47731892401661));
#26689=CARTESIAN_POINT('Ctrl Pts',(0.159116239676119,-0.0914615001005527,
1.48843363689838));
#26690=CARTESIAN_POINT('Ctrl Pts',(0.163130774348862,0.0840924145785586,
1.49954834978016));
#26691=CARTESIAN_POINT('Ctrl Pts',(0.0178071307235557,0.18266387115329,
1.51066306266194));
#26692=CARTESIAN_POINT('Ctrl Pts',(-0.143818062830546,0.114015562678875,
1.52177777554371));
#26693=CARTESIAN_POINT('Ctrl Pts',(-0.173784912977673,-0.0590083701745273,
1.53289248842549));
#26694=CARTESIAN_POINT('Ctrl Pts',(-0.0446602463747498,-0.178013050429057,
1.54400720130726));
#26695=CARTESIAN_POINT('Ctrl Pts',(0.125348673138568,-0.134055562628755,
1.55512191418904));
#26696=CARTESIAN_POINT('Ctrl Pts',(0.180607064596649,0.0326231811308033,
1.56623662707082));
#26697=CARTESIAN_POINT('Ctrl Pts',(0.0705285959663834,0.169437011542113,
1.57735133995259));
#26698=CARTESIAN_POINT('Ctrl Pts',(-0.104115323797061,0.151139614528901,
1.58846605283437));
#26699=CARTESIAN_POINT('Ctrl Pts',(-0.183446799597517,-0.00551864537181648,
1.59958076571614));
#26700=CARTESIAN_POINT('Ctrl Pts',(-0.0948417779722103,-0.157124857614515,
1.61069547859792));
#26701=CARTESIAN_POINT('Ctrl Pts',(0.0805862137851994,-0.164891012117331,
1.6218101914797));
#26702=CARTESIAN_POINT('Ctrl Pts',(0.182241501338543,-0.0217075774600834,
1.63292490436147));
#26703=CARTESIAN_POINT('Ctrl Pts',(0.11706368257684,0.141348073743014,1.64403961724325));
#26704=CARTESIAN_POINT('Ctrl Pts',(-0.0552801639970045,0.17500653472878,
1.65515433012502));
#26705=CARTESIAN_POINT('Ctrl Pts',(-0.177017746852174,0.0484551445018068,
1.66626904300681));
#26706=CARTESIAN_POINT('Ctrl Pts',(-0.136704312988724,-0.122454540706307,
1.67738375588858));
#26707=CARTESIAN_POINT('Ctrl Pts',(0.0287551771520279,-0.181263133362156,
1.68849846877036));
#26708=CARTESIAN_POINT('Ctrl Pts',(0.167890720816941,-0.0741342673321824,
1.69961318165213));
#26709=CARTESIAN_POINT('Ctrl Pts',(0.153330589953088,0.100860864134458,
1.71072789453391));
#26710=CARTESIAN_POINT('Ctrl Pts',(-0.00159613374009132,0.183522848949103,
1.72184260741568));
#26711=CARTESIAN_POINT('Ctrl Pts',(-0.155061675715616,0.0981787169073654,
1.73295732029746));
#26712=CARTESIAN_POINT('Ctrl Pts',(-0.166575901223461,-0.0770431882836061,
1.74407203317924));
#26713=CARTESIAN_POINT('Ctrl Pts',(-0.0255981046933993,-0.181735854375017,
1.75518674606101));
#26714=CARTESIAN_POINT('Ctrl Pts',(0.138813494183606,-0.120058309007955,
1.76630145894279));
#26715=CARTESIAN_POINT('Ctrl Pts',(0.176148185424323,0.0515266969738023,
1.77741617182456));
#26716=CARTESIAN_POINT('Ctrl Pts',(0.0522279005468018,0.175941553175437,
1.78853088470634));
#26717=CARTESIAN_POINT('Ctrl Pts',(-0.119504451398526,0.139290594891575,
1.79964559758812));
#26718=CARTESIAN_POINT('Ctrl Pts',(-0.181836372054304,-0.0248740331960887,
1.81076031046989));
#26719=CARTESIAN_POINT('Ctrl Pts',(-0.0777060622737596,-0.166267710681354,
1.82187502335167));
#26720=CARTESIAN_POINT('Ctrl Pts',(0.0975603150513518,-0.155451499370037,
1.83298973623345));
#26721=CARTESIAN_POINT('Ctrl Pts',(0.183515035626797,-0.00232710726154151,
1.84410444911522));
#26722=CARTESIAN_POINT('Ctrl Pts',(0.101470792057078,0.152927636771843,
1.855219161997));
#26723=CARTESIAN_POINT('Ctrl Pts',(-0.0734649570961186,0.168184671739659,
1.86633387487877));
#26724=CARTESIAN_POINT('Ctrl Pts',(-0.18114716132335,0.0294769346066355,
1.87744858776055));
#26725=CARTESIAN_POINT('Ctrl Pts',(-0.122998073546538,-0.136215482354805,
1.88856330064232));
#26726=CARTESIAN_POINT('Ctrl Pts',(0.0477496842907016,-0.177209343375145,
1.8996780135241));
#26727=CARTESIAN_POINT('Ctrl Pts',(0.174784961176733,-0.055976790509635,
1.91079272640588));
#26728=CARTESIAN_POINT('Ctrl Pts',(0.141813226508904,0.116499753289206,
1.92190743928765));
#26729=CARTESIAN_POINT('Ctrl Pts',(-0.0209815227920695,0.182326518725712,
1.93302215216943));
#26730=CARTESIAN_POINT('Ctrl Pts',(-0.164568722786704,0.0812423486222812,
1.94413686505121));
#26731=CARTESIAN_POINT('Ctrl Pts',(-0.157501373608142,-0.0942151847679616,
1.95525157793298));
#26732=CARTESIAN_POINT('Ctrl Pts',(-0.00624928486731097,-0.183423363200978,
1.96636629081476));
#26733=CARTESIAN_POINT('Ctrl Pts',(0.150723715954467,-0.104716499073386,
1.97748100369653));
#26734=CARTESIAN_POINT('Ctrl Pts',(0.169716588521531,0.0698531553326882,
1.98859571657831));
#26735=CARTESIAN_POINT('Ctrl Pts',(0.0333422947280978,0.180475691192936,
1.99971042946009));
#26736=CARTESIAN_POINT('Ctrl Pts',(-0.133555225445056,0.125881632836647,
2.01082514234186));
#26737=CARTESIAN_POINT('Ctrl Pts',(-0.178189523674224,-0.0439508518929735,
2.02193985522364));
#26738=CARTESIAN_POINT('Ctrl Pts',(-0.0597001012958023,-0.173548499372694,
2.03305456810542));
#26739=CARTESIAN_POINT('Ctrl Pts',(0.113441819405896,-0.144271055098171,
2.04416928098719));
#26740=CARTESIAN_POINT('Ctrl Pts',(0.182733349399699,0.0170794246634578,
2.05528399386897));
#26741=CARTESIAN_POINT('Ctrl Pts',(0.0847415104331493,0.162794533502435,
2.06639870675075));
#26742=CARTESIAN_POINT('Ctrl Pts',(-0.0908270018729541,0.159479275957466,
2.07751341963252));
#26743=CARTESIAN_POINT('Ctrl Pts',(-0.183247873568771,0.0101686067947032,
2.0886281325143));
#26744=CARTESIAN_POINT('Ctrl Pts',(-0.107914354784435,-0.148450920362924,
2.09974284539607));
#26745=CARTESIAN_POINT('Ctrl Pts',(0.0662094334203013,-0.17117095155347,
2.11085755827785));
#26746=CARTESIAN_POINT('Ctrl Pts',(0.179721750863506,-0.0371924187228543,
2.12197227115963));
#26747=CARTESIAN_POINT('Ctrl Pts',(0.128707669121284,0.130833939051324,
2.1330869840414));
#26748=CARTESIAN_POINT('Ctrl Pts',(-0.0401319355356154,0.179088278484728,
2.14420169692318));
#26749=CARTESIAN_POINT('Ctrl Pts',(-0.172232733083604,0.063396131372761,
2.15531640980495));
#26750=CARTESIAN_POINT('Ctrl Pts',(-0.146662956946516,-0.110332046861714,
2.16643112268673));
#26751=CARTESIAN_POINT('Ctrl Pts',(0.0131695208063343,-0.1830566786303,
2.17754583556851));
#26752=CARTESIAN_POINT('Ctrl Pts',(0.160945955671087,-0.0882019478537668,
2.18866054845028));
#26753=CARTESIAN_POINT('Ctrl Pts',(0.161384298584102,0.0873973129685732,
2.19977526133206));
#26754=CARTESIAN_POINT('Ctrl Pts',(0.0140832896991538,0.182988650085996,
2.21088997421383));
#26755=CARTESIAN_POINT('Ctrl Pts',(-0.146110303090852,0.111062891877556,
2.22200468709561));
#26756=CARTESIAN_POINT('Ctrl Pts',(-0.172547068633587,-0.0625354449444508,
2.23311939997739));
#26757=CARTESIAN_POINT('Ctrl Pts',(-0.0410255997730136,-0.178885706640729,
2.24423411285916));
#26758=CARTESIAN_POINT('Ctrl Pts',(0.128052966639604,-0.131474849570047,
2.25534882574094));
#26759=CARTESIAN_POINT('Ctrl Pts',(0.179905006972722,0.0362946014689825,
2.26646353862272));
#26760=CARTESIAN_POINT('Ctrl Pts',(0.0670635535236872,0.17083841355505,
2.27757825150449));
#26761=CARTESIAN_POINT('Ctrl Pts',(-0.107172544846188,0.148987553701467,
2.28869296438627));
#26762=CARTESIAN_POINT('Ctrl Pts',(-0.183295049527548,-0.00925305504128419,
2.29980767726805));
#26763=CARTESIAN_POINT('Ctrl Pts',(-0.0916245701370072,-0.15902486674809,
2.31092239014982));
#26764=CARTESIAN_POINT('Ctrl Pts',(0.0839324233649617,-0.163213606279465,
2.3220371030316));
#26765=CARTESIAN_POINT('Ctrl Pts',(0.182636797030692,-0.0179952824654467,
2.33315181591337));
#26766=CARTESIAN_POINT('Ctrl Pts',(0.114177823608791,0.143710045180207,
2.34426652879515));
#26767=CARTESIAN_POINT('Ctrl Pts',(-0.0588655274452063,0.173830775601519,
2.35538124167692));
#26768=CARTESIAN_POINT('Ctrl Pts',(-0.177905565768648,0.0448658907444426,
2.3664959545587));
#26769=CARTESIAN_POINT('Ctrl Pts',(-0.134302673977538,-0.125263140298141,
2.37761066744048));
#26770=CARTESIAN_POINT('Ctrl Pts',(0.0327061607400811,-0.180546868845806,
2.38872656798691));
#26771=CARTESIAN_POINT('Ctrl Pts',(0.123427388818086,-0.107442269004469,
2.39613756423943));
#26772=CARTESIAN_POINT('Ctrl Pts',(0.143308829964112,-0.0597686701569069,
2.39984365619801));
#26773=CARTESIAN_POINT('Ctrl Pts',(-0.0743730976566809,0.151458124609491,
-0.0153976563500216));
#26774=CARTESIAN_POINT('Ctrl Pts',(-0.124748468758219,0.126722150817118,
-0.0116922117789939));
#26775=CARTESIAN_POINT('Ctrl Pts',(-0.197999378815845,0.02347308803922,
-0.00428186291404084));
#26776=CARTESIAN_POINT('Ctrl Pts',(-0.126947343158939,-0.153991895501451,
0.00683339024483763));
#26777=CARTESIAN_POINT('Ctrl Pts',(0.0604801393858151,-0.189986453587436,
0.0179481031266138));
#26778=CARTESIAN_POINT('Ctrl Pts',(0.19245631142679,-0.0523034063678348,
0.0290628160083901));
#26779=CARTESIAN_POINT('Ctrl Pts',(0.148292536175391,0.133388556567168,
0.0401775288901662));
#26780=CARTESIAN_POINT('Ctrl Pts',(-0.0316490098340019,0.196902896413978,
0.0512922417719424));
#26781=CARTESIAN_POINT('Ctrl Pts',(-0.182605220667447,0.0801975341066568,
0.0624069546537186));
#26782=CARTESIAN_POINT('Ctrl Pts',(-0.166401785140401,-0.109943209771101,
0.0735216675354948));
#26783=CARTESIAN_POINT('Ctrl Pts',(0.00213765606661008,-0.199426646202769,
0.0846363804172708));
#26784=CARTESIAN_POINT('Ctrl Pts',(0.168718402768423,-0.106349933719559,
0.0957510932990472));
#26785=CARTESIAN_POINT('Ctrl Pts',(0.180846706383503,0.0840875839295365,
0.106865806180823));
#26786=CARTESIAN_POINT('Ctrl Pts',(0.0274182790092828,0.197545653790497,
0.1179805190626));
#26787=CARTESIAN_POINT('Ctrl Pts',(-0.151109972610529,0.130161162732459,
0.129095231944376));
#26788=CARTESIAN_POINT('Ctrl Pts',(-0.191304632630316,-0.056379843368586,
0.140209944826152));
#26789=CARTESIAN_POINT('Ctrl Pts',(-0.0563692653678523,-0.191307678458572,
0.151324657707928));
#26790=CARTESIAN_POINT('Ctrl Pts',(0.130169346744173,-0.151102877015818,
0.162439370589704));
#26791=CARTESIAN_POINT('Ctrl Pts',(0.197544361561446,0.0274292125933766,
0.17355408347148));
#26792=CARTESIAN_POINT('Ctrl Pts',(0.0840772459171892,0.180851181100206,
0.184668796353257));
#26793=CARTESIAN_POINT('Ctrl Pts',(-0.106358436229481,0.168712828555055,
0.195783509235032));
#26794=CARTESIAN_POINT('Ctrl Pts',(-0.199428218471545,0.00212619416399677,
0.206898222116809));
#26795=CARTESIAN_POINT('Ctrl Pts',(-0.109931301009821,-0.166406861794485,
0.218012934998585));
#26796=CARTESIAN_POINT('Ctrl Pts',(0.0802022999186832,-0.182602645249051,
0.229127647880362));
#26797=CARTESIAN_POINT('Ctrl Pts',(0.196914651268626,-0.0316347117549218,
0.240242360762137));
#26798=CARTESIAN_POINT('Ctrl Pts',(0.133361351004721,0.148293239496936,
0.251357073643914));
#26799=CARTESIAN_POINT('Ctrl Pts',(-0.0522776886004238,0.192466044149931,
0.26247178652569));
#26800=CARTESIAN_POINT('Ctrl Pts',(-0.190059082690547,0.060445677645449,
0.273586499407466));
#26801=CARTESIAN_POINT('Ctrl Pts',(-0.153850760269675,-0.126909725468206,
0.284701212289243));
#26802=CARTESIAN_POINT('Ctrl Pts',(0.023200345233862,-0.19808553415799,
0.295815925171018));
#26803=CARTESIAN_POINT('Ctrl Pts',(0.179012678926803,-0.0879238058898391,
0.306930638052795));
#26804=CARTESIAN_POINT('Ctrl Pts',(0.170947733972349,0.102727830250495,
0.318045350934571));
#26805=CARTESIAN_POINT('Ctrl Pts',(0.00638856971982268,0.199337204345436,
0.329160063816347));
#26806=CARTESIAN_POINT('Ctrl Pts',(-0.16401901502788,0.113463199179825,
0.340274776698123));
#26807=CARTESIAN_POINT('Ctrl Pts',(-0.184275280943301,-0.0762807688220648,
0.351389489579899));
#26808=CARTESIAN_POINT('Ctrl Pts',(-0.0358366156219873,-0.196193455139879,
0.362504202461675));
#26809=CARTESIAN_POINT('Ctrl Pts',(0.145408703837682,-0.136500709548084,
0.373618915343452));
#26810=CARTESIAN_POINT('Ctrl Pts',(0.193539526498743,0.048151703412559,
0.384733628225228));
#26811=CARTESIAN_POINT('Ctrl Pts',(0.0644944580298395,0.188723606743685,
0.395848341107004));
#26812=CARTESIAN_POINT('Ctrl Pts',(-0.123592105895363,0.156528355959058,
0.40696305398878));
#26813=CARTESIAN_POINT('Ctrl Pts',(-0.19853619244248,-0.0189608847193331,
0.418077766870556));
#26814=CARTESIAN_POINT('Ctrl Pts',(-0.0917301866239241,-0.177092370589023,
0.429192479752332));
#26815=CARTESIAN_POINT('Ctrl Pts',(0.099050280911231,-0.173104525389443,
0.440307192634109));
#26816=CARTESIAN_POINT('Ctrl Pts',(0.199155101437193,-0.0106480247200912,
0.451421905515884));
#26817=CARTESIAN_POINT('Ctrl Pts',(0.116943248937439,0.16155621741937,0.462536618397661));
#26818=CARTESIAN_POINT('Ctrl Pts',(-0.0723243803173798,0.1858637104725,
0.473651331279438));
#26819=CARTESIAN_POINT('Ctrl Pts',(-0.195382606433862,0.0400221433959911,
0.484766044161213));
#26820=CARTESIAN_POINT('Ctrl Pts',(-0.139577692640525,-0.142457722065341,
0.49588075704299));
#26821=CARTESIAN_POINT('Ctrl Pts',(0.0440037147861017,-0.194524568998165,
0.506995469924765));
#26822=CARTESIAN_POINT('Ctrl Pts',(0.18730189159157,-0.0685137669751007,
0.518110182806543));
#26823=CARTESIAN_POINT('Ctrl Pts',(0.159134424384059,0.120218009611093,
0.529224895688318));
#26824=CARTESIAN_POINT('Ctrl Pts',(-0.0147127598289137,0.198896127556861,
0.540339608570095));
#26825=CARTESIAN_POINT('Ctrl Pts',(-0.175091138052601,0.0954946502917501,
0.55145432145187));
#26826=CARTESIAN_POINT('Ctrl Pts',(-0.17518221489323,-0.0953274695143051,
0.562569034333647));
#26827=CARTESIAN_POINT('Ctrl Pts',(-0.0149026139951197,-0.198881992535802,
0.573683747215423));
#26828=CARTESIAN_POINT('Ctrl Pts',(0.15901959501782,-0.12036986026106,0.584798460097199));
#26829=CARTESIAN_POINT('Ctrl Pts',(0.1873672076467,0.0683349424348715,0.595913172978975));
#26830=CARTESIAN_POINT('Ctrl Pts',(0.0441893826355188,0.194482475614617,
0.607027885860752));
#26831=CARTESIAN_POINT('Ctrl Pts',(-0.139441642755814,0.142590894255063,
0.618142598742528));
#26832=CARTESIAN_POINT('Ctrl Pts',(-0.195420721473322,-0.0398356182046292,
0.629257311624304));
#26833=CARTESIAN_POINT('Ctrl Pts',(-0.0725017678422208,-0.18579458689276,
0.64037202450608));
#26834=CARTESIAN_POINT('Ctrl Pts',(0.116788978457446,-0.161667774679324,
0.651486737387856));
#26835=CARTESIAN_POINT('Ctrl Pts',(0.199165175017855,0.0104579117899193,
0.662601450269632));
#26836=CARTESIAN_POINT('Ctrl Pts',(0.0992154766862795,0.173009895800249,
0.673716163151409));
#26837=CARTESIAN_POINT('Ctrl Pts',(-0.0915610972390791,0.177179853062572,
0.684830876033184));
#26838=CARTESIAN_POINT('Ctrl Pts',(-0.198518002440172,0.0191503933657419,
0.695945588914962));
#26839=CARTESIAN_POINT('Ctrl Pts',(-0.123741467325564,-0.156410306959021,
0.707060301796736));
#26840=CARTESIAN_POINT('Ctrl Pts',(0.0643142781899493,-0.18878508542733,
0.718175014678514));
#26841=CARTESIAN_POINT('Ctrl Pts',(0.193493474006132,-0.0483364290772185,
0.729289727560289));
#26842=CARTESIAN_POINT('Ctrl Pts',(0.145538937477972,0.136361844137873,
0.740404440442067));
#26843=CARTESIAN_POINT('Ctrl Pts',(-0.0356493183232534,0.196227574418036,
0.75151915332384));
#26844=CARTESIAN_POINT('Ctrl Pts',(-0.184202381425786,0.0764566382727335,
0.76263386620562));
#26845=CARTESIAN_POINT('Ctrl Pts',(-0.164127249204111,-0.113306579365854,
0.773748579087393));
#26846=CARTESIAN_POINT('Ctrl Pts',(0.00619828489940304,-0.199343211881429,
0.784863291969171));
#26847=CARTESIAN_POINT('Ctrl Pts',(0.170849594877248,-0.102890965537207,
0.795978004850945));
#26848=CARTESIAN_POINT('Ctrl Pts',(0.17909652705594,0.0877528851685207,
0.807092717732724));
#26849=CARTESIAN_POINT('Ctrl Pts',(0.0233894217650114,0.198063297479358,
0.818207430614498));
#26850=CARTESIAN_POINT('Ctrl Pts',(-0.153729545584279,0.127056529440048,
0.829322143496276));
#26851=CARTESIAN_POINT('Ctrl Pts',(-0.1901166959004,-0.060264224866941,
0.84043685637805));
#26852=CARTESIAN_POINT('Ctrl Pts',(-0.0524613876851037,-0.192416053542971,
0.851551569259829));
#26853=CARTESIAN_POINT('Ctrl Pts',(0.133219733557517,-0.148420475170249,
0.862666282141603));
#26854=CARTESIAN_POINT('Ctrl Pts',(0.196944759132467,0.0314467281152284,
0.87378099502338));
#26855=CARTESIAN_POINT('Ctrl Pts',(0.0803765710474773,0.182526002765492,
0.884895707905156));
#26856=CARTESIAN_POINT('Ctrl Pts',(-0.109772403654785,0.166511724075962,
0.896010420786932));
#26857=CARTESIAN_POINT('Ctrl Pts',(-0.199430156791788,-0.00193582563815892,
0.907125133668708));
#26858=CARTESIAN_POINT('Ctrl Pts',(-0.106519437291686,-0.168611222455568,
0.918239846550485));
#26859=CARTESIAN_POINT('Ctrl Pts',(0.0839045735047286,-0.180931361029226,
0.92935455943226));
#26860=CARTESIAN_POINT('Ctrl Pts',(0.197518085435524,-0.0276177621248288,
0.940469272314037));
#26861=CARTESIAN_POINT('Ctrl Pts',(0.130313531752415,0.150978535895375,
0.951583985195813));
#26862=CARTESIAN_POINT('Ctrl Pts',(-0.05618663317982,0.19136143057266,0.962698698077589));
#26863=CARTESIAN_POINT('Ctrl Pts',(-0.191250706563621,0.0565623735164518,
0.973813410959366));
#26864=CARTESIAN_POINT('Ctrl Pts',(-0.151234190583289,-0.130016746834843,
0.984928123841142));
#26865=CARTESIAN_POINT('Ctrl Pts',(0.0272297679978432,-0.197571947891603,
0.996042836722918));
#26866=CARTESIAN_POINT('Ctrl Pts',(0.180766216950535,-0.0842597749124158,
1.0071575496047));
#26867=CARTESIAN_POINT('Ctrl Pts',(0.168820109684298,0.106188066302576,
1.01827226248647));
#26868=CARTESIAN_POINT('Ctrl Pts',(0.00232751821873696,0.199425970018551,
1.02938697536825));
#26869=CARTESIAN_POINT('Ctrl Pts',(-0.166295801382756,0.110099233881827,
1.04050168825003));
#26870=CARTESIAN_POINT('Ctrl Pts',(-0.18268351653597,-0.0800179207737264,
1.0516164011318));
#26871=CARTESIAN_POINT('Ctrl Pts',(-0.0318334822611076,-0.196882615448979,
1.06273111401358));
#26872=CARTESIAN_POINT('Ctrl Pts',(0.148158534994787,-0.133510985941596,
1.07384582689535));
#26873=CARTESIAN_POINT('Ctrl Pts',(0.192518720649659,0.0520833664264994,
1.08496053977713));
#26874=CARTESIAN_POINT('Ctrl Pts',(0.0606375125831525,0.189997965585494,
1.09607525265891));
#26875=CARTESIAN_POINT('Ctrl Pts',(-0.126754347607934,0.153978797960581,
1.10718996554068));
#26876=CARTESIAN_POINT('Ctrl Pts',(-0.198108854095019,-0.0230003649548643,
1.11830467842246));
#26877=CARTESIAN_POINT('Ctrl Pts',(-0.0881044753971729,-0.178923828133336,
1.12941939130423));
#26878=CARTESIAN_POINT('Ctrl Pts',(0.102555205209445,-0.171051351188312,
1.14053410418601));
#26879=CARTESIAN_POINT('Ctrl Pts',(0.199330653474907,-0.00658979849198673,
1.15164881706779));
#26880=CARTESIAN_POINT('Ctrl Pts',(0.11362871948236,0.163904389714545,1.16276352994956));
#26881=CARTESIAN_POINT('Ctrl Pts',(-0.0760947030218921,0.184352192910496,
1.17387824283134));
#26882=CARTESIAN_POINT('Ctrl Pts',(-0.19615717790434,0.0360346557566957,
1.18499295571311));
#26883=CARTESIAN_POINT('Ctrl Pts',(-0.136647430897652,-0.14527083151125,
1.19610766859489));
#26884=CARTESIAN_POINT('Ctrl Pts',(0.0479562996373891,-0.193588037295664,
1.20722238147667));
#26885=CARTESIAN_POINT('Ctrl Pts',(0.188658403061609,-0.0646849427080351,
1.21833709435844));
#26886=CARTESIAN_POINT('Ctrl Pts',(0.156653043125246,0.123434026664039,
1.22945180724022));
#26887=CARTESIAN_POINT('Ctrl Pts',(-0.0187604516559904,0.198555232397844,
1.240566520122));
#26888=CARTESIAN_POINT('Ctrl Pts',(-0.176999678212625,0.0919089156258833,
1.25168123300377));
#26889=CARTESIAN_POINT('Ctrl Pts',(-0.173204428999001,-0.0988754804490419,
1.26279594588555));
#26890=CARTESIAN_POINT('Ctrl Pts',(-0.0108490674882994,-0.199144250716743,
1.27391065876733));
#26891=CARTESIAN_POINT('Ctrl Pts',(0.161438080231363,-0.11710628125814,
1.2850253716491));
#26892=CARTESIAN_POINT('Ctrl Pts',(0.185936627633784,0.0721367130043656,
1.29614008453088));
#26893=CARTESIAN_POINT('Ctrl Pts',(0.0402193628416877,0.195342104297838,
1.30725479741266));
#26894=CARTESIAN_POINT('Ctrl Pts',(-0.142316745010891,0.139721433389453,
1.31836951029443));
#26895=CARTESIAN_POINT('Ctrl Pts',(-0.194568891875317,-0.0438073187185638,
1.32948422317621));
#26896=CARTESIAN_POINT('Ctrl Pts',(-0.0687028143758259,-0.187232631118989,
1.34059893605798));
#26897=CARTESIAN_POINT('Ctrl Pts',(0.120057301258331,-0.159255704053152,
1.35171364893976));
#26898=CARTESIAN_POINT('Ctrl Pts',(0.198910878822871,0.0145119655736819,
1.36282836182153));
#26899=CARTESIAN_POINT('Ctrl Pts',(0.0956713571200331,0.174994646448712,
1.37394307470331));
#26900=CARTESIAN_POINT('Ctrl Pts',(-0.0951505735098516,0.175278359245073,
1.38505778758509));
#26901=CARTESIAN_POINT('Ctrl Pts',(-0.198866846922735,0.0151033788904271,
1.39617250046686));
#26902=CARTESIAN_POINT('Ctrl Pts',(-0.12053033010116,-0.158897999938967,
1.40728721334864));
#26903=CARTESIAN_POINT('Ctrl Pts',(0.0681457593658351,-0.187436096681916,
1.41840192623042));
#26904=CARTESIAN_POINT('Ctrl Pts',(0.194437767085829,-0.0443856912706738,
1.42951663911219));
#26905=CARTESIAN_POINT('Ctrl Pts',(0.142731588719601,0.139297625394252,
1.44063135199397));
#26906=CARTESIAN_POINT('Ctrl Pts',(-0.0396383195899908,0.195460836176919,
1.45174606487574));
#26907=CARTESIAN_POINT('Ctrl Pts',(-0.185721301278944,0.0726892915782933,
1.46286077775752));
#26908=CARTESIAN_POINT('Ctrl Pts',(-0.161785591431329,-0.116625714420593,
1.4739754906393));
#26909=CARTESIAN_POINT('Ctrl Pts',(0.0102568480978256,-0.199175630853768,
1.48509020352107));
#26910=CARTESIAN_POINT('Ctrl Pts',(0.172909649061707,-0.0993900805928641,
1.49620491640285));
#26911=CARTESIAN_POINT('Ctrl Pts',(0.177272194222541,0.0913821865268278,
1.50731962928462));
#26912=CARTESIAN_POINT('Ctrl Pts',(0.0193507886465428,0.198498568855433,
1.5184343421664));
#26913=CARTESIAN_POINT('Ctrl Pts',(-0.156285309553457,0.123899301356701,
1.52954905504818));
#26914=CARTESIAN_POINT('Ctrl Pts',(-0.188849914856919,-0.0641236658140599,
1.54066376792995));
#26915=CARTESIAN_POINT('Ctrl Pts',(-0.0485317371965617,-0.193444579514605,
1.55177848081173));
#26916=CARTESIAN_POINT('Ctrl Pts',(0.136214852279427,-0.145676521366322,
1.56289319369351));
#26917=CARTESIAN_POINT('Ctrl Pts',(0.196263462617248,0.0354512073191666,
1.57400790657528));
#26918=CARTESIAN_POINT('Ctrl Pts',(0.0766425526532328,0.184125104159359,
1.58512261945706));
#26919=CARTESIAN_POINT('Ctrl Pts',(-0.113140834250107,0.164241549201438,
1.59623733233883));
#26920=CARTESIAN_POINT('Ctrl Pts',(-0.199349367509344,-0.00599704364859195,
1.60735204522061));
#26921=CARTESIAN_POINT('Ctrl Pts',(-0.103063386735022,-0.170745638812843,
1.61846675810238));
#26922=CARTESIAN_POINT('Ctrl Pts',(0.0875720415035815,-0.179185022827784,
1.62958147098416));
#26923=CARTESIAN_POINT('Ctrl Pts',(0.198039584803329,-0.0235893558585985,
1.64069618386594));
#26924=CARTESIAN_POINT('Ctrl Pts',(0.127211655538323,0.153601202970868,
1.65181089674772));
#26925=CARTESIAN_POINT('Ctrl Pts',(-0.0600722702865052,0.190177436099879,
1.66292560962949));
#26926=CARTESIAN_POINT('Ctrl Pts',(-0.192362995431554,0.052655606040559,
1.67404032251127));
#26927=CARTESIAN_POINT('Ctrl Pts',(-0.148554885612024,-0.133069834371645,
1.68515503539304));
#26928=CARTESIAN_POINT('Ctrl Pts',(0.0312478952505764,-0.196976404427808,
1.69626974827482));
#26929=CARTESIAN_POINT('Ctrl Pts',(0.182444769159104,-0.0805607911168946,
1.7073844611566));
#26930=CARTESIAN_POINT('Ctrl Pts',(0.166622455088041,0.1096042531991,1.71849917403837));
#26931=CARTESIAN_POINT('Ctrl Pts',(-0.00173449878791257,0.199432009398825,
1.72961388692015));
#26932=CARTESIAN_POINT('Ctrl Pts',(-0.168503604569103,0.106689596991075,
1.74072859980192));
#26933=CARTESIAN_POINT('Ctrl Pts',(-0.181015970973881,-0.0837218795254947,
1.7518433126837));
#26934=CARTESIAN_POINT('Ctrl Pts',(-0.0278171436692394,-0.197490104503956,
1.76295802556548));
#26935=CARTESIAN_POINT('Ctrl Pts',(0.150846906721609,-0.130465879031342,
1.77407273844725));
#26936=CARTESIAN_POINT('Ctrl Pts',(0.191418053786163,0.0559934241104793,
1.78518745132903));
#26937=CARTESIAN_POINT('Ctrl Pts',(0.0567554133579225,0.191193509077766,
1.79630216421081));
#26938=CARTESIAN_POINT('Ctrl Pts',(-0.129864008819537,0.151365366158238,
1.80741687709258));
#26939=CARTESIAN_POINT('Ctrl Pts',(-0.197599335822427,-0.0270303041313708,
1.81853158997436));
#26940=CARTESIAN_POINT('Ctrl Pts',(-0.084442216489475,-0.180681064124725,
1.82964630285613));
#26941=CARTESIAN_POINT('Ctrl Pts',(0.106017587345052,-0.168927221111439,
1.84076101573791));
#26942=CARTESIAN_POINT('Ctrl Pts',(0.199423518758144,-0.0025288386700214,
1.85187572861969));
#26943=CARTESIAN_POINT('Ctrl Pts',(0.110267054326543,0.166184570851345,
1.86299044150146));
#26944=CARTESIAN_POINT('Ctrl Pts',(-0.079833459964113,0.182764201990043,
1.87410515438324));
#26945=CARTESIAN_POINT('Ctrl Pts',(-0.19685037904805,0.0320322201468692,
1.88521986726501));
#26946=CARTESIAN_POINT('Ctrl Pts',(-0.133660484784501,-0.148023679409987,
1.89633458014679));
#26947=CARTESIAN_POINT('Ctrl Pts',(0.0518889911571499,-0.19257120100262,
1.90744929302857));
#26948=CARTESIAN_POINT('Ctrl Pts',(0.189936654862191,-0.0608292856990732,
1.91856400591034));
#26949=CARTESIAN_POINT('Ctrl Pts',(0.154106678726662,0.12659884055842,1.92967871879212));
#26950=CARTESIAN_POINT('Ctrl Pts',(-0.0228003612336629,0.198131972146125,
1.9407934316739));
#26951=CARTESIAN_POINT('Ctrl Pts',(-0.178834794999575,0.0882850551132964,
1.95190814455567));
#26952=CARTESIAN_POINT('Ctrl Pts',(-0.171154794084838,-0.102382475652217,
1.96302285743745));
#26953=CARTESIAN_POINT('Ctrl Pts',(-0.00679102054882718,-0.19932389946718,
1.97413757031922));
#26954=CARTESIAN_POINT('Ctrl Pts',(0.163789597366124,-0.11379412398511,
1.985252283201));
#26955=CARTESIAN_POINT('Ctrl Pts',(0.184428917003948,0.0759085596731913,
1.99636699608278));
#26956=CARTESIAN_POINT('Ctrl Pts',(0.0362326591684271,0.196120700764793,
2.00748170896455));
#26957=CARTESIAN_POINT('Ctrl Pts',(-0.145132811138998,0.136794012989519,
2.01859642184633));
#26958=CARTESIAN_POINT('Ctrl Pts',(-0.19363635080679,-0.0477608469898892,
2.02971113472811));
#26959=CARTESIAN_POINT('Ctrl Pts',(-0.0648753614654078,-0.188593007117311,
2.04082584760988));
#26960=CARTESIAN_POINT('Ctrl Pts',(0.123275821640341,-0.156777570646236,
2.05194056049166));
#26961=CARTESIAN_POINT('Ctrl Pts',(0.198574070006218,0.0185599994742601,
2.06305527337343));
#26962=CARTESIAN_POINT('Ctrl Pts',(0.0920875509613561,0.176906805454723,
2.07416998625521));
#26963=CARTESIAN_POINT('Ctrl Pts',(-0.0987005792189857,0.173304156097139,
2.08528469913698));
#26964=CARTESIAN_POINT('Ctrl Pts',(-0.199133197055029,0.0110500991972711,
2.09639941201877));
#26965=CARTESIAN_POINT('Ctrl Pts',(-0.117269194222271,-0.161319778515938,
2.10751412490054));
#26966=CARTESIAN_POINT('Ctrl Pts',(0.0719489721513163,-0.186009355317303,
2.11862883778232));
#26967=CARTESIAN_POINT('Ctrl Pts',(0.195301403136589,-0.0404165412795961,
2.12974355066409));
#26968=CARTESIAN_POINT('Ctrl Pts',(0.139865031656166,0.142175622882825,
2.14085826354587));
#26969=CARTESIAN_POINT('Ctrl Pts',(-0.0436108778321787,0.194613016539923,
2.15197297642764));
#26970=CARTESIAN_POINT('Ctrl Pts',(-0.187163180169686,0.068891791622564,
2.16308768930942));
#26971=CARTESIAN_POINT('Ctrl Pts',(-0.159376820792098,-0.119896470290846,
2.1742024021912));
#26972=CARTESIAN_POINT('Ctrl Pts',(0.0143111553262565,-0.198925427880866,
2.18531711507297));
#26973=CARTESIAN_POINT('Ctrl Pts',(0.174897978796096,-0.0958479654936306,
2.19643182795475));
#26974=CARTESIAN_POINT('Ctrl Pts',(0.175374320616466,0.0949735787188828,
2.20754654083652));
#26975=CARTESIAN_POINT('Ctrl Pts',(0.0153041366768783,0.198851502103424,
2.2186612537183));
#26976=CARTESIAN_POINT('Ctrl Pts',(-0.158776258684615,0.120690670527502,
2.22977596660007));
#26977=CARTESIAN_POINT('Ctrl Pts',(-0.187504764722873,-0.0679564943293847,
2.24089067948186));
#26978=CARTESIAN_POINT('Ctrl Pts',(-0.0445820117024905,-0.19439288422328,
2.25200539236363));
#26979=CARTESIAN_POINT('Ctrl Pts',(0.139153574569345,-0.142872092414138,
2.26312010524541));
#26980=CARTESIAN_POINT('Ctrl Pts',(0.195500545283218,0.0394408943776638,
2.27423481812718));
#26981=CARTESIAN_POINT('Ctrl Pts',(0.0728771339004392,0.185647990388598,
2.28534953100895));
#26982=CARTESIAN_POINT('Ctrl Pts',(-0.116463078540096,0.161902931325674,
2.29646424389074));
#26983=CARTESIAN_POINT('Ctrl Pts',(-0.199184462585767,-0.0100551804340931,
2.30757895677251));
#26984=CARTESIAN_POINT('Ctrl Pts',(-0.0995672867839686,-0.172810355231288,
2.31869366965429));
#26985=CARTESIAN_POINT('Ctrl Pts',(0.0912083260544317,-0.177362206656727,
2.32980838253606));
#26986=CARTESIAN_POINT('Ctrl Pts',(0.198469147741369,-0.0195552508166324,
2.34092309541784));
#26987=CARTESIAN_POINT('Ctrl Pts',(0.124075628301739,0.156167928109233,
2.35203780829962));
#26988=CARTESIAN_POINT('Ctrl Pts',(-0.0639684403873645,0.188899753202837,
2.36315252118139));
#26989=CARTESIAN_POINT('Ctrl Pts',(-0.193327777263944,0.048755208388864,
2.37426723406317));
#26990=CARTESIAN_POINT('Ctrl Pts',(-0.145945054211769,-0.136121904799952,
2.38538194694494));
#26991=CARTESIAN_POINT('Ctrl Pts',(0.035541380233941,-0.196198048639552,
2.39649784749138));
#26992=CARTESIAN_POINT('Ctrl Pts',(0.134127016378589,-0.116756184445853,
2.40390884374389));
#26993=CARTESIAN_POINT('Ctrl Pts',(0.155731932497757,-0.0649498743984335,
2.40761493570248));
#26994=CARTESIAN_POINT('Ctrl Pts',(-0.0803060145807513,0.163540295435979,
-0.00762637684555866));
#26995=CARTESIAN_POINT('Ctrl Pts',(-0.134699947516894,0.136831074835686,
-0.00392093227453097));
#26996=CARTESIAN_POINT('Ctrl Pts',(-0.213794254954446,0.0253455914803241,
0.00348941659042212));
#26997=CARTESIAN_POINT('Ctrl Pts',(-0.137074231300261,-0.166276191191372,
0.0146046697493006));
#26998=CARTESIAN_POINT('Ctrl Pts',(0.0653047823526677,-0.205142119834331,
0.0257193826310768));
#26999=CARTESIAN_POINT('Ctrl Pts',(0.207809004042586,-0.0564757721103276,
0.0368340955128529));
#27000=CARTESIAN_POINT('Ctrl Pts',(0.160122180567089,0.144029275451672,
0.0479488083946291));
#27001=CARTESIAN_POINT('Ctrl Pts',(-0.0341737257862836,0.212610303572477,
0.0590635212764054));
#27002=CARTESIAN_POINT('Ctrl Pts',(-0.197172068603809,0.0865950800252895,
0.0701782341581814));
#27003=CARTESIAN_POINT('Ctrl Pts',(-0.179676046914621,-0.11871363819871,
0.0812929470399578));
#27004=CARTESIAN_POINT('Ctrl Pts',(0.00230818191877068,-0.215335378817728,
0.0924076599217337));
#27005=CARTESIAN_POINT('Ctrl Pts',(0.182177466579471,-0.114833718065218,
0.10352237280351));
#27006=CARTESIAN_POINT('Ctrl Pts',(0.195273273499442,0.0907954482718646,
0.114637085685286));
#27007=CARTESIAN_POINT('Ctrl Pts',(0.0296054996130767,0.213304335216675,
0.125751798567062));
#27008=CARTESIAN_POINT('Ctrl Pts',(-0.163164370533217,0.140544424819997,
0.136866511448838));
#27009=CARTESIAN_POINT('Ctrl Pts',(-0.206565453119791,-0.0608773960783323,
0.147981224330614));
#27010=CARTESIAN_POINT('Ctrl Pts',(-0.0608659742455931,-0.206568741920933,
0.159095937212391));
#27011=CARTESIAN_POINT('Ctrl Pts',(0.14055326168958,-0.163156708906222,
0.170210650094167));
#27012=CARTESIAN_POINT('Ctrl Pts',(0.213302939903473,0.0296173053948973,
0.181325362975943));
#27013=CARTESIAN_POINT('Ctrl Pts',(0.0907842855719502,0.195278105174824,
0.192440075857719));
#27014=CARTESIAN_POINT('Ctrl Pts',(-0.114842898840363,0.182171447697987,
0.203554788739495));
#27015=CARTESIAN_POINT('Ctrl Pts',(-0.215337076510083,0.0022958056732197,
0.214669501621272));
#27016=CARTESIAN_POINT('Ctrl Pts',(-0.118700779447527,-0.179681528545344,
0.225784214503048));
#27017=CARTESIAN_POINT('Ctrl Pts',(0.0866002260173578,-0.197169287738227,
0.236898927384824));
#27018=CARTESIAN_POINT('Ctrl Pts',(0.212622996139529,-0.0341582871157983,
0.2480136402666));
#27019=CARTESIAN_POINT('Ctrl Pts',(0.143999899637515,0.160122939994254,
0.259128353148376));
#27020=CARTESIAN_POINT('Ctrl Pts',(-0.0564480027761305,0.207819513167942,
0.270243066030152));
#27021=CARTESIAN_POINT('Ctrl Pts',(-0.205220542731821,0.0652675715182113,
0.281357778911928));
#27022=CARTESIAN_POINT('Ctrl Pts',(-0.166123797270203,-0.137033612757868,
0.292472491793705));
#27023=CARTESIAN_POINT('Ctrl Pts',(0.0250510913399055,-0.213887283110868,
0.303587204675481));
#27024=CARTESIAN_POINT('Ctrl Pts',(0.193292941358929,-0.0949376946806482,
0.314701917557257));
#27025=CARTESIAN_POINT('Ctrl Pts',(0.18458463677687,0.110922670883321,0.325816630439033));
#27026=CARTESIAN_POINT('Ctrl Pts',(0.00689820095215295,0.21523880197307,
0.336931343320809));
#27027=CARTESIAN_POINT('Ctrl Pts',(-0.177103197626001,0.122514425441503,
0.348046056202586));
#27028=CARTESIAN_POINT('Ctrl Pts',(-0.198975353515812,-0.082365865161802,
0.359160769084362));
#27029=CARTESIAN_POINT('Ctrl Pts',(-0.0386953867371307,-0.211844268499353,
0.370275481966138));
#27030=CARTESIAN_POINT('Ctrl Pts',(0.157008298141093,-0.147389692195589,
0.381390194847914));
#27031=CARTESIAN_POINT('Ctrl Pts',(0.208978629728527,0.0519928780455977,
0.392504907729691));
#27032=CARTESIAN_POINT('Ctrl Pts',(0.0696393326365127,0.203778532727666,
0.403619620611466));
#27033=CARTESIAN_POINT('Ctrl Pts',(-0.133451338868726,0.169014991065379,
0.414734333493244));
#27034=CARTESIAN_POINT('Ctrl Pts',(-0.214373891466652,-0.0204734390890087,
0.425849046375019));
#27035=CARTESIAN_POINT('Ctrl Pts',(-0.0990477193584199,-0.19121944550852,
0.436963759256795));
#27036=CARTESIAN_POINT('Ctrl Pts',(0.106951754783744,-0.186913480518035,
0.448078472138571));
#27037=CARTESIAN_POINT('Ctrl Pts',(0.215042172287536,-0.0114974426959434,
0.459193185020347));
#27038=CARTESIAN_POINT('Ctrl Pts',(0.126272086953288,0.174443936859812,
0.470307897902124));
#27039=CARTESIAN_POINT('Ctrl Pts',(-0.0780938662407537,0.200690495804509,
0.4814226107839));
#27040=CARTESIAN_POINT('Ctrl Pts',(-0.210968736484958,0.0432148039059421,
0.492537323665676));
#27041=CARTESIAN_POINT('Ctrl Pts',(-0.150712133466315,-0.153821909612123,
0.503652036547452));
#27042=CARTESIAN_POINT('Ctrl Pts',(0.0475139946104238,-0.210042251384927,
0.514766749429229));
#27043=CARTESIAN_POINT('Ctrl Pts',(0.202243404014021,-0.0739792713096693,
0.525881462311004));
#27044=CARTESIAN_POINT('Ctrl Pts',(0.171828951698061,0.129808082988056,
0.536996175192781));
#27045=CARTESIAN_POINT('Ctrl Pts',(-0.0158864312845783,0.214762539451667,
0.548110888074557));
#27046=CARTESIAN_POINT('Ctrl Pts',(-0.189058569945809,0.10311248314697,
0.559225600956334));
#27047=CARTESIAN_POINT('Ctrl Pts',(-0.189156912200222,-0.102931965965709,
0.570340313838109));
#27048=CARTESIAN_POINT('Ctrl Pts',(-0.0160914305641474,-0.214747276846734,
0.581455026719887));
#27049=CARTESIAN_POINT('Ctrl Pts',(0.171704962123206,-0.129972047121513,
0.59256973960166));
#27050=CARTESIAN_POINT('Ctrl Pts',(0.202313930484488,0.0737861815152819,
0.603684452483439));
#27051=CARTESIAN_POINT('Ctrl Pts',(0.0477144736208678,0.209996800113174,
0.614799165365213));
#27052=CARTESIAN_POINT('Ctrl Pts',(-0.150565230562319,0.153965705260633,
0.625913878246991));
#27053=CARTESIAN_POINT('Ctrl Pts',(-0.211009892050759,-0.04301339916137,
0.637028591128766));
#27054=CARTESIAN_POINT('Ctrl Pts',(-0.0782854043856557,-0.200615858074238,
0.648143304010544));
#27055=CARTESIAN_POINT('Ctrl Pts',(0.126105509954272,-0.174564393304767,
0.659258016892318));
#27056=CARTESIAN_POINT('Ctrl Pts',(0.215053049461418,0.0112921640101984,
0.670372729774096));
#27057=CARTESIAN_POINT('Ctrl Pts',(0.107130128614298,0.186811302103948,
0.68148744265587));
#27058=CARTESIAN_POINT('Ctrl Pts',(-0.0988651413156588,0.191313906664736,
0.692602155537648));
#27059=CARTESIAN_POINT('Ctrl Pts',(-0.214354250405077,0.0206780652858537,
0.703716868419422));
#27060=CARTESIAN_POINT('Ctrl Pts',(-0.133612615211503,-0.168887525018965,
0.714831581301201));
#27061=CARTESIAN_POINT('Ctrl Pts',(0.069444779427023,-0.203844915710499,
0.725946294182974));
#27062=CARTESIAN_POINT('Ctrl Pts',(0.208928903520267,-0.0521923397109899,
0.737061007064754));
#27063=CARTESIAN_POINT('Ctrl Pts',(0.15714892082517,0.147239749165004,0.748175719946527));
#27064=CARTESIAN_POINT('Ctrl Pts',(-0.0384931482923659,0.211881109552576,
0.759290432828306));
#27065=CARTESIAN_POINT('Ctrl Pts',(-0.19889663863233,0.082555764132184,
0.770405145710079));
#27066=CARTESIAN_POINT('Ctrl Pts',(-0.177220065897029,-0.122345311696611,
0.781519858591858));
#27067=CARTESIAN_POINT('Ctrl Pts',(0.00669273666407072,-0.215245288744339,
0.792634571473632));
#27068=CARTESIAN_POINT('Ctrl Pts',(0.184478668895337,-0.111098819855537,
0.803749284355411));
#27069=CARTESIAN_POINT('Ctrl Pts',(0.193383478250533,0.0947531392113955,
0.814863997237184));
#27070=CARTESIAN_POINT('Ctrl Pts',(0.0252552509506406,0.213863272560084,
0.825978710118963));
#27071=CARTESIAN_POINT('Ctrl Pts',(-0.165992913004264,0.137192127627818,
0.837093423000737));
#27072=CARTESIAN_POINT('Ctrl Pts',(-0.205282751882926,-0.0650716438247963,
0.848208135882515));
#27073=CARTESIAN_POINT('Ctrl Pts',(-0.0566463559688438,-0.20776553469269,
0.859322848764289));
#27074=CARTESIAN_POINT('Ctrl Pts',(0.143846985033473,-0.160260325556478,
0.870437561646068));
#27075=CARTESIAN_POINT('Ctrl Pts',(0.21265550577848,0.033955307579041,0.881552274527841));
#27076=CARTESIAN_POINT('Ctrl Pts',(0.0867883991639702,0.197086531303496,
0.892666987409619));
#27077=CARTESIAN_POINT('Ctrl Pts',(-0.118529206476762,0.179794755937645,
0.903781700291395));
#27078=CARTESIAN_POINT('Ctrl Pts',(-0.21533916945469,-0.00209025100234086,
0.91489641317317));
#27079=CARTESIAN_POINT('Ctrl Pts',(-0.115016743335963,-0.182061736240973,
0.926011126054948));
#27080=CARTESIAN_POINT('Ctrl Pts',(0.0905978386750332,-0.19536468124536,
0.937125838936722));
#27081=CARTESIAN_POINT('Ctrl Pts',(0.213274567669185,-0.0298208959659301,
0.9482405518185));
#27082=CARTESIAN_POINT('Ctrl Pts',(0.140708948675044,0.163022448802159,
0.959355264700275));
#27083=CARTESIAN_POINT('Ctrl Pts',(-0.060668773058382,0.206626781967583,
0.970469977582052));
#27084=CARTESIAN_POINT('Ctrl Pts',(-0.206507225243924,0.0610744870853927,
0.981584690463829));
#27085=CARTESIAN_POINT('Ctrl Pts',(-0.163298497665817,-0.140388488526573,
0.992699403345604));
#27086=CARTESIAN_POINT('Ctrl Pts',(0.0294019506348888,-0.213332726860067,
1.00381411622738));
#27087=CARTESIAN_POINT('Ctrl Pts',(0.195186363235098,-0.0909813753344305,
1.01492882910915));
#27088=CARTESIAN_POINT('Ctrl Pts',(0.182287286895232,0.11465893810368,1.02604354199093));
#27089=CARTESIAN_POINT('Ctrl Pts',(0.00251318982131648,0.215334648692705,
1.03715825487271));
#27090=CARTESIAN_POINT('Ctrl Pts',(-0.17956160858336,0.118882108719708,
1.04827296775448));
#27091=CARTESIAN_POINT('Ctrl Pts',(-0.197256610317911,-0.086401138514352,
1.05938768063626));
#27092=CARTESIAN_POINT('Ctrl Pts',(-0.0343729140127666,-0.2125884047472,
1.07050239351803));
#27093=CARTESIAN_POINT('Ctrl Pts',(0.159977489797147,-0.144161471305243,
1.08161710639981));
#27094=CARTESIAN_POINT('Ctrl Pts',(0.207876391795947,0.0562381790653505,
1.09273181928158));
#27095=CARTESIAN_POINT('Ctrl Pts',(0.0654747095800873,0.205154550171551,
1.10384653216336));
#27096=CARTESIAN_POINT('Ctrl Pts',(-0.136865840040237,0.166262048828855,
1.11496124504514));
#27097=CARTESIAN_POINT('Ctrl Pts',(-0.213912463334123,-0.0248351581637025,
1.12607595792691));
#27098=CARTESIAN_POINT('Ctrl Pts',(-0.0951327766195131,-0.193197002728692,
1.13719067080869));
#27099=CARTESIAN_POINT('Ctrl Pts',(0.110736275136736,-0.184696519781856,
1.14830538369047));
#27100=CARTESIAN_POINT('Ctrl Pts',(0.215231728524192,-0.00711548221675883,
1.15942009657224));
#27101=CARTESIAN_POINT('Ctrl Pts',(0.122693149687873,0.176979428381826,
1.17053480945402));
#27102=CARTESIAN_POINT('Ctrl Pts',(-0.0821649564551263,0.199058400931525,
1.18164952233579));
#27103=CARTESIAN_POINT('Ctrl Pts',(-0.211805097343413,0.0389092249991713,
1.19276423521757));
#27104=CARTESIAN_POINT('Ctrl Pts',(-0.147548117852297,-0.156859427414909,
1.20387894809935));
#27105=CARTESIAN_POINT('Ctrl Pts',(0.0517818864516966,-0.209031010345815,
1.21499366098112));
#27106=CARTESIAN_POINT('Ctrl Pts',(0.203708127594514,-0.069845012725504,
1.2261083738629));
#27107=CARTESIAN_POINT('Ctrl Pts',(0.169149624820075,0.13328064928532,1.23722308674468));
#27108=CARTESIAN_POINT('Ctrl Pts',(-0.0202570170087886,0.214394450284037,
1.24833779962645));
#27109=CARTESIAN_POINT('Ctrl Pts',(-0.191119358843245,0.0992407059932329,
1.25945251250823));
#27110=CARTESIAN_POINT('Ctrl Pts',(-0.187021353673497,-0.106763010077559,
1.27056722539));
#27111=CARTESIAN_POINT('Ctrl Pts',(-0.0117145231186205,-0.215030455979593,
1.28168193827178));
#27112=CARTESIAN_POINT('Ctrl Pts',(0.17431637559046,-0.12644812474566,1.29279665115356));
#27113=CARTESIAN_POINT('Ctrl Pts',(0.200769229739247,0.0778912282647907,
1.30391136403533));
#27114=CARTESIAN_POINT('Ctrl Pts',(0.0434277560106783,0.210925003398282,
1.31502607691711));
#27115=CARTESIAN_POINT('Ctrl Pts',(-0.153669686486467,0.150867340752861,
1.32614078979889));
#27116=CARTESIAN_POINT('Ctrl Pts',(-0.210090110002236,-0.0473019315666589,
1.33725550268066));
#27117=CARTESIAN_POINT('Ctrl Pts',(-0.074183399466186,-0.202168618470644,
1.34837021556244));
#27118=CARTESIAN_POINT('Ctrl Pts',(0.12963455455201,-0.171959906131605,
1.35948492844422));
#27119=CARTESIAN_POINT('Ctrl Pts',(0.214778467460861,0.0156696191993429,
1.37059964132599));
#27120=CARTESIAN_POINT('Ctrl Pts',(0.103303286294556,0.188954380979731,
1.38171435420777));
#27121=CARTESIAN_POINT('Ctrl Pts',(-0.102740958550925,0.189260726213141,
1.39282906708954));
#27122=CARTESIAN_POINT('Ctrl Pts',(-0.21473092303249,0.0163082109473484,
1.40394377997132));
#27123=CARTESIAN_POINT('Ctrl Pts',(-0.13014531801818,-0.171573667118924,
1.41505849285309));
#27124=CARTESIAN_POINT('Ctrl Pts',(0.0735819068678742,-0.202388314960068,
1.42617320573487));
#27125=CARTESIAN_POINT('Ctrl Pts',(0.209948525079889,-0.0479264422575633,
1.43728791861665));
#27126=CARTESIAN_POINT('Ctrl Pts',(0.154117623253518,0.150409724597099,
1.44840263149842));
#27127=CARTESIAN_POINT('Ctrl Pts',(-0.0428003615721995,0.211053206798612,
1.4595173443802));
#27128=CARTESIAN_POINT('Ctrl Pts',(-0.200536726294642,0.0784878873312067,
1.47063205726198));
#27129=CARTESIAN_POINT('Ctrl Pts',(-0.174691608576182,-0.125929221961204,
1.48174677014375));
#27130=CARTESIAN_POINT('Ctrl Pts',(0.0110750609944887,-0.215064339383955,
1.49286148302553));
#27131=CARTESIAN_POINT('Ctrl Pts',(0.186703058447294,-0.107318661085176,
1.5039761959073));
#27132=CARTESIAN_POINT('Ctrl Pts',(0.191413614096222,0.0986719584750968,
1.51509090878908));
#27133=CARTESIAN_POINT('Ctrl Pts',(0.0208944465695296,0.214333266557577,
1.52620562167086));
#27134=CARTESIAN_POINT('Ctrl Pts',(-0.168752556276368,0.133783040034527,
1.53732033455263));
#27135=CARTESIAN_POINT('Ctrl Pts',(-0.203914916736164,-0.0692389614535924,
1.54843504743441));
#27136=CARTESIAN_POINT('Ctrl Pts',(-0.0524032280183736,-0.208876108600153,
1.55954976031619));
#27137=CARTESIAN_POINT('Ctrl Pts',(0.147081031420287,-0.157297480103887,
1.57066447319796));
#27138=CARTESIAN_POINT('Ctrl Pts',(0.211919860637847,0.0382792335075298,
1.58177918607974));
#27139=CARTESIAN_POINT('Ctrl Pts',(0.0827565093400825,0.198813196776606,
1.59289389896151));
#27140=CARTESIAN_POINT('Ctrl Pts',(-0.122166344703153,0.177343483873975,
1.60400861184329));
#27141=CARTESIAN_POINT('Ctrl Pts',(-0.21525193542117,-0.0064754419253672,
1.61512332472507));
#27142=CARTESIAN_POINT('Ctrl Pts',(-0.111284995497834,-0.184366420011171,
1.62623803760684));
#27143=CARTESIAN_POINT('Ctrl Pts',(0.0945578692219636,-0.193479033538237,
1.63735275048862));
#27144=CARTESIAN_POINT('Ctrl Pts',(0.213837668268116,-0.0254711342571139,
1.6484674633704));
#27145=CARTESIAN_POINT('Ctrl Pts',(0.137359628499805,0.165854332198722,
1.65958217625217));
#27146=CARTESIAN_POINT('Ctrl Pts',(-0.0648643765760059,0.205348337470978,
1.67069688913395));
#27147=CARTESIAN_POINT('Ctrl Pts',(-0.207708244010933,0.0568560675793112,
1.68181160201572));
#27148=CARTESIAN_POINT('Ctrl Pts',(-0.160405458235323,-0.143685128036984,
1.6929263148975));
#27149=CARTESIAN_POINT('Ctrl Pts',(0.0337406133491248,-0.21268967549346,
1.70404102777928));
#27150=CARTESIAN_POINT('Ctrl Pts',(0.196998817501266,-0.0869873149016069,
1.71515574066105));
#27151=CARTESIAN_POINT('Ctrl Pts',(0.179914320222994,0.118347642263741,
1.72627045354283));
#27152=CARTESIAN_POINT('Ctrl Pts',(-0.00187286383573374,0.215341169848548,
1.73738516642461));
#27153=CARTESIAN_POINT('Ctrl Pts',(-0.18194553342259,0.115200477074783,
1.74849987930638));
#27154=CARTESIAN_POINT('Ctrl Pts',(-0.195456040724301,-0.0904005707673835,
1.75961459218816));
#27155=CARTESIAN_POINT('Ctrl Pts',(-0.0300361826450795,-0.213244354632895,
1.77072930506993));
#27156=CARTESIAN_POINT('Ctrl Pts',(0.162880319259612,-0.140873449054729,
1.78184401795171));
#27157=CARTESIAN_POINT('Ctrl Pts',(0.206687922148005,0.0604601512471564,
1.79295873083348));
#27158=CARTESIAN_POINT('Ctrl Pts',(0.0612829261690431,0.206445464980096,
1.80407344371526));
#27159=CARTESIAN_POINT('Ctrl Pts',(-0.140223566240549,0.163440137424902,
1.81518815659704));
#27160=CARTESIAN_POINT('Ctrl Pts',(-0.213362299590549,-0.0291865750666529,
1.82630286947881));
#27161=CARTESIAN_POINT('Ctrl Pts',(-0.0911783707051906,-0.195094417568098,
1.83741758236059));
#27162=CARTESIAN_POINT('Ctrl Pts',(0.114474859638751,-0.18240294285284,
1.84853229524236));
#27163=CARTESIAN_POINT('Ctrl Pts',(0.215332001889489,-0.00273057007850146,
1.85964700812414));
#27164=CARTESIAN_POINT('Ctrl Pts',(0.11906331659601,0.179441504930847,1.87076172100592));
#27165=CARTESIAN_POINT('Ctrl Pts',(-0.0862019628321077,0.197343732240425,
1.88187643388769));
#27166=CARTESIAN_POINT('Ctrl Pts',(-0.212553596772751,0.0345875056871029,
1.89299114676947));
#27167=CARTESIAN_POINT('Ctrl Pts',(-0.144322896022465,-0.15983187646517,
1.90410585965125));
#27168=CARTESIAN_POINT('Ctrl Pts',(0.0560282980235981,-0.207933058630097,
1.91522057253302));
#27169=CARTESIAN_POINT('Ctrl Pts',(0.205088348547649,-0.0656817808885113,
1.9263352854148));
#27170=CARTESIAN_POINT('Ctrl Pts',(0.166400130944419,0.136697927827634,
1.93744999829658));
#27171=CARTESIAN_POINT('Ctrl Pts',(-0.024619199675256,0.213937425566538,
1.94856471117835));
#27172=CARTESIAN_POINT('Ctrl Pts',(-0.193100867212448,0.0953277616043114,
1.95967942406013));
#27173=CARTESIAN_POINT('Ctrl Pts',(-0.184808214561534,-0.110549766536471,
1.9707941369419));
#27174=CARTESIAN_POINT('Ctrl Pts',(-0.00733275623034357,-0.215224435733384,
1.98190884982368));
#27175=CARTESIAN_POINT('Ctrl Pts',(0.176855478777783,-0.122871748896835,
1.99302356270546));
#27176=CARTESIAN_POINT('Ctrl Pts',(0.199141245486367,0.0819639640136945,
2.00413827558723));
#27177=CARTESIAN_POINT('Ctrl Pts',(0.0391230236087566,0.211765710336649,
2.01525298846901));
#27178=CARTESIAN_POINT('Ctrl Pts',(-0.156710396832941,0.147706393142391,
2.02636770135079));
#27179=CARTESIAN_POINT('Ctrl Pts',(-0.209083177939355,-0.0515708420868051,
2.03748241423256));
#27180=CARTESIAN_POINT('Ctrl Pts',(-0.0700506216350135,-0.203637514861929,
2.04859712711434));
#27181=CARTESIAN_POINT('Ctrl Pts',(0.133109823874788,-0.1692840861943,2.05971183999611));
#27182=CARTESIAN_POINT('Ctrl Pts',(0.214414790612736,0.0200405742850625,
2.0708265528779));
#27183=CARTESIAN_POINT('Ctrl Pts',(0.0994335914895629,0.19101907740701,
2.08194126575967));
#27184=CARTESIAN_POINT('Ctrl Pts',(-0.106574156565017,0.187129036236811,
2.09305597864144));
#27185=CARTESIAN_POINT('Ctrl Pts',(-0.215018520541286,0.0119315915998391,
2.10417069152322));
#27186=CARTESIAN_POINT('Ctrl Pts',(-0.126624033660108,-0.174188636668953,
2.11528540440499));
#27187=CARTESIAN_POINT('Ctrl Pts',(0.077688510882331,-0.200847759081134,
2.12640011728678));
#27188=CARTESIAN_POINT('Ctrl Pts',(0.210881055409674,-0.0436406638363383,
2.13751483016855));
#27189=CARTESIAN_POINT('Ctrl Pts',(0.15102239419105,0.153517306714328,2.14862954305032));
#27190=CARTESIAN_POINT('Ctrl Pts',(-0.0470898201287418,0.210137754595118,
2.1597442559321));
#27191=CARTESIAN_POINT('Ctrl Pts',(-0.202093627255768,0.0743874518723669,
2.17085896881387));
#27192=CARTESIAN_POINT('Ctrl Pts',(-0.172090684637681,-0.129460893719979,
2.18197368169565));
#27193=CARTESIAN_POINT('Ctrl Pts',(0.0154527898461788,-0.214794177131431,
2.19308839457743));
#27194=CARTESIAN_POINT('Ctrl Pts',(0.188850001921107,-0.103493983133494,
2.2042031074592));
#27195=CARTESIAN_POINT('Ctrl Pts',(0.189364342648829,0.102549844469193,
2.21531782034099));
#27196=CARTESIAN_POINT('Ctrl Pts',(0.0165249836546031,0.21471435412085,
2.22643253322275));
#27197=CARTESIAN_POINT('Ctrl Pts',(-0.171442214278381,0.130318449177449,
2.23754724610453));
#27198=CARTESIAN_POINT('Ctrl Pts',(-0.20246246081216,-0.0733775437143184,
2.24866195898631));
#27199=CARTESIAN_POINT('Ctrl Pts',(-0.0481384236319674,-0.209900061805832,
2.25977667186808));
#27200=CARTESIAN_POINT('Ctrl Pts',(0.150254182499086,-0.154269335258229,
2.27089138474987));
#27201=CARTESIAN_POINT('Ctrl Pts',(0.211096083593716,0.0425871872863454,
2.28200609763164));
#27202=CARTESIAN_POINT('Ctrl Pts',(0.0786907142771913,0.200457567222148,
2.29312081051341));
#27203=CARTESIAN_POINT('Ctrl Pts',(-0.125753612234005,0.174818308949879,
2.30423552339519));
#27204=CARTESIAN_POINT('Ctrl Pts',(-0.215073875643988,-0.010857305826902,
2.31535023627696));
#27205=CARTESIAN_POINT('Ctrl Pts',(-0.10751000343093,-0.186595843714485,
2.32646494915874));
#27206=CARTESIAN_POINT('Ctrl Pts',(0.0984842287439015,-0.19151080703399,
2.33757966204052));
#27207=CARTESIAN_POINT('Ctrl Pts',(0.214301498452045,-0.0211152191678184,
2.34869437492229));
#27208=CARTESIAN_POINT('Ctrl Pts',(0.133973432994688,0.168625811038259,
2.35980908780407));
#27209=CARTESIAN_POINT('Ctrl Pts',(-0.0690713533295226,0.203968730804155,
2.37092380068584));
#27210=CARTESIAN_POINT('Ctrl Pts',(-0.20874998875924,0.0526445260332857,
2.38203851356764));
#27211=CARTESIAN_POINT('Ctrl Pts',(-0.157587434446001,-0.146980669301764,
2.3931532264494));
#27212=CARTESIAN_POINT('Ctrl Pts',(0.0383765997278007,-0.211849228433297,
2.40426912699585));
#27213=CARTESIAN_POINT('Ctrl Pts',(0.144826643939091,-0.126070099887236,
2.41168012324836));
#27214=CARTESIAN_POINT('Ctrl Pts',(0.168155035031402,-0.07013107863996,
2.41538621520694));
#27215=CARTESIAN_POINT('Ctrl Pts',(-0.0862389315048216,0.175622466262465,
0.0001449026589043));
#27216=CARTESIAN_POINT('Ctrl Pts',(-0.144651426275569,0.146939998854253,
0.00385034722993199));
#27217=CARTESIAN_POINT('Ctrl Pts',(-0.229589131093048,0.0272180949214282,
0.011260696094885));
#27218=CARTESIAN_POINT('Ctrl Pts',(-0.147201119441583,-0.178560486881291,
0.0223759492537636));
#27219=CARTESIAN_POINT('Ctrl Pts',(0.0701294253195201,-0.220297786081225,
0.0334906621355397));
#27220=CARTESIAN_POINT('Ctrl Pts',(0.223161696658383,-0.0606481378528203,
0.0446053750173159));
#27221=CARTESIAN_POINT('Ctrl Pts',(0.171951824958788,0.154669994336176,
0.055720087899092));
#27222=CARTESIAN_POINT('Ctrl Pts',(-0.0366984417385652,0.228317710730976,
0.0668348007808684));
#27223=CARTESIAN_POINT('Ctrl Pts',(-0.211738916540169,0.092992625943922,
0.0779495136626443));
#27224=CARTESIAN_POINT('Ctrl Pts',(-0.192950308688839,-0.12748406662632,
0.0890642265444207));
#27225=CARTESIAN_POINT('Ctrl Pts',(0.00247870777093128,-0.231244111432686,
0.100178939426197));
#27226=CARTESIAN_POINT('Ctrl Pts',(0.195636530390518,-0.123317502410877,
0.111293652307973));
#27227=CARTESIAN_POINT('Ctrl Pts',(0.209699840615381,0.0975033126141929,
0.122408365189749));
#27228=CARTESIAN_POINT('Ctrl Pts',(0.0317927202168705,0.229063016642852,
0.133523078071525));
#27229=CARTESIAN_POINT('Ctrl Pts',(-0.175218768455904,0.150927686907536,
0.144637790953302));
#27230=CARTESIAN_POINT('Ctrl Pts',(-0.221826273609266,-0.0653749487880787,
0.155752503835078));
#27231=CARTESIAN_POINT('Ctrl Pts',(-0.0653626831233337,-0.221829805383293,
0.166867216716854));
#27232=CARTESIAN_POINT('Ctrl Pts',(0.150937176634988,-0.175210540796626,
0.17798192959863));
#27233=CARTESIAN_POINT('Ctrl Pts',(0.229061518245498,0.0318053981964183,
0.189096642480406));
#27234=CARTESIAN_POINT('Ctrl Pts',(0.0974913252267112,0.209705029249441,
0.200211355362183));
#27235=CARTESIAN_POINT('Ctrl Pts',(-0.123327361451243,0.195630066840919,
0.211326068243959));
#27236=CARTESIAN_POINT('Ctrl Pts',(-0.23124593454862,0.00246541718244239,
0.222440781125735));
#27237=CARTESIAN_POINT('Ctrl Pts',(-0.127470257885232,-0.192956195296204,
0.233555494007511));
#27238=CARTESIAN_POINT('Ctrl Pts',(0.0929981521160323,-0.211735930227402,
0.244670206889288));
#27239=CARTESIAN_POINT('Ctrl Pts',(0.228331341010431,-0.0366818624766748,
0.255784919771063));
#27240=CARTESIAN_POINT('Ctrl Pts',(0.15463844827031,0.171952640491572,0.26689963265284));
#27241=CARTESIAN_POINT('Ctrl Pts',(-0.0606183169518371,0.223172982185952,
0.278014345534616));
#27242=CARTESIAN_POINT('Ctrl Pts',(-0.220382002773095,0.0700894653909738,
0.289129058416392));
#27243=CARTESIAN_POINT('Ctrl Pts',(-0.178396834270733,-0.14715750004753,
0.300243771298168));
#27244=CARTESIAN_POINT('Ctrl Pts',(0.0269018374459491,-0.229689032063747,
0.311358484179945));
#27245=CARTESIAN_POINT('Ctrl Pts',(0.207573203791055,-0.101951583471458,
0.32247319706172));
#27246=CARTESIAN_POINT('Ctrl Pts',(0.198221539581392,0.119117511516148,
0.333587909943497));
#27247=CARTESIAN_POINT('Ctrl Pts',(0.00740783218448367,0.231140399600704,
0.344702622825273));
#27248=CARTESIAN_POINT('Ctrl Pts',(-0.190187380224124,0.131565651703181,
0.355817335707049));
#27249=CARTESIAN_POINT('Ctrl Pts',(-0.213675426088322,-0.0884509615015388,
0.366932048588825));
#27250=CARTESIAN_POINT('Ctrl Pts',(-0.0415541578522746,-0.227495081858827,
0.378046761470602));
#27251=CARTESIAN_POINT('Ctrl Pts',(0.168607892444504,-0.158278674843094,
0.389161474352377));
#27252=CARTESIAN_POINT('Ctrl Pts',(0.22441773295831,0.0558340526786359,
0.400276187234154));
#27253=CARTESIAN_POINT('Ctrl Pts',(0.0747842072431861,0.218833458711647,
0.41139090011593));
#27254=CARTESIAN_POINT('Ctrl Pts',(-0.143310571842089,0.181501626171699,
0.422505612997706));
#27255=CARTESIAN_POINT('Ctrl Pts',(-0.230211590490823,-0.021985993458684,
0.433620325879483));
#27256=CARTESIAN_POINT('Ctrl Pts',(-0.106365252092917,-0.205346520428016,
0.444735038761259));
#27257=CARTESIAN_POINT('Ctrl Pts',(0.114853228656257,-0.200722435646626,
0.455849751643035));
#27258=CARTESIAN_POINT('Ctrl Pts',(0.230929243137877,-0.0123468606717962,
0.466964464524811));
#27259=CARTESIAN_POINT('Ctrl Pts',(0.135600924969137,0.187331656300253,
0.478079177406587));
#27260=CARTESIAN_POINT('Ctrl Pts',(-0.0838633521641277,0.215517281136517,
0.489193890288364));
#27261=CARTESIAN_POINT('Ctrl Pts',(-0.226554866536053,0.0464074644158934,
0.500308603170139));
#27262=CARTESIAN_POINT('Ctrl Pts',(-0.161846574292104,-0.165186097158907,
0.511423316051917));
#27263=CARTESIAN_POINT('Ctrl Pts',(0.0510242744347459,-0.22555993377169,
0.522538028933691));
#27264=CARTESIAN_POINT('Ctrl Pts',(0.217184916436474,-0.079444775644238,
0.533652741815469));
#27265=CARTESIAN_POINT('Ctrl Pts',(0.184523479012063,0.139398156365019,
0.544767454697244));
#27266=CARTESIAN_POINT('Ctrl Pts',(-0.0170601027402429,0.230628951346473,
0.555882167579021));
#27267=CARTESIAN_POINT('Ctrl Pts',(-0.203026001839017,0.110730316002189,
0.566996880460796));
#27268=CARTESIAN_POINT('Ctrl Pts',(-0.203131609507214,-0.110536462417114,
0.578111593342573));
#27269=CARTESIAN_POINT('Ctrl Pts',(-0.017280247133175,-0.230612561157665,
0.589226306224349));
#27270=CARTESIAN_POINT('Ctrl Pts',(0.184390329228592,-0.139574233981967,
0.600341019106125));
#27271=CARTESIAN_POINT('Ctrl Pts',(0.217260653322277,0.0792374205956927,
0.611455731987902));
#27272=CARTESIAN_POINT('Ctrl Pts',(0.0512395646062169,0.225511124611729,
0.622570444869677));
#27273=CARTESIAN_POINT('Ctrl Pts',(-0.161688818368825,0.165340516266203,
0.633685157751454));
#27274=CARTESIAN_POINT('Ctrl Pts',(-0.226599062628197,-0.0461911801181109,
0.644799870633229));
#27275=CARTESIAN_POINT('Ctrl Pts',(-0.0840690409290904,-0.215437129255717,
0.655914583515006));
#27276=CARTESIAN_POINT('Ctrl Pts',(0.135422041451098,-0.18746101193021,
0.667029296396782));
#27277=CARTESIAN_POINT('Ctrl Pts',(0.230940923904982,0.0121264162304775,
0.678144009278559));
#27278=CARTESIAN_POINT('Ctrl Pts',(0.115044780542316,0.200612708407647,
0.689258722160335));
#27279=CARTESIAN_POINT('Ctrl Pts',(-0.106169185392238,0.2054479602669,0.700373435042111));
#27280=CARTESIAN_POINT('Ctrl Pts',(-0.230190498369983,0.0222057372059658,
0.711488147923888));
#27281=CARTESIAN_POINT('Ctrl Pts',(-0.143483763097442,-0.181364743078909,
0.722602860805663));
#27282=CARTESIAN_POINT('Ctrl Pts',(0.0745752806640969,-0.218904745993668,
0.73371757368744));
#27283=CARTESIAN_POINT('Ctrl Pts',(0.224364333034403,-0.0560482503447613,
0.744832286569215));
#27284=CARTESIAN_POINT('Ctrl Pts',(0.168758904172368,0.158117654192133,
0.755946999450992));
#27285=CARTESIAN_POINT('Ctrl Pts',(-0.0413369782614782,0.227534644687114,
0.767061712332768));
#27286=CARTESIAN_POINT('Ctrl Pts',(-0.213590895838874,0.0886548899916345,
0.778176425214544));
#27287=CARTESIAN_POINT('Ctrl Pts',(-0.190312882589949,-0.131384044027369,
0.78929113809632));
#27288=CARTESIAN_POINT('Ctrl Pts',(0.00718718842873861,-0.231147365607249,
0.800405850978096));
#27289=CARTESIAN_POINT('Ctrl Pts',(0.198107742913426,-0.119306674173869,
0.811520563859873));
#27290=CARTESIAN_POINT('Ctrl Pts',(0.207670429445126,0.101753393254271,
0.822635276741649));
#27291=CARTESIAN_POINT('Ctrl Pts',(0.0271210801362698,0.229663247640808,
0.833749989623426));
#27292=CARTESIAN_POINT('Ctrl Pts',(-0.178256280424249,0.147327725815587,
0.8448647025052));
#27293=CARTESIAN_POINT('Ctrl Pts',(-0.220448807865454,-0.0698790627826517,
0.855979415386978));
#27294=CARTESIAN_POINT('Ctrl Pts',(-0.0608313242525837,-0.223115015842409,
0.867094128268752));
#27295=CARTESIAN_POINT('Ctrl Pts',(0.154474236509428,-0.172100175942706,
0.878208841150531));
#27296=CARTESIAN_POINT('Ctrl Pts',(0.228366252424493,0.0364638870428536,
0.889323554032305));
#27297=CARTESIAN_POINT('Ctrl Pts',(0.0932002272804631,0.2116470598415,0.900438266914083));
#27298=CARTESIAN_POINT('Ctrl Pts',(-0.12728600929874,0.193077787799328,
0.911552979795857));
#27299=CARTESIAN_POINT('Ctrl Pts',(-0.231248182117593,-0.00224467636652307,
0.922667692677635));
#27300=CARTESIAN_POINT('Ctrl Pts',(-0.123514049380241,-0.195512250026378,
0.93378240555941));
#27301=CARTESIAN_POINT('Ctrl Pts',(0.0972911038453378,-0.209798001461494,
0.944897118441188));
#27302=CARTESIAN_POINT('Ctrl Pts',(0.229031049902846,-0.0320240298070313,
0.956011831322962));
#27303=CARTESIAN_POINT('Ctrl Pts',(0.151104365597674,0.175066361708942,
0.96712654420474));
#27304=CARTESIAN_POINT('Ctrl Pts',(-0.0651509129369443,0.221892133362506,
0.978241257086515));
#27305=CARTESIAN_POINT('Ctrl Pts',(-0.221763743924227,0.0655866006543337,
0.989355969968292));
#27306=CARTESIAN_POINT('Ctrl Pts',(-0.175362804748344,-0.150760230218302,
1.00047068285007));
#27307=CARTESIAN_POINT('Ctrl Pts',(0.0315741332719343,-0.229093505828532,
1.01158539573184));
#27308=CARTESIAN_POINT('Ctrl Pts',(0.209606509519663,-0.0977029757564454,
1.02270010861362));
#27309=CARTESIAN_POINT('Ctrl Pts',(0.195754464106167,0.123129809904786,
1.03381482149539));
#27310=CARTESIAN_POINT('Ctrl Pts',(0.00269886142389581,0.231243327366859,
1.04492953437717));
#27311=CARTESIAN_POINT('Ctrl Pts',(-0.192827415783965,0.127664983557588,
1.05604424725895));
#27312=CARTESIAN_POINT('Ctrl Pts',(-0.211829704099851,-0.0927843562549774,
1.06715896014072));
#27313=CARTESIAN_POINT('Ctrl Pts',(-0.0369123457644256,-0.228294194045422,
1.0782736730225));
#27314=CARTESIAN_POINT('Ctrl Pts',(0.171796444599506,-0.15481195666889,
1.08938838590428));
#27315=CARTESIAN_POINT('Ctrl Pts',(0.223234062942235,0.0603929917042014,
1.10050309878605));
#27316=CARTESIAN_POINT('Ctrl Pts',(0.0703119065770221,0.220311134757609,
1.11161781166783));
#27317=CARTESIAN_POINT('Ctrl Pts',(-0.14697733247254,0.17854529969713,1.1227325245496));
#27318=CARTESIAN_POINT('Ctrl Pts',(-0.229716072573226,-0.0266699513725409,
1.13384723743138));
#27319=CARTESIAN_POINT('Ctrl Pts',(-0.102161077841853,-0.207470177324048,
1.14496195031315));
#27320=CARTESIAN_POINT('Ctrl Pts',(0.118917345064028,-0.1983416883754,1.15607666319493));
#27321=CARTESIAN_POINT('Ctrl Pts',(0.231132803573477,-0.00764116594153085,
1.16719137607671));
#27322=CARTESIAN_POINT('Ctrl Pts',(0.131757579893385,0.190054467049106,
1.17830608895849));
#27323=CARTESIAN_POINT('Ctrl Pts',(-0.0882352098883608,0.213764608952554,
1.18942080184026));
#27324=CARTESIAN_POINT('Ctrl Pts',(-0.227453016782484,0.041783794241647,
1.20053551472204));
#27325=CARTESIAN_POINT('Ctrl Pts',(-0.158448804806942,-0.168448023318568,
1.21165022760381));
#27326=CARTESIAN_POINT('Ctrl Pts',(0.0556074732660041,-0.224473983395965,
1.22276494048559));
#27327=CARTESIAN_POINT('Ctrl Pts',(0.218757852127418,-0.0750050827429731,
1.23387965336737));
#27328=CARTESIAN_POINT('Ctrl Pts',(0.181646206514904,0.143127271906602,
1.24499436624914));
#27329=CARTESIAN_POINT('Ctrl Pts',(-0.0217535823615871,0.230233668170229,
1.25610907913092));
#27330=CARTESIAN_POINT('Ctrl Pts',(-0.205239039473866,0.106572496360582,
1.2672237920127));
#27331=CARTESIAN_POINT('Ctrl Pts',(-0.200838278347996,-0.114650539706076,
1.27833850489447));
#27332=CARTESIAN_POINT('Ctrl Pts',(-0.012579978748941,-0.230916661242444,
1.28945321777625));
#27333=CARTESIAN_POINT('Ctrl Pts',(0.187194670949558,-0.13578996823318,
1.30056793065802));
#27334=CARTESIAN_POINT('Ctrl Pts',(0.215601831844711,0.0836457435252159,
1.3116826435398));
#27335=CARTESIAN_POINT('Ctrl Pts',(0.0466361491796686,0.226507902498727,
1.32279735642157));
#27336=CARTESIAN_POINT('Ctrl Pts',(-0.165022627962041,0.162013248116267,
1.33391206930335));
#27337=CARTESIAN_POINT('Ctrl Pts',(-0.225611328129155,-0.050796544414754,
1.34502678218513));
#27338=CARTESIAN_POINT('Ctrl Pts',(-0.079663984556546,-0.217104605822299,
1.3561414950669));
#27339=CARTESIAN_POINT('Ctrl Pts',(0.13921180784569,-0.184664108210057,
1.36725620794868));
#27340=CARTESIAN_POINT('Ctrl Pts',(0.230646056098852,0.0168272728250036,
1.37837092083046));
#27341=CARTESIAN_POINT('Ctrl Pts',(0.110935215469079,0.202914115510752,
1.38948563371223));
#27342=CARTESIAN_POINT('Ctrl Pts',(-0.110331343591998,0.203243093181209,
1.40060034659401));
#27343=CARTESIAN_POINT('Ctrl Pts',(-0.230594999142245,0.0175130430042696,
1.41171505947578));
#27344=CARTESIAN_POINT('Ctrl Pts',(-0.139760305935199,-0.184249334298881,
1.42282977235756));
#27345=CARTESIAN_POINT('Ctrl Pts',(0.079018054369913,-0.217340533238222,
1.43394448523934));
#27346=CARTESIAN_POINT('Ctrl Pts',(0.22545928307395,-0.0514671932444525,
1.44505919812111));
#27347=CARTESIAN_POINT('Ctrl Pts',(0.165503657787434,0.161521823799947,
1.45617391100289));
#27348=CARTESIAN_POINT('Ctrl Pts',(-0.0459624035544085,0.226645577420305,
1.46728862388466));
#27349=CARTESIAN_POINT('Ctrl Pts',(-0.215352151310341,0.0842864830841198,
1.47840333676644));
#27350=CARTESIAN_POINT('Ctrl Pts',(-0.187597625721037,-0.135232729501817,
1.48951804964822));
#27351=CARTESIAN_POINT('Ctrl Pts',(0.011893273891152,-0.230953047914141,
1.50063276252999));
#27352=CARTESIAN_POINT('Ctrl Pts',(0.200496467832881,-0.115247241577487,
1.51174747541177));
#27353=CARTESIAN_POINT('Ctrl Pts',(0.205555033969902,0.105961730423366,
1.52286218829354));
#27354=CARTESIAN_POINT('Ctrl Pts',(0.0224381044925165,0.230167964259722,
1.53397690117532));
#27355=CARTESIAN_POINT('Ctrl Pts',(-0.181219802999278,0.143666778712352,
1.5450916140571));
#27356=CARTESIAN_POINT('Ctrl Pts',(-0.218979918615408,-0.0743542570931251,
1.55620632693887));
#27357=CARTESIAN_POINT('Ctrl Pts',(-0.0562747188401855,-0.224307637685701,
1.56732103982065));
#27358=CARTESIAN_POINT('Ctrl Pts',(0.157947210561147,-0.168918438841454,
1.57843575270243));
#27359=CARTESIAN_POINT('Ctrl Pts',(0.227576258658446,0.0411072596958934,
1.5895504655842));
#27360=CARTESIAN_POINT('Ctrl Pts',(0.0888704660269324,0.213501289393851,
1.60066517846598));
#27361=CARTESIAN_POINT('Ctrl Pts',(-0.131191855156199,0.190445418546512,
1.61177989134775));
#27362=CARTESIAN_POINT('Ctrl Pts',(-0.231154503332997,-0.00695384020214284,
1.62289460422953));
#27363=CARTESIAN_POINT('Ctrl Pts',(-0.119506604260646,-0.197987201209499,
1.63400931711131));
#27364=CARTESIAN_POINT('Ctrl Pts',(0.101543696940346,-0.207773044248692,
1.64512402999308));
#27365=CARTESIAN_POINT('Ctrl Pts',(0.229635751732902,-0.0273529126556294,
1.65623874287486));
#27366=CARTESIAN_POINT('Ctrl Pts',(0.147507601461287,0.178107461426576,
1.66735345575664));
#27367=CARTESIAN_POINT('Ctrl Pts',(-0.0696564828655069,0.220519238842077,
1.67846816863841));
#27368=CARTESIAN_POINT('Ctrl Pts',(-0.223053492590313,0.0610565291180635,
1.68958288152019));
#27369=CARTESIAN_POINT('Ctrl Pts',(-0.172256030858622,-0.154300421702323,
1.70069759440197));
#27370=CARTESIAN_POINT('Ctrl Pts',(0.0362333314476733,-0.228402946559112,
1.71181230728374));
#27371=CARTESIAN_POINT('Ctrl Pts',(0.211552865843429,-0.0934138386863192,
1.72292702016552));
#27372=CARTESIAN_POINT('Ctrl Pts',(0.193206185357947,0.127091031328383,
1.73404173304729));
#27373=CARTESIAN_POINT('Ctrl Pts',(-0.00201122888355521,0.23125033029827,
1.74515644592907));
#27374=CARTESIAN_POINT('Ctrl Pts',(-0.195387462276077,0.123711357158493,
1.75627115881084));
#27375=CARTESIAN_POINT('Ctrl Pts',(-0.209896110474722,-0.0970792620092718,
1.76738587169262));
#27376=CARTESIAN_POINT('Ctrl Pts',(-0.0322552216209195,-0.228998604761835,
1.7785005845744));
#27377=CARTESIAN_POINT('Ctrl Pts',(0.174913731797615,-0.151281019078116,
1.78961529745618));
#27378=CARTESIAN_POINT('Ctrl Pts',(0.221957790509845,0.0649268783838334,
1.80073001033795));
#27379=CARTESIAN_POINT('Ctrl Pts',(0.0658104389801637,0.221697420882426,
1.81184472321973));
#27380=CARTESIAN_POINT('Ctrl Pts',(-0.15058312366156,0.175514908691566,
1.8229594361015));
#27381=CARTESIAN_POINT('Ctrl Pts',(-0.229125263358671,-0.0313428460019351,
1.83407414898328));
#27382=CARTESIAN_POINT('Ctrl Pts',(-0.097914524920906,-0.20950777101147,
1.84518886186505));
#27383=CARTESIAN_POINT('Ctrl Pts',(0.122932131932451,-0.195878664594243,
1.85630357474683));
#27384=CARTESIAN_POINT('Ctrl Pts',(0.231240485020835,-0.0029323014869812,
1.86741828762861));
#27385=CARTESIAN_POINT('Ctrl Pts',(0.127859578865474,0.192698439010348,
1.87853300051039));
#27386=CARTESIAN_POINT('Ctrl Pts',(-0.0925704657001019,0.211923262490807,
1.88964771339216));
#27387=CARTESIAN_POINT('Ctrl Pts',(-0.228256814497451,0.0371427912273366,
1.90076242627394));
#27388=CARTESIAN_POINT('Ctrl Pts',(-0.154985307260428,-0.171640073520352,
1.91187713915571));
#27389=CARTESIAN_POINT('Ctrl Pts',(0.0601676048900462,-0.223294916257574,
1.92299185203749));
#27390=CARTESIAN_POINT('Ctrl Pts',(0.220240042233107,-0.0705342760779494,
1.93410656491926));
#27391=CARTESIAN_POINT('Ctrl Pts',(0.178693583162176,0.146797015096847,
1.94522127780104));
#27392=CARTESIAN_POINT('Ctrl Pts',(-0.0264380381168497,0.229742878986952,
1.95633599068282));
#27393=CARTESIAN_POINT('Ctrl Pts',(-0.207366939425321,0.102370468095326,
1.96745070356459));
#27394=CARTESIAN_POINT('Ctrl Pts',(-0.19846163503823,-0.118717057420726,
1.97856541644637));
#27395=CARTESIAN_POINT('Ctrl Pts',(-0.00787449191185959,-0.231124971999587,
1.98968012932815));
#27396=CARTESIAN_POINT('Ctrl Pts',(0.189921360189439,-0.13194937380856,
2.00079484220992));
#27397=CARTESIAN_POINT('Ctrl Pts',(0.213853573968784,0.0880193683541974,
2.0119095550917));
#27398=CARTESIAN_POINT('Ctrl Pts',(0.0420133880490859,0.227410719908507,
2.02302426797347));
#27399=CARTESIAN_POINT('Ctrl Pts',(-0.168287982526885,0.158618773295263,
2.03413898085525));
#27400=CARTESIAN_POINT('Ctrl Pts',(-0.22453000507192,-0.0553808371837207,
2.04525369373703));
#27401=CARTESIAN_POINT('Ctrl Pts',(-0.075225881804619,-0.218682022606547,
2.0563684066188));
#27402=CARTESIAN_POINT('Ctrl Pts',(0.142943826109234,-0.181790601742365,
2.06748311950058));
#27403=CARTESIAN_POINT('Ctrl Pts',(0.230255511219254,0.0215211490958647,
2.07859783238236));
#27404=CARTESIAN_POINT('Ctrl Pts',(0.106779632017769,0.205131349359298,
2.08971254526413));
#27405=CARTESIAN_POINT('Ctrl Pts',(-0.114447733911049,0.200953916376482,
2.10082725814591));
#27406=CARTESIAN_POINT('Ctrl Pts',(-0.230903844027544,0.0128130840024069,
2.11194197102768));
#27407=CARTESIAN_POINT('Ctrl Pts',(-0.135978873097944,-0.187057494821968,
2.12305668390946));
#27408=CARTESIAN_POINT('Ctrl Pts',(0.0834280496133461,-0.215686162844967,
2.13417139679123));
#27409=CARTESIAN_POINT('Ctrl Pts',(0.226460707682758,-0.0468647863930802,
2.14528610967301));
#27410=CARTESIAN_POINT('Ctrl Pts',(0.162179756725932,0.164858990545831,
2.15640082255479));
#27411=CARTESIAN_POINT('Ctrl Pts',(-0.0505687624253055,0.225662492650313,
2.16751553543657));
#27412=CARTESIAN_POINT('Ctrl Pts',(-0.21702407434185,0.0798831121221699,
2.17863024831834));
#27413=CARTESIAN_POINT('Ctrl Pts',(-0.184804548483264,-0.139025317149112,
2.18974496120012));
#27414=CARTESIAN_POINT('Ctrl Pts',(0.016594424366101,-0.230662926381996,
2.20085967408189));
#27415=CARTESIAN_POINT('Ctrl Pts',(0.202802025046116,-0.111140000773359,
2.21197438696367));
#27416=CARTESIAN_POINT('Ctrl Pts',(0.203354364681193,0.110126110219503,
2.22308909984544));
#27417=CARTESIAN_POINT('Ctrl Pts',(0.0177458306323277,0.230577206138279,
2.23420381272722));
#27418=CARTESIAN_POINT('Ctrl Pts',(-0.184108169872144,0.139946227827396,
2.245318525609));
#27419=CARTESIAN_POINT('Ctrl Pts',(-0.217420156901447,-0.0787985930992519,
2.25643323849078));
#27420=CARTESIAN_POINT('Ctrl Pts',(-0.0516948355614441,-0.225407239388384,
2.26754795137255));
#27421=CARTESIAN_POINT('Ctrl Pts',(0.161354790428826,-0.16566657810232,
2.27866266425433));
#27422=CARTESIAN_POINT('Ctrl Pts',(0.226691621904214,0.0457334801950268,
2.2897773771361));
#27423=CARTESIAN_POINT('Ctrl Pts',(0.0845042946539431,0.215267144055698,
2.30089209001788));
#27424=CARTESIAN_POINT('Ctrl Pts',(-0.135044145927914,0.187733686574086,
2.31200680289966));
#27425=CARTESIAN_POINT('Ctrl Pts',(-0.230963288702208,-0.011659431219711,
2.32312151578143));
#27426=CARTESIAN_POINT('Ctrl Pts',(-0.115452720077891,-0.200381332197683,
2.33423622866321));
#27427=CARTESIAN_POINT('Ctrl Pts',(0.105760131433371,-0.205659407411252,
2.34535094154498));
#27428=CARTESIAN_POINT('Ctrl Pts',(0.230133849162723,-0.0226751875190042,
2.35646565442676));
#27429=CARTESIAN_POINT('Ctrl Pts',(0.143871237687637,0.181083693967286,
2.36758036730854));
#27430=CARTESIAN_POINT('Ctrl Pts',(-0.0741742662716807,0.219037708405472,
2.37869508019031));
#27431=CARTESIAN_POINT('Ctrl Pts',(-0.224172200254536,0.0565338436777074,
2.38980979307209));
#27432=CARTESIAN_POINT('Ctrl Pts',(-0.169229814680232,-0.157839433803576,
2.40092450595386));
#27433=CARTESIAN_POINT('Ctrl Pts',(0.0412118192216604,-0.227500408227043,
2.4120404065003));
#27434=CARTESIAN_POINT('Ctrl Pts',(0.155526271499594,-0.13538401532862,
2.41945140275281));
#27435=CARTESIAN_POINT('Ctrl Pts',(0.180578137565047,-0.0753122828814866,
2.4231574947114));
#27436=CARTESIAN_POINT('Ctrl Pts',(-0.15199516870275,-0.123304110510785,
2.4));
#27437=CARTESIAN_POINT('Ctrl Pts',(-0.148824665831025,-0.126538769486475,
2.4));
#27438=CARTESIAN_POINT('Ctrl Pts',(-0.145540355431101,-0.129648441844686,
2.4));
#27439=CARTESIAN_POINT('Ctrl Pts',(-0.142144069729336,-0.132625074476752,
2.4));
#27440=CARTESIAN_POINT('Ctrl Pts',(-0.132540690324889,-0.141041837677364,
2.4));
#27441=CARTESIAN_POINT('Ctrl Pts',(-0.122043505462798,-0.148398554468019,
2.4));
#27442=CARTESIAN_POINT('Ctrl Pts',(-0.110860112905452,-0.154651338932229,
2.4));
#27443=CARTESIAN_POINT('Ctrl Pts',(-0.105435415437936,-0.157684359893801,
2.4));
#27444=CARTESIAN_POINT('Ctrl Pts',(-0.099848934821215,-0.160456894218315,
2.4));
#27445=CARTESIAN_POINT('Ctrl Pts',(-0.0941236483875528,-0.162959592659119,
2.4));
#27446=CARTESIAN_POINT('Ctrl Pts',(-0.0907590799609226,-0.164430348795581,
2.4));
#27447=CARTESIAN_POINT('Ctrl Pts',(-0.0873466982488514,-0.16580752592612,
2.4));
#27448=CARTESIAN_POINT('Ctrl Pts',(-0.0839043527287589,-0.167084756767952,
2.4));
#27449=CARTESIAN_POINT('Ctrl Pts',(-0.0722287249452664,-0.171416823905253,
2.4));
#27450=CARTESIAN_POINT('Ctrl Pts',(-0.0601713335654445,-0.174620056925232,
2.4));
#27451=CARTESIAN_POINT('Ctrl Pts',(-0.0479233473597519,-0.176639901583043,
2.4));
#27452=CARTESIAN_POINT('Ctrl Pts',(-0.0398564206582088,-0.177970237732139,
2.4));
#27453=CARTESIAN_POINT('Ctrl Pts',(-0.0317065647200675,-0.178786199153318,
2.4));
#27454=CARTESIAN_POINT('Ctrl Pts',(-0.0235309431251825,-0.179059833327106,
2.4));
#27455=CARTESIAN_POINT('Ctrl Pts',(-0.0192489471657408,-0.179203149699191,
2.4));
#27456=CARTESIAN_POINT('Ctrl Pts',(-0.0149655652356923,-0.179197037719655,
2.4));
#27457=CARTESIAN_POINT('Ctrl Pts',(-0.0107021384747464,-0.179038942029942,
2.4));
#27458=CARTESIAN_POINT('Ctrl Pts',(-0.00225095961565695,-0.178725556805913,
2.4));
#27459=CARTESIAN_POINT('Ctrl Pts',(0.00613674255370757,-0.177816520060091,
2.4));
#27460=CARTESIAN_POINT('Ctrl Pts',(0.014397712940729,-0.176286708862887,
2.4));
#27461=CARTESIAN_POINT('Ctrl Pts',(0.0175977987980585,-0.175694099647843,
2.4));
#27462=CARTESIAN_POINT('Ctrl Pts',(0.0207787832759882,-0.175008200507475,
2.4));
#27463=CARTESIAN_POINT('Ctrl Pts',(0.0239367001203762,-0.174227024096589,
2.4));
#27464=CARTESIAN_POINT('Ctrl Pts',(0.0263036255441011,-0.173641515864912,
2.4));
#27465=CARTESIAN_POINT('Ctrl Pts',(0.0286575889694442,-0.173002476522167,
2.4));
#27466=CARTESIAN_POINT('Ctrl Pts',(0.0309968484005305,-0.172308959609583,
2.4));
#27467=CARTESIAN_POINT('Ctrl Pts',(0.0360874731122647,-0.170799749350007,
2.4));
#27468=CARTESIAN_POINT('Ctrl Pts',(0.0411108443148083,-0.16903165817095,
2.4));
#27469=CARTESIAN_POINT('Ctrl Pts',(0.0460449062726198,-0.16701820095113,
2.4));
#27470=CARTESIAN_POINT('Ctrl Pts',(0.0500648589951711,-0.16537776698379,
2.4));
#27471=CARTESIAN_POINT('Ctrl Pts',(0.0540173393440258,-0.163577829383814,
2.4));
#27472=CARTESIAN_POINT('Ctrl Pts',(0.0578908054835579,-0.161628640771827,
2.4));
#27473=CARTESIAN_POINT('Ctrl Pts',(0.0680358083015658,-0.156523517027585,
2.4));
#27474=CARTESIAN_POINT('Ctrl Pts',(0.0776550402843555,-0.150390999806698,
2.4));
#27475=CARTESIAN_POINT('Ctrl Pts',(0.086613738132899,-0.143350130393655,
2.4));
#27476=CARTESIAN_POINT('Ctrl Pts',(0.0907533250321785,-0.140096723338911,
2.4));
#27477=CARTESIAN_POINT('Ctrl Pts',(0.0947518982198043,-0.136648454397042,
2.4));
#27478=CARTESIAN_POINT('Ctrl Pts',(0.09859173507754,-0.133016695765916,
2.4));
#27479=CARTESIAN_POINT('Ctrl Pts',(0.102112604578935,-0.129686619860478,
2.4));
#27480=CARTESIAN_POINT('Ctrl Pts',(0.105494621732796,-0.126206936464483,
2.4));
#27481=CARTESIAN_POINT('Ctrl Pts',(0.108717820867798,-0.122595988102291,
2.4));
#27482=CARTESIAN_POINT('Ctrl Pts',(0.1145699112897,-0.116039894159817,2.4));
#27483=CARTESIAN_POINT('Ctrl Pts',(0.119909157676967,-0.109042420774433,
2.4));
#27484=CARTESIAN_POINT('Ctrl Pts',(0.124658963353444,-0.101655155004293,
2.4));
#27485=CARTESIAN_POINT('Ctrl Pts',(0.127026507874596,-0.097972966344028,
2.4));
#27486=CARTESIAN_POINT('Ctrl Pts',(0.129246602375859,-0.0941942185358602,
2.4));
#27487=CARTESIAN_POINT('Ctrl Pts',(0.131302274414547,-0.0903383755883276,
2.4));
#27488=CARTESIAN_POINT('Ctrl Pts',(0.13645721812277,-0.0806692002684345,
2.4));
#27489=CARTESIAN_POINT('Ctrl Pts',(0.140595547790541,-0.0704960807205455,
2.4));
#27490=CARTESIAN_POINT('Ctrl Pts',(0.143545299885864,-0.0599211930845618,
2.4));
#27491=CARTESIAN_POINT('',(-0.0904498980258696,-0.126704579043882,-7.30113716837731E-5));
#27492=CARTESIAN_POINT('Ctrl Pts',(-0.0905547187627354,-0.126790994435269,
1.91686944095437E-16));
#27493=CARTESIAN_POINT('Ctrl Pts',(-0.0937786982673176,-0.125067385071004,
-8.80357328303703E-17));
#27494=CARTESIAN_POINT('Ctrl Pts',(-0.0969317870940272,-0.123225562125392,
7.25923314697896E-17));
#27495=CARTESIAN_POINT('Ctrl Pts',(-0.100006715605072,-0.121266986978485,
7.89299181569447E-17));
#27496=CARTESIAN_POINT('Ctrl Pts',(-0.107443591426572,-0.116530070298209,
9.7298243307645E-17));
#27497=CARTESIAN_POINT('Ctrl Pts',(-0.114423960357986,-0.111111926712851,
-8.60222442940798E-17));
#27498=CARTESIAN_POINT('Ctrl Pts',(-0.120920626723875,-0.105114084706488,
1.07552855510562E-16));
#27499=CARTESIAN_POINT('Ctrl Pts',(-0.124692476039581,-0.101631843970501,
1.99916285244735E-16));
#27500=CARTESIAN_POINT('Ctrl Pts',(-0.128299160177052,-0.0979546858534835,
1.21953705927638E-16));
#27501=CARTESIAN_POINT('Ctrl Pts',(-0.131721852029444,-0.0941163405780606,
1.34441069388203E-16));
#27502=CARTESIAN_POINT('Ctrl Pts',(-0.137478284443309,-0.0876608441115559,
1.55442861804271E-16));
#27503=CARTESIAN_POINT('Ctrl Pts',(-0.142725690997129,-0.0807408650802736,
3.13072395126118E-16));
#27504=CARTESIAN_POINT('Ctrl Pts',(-0.147437251084092,-0.0734399138115947,
2.74086309204336E-16));
#27505=CARTESIAN_POINT('Ctrl Pts',(-0.150181027130752,-0.069188206343348,
2.51382770093966E-16));
#27506=CARTESIAN_POINT('Ctrl Pts',(-0.152742174737604,-0.0648067631725966,
1.97653338405712E-16));
#27507=CARTESIAN_POINT('Ctrl Pts',(-0.155103784497403,-0.0603327855088824,
1.76074432811646E-16));
#27508=CARTESIAN_POINT('Ctrl Pts',(-0.160567427408146,-0.0499821269194385,
1.26151098068711E-16));
#27509=CARTESIAN_POINT('Ctrl Pts',(-0.164980553993685,-0.0391180362903603,
8.13475317118353E-18));
#27510=CARTESIAN_POINT('Ctrl Pts',(-0.168274787260813,-0.0279332056041401,
4.68375338513738E-17));
#27511=CARTESIAN_POINT('Ctrl Pts',(-0.169906523489982,-0.0223930109767741,
6.60082252640462E-17));
#27512=CARTESIAN_POINT('Ctrl Pts',(-0.171263202886852,-0.0167734941869636,
1.43754342025142E-16));
#27513=CARTESIAN_POINT('Ctrl Pts',(-0.17233265600195,-0.0110954126933409,
2.48065457064683E-16));
#27514=CARTESIAN_POINT('Ctrl Pts',(-0.173163133015681,-0.00668613462778462,
3.290675899249E-16));
#27515=CARTESIAN_POINT('Ctrl Pts',(-0.173819585336133,-0.0022423248069032,
-2.23512275233336E-18));
#27516=CARTESIAN_POINT('Ctrl Pts',(-0.174294602869972,0.00220394339803012,
-1.73472347597681E-18));
#27517=CARTESIAN_POINT('Ctrl Pts',(-0.174947783696855,0.00831785906587972,
-1.04664105834344E-18));
#27518=CARTESIAN_POINT('Ctrl Pts',(-0.175260256565538,0.0144468401589108,
2.92331180691467E-16));
#27519=CARTESIAN_POINT('Ctrl Pts',(-0.175221744250391,0.0205647925020219,
2.39391839684799E-16));
#27520=CARTESIAN_POINT('Ctrl Pts',(-0.175173289109206,0.028262232747164,
1.62396291645263E-16));
#27521=CARTESIAN_POINT('Ctrl Pts',(-0.174569669212428,0.0359422811365845,
-1.12250719804115E-16));
#27522=CARTESIAN_POINT('Ctrl Pts',(-0.173446373975916,0.0435656717636887,
-4.5102810375397E-17));
#27523=CARTESIAN_POINT('Ctrl Pts',(-0.172637904118492,0.0490524586146037,
5.18085424066423E-17));
#27524=CARTESIAN_POINT('Ctrl Pts',(-0.171559653499544,0.0545113728394569,
5.96783951772411E-17));
#27525=CARTESIAN_POINT('Ctrl Pts',(-0.170222848604401,0.0599234158566936,
1.73472347597681E-17));
#27526=CARTESIAN_POINT('Ctrl Pts',(-0.169222922852311,0.0639716065867067,
-1.43163367689382E-17));
#27527=CARTESIAN_POINT('Ctrl Pts',(-0.168079794711886,0.0679869286825006,
9.01404419406027E-17));
#27528=CARTESIAN_POINT('Ctrl Pts',(-0.166801973771595,0.0719549338288062,
9.8879238130678E-17));
#27529=CARTESIAN_POINT('Ctrl Pts',(-0.163394778652899,0.0825352642484763,
1.22180455682585E-16));
#27530=CARTESIAN_POINT('Ctrl Pts',(-0.159027462790524,0.0927996140500163,
1.91178027158399E-16));
#27531=CARTESIAN_POINT('Ctrl Pts',(-0.153795590326359,0.102636459258385,
1.00613961606655E-16));
#27532=CARTESIAN_POINT('Ctrl Pts',(-0.150728825820311,0.108402518722398,
4.75280609736047E-17));
#27533=CARTESIAN_POINT('Ctrl Pts',(-0.147364797318139,0.114021013727962,
-1.44861482947255E-16));
#27534=CARTESIAN_POINT('Ctrl Pts',(-0.143715779143174,0.119470837464023,
3.46944695195361E-18));
#27535=CARTESIAN_POINT('Ctrl Pts',(-0.140547585855608,0.124202547242139,
1.32255063770552E-16));
#27536=CARTESIAN_POINT('Ctrl Pts',(-0.13716418235433,0.128805658068609,
-3.06595871754581E-17));
#27537=CARTESIAN_POINT('Ctrl Pts',(-0.133596163369402,0.13323881795393,
-6.59194920871187E-17));
#27538=CARTESIAN_POINT('Ctrl Pts',(-0.125566297160433,0.143215693332807,
-1.45272298273861E-16));
#27539=CARTESIAN_POINT('Ctrl Pts',(-0.116585657780435,0.152364342920442,
-1.57993899402886E-16));
#27540=CARTESIAN_POINT('Ctrl Pts',(-0.106768224044845,0.160520635554423,
-6.93889390390723E-18));
#27541=CARTESIAN_POINT('Ctrl Pts',(-0.100257772229834,0.165929498156689,
9.32335504643276E-17));
#27542=CARTESIAN_POINT('Ctrl Pts',(-0.093378247512691,0.170901777887464,
2.69387857240372E-16));
#27543=CARTESIAN_POINT('Ctrl Pts',(-0.0861525859670521,0.175382131162754,
-2.42861286636753E-17));
#27544=CARTESIAN_POINT('Ctrl Pts',(-0.0903762848818376,-0.126601459829486,
-7.30113716837788E-5));
#27545=CARTESIAN_POINT('Ctrl Pts',(-0.0898498377495766,-0.126977271736114,
-4.86742477891657E-5));
#27546=CARTESIAN_POINT('Ctrl Pts',(-0.0893210464778968,-0.127349799910583,
-2.43371238945576E-5));
#27547=CARTESIAN_POINT('Ctrl Pts',(-0.0887899522119581,-0.127719015366539,
5.55111512312578E-17));
#27548=CARTESIAN_POINT('Ctrl Pts',(0.113598829883088,-0.159281402661362,
-0.0231499042268511));
#27549=CARTESIAN_POINT('Ctrl Pts',(0.166586312519255,-0.121492960388918,
-0.019443812294868));
#27550=CARTESIAN_POINT('Ctrl Pts',(0.23095150288242,0.0104442927835965,
-0.0120328160689595));
#27551=CARTESIAN_POINT('Ctrl Pts',(0.11621706131274,0.200096033890315,-0.000916915549125608));
#27552=CARTESIAN_POINT('Ctrl Pts',(-0.10499236225076,0.205957905231008,
0.0101977973326507));
#27553=CARTESIAN_POINT('Ctrl Pts',(-0.230035845505828,0.0235725168559611,
0.0213125102144268));
#27554=CARTESIAN_POINT('Ctrl Pts',(-0.144519469099591,-0.180546871179966,
0.032427223096203));
#27555=CARTESIAN_POINT('Ctrl Pts',(0.0733113434475644,-0.219303463105964,
0.0435419359779792));
#27556=CARTESIAN_POINT('Ctrl Pts',(0.224021882516666,-0.0573411296239388,
0.0546566488597554));
#27557=CARTESIAN_POINT('Ctrl Pts',(0.169655302903142,0.157136560254222,
0.0657713617415314));
#27558=CARTESIAN_POINT('Ctrl Pts',(-0.0400243713777188,0.227751714669903,
0.0768860746233078));
#27559=CARTESIAN_POINT('Ctrl Pts',(-0.213062639347379,0.0898775913551375,
0.0880007875050837));
#27560=CARTESIAN_POINT('Ctrl Pts',(-0.191053130847012,-0.13027828503737,
0.0991155003868603));
#27561=CARTESIAN_POINT('Ctrl Pts',(0.00585639141000308,-0.231169107852035,
0.110230213268636));
#27562=CARTESIAN_POINT('Ctrl Pts',(0.197404520979761,-0.120436912062476,
0.121344926150413));
#27563=CARTESIAN_POINT('Ctrl Pts',(0.20823862917329,0.100549809014636,0.132459639032189));
#27564=CARTESIAN_POINT('Ctrl Pts',(0.0284404998142444,0.229487890809628,
0.143574351913965));
#27565=CARTESIAN_POINT('Ctrl Pts',(-0.177393481894344,0.14834125742336,
0.154689064795741));
#27566=CARTESIAN_POINT('Ctrl Pts',(-0.220832491835081,-0.0686045495364922,
0.165803777677517));
#27567=CARTESIAN_POINT('Ctrl Pts',(-0.0621102407412604,-0.222746238913572,
0.176918490559294));
#27568=CARTESIAN_POINT('Ctrl Pts',(0.153470869196092,-0.172974751378497,
0.18803320344107));
#27569=CARTESIAN_POINT('Ctrl Pts',(0.228556969297201,0.035146599885103,
0.199147916322846));
#27570=CARTESIAN_POINT('Ctrl Pts',(0.0944104355434771,0.211092967147494,
0.210262629204622));
#27571=CARTESIAN_POINT('Ctrl Pts',(-0.126164195146967,0.193794136856338,
0.221377342086398));
#27572=CARTESIAN_POINT('Ctrl Pts',(-0.231241727855144,-0.000913669237423759,
0.232492054968175));
#27573=CARTESIAN_POINT('Ctrl Pts',(-0.124628863434608,-0.194785055445563,
0.243606767849951));
#27574=CARTESIAN_POINT('Ctrl Pts',(0.0960755786891363,-0.210340330602452,
0.254721480731727));
#27575=CARTESIAN_POINT('Ctrl Pts',(0.228827567011875,-0.0333394068786314,
0.265836193613503));
#27576=CARTESIAN_POINT('Ctrl Pts',(0.152099203503735,0.174182099430741,
0.27695090649528));
#27577=CARTESIAN_POINT('Ctrl Pts',(-0.0638684792613543,0.222248484439645,
0.288065619377055));
#27578=CARTESIAN_POINT('Ctrl Pts',(-0.221367719264692,0.0668573432203991,
0.299180332258832));
#27579=CARTESIAN_POINT('Ctrl Pts',(-0.176215730145938,-0.149738398293394,
0.310295045140607));
#27580=CARTESIAN_POINT('Ctrl Pts',(0.0302530689509243,-0.229256021283673,
0.321409758022384));
#27581=CARTESIAN_POINT('Ctrl Pts',(0.209026675506927,-0.0989010637032879,
0.33252447090416));
#27582=CARTESIAN_POINT('Ctrl Pts',(0.196446669842519,0.121992939889483,
0.343639183785936));
#27583=CARTESIAN_POINT('Ctrl Pts',(0.00402942669754128,0.231208423712843,
0.354753896667712));
#27584=CARTESIAN_POINT('Ctrl Pts',(-0.192076557857611,0.128763998838017,
0.365868609549488));
#27585=CARTESIAN_POINT('Ctrl Pts',(-0.212345926919954,-0.0915575163255094,
0.376983322431265));
#27586=CARTESIAN_POINT('Ctrl Pts',(-0.0382230727993462,-0.22806264091471,
0.38809803531304));
#27587=CARTESIAN_POINT('Ctrl Pts',(0.170891119305128,-0.155787665807794,
0.399212748194818));
#27588=CARTESIAN_POINT('Ctrl Pts',(0.223562920044702,0.0591032338902731,
0.410327461076593));
#27589=CARTESIAN_POINT('Ctrl Pts',(0.0715738936182804,0.219888037936411,
0.42144217395837));
#27590=CARTESIAN_POINT('Ctrl Pts',(-0.145937502387498,0.179376188141297,
0.432556886840145));
#27591=CARTESIAN_POINT('Ctrl Pts',(-0.22985031260278,-0.0253457150541741,
0.443671599721922));
#27592=CARTESIAN_POINT('Ctrl Pts',(-0.103346497859673,-0.206864866169546,
0.454786312603698));
#27593=CARTESIAN_POINT('Ctrl Pts',(0.117765938619279,-0.19900943489273,
0.465901025485474));
#27594=CARTESIAN_POINT('Ctrl Pts',(0.231069466514541,-0.00897068112737101,
0.477015738367251));
#27595=CARTESIAN_POINT('Ctrl Pts',(0.13284029417393,0.189280288775634,0.488130451249026));
#27596=CARTESIAN_POINT('Ctrl Pts',(-0.0869976157926483,0.2142544896183,
0.499245164130803));
#27597=CARTESIAN_POINT('Ctrl Pts',(-0.227193499228025,0.0430892722580614,
0.510359877012579));
#27598=CARTESIAN_POINT('Ctrl Pts',(-0.159404939315424,-0.167522048689269,
0.521474589894355));
#27599=CARTESIAN_POINT('Ctrl Pts',(0.0543109806804912,-0.224775196257787,
0.532589302776132));
#27600=CARTESIAN_POINT('Ctrl Pts',(0.218307876483828,-0.0762577375767544,
0.543704015657907));
#27601=CARTESIAN_POINT('Ctrl Pts',(0.182454678322123,0.142069918820186,
0.554818728539684));
#27602=CARTESIAN_POINT('Ctrl Pts',(-0.0204267791691959,0.230339571433083,
0.56593344142146));
#27603=CARTESIAN_POINT('Ctrl Pts',(-0.204608527780934,0.107744706758718,
0.577048154303235));
#27604=CARTESIAN_POINT('Ctrl Pts',(-0.201481260512532,-0.113485122978673,
0.588162867185013));
#27605=CARTESIAN_POINT('Ctrl Pts',(-0.0139078363112272,-0.230824919721298,
0.599277580066788));
#27606=CARTESIAN_POINT('Ctrl Pts',(0.186397526097791,-0.136855886756203,
0.610392292948565));
#27607=CARTESIAN_POINT('Ctrl Pts',(0.216065146500031,0.0823979607946937,
0.621507005830341));
#27608=CARTESIAN_POINT('Ctrl Pts',(0.0479357816258322,0.22622053910979,
0.632621718712117));
#27609=CARTESIAN_POINT('Ctrl Pts',(-0.164076427131555,0.162949371078709,
0.643736431593893));
#27610=CARTESIAN_POINT('Ctrl Pts',(-0.225884759107982,-0.0494939095034147,
0.65485114447567));
#27611=CARTESIAN_POINT('Ctrl Pts',(-0.0809067347692004,-0.216627956977371,
0.665965857357445));
#27612=CARTESIAN_POINT('Ctrl Pts',(0.13813741492639,-0.185449793940728,
0.677080570239222));
#27613=CARTESIAN_POINT('Ctrl Pts',(0.230723574201407,0.0154985090551028,
0.688195283120998));
#27614=CARTESIAN_POINT('Ctrl Pts',(0.112093680593801,0.202258691398264,
0.699309996002774));
#27615=CARTESIAN_POINT('Ctrl Pts',(-0.109152449131232,0.203861017175568,
0.71042470888455));
#27616=CARTESIAN_POINT('Ctrl Pts',(-0.230474895081132,0.0188386361646833,
0.721539421766327));
#27617=CARTESIAN_POINT('Ctrl Pts',(-0.14080894161815,-0.183429587132448,
0.732654134648102));
#27618=CARTESIAN_POINT('Ctrl Pts',(0.0777606531918726,-0.217777070166666,
0.743768847529879));
#27619=CARTESIAN_POINT('Ctrl Pts',(0.225144205164223,-0.052760386239807,
0.754883560411655));
#27620=CARTESIAN_POINT('Ctrl Pts',(0.166419341432716,0.160555829144583,
0.765998273293431));
#27621=CARTESIAN_POINT('Ctrl Pts',(-0.0446542215698074,0.226891101569008,
0.777112986175206));
#27622=CARTESIAN_POINT('Ctrl Pts',(-0.21484904707372,0.0855187607880183,
0.788227699056984));
#27623=CARTESIAN_POINT('Ctrl Pts',(-0.188360166347894,-0.134141787704641,
0.79934241193876));
#27624=CARTESIAN_POINT('Ctrl Pts',(0.0105631567361596,-0.231002145433697,
0.810457124820536));
#27625=CARTESIAN_POINT('Ctrl Pts',(0.199816430803703,-0.116391432056113,
0.821571837702312));
#27626=CARTESIAN_POINT('Ctrl Pts',(0.206147617427287,0.104769896937319,
0.832686550584088));
#27627=CARTESIAN_POINT('Ctrl Pts',(0.0237608275074776,0.230019552541438,
0.843801263465864));
#27628=CARTESIAN_POINT('Ctrl Pts',(-0.180377828110171,0.144697652370248,
0.85491597634764));
#27629=CARTESIAN_POINT('Ctrl Pts',(-0.219389478336887,-0.0730878120501113,
0.866030689229417));
#27630=CARTESIAN_POINT('Ctrl Pts',(-0.0575608814467432,-0.223964989233312,
0.877145402111192));
#27631=CARTESIAN_POINT('Ctrl Pts',(0.156961863502205,-0.169813264738413,
0.888260114992969));
#27632=CARTESIAN_POINT('Ctrl Pts',(0.227793763782214,0.0397941284253905,
0.899374827874745));
#27633=CARTESIAN_POINT('Ctrl Pts',(0.0900917081199666,0.212971959664249,
0.910489540756522));
#27634=CARTESIAN_POINT('Ctrl Pts',(-0.130084862998348,0.191184465618692,
0.921604253638297));
#27635=CARTESIAN_POINT('Ctrl Pts',(-0.23117515783393,-0.00562297747292118,
0.932718966520074));
#27636=CARTESIAN_POINT('Ctrl Pts',(-0.12063599724344,-0.197282862013618,
0.94383367940185));
#27637=CARTESIAN_POINT('Ctrl Pts',(0.100339469049717,-0.208340016381933,
0.954948392283626));
#27638=CARTESIAN_POINT('Ctrl Pts',(0.229459100175727,-0.0286721610931074,
0.966063105165402));
#27639=CARTESIAN_POINT('Ctrl Pts',(0.148520242025696,0.177243643563972,
0.977177818047179));
#27640=CARTESIAN_POINT('Ctrl Pts',(-0.0683815726727458,0.220901634204017,
0.988292530928954));
#27641=CARTESIAN_POINT('Ctrl Pts',(-0.222683430172034,0.0623350736104523,
0.999407243810731));
#27642=CARTESIAN_POINT('Ctrl Pts',(-0.173129590107263,-0.153296172504387,
1.01052195669251));
#27643=CARTESIAN_POINT('Ctrl Pts',(0.0349158509402568,-0.228592333266716,
1.02163666957428));
#27644=CARTESIAN_POINT('Ctrl Pts',(0.210997552503568,-0.0946234871092144,
1.03275138245606));
#27645=CARTESIAN_POINT('Ctrl Pts',(0.193921401160202,0.125968494661433,
1.04386609533784));
#27646=CARTESIAN_POINT('Ctrl Pts',(-0.000680228731668428,0.231242532342292,
1.05498080821961));
#27647=CARTESIAN_POINT('Ctrl Pts',(-0.194659142768612,0.124825436557587,
1.06609552110139));
#27648=CARTESIAN_POINT('Ctrl Pts',(-0.210437212200008,-0.0958631899985209,
1.07721023398317));
#27649=CARTESIAN_POINT('Ctrl Pts',(-0.0335703926366225,-0.228793794088533,
1.08832494686494));
#27650=CARTESIAN_POINT('Ctrl Pts',(0.174028465692067,-0.152274963812402,
1.09943965974672));
#27651=CARTESIAN_POINT('Ctrl Pts',(0.222312846772713,0.0636440856247927,
1.1105543726285));
#27652=CARTESIAN_POINT('Ctrl Pts',(0.0670807811141855,0.221300113602127,
1.12166908551027));
#27653=CARTESIAN_POINT('Ctrl Pts',(-0.149560431226741,0.176366802109906,
1.13278379839205));
#27654=CARTESIAN_POINT('Ctrl Pts',(-0.229286445107886,-0.0300216182940176,
1.14389851127382));
#27655=CARTESIAN_POINT('Ctrl Pts',(-0.099112026912242,-0.208926727817555,
1.1550132241556));
#27656=CARTESIAN_POINT('Ctrl Pts',(0.121794563711203,-0.196569722301278,
1.16612793703738));
#27657=CARTESIAN_POINT('Ctrl Pts',(0.231204238171301,-0.00426283084717903,
1.17724264991915));
#27658=CARTESIAN_POINT('Ctrl Pts',(0.128957835590708,0.191946472004472,
1.18835736280093));
#27659=CARTESIAN_POINT('Ctrl Pts',(-0.0913431052659731,0.212438246546079,
1.1994720756827));
#27660=CARTESIAN_POINT('Ctrl Pts',(-0.228023938298392,0.0384532838401966,
1.21058678856448));
#27661=CARTESIAN_POINT('Ctrl Pts',(-0.155960101971211,-0.170733763703413,
1.22170150144625));
#27662=CARTESIAN_POINT('Ctrl Pts',(0.0588775157502169,-0.223622471174715,
1.23281621432803));
#27663=CARTESIAN_POINT('Ctrl Pts',(0.219815671644481,-0.0717958353575546,
1.24393092720981));
#27664=CARTESIAN_POINT('Ctrl Pts',(0.17952342146866,0.145756346755087,1.25504564009158));
#27665=CARTESIAN_POINT('Ctrl Pts',(-0.0251136669571722,0.229875782124103,
1.26616035297336));
#27666=CARTESIAN_POINT('Ctrl Pts',(-0.206760431891084,0.103555276444112,
1.27727506585514));
#27667=CARTESIAN_POINT('Ctrl Pts',(-0.199128218864034,-0.117564977468804,
1.28838977873691));
#27668=CARTESIAN_POINT('Ctrl Pts',(-0.00920394248114851,-0.231060292819875,
1.29950449161869));
#27669=CARTESIAN_POINT('Ctrl Pts',(0.189146089304304,-0.133031306000099,
1.31061920450046));
#27670=CARTESIAN_POINT('Ctrl Pts',(0.214342205026698,0.0867812803517921,
1.32173391738224));
#27671=CARTESIAN_POINT('Ctrl Pts',(0.0433186034159268,0.227149884598909,
1.33284863026401));
#27672=CARTESIAN_POINT('Ctrl Pts',(-0.167361043146336,0.159573972539927,
1.34396334314579));
#27673=CARTESIAN_POINT('Ctrl Pts',(-0.224829908963541,-0.0540840411826741,
1.35507805602757));
#27674=CARTESIAN_POINT('Ctrl Pts',(-0.0764780817475084,-0.218230782630281,
1.36619276890935));
#27675=CARTESIAN_POINT('Ctrl Pts',(0.141885657405372,-0.182598005733494,
1.37730748179112));
#27676=CARTESIAN_POINT('Ctrl Pts',(0.230360075011687,0.0201942396691022,
1.3884221946729));
#27677=CARTESIAN_POINT('Ctrl Pts',(0.107951205315767,0.204499654635592,
1.39953690755467));
#27678=CARTESIAN_POINT('Ctrl Pts',(-0.113281668687639,0.201595721716874,
1.41065162043645));
#27679=CARTESIAN_POINT('Ctrl Pts',(-0.230810762065343,0.0141408482779098,
1.42176633331823));
#27680=CARTESIAN_POINT('Ctrl Pts',(-0.137043986371098,-0.186259274332104,
1.4328810462));
#27681=CARTESIAN_POINT('Ctrl Pts',(0.0821797998293032,-0.21614821760824,
1.44399575908178));
#27682=CARTESIAN_POINT('Ctrl Pts',(0.226172032398009,-0.0481641281054451,
1.45511047196355));
#27683=CARTESIAN_POINT('Ctrl Pts',(0.163114924122819,0.163911845220565,
1.46622518484533));
#27684=CARTESIAN_POINT('Ctrl Pts',(-0.0492658523502109,0.225934608387937,
1.47733989772711));
#27685=CARTESIAN_POINT('Ctrl Pts',(-0.216546170791042,0.0811253806828713,
1.48845461060888));
#27686=CARTESIAN_POINT('Ctrl Pts',(-0.185589149941156,-0.13795013192934,
1.49956932349066));
#27687=CARTESIAN_POINT('Ctrl Pts',(0.0152655844132623,-0.230739102467971,
1.51068403637244));
#27688=CARTESIAN_POINT('Ctrl Pts',(0.202145429136763,-0.112297804761793,
1.52179874925421));
#27689=CARTESIAN_POINT('Ctrl Pts',(0.203971103308708,0.108946594670196,
1.53291346213599));
#27690=CARTESIAN_POINT('Ctrl Pts',(0.0190712922670278,0.230455759933375,
1.54402817501776));
#27691=CARTESIAN_POINT('Ctrl Pts',(-0.183287346247982,0.140994043067697,
1.55514288789954));
#27692=CARTESIAN_POINT('Ctrl Pts',(-0.217855459014481,-0.077540766392869,
1.56625760078132));
#27693=CARTESIAN_POINT('Ctrl Pts',(-0.052987643695869,-0.225090828535423,
1.57737231366309));
#27694=CARTESIAN_POINT('Ctrl Pts',(0.160387746072949,-0.166581338645248,
1.58848702654487));
#27695=CARTESIAN_POINT('Ctrl Pts',(0.226936064644018,0.0444251509743055,
1.59960173942665));
#27696=CARTESIAN_POINT('Ctrl Pts',(0.085735608532081,0.214762605927655,
1.61071645230842));
#27697=CARTESIAN_POINT('Ctrl Pts',(-0.133951568706273,0.188495487257208,
1.6218311651902));
#27698=CARTESIAN_POINT('Ctrl Pts',(-0.231012691292417,-0.0103299533899106,
1.63294587807197));
#27699=CARTESIAN_POINT('Ctrl Pts',(-0.116593088558386,-0.199698831182409,
1.64406059095375));
#27700=CARTESIAN_POINT('Ctrl Pts',(0.104561736373614,-0.206253278184223,
1.65517530383553));
#27701=CARTESIAN_POINT('Ctrl Pts',(0.229995448645884,-0.0239930214308629,
1.6662900167173));
#27702=CARTESIAN_POINT('Ctrl Pts',(0.144879671070419,0.180231663105379,
1.67740472959908));
#27703=CARTESIAN_POINT('Ctrl Pts',(-0.0728662998970503,0.219463149103709,
1.68851944248086));
#27704=CARTESIAN_POINT('Ctrl Pts',(-0.223906767078497,0.0577869460316003,
1.69963415536263));
#27705=CARTESIAN_POINT('Ctrl Pts',(-0.169971632093058,-0.156790356077234,
1.71074886824441));
#27706=CARTESIAN_POINT('Ctrl Pts',(0.0395641490637797,-0.227833820105933,
1.72186358112618));
#27707=CARTESIAN_POINT('Ctrl Pts',(0.212880903058631,-0.0903066586035895,
1.73297829400796));
#27708=CARTESIAN_POINT('Ctrl Pts',(0.191315689600593,0.129891794921208,
1.74409300688973));
#27709=CARTESIAN_POINT('Ctrl Pts',(-0.00538960198695829,0.231180716465768,
1.75520771977151));
#27710=CARTESIAN_POINT('Ctrl Pts',(-0.197160978770901,0.12083509393096,
1.76632243265329));
#27711=CARTESIAN_POINT('Ctrl Pts',(-0.208441203479882,-0.100129097504481,
1.77743714553507));
#27712=CARTESIAN_POINT('Ctrl Pts',(-0.0289037867341024,-0.229430038546902,
1.78855185841684));
#27713=CARTESIAN_POINT('Ctrl Pts',(0.17709362123047,-0.148699094801151,
1.79966657129862));
#27714=CARTESIAN_POINT('Ctrl Pts',(0.220970553225224,0.0681585363879073,
1.81078128418039));
#27715=CARTESIAN_POINT('Ctrl Pts',(0.0625598420215454,0.222620389096423,
1.82189599706217));
#27716=CARTESIAN_POINT('Ctrl Pts',(-0.153121319098175,0.173284255236413,
1.83301070994394));
#27717=CARTESIAN_POINT('Ctrl Pts',(-0.228627464534992,-0.0346850679039896,
1.84412542282572));
#27718=CARTESIAN_POINT('Ctrl Pts',(-0.0948364421085485,-0.210901922047656,
1.8552401357075));
#27719=CARTESIAN_POINT('Ctrl Pts',(0.12577266572998,-0.194048468250533,
1.86635484858927));
#27720=CARTESIAN_POINT('Ctrl Pts',(0.231243101207172,0.000446787749336298,
1.87746956147105));
#27721=CARTESIAN_POINT('Ctrl Pts',(0.12502188245106,0.194533031600284,1.88858427435282));
#27722=CARTESIAN_POINT('Ctrl Pts',(-0.0956507036032086,0.210533879400477,
1.8996989872346));
#27723=CARTESIAN_POINT('Ctrl Pts',(-0.22875978800645,0.0338013441514916,
1.91081370011638));
#27724=CARTESIAN_POINT('Ctrl Pts',(-0.152450568934512,-0.173874654584121,
1.92192841299815));
#27725=CARTESIAN_POINT('Ctrl Pts',(0.0634196271269303,-0.22237698255504,
1.93304312587993));
#27726=CARTESIAN_POINT('Ctrl Pts',(0.221232282412995,-0.0673041506412468,
1.9441578387617));
#27727=CARTESIAN_POINT('Ctrl Pts',(0.176517694337723,0.149382311740377,
1.95527255164348));
#27728=CARTESIAN_POINT('Ctrl Pts',(-0.0297901370418169,0.229316635267117,
1.96638726452526));
#27729=CARTESIAN_POINT('Ctrl Pts',(-0.208826567210671,0.099322889115285,
1.97750197740704));
#27730=CARTESIAN_POINT('Ctrl Pts',(-0.196692574435429,-0.121596063411524,
1.98861669028881));
#27731=CARTESIAN_POINT('Ctrl Pts',(-0.00449623065254251,-0.231199817009248,
1.99973140317059));
#27732=CARTESIAN_POINT('Ctrl Pts',(0.191816190538262,-0.129151540922183,
2.01084611605236));
#27733=CARTESIAN_POINT('Ctrl Pts',(0.212530349676141,0.0911286011185604,
2.02196082893414));
#27734=CARTESIAN_POINT('Ctrl Pts',(0.0386834556929351,0.227985003302295,
2.03307554181592));
#27735=CARTESIAN_POINT('Ctrl Pts',(-0.170576234106037,0.15613237919574,
2.04419025469769));
#27736=CARTESIAN_POINT('Ctrl Pts',(-0.22368179441174,-0.0586517376086509,
2.05530496757947));
#27737=CARTESIAN_POINT('Ctrl Pts',(-0.0720177039274894,-0.219743081336705,
2.06641968046125));
#27738=CARTESIAN_POINT('Ctrl Pts',(0.145575042578183,-0.179670471845826,
2.07753439334302));
#27739=CARTESIAN_POINT('Ctrl Pts',(0.229901017386071,0.0248815932714643,
2.0886491062248));
#27740=CARTESIAN_POINT('Ctrl Pts',(0.103763949480942,0.206655786893781,
2.09976381910657));
#27741=CARTESIAN_POINT('Ctrl Pts',(-0.117363896480564,0.199246799920331,
2.11087853198835));
#27742=CARTESIAN_POINT('Ctrl Pts',(-0.231050883702757,0.00943719442296102,
2.12199324487013));
#27743=CARTESIAN_POINT('Ctrl Pts',(-0.133222182155807,-0.189011697012588,
2.1331079577519));
#27744=CARTESIAN_POINT('Ctrl Pts',(0.0865648562855566,-0.214429702115095,
2.14422267063368));
#27745=CARTESIAN_POINT('Ctrl Pts',(0.227106038835561,-0.0435478902060165,
2.15533738351545));
#27746=CARTESIAN_POINT('Ctrl Pts',(0.159742842467667,0.167199866623727,
2.16645209639723));
#27747=CARTESIAN_POINT('Ctrl Pts',(-0.0538570452843743,0.224884393346986,
2.17756680927901));
#27748=CARTESIAN_POINT('Ctrl Pts',(-0.218153468818653,0.0766983464531386,
2.18868152216078));
#27749=CARTESIAN_POINT('Ctrl Pts',(-0.182741142414774,-0.141701248491403,
2.19979623504256));
#27750=CARTESIAN_POINT('Ctrl Pts',(0.0199616707544952,-0.230380349352727,
2.21091094792433));
#27751=CARTESIAN_POINT('Ctrl Pts',(0.204390589890243,-0.10815758335346,
2.22202566080611));
#27752=CARTESIAN_POINT('Ctrl Pts',(0.20170994550457,0.113078078965284,2.23314037368789));
#27753=CARTESIAN_POINT('Ctrl Pts',(0.0143739066504459,0.230796407208724,
2.24425508656966));
#27754=CARTESIAN_POINT('Ctrl Pts',(-0.186120948441361,0.137231874000472,
2.25536979945144));
#27755=CARTESIAN_POINT('Ctrl Pts',(-0.216230848357744,-0.081961417532537,
2.26648451233322));
#27756=CARTESIAN_POINT('Ctrl Pts',(-0.048392844163279,-0.226123556916373,
2.27759922521499));
#27757=CARTESIAN_POINT('Ctrl Pts',(0.163747892690182,-0.16327981306027,
2.28871393809677));
#27758=CARTESIAN_POINT('Ctrl Pts',(0.225982712376694,0.0490367978780694,
2.29982865097855));
#27759=CARTESIAN_POINT('Ctrl Pts',(0.0813468259969867,0.216465965620237,
2.31094336386032));
#27760=CARTESIAN_POINT('Ctrl Pts',(-0.137768190986319,0.185724889406933,
2.3220580767421));
#27761=CARTESIAN_POINT('Ctrl Pts',(-0.230743965476533,-0.0150261240684335,
2.33317278962387));
#27762=CARTESIAN_POINT('Ctrl Pts',(-0.112521659700458,-0.202044365771375,
2.34428750250565));
#27763=CARTESIAN_POINT('Ctrl Pts',(0.108778414904377,-0.204057369921787,
2.35540221538743));
#27764=CARTESIAN_POINT('Ctrl Pts',(0.23036421697438,-0.0193489636911256,
2.3665169282692));
#27765=CARTESIAN_POINT('Ctrl Pts',(0.141318813665082,0.183231604869622,
2.37763164115098));
#27766=CARTESIAN_POINT('Ctrl Pts',(-0.0776082748673582,0.217759953254891,
2.38874635403276));
#27767=CARTESIAN_POINT('Ctrl Pts',(-0.175417824731111,0.108336165866313,
2.3961561626206));
#27768=CARTESIAN_POINT('Ctrl Pts',(-0.190389869545322,0.0450217421539731,
2.39986106691453));
#27769=CARTESIAN_POINT('Ctrl Pts',(0.10578567459061,-0.148326269272423,
-0.0153811560512364));
#27770=CARTESIAN_POINT('Ctrl Pts',(0.155128758505242,-0.113136858768523,
-0.0116750641192532));
#27771=CARTESIAN_POINT('Ctrl Pts',(0.215067008659125,0.00972595016050153,
-0.00426406789334474));
#27772=CARTESIAN_POINT('Ctrl Pts',(0.108223828032029,0.1863337320444,0.00685183262648915));
#27773=CARTESIAN_POINT('Ctrl Pts',(-0.0977711467537901,0.19179243276145,
0.0179665455082654));
#27774=CARTESIAN_POINT('Ctrl Pts',(-0.214214328808668,0.0219512348848415,
0.0290812583900415));
#27775=CARTESIAN_POINT('Ctrl Pts',(-0.134579639120505,-0.168129131106836,
0.0401959712718177));
#27776=CARTESIAN_POINT('Ctrl Pts',(0.0682691003923698,-0.204220103398932,
0.051310684153594));
#27777=CARTESIAN_POINT('Ctrl Pts',(0.208613997076146,-0.0533972936631411,
0.06242539703537));
#27778=CARTESIAN_POINT('Ctrl Pts',(0.157986668383419,0.146328945874253,
0.0735401099171463));
#27779=CARTESIAN_POINT('Ctrl Pts',(-0.0372715557951986,0.212087297028674,
0.0846548227989223));
#27780=CARTESIAN_POINT('Ctrl Pts',(-0.198408514036763,0.0836959468849107,
0.0957695356806986));
#27781=CARTESIAN_POINT('Ctrl Pts',(-0.177912786162498,-0.121317942107057,
0.106884248562475));
#27782=CARTESIAN_POINT('Ctrl Pts',(0.00545359768767935,-0.215269647088839,
0.117998961444251));
#27783=CARTESIAN_POINT('Ctrl Pts',(0.183827337311238,-0.112153443844903,
0.129113674326027));
#27784=CARTESIAN_POINT('Ctrl Pts',(0.193916291968782,0.0936341455939032,
0.140228387207803));
#27785=CARTESIAN_POINT('Ctrl Pts',(0.0264844053555898,0.21370406160572,
0.15134310008958));
#27786=CARTESIAN_POINT('Ctrl Pts',(-0.165192627155433,0.138138570637568,
0.162457812971356));
#27787=CARTESIAN_POINT('Ctrl Pts',(-0.205643967850216,-0.0638860326305435,
0.173572525853132));
#27788=CARTESIAN_POINT('Ctrl Pts',(-0.0578383925482501,-0.207426090306074,
0.184687238734908));
#27789=CARTESIAN_POINT('Ctrl Pts',(0.142915375489557,-0.161077810225246,
0.195801951616684));
#27790=CARTESIAN_POINT('Ctrl Pts',(0.21283716746355,0.0327292700306685,
0.20691666449846));
#27791=CARTESIAN_POINT('Ctrl Pts',(0.0879170289222095,0.196574312904571,
0.218031377380237));
#27792=CARTESIAN_POINT('Ctrl Pts',(-0.117486813081955,0.180465269934133,
0.229146090262013));
#27793=CARTESIAN_POINT('Ctrl Pts',(-0.215337272398233,-0.000850828452481674,
0.240260803143789));
#27794=CARTESIAN_POINT('Ctrl Pts',(-0.116057079157066,-0.181388034645117,
0.251375516025565));
#27795=CARTESIAN_POINT('Ctrl Pts',(0.0894676460468228,-0.19587344156003,
0.262490228907341));
#27796=CARTESIAN_POINT('Ctrl Pts',(0.213089153877661,-0.0310463730193083,
0.273604941789118));
#27797=CARTESIAN_POINT('Ctrl Pts',(0.141638050883947,0.162202118708908,
0.284719654670894));
#27798=CARTESIAN_POINT('Ctrl Pts',(-0.059475702088586,0.206962570630221,
0.29583436755267));
#27799=CARTESIAN_POINT('Ctrl Pts',(-0.206142383148674,0.0622589965159431,
0.306949080434446));
#27800=CARTESIAN_POINT('Ctrl Pts',(-0.1640958793867,-0.139439618276758,
0.318063793316222));
#27801=CARTESIAN_POINT('Ctrl Pts',(0.0281723087350732,-0.213488139714225,
0.329178506197999));
#27802=CARTESIAN_POINT('Ctrl Pts',(0.194650137670344,-0.0920987984854177,
0.340293219079775));
#27803=CARTESIAN_POINT('Ctrl Pts',(0.182935365723024,0.113602450437052,
0.351407931961551));
#27804=CARTESIAN_POINT('Ctrl Pts',(0.00375228883829077,0.215306258864348,
0.362522644843327));
#27805=CARTESIAN_POINT('Ctrl Pts',(-0.178865823414919,0.119907806216696,
0.373637357725103));
#27806=CARTESIAN_POINT('Ctrl Pts',(-0.197741096003495,-0.0852603291627437,
0.384752070606879));
#27807=CARTESIAN_POINT('Ctrl Pts',(-0.035594147802109,-0.212376838237756,
0.395866783488655));
#27808=CARTESIAN_POINT('Ctrl Pts',(0.159137487206888,-0.1450728263428,0.406981496370432));
#27809=CARTESIAN_POINT('Ctrl Pts',(0.208186601347174,0.0550382030695517,
0.418096209252208));
#27810=CARTESIAN_POINT('Ctrl Pts',(0.0666511497282075,0.204764472058811,
0.429210922133984));
#27811=CARTESIAN_POINT('Ctrl Pts',(-0.13590014222874,0.167038965872701,
0.44032563501576));
#27812=CARTESIAN_POINT('Ctrl Pts',(-0.214041556577407,-0.0236024751993154,
0.451440347897537));
#27813=CARTESIAN_POINT('Ctrl Pts',(-0.0962384824202376,-0.192637014301674,
0.462555060779312));
#27814=CARTESIAN_POINT('Ctrl Pts',(0.109666175905667,-0.185321867678483,
0.473669773661089));
#27815=CARTESIAN_POINT('Ctrl Pts',(0.215176858931472,-0.0083536912798596,
0.484784486542865));
#27816=CARTESIAN_POINT('Ctrl Pts',(0.123703740139465,0.176261877480984,
0.495899199424641));
#27817=CARTESIAN_POINT('Ctrl Pts',(-0.0810140516752797,0.199518390653015,
0.507013912306417));
#27818=CARTESIAN_POINT('Ctrl Pts',(-0.211567474798578,0.0401256574396861,
0.518128625188193));
#27819=CARTESIAN_POINT('Ctrl Pts',(-0.148441309262714,-0.156000136160149,
0.52924333806997));
#27820=CARTESIAN_POINT('Ctrl Pts',(0.0505755537700164,-0.209315499040252,
0.540358050951745));
#27821=CARTESIAN_POINT('Ctrl Pts',(0.203292991715257,-0.0710128460003809,
0.551472763833522));
#27822=CARTESIAN_POINT('Ctrl Pts',(0.16990572216618,0.132298565195555,0.562587476715298));
#27823=CARTESIAN_POINT('Ctrl Pts',(-0.0190218562669204,0.214497164927125,
0.573702189597074));
#27824=CARTESIAN_POINT('Ctrl Pts',(-0.190535863446603,0.10033418917932,
0.584816902478851));
#27825=CARTESIAN_POINT('Ctrl Pts',(-0.187623684879683,-0.105679788274689,
0.595931615360627));
#27826=CARTESIAN_POINT('Ctrl Pts',(-0.012951276415378,-0.214949131695911,
0.607046328242403));
#27827=CARTESIAN_POINT('Ctrl Pts',(0.173577386849575,-0.127443146351959,
0.61816104112418));
#27828=CARTESIAN_POINT('Ctrl Pts',(0.201204513299551,0.0767307539745598,
0.629275754005954));
#27829=CARTESIAN_POINT('Ctrl Pts',(0.0446388312409215,0.210661433402173,
0.640390466887733));
#27830=CARTESIAN_POINT('Ctrl Pts',(-0.152791499229278,0.151741960383025,
0.651505179769506));
#27831=CARTESIAN_POINT('Ctrl Pts',(-0.210348747839816,-0.0460897934453505,
0.662619892651285));
#27832=CARTESIAN_POINT('Ctrl Pts',(-0.0753420922142629,-0.201728614525534,
0.673734605533059));
#27833=CARTESIAN_POINT('Ctrl Pts',(0.128636532957515,-0.172694838273424,
0.684849318414837));
#27834=CARTESIAN_POINT('Ctrl Pts',(0.214854756567229,0.0144325450995374,
0.695964031296612));
#27835=CARTESIAN_POINT('Ctrl Pts',(0.104384047187493,0.188347645247752,
0.707078744178388));
#27836=CARTESIAN_POINT('Ctrl Pts',(-0.10164510916572,0.189839765487378,
0.718193457060165));
#27837=CARTESIAN_POINT('Ctrl Pts',(-0.214623181219824,0.0175429433304858,
0.729308169941941));
#27838=CARTESIAN_POINT('Ctrl Pts',(-0.131124316093717,-0.170813578226583,
0.740422882823717));
#27839=CARTESIAN_POINT('Ctrl Pts',(0.0724123933580511,-0.202798693451838,
0.751537595705493));
#27840=CARTESIAN_POINT('Ctrl Pts',(0.209659128073555,-0.0491316068641172,
0.76265230858727));
#27841=CARTESIAN_POINT('Ctrl Pts',(0.154973271436896,0.149513042634279,
0.773767021469046));
#27842=CARTESIAN_POINT('Ctrl Pts',(-0.0415829719103787,0.211285875592086,
0.784881734350822));
#27843=CARTESIAN_POINT('Ctrl Pts',(-0.200072055348054,0.0796369100757868,
0.795996447232598));
#27844=CARTESIAN_POINT('Ctrl Pts',(-0.175405039678833,-0.12491571891832,
0.807111160114375));
#27845=CARTESIAN_POINT('Ctrl Pts',(0.00983663883061682,-0.215114168092504,
0.81822587299615));
#27846=CARTESIAN_POINT('Ctrl Pts',(0.186073359634179,-0.108386205820036,
0.829340585877927));
#27847=CARTESIAN_POINT('Ctrl Pts',(0.191969096840493,0.0975639822673277,
0.840455298759702));
#27848=CARTESIAN_POINT('Ctrl Pts',(0.0221265938152439,0.214199156449667,
0.85157001164148));
#27849=CARTESIAN_POINT('Ctrl Pts',(-0.167971714563094,0.13474556721595,
0.862684724523254));
#27850=CARTESIAN_POINT('Ctrl Pts',(-0.204300202632679,-0.0680609431455381,
0.873799437405031));
#27851=CARTESIAN_POINT('Ctrl Pts',(-0.0536019312887383,-0.208561016826566,
0.884914150286807));
#27852=CARTESIAN_POINT('Ctrl Pts',(0.146166264499983,-0.158133765843145,
0.896028863168584));
#27853=CARTESIAN_POINT('Ctrl Pts',(0.212126454066791,0.0370571486040605,
0.907143576050359));
#27854=CARTESIAN_POINT('Ctrl Pts',(0.0838953370232766,0.198324071164759,
0.918258288932136));
#27855=CARTESIAN_POINT('Ctrl Pts',(-0.121137823342632,0.178035087927698,
0.929373001813913));
#27856=CARTESIAN_POINT('Ctrl Pts',(-0.215275280962153,-0.00523623760731131,
0.940487714695687));
#27857=CARTESIAN_POINT('Ctrl Pts',(-0.112338836248953,-0.183714045864339,
0.951602427577466));
#27858=CARTESIAN_POINT('Ctrl Pts',(0.093438272492876,-0.194010705918928,
0.962717140459239));
#27859=CARTESIAN_POINT('Ctrl Pts',(0.21367725114797,-0.0267001333229138,
0.973831853341018));
#27860=CARTESIAN_POINT('Ctrl Pts',(0.138305244950313,0.165053094478255,
0.984946566222792));
#27861=CARTESIAN_POINT('Ctrl Pts',(-0.0636783917774306,0.205708354711845,
0.996061279104569));
#27862=CARTESIAN_POINT('Ctrl Pts',(-0.207367601454554,0.0580477617535676,
1.00717599198635));
#27863=CARTESIAN_POINT('Ctrl Pts',(-0.161221999380996,-0.14275269417145,
1.01829070486812));
#27864=CARTESIAN_POINT('Ctrl Pts',(0.0325143916484108,-0.212870099152858,
1.0294054177499));
#27865=CARTESIAN_POINT('Ctrl Pts',(0.196485460735197,-0.0881154271242621,
1.04052013063168));
#27866=CARTESIAN_POINT('Ctrl Pts',(0.180583781192123,0.117304572579115,
1.05163484351345));
#27867=CARTESIAN_POINT('Ctrl Pts',(-0.000633443630793526,0.215338021553975,
1.06274955639523));
#27868=CARTESIAN_POINT('Ctrl Pts',(-0.181270782051193,0.116240132278671,
1.07386426927701));
#27869=CARTESIAN_POINT('Ctrl Pts',(-0.195963659788188,-0.0892698651283455,
1.08497898215878));
#27870=CARTESIAN_POINT('Ctrl Pts',(-0.0312614719270617,-0.213057703804784,
1.09609369504056));
#27871=CARTESIAN_POINT('Ctrl Pts',(0.162059051665856,-0.141801722665054,
1.10720840792233));
#27872=CARTESIAN_POINT('Ctrl Pts',(0.2070225062196,0.059266741906144,1.11832312080411));
#27873=CARTESIAN_POINT('Ctrl Pts',(0.0624670666901483,0.206079427301083,
1.12943783368589));
#27874=CARTESIAN_POINT('Ctrl Pts',(-0.139273891515134,0.164236560850027,
1.14055254656766));
#27875=CARTESIAN_POINT('Ctrl Pts',(-0.213516471033934,-0.0279567769034468,
1.15166725944944));
#27876=CARTESIAN_POINT('Ctrl Pts',(-0.0922952519647008,-0.194557064231516,
1.16278197233121));
#27877=CARTESIAN_POINT('Ctrl Pts',(0.113417718271556,-0.183049954820229,
1.17389668521299));
#27878=CARTESIAN_POINT('Ctrl Pts',(0.215302361198007,-0.00396963980438003,
1.18501139809477));
#27879=CARTESIAN_POINT('Ctrl Pts',(0.120088311171413,0.178744684669536,
1.19612611097654));
#27880=CARTESIAN_POINT('Ctrl Pts',(-0.0850606649708146,0.1978270660257,
1.20724082385832));
#27881=CARTESIAN_POINT('Ctrl Pts',(-0.212340797528712,0.0358085252765923,
1.2183555367401));
#27882=CARTESIAN_POINT('Ctrl Pts',(-0.145233402608328,-0.158990954284894,
1.22947024962187));
#27883=CARTESIAN_POINT('Ctrl Pts',(0.0548280094809581,-0.208242056640751,
1.24058496250365));
#27884=CARTESIAN_POINT('Ctrl Pts',(0.204697083010726,-0.0668578266511397,
1.25169967538542));
#27885=CARTESIAN_POINT('Ctrl Pts',(0.167176072715028,0.135731446206079,
1.2628143882672));
#27886=CARTESIAN_POINT('Ctrl Pts',(-0.0233863870186178,0.214065274343667,
1.27392910114898));
#27887=CARTESIAN_POINT('Ctrl Pts',(-0.192539762854552,0.0964329015301672,
1.28504381403075));
#27888=CARTESIAN_POINT('Ctrl Pts',(-0.185432481868328,-0.109479036558445,
1.29615852691253));
#27889=CARTESIAN_POINT('Ctrl Pts',(-0.00857090927137133,-0.215168316189618,
1.3072732397943));
#27890=CARTESIAN_POINT('Ctrl Pts',(0.176136908045833,-0.123881614461822,
1.31838795267608));
#27891=CARTESIAN_POINT('Ctrl Pts',(0.199600073128609,0.0808125954580599,
1.32950266555786));
#27892=CARTESIAN_POINT('Ctrl Pts',(0.0403392155482017,0.211526859917528,
1.34061737843963));
#27893=CARTESIAN_POINT('Ctrl Pts',(-0.15585020433436,0.148598716638307,
1.35173209132141));
#27894=CARTESIAN_POINT('Ctrl Pts',(-0.209366448689055,-0.0503642228267966,
1.36284680420318));
#27895=CARTESIAN_POINT('Ctrl Pts',(-0.0712180352331336,-0.203221200260076,
1.37396151708496));
#27896=CARTESIAN_POINT('Ctrl Pts',(0.132126977001494,-0.170039191735495,
1.38507622996674));
#27897=CARTESIAN_POINT('Ctrl Pts',(0.214516258300679,0.0188053104810904,
1.39619094284852));
#27898=CARTESIAN_POINT('Ctrl Pts',(0.100526485078686,0.190434478431135,
1.40730565573029));
#27899=CARTESIAN_POINT('Ctrl Pts',(-0.105490327261336,0.187730273615925,
1.41842036861207));
#27900=CARTESIAN_POINT('Ctrl Pts',(-0.21493594778207,0.013168262172261,
1.42953508149384));
#27901=CARTESIAN_POINT('Ctrl Pts',(-0.127618308760518,-0.173448643830728,
1.44064979437562));
#27902=CARTESIAN_POINT('Ctrl Pts',(0.0765275977896153,-0.201281870902883,
1.45176450725739));
#27903=CARTESIAN_POINT('Ctrl Pts',(0.210616262908487,-0.044851472395862,
1.46287922013917));
#27904=CARTESIAN_POINT('Ctrl Pts',(0.151896126939755,0.152638237012603,
1.47399393302095));
#27905=CARTESIAN_POINT('Ctrl Pts',(-0.0458774217173872,0.210395168561873,
1.48510864590272));
#27906=CARTESIAN_POINT('Ctrl Pts',(-0.201652453469104,0.0755456999934797,
1.4962233587845));
#27907=CARTESIAN_POINT('Ctrl Pts',(-0.172824609579421,-0.128462131001064,
1.50733807166628));
#27908=CARTESIAN_POINT('Ctrl Pts',(0.0142156406614265,-0.214869216823162,
1.51845278454805));
#27909=CARTESIAN_POINT('Ctrl Pts',(0.18824217299288,-0.104574132004682,
1.52956749742983));
#27910=CARTESIAN_POINT('Ctrl Pts',(0.189942280063182,0.101453413062418,
1.5406822103116));
#27911=CARTESIAN_POINT('Ctrl Pts',(0.0177595976988407,0.214605362158519,
1.55179692319338));
#27912=CARTESIAN_POINT('Ctrl Pts',(-0.170681120454501,0.131296686546196,
1.56291163607516));
#27913=CARTESIAN_POINT('Ctrl Pts',(-0.202871690833546,-0.0722076300397131,
1.57402634895693));
#27914=CARTESIAN_POINT('Ctrl Pts',(-0.0493432338968959,-0.20960942260836,
1.58514106183871));
#27915=CARTESIAN_POINT('Ctrl Pts',(0.149356520061482,-0.155124126726753,
1.59625577472049));
#27916=CARTESIAN_POINT('Ctrl Pts',(0.211327746174964,0.0413696564431422,
1.60737048760226));
#27917=CARTESIAN_POINT('Ctrl Pts',(0.0798388433607749,0.199991559492963,
1.61848520048404));
#27918=CARTESIAN_POINT('Ctrl Pts',(-0.124738582894269,0.175531053421164,
1.62959991336581));
#27919=CARTESIAN_POINT('Ctrl Pts',(-0.215123988623049,-0.00961947485696401,
1.64071462624759));
#27920=CARTESIAN_POINT('Ctrl Pts',(-0.108573992693813,-0.185963848336544,
1.65182933912937));
#27921=CARTESIAN_POINT('Ctrl Pts',(0.0973701386716032,-0.192067490410758,
1.66294405201114));
#27922=CARTESIAN_POINT('Ctrl Pts',(0.214176710383506,-0.0223428177926071,
1.67405876489292));
#27923=CARTESIAN_POINT('Ctrl Pts',(0.134915066945881,0.167835602565731,
1.68517347777469));
#27924=CARTESIAN_POINT('Ctrl Pts',(-0.0678546662625307,0.204368806435851,
1.69628819065647));
#27925=CARTESIAN_POINT('Ctrl Pts',(-0.208506799103289,0.0538124474941849,
1.70740290353825));
#27926=CARTESIAN_POINT('Ctrl Pts',(-0.158281240931237,-0.146006553095679,
1.71851761642002));
#27927=CARTESIAN_POINT('Ctrl Pts',(0.0368429868742704,-0.212163755377294,
1.7296323293018));
#27928=CARTESIAN_POINT('Ctrl Pts',(0.198239277294426,-0.0840955035385219,
1.74074704218357));
#27929=CARTESIAN_POINT('Ctrl Pts',(0.178157286523072,0.120958034195128,
1.75186175506535));
#27930=CARTESIAN_POINT('Ctrl Pts',(-0.00501891333345269,0.215280457279719,
1.76297646794713));
#27931=CARTESIAN_POINT('Ctrl Pts',(-0.183600545566271,0.112524239368154,
1.7740911808289));
#27932=CARTESIAN_POINT('Ctrl Pts',(-0.194104933521689,-0.0932423699835773,
1.78520589371068));
#27933=CARTESIAN_POINT('Ctrl Pts',(-0.0269158281034883,-0.213650188333915,
1.79632060659246));
#27934=CARTESIAN_POINT('Ctrl Pts',(0.164913390453403,-0.138471796503031,
1.80743531947423));
#27935=CARTESIAN_POINT('Ctrl Pts',(0.205772533587259,0.0634706955901187,
1.81855003235601));
#27936=CARTESIAN_POINT('Ctrl Pts',(0.0582570709341164,0.207308896248547,
1.82966474523779));
#27937=CARTESIAN_POINT('Ctrl Pts',(-0.142589866917423,0.161366026877052,
1.84077945811956));
#27938=CARTESIAN_POINT('Ctrl Pts',(-0.212902814145765,-0.0322994815194884,
1.85189417100134));
#27939=CARTESIAN_POINT('Ctrl Pts',(-0.0883137354016025,-0.196396407597057,
1.86300888388311));
#27940=CARTESIAN_POINT('Ctrl Pts',(0.117122212464671,-0.180702108800628,
1.87412359676489));
#27941=CARTESIAN_POINT('Ctrl Pts',(0.215338551293191,0.000416058365307058,
1.88523830964666));
#27942=CARTESIAN_POINT('Ctrl Pts',(0.116423066921421,0.181153344617824,
1.89635302252844));
#27943=CARTESIAN_POINT('Ctrl Pts',(-0.089071993225153,0.196053678365167,
1.90746773541022));
#27944=CARTESIAN_POINT('Ctrl Pts',(-0.213026036609469,0.0314765389468832,
1.91858244829199));
#27945=CARTESIAN_POINT('Ctrl Pts',(-0.141965249933099,-0.161915819452723,
1.92969716117377));
#27946=CARTESIAN_POINT('Ctrl Pts',(0.059057721323464,-0.207082230840055,
1.94081187405555));
#27947=CARTESIAN_POINT('Ctrl Pts',(0.206016261438301,-0.0626750731997882,
1.95192658693732));
#27948=CARTESIAN_POINT('Ctrl Pts',(0.164377074939183,0.139108022816996,
1.9630412998191));
#27949=CARTESIAN_POINT('Ctrl Pts',(-0.0277412165808244,0.213544584759783,
1.97415601270088));
#27950=CARTESIAN_POINT('Ctrl Pts',(-0.19446379251932,0.0924916113851058,
1.98527072558265));
#27951=CARTESIAN_POINT('Ctrl Pts',(-0.183164357370848,-0.113232870521543,
1.99638543846443));
#27952=CARTESIAN_POINT('Ctrl Pts',(-0.00418698672498783,-0.215298244116777,
2.0075001513462));
#27953=CARTESIAN_POINT('Ctrl Pts',(0.178623363765053,-0.120268693743865,
2.01861486422798));
#27954=CARTESIAN_POINT('Ctrl Pts',(0.197912834442113,0.0848609140934513,
2.02972957710976));
#27955=CARTESIAN_POINT('Ctrl Pts',(0.0360228662582626,0.212304540422618,
2.04084428999153));
#27956=CARTESIAN_POINT('Ctrl Pts',(-0.158844259334395,0.145393830866544,
2.05195900287331));
#27957=CARTESIAN_POINT('Ctrl Pts',(-0.208297299715472,-0.0546177600176673,
2.06307371575508));
#27958=CARTESIAN_POINT('Ctrl Pts',(-0.0670644354372087,-0.204629485354265,
2.07418842863686));
#27959=CARTESIAN_POINT('Ctrl Pts',(0.135562611855587,-0.167313009190196,
2.08530314151863));
#27960=CARTESIAN_POINT('Ctrl Pts',(0.214088773962576,0.0231702750091667,
2.09641785440042));
#27961=CARTESIAN_POINT('Ctrl Pts',(0.0966272223518926,0.192442315181511,
2.10753256728219));
#27962=CARTESIAN_POINT('Ctrl Pts',(-0.109291785615718,0.185542907099355,
2.11864728016397));
#27963=CARTESIAN_POINT('Ctrl Pts',(-0.215159554217309,0.00878811849825859,
2.12976199304574));
#27964=CARTESIAN_POINT('Ctrl Pts',(-0.124059362444929,-0.176011759052189,
2.14087670592752));
#27965=CARTESIAN_POINT('Ctrl Pts',(0.0806110567109805,-0.19968155229992,
2.1519914188093));
#27966=CARTESIAN_POINT('Ctrl Pts',(0.211486029799309,-0.0405527323404903,
2.16310613169107));
#27967=CARTESIAN_POINT('Ctrl Pts',(0.148755971948441,0.155700113288616,
2.17422084457285));
#27968=CARTESIAN_POINT('Ctrl Pts',(-0.0501528393622344,0.20941718571921,
2.18533555745462));
#27969=CARTESIAN_POINT('Ctrl Pts',(-0.203149203975196,0.0714231504662535,
2.1964502703364));
#27970=CARTESIAN_POINT('Ctrl Pts',(-0.170172483692846,-0.131955251453046,
2.20756498321817));
#27971=CARTESIAN_POINT('Ctrl Pts',(0.0185887373038336,-0.21453513820328,
2.21867969609995));
#27972=CARTESIAN_POINT('Ctrl Pts',(0.190332914993618,-0.100718668747836,
2.22979440898173));
#27973=CARTESIAN_POINT('Ctrl Pts',(0.187836641264677,0.105300740131422,
2.2409091218635));
#27974=CARTESIAN_POINT('Ctrl Pts',(0.0133852911432732,0.214922580230725,
2.25202383474528));
#27975=CARTESIAN_POINT('Ctrl Pts',(-0.173319831785035,0.1277932737636,2.26313854762705));
#27976=CARTESIAN_POINT('Ctrl Pts',(-0.201358818434712,-0.0763242354961321,
2.27425326050883));
#27977=CARTESIAN_POINT('Ctrl Pts',(-0.0450644577099939,-0.210571121496985,
2.28536797339061));
#27978=CARTESIAN_POINT('Ctrl Pts',(0.152485560888693,-0.152049675066076,
2.29648268627238));
#27979=CARTESIAN_POINT('Ctrl Pts',(0.210439964031213,0.0456641212645707,
2.30759739915416));
#27980=CARTESIAN_POINT('Ctrl Pts',(0.075751914634623,0.201577764688349,
2.31871211203594));
#27981=CARTESIAN_POINT('Ctrl Pts',(-0.128292703680264,0.172951013090535,
2.32982682491771));
#27982=CARTESIAN_POINT('Ctrl Pts',(-0.214873745361368,-0.0139926500360693,
2.34094153779949));
#27983=CARTESIAN_POINT('Ctrl Pts',(-0.104782590540052,-0.188148060612542,
2.35205625068127));
#27984=CARTESIAN_POINT('Ctrl Pts',(0.101296800445916,-0.190022613389401,
2.36317096356304));
#27985=CARTESIAN_POINT('Ctrl Pts',(0.214520115385455,-0.0180181713033658,
2.37428567644482));
#27986=CARTESIAN_POINT('Ctrl Pts',(0.131599119914276,0.170629212883634,
2.3854003893266));
#27987=CARTESIAN_POINT('Ctrl Pts',(-0.0722704953836764,0.202782753815304,
2.39651510220837));
#27988=CARTESIAN_POINT('Ctrl Pts',(-0.163352852696599,0.100884968626203,
2.40392491079622));
#27989=CARTESIAN_POINT('Ctrl Pts',(-0.177295142967567,0.0419252149859687,
2.40762981509015));
#27990=CARTESIAN_POINT('Ctrl Pts',(0.0979725192981311,-0.137371135883486,
-0.00761240787562157));
#27991=CARTESIAN_POINT('Ctrl Pts',(0.143671204491229,-0.104780757148129,
-0.00390631594363848));
#27992=CARTESIAN_POINT('Ctrl Pts',(0.199182514435829,0.00900760753740661,
0.00350468028227001));
#27993=CARTESIAN_POINT('Ctrl Pts',(0.100230594751318,0.172571430198485,
0.0146205808021039));
#27994=CARTESIAN_POINT('Ctrl Pts',(-0.0905499312568196,0.177626960291894,
0.0257352936838801));
#27995=CARTESIAN_POINT('Ctrl Pts',(-0.198392812111508,0.0203299529137219,
0.0368500065656563));
#27996=CARTESIAN_POINT('Ctrl Pts',(-0.124639809141419,-0.155711391033705,
0.0479647194474324));
#27997=CARTESIAN_POINT('Ctrl Pts',(0.0632268573371749,-0.1891367436919,
0.0590794323292087));
#27998=CARTESIAN_POINT('Ctrl Pts',(0.193206111635628,-0.0494534577023437,
0.0701941452109847));
#27999=CARTESIAN_POINT('Ctrl Pts',(0.146318033863695,0.135521331494285,
0.0813088580927611));
#28000=CARTESIAN_POINT('Ctrl Pts',(-0.034518740212678,0.196422879387445,
0.092423570974537));
#28001=CARTESIAN_POINT('Ctrl Pts',(-0.183754388726148,0.0775143024146838,
0.103538283856313));
#28002=CARTESIAN_POINT('Ctrl Pts',(-0.164772441477984,-0.112357599176744,
0.114652996738089));
#28003=CARTESIAN_POINT('Ctrl Pts',(0.00505080396535491,-0.199370186325643,
0.125767709619866));
#28004=CARTESIAN_POINT('Ctrl Pts',(0.170250153642716,-0.10386997562733,
0.136882422501642));
#28005=CARTESIAN_POINT('Ctrl Pts',(0.179593954764274,0.0867184821731703,
0.147997135383418));
#28006=CARTESIAN_POINT('Ctrl Pts',(0.0245283108969357,0.197920232401811,
0.159111848265194));
#28007=CARTESIAN_POINT('Ctrl Pts',(-0.152991772416522,0.127935883851777,
0.170226561146971));
#28008=CARTESIAN_POINT('Ctrl Pts',(-0.190455443865352,-0.0591675157245945,
0.181341274028746));
#28009=CARTESIAN_POINT('Ctrl Pts',(-0.0535665443552399,-0.192105941698575,
0.192455986910523));
#28010=CARTESIAN_POINT('Ctrl Pts',(0.132359881783023,-0.149180869071993,
0.203570699792299));
#28011=CARTESIAN_POINT('Ctrl Pts',(0.1971173656299,0.0303119401762338,0.214685412674075));
#28012=CARTESIAN_POINT('Ctrl Pts',(0.0814236223009415,0.18205565866165,
0.225800125555851));
#28013=CARTESIAN_POINT('Ctrl Pts',(-0.108809431016943,0.16713640301193,
0.236914838437627));
#28014=CARTESIAN_POINT('Ctrl Pts',(-0.199432816941323,-0.000787987667539729,
0.248029551319403));
#28015=CARTESIAN_POINT('Ctrl Pts',(-0.107485294879524,-0.167991013844673,
0.25914426420118));
#28016=CARTESIAN_POINT('Ctrl Pts',(0.0828597134045088,-0.181406552517609,
0.270258977082955));
#28017=CARTESIAN_POINT('Ctrl Pts',(0.197350740743448,-0.0287533391599853,
0.281373689964733));
#28018=CARTESIAN_POINT('Ctrl Pts',(0.131176898264159,0.150222137987075,
0.292488402846508));
#28019=CARTESIAN_POINT('Ctrl Pts',(-0.0550829249158173,0.191676656820797,
0.303603115728285));
#28020=CARTESIAN_POINT('Ctrl Pts',(-0.190917047032656,0.0576606498114871,
0.31471782861006));
#28021=CARTESIAN_POINT('Ctrl Pts',(-0.151976028627464,-0.129140838260122,
0.325832541491837));
#28022=CARTESIAN_POINT('Ctrl Pts',(0.0260915485192222,-0.197720258144776,
0.336947254373613));
#28023=CARTESIAN_POINT('Ctrl Pts',(0.180273599833761,-0.0852965332675473,
0.348061967255389));
#28024=CARTESIAN_POINT('Ctrl Pts',(0.169424061603529,0.10521196098462,0.359176680137165));
#28025=CARTESIAN_POINT('Ctrl Pts',(0.0034751509790407,0.199404094015852,
0.370291393018941));
#28026=CARTESIAN_POINT('Ctrl Pts',(-0.165655088972228,0.111051613595375,
0.381406105900718));
#28027=CARTESIAN_POINT('Ctrl Pts',(-0.183136265087034,-0.078963141999978,
0.392520818782493));
#28028=CARTESIAN_POINT('Ctrl Pts',(-0.0329652228048722,-0.196691035560804,
0.40363553166427));
#28029=CARTESIAN_POINT('Ctrl Pts',(0.147383855108649,-0.134357986877806,
0.414750244546046));
#28030=CARTESIAN_POINT('Ctrl Pts',(0.192810282649647,0.0509731722488304,
0.425864957427822));
#28031=CARTESIAN_POINT('Ctrl Pts',(0.0617284058381346,0.18964090618121,
0.436979670309599));
#28032=CARTESIAN_POINT('Ctrl Pts',(-0.125862782069983,0.154701743604105,
0.448094383191375));
#28033=CARTESIAN_POINT('Ctrl Pts',(-0.198232800552033,-0.0218592353444565,
0.459209096073151));
#28034=CARTESIAN_POINT('Ctrl Pts',(-0.089130466980802,-0.178409162433804,
0.470323808954927));
#28035=CARTESIAN_POINT('Ctrl Pts',(0.101566413192055,-0.171634300464235,
0.481438521836703));
#28036=CARTESIAN_POINT('Ctrl Pts',(0.199284251348403,-0.00773670143234845,
0.49255323471848));
#28037=CARTESIAN_POINT('Ctrl Pts',(0.114567186105001,0.163243466186335,
0.503667947600255));
#28038=CARTESIAN_POINT('Ctrl Pts',(-0.075030487557911,0.184782291687729,
0.514782660482032));
#28039=CARTESIAN_POINT('Ctrl Pts',(-0.195941450369131,0.0371620426213107,
0.525897373363808));
#28040=CARTESIAN_POINT('Ctrl Pts',(-0.137477679210005,-0.14447822363103,
0.537012086245585));
#28041=CARTESIAN_POINT('Ctrl Pts',(0.0468401268595415,-0.193855801822718,
0.54812679912736));
#28042=CARTESIAN_POINT('Ctrl Pts',(0.188278106946687,-0.0657679544240076,
0.559241512009136));
#28043=CARTESIAN_POINT('Ctrl Pts',(0.157356766010237,0.122527211570924,
0.570356224890914));
#28044=CARTESIAN_POINT('Ctrl Pts',(-0.0176169333646449,0.198654758421167,
0.581470937772688));
#28045=CARTESIAN_POINT('Ctrl Pts',(-0.176463199112271,0.0929236715999202,
0.592585650654466));
#28046=CARTESIAN_POINT('Ctrl Pts',(-0.173766109246834,-0.0978744535707046,
0.60370036353624));
#28047=CARTESIAN_POINT('Ctrl Pts',(-0.0119947165195289,-0.199073343670525,
0.614815076418018));
#28048=CARTESIAN_POINT('Ctrl Pts',(0.160757247601359,-0.118030405947714,
0.625929789299793));
#28049=CARTESIAN_POINT('Ctrl Pts',(0.186343880099073,0.0710635471544257,
0.63704450218157));
#28050=CARTESIAN_POINT('Ctrl Pts',(0.0413418808560108,0.195102327694556,
0.648159215063346));
#28051=CARTESIAN_POINT('Ctrl Pts',(-0.141506571327,0.14053454968734,0.659273927945122));
#28052=CARTESIAN_POINT('Ctrl Pts',(-0.19481273657165,-0.0426856773872861,
0.670388640826899));
#28053=CARTESIAN_POINT('Ctrl Pts',(-0.0697774496593251,-0.186829272073696,
0.681503353708673));
#28054=CARTESIAN_POINT('Ctrl Pts',(0.119135650988641,-0.15993988260612,
0.692618066590452));
#28055=CARTESIAN_POINT('Ctrl Pts',(0.198985938933051,0.0133665811439721,
0.703732779472226));
#28056=CARTESIAN_POINT('Ctrl Pts',(0.0966744137811841,0.174436599097239,
0.714847492354004));
#28057=CARTESIAN_POINT('Ctrl Pts',(-0.0941377692002065,0.175818513799189,
0.725962205235778));
#28058=CARTESIAN_POINT('Ctrl Pts',(-0.198771467358517,0.0162472504962885,
0.737076918117557));
#28059=CARTESIAN_POINT('Ctrl Pts',(-0.121439690569283,-0.158197569320718,
0.748191630999331));
#28060=CARTESIAN_POINT('Ctrl Pts',(0.0670641335242294,-0.18782031673701,
0.759306343881108));
#28061=CARTESIAN_POINT('Ctrl Pts',(0.194174050982888,-0.0455028274884275,
0.770421056762883));
#28062=CARTESIAN_POINT('Ctrl Pts',(0.143527201441076,0.138470256123977,
0.781535769644661));
#28063=CARTESIAN_POINT('Ctrl Pts',(-0.0385117222509501,0.195680649615163,
0.792650482526435));
#28064=CARTESIAN_POINT('Ctrl Pts',(-0.185295063622389,0.073755059363555,
0.803765195408213));
#28065=CARTESIAN_POINT('Ctrl Pts',(-0.162449913009773,-0.115689650131998,
0.814879908289988));
#28066=CARTESIAN_POINT('Ctrl Pts',(0.00911012092507392,-0.19922619075131,
0.825994621171765));
#28067=CARTESIAN_POINT('Ctrl Pts',(0.172330288464656,-0.100380979583959,
0.837109334053541));
#28068=CARTESIAN_POINT('Ctrl Pts',(0.177790576253697,0.090358067597337,
0.848224046935317));
#28069=CARTESIAN_POINT('Ctrl Pts',(0.0204923601230103,0.198378760357896,
0.859338759817094));
#28070=CARTESIAN_POINT('Ctrl Pts',(-0.155565601016018,0.124793482061652,
0.870453472698869));
#28071=CARTESIAN_POINT('Ctrl Pts',(-0.189210926928472,-0.0630340742409649,
0.881568185580646));
#28072=CARTESIAN_POINT('Ctrl Pts',(-0.0496429811307334,-0.19315704441982,
0.892682898462421));
#28073=CARTESIAN_POINT('Ctrl Pts',(0.13537066549776,-0.146454266947876,
0.903797611344198));
#28074=CARTESIAN_POINT('Ctrl Pts',(0.196459144351367,0.0343201687827305,
0.914912324225975));
#28075=CARTESIAN_POINT('Ctrl Pts',(0.077698965926587,0.183676182665271,
0.92602703710775));
#28076=CARTESIAN_POINT('Ctrl Pts',(-0.112190783686916,0.164885710236704,
0.937141749989527));
#28077=CARTESIAN_POINT('Ctrl Pts',(-0.199375404090374,-0.0048494977417013,
0.948256462871302));
#28078=CARTESIAN_POINT('Ctrl Pts',(-0.104041675254465,-0.170145229715061,
0.959371175753079));
#28079=CARTESIAN_POINT('Ctrl Pts',(0.0865370759360344,-0.179681395455923,
0.970485888634854));
#28080=CARTESIAN_POINT('Ctrl Pts',(0.197895402120212,-0.0247281055527204,
0.981600601516632));
#28081=CARTESIAN_POINT('Ctrl Pts',(0.128090247874932,0.152862545392537,
0.992715314398406));
#28082=CARTESIAN_POINT('Ctrl Pts',(-0.0589752108821156,0.190515075219671,
1.00383002728019));
#28083=CARTESIAN_POINT('Ctrl Pts',(-0.192051772737075,0.0537604498966828,
1.01494474016196));
#28084=CARTESIAN_POINT('Ctrl Pts',(-0.149314408654731,-0.132209215838514,
1.02605945304374));
#28085=CARTESIAN_POINT('Ctrl Pts',(0.0301129323565648,-0.197147865039,1.03717416592551));
#28086=CARTESIAN_POINT('Ctrl Pts',(0.181973368966827,-0.0816073671393096,
1.04828887880729));
#28087=CARTESIAN_POINT('Ctrl Pts',(0.167246161224046,0.108640650496798,
1.05940359168907));
#28088=CARTESIAN_POINT('Ctrl Pts',(-0.000586658529918816,0.199433510765659,
1.07051830457085));
#28089=CARTESIAN_POINT('Ctrl Pts',(-0.167882421333772,0.107654827999754,
1.08163301745262));
#28090=CARTESIAN_POINT('Ctrl Pts',(-0.181490107376369,-0.0826765402581706,
1.0927477303344));
#28091=CARTESIAN_POINT('Ctrl Pts',(-0.028952551217501,-0.197321613521035,
1.10386244321617));
#28092=CARTESIAN_POINT('Ctrl Pts',(0.150089637639646,-0.131328481517706,
1.11497715609795));
#28093=CARTESIAN_POINT('Ctrl Pts',(0.191732165666487,0.0548893981874959,
1.12609186897972));
#28094=CARTESIAN_POINT('Ctrl Pts',(0.0578533522661112,0.19085874100004,
1.1372065818615));
#28095=CARTESIAN_POINT('Ctrl Pts',(-0.128987351803526,0.152106319590148,
1.14832129474328));
#28096=CARTESIAN_POINT('Ctrl Pts',(-0.197746496959982,-0.0258919355128762,
1.15943600762505));
#28097=CARTESIAN_POINT('Ctrl Pts',(-0.0854784770171591,-0.180187400645477,
1.17055072050683));
#28098=CARTESIAN_POINT('Ctrl Pts',(0.105040872831909,-0.16953018733918,
1.18166543338861));
#28099=CARTESIAN_POINT('Ctrl Pts',(0.199400484224714,-0.00367644876158102,
1.19278014627038));
#28100=CARTESIAN_POINT('Ctrl Pts',(0.111218786752117,0.1655428973346,1.20389485915216));
#28101=CARTESIAN_POINT('Ctrl Pts',(-0.0787782246756555,0.18321588550532,
1.21500957203393));
#28102=CARTESIAN_POINT('Ctrl Pts',(-0.196657656759033,0.033163766712988,
1.22612428491571));
#28103=CARTESIAN_POINT('Ctrl Pts',(-0.134506703245444,-0.147248144866374,
1.23723899779749));
#28104=CARTESIAN_POINT('Ctrl Pts',(0.0507785032116992,-0.192861642106786,
1.24835371067926));
#28105=CARTESIAN_POINT('Ctrl Pts',(0.18957849437697,-0.0619198179447247,
1.25946842356104));
#28106=CARTESIAN_POINT('Ctrl Pts',(0.154828723961395,0.125706545657069,
1.27058313644281));
#28107=CARTESIAN_POINT('Ctrl Pts',(-0.0216591070800636,0.198254766563231,
1.28169784932459));
#28108=CARTESIAN_POINT('Ctrl Pts',(-0.17831909381802,0.0893105266162228,
1.29281256220637));
#28109=CARTESIAN_POINT('Ctrl Pts',(-0.171736744872623,-0.101393095648087,
1.30392727508814));
#28110=CARTESIAN_POINT('Ctrl Pts',(-0.00793787606159387,-0.199276339559359,
1.31504198796992));
#28111=CARTESIAN_POINT('Ctrl Pts',(0.163127726787361,-0.114731922923546,
1.3261567008517));
#28112=CARTESIAN_POINT('Ctrl Pts',(0.184857941230518,0.0748439105643279,
1.33727141373347));
#28113=CARTESIAN_POINT('Ctrl Pts',(0.0373598276804767,0.195903835236148,
1.34838612661525));
#28114=CARTESIAN_POINT('Ctrl Pts',(-0.144339365522383,0.137623460736688,
1.35950083949703));
#28115=CARTESIAN_POINT('Ctrl Pts',(-0.193902988414568,-0.0466444044709194,
1.3706155523788));
#28116=CARTESIAN_POINT('Ctrl Pts',(-0.0659579887187589,-0.188211617889871,
1.38173026526058));
#28117=CARTESIAN_POINT('Ctrl Pts',(0.122368296597616,-0.157480377737496,
1.39284497814235));
#28118=CARTESIAN_POINT('Ctrl Pts',(0.19867244158967,0.017416381293079,1.40395969102413));
#28119=CARTESIAN_POINT('Ctrl Pts',(0.0931017648416045,0.176369302226678,
1.41507440390591));
#28120=CARTESIAN_POINT('Ctrl Pts',(-0.0976989858350325,0.173864825514976,
1.42618911678768));
#28121=CARTESIAN_POINT('Ctrl Pts',(-0.199061133498795,0.0121956760666124,
1.43730382966946));
#28122=CARTESIAN_POINT('Ctrl Pts',(-0.118192631149939,-0.160638013329352,
1.44841854255123));
#28123=CARTESIAN_POINT('Ctrl Pts',(0.0708753957499276,-0.186415524197525,
1.45953325543301));
#28124=CARTESIAN_POINT('Ctrl Pts',(0.195060493418966,-0.041538816686279,
1.47064796831478));
#28125=CARTESIAN_POINT('Ctrl Pts',(0.140677329756692,0.141364628804641,
1.48176268119656));
#28126=CARTESIAN_POINT('Ctrl Pts',(-0.0424889910845633,0.194855728735808,
1.49287739407834));
#28127=CARTESIAN_POINT('Ctrl Pts',(-0.186758736147166,0.0699660193040883,
1.50399210696011));
#28128=CARTESIAN_POINT('Ctrl Pts',(-0.160060069217685,-0.118974130072788,
1.51510681984189));
#28129=CARTESIAN_POINT('Ctrl Pts',(0.0131656969095905,-0.198999331178352,
1.52622153272367));
#28130=CARTESIAN_POINT('Ctrl Pts',(0.174338916848997,-0.0968504592475705,
1.53733624560544));
#28131=CARTESIAN_POINT('Ctrl Pts',(0.175913456817656,0.0939602314546404,
1.54845095848722));
#28132=CARTESIAN_POINT('Ctrl Pts',(0.0164479031306532,0.198754964383664,
1.559565671369));
#28133=CARTESIAN_POINT('Ctrl Pts',(-0.158074894661018,0.121599330024695,
1.57068038425077));
#28134=CARTESIAN_POINT('Ctrl Pts',(-0.18788792265261,-0.0668744936865572,
1.58179509713255));
#28135=CARTESIAN_POINT('Ctrl Pts',(-0.0456988240979224,-0.194128016681297,
1.59290981001432));
#28136=CARTESIAN_POINT('Ctrl Pts',(0.138325294050016,-0.143666914808259,
1.6040245228961));
#28137=CARTESIAN_POINT('Ctrl Pts',(0.195719427705911,0.0383141619119788,
1.61513923577788));
#28138=CARTESIAN_POINT('Ctrl Pts',(0.0739420781894689,0.185220513058271,
1.62625394865965));
#28139=CARTESIAN_POINT('Ctrl Pts',(-0.115525597082264,0.162566619585121,
1.63736866154143));
#28140=CARTESIAN_POINT('Ctrl Pts',(-0.199235285953682,-0.00890899632401715,
1.6484833744232));
#28141=CARTESIAN_POINT('Ctrl Pts',(-0.100554896829241,-0.172228865490681,
1.65959808730498));
#28142=CARTESIAN_POINT('Ctrl Pts',(0.0901785409695924,-0.177881702637294,
1.67071280018676));
#28143=CARTESIAN_POINT('Ctrl Pts',(0.198357972121127,-0.0206926141543518,
1.68182751306853));
#28144=CARTESIAN_POINT('Ctrl Pts',(0.124950462821344,0.155439542026084,
1.69294222595031));
#28145=CARTESIAN_POINT('Ctrl Pts',(-0.062843032628011,0.189274463767994,
1.70405693883209));
#28146=CARTESIAN_POINT('Ctrl Pts',(-0.193106831128081,0.0498379489567696,
1.71517165171386));
#28147=CARTESIAN_POINT('Ctrl Pts',(-0.146590849769418,-0.135222750114125,
1.72628636459564));
#28148=CARTESIAN_POINT('Ctrl Pts',(0.0341218246847609,-0.196493690648655,
1.73740107747742));
#28149=CARTESIAN_POINT('Ctrl Pts',(0.183597651530221,-0.0778843484734545,
1.74851579035919));
#28150=CARTESIAN_POINT('Ctrl Pts',(0.164998883445552,0.112024273469048,
1.75963050324097));
#28151=CARTESIAN_POINT('Ctrl Pts',(-0.00464822467994746,0.199380198093671,
1.77074521612274));
#28152=CARTESIAN_POINT('Ctrl Pts',(-0.170040112361639,0.104213384805349,
1.78185992900452));
#28153=CARTESIAN_POINT('Ctrl Pts',(-0.179768663563496,-0.0863556424626734,
1.7929746418863));
#28154=CARTESIAN_POINT('Ctrl Pts',(-0.0249278694728741,-0.197870338120928,
1.80408935476807));
#28155=CARTESIAN_POINT('Ctrl Pts',(0.152733159676335,-0.128244498204911,
1.81520406764985));
#28156=CARTESIAN_POINT('Ctrl Pts',(0.190574513949296,0.0587828547923301,
1.82631878053162));
#28157=CARTESIAN_POINT('Ctrl Pts',(0.0539542998466873,0.191997403400672,
1.8374334934134));
#28158=CARTESIAN_POINT('Ctrl Pts',(-0.132058414736671,0.149447798517691,
1.84854820629517));
#28159=CARTESIAN_POINT('Ctrl Pts',(-0.197178163756537,-0.0299138951349875,
1.85966291917695));
#28160=CARTESIAN_POINT('Ctrl Pts',(-0.0817910286946564,-0.181890893146459,
1.87077763205873));
#28161=CARTESIAN_POINT('Ctrl Pts',(0.108471759199364,-0.167355749350723,
1.8818923449405));
#28162=CARTESIAN_POINT('Ctrl Pts',(0.19943400137921,0.000385328981277993,
1.89300705782228));
#28163=CARTESIAN_POINT('Ctrl Pts',(0.107824251391782,0.167773657635365,
1.90412177070405));
#28164=CARTESIAN_POINT('Ctrl Pts',(-0.0824932828470974,0.181573477329856,
1.91523648358584));
#28165=CARTESIAN_POINT('Ctrl Pts',(-0.197292285212489,0.0291517337422745,
1.92635119646761));
#28166=CARTESIAN_POINT('Ctrl Pts',(-0.131479930931687,-0.149956984321324,
1.93746590934939));
#28167=CARTESIAN_POINT('Ctrl Pts',(0.0546958155199975,-0.19178747912507,
1.94858062223116));
#28168=CARTESIAN_POINT('Ctrl Pts',(0.190800240463607,-0.0580459957583295,
1.95969533511294));
#28169=CARTESIAN_POINT('Ctrl Pts',(0.152236455540641,0.128833733893613,
1.97081004799471));
#28170=CARTESIAN_POINT('Ctrl Pts',(-0.0256922961198321,0.19777253425245,
1.98192476087649));
#28171=CARTESIAN_POINT('Ctrl Pts',(-0.18010101782797,0.0856603336549266,
1.99303947375827));
#28172=CARTESIAN_POINT('Ctrl Pts',(-0.169636140306269,-0.104869677631563,
2.00415418664004));
#28173=CARTESIAN_POINT('Ctrl Pts',(-0.00387774279743271,-0.199396671224306,
2.01526889952182));
#28174=CARTESIAN_POINT('Ctrl Pts',(0.165430536991843,-0.111385846565546,
2.02638361240359));
#28175=CARTESIAN_POINT('Ctrl Pts',(0.183295319208086,0.0785932270683423,
2.03749832528537));
#28176=CARTESIAN_POINT('Ctrl Pts',(0.03336227682359,0.19662407754294,2.04861303816715));
#28177=CARTESIAN_POINT('Ctrl Pts',(-0.147112284562752,0.134655282537346,
2.05972775104892));
#28178=CARTESIAN_POINT('Ctrl Pts',(-0.192912805019205,-0.0505837824266837,
2.0708424639307));
#28179=CARTESIAN_POINT('Ctrl Pts',(-0.0621111669469283,-0.189515889371824,
2.08195717681248));
#28180=CARTESIAN_POINT('Ctrl Pts',(0.12555018113299,-0.154955546534564,
2.09307188969425));
#28181=CARTESIAN_POINT('Ctrl Pts',(0.198276530539081,0.021458956746869,
2.10418660257603));
#28182=CARTESIAN_POINT('Ctrl Pts',(0.0894904952228435,0.178228843469243,
2.11530131545781));
#28183=CARTESIAN_POINT('Ctrl Pts',(-0.101219674750872,0.171839014278377,
2.12641602833958));
#28184=CARTESIAN_POINT('Ctrl Pts',(-0.199268224731861,0.00813904257355614,
2.13753074122136));
#28185=CARTESIAN_POINT('Ctrl Pts',(-0.11489654273405,-0.16301182109179,
2.14864545410313));
#28186=CARTESIAN_POINT('Ctrl Pts',(0.0746572571364039,-0.184933402484744,
2.15976016698491));
#28187=CARTESIAN_POINT('Ctrl Pts',(0.195866020763059,-0.0375575744749643,
2.17087487986668));
#28188=CARTESIAN_POINT('Ctrl Pts',(0.137769101429214,0.144200359953505,
2.18198959274846));
#28189=CARTESIAN_POINT('Ctrl Pts',(-0.0464486334400941,0.193949978091433,
2.19310430563024));
#28190=CARTESIAN_POINT('Ctrl Pts',(-0.18814493913174,0.0661479544793682,
2.20421901851201));
#28191=CARTESIAN_POINT('Ctrl Pts',(-0.157603824970919,-0.122209254414689,
2.21533373139379));
#28192=CARTESIAN_POINT('Ctrl Pts',(0.0172158038531715,-0.198689927053832,
2.22644844427557));
#28193=CARTESIAN_POINT('Ctrl Pts',(0.176275240096993,-0.0932797541422112,
2.23756315715734));
#28194=CARTESIAN_POINT('Ctrl Pts',(0.173963337024785,0.0975234012975608,
2.24867787003912));
#28195=CARTESIAN_POINT('Ctrl Pts',(0.0123966756361006,0.199048753252725,
2.2597925829209));
#28196=CARTESIAN_POINT('Ctrl Pts',(-0.16051871512871,0.118354673526729,
2.27090729580267));
#28197=CARTESIAN_POINT('Ctrl Pts',(-0.186486788511679,-0.0706870534597272,
2.28202200868445));
#28198=CARTESIAN_POINT('Ctrl Pts',(-0.0417360712567089,-0.195018686077598,
2.29313672156622));
#28199=CARTESIAN_POINT('Ctrl Pts',(0.141223229087202,-0.140819537071881,
2.304251434448));
#28200=CARTESIAN_POINT('Ctrl Pts',(0.194897215685731,0.0422914446510719,
2.31536614732978));
#28201=CARTESIAN_POINT('Ctrl Pts',(0.0701570032722593,0.18668956375646,
2.32648086021155));
#28202=CARTESIAN_POINT('Ctrl Pts',(-0.118817216374208,0.160177136774138,
2.33759557309333));
#28203=CARTESIAN_POINT('Ctrl Pts',(-0.199003525246202,-0.0129591760037057,
2.3487102859751));
#28204=CARTESIAN_POINT('Ctrl Pts',(-0.097043521379645,-0.174251755453708,
2.35982499885688));
#28205=CARTESIAN_POINT('Ctrl Pts',(0.0938151859874535,-0.175987856857017,
2.37093971173865));
#28206=CARTESIAN_POINT('Ctrl Pts',(0.198676013796531,-0.0166873789156056,
2.38205442462043));
#28207=CARTESIAN_POINT('Ctrl Pts',(0.121879426163471,0.158026820897646,
2.39316913750221));
#28208=CARTESIAN_POINT('Ctrl Pts',(-0.0669327158999945,0.187805554375717,
2.40428385038399));
#28209=CARTESIAN_POINT('Ctrl Pts',(-0.151287880662087,0.0934337713860927,
2.41169365897184));
#28210=CARTESIAN_POINT('Ctrl Pts',(-0.164200416389812,0.0388286878179645,
2.41539856326576));
#28211=CARTESIAN_POINT('Ctrl Pts',(0.0901593640056525,-0.126416002494549,
0.00015634029999317));
#28212=CARTESIAN_POINT('Ctrl Pts',(0.132213650477217,-0.0964246555277346,
0.00386243223197628));
#28213=CARTESIAN_POINT('Ctrl Pts',(0.183298020212533,0.00828926491431173,
0.0112734284578848));
#28214=CARTESIAN_POINT('Ctrl Pts',(0.0922373614706075,0.158809128352571,
0.0223893289777186));
#28215=CARTESIAN_POINT('Ctrl Pts',(-0.0833287157598494,0.163461487822337,
0.0335040418594948));
#28216=CARTESIAN_POINT('Ctrl Pts',(-0.182571295414348,0.0187086709426025,
0.044618754741271));
#28217=CARTESIAN_POINT('Ctrl Pts',(-0.114699979162333,-0.143293650960574,
0.0557334676230472));
#28218=CARTESIAN_POINT('Ctrl Pts',(0.0581846142819802,-0.174053383984867,
0.0668481805048234));
#28219=CARTESIAN_POINT('Ctrl Pts',(0.177798226195109,-0.0455096217415463,
0.0779628933865995));
#28220=CARTESIAN_POINT('Ctrl Pts',(0.134649399343971,0.124713717114316,
0.0890776062683758));
#28221=CARTESIAN_POINT('Ctrl Pts',(-0.0317659246301578,0.180758461746217,
0.100192319150151));
#28222=CARTESIAN_POINT('Ctrl Pts',(-0.169100263415532,0.0713326579444572,
0.111307032031928));
#28223=CARTESIAN_POINT('Ctrl Pts',(-0.151632096793471,-0.10339725624643,
0.122421744913704));
#28224=CARTESIAN_POINT('Ctrl Pts',(0.0046480102430308,-0.183470725562448,
0.13353645779548));
#28225=CARTESIAN_POINT('Ctrl Pts',(0.156672969974193,-0.0955865074097566,
0.144651170677256));
#28226=CARTESIAN_POINT('Ctrl Pts',(0.165271617559767,0.0798028187524376,
0.155765883559033));
#28227=CARTESIAN_POINT('Ctrl Pts',(0.0225722164382812,0.182136403197904,
0.166880596440809));
#28228=CARTESIAN_POINT('Ctrl Pts',(-0.140790917677612,0.117733197065986,
0.177995309322585));
#28229=CARTESIAN_POINT('Ctrl Pts',(-0.175266919880487,-0.0544489988186458,
0.189110022204361));
#28230=CARTESIAN_POINT('Ctrl Pts',(-0.0492946961622294,-0.176785793091077,
0.200224735086137));
#28231=CARTESIAN_POINT('Ctrl Pts',(0.121804388076487,-0.137283927918741,
0.211339447967913));
#28232=CARTESIAN_POINT('Ctrl Pts',(0.181397563796251,0.0278946103217992,
0.22245416084969));
#28233=CARTESIAN_POINT('Ctrl Pts',(0.0749302156796734,0.167537004418727,
0.233568873731466));
#28234=CARTESIAN_POINT('Ctrl Pts',(-0.100132048951932,0.153807536089727,
0.244683586613242));
#28235=CARTESIAN_POINT('Ctrl Pts',(-0.183528361484412,-0.000725146882597591,
0.255798299495018));
#28236=CARTESIAN_POINT('Ctrl Pts',(-0.0989135106019816,-0.154593993044227,
0.266913012376794));
#28237=CARTESIAN_POINT('Ctrl Pts',(0.0762517807621952,-0.166939663475187,
0.27802772525857));
#28238=CARTESIAN_POINT('Ctrl Pts',(0.181612327609234,-0.0264603053006625,
0.289142438140347));
#28239=CARTESIAN_POINT('Ctrl Pts',(0.120715745644371,0.138242157265243,
0.300257151022123));
#28240=CARTESIAN_POINT('Ctrl Pts',(-0.0506901477430488,0.176390743011373,
0.311371863903899));
#28241=CARTESIAN_POINT('Ctrl Pts',(-0.175691710916637,0.053062303107031,
0.322486576785675));
#28242=CARTESIAN_POINT('Ctrl Pts',(-0.139856177868226,-0.118842058243485,
0.333601289667452));
#28243=CARTESIAN_POINT('Ctrl Pts',(0.0240107883033711,-0.181952376575327,
0.344716002549227));
#28244=CARTESIAN_POINT('Ctrl Pts',(0.165897061997177,-0.0784942680496771,
0.355830715431004));
#28245=CARTESIAN_POINT('Ctrl Pts',(0.155912757484034,0.0968214715321897,
0.366945428312779));
#28246=CARTESIAN_POINT('Ctrl Pts',(0.00319801311979034,0.183501929167357,
0.378060141194556));
#28247=CARTESIAN_POINT('Ctrl Pts',(-0.152444354529535,0.102195420974054,
0.389174854076332));
#28248=CARTESIAN_POINT('Ctrl Pts',(-0.168531434170574,-0.0726659548372124,
0.400289566958108));
#28249=CARTESIAN_POINT('Ctrl Pts',(-0.0303362978076353,-0.18100523288385,
0.411404279839885));
#28250=CARTESIAN_POINT('Ctrl Pts',(0.13563022301041,-0.123643147412814,
0.422518992721661));
#28251=CARTESIAN_POINT('Ctrl Pts',(0.17743396395212,0.0469081414281092,
0.433633705603437));
#28252=CARTESIAN_POINT('Ctrl Pts',(0.0568056619480616,0.17451734030361,
0.444748418485213));
#28253=CARTESIAN_POINT('Ctrl Pts',(-0.115825421911227,0.142364521335509,
0.455863131366989));
#28254=CARTESIAN_POINT('Ctrl Pts',(-0.18242404452666,-0.020115995489598,
0.466977844248765));
#28255=CARTESIAN_POINT('Ctrl Pts',(-0.0820224515413663,-0.164181310565931,
0.478092557130542));
#28256=CARTESIAN_POINT('Ctrl Pts',(0.0934666504784431,-0.157946733249989,
0.489207270012318));
#28257=CARTESIAN_POINT('Ctrl Pts',(0.183391643765334,-0.00711971158483698,
0.500321982894094));
#28258=CARTESIAN_POINT('Ctrl Pts',(0.105430632070536,0.150225054891685,
0.51143669577587));
#28259=CARTESIAN_POINT('Ctrl Pts',(-0.0690469234405426,0.170046192722443,
0.522551408657646));
#28260=CARTESIAN_POINT('Ctrl Pts',(-0.180315425939685,0.0341984278029353,
0.533666121539423));
#28261=CARTESIAN_POINT('Ctrl Pts',(-0.126514049157296,-0.132956311101909,
0.544780834421199));
#28262=CARTESIAN_POINT('Ctrl Pts',(0.0431046999490668,-0.178396104605183,
0.555895547302975));
#28263=CARTESIAN_POINT('Ctrl Pts',(0.173263222178117,-0.060523062847634,
0.567010260184751));
#28264=CARTESIAN_POINT('Ctrl Pts',(0.144807809854295,0.112755857946294,
0.578124973066527));
#28265=CARTESIAN_POINT('Ctrl Pts',(-0.0162120104623694,0.182812351915209,
0.589239685948304));
#28266=CARTESIAN_POINT('Ctrl Pts',(-0.16239053477794,0.0855131540205209,
0.600354398830079));
#28267=CARTESIAN_POINT('Ctrl Pts',(-0.159908533613985,-0.0900691188667203,
0.611469111711856));
#28268=CARTESIAN_POINT('Ctrl Pts',(-0.0110381566236799,-0.183197555645139,
0.622583824593632));
#28269=CARTESIAN_POINT('Ctrl Pts',(0.147937108353142,-0.108617665543471,
0.633698537475408));
#28270=CARTESIAN_POINT('Ctrl Pts',(0.171483246898593,0.0653963403342919,
0.644813250357184));
#28271=CARTESIAN_POINT('Ctrl Pts',(0.0380449304711,0.179543221986939,0.65592796323896));
#28272=CARTESIAN_POINT('Ctrl Pts',(-0.130221643424722,0.129327138991656,
0.667042676120737));
#28273=CARTESIAN_POINT('Ctrl Pts',(-0.179276725303484,-0.039281561329222,
0.678157389002513));
#28274=CARTESIAN_POINT('Ctrl Pts',(-0.0642128071043873,-0.171929929621858,
0.689272101884288));
#28275=CARTESIAN_POINT('Ctrl Pts',(0.109634769019767,-0.147184926938816,
0.700386814766066));
#28276=CARTESIAN_POINT('Ctrl Pts',(0.183117121298874,0.0123006171884068,
0.711501527647841));
#28277=CARTESIAN_POINT('Ctrl Pts',(0.0889647803748755,0.160525552946727,
0.722616240529618));
#28278=CARTESIAN_POINT('Ctrl Pts',(-0.0866304292346941,0.161797262110999,
0.733730953411393));
#28279=CARTESIAN_POINT('Ctrl Pts',(-0.182919753497209,0.014951557662091,
0.74484566629317));
#28280=CARTESIAN_POINT('Ctrl Pts',(-0.11175506504485,-0.145581560414854,
0.755960379174946));
#28281=CARTESIAN_POINT('Ctrl Pts',(0.0617158736904078,-0.172841940022184,
0.767075092056721));
#28282=CARTESIAN_POINT('Ctrl Pts',(0.178688973892221,-0.0418740481127377,
0.778189804938499));
#28283=CARTESIAN_POINT('Ctrl Pts',(0.132081131445255,0.127427469613673,
0.789304517820274));
#28284=CARTESIAN_POINT('Ctrl Pts',(-0.0354404725915213,0.180075423638242,
0.800419230702051));
#28285=CARTESIAN_POINT('Ctrl Pts',(-0.170518071896724,0.0678732086513234,
0.811533943583826));
#28286=CARTESIAN_POINT('Ctrl Pts',(-0.149494786340711,-0.106463581345676,
0.822648656465604));
#28287=CARTESIAN_POINT('Ctrl Pts',(0.00838360301953096,-0.183338213410116,
0.833763369347378));
#28288=CARTESIAN_POINT('Ctrl Pts',(0.158587217295133,-0.0923757533478818,
0.844878082229157));
#28289=CARTESIAN_POINT('Ctrl Pts',(0.163612055666903,0.0831521529273459,
0.85599279511093));
#28290=CARTESIAN_POINT('Ctrl Pts',(0.0188581264307767,0.182558364266125,
0.867107507992709));
#28291=CARTESIAN_POINT('Ctrl Pts',(-0.143159487468943,0.114841396907353,
0.878222220874483));
#28292=CARTESIAN_POINT('Ctrl Pts',(-0.174121651224263,-0.0580072053363914,
0.88933693375626));
#28293=CARTESIAN_POINT('Ctrl Pts',(-0.0456840309727285,-0.177753072013075,
0.900451646638036));
#28294=CARTESIAN_POINT('Ctrl Pts',(0.124575066495539,-0.134774768052608,
0.911566359519812));
#28295=CARTESIAN_POINT('Ctrl Pts',(0.180791834635944,0.0315831889614004,
0.922681072401588));
#28296=CARTESIAN_POINT('Ctrl Pts',(0.071502594829897,0.169028294165782,
0.933795785283364));
#28297=CARTESIAN_POINT('Ctrl Pts',(-0.103243744031201,0.15173633254571,
0.944910498165141));
#28298=CARTESIAN_POINT('Ctrl Pts',(-0.183475527218596,-0.00446275787609136,
0.956025211046916));
#28299=CARTESIAN_POINT('Ctrl Pts',(-0.0957445142599781,-0.156576413565783,
0.967139923928694));
#28300=CARTESIAN_POINT('Ctrl Pts',(0.0796358793791929,-0.165352084992918,
0.978254636810468));
#28301=CARTESIAN_POINT('Ctrl Pts',(0.182113553092454,-0.0227560777825268,
0.989369349692247));
#28302=CARTESIAN_POINT('Ctrl Pts',(0.117875250799549,0.140671996306819,
1.00048406257403));
#28303=CARTESIAN_POINT('Ctrl Pts',(-0.0542720299868005,0.175321795727498,
1.0115987754558));
#28304=CARTESIAN_POINT('Ctrl Pts',(-0.176735944019595,0.0494731380397978,
1.02271348833758));
#28305=CARTESIAN_POINT('Ctrl Pts',(-0.137406817928465,-0.121665737505578,
1.03382820121935));
#28306=CARTESIAN_POINT('Ctrl Pts',(0.027711473064719,-0.181425630925142,
1.04494291410113));
#28307=CARTESIAN_POINT('Ctrl Pts',(0.167461277198455,-0.0750993071543572,
1.05605762698291));
#28308=CARTESIAN_POINT('Ctrl Pts',(0.153908541255967,0.0999767284144798,
1.06717233986468));
#28309=CARTESIAN_POINT('Ctrl Pts',(-0.000539873429044207,0.183528999977341,
1.07828705274646));
#28310=CARTESIAN_POINT('Ctrl Pts',(-0.154494060616352,0.0990695237208374,
1.08940176562824));
#28311=CARTESIAN_POINT('Ctrl Pts',(-0.167016554964549,-0.0760832153879955,
1.10051647851001));
#28312=CARTESIAN_POINT('Ctrl Pts',(-0.0266436305079402,-0.181585523237285,
1.11163119139179));
#28313=CARTESIAN_POINT('Ctrl Pts',(0.138120223613435,-0.120855240370358,
1.12274590427356));
#28314=CARTESIAN_POINT('Ctrl Pts',(0.176441825113375,0.0505120544688475,
1.13386061715534));
#28315=CARTESIAN_POINT('Ctrl Pts',(0.053239637842074,0.175638054698995,
1.14497533003712));
#28316=CARTESIAN_POINT('Ctrl Pts',(-0.118700812091919,0.139976078330269,
1.15609004291889));
#28317=CARTESIAN_POINT('Ctrl Pts',(-0.181976522886029,-0.0238270941223055,
1.16720475580067));
#28318=CARTESIAN_POINT('Ctrl Pts',(-0.078661702069618,-0.165817737059439,
1.17831946868244));
#28319=CARTESIAN_POINT('Ctrl Pts',(0.0966640273922626,-0.156010419858132,
1.18943418156422));
#28320=CARTESIAN_POINT('Ctrl Pts',(0.18349860725142,-0.00338325771878211,
1.200548894446));
#28321=CARTESIAN_POINT('Ctrl Pts',(0.102349262332821,0.152341109999664,
1.21166360732777));
#28322=CARTESIAN_POINT('Ctrl Pts',(-0.0724957843804967,0.168604704984941,
1.22277832020955));
#28323=CARTESIAN_POINT('Ctrl Pts',(-0.180974515989352,0.0305190081493839,
1.23389303309133));
#28324=CARTESIAN_POINT('Ctrl Pts',(-0.123780003882562,-0.135505335447854,
1.2450077459731));
#28325=CARTESIAN_POINT('Ctrl Pts',(0.0467289969424402,-0.177481227572822,
1.25612245885488));
#28326=CARTESIAN_POINT('Ctrl Pts',(0.174459905743215,-0.05698180923831,
1.26723717173665));
#28327=CARTESIAN_POINT('Ctrl Pts',(0.142481375207763,0.115681645108059,
1.27835188461843));
#28328=CARTESIAN_POINT('Ctrl Pts',(-0.019931827141509,0.182444258782795,
1.28946659750021));
#28329=CARTESIAN_POINT('Ctrl Pts',(-0.164098424781489,0.082188151702278,
1.30058131038198));
#28330=CARTESIAN_POINT('Ctrl Pts',(-0.158041007876917,-0.0933071547377274,
1.31169602326376));
#28331=CARTESIAN_POINT('Ctrl Pts',(-0.00730484285181677,-0.183384362929101,
1.32281073614554));
#28332=CARTESIAN_POINT('Ctrl Pts',(0.150118545528891,-0.10558223138527,
1.33392544902731));
#28333=CARTESIAN_POINT('Ctrl Pts',(0.170115809332428,0.068875225670596,
1.34504016190909));
#28334=CARTESIAN_POINT('Ctrl Pts',(0.0343804398127517,0.180280810554767,
1.35615487479086));
#28335=CARTESIAN_POINT('Ctrl Pts',(-0.132828526710406,0.126648204835068,
1.36726958767264));
#28336=CARTESIAN_POINT('Ctrl Pts',(-0.178439528140082,-0.0429245861150422,
1.37838430055441));
#28337=CARTESIAN_POINT('Ctrl Pts',(-0.060697942204384,-0.173202035519666,
1.38949901343619));
#28338=CARTESIAN_POINT('Ctrl Pts',(0.112609616193738,-0.144921563739498,
1.40061372631797));
#28339=CARTESIAN_POINT('Ctrl Pts',(0.182828624878661,0.0160274521050675,
1.41172843919975));
#28340=CARTESIAN_POINT('Ctrl Pts',(0.0856770446045232,0.162304126022221,
1.42284315208152));
#28341=CARTESIAN_POINT('Ctrl Pts',(-0.0899076444087289,0.159999377414026,
1.4339578649633));
#28342=CARTESIAN_POINT('Ctrl Pts',(-0.18318631921552,0.0112230899609635,
1.44507257784508));
#28343=CARTESIAN_POINT('Ctrl Pts',(-0.10876695353936,-0.147827382827977,
1.45618729072685));
#28344=CARTESIAN_POINT('Ctrl Pts',(0.0652231937102401,-0.171549177492167,
1.46730200360863));
#28345=CARTESIAN_POINT('Ctrl Pts',(0.179504723929444,-0.038226160976696,
1.4784167164904));
#28346=CARTESIAN_POINT('Ctrl Pts',(0.129458532573627,0.130091020596679,
1.48953142937218));
#28347=CARTESIAN_POINT('Ctrl Pts',(-0.0391005604517399,0.179316288909742,
1.50064614225395));
#28348=CARTESIAN_POINT('Ctrl Pts',(-0.171865018825228,0.0643863386146969,
1.51176085513573));
#28349=CARTESIAN_POINT('Ctrl Pts',(-0.147295528855949,-0.109486129144512,
1.52287556801751));
#28350=CARTESIAN_POINT('Ctrl Pts',(0.0121157531577547,-0.183129445533543,
1.53399028089928));
#28351=CARTESIAN_POINT('Ctrl Pts',(0.160435660705114,-0.0891267864904594,
1.54510499378106));
#28352=CARTESIAN_POINT('Ctrl Pts',(0.16188463357213,0.0864670498468623,
1.55621970666283));
#28353=CARTESIAN_POINT('Ctrl Pts',(0.0151362085624658,0.182904566608809,
1.56733441954461));
#28354=CARTESIAN_POINT('Ctrl Pts',(-0.145468668867536,0.111901973503194,
1.57844913242639));
#28355=CARTESIAN_POINT('Ctrl Pts',(-0.172904154471676,-0.0615413573334011,
1.58956384530816));
#28356=CARTESIAN_POINT('Ctrl Pts',(-0.0420544142989491,-0.178646610754234,
1.60067855818994));
#28357=CARTESIAN_POINT('Ctrl Pts',(0.12729406803855,-0.132209702889763,
1.61179327107171));
#28358=CARTESIAN_POINT('Ctrl Pts',(0.180111109236858,0.0352586673808153,
1.62290798395349));
#28359=CARTESIAN_POINT('Ctrl Pts',(0.0680453130181629,0.17044946662358,
1.63402269683527));
#28360=CARTESIAN_POINT('Ctrl Pts',(-0.106312611270259,0.149602185749077,
1.64513740971704));
#28361=CARTESIAN_POINT('Ctrl Pts',(-0.183346583284314,-0.00819851779107011,
1.65625212259882));
#28362=CARTESIAN_POINT('Ctrl Pts',(-0.0925358009646688,-0.158493882644819,
1.6673668354806));
#28363=CARTESIAN_POINT('Ctrl Pts',(0.0829869432675812,-0.163695914863828,
1.67848154836237));
#28364=CARTESIAN_POINT('Ctrl Pts',(0.182539233858749,-0.0190424105160965,
1.68959626124415));
#28365=CARTESIAN_POINT('Ctrl Pts',(0.114985858696805,0.143043481486438,
1.70071097412593));
#28366=CARTESIAN_POINT('Ctrl Pts',(-0.057831398993491,0.174180121100136,
1.7118256870077));
#28367=CARTESIAN_POINT('Ctrl Pts',(-0.177706863152873,0.0458634504193542,
1.72294039988948));
#28368=CARTESIAN_POINT('Ctrl Pts',(-0.134900458607596,-0.12443894713257,
1.73405511277125));
#28369=CARTESIAN_POINT('Ctrl Pts',(0.0314006624952514,-0.180823625920016,
1.74516982565303));
#28370=CARTESIAN_POINT('Ctrl Pts',(0.168956025766015,-0.0716731934083868,
1.75628453853481));
#28371=CARTESIAN_POINT('Ctrl Pts',(0.151840480368031,0.103090512742967,
1.76739925141658));
#28372=CARTESIAN_POINT('Ctrl Pts',(-0.00427753602644203,0.183479938907623,
1.77851396429836));
#28373=CARTESIAN_POINT('Ctrl Pts',(-0.156479679157009,0.0959025302425444,
1.78962867718014));
#28374=CARTESIAN_POINT('Ctrl Pts',(-0.165432393605304,-0.0794689149417693,
1.80074339006191));
#28375=CARTESIAN_POINT('Ctrl Pts',(-0.0229399108422602,-0.18209048790794,
1.81185810294369));
#28376=CARTESIAN_POINT('Ctrl Pts',(0.140552928899268,-0.118017199906791,
1.82297281582546));
#28377=CARTESIAN_POINT('Ctrl Pts',(0.175376494311331,0.0540950139945414,
1.83408752870724));
#28378=CARTESIAN_POINT('Ctrl Pts',(0.0496515287592585,0.176685910552798,
1.84520224158902));
#28379=CARTESIAN_POINT('Ctrl Pts',(-0.121526962555918,0.137529570158329,
1.85631695447079));
#28380=CARTESIAN_POINT('Ctrl Pts',(-0.181453513367309,-0.0275283087504863,
1.86743166735257));
#28381=CARTESIAN_POINT('Ctrl Pts',(-0.0752683219877107,-0.167385378695861,
1.87854638023434));
#28382=CARTESIAN_POINT('Ctrl Pts',(0.0998213059340555,-0.154009389900818,
1.88966109311612));
#28383=CARTESIAN_POINT('Ctrl Pts',(0.183529451465229,0.000354599597248665,
1.9007758059979));
#28384=CARTESIAN_POINT('Ctrl Pts',(0.0992254358621439,0.154393970652905,
1.91189051887967));
#28385=CARTESIAN_POINT('Ctrl Pts',(-0.075914572469042,0.167093276294544,
1.92300523176145));
#28386=CARTESIAN_POINT('Ctrl Pts',(-0.181558533815509,0.0268269285376663,
1.93411994464322));
#28387=CARTESIAN_POINT('Ctrl Pts',(-0.120994611930274,-0.137998149189926,
1.945234657525));
#28388=CARTESIAN_POINT('Ctrl Pts',(0.0503339097165312,-0.176492727410085,
1.95634937040678));
#28389=CARTESIAN_POINT('Ctrl Pts',(0.175584219488913,-0.0534169183168714,
1.96746408328856));
#28390=CARTESIAN_POINT('Ctrl Pts',(0.140095836142101,0.118559444970232,
1.97857879617033));
#28391=CARTESIAN_POINT('Ctrl Pts',(-0.0236433756588397,0.182000483745117,
1.98969350905211));
#28392=CARTESIAN_POINT('Ctrl Pts',(-0.165738243136619,0.0788290559247478,
2.00080822193388));
#28393=CARTESIAN_POINT('Ctrl Pts',(-0.156107923241689,-0.0965064847415824,
2.01192293481566));
#28394=CARTESIAN_POINT('Ctrl Pts',(-0.00356849886987757,-0.183495098331836,
2.02303764769743));
#28395=CARTESIAN_POINT('Ctrl Pts',(0.152237710218634,-0.102502999387228,
2.03415236057921));
#28396=CARTESIAN_POINT('Ctrl Pts',(0.168677803974058,0.0723255400432333,
2.04526707346099));
#28397=CARTESIAN_POINT('Ctrl Pts',(0.0307016873889171,0.180943614663262,
2.05638178634276));
#28398=CARTESIAN_POINT('Ctrl Pts',(-0.13538030979111,0.123916734208149,
2.06749649922454));
#28399=CARTESIAN_POINT('Ctrl Pts',(-0.177528310322938,-0.0465498048357001,
2.07861121210631));
#28400=CARTESIAN_POINT('Ctrl Pts',(-0.0571578984566474,-0.174402293389383,
2.08972592498809));
#28401=CARTESIAN_POINT('Ctrl Pts',(0.115537750410393,-0.142598083878933,
2.10084063786986));
#28402=CARTESIAN_POINT('Ctrl Pts',(0.182464287115587,0.0197476384845713,
2.11195535075165));
#28403=CARTESIAN_POINT('Ctrl Pts',(0.0823537680937941,0.164015371756973,
2.12307006363342));
#28404=CARTESIAN_POINT('Ctrl Pts',(-0.0931475638860256,0.1581351214574,
2.1341847765152));
#28405=CARTESIAN_POINT('Ctrl Pts',(-0.183376895246413,0.00748996664885357,
2.14529948939697));
#28406=CARTESIAN_POINT('Ctrl Pts',(-0.105733723023171,-0.150011883131391,
2.15641420227875));
#28407=CARTESIAN_POINT('Ctrl Pts',(0.0687034575618276,-0.170185252669568,
2.16752891516052));
#28408=CARTESIAN_POINT('Ctrl Pts',(0.180246011726807,-0.0345624166094378,
2.1786436280423));
#28409=CARTESIAN_POINT('Ctrl Pts',(0.126782230909987,0.132700606618394,
2.18975834092408));
#28410=CARTESIAN_POINT('Ctrl Pts',(-0.0427444275179538,0.178482770463656,
2.20087305380585));
#28411=CARTESIAN_POINT('Ctrl Pts',(-0.173140674288284,0.0608727584924831,
2.21198776668763));
#28412=CARTESIAN_POINT('Ctrl Pts',(-0.14503516624899,-0.112463257376332,
2.2231024795694));
#28413=CARTESIAN_POINT('Ctrl Pts',(0.0158428704025093,-0.182844715904384,
2.23421719245118));
#28414=CARTESIAN_POINT('Ctrl Pts',(0.162217565200369,-0.085840839536587,
2.24533190533296));
#28415=CARTESIAN_POINT('Ctrl Pts',(0.160090032784892,0.0897460624636993,
2.25644661821473));
#28416=CARTESIAN_POINT('Ctrl Pts',(0.0114080601289279,0.183174926274725,
2.26756133109651));
#28417=CARTESIAN_POINT('Ctrl Pts',(-0.147717598472383,0.108916073289857,
2.27867604397829));
#28418=CARTESIAN_POINT('Ctrl Pts',(-0.171614758588647,-0.0650498714233224,
2.28979075686006));
#28419=CARTESIAN_POINT('Ctrl Pts',(-0.0384076848034237,-0.179466250658209,
2.30090546974184));
#28420=CARTESIAN_POINT('Ctrl Pts',(0.129960897285711,-0.129589399077687,
2.31202018262361));
#28421=CARTESIAN_POINT('Ctrl Pts',(0.17935446734025,0.0389187680375732,
2.32313489550539));
#28422=CARTESIAN_POINT('Ctrl Pts',(0.0645620919098956,0.171801362824571,
2.33424960838716));
#28423=CARTESIAN_POINT('Ctrl Pts',(-0.109341729068153,0.14740326045774,
2.34536432126895));
#28424=CARTESIAN_POINT('Ctrl Pts',(-0.183133305131037,-0.0119257019713418,
2.35647903415071));
#28425=CARTESIAN_POINT('Ctrl Pts',(-0.0893044522192385,-0.160355450294875,
2.3675937470325));
#28426=CARTESIAN_POINT('Ctrl Pts',(0.0863335715289918,-0.161953100324632,
2.37870845991427));
#28427=CARTESIAN_POINT('Ctrl Pts',(0.182831912207608,-0.0153565865278459,
2.38982317279605));
#28428=CARTESIAN_POINT('Ctrl Pts',(0.112159732412666,0.145424428911658,
2.40093788567783));
#28429=CARTESIAN_POINT('Ctrl Pts',(-0.0615949364163127,0.172828354936131,
2.4120525985596));
#28430=CARTESIAN_POINT('Ctrl Pts',(-0.139222908627576,0.085982574145982,
2.41946240714745));
#28431=CARTESIAN_POINT('Ctrl Pts',(-0.151105689812057,0.0357321606499603,
2.42316731144138));
#28432=CARTESIAN_POINT('',(0.103380467594096,0.116394573955406,2.40007508722328));
#28433=CARTESIAN_POINT('Ctrl Pts',(0.103461767481305,0.116497970106859,
2.4));
#28434=CARTESIAN_POINT('Ctrl Pts',(0.101062838412543,0.119258880418803,
2.4));
#28435=CARTESIAN_POINT('Ctrl Pts',(0.0985654514169241,0.121922998634949,
2.4));
#28436=CARTESIAN_POINT('Ctrl Pts',(0.095972990647464,0.124483778490481,
2.4));
#28437=CARTESIAN_POINT('Ctrl Pts',(0.0883971619082253,0.131967027553669,
2.4));
#28438=CARTESIAN_POINT('Ctrl Pts',(0.0800129758471178,0.138570016932135,
2.4));
#28439=CARTESIAN_POINT('Ctrl Pts',(0.0710089580556215,0.144290176540958,
2.4));
#28440=CARTESIAN_POINT('Ctrl Pts',(0.0663636114037173,0.147241317343045,
2.4));
#28441=CARTESIAN_POINT('Ctrl Pts',(0.0615524547995155,0.149957058484752,
2.4));
#28442=CARTESIAN_POINT('Ctrl Pts',(0.0565975106583602,0.152433694248754,
2.4));
#28443=CARTESIAN_POINT('Ctrl Pts',(0.0527699197084543,0.154346843694329,
2.4));
#28444=CARTESIAN_POINT('Ctrl Pts',(0.0488630480765027,0.156113602347608,
2.4));
#28445=CARTESIAN_POINT('Ctrl Pts',(0.0449001875407907,0.157728503257228,
2.4));
#28446=CARTESIAN_POINT('Ctrl Pts',(0.035918044860841,0.161388806276592,
2.4));
#28447=CARTESIAN_POINT('Ctrl Pts',(0.0266316597928958,0.164279400994296,
2.4));
#28448=CARTESIAN_POINT('Ctrl Pts',(0.0171631885948985,0.16639083815603,
2.4));
#28449=CARTESIAN_POINT('Ctrl Pts',(0.00998520832101847,0.167991503562255,
2.4));
#28450=CARTESIAN_POINT('Ctrl Pts',(0.00270180372882996,0.169144080993686,
2.4));
#28451=CARTESIAN_POINT('Ctrl Pts',(-0.00463850986789263,0.169835856818611,
2.4));
#28452=CARTESIAN_POINT('Ctrl Pts',(-0.00897136590947692,0.170244199735156,
2.4));
#28453=CARTESIAN_POINT('Ctrl Pts',(-0.0133190494795881,0.170490952148472,
2.4));
#28454=CARTESIAN_POINT('Ctrl Pts',(-0.0176555019082484,0.170574199016548,
2.4));
#28455=CARTESIAN_POINT('Ctrl Pts',(-0.0285870584998179,0.170784052085254,
2.4));
#28456=CARTESIAN_POINT('Ctrl Pts',(-0.039474963002183,0.169960336922977,
2.4));
#28457=CARTESIAN_POINT('Ctrl Pts',(-0.0501623159300887,0.168075457674568,
2.4));
#28458=CARTESIAN_POINT('Ctrl Pts',(-0.0531380387349237,0.167550643138949,
2.4));
#28459=CARTESIAN_POINT('Ctrl Pts',(-0.0560982762643852,0.166943351080139,
2.4));
#28460=CARTESIAN_POINT('Ctrl Pts',(-0.059039724474309,0.1662524758191,2.4));
#28461=CARTESIAN_POINT('Ctrl Pts',(-0.0633625816644486,0.165237140896798,
2.4));
#28462=CARTESIAN_POINT('Ctrl Pts',(-0.0676448709143601,0.164041331557733,
2.4));
#28463=CARTESIAN_POINT('Ctrl Pts',(-0.0718806214018753,0.162672203759917,
2.4));
#28464=CARTESIAN_POINT('Ctrl Pts',(-0.0757157250276606,0.161432577630607,
2.4));
#28465=CARTESIAN_POINT('Ctrl Pts',(-0.0795060665151785,0.160052743939154,
2.4));
#28466=CARTESIAN_POINT('Ctrl Pts',(-0.083238263168423,0.158543149031955,
2.4));
#28467=CARTESIAN_POINT('Ctrl Pts',(-0.0942712060057412,0.154080556123256,
2.4));
#28468=CARTESIAN_POINT('Ctrl Pts',(-0.104821070565539,0.148480110078236,
2.4));
#28469=CARTESIAN_POINT('Ctrl Pts',(-0.114778874551992,0.141898905553672,
2.4));
#28470=CARTESIAN_POINT('Ctrl Pts',(-0.120197102208962,0.13831794890704,
2.4));
#28471=CARTESIAN_POINT('Ctrl Pts',(-0.125439738625044,0.134445884472761,
2.4));
#28472=CARTESIAN_POINT('Ctrl Pts',(-0.130488353457401,0.130301426506045,
2.4));
#28473=CARTESIAN_POINT('Ctrl Pts',(-0.134449742315667,0.127049483119975,
2.4));
#28474=CARTESIAN_POINT('Ctrl Pts',(-0.138288930969708,0.123631215695906,
2.4));
#28475=CARTESIAN_POINT('Ctrl Pts',(-0.141981521250133,0.120071365074424,
2.4));
#28476=CARTESIAN_POINT('Ctrl Pts',(-0.148243719704175,0.11403427745692,
2.4));
#28477=CARTESIAN_POINT('Ctrl Pts',(-0.154096955106979,0.107580854604382,
2.4));
#28478=CARTESIAN_POINT('Ctrl Pts',(-0.159498257185175,0.100759941050575,
2.4));
#28479=CARTESIAN_POINT('Ctrl Pts',(-0.162517575610272,0.0969470622908144,
2.4));
#28480=CARTESIAN_POINT('Ctrl Pts',(-0.165397051519882,0.0930169578682919,
2.4));
#28481=CARTESIAN_POINT('Ctrl Pts',(-0.16812342541814,0.0889841305063993,
2.4));
#28482=CARTESIAN_POINT('Ctrl Pts',(-0.174697816516933,0.0792593512573283,
2.4));
#28483=CARTESIAN_POINT('Ctrl Pts',(-0.180364044921554,0.0689697058721336,
2.4));
#28484=CARTESIAN_POINT('Ctrl Pts',(-0.185015139554039,0.0582282398394182,
2.4));
#28485=CARTESIAN_POINT('Ctrl Pts',(-0.186897941765302,0.0538800040806022,
2.4));
#28486=CARTESIAN_POINT('Ctrl Pts',(-0.188614220377741,0.0494572905282926,
2.4));
#28487=CARTESIAN_POINT('Ctrl Pts',(-0.190155688860645,0.0449663651403318,
2.4));
#28488=CARTESIAN_POINT('Ctrl Pts',(0.104759235283674,0.114983934194216,
2.4));
#28489=CARTESIAN_POINT('Ctrl Pts',(0.10427439309968,0.115425662830347,2.40002502907443));
#28490=CARTESIAN_POINT('Ctrl Pts',(0.103786756983843,0.115864324841204,
2.40005005814885));
#28491=CARTESIAN_POINT('Ctrl Pts',(0.10329636595052,0.11629988513071,2.40007508722328));
#28492=CARTESIAN_POINT('Ctrl Pts',(0.0863566694936598,0.175642871684081,
3.00324001778485E-17));
#28493=CARTESIAN_POINT('Ctrl Pts',(0.0902251377602555,0.173267020623209,
1.02990543755693E-16));
#28494=CARTESIAN_POINT('Ctrl Pts',(0.0939991325874576,0.170750246590702,
-9.76497076806834E-17));
#28495=CARTESIAN_POINT('Ctrl Pts',(0.0976698484646395,0.16809208422283,
-8.68445940160889E-17));
#28496=CARTESIAN_POINT('Ctrl Pts',(0.104400047624094,0.163218385812893,
-6.02536217891983E-17));
#28497=CARTESIAN_POINT('Ctrl Pts',(0.110783523872764,0.157869648682406,
-3.87972721901173E-17));
#28498=CARTESIAN_POINT('Ctrl Pts',(0.11679477944429,0.152098287545979,-3.64291929955129E-17));
#28499=CARTESIAN_POINT('Ctrl Pts',(0.122324543199851,0.146789203070577,
-3.42507931013796E-17));
#28500=CARTESIAN_POINT('Ctrl Pts',(0.127544162554551,0.141115067318068,
-1.26605818491442E-17));
#28501=CARTESIAN_POINT('Ctrl Pts',(0.132400641086032,0.135150809061649,
-8.89045781438114E-17));
#28502=CARTESIAN_POINT('Ctrl Pts',(0.137099361104822,0.129380294585985,
-1.62671854037244E-16));
#28503=CARTESIAN_POINT('Ctrl Pts',(0.141463395349392,0.123334515287111,
-5.10858319320469E-17));
#28504=CARTESIAN_POINT('Ctrl Pts',(0.145472480412238,0.117050620606459,
-9.0205620750794E-17));
#28505=CARTESIAN_POINT('Ctrl Pts',(0.148028749789222,0.113043889073319,
-1.15149146922942E-16));
#28506=CARTESIAN_POINT('Ctrl Pts',(0.150440599606425,0.108940295545949,
-4.4214120273351E-17));
#28507=CARTESIAN_POINT('Ctrl Pts',(0.152701484434877,0.104749210972548,
-9.36750677027476E-17));
#28508=CARTESIAN_POINT('Ctrl Pts',(0.154529352382147,0.101360825567148,
-1.33662987171292E-16));
#28509=CARTESIAN_POINT('Ctrl Pts',(0.156257288991465,0.0979170901241365,
-9.60317181142712E-17));
#28510=CARTESIAN_POINT('Ctrl Pts',(0.157877700765807,0.0944331993150869,
-1.64798730217797E-17));
#28511=CARTESIAN_POINT('Ctrl Pts',(0.163035894966784,0.0833430642934671,
2.36754442187825E-16));
#28512=CARTESIAN_POINT('Ctrl Pts',(0.16712377054151,0.0718185232873831,
4.96472933007523E-18));
#28513=CARTESIAN_POINT('Ctrl Pts',(0.170039561512778,0.0600249603217789,
-7.11236625150491E-17));
#28514=CARTESIAN_POINT('Ctrl Pts',(0.171494712723099,0.0541392786688407,
-1.09096245795481E-16));
#28515=CARTESIAN_POINT('Ctrl Pts',(0.17265715824647,0.0481865085500087,
-8.55724220067749E-17));
#28516=CARTESIAN_POINT('Ctrl Pts',(0.173509220055223,0.0421877481517497,
-2.25514051876985E-17));
#28517=CARTESIAN_POINT('Ctrl Pts',(0.174254193713336,0.036942919159156,
3.25490546091879E-17));
#28518=CARTESIAN_POINT('Ctrl Pts',(0.174761331352098,0.0316591437943461,
-1.13288127970075E-16));
#28519=CARTESIAN_POINT('Ctrl Pts',(0.175017019263399,0.0263849939813338,
-1.31838984174237E-16));
#28520=CARTESIAN_POINT('Ctrl Pts',(0.175312644314683,0.0202870490256223,
-1.53287388945601E-16));
#28521=CARTESIAN_POINT('Ctrl Pts',(0.175274136046595,0.0141923338965255,
-1.87526340687399E-16));
#28522=CARTESIAN_POINT('Ctrl Pts',(0.174886275518905,0.00812263339345144,
-1.05818132034585E-16));
#28523=CARTESIAN_POINT('Ctrl Pts',(0.174375504119754,0.000129478130005221,
-7.9097615780314E-18));
#28524=CARTESIAN_POINT('Ctrl Pts',(0.173259119449215,-0.00782060291629472,
-1.15450484634852E-16));
#28525=CARTESIAN_POINT('Ctrl Pts',(0.171567084712523,-0.0156736935166775,
-7.28583859910259E-17));
#28526=CARTESIAN_POINT('Ctrl Pts',(0.170483272838823,-0.0207038933425822,
-4.55765452374446E-17));
#28527=CARTESIAN_POINT('Ctrl Pts',(0.169162566961701,-0.0256957555113034,
2.18154106348517E-16));
#28528=CARTESIAN_POINT('Ctrl Pts',(0.16761260374838,-0.0306286181104371,
2.77555756156289E-17));
#28529=CARTESIAN_POINT('Ctrl Pts',(0.166323465714418,-0.0347313869621074,
-1.30603013458363E-16));
#28530=CARTESIAN_POINT('Ctrl Pts',(0.164878296492824,-0.0387849189721862,
-7.45107699010496E-17));
#28531=CARTESIAN_POINT('Ctrl Pts',(0.163285258777898,-0.0427743425247604,
-2.77555756156289E-17));
#28532=CARTESIAN_POINT('Ctrl Pts',(0.159781230740532,-0.0515494341940759,
7.50866296464515E-17));
#28533=CARTESIAN_POINT('Ctrl Pts',(0.15555905845194,-0.0600274982283718,
-1.67125813435077E-16));
#28534=CARTESIAN_POINT('Ctrl Pts',(0.150667339924487,-0.068116122664101,
-1.45716771982052E-16));
#28535=CARTESIAN_POINT('Ctrl Pts',(0.146817200022984,-0.0744824611019111,
-1.28866292076344E-16));
#28536=CARTESIAN_POINT('Ctrl Pts',(0.142551803362311,-0.0806074016922841,
-2.96987614464865E-16));
#28537=CARTESIAN_POINT('Ctrl Pts',(0.137888788869483,-0.0864371653375756,
-4.85722573273506E-17));
#28538=CARTESIAN_POINT('Ctrl Pts',(0.135609742264458,-0.0892864601584125,
7.28406563985689E-17));
#28539=CARTESIAN_POINT('Ctrl Pts',(0.133240253652339,-0.0920591324808986,
7.04833804390097E-17));
#28540=CARTESIAN_POINT('Ctrl Pts',(0.130787574864596,-0.0947448381828875,
3.12250225675825E-17));
#28541=CARTESIAN_POINT('Ctrl Pts',(0.125477874028838,-0.100559009154527,
-5.37637401852564E-17));
#28542=CARTESIAN_POINT('Ctrl Pts',(0.119772613931372,-0.105974110081735,
-1.21563507678846E-16));
#28543=CARTESIAN_POINT('Ctrl Pts',(0.113697442368773,-0.110930478022775,
-6.93889390390723E-17));
#28544=CARTESIAN_POINT('Ctrl Pts',(0.10643549160352,-0.116855067903314,
-7.02211618374062E-18));
#28545=CARTESIAN_POINT('Ctrl Pts',(0.0986448235562052,-0.12212533697402,
-1.11878079465019E-16));
#28546=CARTESIAN_POINT('Ctrl Pts',(0.0903606778650216,-0.126612599672285,
-1.73472347597681E-17));
#28547=CARTESIAN_POINT('Origin',(-0.0866025403784439,-0.15,-0.3));
#28548=CARTESIAN_POINT('',(-0.0866025403784439,-0.15,-0.3));
#28549=CARTESIAN_POINT('',(0.0866025403784439,-0.15,-0.3));
#28550=CARTESIAN_POINT('',(-0.043301270189222,-0.15,-0.3));
#28551=CARTESIAN_POINT('',(-0.0866025403784439,-0.15,-0.1));
#28552=CARTESIAN_POINT('',(-0.0866025403784439,-0.15,-0.3));
#28553=CARTESIAN_POINT('',(0.0866025403784439,-0.15,-0.1));
#28554=CARTESIAN_POINT('',(-0.0866025403784439,-0.15,-0.1));
#28555=CARTESIAN_POINT('',(0.0866025403784439,-0.15,-0.3));
#28556=CARTESIAN_POINT('Origin',(-0.173205080756888,2.12115047744981E-17,
-0.3));
#28557=CARTESIAN_POINT('',(-0.173205080756888,2.12115047744981E-17,-0.3));
#28558=CARTESIAN_POINT('',(-0.151554445662277,-0.0375,-0.3));
#28559=CARTESIAN_POINT('',(-0.173205080756888,2.77555756156289E-17,-0.1));
#28560=CARTESIAN_POINT('',(-0.173205080756888,2.12115047744981E-17,-0.3));
#28561=CARTESIAN_POINT('',(-0.173205080756888,2.12115047744981E-17,-0.1));
#28562=CARTESIAN_POINT('Origin',(-0.0866025403784438,0.15,-0.3));
#28563=CARTESIAN_POINT('',(-0.0866025403784438,0.15,-0.3));
#28564=CARTESIAN_POINT('',(-0.108253175473055,0.1125,-0.3));
#28565=CARTESIAN_POINT('',(-0.0866025403784438,0.15,-0.1));
#28566=CARTESIAN_POINT('',(-0.0866025403784438,0.15,-0.3));
#28567=CARTESIAN_POINT('',(-0.0866025403784438,0.15,-0.1));
#28568=CARTESIAN_POINT('Origin',(0.0866025403784439,0.15,-0.3));
#28569=CARTESIAN_POINT('',(0.0866025403784439,0.15,-0.3));
#28570=CARTESIAN_POINT('',(0.043301270189222,0.15,-0.3));
#28571=CARTESIAN_POINT('',(0.0866025403784439,0.15,-0.1));
#28572=CARTESIAN_POINT('',(0.0866025403784439,0.15,-0.3));
#28573=CARTESIAN_POINT('',(0.0866025403784439,0.15,-0.1));
#28574=CARTESIAN_POINT('Origin',(0.173205080756888,0.,-0.3));
#28575=CARTESIAN_POINT('',(0.173205080756888,0.,-0.3));
#28576=CARTESIAN_POINT('',(0.151554445662277,0.0375,-0.3));
#28577=CARTESIAN_POINT('',(0.173205080756888,0.,-0.1));
#28578=CARTESIAN_POINT('',(0.173205080756888,0.,-0.3));
#28579=CARTESIAN_POINT('',(0.173205080756888,0.,-0.1));
#28580=CARTESIAN_POINT('Origin',(0.0866025403784439,-0.15,-0.3));
#28581=CARTESIAN_POINT('',(0.108253175473055,-0.1125,-0.3));
#28582=CARTESIAN_POINT('',(0.0866025403784439,-0.15,-0.1));
#28583=CARTESIAN_POINT('Origin',(0.,2.77555756156289E-17,-0.1));
#28584=CARTESIAN_POINT('Origin',(0.,0.,0.));
#28585=CARTESIAN_POINT('',(-0.4,-4.89858719658941E-17,0.));
#28586=CARTESIAN_POINT('Origin',(0.,0.,0.));
#28587=CARTESIAN_POINT('Origin',(0.,0.,-0.3));
#28588=CARTESIAN_POINT('',(-0.4,-4.89858719658941E-17,-0.3));
#28589=CARTESIAN_POINT('',(-0.4,-4.89858719658941E-17,-0.3));
#28590=CARTESIAN_POINT('Origin',(0.,0.,-0.3));
#28591=CARTESIAN_POINT('Origin',(0.,0.,-0.3));
#28592=CARTESIAN_POINT('Origin',(0.,0.,2.4));
#31543=UNCERTAINTY_MEASURE_WITH_UNIT(LENGTH_MEASURE(0.001),#31567,
'DISTANCE_ACCURACY_VALUE',
'Maximum model space distance between geometric entities at asserted c
onnectivities');
#31549=UNCERTAINTY_MEASURE_WITH_UNIT(LENGTH_MEASURE(0.001),#31567,
'DISTANCE_ACCURACY_VALUE',
'Maximum model space distance between geometric entities at asserted c
onnectivities');
#31560=(
GEOMETRIC_REPRESENTATION_CONTEXT(3)
GLOBAL_UNCERTAINTY_ASSIGNED_CONTEXT((#31543))
GLOBAL_UNIT_ASSIGNED_CONTEXT((#31567,#31569,#31570))
REPRESENTATION_CONTEXT('','3D')
);
#31566=(
GEOMETRIC_REPRESENTATION_CONTEXT(3)
GLOBAL_UNCERTAINTY_ASSIGNED_CONTEXT((#31549))
GLOBAL_UNIT_ASSIGNED_CONTEXT((#31567,#31569,#31570))
REPRESENTATION_CONTEXT('','3D')
);
#31567=(
LENGTH_UNIT()
NAMED_UNIT(*)
SI_UNIT(.CENTI.,.METRE.)
);
#31569=(
NAMED_UNIT(*)
PLANE_ANGLE_UNIT()
SI_UNIT($,.RADIAN.)
);
#31570=(
NAMED_UNIT(*)
SI_UNIT($,.STERADIAN.)
SOLID_ANGLE_UNIT()
);
#31581=SHAPE_DEFINITION_REPRESENTATION(#31597,#31645);
#31597=PRODUCT_DEFINITION_SHAPE('',$,#31662);
#31645=SHAPE_REPRESENTATION('',(#6089),#31560);
#31651=PRODUCT_DEFINITION_CONTEXT('part definition',#31701,'design');
#31662=PRODUCT_DEFINITION('Socket head screw M4x24',
'Socket head screw M4x24',#31678,#31651);
#31678=PRODUCT_DEFINITION_FORMATION('',$,#31713);
#31701=APPLICATION_CONTEXT(
'Core Data for Automotive Mechanical Design Process');
#31702=PRODUCT_CONTEXT('part definition',#31701,'mechanical');
#31713=PRODUCT('Socket head screw M4x24','Socket head screw M4x24',$,(#31702));
#31720=PRESENTATION_STYLE_ASSIGNMENT((#31727));
#31727=SURFACE_STYLE_USAGE(.BOTH.,#31734);
#31734=SURFACE_SIDE_STYLE('',(#31741));
#31741=SURFACE_STYLE_FILL_AREA(#31748);
#31748=FILL_AREA_STYLE('Opaque(155,165,179)',(#31755));
#31755=FILL_AREA_STYLE_COLOUR('Opaque(155,165,179)',#31762);
#31762=COLOUR_RGB('Opaque(155,165,179)',0.607843137254902,0.647058823529412,
0.701960784313725);
ENDSEC;
END-ISO-10303-21;
